ISO-10303-21;
HEADER;
FILE_DESCRIPTION (('STEP AP214'),
    '1' );
FILE_NAME ('2. Support.step',
    '2026-10-09T08:13:37',
    ( '' ),
    ( '' ),
    'SwSTEP 2.0',
    'SolidWorks 2021',
    '' );
FILE_SCHEMA (( 'AUTOMOTIVE_DESIGN' ));
ENDSEC;

DATA;
#2=DIRECTION ( 'NONE',  ( 0.000000000000000000, -1.000000000000000000, 0.000000000000000000 ) ) ;
#4=EDGE_CURVE ( 'NONE', #67546, #44738, #50850, .T. ) ;
#5=TOROIDAL_SURFACE ( 'NONE', #4527, 1.000000000000000000, 0.5000000000000000000 ) ;
#8=( LENGTH_UNIT ( ) NAMED_UNIT ( * ) SI_UNIT ( .MILLI., .METRE. ) );
#12=EDGE_CURVE ( 'NONE', #66900, #26262, #59644, .T. ) ;
#22=ORIENTED_EDGE ( 'NONE', *, *, #11042, .T. ) ;
#24=CARTESIAN_POINT ( 'NONE',  ( -48.00000000000000000, 13.41640786499872284, -7.000000000000000000 ) ) ;
#25=CARTESIAN_POINT ( 'NONE',  ( -71.49999999999998579, 64.07124727947029896, 7.000000000000000000 ) ) ;
#26=EDGE_CURVE ( 'NONE', #13502, #64475, #59831, .T. ) ;
#28=CARTESIAN_POINT ( 'NONE',  ( -5.598654528085806881, 124.7449999999999903, -7.705886871421374629 ) ) ;
#35=EDGE_LOOP ( 'NONE', ( #36552, #43299, #63091, #34996 ) ) ;
#39=DIRECTION ( 'NONE',  ( -0.000000000000000000, 1.000000000000000000, -0.000000000000000000 ) ) ;
#42=CARTESIAN_POINT ( 'NONE',  ( 47.50000000000000000, 1.797044900979284448E-15, -9.500000000000000000 ) ) ;
#46=ADVANCED_FACE ( 'NONE', ( #69199 ), #64244, .F. ) ;
#48=FACE_OUTER_BOUND ( 'NONE', #30012, .T. ) ;
#50=VECTOR ( 'NONE', #19293, 1000.000000000000000 ) ;
#56=FILL_AREA_STYLE ('',( #48034 ) ) ;
#57=CIRCLE ( 'NONE', #46222, 13.49999999999999822 ) ;
#58=( NAMED_UNIT ( * ) SI_UNIT ( $, .STERADIAN. ) SOLID_ANGLE_UNIT ( ) );
#59=VECTOR ( 'NONE', #65967, 1000.000000000000000 ) ;
#60=DIRECTION ( 'NONE',  ( 0.000000000000000000, 0.000000000000000000, 1.000000000000000000 ) ) ;
#61=CARTESIAN_POINT ( 'NONE',  ( 2.607480562269071989, 140.7070736234661581, 8.025000000000002132 ) ) ;
#66=VECTOR ( 'NONE', #60751, 1000.000000000000000 ) ;
#69=( NAMED_UNIT ( * ) SI_UNIT ( $, .STERADIAN. ) SOLID_ANGLE_UNIT ( ) );
#73=FACE_OUTER_BOUND ( 'NONE', #54146, .T. ) ;
#74=ORIENTED_EDGE ( 'NONE', *, *, #39587, .T. ) ;
#79=SURFACE_STYLE_FILL_AREA ( #11398 ) ;
#80=LINE ( 'NONE', #20219, #38004 ) ;
#82=ORIENTED_EDGE ( 'NONE', *, *, #21496, .T. ) ;
#86=( LENGTH_UNIT ( ) NAMED_UNIT ( * ) SI_UNIT ( .MILLI., .METRE. ) );
#89=ORIENTED_EDGE ( 'NONE', *, *, #8280, .T. ) ;
#93=CARTESIAN_POINT ( 'NONE',  ( 71.50000000000000000, 14.49137674618942562, -7.000000000000000000 ) ) ;
#97=CARTESIAN_POINT ( 'NONE',  ( 3.094860106618431583, 126.0949999999999847, 9.525000000000000355 ) ) ;
#101=EDGE_CURVE ( 'NONE', #11552, #53103, #65288, .T. ) ;
#103=CARTESIAN_POINT ( 'NONE',  ( 0.000000000000000000, 154.4258142642185305, -9.450814264218562855 ) ) ;
#104=ORIENTED_EDGE ( 'NONE', *, *, #55820, .T. ) ;
#105=CARTESIAN_POINT ( 'NONE',  ( 15.98999599679679839, 118.4999999999999716, -9.500000000000000000 ) ) ;
#106=SURFACE_STYLE_USAGE ( .BOTH. , #32519 ) ;
#107=STYLED_ITEM ( 'NONE', ( #51157 ), #11664 ) ;
#111=COLOUR_RGB ( '', 0.31764706, 0.68627451, 0.89019608) ;
#115=ORIENTED_EDGE ( 'NONE', *, *, #22584, .F. ) ;
#116=AXIS2_PLACEMENT_3D ( 'NONE', #7910, #46285, #57492 ) ;
#117=CARTESIAN_POINT ( 'NONE',  ( 44.47787316461994322, 9.825957721539964496, -3.000913084730224334 ) ) ;
#118=LINE ( 'NONE', #36494, #27806 ) ;
#122=CARTESIAN_POINT ( 'NONE',  ( -74.50000000000000000, 7.768687147774684831, 6.500000000000000000 ) ) ;
#123=CIRCLE ( 'NONE', #49622, 13.99999999999999822 ) ;
#126=CARTESIAN_POINT ( 'NONE',  ( 3.094860106618435136, 161.4050000000000296, -9.525000000000000355 ) ) ;
#128=AXIS2_PLACEMENT_3D ( 'NONE', #2627, #68021, #19809 ) ;
#140=( NAMED_UNIT ( * ) PLANE_ANGLE_UNIT ( ) SI_UNIT ( $, .RADIAN. ) );
#143=CARTESIAN_POINT ( 'NONE',  ( -8.437984349512095861, 109.8070736234661666, -5.166775262442723748E-16 ) ) ;
#146=CARTESIAN_POINT ( 'NONE',  ( 75.00000000000000000, 19.97932849626359442, -6.162720495828226674 ) ) ;
#148=FILL_AREA_STYLE ('',( #5466 ) ) ;
#150=ORIENTED_EDGE ( 'NONE', *, *, #13034, .F. ) ;
#155=CARTESIAN_POINT ( 'NONE',  ( -9.058813317711338797, 132.4549999999999841, 2.943386871421373563 ) ) ;
#159=LINE ( 'NONE', #54035, #22728 ) ;
#163=( GEOMETRIC_REPRESENTATION_CONTEXT ( 3 ) GLOBAL_UNCERTAINTY_ASSIGNED_CONTEXT ( ( #7392 ) ) GLOBAL_UNIT_ASSIGNED_CONTEXT ( ( #22652, #18065, #24030 ) ) REPRESENTATION_CONTEXT ( 'NONE', 'WORKASPACE' ) );
#165=CARTESIAN_POINT ( 'NONE',  ( -60.00000000000000000, -2.024042244987997205E-14, -11.50000000000000000 ) ) ;
#168=SURFACE_STYLE_FILL_AREA ( #63900 ) ;
#169=EDGE_CURVE ( 'NONE', #40912, #47500, #6890, .T. ) ;
#170=( LENGTH_UNIT ( ) NAMED_UNIT ( * ) SI_UNIT ( .MILLI., .METRE. ) );
#172=FACE_OUTER_BOUND ( 'NONE', #8225, .T. ) ;
#176=CARTESIAN_POINT ( 'NONE',  ( 20.03861782943699765, 115.4999999895429994, -10.00000000000000000 ) ) ;
#185=DIRECTION ( 'NONE',  ( -1.000000000000000000, 0.000000000000000000, 0.000000000000000000 ) ) ;
#186=EDGE_CURVE ( 'NONE', #21243, #60834, #11121, .T. ) ;
#188=CARTESIAN_POINT ( 'NONE',  ( -9.827790563157511022E-16, 121.4429263765338050, 8.025000000000000355 ) ) ;
#189=CARTESIAN_POINT ( 'NONE',  ( -2.652578976365682184, 154.0340937016761984, 8.678865135533699871 ) ) ;
#190=ORIENTED_EDGE ( 'NONE', *, *, #17439, .F. ) ;
#194=FACE_BOUND ( 'NONE', #69314, .T. ) ;
#195=DIRECTION ( 'NONE',  ( 1.000000000000000000, 0.000000000000000000, 0.000000000000000000 ) ) ;
#197=VERTEX_POINT ( 'NONE', #32571 ) ;
#198=SURFACE_SIDE_STYLE ('',( #59328 ) ) ;
#205=FILL_AREA_STYLE_COLOUR ( '', #39242 ) ;
#208=SURFACE_STYLE_USAGE ( .BOTH. , #48512 ) ;
#210=CARTESIAN_POINT ( 'NONE',  ( -75.01496064257371188, 35.97861232747153082, -9.531191624918911032 ) ) ;
#212=CARTESIAN_POINT ( 'NONE',  ( 9.058813317711338797, 133.9549999999999841, -2.943386871421372675 ) ) ;
#215=DIRECTION ( 'NONE',  ( 4.336808689941999001E-16, -1.000000000000000000, -0.000000000000000000 ) ) ;
#217=UNCERTAINTY_MEASURE_WITH_UNIT (LENGTH_MEASURE( 1.000000000000000082E-05 ), #32735, 'distance_accuracy_value', 'NONE');
#220=ORIENTED_EDGE ( 'NONE', *, *, #67345, .F. ) ;
#222=( LENGTH_UNIT ( ) NAMED_UNIT ( * ) SI_UNIT ( .MILLI., .METRE. ) );
#223=COLOUR_RGB ( '', 0.09019608, 0.27058824, 0.51372549) ;
#225=AXIS2_PLACEMENT_3D ( 'NONE', #1591, #39312, #61408 ) ;
#226=CARTESIAN_POINT ( 'NONE',  ( -9.827790563157511022E-16, 137.5570736234661808, 8.025000000000000355 ) ) ;
#228=ORIENTED_EDGE ( 'NONE', *, *, #50580, .F. ) ;
#229=CARTESIAN_POINT ( 'NONE',  ( -6.826472737025120807, 135.9929263765338021, 4.959722759717906548 ) ) ;
#232=AXIS2_PLACEMENT_3D ( 'NONE', #24788, #2610, #8300 ) ;
#233=DIRECTION ( 'NONE',  ( -0.000000000000000000, 1.000000000000000000, -0.000000000000000000 ) ) ;
#235=STYLED_ITEM ( 'NONE', ( #26376 ), #25017 ) ;
#236=DIRECTION ( 'NONE',  ( 0.000000000000000000, 0.000000000000000000, -1.000000000000000000 ) ) ;
#237=CARTESIAN_POINT ( 'NONE',  ( 7.632228543268607446, 140.0429263765338135, 2.479861379858954606 ) ) ;
#238=ORIENTED_EDGE ( 'NONE', *, *, #66575, .F. ) ;
#242=CARTESIAN_POINT ( 'NONE',  ( -45.00000000000000000, 99.99999999999992895, 9.500000000000000000 ) ) ;
#245=DIRECTION ( 'NONE',  ( 0.000000000000000000, 0.000000000000000000, 1.000000000000000000 ) ) ;
#249=PRESENTATION_STYLE_ASSIGNMENT (( #27017 ) ) ;
#250=CARTESIAN_POINT ( 'NONE',  ( -5.598654528085806881, 154.7450000000000045, -7.705886871421374629 ) ) ;
#252=ADVANCED_FACE ( 'NONE', ( #46303 ), #29740, .T. ) ;
#254=AXIS2_PLACEMENT_3D ( 'NONE', #63574, #19953, #15420 ) ;
#255=FACE_OUTER_BOUND ( 'NONE', #52685, .T. ) ;
#257=ORIENTED_EDGE ( 'NONE', *, *, #41024, .T. ) ;
#258=CARTESIAN_POINT ( 'NONE',  ( 6.826472737025121695, 125.4929263765338021, -4.959722759717905660 ) ) ;
#263=CYLINDRICAL_SURFACE ( 'NONE', #24226, 0.5000000000000004441 ) ;
#267=EDGE_CURVE ( 'NONE', #53683, #25670, #29372, .T. ) ;
#269=PRESENTATION_STYLE_ASSIGNMENT (( #22843 ) ) ;
#272=AXIS2_PLACEMENT_3D ( 'NONE', #51746, #29926, #40167 ) ;
#273=CYLINDRICAL_SURFACE ( 'NONE', #56704, 18.00000000000000355 ) ;
#278=EDGE_CURVE ( 'NONE', #12588, #35727, #7038, .T. ) ;
#279=( LENGTH_UNIT ( ) NAMED_UNIT ( * ) SI_UNIT ( .MILLI., .METRE. ) );
#280=CARTESIAN_POINT ( 'NONE',  ( 41.47746817312157219, 107.6230562796895072, 3.580135233560061803 ) ) ;
#281=ORIENTED_EDGE ( 'NONE', *, *, #65356, .T. ) ;
#283=CARTESIAN_POINT ( 'NONE',  ( -44.99928864675339923, 9.682073287424886487, 3.525366027039916528 ) ) ;
#289=DIRECTION ( 'NONE',  ( 1.000000000000000000, 0.000000000000000000, -0.000000000000000000 ) ) ;
#293=FACE_OUTER_BOUND ( 'NONE', #40694, .T. ) ;
#296=DIRECTION ( 'NONE',  ( -0.000000000000000000, 1.000000000000000000, -0.000000000000000000 ) ) ;
#299=CARTESIAN_POINT ( 'NONE',  ( 4.716976649647096842, 125.8570736234661496, 6.492361379858953896 ) ) ;
#301=CARTESIAN_POINT ( 'NONE',  ( 5.598654528085805993, 112.3549999999999898, 7.705886871421374629 ) ) ;
#304=( GEOMETRIC_REPRESENTATION_CONTEXT ( 3 ) GLOBAL_UNCERTAINTY_ASSIGNED_CONTEXT ( ( #58594 ) ) GLOBAL_UNIT_ASSIGNED_CONTEXT ( ( #4162, #68574, #20369 ) ) REPRESENTATION_CONTEXT ( 'NONE', 'WORKASPACE' ) );
#307=CYLINDRICAL_SURFACE ( 'NONE', #23624, 13.99999999999999822 ) ;
#310=ADVANCED_FACE ( 'NONE', ( #67035 ), #58895, .T. ) ;
#311=STYLED_ITEM ( 'NONE', ( #371 ), #47003 ) ;
#315=FACE_OUTER_BOUND ( 'NONE', #23935, .T. ) ;
#319=ORIENTED_EDGE ( 'NONE', *, *, #13976, .T. ) ;
#320=VERTEX_POINT ( 'NONE', #28678 ) ;
#321=( GEOMETRIC_REPRESENTATION_CONTEXT ( 3 ) GLOBAL_UNCERTAINTY_ASSIGNED_CONTEXT ( ( #54569 ) ) GLOBAL_UNIT_ASSIGNED_CONTEXT ( ( #7356, #56918, #50953 ) ) REPRESENTATION_CONTEXT ( 'NONE', 'WORKASPACE' ) );
#324=ADVANCED_FACE ( 'NONE', ( #66322 ), #18147, .F. ) ;
#326=CARTESIAN_POINT ( 'NONE',  ( -45.84245570871746622, 9.151528339695964576, 6.292049778185707432 ) ) ;
#333=CIRCLE ( 'NONE', #2606, 13.50000000000000178 ) ;
#336=SURFACE_STYLE_USAGE ( .BOTH. , #31016 ) ;
#340=CARTESIAN_POINT ( 'NONE',  ( -1.166476076187854022E-15, 134.9449999999999932, 9.525000000000000355 ) ) ;
#341=ORIENTED_EDGE ( 'NONE', *, *, #5446, .F. ) ;
#342=AXIS2_PLACEMENT_3D ( 'NONE', #10777, #58965, #31869 ) ;
#344=CARTESIAN_POINT ( 'NONE',  ( 9.058813317711337021, 130.6550000000000011, 2.943386871421375783 ) ) ;
#348=CARTESIAN_POINT ( 'NONE',  ( -15.48999599679678951, 117.4999999999999716, -10.00000000000000000 ) ) ;
#350=CARTESIAN_POINT ( 'NONE',  ( 5.598654528085805993, 148.3549999999999898, 7.705886871421374629 ) ) ;
#351=CARTESIAN_POINT ( 'NONE',  ( -74.99999999999998579, 119.9999999999997726, 9.500000000000000000 ) ) ;
#352=UNCERTAINTY_MEASURE_WITH_UNIT (LENGTH_MEASURE( 1.000000000000000082E-05 ), #2968, 'distance_accuracy_value', 'NONE');
#353=CARTESIAN_POINT ( 'NONE',  ( -69.50000000000000000, 50.00000000000000000, -12.00000000000000000 ) ) ;
#355=MECHANICAL_DESIGN_GEOMETRIC_PRESENTATION_REPRESENTATION('',(#14033),#16160);
#357=FILL_AREA_STYLE ('',( #26774 ) ) ;
#358=FILL_AREA_STYLE_COLOUR ( '', #9295 ) ;
#361=STYLED_ITEM ( 'NONE', ( #59359 ), #48177 ) ;
#367=SURFACE_STYLE_FILL_AREA ( #58828 ) ;
#368=UNCERTAINTY_MEASURE_WITH_UNIT (LENGTH_MEASURE( 1.000000000000000082E-05 ), #47808, 'distance_accuracy_value', 'NONE');
#369=VECTOR ( 'NONE', #21449, 1000.000000000000114 ) ;
#370=FILL_AREA_STYLE ('',( #16639 ) ) ;
#371=PRESENTATION_STYLE_ASSIGNMENT (( #36383 ) ) ;
#373=VERTEX_POINT ( 'NONE', #69120 ) ;
#376=AXIS2_PLACEMENT_3D ( 'NONE', #14154, #19764, #67612 ) ;
#379=CARTESIAN_POINT ( 'NONE',  ( 71.99999999999998579, 63.67479433117734544, -9.500000000000000000 ) ) ;
#380=( GEOMETRIC_REPRESENTATION_CONTEXT ( 3 ) GLOBAL_UNCERTAINTY_ASSIGNED_CONTEXT ( ( #3120 ) ) GLOBAL_UNIT_ASSIGNED_CONTEXT ( ( #49416, #10736, #5098 ) ) REPRESENTATION_CONTEXT ( 'NONE', 'WORKASPACE' ) );
#382=DIRECTION ( 'NONE',  ( -0.000000000000000000, 1.000000000000000000, -0.000000000000000000 ) ) ;
#384=SURFACE_SIDE_STYLE ('',( #16992 ) ) ;
#386=ORIENTED_EDGE ( 'NONE', *, *, #25244, .T. ) ;
#390=( GEOMETRIC_REPRESENTATION_CONTEXT ( 3 ) GLOBAL_UNCERTAINTY_ASSIGNED_CONTEXT ( ( #37775 ) ) GLOBAL_UNIT_ASSIGNED_CONTEXT ( ( #23177, #45009, #60773 ) ) REPRESENTATION_CONTEXT ( 'NONE', 'WORKASPACE' ) );
#393=CARTESIAN_POINT ( 'NONE',  ( 10.01517768586949231, 132.6949999999999363, 1.839758294383810543E-15 ) ) ;
#403=SURFACE_STYLE_FILL_AREA ( #27517 ) ;
#406=ORIENTED_EDGE ( 'NONE', *, *, #2305, .T. ) ;
#407=CARTESIAN_POINT ( 'NONE',  ( 15.98999599679679839, 118.4999999999999716, 9.500000000000000000 ) ) ;
#411=DIRECTION ( 'NONE',  ( 1.000000000000000000, 2.116950682547968038E-14, 0.000000000000000000 ) ) ;
#415=( LENGTH_UNIT ( ) NAMED_UNIT ( * ) SI_UNIT ( .MILLI., .METRE. ) );
#422=DIRECTION ( 'NONE',  ( 1.000000000000000000, 0.000000000000000000, 0.000000000000000000 ) ) ;
#426=AXIS2_PLACEMENT_3D ( 'NONE', #33230, #23025, #2543 ) ;
#427=( BOUNDED_SURFACE ( )  B_SPLINE_SURFACE ( 3, 2, ( 
 ( #49244, #43328, #49944 ),
 ( #55178, #22502, #32695 ),
 ( #44001, #54149, #283 ),
 ( #65414, #17262, #38724 ),
 ( #17597, #60131, #11944 ),
 ( #54828, #22857, #44353 ),
 ( #65756, #39063, #13666 ),
 ( #39400, #66088, #40781 ) ),
 .UNSPECIFIED., .F., .F., .F. ) 
 B_SPLINE_SURFACE_WITH_KNOTS ( ( 4, 2, 2, 4 ),
 ( 3, 3 ),
 ( 0.003346294263012634333, 0.003496419684072975091, 0.003646545105133316284, 0.003946795947253998668 ),
 ( 0.000000000000000000, 1.000000000000000000 ),
 .UNSPECIFIED. ) 
 GEOMETRIC_REPRESENTATION_ITEM ( )  RATIONAL_B_SPLINE_SURFACE ( (
 ( 1.000000000000000000, 0.2907356542125085763, 1.000000000000000000),
 ( 1.000000000000000000, 0.3025307796950364447, 1.000000000000000000),
 ( 1.000000000000000000, 0.3140637513638668277, 1.000000000000000000),
 ( 1.000000000000000000, 0.3350422074605917677, 1.000000000000000000),
 ( 1.000000000000000000, 0.3444808824053638974, 1.000000000000000000),
 ( 1.000000000000000000, 0.3678721613322129547, 1.000000000000000000),
 ( 1.000000000000000000, 0.3767760736214396111, 1.000000000000000000),
 ( 1.000000000000000000, 0.3766558475679890328, 1.000000000000000000) ) ) 
 REPRESENTATION_ITEM ( '' )  SURFACE ( )  );
#428=CARTESIAN_POINT ( 'NONE',  ( -7.632228543268607446, 139.6570736234661467, -2.479861379858953718 ) ) ;
#429=ORIENTED_EDGE ( 'NONE', *, *, #23613, .F. ) ;
#440=ORIENTED_EDGE ( 'NONE', *, *, #34479, .T. ) ;
#446=DIRECTION ( 'NONE',  ( 0.000000000000000000, 0.000000000000000000, 1.000000000000000000 ) ) ;
#449=PRESENTATION_STYLE_ASSIGNMENT (( #6812 ) ) ;
#456=LINE ( 'NONE', #49090, #15967 ) ;
#457=SURFACE_SIDE_STYLE ('',( #43491 ) ) ;
#458=( LENGTH_UNIT ( ) NAMED_UNIT ( * ) SI_UNIT ( .MILLI., .METRE. ) );
#463=CARTESIAN_POINT ( 'NONE',  ( 5.598654528085809545, 136.1449999999999818, -7.705886871421373741 ) ) ;
#465=PRESENTATION_STYLE_ASSIGNMENT (( #5780 ) ) ;
#467=( NAMED_UNIT ( * ) PLANE_ANGLE_UNIT ( ) SI_UNIT ( $, .RADIAN. ) );
#469=FACE_OUTER_BOUND ( 'NONE', #45688, .T. ) ;
#470=CIRCLE ( 'NONE', #10679, 0.5000000000000004441 ) ;
#473=CARTESIAN_POINT ( 'NONE',  ( 75.00000000000000000, -2.215169945516535778E-14, -9.500000000000000000 ) ) ;
#478=TOROIDAL_SURFACE ( 'NONE', #19609, 27.49999999999999645, 0.5000000000000000000 ) ;
#479=SURFACE_STYLE_USAGE ( .BOTH. , #37889 ) ;
#480=CIRCLE ( 'NONE', #20796, 0.5000000000000004441 ) ;
#483=PRESENTATION_STYLE_ASSIGNMENT (( #53340 ) ) ;
#489=SURFACE_SIDE_STYLE ('',( #28657 ) ) ;
#493=CIRCLE ( 'NONE', #39921, 0.5000000000000004441 ) ;
#495=EDGE_CURVE ( 'NONE', #60866, #33108, #37843, .T. ) ;
#496=EDGE_LOOP ( 'NONE', ( #21915, #36794, #9814, #1766 ) ) ;
#498=SURFACE_STYLE_FILL_AREA ( #48799 ) ;
#499=ORIENTED_EDGE ( 'NONE', *, *, #68459, .T. ) ;
#501=EDGE_CURVE ( 'NONE', #29891, #48746, #14250, .T. ) ;
#502=CARTESIAN_POINT ( 'NONE',  ( 8.437984349512095861, 114.3070736234661666, 1.550032578732817026E-15 ) ) ;
#503=( LENGTH_UNIT ( ) NAMED_UNIT ( * ) SI_UNIT ( .MILLI., .METRE. ) );
#505=DIRECTION ( 'NONE',  ( 1.000000000000000000, 0.000000000000000000, 0.000000000000000000 ) ) ;
#508=ADVANCED_FACE ( 'NONE', ( #27196 ), #65200, .F. ) ;
#512=ORIENTED_EDGE ( 'NONE', *, *, #8696, .F. ) ;
#513=CARTESIAN_POINT ( 'NONE',  ( -10.01517768586949231, 126.3049999999999784, -6.132527647946036459E-16 ) ) ;
#516=CARTESIAN_POINT ( 'NONE',  ( 6.826472737025121695, 149.4929263765338021, -4.959722759717905660 ) ) ;
#520=FILL_AREA_STYLE ('',( #23094 ) ) ;
#526=CYLINDRICAL_SURFACE ( 'NONE', #25539, 8.025000000000000355 ) ;
#528=DIRECTION ( 'NONE',  ( 1.000000000000000000, 0.000000000000000000, 0.000000000000000000 ) ) ;
#530=CARTESIAN_POINT ( 'NONE',  ( -68.49999999999998579, -1.919947267060472329E-14, -10.49999999999999822 ) ) ;
#532=CARTESIAN_POINT ( 'NONE',  ( 44.97237157117557871, 9.999999999999980460, 3.164074568774512652 ) ) ;
#535=CARTESIAN_POINT ( 'NONE',  ( 24.21231517720798010, 113.4999999999999858, 10.00000000000000000 ) ) ;
#537=CIRCLE ( 'NONE', #69160, 1.000000000000000888 ) ;
#542=CARTESIAN_POINT ( 'NONE',  ( 0.000000000000000000, 109.9999999999999858, 0.000000000000000000 ) ) ;
#543=SURFACE_SIDE_STYLE ('',( #44265 ) ) ;
#544=STYLED_ITEM ( 'NONE', ( #19652 ), #63859 ) ;
#546=FILL_AREA_STYLE ('',( #7873 ) ) ;
#552=CIRCLE ( 'NONE', #64648, 1.000000000000000888 ) ;
#555=DIRECTION ( 'NONE',  ( 0.000000000000000000, 1.000000000000000000, 0.000000000000000000 ) ) ;
#557=LINE ( 'NONE', #64975, #11108 ) ;
#558=( NAMED_UNIT ( * ) SI_UNIT ( $, .STERADIAN. ) SOLID_ANGLE_UNIT ( ) );
#565=CARTESIAN_POINT ( 'NONE',  ( 9.058813317711337021, 136.6550000000000011, 2.943386871421375783 ) ) ;
#572=DIRECTION ( 'NONE',  ( 1.000000000000000000, 0.000000000000000000, 0.000000000000000000 ) ) ;
#577=EDGE_CURVE ( 'NONE', #48904, #13709, #23970, .T. ) ;
#579=EDGE_CURVE ( 'NONE', #15724, #20480, #67919, .T. ) ;
#580=FACE_OUTER_BOUND ( 'NONE', #29985, .T. ) ;
#584=CARTESIAN_POINT ( 'NONE',  ( -34.99999999999999289, 99.99999999999998579, -9.500000000000000000 ) ) ;
#586=CIRCLE ( 'NONE', #9675, 14.49999999999999822 ) ;
#594=( LENGTH_UNIT ( ) NAMED_UNIT ( * ) SI_UNIT ( .MILLI., .METRE. ) );
#596=ORIENTED_EDGE ( 'NONE', *, *, #59481, .F. ) ;
#599=VERTEX_POINT ( 'NONE', #55698 ) ;
#602=( GEOMETRIC_REPRESENTATION_CONTEXT ( 3 ) GLOBAL_UNCERTAINTY_ASSIGNED_CONTEXT ( ( #27133 ) ) GLOBAL_UNIT_ASSIGNED_CONTEXT ( ( #69280, #58715, #31973 ) ) REPRESENTATION_CONTEXT ( 'NONE', 'WORKASPACE' ) );
#605=ORIENTED_EDGE ( 'NONE', *, *, #66146, .T. ) ;
#610=CARTESIAN_POINT ( 'NONE',  ( 7.632228543268607446, 140.0429263765338135, 2.479861379858954606 ) ) ;
#613=CARTESIAN_POINT ( 'NONE',  ( 60.00000000000000000, 1.797044900979284448E-15, -10.00000000000000000 ) ) ;
#614=VECTOR ( 'NONE', #3377, 1000.000000000000000 ) ;
#615=PRESENTATION_STYLE_ASSIGNMENT (( #48916 ) ) ;
#620=AXIS2_PLACEMENT_3D ( 'NONE', #68621, #62294, #58074 ) ;
#622=DIRECTION ( 'NONE',  ( 0.000000000000000000, 1.712231188808094676E-15, 1.000000000000000000 ) ) ;
#623=FACE_OUTER_BOUND ( 'NONE', #46827, .T. ) ;
#629=FILL_AREA_STYLE ('',( #37340 ) ) ;
#630=CARTESIAN_POINT ( 'NONE',  ( 40.99999999999998579, 107.7459666924148252, 2.999999999999999556 ) ) ;
#631=VERTEX_POINT ( 'NONE', #30590 ) ;
#633=FILL_AREA_STYLE_COLOUR ( '', #8694 ) ;
#635=EDGE_LOOP ( 'NONE', ( #19968, #33329, #40400, #68725 ) ) ;
#636=PRESENTATION_STYLE_ASSIGNMENT (( #5968 ) ) ;
#644=DIRECTION ( 'NONE',  ( -0.000000000000000000, -0.000000000000000000, -1.000000000000000000 ) ) ;
#646=ADVANCED_FACE ( 'NONE', ( #52096 ), #14421, .T. ) ;
#648=CARTESIAN_POINT ( 'NONE',  ( -9.058813317711338797, 158.3449999999999989, 2.943386871421373563 ) ) ;
#650=CARTESIAN_POINT ( 'NONE',  ( -9.827790563157511022E-16, 113.5570736234661666, 8.025000000000000355 ) ) ;
#655=ADVANCED_FACE ( 'NONE', ( #2147 ), #7166, .F. ) ;
#657=EDGE_LOOP ( 'NONE', ( #60359, #62367, #34898 ) ) ;
#660=CARTESIAN_POINT ( 'NONE',  ( 60.00000000000000000, 1.797044900979284448E-15, 6.500000000000000000 ) ) ;
#663=FILL_AREA_STYLE ('',( #53838 ) ) ;
#665=EDGE_LOOP ( 'NONE', ( #49715, #50790 ) ) ;
#670=CARTESIAN_POINT ( 'NONE',  ( -23.71231517720798010, 117.4999999999999716, 9.500000000000000000 ) ) ;
#674=ORIENTED_EDGE ( 'NONE', *, *, #55012, .F. ) ;
#675=ORIENTED_EDGE ( 'NONE', *, *, #6557, .F. ) ;
#676=CARTESIAN_POINT ( 'NONE',  ( 0.000000000000000000, 152.9429263765338192, -8.025000000000000355 ) ) ;
#677=ORIENTED_EDGE ( 'NONE', *, *, #58749, .T. ) ;
#679=CARTESIAN_POINT ( 'NONE',  ( -1.166476076187854022E-15, 128.9449999999999648, 9.525000000000000355 ) ) ;
#680=FACE_OUTER_BOUND ( 'NONE', #24766, .T. ) ;
#683=CARTESIAN_POINT ( 'NONE',  ( -3.094860106618434248, 126.9049999999999869, 9.525000000000000355 ) ) ;
#687=ORIENTED_EDGE ( 'NONE', *, *, #50668, .F. ) ;
#688=CARTESIAN_POINT ( 'NONE',  ( 9.058813317711337021, 154.6549999999999727, 2.943386871421375783 ) ) ;
#690=COLOUR_RGB ( '', 0.40784314, 0.44705882, 0.49803922) ;
#691=FILL_AREA_STYLE ('',( #44075 ) ) ;
#693=AXIS2_PLACEMENT_3D ( 'NONE', #42691, #64090, #15943 ) ;
#695=COLOUR_RGB ( '', 0.66274510, 0.83137255, 0.94901961) ;
#698=CARTESIAN_POINT ( 'NONE',  ( 34.99999999999999289, 99.99999999999997158, -4.000000000000000000 ) ) ;
#701=CARTESIAN_POINT ( 'NONE',  ( 1.518239866961975881, 111.9742333516235959, -7.925161578318684619 ) ) ;
#703=( LENGTH_UNIT ( ) NAMED_UNIT ( * ) SI_UNIT ( .MILLI., .METRE. ) );
#706=( NAMED_UNIT ( * ) PLANE_ANGLE_UNIT ( ) SI_UNIT ( $, .RADIAN. ) );
#708=AXIS2_PLACEMENT_3D ( 'NONE', #33466, #2431, #60873 ) ;
#711=EDGE_LOOP ( 'NONE', ( #27099, #281, #7477, #38071, #31799, #34233, #57951, #19950, #23018, #67509, #55080, #10516, #52770, #24683, #63743, #40061, #46422, #12294, #62526, #64426 ) ) ;
#714=CARTESIAN_POINT ( 'NONE',  ( 2.607480562268988500, 143.7070736234661581, 8.025000000000062528 ) ) ;
#719=CYLINDRICAL_SURFACE ( 'NONE', #3216, 0.5000000000000004441 ) ;
#722=EDGE_CURVE ( 'NONE', #61387, #65027, #68863, .T. ) ;
#723=CARTESIAN_POINT ( 'NONE',  ( 8.102448949553183510, 129.9950000000000045, -5.886773742842746238 ) ) ;
#725=DIRECTION ( 'NONE',  ( 0.000000000000000000, 0.000000000000000000, 1.000000000000000000 ) ) ;
#726=LINE ( 'NONE', #12376, #44759 ) ;
#727=LINE ( 'NONE', #38132, #38212 ) ;
#734=CARTESIAN_POINT ( 'NONE',  ( -6.826472737025120807, 148.5070736234661410, -4.959722759717907437 ) ) ;
#742=CARTESIAN_POINT ( 'NONE',  ( 34.99999999999999289, 99.99999999999997158, 9.500000000000000000 ) ) ;
#750=SURFACE_SIDE_STYLE ('',( #61895 ) ) ;
#752=CARTESIAN_POINT ( 'NONE',  ( -2.607480562269073765, 151.2070736234661581, -8.025000000000000355 ) ) ;
#753=ORIENTED_EDGE ( 'NONE', *, *, #45483, .T. ) ;
#757=ORIENTED_EDGE ( 'NONE', *, *, #23978, .T. ) ;
#758=( NAMED_UNIT ( * ) PLANE_ANGLE_UNIT ( ) SI_UNIT ( $, .RADIAN. ) );
#759=( NAMED_UNIT ( * ) SI_UNIT ( $, .STERADIAN. ) SOLID_ANGLE_UNIT ( ) );
#760=( LENGTH_UNIT ( ) NAMED_UNIT ( * ) SI_UNIT ( .MILLI., .METRE. ) );
#761=( NAMED_UNIT ( * ) PLANE_ANGLE_UNIT ( ) SI_UNIT ( $, .RADIAN. ) );
#764=ORIENTED_EDGE ( 'NONE', *, *, #13916, .F. ) ;
#765=DIRECTION ( 'NONE',  ( 0.8946296187927070820, 0.000000000000000000, -0.4468085106382997385 ) ) ;
#767=LINE ( 'NONE', #44165, #46999 ) ;
#768=CARTESIAN_POINT ( 'NONE',  ( -45.00000000000000000, 8.189706559487571980, -5.659622407587006521 ) ) ;
#770=CARTESIAN_POINT ( 'NONE',  ( -74.50000000000000000, 7.768687147774684831, 6.999999999999999112 ) ) ;
#772=ORIENTED_EDGE ( 'NONE', *, *, #14294, .T. ) ;
#774=CARTESIAN_POINT ( 'NONE',  ( 45.00000000000000000, 10.69371294329215516, -6.262534692517951029 ) ) ;
#778=PRESENTATION_STYLE_ASSIGNMENT (( #43137 ) ) ;
#781=CARTESIAN_POINT ( 'NONE',  ( -5.598654528085808657, 134.6449999999999818, 7.705886871421373741 ) ) ;
#785=ORIENTED_EDGE ( 'NONE', *, *, #43825, .T. ) ;
#788=PRESENTATION_STYLE_ASSIGNMENT (( #17764 ) ) ;
#790=CONICAL_SURFACE ( 'NONE', #40211, 5.500000000000005329, 0.7853981633974309595 ) ;
#796=FILL_AREA_STYLE_COLOUR ( '', #11802 ) ;
#800=CARTESIAN_POINT ( 'NONE',  ( 45.00000000000000000, 10.69371294336137801, -4.000000000000001776 ) ) ;
#801=EDGE_CURVE ( 'NONE', #31294, #36166, #8564, .T. ) ;
#808=FILL_AREA_STYLE_COLOUR ( '', #61266 ) ;
#809=CARTESIAN_POINT ( 'NONE',  ( 4.716976649647096842, 152.8570736234661638, 6.492361379858953896 ) ) ;
#813=( BOUNDED_CURVE ( )  B_SPLINE_CURVE ( 2, ( #63359, #19750, #9216, #41245, #67966, #8856, #68296, #24330, #46539, #57038, #30276 ),
 .UNSPECIFIED., .F., .F. ) 
 B_SPLINE_CURVE_WITH_KNOTS ( ( 3, 2, 2, 2, 2, 3 ),
 ( 0.6470588235294120194, 0.6529411764705884691, 0.6588235294117649188, 0.6647058823529413685, 0.6705882352941178182, 0.6764705882352943789 ),
 .UNSPECIFIED. ) 
 CURVE ( )  GEOMETRIC_REPRESENTATION_ITEM ( )  RATIONAL_B_SPLINE_CURVE ( ( 0.9999999999999981126, 0.9510565162951554186, 1.000000000000000000, 0.9510565162951535312, 1.000000000000000000, 0.9510565162951535312, 1.000000000000000000, 0.9510565162951535312, 1.000000000000000000, 0.9510565162951516438, 1.000000000000001776 ) ) 
 REPRESENTATION_ITEM ( '' )  );
#817=CYLINDRICAL_SURFACE ( 'NONE', #68549, 8.025000000000000355 ) ;
#819=STYLED_ITEM ( 'NONE', ( #43125 ), #50506 ) ;
#820=CIRCLE ( 'NONE', #40245, 0.4999999999999994449 ) ;
#828=COLOUR_RGB ( '', 0.09019608, 0.27058824, 0.51372549) ;
#830=CARTESIAN_POINT ( 'NONE',  ( 6.826472737025119919, 123.0070736234661695, 4.959722759717908325 ) ) ;
#831=DIRECTION ( 'NONE',  ( 0.000000000000000000, -1.000000000000000000, 0.000000000000000000 ) ) ;
#832=CARTESIAN_POINT ( 'NONE',  ( 74.65811388300841145, 19.88603796100278487, -6.000000000000000000 ) ) ;
#836=CARTESIAN_POINT ( 'NONE',  ( 15.98999599679679839, 146.4999999999999716, 7.000000000000000000 ) ) ;
#838=DIRECTION ( 'NONE',  ( -0.000000000000000000, -0.000000000000000000, -1.000000000000000000 ) ) ;
#839=DIRECTION ( 'NONE',  ( -0.000000000000000000, 1.000000000000000000, -0.000000000000000000 ) ) ;
#843=CARTESIAN_POINT ( 'NONE',  ( 8.209205615337721085, 153.6217806035195110, -2.745863952952167342 ) ) ;
#846=AXIS2_PLACEMENT_3D ( 'NONE', #22168, #7704, #65057 ) ;
#848=CARTESIAN_POINT ( 'NONE',  ( 2.607480562269076430, 161.7929263765338135, -8.025000000000000355 ) ) ;
#849=VERTEX_POINT ( 'NONE', #14704 ) ;
#853=CARTESIAN_POINT ( 'NONE',  ( 72.49999999999998579, 64.07124727947029896, -10.00000000000000000 ) ) ;
#855=SURFACE_STYLE_FILL_AREA ( #64264 ) ;
#856=CIRCLE ( 'NONE', #40278, 16.44999999999999218 ) ;
#858=CARTESIAN_POINT ( 'NONE',  ( -75.00000000000000000, 7.768687147774688384, -6.999999999999999112 ) ) ;
#870=( NAMED_UNIT ( * ) PLANE_ANGLE_UNIT ( ) SI_UNIT ( $, .RADIAN. ) );
#881=DIRECTION ( 'NONE',  ( 1.000000000000000000, 0.000000000000000000, 0.000000000000000000 ) ) ;
#886=EDGE_CURVE ( 'NONE', #36075, #3129, #2705, .T. ) ;
#888=CARTESIAN_POINT ( 'NONE',  ( -8.102448949553181734, 138.6049999999999329, 5.886773742842747126 ) ) ;
#890=CARTESIAN_POINT ( 'NONE',  ( 7.186760109404651153, 154.4703037126919867, 6.248938465618627980 ) ) ;
#896=AXIS2_PLACEMENT_3D ( 'NONE', #40176, #45807, #61574 ) ;
#897=DIRECTION ( 'NONE',  ( 0.000000000000000000, 0.000000000000000000, 1.000000000000000000 ) ) ;
#899=MECHANICAL_DESIGN_GEOMETRIC_PRESENTATION_REPRESENTATION('',(#50407),#5477);
#901=CYLINDRICAL_SURFACE ( 'NONE', #61063, 5.000000000000004441 ) ;
#903=COLOUR_RGB ( '', 0.31764706, 0.68627451, 0.89019608) ;
#905=MECHANICAL_DESIGN_GEOMETRIC_PRESENTATION_REPRESENTATION('',(#66119),#43731);
#907=( GEOMETRIC_REPRESENTATION_CONTEXT ( 3 ) GLOBAL_UNCERTAINTY_ASSIGNED_CONTEXT ( ( #51593 ) ) GLOBAL_UNIT_ASSIGNED_CONTEXT ( ( #5704, #16660, #55985 ) ) REPRESENTATION_CONTEXT ( 'NONE', 'WORKASPACE' ) );
#908=EDGE_LOOP ( 'NONE', ( #67803, #57612, #55838, #66761 ) ) ;
#911=SURFACE_STYLE_FILL_AREA ( #38685 ) ;
#919=CARTESIAN_POINT ( 'NONE',  ( 10.01517768586949231, 156.6949999999999932, 1.839758294383810543E-15 ) ) ;
#921=ORIENTED_EDGE ( 'NONE', *, *, #6986, .F. ) ;
#926=CARTESIAN_POINT ( 'NONE',  ( -2.607480562269073765, 132.0929263765338249, -8.025000000000000355 ) ) ;
#927=CARTESIAN_POINT ( 'NONE',  ( 45.50000000000000000, -1.469576158976824618E-14, 10.00000000000000000 ) ) ;
#936=( LENGTH_UNIT ( ) NAMED_UNIT ( * ) SI_UNIT ( .MILLI., .METRE. ) );
#940=( LENGTH_UNIT ( ) NAMED_UNIT ( * ) SI_UNIT ( .MILLI., .METRE. ) );
#942=ORIENTED_EDGE ( 'NONE', *, *, #69657, .F. ) ;
#943=AXIS2_PLACEMENT_3D ( 'NONE', #27160, #59885, #725 ) ;
#944=CARTESIAN_POINT ( 'NONE',  ( 41.61212508608636540, 107.5086115709064956, 4.000000005149253468 ) ) ;
#948=MECHANICAL_DESIGN_GEOMETRIC_PRESENTATION_REPRESENTATION('',(#61662),#15669);
#952=CARTESIAN_POINT ( 'NONE',  ( -20.57648123223228254, 154.9999999999999716, -10.27659574468085069 ) ) ;
#953=ADVANCED_FACE ( 'NONE', ( #51633 ), #51996, .T. ) ;
#955=CARTESIAN_POINT ( 'NONE',  ( 44.50000000000000000, 99.99999999999998579, -3.500000000000000000 ) ) ;
#956=EDGE_CURVE ( 'NONE', #7813, #35108, #56198, .T. ) ;
#960=DIRECTION ( 'NONE',  ( 1.000000000000000000, 0.000000000000000000, 0.000000000000000000 ) ) ;
#962=AXIS2_PLACEMENT_3D ( 'NONE', #56401, #8236, #63071 ) ;
#964=AXIS2_PLACEMENT_3D ( 'NONE', #69437, #21227, #422 ) ;
#971=ADVANCED_FACE ( 'NONE', ( #15752 ), #57965, .T. ) ;
#973=CARTESIAN_POINT ( 'NONE',  ( 5.598654528085809545, 160.1449999999999818, -7.705886871421373741 ) ) ;
#981=EDGE_LOOP ( 'NONE', ( #30979, #51142, #59233 ) ) ;
#985=DIRECTION ( 'NONE',  ( 0.000000000000000000, 1.000000000000000000, -0.000000000000000000 ) ) ;
#995=( NAMED_UNIT ( * ) PLANE_ANGLE_UNIT ( ) SI_UNIT ( $, .RADIAN. ) );
#999=DIRECTION ( 'NONE',  ( 0.000000000000000000, 0.000000000000000000, 1.000000000000000000 ) ) ;
#1002=ORIENTED_EDGE ( 'NONE', *, *, #18036, .T. ) ;
#1011=CARTESIAN_POINT ( 'NONE',  ( -10.01517768586949231, 128.1950000000000216, -6.132527647946036459E-16 ) ) ;
#1012=VERTEX_POINT ( 'NONE', #58990 ) ;
#1013=DIRECTION ( 'NONE',  ( 0.000000000000000000, 0.000000000000000000, 1.000000000000000000 ) ) ;
#1014=CARTESIAN_POINT ( 'NONE',  ( 3.094860106618431583, 130.2049999999999841, 9.525000000000000355 ) ) ;
#1017=MECHANICAL_DESIGN_GEOMETRIC_PRESENTATION_REPRESENTATION('',(#69588),#41554);
#1020=CARTESIAN_POINT ( 'NONE',  ( -9.058813317711338797, 159.4549999999999841, 2.943386871421373563 ) ) ;
#1022=UNCERTAINTY_MEASURE_WITH_UNIT (LENGTH_MEASURE( 1.000000000000000082E-05 ), #27650, 'distance_accuracy_value', 'NONE');
#1024=( NAMED_UNIT ( * ) PLANE_ANGLE_UNIT ( ) SI_UNIT ( $, .RADIAN. ) );
#1028=CARTESIAN_POINT ( 'NONE',  ( 20.71231517720798010, 109.9999999999999858, 9.500000000000000000 ) ) ;
#1031=LINE ( 'NONE', #22576, #25461 ) ;
#1032=FACE_OUTER_BOUND ( 'NONE', #23249, .T. ) ;
#1036=UNCERTAINTY_MEASURE_WITH_UNIT (LENGTH_MEASURE( 1.000000000000000082E-05 ), #23838, 'distance_accuracy_value', 'NONE');
#1040=FACE_OUTER_BOUND ( 'NONE', #32390, .T. ) ;
#1041=( NAMED_UNIT ( * ) PLANE_ANGLE_UNIT ( ) SI_UNIT ( $, .RADIAN. ) );
#1042=( NAMED_UNIT ( * ) SI_UNIT ( $, .STERADIAN. ) SOLID_ANGLE_UNIT ( ) );
#1045=AXIS2_PLACEMENT_3D ( 'NONE', #18634, #23539, #28450 ) ;
#1046=EDGE_CURVE ( 'NONE', #39125, #41202, #52649, .T. ) ;
#1047=SURFACE_SIDE_STYLE ('',( #65491 ) ) ;
#1049=ORIENTED_EDGE ( 'NONE', *, *, #65191, .F. ) ;
#1051=EDGE_CURVE ( 'NONE', #31668, #16942, #44246, .T. ) ;
#1053=COLOUR_RGB ( '', 0.66274510, 0.83137255, 0.94901961) ;
#1054=FILL_AREA_STYLE_COLOUR ( '', #68815 ) ;
#1055=DIRECTION ( 'NONE',  ( 0.000000000000000000, 0.000000000000000000, -1.000000000000000000 ) ) ;
#1059=ORIENTED_EDGE ( 'NONE', *, *, #66159, .T. ) ;
#1060=PRESENTATION_STYLE_ASSIGNMENT (( #22250 ) ) ;
#1063=CARTESIAN_POINT ( 'NONE',  ( 5.598654528085809545, 127.1449999999999818, -7.705886871421373741 ) ) ;
#1066=AXIS2_PLACEMENT_3D ( 'NONE', #10576, #69647, #37700 ) ;
#1067=CARTESIAN_POINT ( 'NONE',  ( -71.49999999999998579, 119.9999999999997868, -7.500000000000000000 ) ) ;
#1077=ORIENTED_EDGE ( 'NONE', *, *, #50915, .F. ) ;
#1079=DIRECTION ( 'NONE',  ( 0.000000000000000000, -1.000000000000000000, 0.000000000000000000 ) ) ;
#1083=CARTESIAN_POINT ( 'NONE',  ( -45.91547277936962246, 9.430195807687217879, 6.039758700367571898 ) ) ;
#1090=STYLED_ITEM ( 'NONE', ( #6246 ), #69414 ) ;
#1094=VERTEX_POINT ( 'NONE', #11133 ) ;
#1095=LINE ( 'NONE', #22635, #20169 ) ;
#1097=( NAMED_UNIT ( * ) SI_UNIT ( $, .STERADIAN. ) SOLID_ANGLE_UNIT ( ) );
#1099=FACE_BOUND ( 'NONE', #16181, .T. ) ;
#1100=CARTESIAN_POINT ( 'NONE',  ( -9.827790563157511022E-16, 149.5570736234661524, 8.025000000000000355 ) ) ;
#1102=AXIS2_PLACEMENT_3D ( 'NONE', #7032, #1705, #66107 ) ;
#1103=CARTESIAN_POINT ( 'NONE',  ( 2.607480562268992941, 137.7929263765338419, -8.025000000000060751 ) ) ;
#1104=STYLED_ITEM ( 'NONE', ( #33830 ), #11987 ) ;
#1106=UNCERTAINTY_MEASURE_WITH_UNIT (LENGTH_MEASURE( 1.000000000000000082E-05 ), #415, 'distance_accuracy_value', 'NONE');
#1109=ADVANCED_FACE ( 'NONE', ( #28690 ), #54044, .F. ) ;
#1113=DIRECTION ( 'NONE',  ( -0.000000000000000000, -0.000000000000000000, -1.000000000000000000 ) ) ;
#1114=CARTESIAN_POINT ( 'NONE',  ( 20.57648123223228254, 110.4999999999999858, -10.27659574468085069 ) ) ;
#1119=STYLED_ITEM ( 'NONE', ( #55497 ), #34613 ) ;
#1121=SURFACE_STYLE_USAGE ( .BOTH. , #5755 ) ;
#1122=EDGE_CURVE ( 'NONE', #7643, #49707, #24655, .T. ) ;
#1124=FILL_AREA_STYLE ('',( #6457 ) ) ;
#1125=CARTESIAN_POINT ( 'NONE',  ( -45.00000000000000000, 9.708372675170615196, -6.000000000000000888 ) ) ;
#1128=( LENGTH_UNIT ( ) NAMED_UNIT ( * ) SI_UNIT ( .MILLI., .METRE. ) );
#1130=CARTESIAN_POINT ( 'NONE',  ( 44.99999999999999289, 9.639620389971918613, -6.500000000000007105 ) ) ;
#1131=CARTESIAN_POINT ( 'NONE',  ( 0.000000000000000000, 111.9999999999999858, 0.000000000000000000 ) ) ;
#1133=ORIENTED_EDGE ( 'NONE', *, *, #57435, .T. ) ;
#1137=( NAMED_UNIT ( * ) SI_UNIT ( $, .STERADIAN. ) SOLID_ANGLE_UNIT ( ) );
#1138=DIRECTION ( 'NONE',  ( 0.000000000000000000, 1.000000000000000000, -0.000000000000000000 ) ) ;
#1139=SURFACE_SIDE_STYLE ('',( #43493 ) ) ;
#1141=AXIS2_PLACEMENT_3D ( 'NONE', #3631, #7905, #30372 ) ;
#1142=CARTESIAN_POINT ( 'NONE',  ( 5.598654528085809545, 130.1449999999999818, -7.705886871421373741 ) ) ;
#1146=DIRECTION ( 'NONE',  ( 1.000000000000000000, 1.601283208593975100E-14, 0.000000000000000000 ) ) ;
#1149=CARTESIAN_POINT ( 'NONE',  ( -15.98999599679679839, 118.4999999999999716, 7.000000000000000000 ) ) ;
#1160=SURFACE_STYLE_USAGE ( .BOTH. , #38912 ) ;
#1170=FILL_AREA_STYLE_COLOUR ( '', #43640 ) ;
#1171=CARTESIAN_POINT ( 'NONE',  ( -60.00000000000000000, -2.024042244987997205E-14, 12.00000000000000000 ) ) ;
#1172=COLOUR_RGB ( '', 0.31764706, 0.68627451, 0.89019608) ;
#1176=CYLINDRICAL_SURFACE ( 'NONE', #1141, 0.5000000000000004441 ) ;
#1177=ADVANCED_FACE ( 'NONE', ( #61050 ), #66333, .F. ) ;
#1178=VECTOR ( 'NONE', #18203, 1000.000000000000000 ) ;
#1179=CARTESIAN_POINT ( 'NONE',  ( -48.50000000000000000, 14.49137674618942562, -7.500000000000000000 ) ) ;
#1181=MECHANICAL_DESIGN_GEOMETRIC_PRESENTATION_REPRESENTATION('',(#46236),#52936);
#1183=ORIENTED_EDGE ( 'NONE', *, *, #62423, .F. ) ;
#1188=AXIS2_PLACEMENT_3D ( 'NONE', #63108, #10004, #20185 ) ;
#1189=CARTESIAN_POINT ( 'NONE',  ( -7.632228543268607446, 127.6570736234661467, -2.479861379858953718 ) ) ;
#1192=CARTESIAN_POINT ( 'NONE',  ( 34.99999999999992895, 110.4999999999999858, -10.00000000000000000 ) ) ;
#1194=DIRECTION ( 'NONE',  ( 0.000000000000000000, 0.000000000000000000, 1.000000000000000000 ) ) ;
#1196=AXIS2_PLACEMENT_3D ( 'NONE', #18355, #29584, #13059 ) ;
#1206=AXIS2_PLACEMENT_3D ( 'NONE', #46550, #19759, #14477 ) ;
#1207=CARTESIAN_POINT ( 'NONE',  ( 2.607480562269034241, 134.7929263765338135, -8.025000000000032330 ) ) ;
#1211=EDGE_CURVE ( 'NONE', #8109, #66508, #33662, .T. ) ;
#1223=DIRECTION ( 'NONE',  ( 1.224646799147353207E-16, 1.000000000000000000, -0.000000000000000000 ) ) ;
#1227=DIRECTION ( 'NONE',  ( -0.000000000000000000, -0.000000000000000000, -1.000000000000000000 ) ) ;
#1228=CARTESIAN_POINT ( 'NONE',  ( 60.00000000000000000, 1.797044900979284448E-15, -7.000000000000000888 ) ) ;
#1230=( NAMED_UNIT ( * ) PLANE_ANGLE_UNIT ( ) SI_UNIT ( $, .RADIAN. ) );
#1231=CARTESIAN_POINT ( 'NONE',  ( -8.440061761865273127, 153.6413859836615359, 2.039925464057752880 ) ) ;
#1233=CIRCLE ( 'NONE', #28222, 7.500000000000000000 ) ;
#1234=SURFACE_STYLE_FILL_AREA ( #22069 ) ;
#1235=DIRECTION ( 'NONE',  ( 1.000000000000000000, 0.000000000000000000, 0.000000000000000000 ) ) ;
#1237=CYLINDRICAL_SURFACE ( 'NONE', #33201, 0.5000000000000004441 ) ;
#1247=ORIENTED_EDGE ( 'NONE', *, *, #15835, .T. ) ;
#1249=CARTESIAN_POINT ( 'NONE',  ( 44.83562443654408725, 9.945208145515103126, 3.584089800673137205 ) ) ;
#1254=( NAMED_UNIT ( * ) PLANE_ANGLE_UNIT ( ) SI_UNIT ( $, .RADIAN. ) );
#1256=CARTESIAN_POINT ( 'NONE',  ( -5.598654528085806881, 137.8549999999999898, -7.705886871421374629 ) ) ;
#1258=( GEOMETRIC_REPRESENTATION_CONTEXT ( 3 ) GLOBAL_UNCERTAINTY_ASSIGNED_CONTEXT ( ( #60738 ) ) GLOBAL_UNIT_ASSIGNED_CONTEXT ( ( #46100, #63287, #19676 ) ) REPRESENTATION_CONTEXT ( 'NONE', 'WORKASPACE' ) );
#1260=SURFACE_STYLE_USAGE ( .BOTH. , #49535 ) ;
#1264=AXIS2_PLACEMENT_3D ( 'NONE', #69527, #68504, #26267 ) ;
#1273=( GEOMETRIC_REPRESENTATION_CONTEXT ( 3 ) GLOBAL_UNCERTAINTY_ASSIGNED_CONTEXT ( ( #62316 ) ) GLOBAL_UNIT_ASSIGNED_CONTEXT ( ( #32324, #36270, #26006 ) ) REPRESENTATION_CONTEXT ( 'NONE', 'WORKASPACE' ) );
#1275=SURFACE_STYLE_USAGE ( .BOTH. , #28387 ) ;
#1276=DIRECTION ( 'NONE',  ( -1.000000000000000000, 0.000000000000000000, 0.000000000000000000 ) ) ;
#1280=ORIENTED_EDGE ( 'NONE', *, *, #13683, .F. ) ;
#1282=VECTOR ( 'NONE', #24541, 1000.000000000000000 ) ;
#1283=EDGE_LOOP ( 'NONE', ( #11813, #37848, #54579, #36242 ) ) ;
#1289=CARTESIAN_POINT ( 'NONE',  ( 8.102448949553183510, 156.9949999999999761, -5.886773742842746238 ) ) ;
#1291=ORIENTED_EDGE ( 'NONE', *, *, #47372, .F. ) ;
#1294=CARTESIAN_POINT ( 'NONE',  ( -7.315997198399062817, 110.4999999999999716, -6.115009789855206712 ) ) ;
#1295=( NAMED_UNIT ( * ) PLANE_ANGLE_UNIT ( ) SI_UNIT ( $, .RADIAN. ) );
#1296=DIRECTION ( 'NONE',  ( 1.000000000000000000, 0.000000000000000000, 0.000000000000000000 ) ) ;
#1297=DIRECTION ( 'NONE',  ( 0.000000000000000000, 0.000000000000000000, -1.000000000000000000 ) ) ;
#1299=CARTESIAN_POINT ( 'NONE',  ( 2.607480562269071989, 136.5929263765338249, 8.025000000000002132 ) ) ;
#1302=AXIS2_PLACEMENT_3D ( 'NONE', #29668, #24371, #46230 ) ;
#1303=EDGE_CURVE ( 'NONE', #9072, #69035, #35880, .T. ) ;
#1305=FACE_OUTER_BOUND ( 'NONE', #25216, .T. ) ;
#1308=ORIENTED_EDGE ( 'NONE', *, *, #5446, .T. ) ;
#1318=( GEOMETRIC_REPRESENTATION_CONTEXT ( 3 ) GLOBAL_UNCERTAINTY_ASSIGNED_CONTEXT ( ( #10073 ) ) GLOBAL_UNIT_ASSIGNED_CONTEXT ( ( #1753, #7084, #39471 ) ) REPRESENTATION_CONTEXT ( 'NONE', 'WORKASPACE' ) );
#1321=CARTESIAN_POINT ( 'NONE',  ( -45.00000000000000000, 9.708372675170618749, -6.000000000000000000 ) ) ;
#1322=ORIENTED_EDGE ( 'NONE', *, *, #36239, .F. ) ;
#1326=CARTESIAN_POINT ( 'NONE',  ( 0.000000000000000000, 87.30187232391182306, 8.025000000000000355 ) ) ;
#1328=ORIENTED_EDGE ( 'NONE', *, *, #29654, .T. ) ;
#1329=FILL_AREA_STYLE ('',( #60802 ) ) ;
#1330=AXIS2_PLACEMENT_3D ( 'NONE', #45095, #48989, #61227 ) ;
#1334=ADVANCED_FACE ( 'NONE', ( #63825 ), #59512, .T. ) ;
#1338=DIRECTION ( 'NONE',  ( 0.000000000000000000, 0.000000000000000000, 1.000000000000000000 ) ) ;
#1340=DIRECTION ( 'NONE',  ( -1.000000000000000000, 1.224646799147349509E-16, 0.000000000000000000 ) ) ;
#1342=CONICAL_SURFACE ( 'NONE', #66540, 5.499999999999976907, 0.7853981633974309595 ) ;
#1344=CARTESIAN_POINT ( 'NONE',  ( -8.102448949553181734, 111.0049999999999955, -5.886773742842749790 ) ) ;
#1346=AXIS2_PLACEMENT_3D ( 'NONE', #38983, #42884, #22765 ) ;
#1349=( NAMED_UNIT ( * ) SI_UNIT ( $, .STERADIAN. ) SOLID_ANGLE_UNIT ( ) );
#1352=AXIS2_PLACEMENT_3D ( 'NONE', #3507, #4216, #14826 ) ;
#1353=DIRECTION ( 'NONE',  ( -0.000000000000000000, 1.000000000000000000, -0.000000000000000000 ) ) ;
#1354=DIRECTION ( 'NONE',  ( -0.000000000000000000, -1.000000000000000000, 0.000000000000000000 ) ) ;
#1355=VERTEX_POINT ( 'NONE', #52277 ) ;
#1357=( GEOMETRIC_REPRESENTATION_CONTEXT ( 3 ) GLOBAL_UNCERTAINTY_ASSIGNED_CONTEXT ( ( #38268 ) ) GLOBAL_UNIT_ASSIGNED_CONTEXT ( ( #67368, #13909, #8640 ) ) REPRESENTATION_CONTEXT ( 'NONE', 'WORKASPACE' ) );
#1360=CIRCLE ( 'NONE', #37436, 16.94999999999999218 ) ;
#1364=ORIENTED_EDGE ( 'NONE', *, *, #65878, .T. ) ;
#1365=CIRCLE ( 'NONE', #55345, 0.5000000000000004441 ) ;
#1366=ORIENTED_EDGE ( 'NONE', *, *, #32459, .F. ) ;
#1368=DIRECTION ( 'NONE',  ( 0.000000000000000000, 1.000000000000000000, 0.000000000000000000 ) ) ;
#1369=MECHANICAL_DESIGN_GEOMETRIC_PRESENTATION_REPRESENTATION('',(#7050),#50843);
#1371=DIRECTION ( 'NONE',  ( -0.000000000000000000, -1.000000000000000000, 0.000000000000000000 ) ) ;
#1376=ORIENTED_EDGE ( 'NONE', *, *, #28257, .T. ) ;
#1377=EDGE_CURVE ( 'NONE', #47061, #49280, #37856, .T. ) ;
#1379=FILL_AREA_STYLE_COLOUR ( '', #46788 ) ;
#1384=CIRCLE ( 'NONE', #58745, 0.5000000000000004441 ) ;
#1387=CARTESIAN_POINT ( 'NONE',  ( 9.058813317711337021, 129.5449999999999875, 2.943386871421375783 ) ) ;
#1388=DIRECTION ( 'NONE',  ( 0.000000000000000000, 0.000000000000000000, 1.000000000000000000 ) ) ;
#1389=AXIS2_PLACEMENT_3D ( 'NONE', #58474, #53213, #1407 ) ;
#1392=CARTESIAN_POINT ( 'NONE',  ( -10.01517768586949408, 126.3049999999999784, -6.132527647946036459E-16 ) ) ;
#1397=CARTESIAN_POINT ( 'NONE',  ( -3.094860106618434248, 153.9049999999999443, 9.525000000000000355 ) ) ;
#1403=PRESENTATION_STYLE_ASSIGNMENT (( #49658 ) ) ;
#1404=FILL_AREA_STYLE_COLOUR ( '', #32070 ) ;
#1405=VECTOR ( 'NONE', #56854, 1000.000000000000000 ) ;
#1407=DIRECTION ( 'NONE',  ( -1.000000000000000000, 0.000000000000000000, 0.000000000000000000 ) ) ;
#1408=VERTEX_POINT ( 'NONE', #12088 ) ;
#1410=FILL_AREA_STYLE_COLOUR ( '', #38556 ) ;
#1413=FILL_AREA_STYLE_COLOUR ( '', #18303 ) ;
#1415=FILL_AREA_STYLE_COLOUR ( '', #31002 ) ;
#1417=EDGE_LOOP ( 'NONE', ( #28875, #48706, #35094, #7610 ) ) ;
#1418=CARTESIAN_POINT ( 'NONE',  ( -45.03917211512175811, 8.121391520911325657, -3.616130125723889144 ) ) ;
#1422=CARTESIAN_POINT ( 'NONE',  ( -44.99999999999977973, 146.9999999999999716, 7.000000000000000000 ) ) ;
#1423=DIRECTION ( 'NONE',  ( 1.000000000000000000, 0.000000000000000000, 0.000000000000000000 ) ) ;
#1425=CARTESIAN_POINT ( 'NONE',  ( 23.21231517720797655, 117.4999999999999716, 10.00000000000000000 ) ) ;
#1426=ORIENTED_EDGE ( 'NONE', *, *, #62891, .F. ) ;
#1428=CARTESIAN_POINT ( 'NONE',  ( 3.094860106618435136, 127.2949999999999875, -9.525000000000000355 ) ) ;
#1430=CIRCLE ( 'NONE', #65510, 0.5000000000000004441 ) ;
#1437=( GEOMETRIC_REPRESENTATION_CONTEXT ( 3 ) GLOBAL_UNCERTAINTY_ASSIGNED_CONTEXT ( ( #62085 ) ) GLOBAL_UNIT_ASSIGNED_CONTEXT ( ( #52179, #58131, #19436 ) ) REPRESENTATION_CONTEXT ( 'NONE', 'WORKASPACE' ) );
#1438=AXIS2_PLACEMENT_3D ( 'NONE', #23559, #55221, #1717 ) ;
#1440=EDGE_CURVE ( 'NONE', #65459, #13986, #26856, .T. ) ;
#1441=CARTESIAN_POINT ( 'NONE',  ( 74.99999999999998579, 50.00000000000000000, 7.500000000000000000 ) ) ;
#1443=DIRECTION ( 'NONE',  ( -0.000000000000000000, -0.000000000000000000, -1.000000000000000000 ) ) ;
#1448=FILL_AREA_STYLE_COLOUR ( '', #19215 ) ;
#1449=CIRCLE ( 'NONE', #48762, 0.5000000000000004441 ) ;
#1450=ADVANCED_FACE ( 'NONE', ( #44513 ), #56041, .F. ) ;
#1451=FILL_AREA_STYLE ('',( #21946 ) ) ;
#1457=ADVANCED_FACE ( 'NONE', ( #2536 ), #45872, .F. ) ;
#1458=ORIENTED_EDGE ( 'NONE', *, *, #68873, .F. ) ;
#1459=FACE_OUTER_BOUND ( 'NONE', #69682, .T. ) ;
#1463=TOROIDAL_SURFACE ( 'NONE', #36424, 10.49999999999999822, 0.5000000000000000000 ) ;
#1466=CARTESIAN_POINT ( 'NONE',  ( -4.716976649647098618, 155.2570736234661695, 6.492361379858953008 ) ) ;
#1467=COLOUR_RGB ( '', 0.08235294, 0.09019608, 0.10196078) ;
#1476=EDGE_LOOP ( 'NONE', ( #27866, #33163, #13088, #60927 ) ) ;
#1480=ORIENTED_EDGE ( 'NONE', *, *, #10436, .F. ) ;
#1483=DIRECTION ( 'NONE',  ( -0.000000000000000000, -1.000000000000000000, -0.000000000000000000 ) ) ;
#1484=CARTESIAN_POINT ( 'NONE',  ( -45.00000000000000000, 8.747695062214377870, -6.883368695987051034 ) ) ;
#1489=ORIENTED_EDGE ( 'NONE', *, *, #35919, .F. ) ;
#1490=CIRCLE ( 'NONE', #62198, 0.5000000000000003331 ) ;
#1491=CIRCLE ( 'NONE', #40906, 16.50000000000000000 ) ;
#1492=CARTESIAN_POINT ( 'NONE',  ( -71.99999999999998579, 64.07124727947029896, 9.500000000000000000 ) ) ;
#1494=EDGE_LOOP ( 'NONE', ( #28905, #64829, #57228, #9435, #16796, #47009, #29650 ) ) ;
#1502=CARTESIAN_POINT ( 'NONE',  ( 0.000000000000000000, 133.4449999999999932, -9.525000000000000355 ) ) ;
#1507=ORIENTED_EDGE ( 'NONE', *, *, #64505, .T. ) ;
#1514=DIRECTION ( 'NONE',  ( -0.000000000000000000, -0.000000000000000000, 1.000000000000000000 ) ) ;
#1518=MECHANICAL_DESIGN_GEOMETRIC_PRESENTATION_REPRESENTATION('',(#62224),#67871);
#1526=STYLED_ITEM ( 'NONE', ( #69011 ), #38236 ) ;
#1527=EDGE_CURVE ( 'NONE', #61621, #8720, #51254, .T. ) ;
#1528=CARTESIAN_POINT ( 'NONE',  ( -24.21231517720798010, 112.4999999999999858, -10.00000000000000000 ) ) ;
#1530=( GEOMETRIC_REPRESENTATION_CONTEXT ( 3 ) GLOBAL_UNCERTAINTY_ASSIGNED_CONTEXT ( ( #1022 ) ) GLOBAL_UNIT_ASSIGNED_CONTEXT ( ( #27650, #5492, #59675 ) ) REPRESENTATION_CONTEXT ( 'NONE', 'WORKASPACE' ) );
#1531=DIRECTION ( 'NONE',  ( 1.000000000000000000, 0.000000000000000000, 0.000000000000000000 ) ) ;
#1532=FILL_AREA_STYLE_COLOUR ( '', #19254 ) ;
#1536=STYLED_ITEM ( 'NONE', ( #12096 ), #56123 ) ;
#1539=( LENGTH_UNIT ( ) NAMED_UNIT ( * ) SI_UNIT ( .MILLI., .METRE. ) );
#1541=DIRECTION ( 'NONE',  ( 0.000000000000000000, 0.000000000000000000, -1.000000000000000000 ) ) ;
#1542=FACE_OUTER_BOUND ( 'NONE', #12338, .T. ) ;
#1547=ADVANCED_FACE ( 'NONE', ( #20862 ), #47907, .T. ) ;
#1548=CARTESIAN_POINT ( 'NONE',  ( -15.48999599679679662, 146.4999999999999716, -7.500000000000000000 ) ) ;
#1552=CARTESIAN_POINT ( 'NONE',  ( -4.716976649647098618, 128.2570736234661695, 6.492361379858953008 ) ) ;
#1554=( GEOMETRIC_REPRESENTATION_CONTEXT ( 3 ) GLOBAL_UNCERTAINTY_ASSIGNED_CONTEXT ( ( #62966 ) ) GLOBAL_UNIT_ASSIGNED_CONTEXT ( ( #48576, #59403, #49235 ) ) REPRESENTATION_CONTEXT ( 'NONE', 'WORKASPACE' ) );
#1555=LINE ( 'NONE', #34318, #59 ) ;
#1560=TOROIDAL_SURFACE ( 'NONE', #6083, 13.49999999999999822, 0.5000000000000000000 ) ;
#1568=CARTESIAN_POINT ( 'NONE',  ( -20.46001754528041161, 114.7916627990982192, -10.31416700829639588 ) ) ;
#1569=FACE_OUTER_BOUND ( 'NONE', #46402, .T. ) ;
#1571=ORIENTED_EDGE ( 'NONE', *, *, #19374, .T. ) ;
#1572=CARTESIAN_POINT ( 'NONE',  ( 2.607480562269071989, 160.5929263765337964, 8.025000000000002132 ) ) ;
#1577=VERTEX_POINT ( 'NONE', #26111 ) ;
#1590=ORIENTED_EDGE ( 'NONE', *, *, #7241, .T. ) ;
#1591=CARTESIAN_POINT ( 'NONE',  ( -23.21231517720797655, 117.4999999999999716, -7.500000000000000000 ) ) ;
#1592=DIRECTION ( 'NONE',  ( 0.000000000000000000, 0.000000000000000000, -1.000000000000000000 ) ) ;
#1593=CARTESIAN_POINT ( 'NONE',  ( -34.99999999999992895, 112.9999999999999858, -7.500000000000000000 ) ) ;
#1604=AXIS2_PLACEMENT_3D ( 'NONE', #45387, #50619, #61489 ) ;
#1605=CARTESIAN_POINT ( 'NONE',  ( 44.97464006314717722, 9.991546687716530428, 3.784415753861383180 ) ) ;
#1606=DIRECTION ( 'NONE',  ( -0.000000000000000000, 1.000000000000000000, -0.000000000000000000 ) ) ;
#1613=CARTESIAN_POINT ( 'NONE',  ( 8.102448949553183510, 149.1049999999999898, -5.886773742842746238 ) ) ;
#1615=CIRCLE ( 'NONE', #33116, 8.000000000000000000 ) ;
#1618=CARTESIAN_POINT ( 'NONE',  ( 6.669484432089998194, 154.4410788397644296, 6.756431230636611218 ) ) ;
#1619=UNCERTAINTY_MEASURE_WITH_UNIT (LENGTH_MEASURE( 1.000000000000000082E-05 ), #22366, 'distance_accuracy_value', 'NONE');
#1623=( NAMED_UNIT ( * ) PLANE_ANGLE_UNIT ( ) SI_UNIT ( $, .RADIAN. ) );
#1624=FILL_AREA_STYLE ('',( #50225 ) ) ;
#1628=CARTESIAN_POINT ( 'NONE',  ( -72.49999999999998579, 119.9999999999997868, 10.00000000000000000 ) ) ;
#1631=EDGE_CURVE ( 'NONE', #16182, #69681, #26785, .T. ) ;
#1633=ORIENTED_EDGE ( 'NONE', *, *, #46764, .T. ) ;
#1634=( LENGTH_UNIT ( ) NAMED_UNIT ( * ) SI_UNIT ( .MILLI., .METRE. ) );
#1635=CIRCLE ( 'NONE', #50027, 13.99999999999999822 ) ;
#1637=AXIS2_PLACEMENT_3D ( 'NONE', #41069, #3710, #52317 ) ;
#1638=EDGE_CURVE ( 'NONE', #24543, #61513, #25382, .T. ) ;
#1639=( LENGTH_UNIT ( ) NAMED_UNIT ( * ) SI_UNIT ( .MILLI., .METRE. ) );
#1640=DIRECTION ( 'NONE',  ( 0.000000000000000000, -1.000000000000000000, 0.000000000000000000 ) ) ;
#1641=( BOUNDED_SURFACE ( )  B_SPLINE_SURFACE ( 3, 2, ( 
 ( #832, #59649, #11466 ),
 ( #38942, #48455, #54708 ),
 ( #5828, #146, #21676 ),
 ( #32938, #6514, #43196 ),
 ( #64601, #27957, #16448 ),
 ( #49466, #65630, #55058 ),
 ( #40659, #8633, #34319 ),
 ( #18820, #56455, #30063 ),
 ( #12853, #3292, #55772 ),
 ( #2601, #45254, #45610 ) ),
 .UNSPECIFIED., .F., .F., .F. ) 
 B_SPLINE_SURFACE_WITH_KNOTS ( ( 4, 2, 2, 2, 4 ),
 ( 3, 3 ),
 ( 3.141592653589793116, 3.534291735288517255, 3.926990816987241395, 4.319689898685965090, 4.712388980384689674 ),
 ( 0.000000000000000000, 1.000000000000000000 ),
 .UNSPECIFIED. ) 
 GEOMETRIC_REPRESENTATION_ITEM ( )  RATIONAL_B_SPLINE_SURFACE ( (
 ( 1.000000000000000000, 0.8112421851755602376, 1.000000000000000000),
 ( 1.000000000000000000, 0.8112499556556433955, 1.000000000000000000),
 ( 1.000000000000000000, 0.8087168080150066718, 1.000000000000000000),
 ( 1.000000000000000000, 0.7988629633398904861, 1.000000000000000000),
 ( 1.000000000000000000, 0.7915339219236784407, 1.000000000000000000),
 ( 1.000000000000000000, 0.7728233248393433508, 1.000000000000000000),
 ( 1.000000000000000000, 0.7614408922480963016, 1.000000000000000000),
 ( 1.000000000000000000, 0.7359001690392014128, 1.000000000000000000),
 ( 1.000000000000000000, 0.7217502572879682665, 1.000000000000000000),
 ( 1.000000000000000000, 0.7071067811865475727, 1.000000000000000000) ) ) 
 REPRESENTATION_ITEM ( '' )  SURFACE ( )  );
#1643=CARTESIAN_POINT ( 'NONE',  ( 71.74137931034481142, 36.89918356738973415, -10.00000000000000000 ) ) ;
#1647=( LENGTH_UNIT ( ) NAMED_UNIT ( * ) SI_UNIT ( .MILLI., .METRE. ) );
#1648=DIRECTION ( 'NONE',  ( 1.000000000000000000, 0.000000000000000000, -0.000000000000000000 ) ) ;
#1654=EDGE_LOOP ( 'NONE', ( #63446, #32269, #54881, #12806 ) ) ;
#1655=EDGE_LOOP ( 'NONE', ( #19080, #40394, #14488, #19156 ) ) ;
#1657=CARTESIAN_POINT ( 'NONE',  ( -74.42859372179059108, 8.073499555448577780, -6.500000000000000888 ) ) ;
#1659=SURFACE_STYLE_USAGE ( .BOTH. , #60434 ) ;
#1660=VERTEX_POINT ( 'NONE', #43729 ) ;
#1661=CARTESIAN_POINT ( 'NONE',  ( -6.826472737025120807, 132.3929263765338362, -4.959722759717907437 ) ) ;
#1668=TOROIDAL_SURFACE ( 'NONE', #28618, 8.499999999999998224, 0.5000000000000000000 ) ;
#1672=SURFACE_STYLE_FILL_AREA ( #29489 ) ;
#1673=FILL_AREA_STYLE ('',( #34756 ) ) ;
#1674=EDGE_LOOP ( 'NONE', ( #43799, #46856, #2229, #60113 ) ) ;
#1678=CARTESIAN_POINT ( 'NONE',  ( -45.00000000000000000, 7.768687147774684831, -6.999999999999999112 ) ) ;
#1679=ORIENTED_EDGE ( 'NONE', *, *, #11278, .T. ) ;
#1685=EDGE_LOOP ( 'NONE', ( #59397, #57758, #23436, #341 ) ) ;
#1687=( NAMED_UNIT ( * ) SI_UNIT ( $, .STERADIAN. ) SOLID_ANGLE_UNIT ( ) );
#1689=TOROIDAL_SURFACE ( 'NONE', #36598, 9.499999999999996447, 0.5000000000000000000 ) ;
#1690=AXIS2_PLACEMENT_3D ( 'NONE', #2054, #13035, #33454 ) ;
#1692=SURFACE_STYLE_FILL_AREA ( #49957 ) ;
#1695=VECTOR ( 'NONE', #24083, 1000.000000000000000 ) ;
#1696=DIRECTION ( 'NONE',  ( 0.7071067811865352493, 8.659560562354781249E-17, -0.7071067811865597852 ) ) ;
#1697=LINE ( 'NONE', #55562, #35972 ) ;
#1699=EDGE_CURVE ( 'NONE', #24423, #69362, #16641, .T. ) ;
#1702=CARTESIAN_POINT ( 'NONE',  ( 9.058813317711337021, 115.6549999999999869, 2.943386871421375783 ) ) ;
#1705=DIRECTION ( 'NONE',  ( 0.000000000000000000, -1.000000000000000000, -0.000000000000000000 ) ) ;
#1707=UNCERTAINTY_MEASURE_WITH_UNIT (LENGTH_MEASURE( 1.000000000000000082E-05 ), #61396, 'distance_accuracy_value', 'NONE');
#1708=CIRCLE ( 'NONE', #23156, 0.5000000000000004441 ) ;
#1709=CYLINDRICAL_SURFACE ( 'NONE', #68980, 0.5000000000000004441 ) ;
#1714=SURFACE_SIDE_STYLE ('',( #49980 ) ) ;
#1717=DIRECTION ( 'NONE',  ( -1.000000000000000000, 0.000000000000000000, 0.000000000000000000 ) ) ;
#1719=DIRECTION ( 'NONE',  ( 1.000000000000000000, 0.000000000000000000, 0.000000000000000000 ) ) ;
#1720=EDGE_LOOP ( 'NONE', ( #55191, #20863, #22219, #51454 ) ) ;
#1721=VERTEX_POINT ( 'NONE', #11327 ) ;
#1722=COLOUR_RGB ( '', 0.40784314, 0.44705882, 0.49803922) ;
#1723=DIRECTION ( 'NONE',  ( -0.000000000000000000, -0.000000000000000000, -1.000000000000000000 ) ) ;
#1724=CARTESIAN_POINT ( 'NONE',  ( 71.49999999999998579, 64.07124727947029896, 7.500000000000000000 ) ) ;
#1725=LINE ( 'NONE', #54872, #40584 ) ;
#1726=CARTESIAN_POINT ( 'NONE',  ( -51.50000000000000000, -2.024042244987997205E-14, 10.50000000000000000 ) ) ;
#1728=SPHERICAL_SURFACE ( 'NONE', #52931, 0.5000000000000000000 ) ;
#1732=STYLED_ITEM ( 'NONE', ( #50330 ), #39268 ) ;
#1733=EDGE_CURVE ( 'NONE', #6729, #52429, #35213, .T. ) ;
#1734=ORIENTED_EDGE ( 'NONE', *, *, #43890, .T. ) ;
#1735=CARTESIAN_POINT ( 'NONE',  ( -0.4882456337924103162, 152.9710135830613069, -8.025000000000005684 ) ) ;
#1739=AXIS2_PLACEMENT_3D ( 'NONE', #15953, #4662, #41642 ) ;
#1740=LINE ( 'NONE', #30843, #5683 ) ;
#1741=ADVANCED_FACE ( 'NONE', ( #28162 ), #27492, .F. ) ;
#1742=FACE_OUTER_BOUND ( 'NONE', #52453, .T. ) ;
#1743=CARTESIAN_POINT ( 'NONE',  ( 8.102448949553181734, 132.3949999999999534, 5.886773742842750679 ) ) ;
#1744=ORIENTED_EDGE ( 'NONE', *, *, #38315, .T. ) ;
#1745=CARTESIAN_POINT ( 'NONE',  ( -8.102448949553179958, 141.0049999999999670, -5.886773742842749790 ) ) ;
#1747=CARTESIAN_POINT ( 'NONE',  ( 44.99999999999998579, 119.9999999999999716, 10.00000000000000000 ) ) ;
#1749=CARTESIAN_POINT ( 'NONE',  ( 0.000000000000000000, 161.5550000000000068, -9.525000000000000355 ) ) ;
#1751=UNCERTAINTY_MEASURE_WITH_UNIT (LENGTH_MEASURE( 1.000000000000000082E-05 ), #36044, 'distance_accuracy_value', 'NONE');
#1753=( LENGTH_UNIT ( ) NAMED_UNIT ( * ) SI_UNIT ( .MILLI., .METRE. ) );
#1754=PRESENTATION_STYLE_ASSIGNMENT (( #22929 ) ) ;
#1755=ORIENTED_EDGE ( 'NONE', *, *, #50050, .F. ) ;
#1758=CARTESIAN_POINT ( 'NONE',  ( -74.99999999999998579, 119.9999999999997726, -9.500000000000000000 ) ) ;
#1759=SURFACE_SIDE_STYLE ('',( #50022 ) ) ;
#1764=CARTESIAN_POINT ( 'NONE',  ( 48.50000000000000000, 99.99999999999998579, 7.500000000000000000 ) ) ;
#1766=ORIENTED_EDGE ( 'NONE', *, *, #12022, .F. ) ;
#1775=( BOUNDED_CURVE ( )  B_SPLINE_CURVE ( 2, ( #49571, #53783, #43311, #60108, #6619, #11923, #21433, #64352, #17240, #11226, #16201 ),
 .UNSPECIFIED., .F., .F. ) 
 B_SPLINE_CURVE_WITH_KNOTS ( ( 3, 2, 2, 2, 2, 3 ),
 ( 0.2647058823529411242, 0.2705882352941175739, 0.2764705882352940791, 0.2823529411764705843, 0.2882352941176470340, 0.2941176470588235392 ),
 .UNSPECIFIED. ) 
 CURVE ( )  GEOMETRIC_REPRESENTATION_ITEM ( )  RATIONAL_B_SPLINE_CURVE ( ( 1.000000000000000666, 0.9510565162951531981, 1.000000000000000000, 0.9510565162951535312, 1.000000000000000000, 0.9510565162951535312, 1.000000000000000000, 0.9510565162951535312, 1.000000000000000000, 0.9510565162951535312, 1.000000000000000000 ) ) 
 REPRESENTATION_ITEM ( '' )  );
#1777=CARTESIAN_POINT ( 'NONE',  ( -75.00000000000000000, 8.841134989787066800, -6.848475133234801504 ) ) ;
#1779=DIRECTION ( 'NONE',  ( 1.000000000000000000, 0.000000000000000000, 0.000000000000000000 ) ) ;
#1782=AXIS2_PLACEMENT_3D ( 'NONE', #26676, #58364, #37307 ) ;
#1783=ADVANCED_FACE ( 'NONE', ( #39485 ), #63546, .T. ) ;
#1784=CARTESIAN_POINT ( 'NONE',  ( 3.094860106618435136, 130.2949999999999591, -9.525000000000000355 ) ) ;
#1791=ADVANCED_FACE ( 'NONE', ( #23614 ), #55969, .F. ) ;
#1796=EDGE_LOOP ( 'NONE', ( #11898, #17901, #30240, #23916 ) ) ;
#1800=FACE_BOUND ( 'NONE', #63024, .T. ) ;
#1807=AXIS2_PLACEMENT_3D ( 'NONE', #58819, #22571, #64084 ) ;
#1808=SURFACE_STYLE_USAGE ( .BOTH. , #12757 ) ;
#1809=CARTESIAN_POINT ( 'NONE',  ( 2.607480562269071989, 155.7070736234661297, 8.025000000000002132 ) ) ;
#1815=CARTESIAN_POINT ( 'NONE',  ( 8.102448949553183510, 131.1049999999999898, -5.886773742842746238 ) ) ;
#1817=DIRECTION ( 'NONE',  ( 0.000000000000000000, 0.000000000000000000, 1.000000000000000000 ) ) ;
#1818=SURFACE_STYLE_USAGE ( .BOTH. , #39901 ) ;
#1819=( GEOMETRIC_REPRESENTATION_CONTEXT ( 3 ) GLOBAL_UNCERTAINTY_ASSIGNED_CONTEXT ( ( #30589 ) ) GLOBAL_UNIT_ASSIGNED_CONTEXT ( ( #44578, #59656, #11474 ) ) REPRESENTATION_CONTEXT ( 'NONE', 'WORKASPACE' ) );
#1822=SURFACE_SIDE_STYLE ('',( #39904 ) ) ;
#1825=SURFACE_SIDE_STYLE ('',( #7509 ) ) ;
#1826=PRESENTATION_STYLE_ASSIGNMENT (( #35294 ) ) ;
#1831=CARTESIAN_POINT ( 'NONE',  ( -45.00000000000000000, 8.062885781073932279, -5.999999999999994671 ) ) ;
#1838=CARTESIAN_POINT ( 'NONE',  ( -75.00000000000000000, 9.371995676438187317, 6.584629826274253084 ) ) ;
#1841=CARTESIAN_POINT ( 'NONE',  ( -4.716976649647097730, 118.3570736234661638, -6.492361379858953896 ) ) ;
#1843=( NAMED_UNIT ( * ) SI_UNIT ( $, .STERADIAN. ) SOLID_ANGLE_UNIT ( ) );
#1847=CARTESIAN_POINT ( 'NONE',  ( -9.058813317711337021, 143.0449999999999875, -2.943386871421374895 ) ) ;
#1851=EDGE_CURVE ( 'NONE', #21243, #7407, #37805, .T. ) ;
#1855=EDGE_CURVE ( 'NONE', #49204, #16450, #7425, .T. ) ;
#1856=LINE ( 'NONE', #54338, #19580 ) ;
#1858=DIRECTION ( 'NONE',  ( -0.000000000000000000, 1.000000000000000000, 0.000000000000000000 ) ) ;
#1863=EDGE_CURVE ( 'NONE', #47273, #12421, #35916, .T. ) ;
#1867=FILL_AREA_STYLE ('',( #38215 ) ) ;
#1868=ADVANCED_FACE ( 'NONE', ( #10223 ), #41222, .F. ) ;
#1872=CARTESIAN_POINT ( 'NONE',  ( 44.99999999999977263, 147.4999999999999716, 10.00000000000000000 ) ) ;
#1882=( LENGTH_UNIT ( ) NAMED_UNIT ( * ) SI_UNIT ( .MILLI., .METRE. ) );
#1884=FACE_OUTER_BOUND ( 'NONE', #26846, .T. ) ;
#1886=CARTESIAN_POINT ( 'NONE',  ( -23.21231517720797655, 118.4999999999999716, -7.500000000000000000 ) ) ;
#1887=CARTESIAN_POINT ( 'NONE',  ( 8.437984349512095861, 120.3070736234661382, 1.550032578732817026E-15 ) ) ;
#1888=CARTESIAN_POINT ( 'NONE',  ( 20.83091330386927353, 149.9514755777528023, 9.751095921151032186 ) ) ;
#1889=AXIS2_PLACEMENT_3D ( 'NONE', #49833, #7264, #6904 ) ;
#1894=CARTESIAN_POINT ( 'NONE',  ( 7.632228543268607446, 150.1570736234661751, 2.479861379858954606 ) ) ;
#1896=( NAMED_UNIT ( * ) PLANE_ANGLE_UNIT ( ) SI_UNIT ( $, .RADIAN. ) );
#1900=CARTESIAN_POINT ( 'NONE',  ( 0.000000000000000000, 154.4258142642185305, -9.450814264218562855 ) ) ;
#1903=SURFACE_SIDE_STYLE ('',( #5848 ) ) ;
#1904=VECTOR ( 'NONE', #13869, 1000.000000000000000 ) ;
#1907=ORIENTED_EDGE ( 'NONE', *, *, #2071, .T. ) ;
#1911=CYLINDRICAL_SURFACE ( 'NONE', #25691, 0.5000000000000004441 ) ;
#1916=EDGE_CURVE ( 'NONE', #24423, #11684, #20782, .T. ) ;
#1919=CARTESIAN_POINT ( 'NONE',  ( -34.99999999999992895, 112.9999999999999858, 7.000000000000000000 ) ) ;
#1922=( NAMED_UNIT ( * ) PLANE_ANGLE_UNIT ( ) SI_UNIT ( $, .RADIAN. ) );
#1925=CARTESIAN_POINT ( 'NONE',  ( -40.99999999999997868, 9.999999999999978684, -3.000000000000000444 ) ) ;
#1930=DIRECTION ( 'NONE',  ( 0.000000000000000000, 1.000000000000000000, 0.000000000000000000 ) ) ;
#1931=DIRECTION ( 'NONE',  ( -0.000000000000000000, -0.000000000000000000, -1.000000000000000000 ) ) ;
#1932=STYLED_ITEM ( 'NONE', ( #2654 ), #67274 ) ;
#1933=EDGE_CURVE ( 'NONE', #67575, #60632, #52084, .T. ) ;
#1934=LINE ( 'NONE', #19568, #57474 ) ;
#1937=CARTESIAN_POINT ( 'NONE',  ( -23.71231517720798010, 113.4999999999999858, -7.500000000000000000 ) ) ;
#1940=CARTESIAN_POINT ( 'NONE',  ( -9.058813317711338797, 147.4550000000000125, 2.943386871421373563 ) ) ;
#1941=( GEOMETRIC_REPRESENTATION_CONTEXT ( 3 ) GLOBAL_UNCERTAINTY_ASSIGNED_CONTEXT ( ( #64365 ) ) GLOBAL_UNIT_ASSIGNED_CONTEXT ( ( #6172, #65257, #12473 ) ) REPRESENTATION_CONTEXT ( 'NONE', 'WORKASPACE' ) );
#1945=FACE_OUTER_BOUND ( 'NONE', #16092, .T. ) ;
#1946=( GEOMETRIC_REPRESENTATION_CONTEXT ( 3 ) GLOBAL_UNCERTAINTY_ASSIGNED_CONTEXT ( ( #29065 ) ) GLOBAL_UNIT_ASSIGNED_CONTEXT ( ( #28549, #6078, #22259 ) ) REPRESENTATION_CONTEXT ( 'NONE', 'WORKASPACE' ) );
#1947=DIRECTION ( 'NONE',  ( -0.9704308468600219006, 0.2413793103448194366, -0.000000000000000000 ) ) ;
#1948=SURFACE_SIDE_STYLE ('',( #6585 ) ) ;
#1949=DIRECTION ( 'NONE',  ( -1.274184670190250597E-16, 1.000000000000000000, 2.430666987508112707E-16 ) ) ;
#1954=EDGE_CURVE ( 'NONE', #68674, #68077, #15517, .T. ) ;
#1955=CARTESIAN_POINT ( 'NONE',  ( -45.00000000000000000, 9.119539144243722362, 6.744166081069411511 ) ) ;
#1961=EDGE_LOOP ( 'NONE', ( #38716, #66795 ) ) ;
#1964=CARTESIAN_POINT ( 'NONE',  ( -10.01517768586949231, 111.3049999999999784, -6.132527647946036459E-16 ) ) ;
#1965=DIRECTION ( 'NONE',  ( 1.000000000000000000, 0.000000000000000000, 0.000000000000000000 ) ) ;
#1968=ORIENTED_EDGE ( 'NONE', *, *, #20890, .F. ) ;
#1971=( NAMED_UNIT ( * ) PLANE_ANGLE_UNIT ( ) SI_UNIT ( $, .RADIAN. ) );
#1975=CARTESIAN_POINT ( 'NONE',  ( 7.632228543268608334, 131.3429263765338249, -2.479861379858951942 ) ) ;
#1978=MECHANICAL_DESIGN_GEOMETRIC_PRESENTATION_REPRESENTATION('',(#28996),#50373);
#1981=DIRECTION ( 'NONE',  ( 1.000000000000000000, 0.000000000000000000, 0.000000000000000000 ) ) ;
#1988=FILL_AREA_STYLE_COLOUR ( '', #62186 ) ;
#1990=FACE_OUTER_BOUND ( 'NONE', #59284, .T. ) ;
#1991=SURFACE_SIDE_STYLE ('',( #17253 ) ) ;
#1993=ADVANCED_FACE ( 'NONE', ( #15861 ), #23429, .F. ) ;
#1994=CARTESIAN_POINT ( 'NONE',  ( -41.49999999999998579, 106.9282032302754999, 4.000000000000000000 ) ) ;
#1995=CARTESIAN_POINT ( 'NONE',  ( 14.98999599679679662, 146.4999999999999716, 10.00000000000000000 ) ) ;
#1998=VECTOR ( 'NONE', #11601, 1000.000000000000000 ) ;
#2000=CYLINDRICAL_SURFACE ( 'NONE', #13705, 0.5000000000000004441 ) ;
#2006=FILL_AREA_STYLE ('',( #54156 ) ) ;
#2008=EDGE_CURVE ( 'NONE', #25443, #68774, #23034, .T. ) ;
#2015=CARTESIAN_POINT ( 'NONE',  ( 20.94636006565341191, 149.9999999999999716, 9.500000000000000000 ) ) ;
#2018=CARTESIAN_POINT ( 'NONE',  ( 8.102448949553181734, 115.5049999999999812, 5.886773742842750679 ) ) ;
#2032=AXIS2_PLACEMENT_3D ( 'NONE', #2468, #7114, #12725 ) ;
#2034=SURFACE_STYLE_USAGE ( .BOTH. , #28831 ) ;
#2039=DIRECTION ( 'NONE',  ( -0.000000000000000000, -0.000000000000000000, 1.000000000000000000 ) ) ;
#2040=SURFACE_SIDE_STYLE ('',( #30561 ) ) ;
#2041=EDGE_CURVE ( 'NONE', #69341, #849, #65697, .T. ) ;
#2042=CYLINDRICAL_SURFACE ( 'NONE', #45127, 26.99999999999999645 ) ;
#2044=CARTESIAN_POINT ( 'NONE',  ( 34.99999999999999289, 99.99999999999998579, 9.500000000000000000 ) ) ;
#2045=CARTESIAN_POINT ( 'NONE',  ( -12.72792206135785698, 114.9999999999999574, -10.50000000000000000 ) ) ;
#2046=EDGE_LOOP ( 'NONE', ( #10391, #5930, #64883, #11389 ) ) ;
#2048=VERTEX_POINT ( 'NONE', #54736 ) ;
#2051=SPHERICAL_SURFACE ( 'NONE', #28727, 0.5000000000000000000 ) ;
#2052=VERTEX_POINT ( 'NONE', #11845 ) ;
#2054=CARTESIAN_POINT ( 'NONE',  ( -74.99999999999998579, 50.00000000000000000, 11.50000000000000000 ) ) ;
#2055=( BOUNDED_CURVE ( )  B_SPLINE_CURVE ( 2, ( #5695, #21907, #48678, #43419, #6061 ),
 .UNSPECIFIED., .F., .F. ) 
 B_SPLINE_CURVE_WITH_KNOTS ( ( 3, 2, 3 ),
 ( 0.02072354678354213983, 0.02352941176470589243, 0.02941176470588238029 ),
 .UNSPECIFIED. ) 
 CURVE ( )  GEOMETRIC_REPRESENTATION_ITEM ( )  RATIONAL_B_SPLINE_CURVE ( ( 0.9755800536518703936, 0.9766541028127901924, 1.000000000000000000, 0.9510565162951533091, 1.000000000000000222 ) ) 
 REPRESENTATION_ITEM ( '' )  );
#2056=CARTESIAN_POINT ( 'NONE',  ( 9.058813317711338797, 141.8449999999999989, -2.943386871421372675 ) ) ;
#2057=DIRECTION ( 'NONE',  ( 0.000000000000000000, 0.000000000000000000, -1.000000000000000000 ) ) ;
#2061=CARTESIAN_POINT ( 'NONE',  ( 3.094860106618435136, 143.4050000000000011, -9.525000000000000355 ) ) ;
#2063=FILL_AREA_STYLE ('',( #29197 ) ) ;
#2064=ORIENTED_EDGE ( 'NONE', *, *, #14220, .T. ) ;
#2065=CARTESIAN_POINT ( 'NONE',  ( 9.058813317711338797, 157.9549999999999841, -2.943386871421372675 ) ) ;
#2067=VECTOR ( 'NONE', #61071, 1000.000000000000000 ) ;
#2069=SURFACE_STYLE_FILL_AREA ( #2798 ) ;
#2071=EDGE_CURVE ( 'NONE', #6097, #12107, #64557, .T. ) ;
#2072=VERTEX_POINT ( 'NONE', #6913 ) ;
#2074=PRESENTATION_STYLE_ASSIGNMENT (( #39474 ) ) ;
#2075=ORIENTED_EDGE ( 'NONE', *, *, #11594, .T. ) ;
#2077=TOROIDAL_SURFACE ( 'NONE', #23529, 13.49999999999999822, 0.5000000000000000000 ) ;
#2078=CARTESIAN_POINT ( 'NONE',  ( 0.000000000000000000, 87.30187232391182306, 0.000000000000000000 ) ) ;
#2082=FILL_AREA_STYLE ('',( #1413 ) ) ;
#2084=ADVANCED_FACE ( 'NONE', ( #39306 ), #61184, .T. ) ;
#2085=CYLINDRICAL_SURFACE ( 'NONE', #54345, 0.5000000000000004441 ) ;
#2086=FILL_AREA_STYLE_COLOUR ( '', #60184 ) ;
#2087=ORIENTED_EDGE ( 'NONE', *, *, #1211, .F. ) ;
#2094=EDGE_LOOP ( 'NONE', ( #31610, #22040, #48479, #53765, #19223, #15545, #17600, #48450 ) ) ;
#2097=CARTESIAN_POINT ( 'NONE',  ( 71.49999999999998579, 64.07124727947029896, -7.000000000000000000 ) ) ;
#2098=FACE_OUTER_BOUND ( 'NONE', #34418, .T. ) ;
#2105=CARTESIAN_POINT ( 'NONE',  ( 5.598654528085809545, 139.1449999999999818, -7.705886871421373741 ) ) ;
#2107=EDGE_CURVE ( 'NONE', #53683, #49361, #28699, .T. ) ;
#2109=SURFACE_SIDE_STYLE ('',( #7802 ) ) ;
#2116=CARTESIAN_POINT ( 'NONE',  ( -6.826472737025120807, 129.3929263765338362, -4.959722759717907437 ) ) ;
#2120=AXIS2_PLACEMENT_3D ( 'NONE', #24384, #41302, #36009 ) ;
#2121=CARTESIAN_POINT ( 'NONE',  ( 0.000000000000000000, 110.4999999999999858, -9.525000000000000355 ) ) ;
#2125=EDGE_LOOP ( 'NONE', ( #16141, #49060, #3649, #28198 ) ) ;
#2128=FACE_OUTER_BOUND ( 'NONE', #19966, .T. ) ;
#2129=DIRECTION ( 'NONE',  ( 0.000000000000000000, 0.000000000000000000, -1.000000000000000000 ) ) ;
#2133=CARTESIAN_POINT ( 'NONE',  ( 6.826472737025121695, 156.6070736234661638, -4.959722759717905660 ) ) ;
#2134=( GEOMETRIC_REPRESENTATION_CONTEXT ( 3 ) GLOBAL_UNCERTAINTY_ASSIGNED_CONTEXT ( ( #22848 ) ) GLOBAL_UNIT_ASSIGNED_CONTEXT ( ( #12733, #39868, #7123 ) ) REPRESENTATION_CONTEXT ( 'NONE', 'WORKASPACE' ) );
#2135=ORIENTED_EDGE ( 'NONE', *, *, #40737, .F. ) ;
#2138=CARTESIAN_POINT ( 'NONE',  ( 10.01517768586949408, 115.8049999999999784, 1.839758294383810543E-15 ) ) ;
#2140=SURFACE_STYLE_USAGE ( .BOTH. , #7499 ) ;
#2141=CARTESIAN_POINT ( 'NONE',  ( 3.094860106618431583, 130.2049999999999841, 9.525000000000000355 ) ) ;
#2142=CIRCLE ( 'NONE', #15753, 0.5000000000000004441 ) ;
#2145=CARTESIAN_POINT ( 'NONE',  ( 20.35445791815277161, 114.9981483343694748, 10.00000000000000000 ) ) ;
#2147=FACE_OUTER_BOUND ( 'NONE', #2966, .T. ) ;
#2149=EDGE_LOOP ( 'NONE', ( #32277, #8973, #40586, #52611 ) ) ;
#2150=DIRECTION ( 'NONE',  ( -0.000000000000000000, -0.000000000000000000, -1.000000000000000000 ) ) ;
#2151=CIRCLE ( 'NONE', #56147, 0.5000000000000006661 ) ;
#2153=ORIENTED_EDGE ( 'NONE', *, *, #63854, .F. ) ;
#2159=DIRECTION ( 'NONE',  ( -1.000000000000000000, 0.000000000000000000, 0.000000000000000000 ) ) ;
#2160=VERTEX_POINT ( 'NONE', #62102 ) ;
#2165=CARTESIAN_POINT ( 'NONE',  ( -74.15772097241708138, 9.150846973920840455, 6.292314909082026730 ) ) ;
#2169=AXIS2_PLACEMENT_3D ( 'NONE', #7764, #24622, #8816 ) ;
#2170=LINE ( 'NONE', #6824, #63953 ) ;
#2176=CARTESIAN_POINT ( 'NONE',  ( -1.166476076187854022E-15, 146.9449999999999932, 9.525000000000000355 ) ) ;
#2178=COLOUR_RGB ( '', 0.08235294, 0.09019608, 0.10196078) ;
#2179=CARTESIAN_POINT ( 'NONE',  ( -71.49999999999998579, 50.00000000000000000, 7.500000000000000000 ) ) ;
#2182=SURFACE_STYLE_FILL_AREA ( #38901 ) ;
#2183=PRESENTATION_STYLE_ASSIGNMENT (( #50454 ) ) ;
#2184=CARTESIAN_POINT ( 'NONE',  ( -24.21231517720798010, 113.4999999999999858, -9.500000000000000000 ) ) ;
#2187=FACE_OUTER_BOUND ( 'NONE', #39719, .T. ) ;
#2188=CARTESIAN_POINT ( 'NONE',  ( -3.094860106618434248, 113.7950000000000017, 9.525000000000000355 ) ) ;
#2190=TOROIDAL_SURFACE ( 'NONE', #42791, 13.50000000000000178, 0.5000000000000000000 ) ;
#2192=DIRECTION ( 'NONE',  ( -0.000000000000000000, -0.000000000000000000, -1.000000000000000000 ) ) ;
#2197=CARTESIAN_POINT ( 'NONE',  ( -15.98999599679679839, 146.9999999999999716, -7.000000000000000000 ) ) ;
#2198=SURFACE_STYLE_FILL_AREA ( #39949 ) ;
#2203=DIRECTION ( 'NONE',  ( 0.000000000000000000, 0.000000000000000000, -1.000000000000000000 ) ) ;
#2204=FACE_OUTER_BOUND ( 'NONE', #25068, .T. ) ;
#2206=AXIS2_PLACEMENT_3D ( 'NONE', #42196, #5501, #69549 ) ;
#2210=DIRECTION ( 'NONE',  ( 0.000000000000000000, 0.000000000000000000, 1.000000000000000000 ) ) ;
#2212=SURFACE_STYLE_USAGE ( .BOTH. , #38931 ) ;
#2213=DIRECTION ( 'NONE',  ( 1.000000000000000000, 0.000000000000000000, 0.000000000000000000 ) ) ;
#2217=CIRCLE ( 'NONE', #40487, 1.000000000000000888 ) ;
#2219=( GEOMETRIC_REPRESENTATION_CONTEXT ( 3 ) GLOBAL_UNCERTAINTY_ASSIGNED_CONTEXT ( ( #3136 ) ) GLOBAL_UNIT_ASSIGNED_CONTEXT ( ( #12265, #65048, #59788 ) ) REPRESENTATION_CONTEXT ( 'NONE', 'WORKASPACE' ) );
#2222=AXIS2_PLACEMENT_3D ( 'NONE', #12572, #11543, #1276 ) ;
#2223=CARTESIAN_POINT ( 'NONE',  ( 6.826472737025119919, 120.0070736234661553, 4.959722759717908325 ) ) ;
#2226=CARTESIAN_POINT ( 'NONE',  ( -60.00000000000000000, -2.024042244987997205E-14, 9.500000000000000000 ) ) ;
#2229=ORIENTED_EDGE ( 'NONE', *, *, #50611, .F. ) ;
#2231=CARTESIAN_POINT ( 'NONE',  ( -44.99999999999977973, 149.4999999999999716, 10.00000000000000000 ) ) ;
#2232=CARTESIAN_POINT ( 'NONE',  ( 15.48999599679679662, 146.9999999999999716, 9.500000000000000000 ) ) ;
#2233=CIRCLE ( 'NONE', #41670, 0.5000000000000004441 ) ;
#2237=EDGE_LOOP ( 'NONE', ( #52641, #18976, #63639, #50020, #406, #65293 ) ) ;
#2240=EDGE_CURVE ( 'NONE', #40785, #2052, #51105, .T. ) ;
#2241=UNCERTAINTY_MEASURE_WITH_UNIT (LENGTH_MEASURE( 1.000000000000000082E-05 ), #47721, 'distance_accuracy_value', 'NONE');
#2242=ORIENTED_EDGE ( 'NONE', *, *, #45483, .F. ) ;
#2244=( GEOMETRIC_REPRESENTATION_CONTEXT ( 3 ) GLOBAL_UNCERTAINTY_ASSIGNED_CONTEXT ( ( #18558 ) ) GLOBAL_UNIT_ASSIGNED_CONTEXT ( ( #33255, #6489, #27932 ) ) REPRESENTATION_CONTEXT ( 'NONE', 'WORKASPACE' ) );
#2247=ORIENTED_EDGE ( 'NONE', *, *, #44208, .F. ) ;
#2248=( NAMED_UNIT ( * ) PLANE_ANGLE_UNIT ( ) SI_UNIT ( $, .RADIAN. ) );
#2251=PRESENTATION_STYLE_ASSIGNMENT (( #17499 ) ) ;
#2252=CARTESIAN_POINT ( 'NONE',  ( -60.00000000000000000, -2.024042244987997205E-14, -12.00000000000000000 ) ) ;
#2255=STYLED_ITEM ( 'NONE', ( #7634 ), #59871 ) ;
#2257=CARTESIAN_POINT ( 'NONE',  ( -9.058813317711338797, 113.3449999999999847, 2.943386871421373563 ) ) ;
#2263=ORIENTED_EDGE ( 'NONE', *, *, #55554, .F. ) ;
#2265=DIRECTION ( 'NONE',  ( 1.000000000000000000, 0.000000000000000000, 0.000000000000000000 ) ) ;
#2266=ORIENTED_EDGE ( 'NONE', *, *, #61589, .T. ) ;
#2275=VECTOR ( 'NONE', #13608, 1000.000000000000000 ) ;
#2277=LINE ( 'NONE', #19905, #15497 ) ;
#2283=CARTESIAN_POINT ( 'NONE',  ( -9.058813317711337021, 147.1549999999999727, -2.943386871421374895 ) ) ;
#2284=DIRECTION ( 'NONE',  ( 1.000000000000000000, 0.000000000000000000, 0.000000000000000000 ) ) ;
#2289=CARTESIAN_POINT ( 'NONE',  ( 2.128399401614408669E-13, 154.1464374838464266, 9.171437483846471395 ) ) ;
#2292=LINE ( 'NONE', #44971, #1178 ) ;
#2295=DIRECTION ( 'NONE',  ( -0.000000000000000000, -1.000000000000000000, 0.000000000000000000 ) ) ;
#2301=COLOUR_RGB ( '', 0.72549020, 0.75294118, 0.79215686) ;
#2302=PRESENTATION_STYLE_ASSIGNMENT (( #24862 ) ) ;
#2305=EDGE_CURVE ( 'NONE', #12184, #14271, #61069, .T. ) ;
#2307=ORIENTED_EDGE ( 'NONE', *, *, #53747, .T. ) ;
#2309=ORIENTED_EDGE ( 'NONE', *, *, #52854, .F. ) ;
#2310=CYLINDRICAL_SURFACE ( 'NONE', #30887, 8.999999999999994671 ) ;
#2311=SURFACE_STYLE_FILL_AREA ( #44316 ) ;
#2312=ADVANCED_FACE ( 'NONE', ( #11730 ), #7157, .T. ) ;
#2314=CARTESIAN_POINT ( 'NONE',  ( 60.00000000000000000, 1.797044900979284448E-15, 12.00000000000000000 ) ) ;
#2316=EDGE_LOOP ( 'NONE', ( #2064, #58531, #51021, #55262, #12760, #47189, #49016, #60845, #46783, #49150, #16273, #54383, #35609, #26887, #4168, #57985, #52372, #63290, #69459, #15058 ) ) ;
#2317=STYLED_ITEM ( 'NONE', ( #33777 ), #21691 ) ;
#2319=CARTESIAN_POINT ( 'NONE',  ( 74.99999999999998579, 50.00000000000000000, 7.500000000000000000 ) ) ;
#2320=AXIS2_PLACEMENT_3D ( 'NONE', #35367, #24430, #13187 ) ;
#2321=CARTESIAN_POINT ( 'NONE',  ( -47.50000000000000000, 99.99999999999992895, -10.00000000000000000 ) ) ;
#2324=CIRCLE ( 'NONE', #116, 8.500000000000007105 ) ;
#2329=DIRECTION ( 'NONE',  ( 0.000000000000000000, 0.000000000000000000, 1.000000000000000000 ) ) ;
#2330=ORIENTED_EDGE ( 'NONE', *, *, #34952, .F. ) ;
#2331=CARTESIAN_POINT ( 'NONE',  ( -6.826472737025120807, 147.3929263765337794, -4.959722759717907437 ) ) ;
#2332=CARTESIAN_POINT ( 'NONE',  ( 15.98999599679679839, 146.4999999999999716, 7.000000000000000000 ) ) ;
#2334=CIRCLE ( 'NONE', #61949, 0.5000000000000004441 ) ;
#2336=ORIENTED_EDGE ( 'NONE', *, *, #42742, .F. ) ;
#2337=CIRCLE ( 'NONE', #41712, 0.5000000000000004441 ) ;
#2338=LINE ( 'NONE', #62863, #19512 ) ;
#2340=FACE_OUTER_BOUND ( 'NONE', #59199, .T. ) ;
#2345=DIRECTION ( 'NONE',  ( 1.000000000000000000, 0.000000000000000000, 0.000000000000000000 ) ) ;
#2346=ORIENTED_EDGE ( 'NONE', *, *, #10261, .T. ) ;
#2347=AXIS2_PLACEMENT_3D ( 'NONE', #43451, #65881, #11367 ) ;
#2348=SURFACE_STYLE_USAGE ( .BOTH. , #46777 ) ;
#2351=CARTESIAN_POINT ( 'NONE',  ( -45.00000000000000000, 9.117000356772807734, -6.738247770644822054 ) ) ;
#2354=ORIENTED_EDGE ( 'NONE', *, *, #62987, .F. ) ;
#2355=( LENGTH_UNIT ( ) NAMED_UNIT ( * ) SI_UNIT ( .MILLI., .METRE. ) );
#2356=CARTESIAN_POINT ( 'NONE',  ( -20.56536453975222756, 115.3173173917729173, 10.00000000000000000 ) ) ;
#2359=ORIENTED_EDGE ( 'NONE', *, *, #20850, .F. ) ;
#2365=CARTESIAN_POINT ( 'NONE',  ( -60.00000000000000000, -2.024042244987997205E-14, -7.000000000000024869 ) ) ;
#2370=COLOUR_RGB ( '', 0.09019608, 0.27058824, 0.51372549) ;
#2372=CARTESIAN_POINT ( 'NONE',  ( 8.706197787039554825, 154.4999999999999147, -3.888687344776530885 ) ) ;
#2374=CARTESIAN_POINT ( 'NONE',  ( -55.00000000000000000, -2.024042244987997205E-14, -12.00000000000000000 ) ) ;
#2377=CARTESIAN_POINT ( 'NONE',  ( -9.058813317711337021, 114.1549999999999869, -2.943386871421374895 ) ) ;
#2383=UNCERTAINTY_MEASURE_WITH_UNIT (LENGTH_MEASURE( 1.000000000000000082E-05 ), #3755, 'distance_accuracy_value', 'NONE');
#2392=CYLINDRICAL_SURFACE ( 'NONE', #48244, 8.025000000000000355 ) ;
#2394=EDGE_CURVE ( 'NONE', #2414, #7688, #21767, .T. ) ;
#2400=DIRECTION ( 'NONE',  ( 0.000000000000000000, 1.000000000000000000, 0.000000000000000000 ) ) ;
#2401=CARTESIAN_POINT ( 'NONE',  ( 0.000000000000000000, 115.4999999999999574, 16.50000000000000000 ) ) ;
#2404=DIRECTION ( 'NONE',  ( 0.000000000000000000, 0.000000000000000000, -1.000000000000000000 ) ) ;
#2411=VERTEX_POINT ( 'NONE', #19433 ) ;
#2414=VERTEX_POINT ( 'NONE', #40931 ) ;
#2416=CIRCLE ( 'NONE', #29430, 22.50000000000000000 ) ;
#2418=DIRECTION ( 'NONE',  ( 0.000000000000000000, 0.000000000000000000, 1.000000000000000000 ) ) ;
#2419=CARTESIAN_POINT ( 'NONE',  ( 9.058813317711338797, 135.8449999999999989, -2.943386871421372675 ) ) ;
#2421=VERTEX_POINT ( 'NONE', #34234 ) ;
#2424=CARTESIAN_POINT ( 'NONE',  ( -5.598654528085806881, 137.8549999999999898, -7.705886871421374629 ) ) ;
#2426=( LENGTH_UNIT ( ) NAMED_UNIT ( * ) SI_UNIT ( .MILLI., .METRE. ) );
#2427=ADVANCED_FACE ( 'NONE', ( #28925 ), #13816, .T. ) ;
#2429=ORIENTED_EDGE ( 'NONE', *, *, #19167, .T. ) ;
#2430=CARTESIAN_POINT ( 'NONE',  ( -4.716976649647097730, 117.2429263765338163, -6.492361379858953896 ) ) ;
#2431=DIRECTION ( 'NONE',  ( -0.000000000000000000, -1.000000000000000000, -0.000000000000000000 ) ) ;
#2433=AXIS2_PLACEMENT_3D ( 'NONE', #68780, #10385, #31108 ) ;
#2439=( LENGTH_UNIT ( ) NAMED_UNIT ( * ) SI_UNIT ( .MILLI., .METRE. ) );
#2442=CARTESIAN_POINT ( 'NONE',  ( -70.87837837837835764, 13.70805908423323949, 9.500000000000000000 ) ) ;
#2449=AXIS2_PLACEMENT_3D ( 'NONE', #60100, #28770, #27718 ) ;
#2450=DIRECTION ( 'NONE',  ( 1.000000000000000000, 0.000000000000000000, 0.000000000000000000 ) ) ;
#2451=PRESENTATION_STYLE_ASSIGNMENT (( #29224 ) ) ;
#2452=FILL_AREA_STYLE ('',( #12705 ) ) ;
#2460=FILL_AREA_STYLE_COLOUR ( '', #22760 ) ;
#2461=DIRECTION ( 'NONE',  ( -1.000000000000000000, 0.000000000000000000, 0.000000000000000000 ) ) ;
#2464=AXIS2_PLACEMENT_3D ( 'NONE', #34955, #56400, #56047 ) ;
#2468=CARTESIAN_POINT ( 'NONE',  ( 41.49999999999997868, 9.999999999999980460, 3.000000000000000000 ) ) ;
#2470=CARTESIAN_POINT ( 'NONE',  ( 3.094860106618435136, 142.2950000000000159, -9.525000000000000355 ) ) ;
#2474=AXIS2_PLACEMENT_3D ( 'NONE', #30122, #24853, #47059 ) ;
#2477=SURFACE_STYLE_USAGE ( .BOTH. , #50733 ) ;
#2479=COLOUR_RGB ( '', 0.72549020, 0.75294118, 0.79215686) ;
#2484=EDGE_CURVE ( 'NONE', #6265, #30255, #38713, .T. ) ;
#2489=CARTESIAN_POINT ( 'NONE',  ( -7.632228543268608334, 129.8429263765338249, 2.479861379858952830 ) ) ;
#2493=EDGE_CURVE ( 'NONE', #39125, #5467, #47624, .T. ) ;
#2494=FILL_AREA_STYLE_COLOUR ( '', #60778 ) ;
#2502=VECTOR ( 'NONE', #66181, 1000.000000000000000 ) ;
#2505=CYLINDRICAL_SURFACE ( 'NONE', #61236, 4.999999999999997335 ) ;
#2506=ORIENTED_EDGE ( 'NONE', *, *, #54300, .F. ) ;
#2508=( NAMED_UNIT ( * ) SI_UNIT ( $, .STERADIAN. ) SOLID_ANGLE_UNIT ( ) );
#2510=CARTESIAN_POINT ( 'NONE',  ( -1.166476076187854022E-15, 110.9449999999999932, 9.525000000000000355 ) ) ;
#2511=AXIS2_PLACEMENT_3D ( 'NONE', #35926, #24641, #36995 ) ;
#2512=EDGE_LOOP ( 'NONE', ( #675, #60942, #31621 ) ) ;
#2514=CARTESIAN_POINT ( 'NONE',  ( 0.000000000000000000, 110.5549999999999926, -9.525000000000000355 ) ) ;
#2517=CARTESIAN_POINT ( 'NONE',  ( 10.01517768586949231, 124.8049999999999642, 1.839758294383810543E-15 ) ) ;
#2518=UNCERTAINTY_MEASURE_WITH_UNIT (LENGTH_MEASURE( 1.000000000000000082E-05 ), #25440, 'distance_accuracy_value', 'NONE');
#2525=CIRCLE ( 'NONE', #9326, 0.5000000000000004441 ) ;
#2526=FACE_OUTER_BOUND ( 'NONE', #13806, .T. ) ;
#2528=EDGE_LOOP ( 'NONE', ( #8203, #68573, #5606, #57331 ) ) ;
#2533=ORIENTED_EDGE ( 'NONE', *, *, #32733, .F. ) ;
#2536=FACE_OUTER_BOUND ( 'NONE', #18430, .T. ) ;
#2537=ORIENTED_EDGE ( 'NONE', *, *, #9870, .T. ) ;
#2538=CARTESIAN_POINT ( 'NONE',  ( -75.00000000000000000, 9.675838479951730520, 6.195399861057270030 ) ) ;
#2541=( NAMED_UNIT ( * ) SI_UNIT ( $, .STERADIAN. ) SOLID_ANGLE_UNIT ( ) );
#2543=DIRECTION ( 'NONE',  ( 1.156482317317873451E-16, 1.000000000000000000, 0.000000000000000000 ) ) ;
#2545=COLOUR_RGB ( '', 0.40784314, 0.44705882, 0.49803922) ;
#2546=DIRECTION ( 'NONE',  ( -0.000000000000000000, -1.000000000000000000, -0.000000000000000000 ) ) ;
#2547=CARTESIAN_POINT ( 'NONE',  ( 9.058813317711338797, 138.8449999999999989, -2.943386871421372675 ) ) ;
#2550=MECHANICAL_DESIGN_GEOMETRIC_PRESENTATION_REPRESENTATION('',(#29722),#45324);
#2553=( NAMED_UNIT ( * ) SI_UNIT ( $, .STERADIAN. ) SOLID_ANGLE_UNIT ( ) );
#2554=DIRECTION ( 'NONE',  ( 0.000000000000000000, 0.000000000000000000, 1.000000000000000000 ) ) ;
#2558=CARTESIAN_POINT ( 'NONE',  ( -74.99999999999998579, 50.00000000000000000, 6.999999999999988454 ) ) ;
#2559=DIRECTION ( 'NONE',  ( 1.000000000000000000, 0.000000000000000000, 0.000000000000000000 ) ) ;
#2560=SURFACE_SIDE_STYLE ('',( #38207 ) ) ;
#2563=CARTESIAN_POINT ( 'NONE',  ( -45.48309787872866394, 9.683080749504640039, -3.000000000000000444 ) ) ;
#2566=CIRCLE ( 'NONE', #3681, 0.5000000000000004441 ) ;
#2568=ADVANCED_FACE ( 'NONE', ( #63726 ), #42673, .F. ) ;
#2579=DIRECTION ( 'NONE',  ( 0.000000000000000000, 0.000000000000000000, 1.000000000000000000 ) ) ;
#2584=FILL_AREA_STYLE_COLOUR ( '', #29362 ) ;
#2585=AXIS2_PLACEMENT_3D ( 'NONE', #13472, #8224, #30005 ) ;
#2587=CARTESIAN_POINT ( 'NONE',  ( -12.72792206135785698, 114.9999999999999574, 10.50000000000000000 ) ) ;
#2590=SURFACE_STYLE_FILL_AREA ( #9320 ) ;
#2593=FACE_OUTER_BOUND ( 'NONE', #50511, .T. ) ;
#2595=CARTESIAN_POINT ( 'NONE',  ( -7.632228543268608334, 133.9570736234661581, 2.479861379858952830 ) ) ;
#2596=AXIS2_PLACEMENT_3D ( 'NONE', #8731, #56207, #51300 ) ;
#2597=CARTESIAN_POINT ( 'NONE',  ( -4.716976649647097730, 133.3570736234661638, -6.492361379858953896 ) ) ;
#2598=CIRCLE ( 'NONE', #64471, 0.5000000000000004441 ) ;
#2601=CARTESIAN_POINT ( 'NONE',  ( 74.50000000000000000, 19.30628705663858469, -6.500000000000000888 ) ) ;
#2604=( GEOMETRIC_REPRESENTATION_CONTEXT ( 3 ) GLOBAL_UNCERTAINTY_ASSIGNED_CONTEXT ( ( #64455 ) ) GLOBAL_UNIT_ASSIGNED_CONTEXT ( ( #35889, #62268, #14095 ) ) REPRESENTATION_CONTEXT ( 'NONE', 'WORKASPACE' ) );
#2606=AXIS2_PLACEMENT_3D ( 'NONE', #33685, #66745, #28741 ) ;
#2607=PLANE ( 'NONE',  #20415 ) ;
#2610=DIRECTION ( 'NONE',  ( -0.000000000000000000, -0.000000000000000000, -1.000000000000000000 ) ) ;
#2619=CARTESIAN_POINT ( 'NONE',  ( -12.34222745343792127, 115.4999999999999574, -10.18181818181818166 ) ) ;
#2621=SURFACE_STYLE_USAGE ( .BOTH. , #61049 ) ;
#2625=FILL_AREA_STYLE ('',( #19537 ) ) ;
#2627=CARTESIAN_POINT ( 'NONE',  ( -74.99999999999998579, 50.00000000000000000, -12.00000000000000000 ) ) ;
#2628=DIRECTION ( 'NONE',  ( -1.000000000000000000, 0.000000000000000000, 0.000000000000000000 ) ) ;
#2630=( GEOMETRIC_REPRESENTATION_CONTEXT ( 3 ) GLOBAL_UNCERTAINTY_ASSIGNED_CONTEXT ( ( #43168 ) ) GLOBAL_UNIT_ASSIGNED_CONTEXT ( ( #37204, #58613, #41428 ) ) REPRESENTATION_CONTEXT ( 'NONE', 'WORKASPACE' ) );
#2634=CARTESIAN_POINT ( 'NONE',  ( -8.102448949553179958, 116.4949999999999761, 5.886773742842747126 ) ) ;
#2638=ORIENTED_EDGE ( 'NONE', *, *, #36605, .F. ) ;
#2640=DIRECTION ( 'NONE',  ( 0.000000000000000000, 0.000000000000000000, 1.000000000000000000 ) ) ;
#2643=COLOUR_RGB ( '', 0.08235294, 0.09019608, 0.10196078) ;
#2646=CARTESIAN_POINT ( 'NONE',  ( -8.425330761298491566, 111.4667181716287132, -1.555325770122464979 ) ) ;
#2647=EDGE_CURVE ( 'NONE', #65093, #44423, #32397, .T. ) ;
#2652=ORIENTED_EDGE ( 'NONE', *, *, #68224, .F. ) ;
#2654=PRESENTATION_STYLE_ASSIGNMENT (( #57556 ) ) ;
#2660=EDGE_CURVE ( 'NONE', #9513, #6729, #35254, .T. ) ;
#2662=CARTESIAN_POINT ( 'NONE',  ( 9.058813317711337021, 142.6549999999999727, 2.943386871421375783 ) ) ;
#2671=EDGE_CURVE ( 'NONE', #60077, #44927, #34143, .T. ) ;
#2672=CIRCLE ( 'NONE', #38727, 0.5000000000000004441 ) ;
#2674=CARTESIAN_POINT ( 'NONE',  ( -70.87837837837835764, 13.70805908423324482, -10.00000000000000000 ) ) ;
#2677=VERTEX_POINT ( 'NONE', #54885 ) ;
#2679=DIRECTION ( 'NONE',  ( 1.156482317317873451E-16, 1.000000000000000000, -0.000000000000000000 ) ) ;
#2682=VERTEX_POINT ( 'NONE', #16283 ) ;
#2684=PRESENTATION_STYLE_ASSIGNMENT (( #41435 ) ) ;
#2687=ORIENTED_EDGE ( 'NONE', *, *, #8457, .T. ) ;
#2689=VERTEX_POINT ( 'NONE', #21512 ) ;
#2690=MECHANICAL_DESIGN_GEOMETRIC_PRESENTATION_REPRESENTATION('',(#37647),#21893);
#2691=CARTESIAN_POINT ( 'NONE',  ( 15.98999599679679839, 146.4999999999999716, 7.500000000000000000 ) ) ;
#2693=CARTESIAN_POINT ( 'NONE',  ( 23.71231517720798010, 117.9999999999999716, -7.500000000000000000 ) ) ;
#2696=COLOUR_RGB ( '', 0.72549020, 0.75294118, 0.79215686) ;
#2697=CARTESIAN_POINT ( 'NONE',  ( -6.408284378168763062, 110.4999999999999858, -7.060458185319238744 ) ) ;
#2698=DIRECTION ( 'NONE',  ( -0.000000000000000000, -1.000000000000000000, -0.000000000000000000 ) ) ;
#2701=CIRCLE ( 'NONE', #20736, 13.99999999999999822 ) ;
#2703=CARTESIAN_POINT ( 'NONE',  ( -7.632228543268608334, 141.8429263765338249, 2.479861379858952830 ) ) ;
#2705=LINE ( 'NONE', #8392, #4009 ) ;
#2708=ORIENTED_EDGE ( 'NONE', *, *, #14870, .F. ) ;
#2713=CARTESIAN_POINT ( 'NONE',  ( -20.46171737063436424, 114.7896496367841479, 10.31361660310133033 ) ) ;
#2717=EDGE_LOOP ( 'NONE', ( #49165, #24446, #55591, #38167 ) ) ;
#2719=CIRCLE ( 'NONE', #65677, 0.5000000000000004441 ) ;
#2723=VERTEX_POINT ( 'NONE', #43030 ) ;
#2724=ORIENTED_EDGE ( 'NONE', *, *, #40458, .T. ) ;
#2725=CARTESIAN_POINT ( 'NONE',  ( -20.99028635741426640, 114.7785533247281933, 10.00000000000000000 ) ) ;
#2727=CIRCLE ( 'NONE', #57874, 0.5000000000000004441 ) ;
#2733=ADVANCED_FACE ( 'NONE', ( #65468 ), #49647, .T. ) ;
#2736=CIRCLE ( 'NONE', #54488, 23.00000000000000000 ) ;
#2737=CARTESIAN_POINT ( 'NONE',  ( -24.21231517720798010, 112.9999999999999858, -7.000000000000000000 ) ) ;
#2739=EDGE_CURVE ( 'NONE', #32017, #48200, #64779, .T. ) ;
#2741=DIRECTION ( 'NONE',  ( 1.000000000000000000, 0.000000000000000000, 0.000000000000000000 ) ) ;
#2748=EDGE_CURVE ( 'NONE', #31048, #55582, #65577, .T. ) ;
#2750=CARTESIAN_POINT ( 'NONE',  ( -3.094860106618432471, 119.7049999999999983, -9.525000000000000355 ) ) ;
#2752=ADVANCED_FACE ( 'NONE', ( #51031 ), #40152, .T. ) ;
#2759=EDGE_LOOP ( 'NONE', ( #42495, #46925, #52957, #46942 ) ) ;
#2768=DIRECTION ( 'NONE',  ( 1.000000000000000000, 0.000000000000000000, 0.000000000000000000 ) ) ;
#2773=DIRECTION ( 'NONE',  ( 1.000000000000000000, 0.000000000000000000, 0.000000000000000000 ) ) ;
#2776=VERTEX_POINT ( 'NONE', #28853 ) ;
#2778=EDGE_LOOP ( 'NONE', ( #37636, #65071, #57160, #39172 ) ) ;
#2788=CARTESIAN_POINT ( 'NONE',  ( -9.058813317711337021, 140.0449999999999875, -2.943386871421374895 ) ) ;
#2792=CARTESIAN_POINT ( 'NONE',  ( -1.166476076187854022E-15, 142.0549999999999784, 9.525000000000000355 ) ) ;
#2793=CARTESIAN_POINT ( 'NONE',  ( 41.00000000735874295, 108.0041655766031425, -3.104053578549443415 ) ) ;
#2794=ORIENTED_EDGE ( 'NONE', *, *, #18808, .F. ) ;
#2795=CARTESIAN_POINT ( 'NONE',  ( 7.632228543268607446, 113.0429263765338135, 2.479861379858954606 ) ) ;
#2796=FILL_AREA_STYLE_COLOUR ( '', #43601 ) ;
#2798=FILL_AREA_STYLE ('',( #46134 ) ) ;
#2800=FACE_OUTER_BOUND ( 'NONE', #50340, .T. ) ;
#2810=ORIENTED_EDGE ( 'NONE', *, *, #53401, .T. ) ;
#2813=( LENGTH_UNIT ( ) NAMED_UNIT ( * ) SI_UNIT ( .MILLI., .METRE. ) );
#2815=ORIENTED_EDGE ( 'NONE', *, *, #6946, .T. ) ;
#2822=EDGE_CURVE ( 'NONE', #26425, #26262, #16209, .T. ) ;
#2826=CARTESIAN_POINT ( 'NONE',  ( -74.15754429128251957, 9.151528339695955694, -6.292049778185740294 ) ) ;
#2827=VERTEX_POINT ( 'NONE', #45450 ) ;
#2829=DIRECTION ( 'NONE',  ( -1.000000000000000000, -1.156482317317873451E-16, 0.000000000000000000 ) ) ;
#2832=CARTESIAN_POINT ( 'NONE',  ( 5.598654528085805993, 135.2450000000000045, 7.705886871421374629 ) ) ;
#2843=AXIS2_PLACEMENT_3D ( 'NONE', #6701, #60503, #7423 ) ;
#2844=CARTESIAN_POINT ( 'NONE',  ( 0.000000000000000000, 154.4258142642185305, -9.450814264218562855 ) ) ;
#2846=VERTEX_POINT ( 'NONE', #41198 ) ;
#2847=LINE ( 'NONE', #61604, #4711 ) ;
#2848=VERTEX_POINT ( 'NONE', #47533 ) ;
#2849=CARTESIAN_POINT ( 'NONE',  ( -15.48999599679679662, 146.4999999999999716, 7.500000000000000000 ) ) ;
#2850=DIRECTION ( 'NONE',  ( -0.000000000000000000, -0.000000000000000000, -1.000000000000000000 ) ) ;
#2851=DIRECTION ( 'NONE',  ( 0.000000000000000000, 0.000000000000000000, 1.000000000000000000 ) ) ;
#2856=DIRECTION ( 'NONE',  ( -1.387778780781444413E-14, 1.000000000000000000, 0.000000000000000000 ) ) ;
#2858=SURFACE_SIDE_STYLE ('',( #46569 ) ) ;
#2860=CARTESIAN_POINT ( 'NONE',  ( -3.094860106618432471, 115.5949999999999704, -9.525000000000000355 ) ) ;
#2863=MECHANICAL_DESIGN_GEOMETRIC_PRESENTATION_REPRESENTATION('',(#40012),#62461);
#2868=CARTESIAN_POINT ( 'NONE',  ( -7.632228543268608334, 121.9570736234661723, 2.479861379858952830 ) ) ;
#2870=CARTESIAN_POINT ( 'NONE',  ( -10.01517768586949231, 138.3049999999999500, -6.132527647946036459E-16 ) ) ;
#2871=FACE_OUTER_BOUND ( 'NONE', #48118, .T. ) ;
#2873=DIRECTION ( 'NONE',  ( -0.000000000000000000, -0.000000000000000000, -1.000000000000000000 ) ) ;
#2877=AXIS2_PLACEMENT_3D ( 'NONE', #8329, #2640, #39313 ) ;
#2878=( NAMED_UNIT ( * ) SI_UNIT ( $, .STERADIAN. ) SOLID_ANGLE_UNIT ( ) );
#2886=( NAMED_UNIT ( * ) SI_UNIT ( $, .STERADIAN. ) SOLID_ANGLE_UNIT ( ) );
#2888=EDGE_CURVE ( 'NONE', #1408, #37840, #67854, .T. ) ;
#2894=CARTESIAN_POINT ( 'NONE',  ( 45.00000000000000000, 10.69371294336137801, 4.000000000000000000 ) ) ;
#2899=CARTESIAN_POINT ( 'NONE',  ( -10.01517768586949408, 140.1949999999999932, -6.132527647946036459E-16 ) ) ;
#2903=SURFACE_STYLE_USAGE ( .BOTH. , #8247 ) ;
#2905=CARTESIAN_POINT ( 'NONE',  ( 7.632228543268608334, 120.4570736234661723, -2.479861379858951942 ) ) ;
#2908=CARTESIAN_POINT ( 'NONE',  ( 0.000000000000000000, 112.4449999999999932, -9.525000000000000355 ) ) ;
#2910=ADVANCED_FACE ( 'NONE', ( #57332 ), #48801, .T. ) ;
#2913=EDGE_LOOP ( 'NONE', ( #66712, #54153, #48643, #45274, #50930, #55390, #8155, #51464 ) ) ;
#2914=CARTESIAN_POINT ( 'NONE',  ( 60.00000000000000000, 1.797044900979284448E-15, 6.999999999999999112 ) ) ;
#2916=( NAMED_UNIT ( * ) PLANE_ANGLE_UNIT ( ) SI_UNIT ( $, .RADIAN. ) );
#2920=AXIS2_PLACEMENT_3D ( 'NONE', #22129, #48557, #21424 ) ;
#2922=COLOUR_RGB ( '', 0.72549020, 0.75294118, 0.79215686) ;
#2923=CARTESIAN_POINT ( 'NONE',  ( -48.50000000000000000, 14.49137674618942562, 7.500000000000000000 ) ) ;
#2927=DIRECTION ( 'NONE',  ( -1.000000000000000000, 0.000000000000000000, 0.000000000000000000 ) ) ;
#2928=DIRECTION ( 'NONE',  ( 0.000000000000000000, 1.000000000000000000, -0.000000000000000000 ) ) ;
#2931=CARTESIAN_POINT ( 'NONE',  ( -41.05030025768335378, 107.9631293162025116, 3.671816393059857297 ) ) ;
#2933=DIRECTION ( 'NONE',  ( 1.000000000000000000, 0.000000000000000000, 0.000000000000000000 ) ) ;
#2936=DIRECTION ( 'NONE',  ( -0.000000000000000000, -1.000000000000000000, -0.000000000000000000 ) ) ;
#2937=ORIENTED_EDGE ( 'NONE', *, *, #25977, .T. ) ;
#2938=CARTESIAN_POINT ( 'NONE',  ( -2.607480562268991608, 134.4070736234661467, 8.025000000000060751 ) ) ;
#2939=CARTESIAN_POINT ( 'NONE',  ( 7.632228543268607446, 138.1570736234661467, 2.479861379858954606 ) ) ;
#2948=CARTESIAN_POINT ( 'NONE',  ( -9.827790563157511022E-16, 149.5570736234661524, 8.025000000000000355 ) ) ;
#2949=FILL_AREA_STYLE ('',( #51205 ) ) ;
#2954=DIRECTION ( 'NONE',  ( -0.000000000000000000, 0.000000000000000000, 1.000000000000000000 ) ) ;
#2955=LINE ( 'NONE', #35726, #35257 ) ;
#2956=UNCERTAINTY_MEASURE_WITH_UNIT (LENGTH_MEASURE( 1.000000000000000082E-05 ), #69313, 'distance_accuracy_value', 'NONE');
#2959=CIRCLE ( 'NONE', #11958, 5.500000000000005329 ) ;
#2960=EDGE_CURVE ( 'NONE', #38702, #26603, #25417, .T. ) ;
#2961=DIRECTION ( 'NONE',  ( -1.156482317317873451E-16, -1.000000000000000000, 0.000000000000000000 ) ) ;
#2966=EDGE_LOOP ( 'NONE', ( #64750, #1328, #2638, #29923 ) ) ;
#2968=( LENGTH_UNIT ( ) NAMED_UNIT ( * ) SI_UNIT ( .MILLI., .METRE. ) );
#2971=CARTESIAN_POINT ( 'NONE',  ( 3.094860106618431583, 114.0949999999999704, 9.525000000000000355 ) ) ;
#2973=( NAMED_UNIT ( * ) PLANE_ANGLE_UNIT ( ) SI_UNIT ( $, .RADIAN. ) );
#2977=CARTESIAN_POINT ( 'NONE',  ( 2.607480562269107072, 122.7929263765338135, -8.024999999999979039 ) ) ;
#2978=FILL_AREA_STYLE ('',( #48844 ) ) ;
#2980=CARTESIAN_POINT ( 'NONE',  ( -74.99999999999998579, 50.00000000000000000, -6.999999999999988454 ) ) ;
#2983=CARTESIAN_POINT ( 'NONE',  ( -8.458988388480607412, 111.4970379835461642, -1.154793543936462719 ) ) ;
#2989=( NAMED_UNIT ( * ) PLANE_ANGLE_UNIT ( ) SI_UNIT ( $, .RADIAN. ) );
#2991=DIRECTION ( 'NONE',  ( 0.000000000000000000, 0.000000000000000000, 1.000000000000000000 ) ) ;
#2993=CARTESIAN_POINT ( 'NONE',  ( -1.166476076187854022E-15, 151.0550000000000068, 9.525000000000000355 ) ) ;
#2995=DIRECTION ( 'NONE',  ( 0.000000000000000000, 0.000000000000000000, 1.000000000000000000 ) ) ;
#3000=CARTESIAN_POINT ( 'NONE',  ( -20.35445791815277161, 114.9981483343694748, -10.00000000000000000 ) ) ;
#3002=( LENGTH_UNIT ( ) NAMED_UNIT ( * ) SI_UNIT ( .MILLI., .METRE. ) );
#3005=CARTESIAN_POINT ( 'NONE',  ( 20.71231517720797655, 149.4999999999999716, 10.00000000000000000 ) ) ;
#3012=( LENGTH_UNIT ( ) NAMED_UNIT ( * ) SI_UNIT ( .MILLI., .METRE. ) );
#3017=CARTESIAN_POINT ( 'NONE',  ( -60.00000000000000000, -2.024042244987997205E-14, -10.49999999999999822 ) ) ;
#3019=ORIENTED_EDGE ( 'NONE', *, *, #4682, .F. ) ;
#3020=LINE ( 'NONE', #61796, #33270 ) ;
#3021=VERTEX_POINT ( 'NONE', #49215 ) ;
#3023=DIRECTION ( 'NONE',  ( 0.000000000000000000, 1.000000000000000000, -0.000000000000000000 ) ) ;
#3025=EDGE_LOOP ( 'NONE', ( #63297, #33534, #67926 ) ) ;
#3029=CARTESIAN_POINT ( 'NONE',  ( -74.50000000000000000, 9.708372675170620525, 6.000000000000000888 ) ) ;
#3031=CARTESIAN_POINT ( 'NONE',  ( -7.632228543268607446, 147.5429263765338135, -2.479861379858953718 ) ) ;
#3032=SURFACE_STYLE_USAGE ( .BOTH. , #40756 ) ;
#3033=PRESENTATION_STYLE_ASSIGNMENT (( #51290 ) ) ;
#3040=CARTESIAN_POINT ( 'NONE',  ( -8.437984349512095861, 139.8070736234661524, -5.166775262442723748E-16 ) ) ;
#3041=CARTESIAN_POINT ( 'NONE',  ( 45.50000000000000000, 10.69371294336137801, 10.00000000000000000 ) ) ;
#3043=CARTESIAN_POINT ( 'NONE',  ( -60.00000000000000000, -2.024042244987997205E-14, 6.500000000000000000 ) ) ;
#3046=FACE_OUTER_BOUND ( 'NONE', #3461, .T. ) ;
#3049=DIRECTION ( 'NONE',  ( -0.000000000000000000, -0.000000000000000000, 1.000000000000000000 ) ) ;
#3052=AXIS2_PLACEMENT_3D ( 'NONE', #32869, #6130, #446 ) ;
#3054=DIRECTION ( 'NONE',  ( -1.000000000000000000, 0.000000000000000000, 0.000000000000000000 ) ) ;
#3056=EDGE_CURVE ( 'NONE', #4894, #56993, #10784, .T. ) ;
#3058=( LENGTH_UNIT ( ) NAMED_UNIT ( * ) SI_UNIT ( .MILLI., .METRE. ) );
#3059=ORIENTED_EDGE ( 'NONE', *, *, #39998, .T. ) ;
#3065=AXIS2_PLACEMENT_3D ( 'NONE', #62820, #58600, #48439 ) ;
#3069=CARTESIAN_POINT ( 'NONE',  ( -75.00000000000002842, 35.50862325381058326, -9.555990219820042597 ) ) ;
#3070=SURFACE_STYLE_USAGE ( .BOTH. , #52034 ) ;
#3074=SURFACE_STYLE_FILL_AREA ( #51328 ) ;
#3078=CARTESIAN_POINT ( 'NONE',  ( 3.094860106618431583, 115.2049999999999983, 9.525000000000000355 ) ) ;
#3085=EDGE_LOOP ( 'NONE', ( #36467, #33112, #55177, #51059 ) ) ;
#3088=DIRECTION ( 'NONE',  ( -0.000000000000000000, 1.000000000000000000, -0.000000000000000000 ) ) ;
#3093=( BOUNDED_SURFACE ( )  B_SPLINE_SURFACE ( 3, 2, ( 
 ( #49399, #1831, #1125 ),
 ( #23340, #59583, #28236 ),
 ( #6810, #16716, #49082 ),
 ( #27895, #768, #33556 ),
 ( #55707, #12426, #34251 ),
 ( #54655, #7176, #43802 ),
 ( #6458, #22660, #44166 ),
 ( #65562, #66247, #11749 ),
 ( #18074, #17413, #54308 ),
 ( #38180, #32870, #48744 ),
 ( #38877, #22306, #33887 ),
 ( #60287, #27207, #65211 ),
 ( #17062, #38541, #59933 ),
 ( #54985, #49746, #1484 ),
 ( #23013, #65913, #55354 ),
 ( #13129, #46594, #57085 ),
 ( #24712, #40239, #13471 ),
 ( #3580, #19087, #8908 ) ),
 .UNSPECIFIED., .F., .F., .F. ) 
 B_SPLINE_SURFACE_WITH_KNOTS ( ( 4, 2, 2, 2, 2, 2, 2, 2, 4 ),
 ( 3, 3 ),
 ( 0.0008275086428995113161, 0.0009765612317269591579, 0.001125613820554406891, 0.001274666409381854625, 0.001423718998209302358, 0.001721824175864198041, 0.002019929353519093508, 0.002616139708828884441, 0.003212350064138675809 ),
 ( 0.000000000000000000, 1.000000000000000000 ),
 .UNSPECIFIED. ) 
 GEOMETRIC_REPRESENTATION_ITEM ( )  RATIONAL_B_SPLINE_SURFACE ( (
 ( 1.000000000000000000, 0.2907356542125085763, 1.000000000000000000),
 ( 1.000000000000000000, 0.2907339171234460951, 1.000000000000000000),
 ( 1.000000000000000000, 0.2933218126491319855, 1.000000000000000000),
 ( 1.000000000000000000, 0.3027174795994745371, 1.000000000000000000),
 ( 1.000000000000000000, 0.3096405143333968435, 1.000000000000000000),
 ( 1.000000000000000000, 0.3258903432231445296, 1.000000000000000000),
 ( 1.000000000000000000, 0.3352112554373404829, 1.000000000000000000),
 ( 1.000000000000000000, 0.3552330613602922571, 1.000000000000000000),
 ( 1.000000000000000000, 0.3657822831406245534, 1.000000000000000000),
 ( 1.000000000000000000, 0.3977110304218586800, 1.000000000000000000),
 ( 1.000000000000000000, 0.4197187326554602249, 1.000000000000000000),
 ( 1.000000000000000000, 0.4623670587026428302, 1.000000000000000000),
 ( 1.000000000000000000, 0.4829316641227516249, 1.000000000000000000),
 ( 1.000000000000000000, 0.5424860661042875121, 1.000000000000000000),
 ( 1.000000000000000000, 0.5795047887219657579, 1.000000000000000000),
 ( 1.000000000000000000, 0.6470713767465448019, 1.000000000000000000),
 ( 1.000000000000000000, 0.6780453138457507301, 1.000000000000000000),
 ( 1.000000000000000000, 0.7071067811865523467, 1.000000000000000000) ) ) 
 REPRESENTATION_ITEM ( '' )  SURFACE ( )  );
#3095=LINE ( 'NONE', #35867, #10249 ) ;
#3097=STYLED_ITEM ( 'NONE', ( #14901 ), #50902 ) ;
#3098=CARTESIAN_POINT ( 'NONE',  ( 75.00000000000000000, 19.30628705663858469, 6.999999999999999112 ) ) ;
#3100=ORIENTED_EDGE ( 'NONE', *, *, #46951, .T. ) ;
#3110=VECTOR ( 'NONE', #34985, 1000.000000000000000 ) ;
#3112=CARTESIAN_POINT ( 'NONE',  ( 8.102448949553183510, 138.9949999999999193, -5.886773742842746238 ) ) ;
#3115=CARTESIAN_POINT ( 'NONE',  ( -1.166476076187854022E-15, 136.0549999999999784, 9.525000000000000355 ) ) ;
#3116=FACE_OUTER_BOUND ( 'NONE', #2717, .T. ) ;
#3118=CARTESIAN_POINT ( 'NONE',  ( 4.716976649647096842, 118.7429263765338163, 6.492361379858953896 ) ) ;
#3119=( LENGTH_UNIT ( ) NAMED_UNIT ( * ) SI_UNIT ( .MILLI., .METRE. ) );
#3120=UNCERTAINTY_MEASURE_WITH_UNIT (LENGTH_MEASURE( 1.000000000000000082E-05 ), #49416, 'distance_accuracy_value', 'NONE');
#3124=EDGE_CURVE ( 'NONE', #37946, #66402, #42729, .T. ) ;
#3126=ORIENTED_EDGE ( 'NONE', *, *, #66262, .T. ) ;
#3128=CARTESIAN_POINT ( 'NONE',  ( 41.16129102860539746, 107.5075374186653931, 3.372645969649438413 ) ) ;
#3129=VERTEX_POINT ( 'NONE', #67448 ) ;
#3136=UNCERTAINTY_MEASURE_WITH_UNIT (LENGTH_MEASURE( 1.000000000000000082E-05 ), #12265, 'distance_accuracy_value', 'NONE');
#3137=EDGE_CURVE ( 'NONE', #13131, #4028, #25567, .T. ) ;
#3138=VECTOR ( 'NONE', #57380, 1000.000000000000000 ) ;
#3139=LINE ( 'NONE', #24631, #21766 ) ;
#3141=CARTESIAN_POINT ( 'NONE',  ( 75.00000000000000000, 20.22733879051532568, 6.503618960537718152 ) ) ;
#3142=DIRECTION ( 'NONE',  ( 0.000000000000000000, -1.000000000000000000, -0.000000000000000000 ) ) ;
#3148=LINE ( 'NONE', #46875, #56947 ) ;
#3150=VERTEX_POINT ( 'NONE', #30492 ) ;
#3155=CIRCLE ( 'NONE', #64955, 0.5000000000000004441 ) ;
#3156=CARTESIAN_POINT ( 'NONE',  ( -74.10600381765247846, 9.348666914230193470, -6.164661031308983574 ) ) ;
#3157=ORIENTED_EDGE ( 'NONE', *, *, #17080, .T. ) ;
#3158=DIRECTION ( 'NONE',  ( 1.000000000000000000, 0.000000000000000000, 0.000000000000000000 ) ) ;
#3161=CARTESIAN_POINT ( 'NONE',  ( 8.102448949553183510, 138.9949999999999193, -5.886773742842746238 ) ) ;
#3166=UNCERTAINTY_MEASURE_WITH_UNIT (LENGTH_MEASURE( 1.000000000000000082E-05 ), #64161, 'distance_accuracy_value', 'NONE');
#3171=SURFACE_SIDE_STYLE ('',( #29963 ) ) ;
#3174=CARTESIAN_POINT ( 'NONE',  ( -44.99999999999977263, 147.4999999999999716, -10.00000000000000000 ) ) ;
#3178=UNCERTAINTY_MEASURE_WITH_UNIT (LENGTH_MEASURE( 1.000000000000000082E-05 ), #48494, 'distance_accuracy_value', 'NONE');
#3179=AXIS2_PLACEMENT_3D ( 'NONE', #19117, #12459, #50465 ) ;
#3181=CARTESIAN_POINT ( 'NONE',  ( -45.00000000000000000, 8.164117261306884643, 6.987107442241105915 ) ) ;
#3182=CARTESIAN_POINT ( 'NONE',  ( -12.72792206135785165, 1.797044900979284448E-15, -10.00000000000000000 ) ) ;
#3184=CIRCLE ( 'NONE', #52726, 30.00000000000000000 ) ;
#3185=ORIENTED_EDGE ( 'NONE', *, *, #32707, .T. ) ;
#3187=ORIENTED_EDGE ( 'NONE', *, *, #43099, .F. ) ;
#3188=( NAMED_UNIT ( * ) PLANE_ANGLE_UNIT ( ) SI_UNIT ( $, .RADIAN. ) );
#3189=CARTESIAN_POINT ( 'NONE',  ( 44.99999999999977973, 146.4999999999999716, -7.500000000000000000 ) ) ;
#3190=ORIENTED_EDGE ( 'NONE', *, *, #22261, .F. ) ;
#3192=AXIS2_PLACEMENT_3D ( 'NONE', #59699, #5883, #49178 ) ;
#3194=PRESENTATION_STYLE_ASSIGNMENT (( #35628 ) ) ;
#3196=CARTESIAN_POINT ( 'NONE',  ( -8.102448949553181734, 113.4949999999999619, 5.886773742842747126 ) ) ;
#3203=SURFACE_STYLE_USAGE ( .BOTH. , #35281 ) ;
#3205=CARTESIAN_POINT ( 'NONE',  ( 9.058813317711337021, 133.6550000000000011, 2.943386871421375783 ) ) ;
#3207=DIRECTION ( 'NONE',  ( 0.000000000000000000, 1.000000000000000000, 0.000000000000000000 ) ) ;
#3208=MECHANICAL_DESIGN_GEOMETRIC_PRESENTATION_REPRESENTATION('',(#6660),#51569);
#3212=FILL_AREA_STYLE_COLOUR ( '', #8585 ) ;
#3214=DIRECTION ( 'NONE',  ( 0.000000000000000000, 0.000000000000000000, -1.000000000000000000 ) ) ;
#3216=AXIS2_PLACEMENT_3D ( 'NONE', #25, #32439, #15972 ) ;
#3217=CYLINDRICAL_SURFACE ( 'NONE', #37402, 8.025000000000000355 ) ;
#3221=CARTESIAN_POINT ( 'NONE',  ( 6.598003871452727154, 111.1717662273375709, 5.909302594220223526 ) ) ;
#3234=PLANE ( 'NONE',  #2464 ) ;
#3236=SURFACE_STYLE_FILL_AREA ( #29679 ) ;
#3239=CARTESIAN_POINT ( 'NONE',  ( 9.058813317711337021, 144.5449999999999875, 2.943386871421375783 ) ) ;
#3241=COLOUR_RGB ( '', 0.40784314, 0.44705882, 0.49803922) ;
#3245=FACE_OUTER_BOUND ( 'NONE', #9534, .T. ) ;
#3250=CARTESIAN_POINT ( 'NONE',  ( 8.102448949553181734, 111.3949999999999818, 5.886773742842750679 ) ) ;
#3253=COLOUR_RGB ( '', 0.09019608, 0.27058824, 0.51372549) ;
#3255=SURFACE_SIDE_STYLE ('',( #13864 ) ) ;
#3257=EDGE_CURVE ( 'NONE', #1660, #4324, #63627, .T. ) ;
#3260=SURFACE_STYLE_USAGE ( .BOTH. , #45902 ) ;
#3264=DIRECTION ( 'NONE',  ( -0.000000000000000000, 1.000000000000000000, -0.000000000000000000 ) ) ;
#3266=DIRECTION ( 'NONE',  ( -0.000000000000000000, 1.000000000000000000, -0.000000000000000000 ) ) ;
#3271=DIRECTION ( 'NONE',  ( 0.000000000000000000, 0.000000000000000000, 1.000000000000000000 ) ) ;
#3272=CARTESIAN_POINT ( 'NONE',  ( 15.98999599679679839, 117.9999999999999716, 7.500000000000000000 ) ) ;
#3273=DIRECTION ( 'NONE',  ( 0.000000000000000000, 0.000000000000000000, 1.000000000000000000 ) ) ;
#3274=CARTESIAN_POINT ( 'NONE',  ( 4.716976649647099507, 123.7570736234661695, -6.492361379858953008 ) ) ;
#3276=AXIS2_PLACEMENT_3D ( 'NONE', #38567, #1858, #55016 ) ;
#3281=DIRECTION ( 'NONE',  ( 1.000000000000000000, 0.000000000000000000, 0.000000000000000000 ) ) ;
#3282=ORIENTED_EDGE ( 'NONE', *, *, #43269, .F. ) ;
#3284=AXIS2_PLACEMENT_3D ( 'NONE', #58560, #62779, #47015 ) ;
#3285=( GEOMETRIC_REPRESENTATION_CONTEXT ( 3 ) GLOBAL_UNCERTAINTY_ASSIGNED_CONTEXT ( ( #45416 ) ) GLOBAL_UNIT_ASSIGNED_CONTEXT ( ( #19173, #51551, #18835 ) ) REPRESENTATION_CONTEXT ( 'NONE', 'WORKASPACE' ) );
#3286=( NAMED_UNIT ( * ) SI_UNIT ( $, .STERADIAN. ) SOLID_ANGLE_UNIT ( ) );
#3287=CARTESIAN_POINT ( 'NONE',  ( -8.437984349512095861, 133.8070736234661808, -5.166775262442723748E-16 ) ) ;
#3290=AXIS2_PLACEMENT_3D ( 'NONE', #13784, #57037, #8854 ) ;
#3292=CARTESIAN_POINT ( 'NONE',  ( 75.00000000000000000, 19.38064346792907244, -6.520279032830151422 ) ) ;
#3295=EDGE_LOOP ( 'NONE', ( #34911, #12190, #19331, #41704 ) ) ;
#3299=AXIS2_PLACEMENT_3D ( 'NONE', #57004, #39476, #8134 ) ;
#3300=EDGE_CURVE ( 'NONE', #9629, #32941, #51908, .T. ) ;
#3302=DIRECTION ( 'NONE',  ( -0.000000000000000000, -0.000000000000000000, -1.000000000000000000 ) ) ;
#3304=ORIENTED_EDGE ( 'NONE', *, *, #15309, .T. ) ;
#3309=PRESENTATION_STYLE_ASSIGNMENT (( #2621 ) ) ;
#3311=STYLED_ITEM ( 'NONE', ( #12915 ), #51621 ) ;
#3316=LINE ( 'NONE', #14627, #7720 ) ;
#3321=( GEOMETRIC_REPRESENTATION_CONTEXT ( 3 ) GLOBAL_UNCERTAINTY_ASSIGNED_CONTEXT ( ( #14394 ) ) GLOBAL_UNIT_ASSIGNED_CONTEXT ( ( #25620, #67165, #8774 ) ) REPRESENTATION_CONTEXT ( 'NONE', 'WORKASPACE' ) );
#3322=CARTESIAN_POINT ( 'NONE',  ( 8.102448949553179958, 111.3949999999999818, 5.886773742842750679 ) ) ;
#3326=ORIENTED_EDGE ( 'NONE', *, *, #31759, .T. ) ;
#3328=( LENGTH_UNIT ( ) NAMED_UNIT ( * ) SI_UNIT ( .MILLI., .METRE. ) );
#3331=FILL_AREA_STYLE_COLOUR ( '', #43740 ) ;
#3333=FILL_AREA_STYLE ('',( #63175 ) ) ;
#3337=EDGE_CURVE ( 'NONE', #197, #35623, #15050, .T. ) ;
#3341=FILL_AREA_STYLE ('',( #51584 ) ) ;
#3346=CARTESIAN_POINT ( 'NONE',  ( 3.094860106618435136, 155.4050000000000011, -9.525000000000000355 ) ) ;
#3350=DIRECTION ( 'NONE',  ( -1.000000000000000000, 0.000000000000000000, 0.000000000000000000 ) ) ;
#3351=CARTESIAN_POINT ( 'NONE',  ( -23.21231517720797655, 117.4999999999999716, 9.500000000000000000 ) ) ;
#3352=EDGE_CURVE ( 'NONE', #65582, #22419, #35622, .T. ) ;
#3357=EDGE_CURVE ( 'NONE', #7095, #44000, #35835, .T. ) ;
#3362=AXIS2_PLACEMENT_3D ( 'NONE', #39768, #65429, #33750 ) ;
#3365=TOROIDAL_SURFACE ( 'NONE', #62967, 8.500000000000012434, 0.5000000000000000000 ) ;
#3369=DIRECTION ( 'NONE',  ( 1.000000000000000000, 0.000000000000000000, 0.000000000000000000 ) ) ;
#3371=EDGE_CURVE ( 'NONE', #12255, #24951, #5001, .T. ) ;
#3372=ORIENTED_EDGE ( 'NONE', *, *, #19056, .T. ) ;
#3373=ORIENTED_EDGE ( 'NONE', *, *, #267, .F. ) ;
#3374=DIRECTION ( 'NONE',  ( 0.000000000000000000, -1.000000000000000000, -0.000000000000000000 ) ) ;
#3376=CARTESIAN_POINT ( 'NONE',  ( -5.598654528085808657, 111.7549999999999955, 7.705886871421373741 ) ) ;
#3377=DIRECTION ( 'NONE',  ( 1.000000000000000000, 0.000000000000000000, 0.000000000000000000 ) ) ;
#3378=VERTEX_POINT ( 'NONE', #25758 ) ;
#3383=CARTESIAN_POINT ( 'NONE',  ( -9.489074601111886054, 110.4999999999999574, -0.9355076952660921208 ) ) ;
#3385=COLOUR_RGB ( '', 0.66274510, 0.83137255, 0.94901961) ;
#3386=( NAMED_UNIT ( * ) SI_UNIT ( $, .STERADIAN. ) SOLID_ANGLE_UNIT ( ) );
#3387=ORIENTED_EDGE ( 'NONE', *, *, #23575, .T. ) ;
#3388=CARTESIAN_POINT ( 'NONE',  ( 6.826472737025121695, 146.4929263765338305, -4.959722759717905660 ) ) ;
#3390=( NAMED_UNIT ( * ) PLANE_ANGLE_UNIT ( ) SI_UNIT ( $, .RADIAN. ) );
#3396=ORIENTED_EDGE ( 'NONE', *, *, #27909, .F. ) ;
#3400=CARTESIAN_POINT ( 'NONE',  ( 41.16151714082911184, 107.5071857241661348, -3.372843186988511377 ) ) ;
#3403=CARTESIAN_POINT ( 'NONE',  ( 44.28021770739998431, 9.999999999999980460, 3.500000000000000000 ) ) ;
#3404=CIRCLE ( 'NONE', #46176, 0.4999999999999994449 ) ;
#3408=ORIENTED_EDGE ( 'NONE', *, *, #41772, .T. ) ;
#3409=MECHANICAL_DESIGN_GEOMETRIC_PRESENTATION_REPRESENTATION('',(#41664),#14669);
#3410=ORIENTED_EDGE ( 'NONE', *, *, #27860, .T. ) ;
#3411=SURFACE_STYLE_USAGE ( .BOTH. , #67479 ) ;
#3414=( NAMED_UNIT ( * ) SI_UNIT ( $, .STERADIAN. ) SOLID_ANGLE_UNIT ( ) );
#3421=SURFACE_STYLE_FILL_AREA ( #32524 ) ;
#3424=CARTESIAN_POINT ( 'NONE',  ( -74.50000000000000000, 36.50926243676796190, -10.00000000000000000 ) ) ;
#3428=CARTESIAN_POINT ( 'NONE',  ( 0.000000000000000000, 125.5550000000000068, -9.525000000000000355 ) ) ;
#3430=CARTESIAN_POINT ( 'NONE',  ( -48.50000000000000000, 99.99999999999992895, -7.500000000000000000 ) ) ;
#3432=COLOUR_RGB ( '', 0.08235294, 0.09019608, 0.10196078) ;
#3434=SURFACE_STYLE_FILL_AREA ( #18642 ) ;
#3435=FILL_AREA_STYLE ('',( #14383 ) ) ;
#3438=EDGE_CURVE ( 'NONE', #6055, #26070, #13551, .T. ) ;
#3446=( GEOMETRIC_REPRESENTATION_CONTEXT ( 3 ) GLOBAL_UNCERTAINTY_ASSIGNED_CONTEXT ( ( #58200 ) ) GLOBAL_UNIT_ASSIGNED_CONTEXT ( ( #13019, #34475, #67177 ) ) REPRESENTATION_CONTEXT ( 'NONE', 'WORKASPACE' ) );
#3447=CARTESIAN_POINT ( 'NONE',  ( 2.607480562269155921, 134.7070736234661581, 8.024999999999941735 ) ) ;
#3450=ORIENTED_EDGE ( 'NONE', *, *, #12218, .F. ) ;
#3451=ORIENTED_EDGE ( 'NONE', *, *, #11238, .T. ) ;
#3458=CARTESIAN_POINT ( 'NONE',  ( -40.78947368421051323, 108.1536491499103505, -3.000000000000000444 ) ) ;
#3459=CARTESIAN_POINT ( 'NONE',  ( 44.99999999999977973, 147.4999999999999716, -10.00000000000000000 ) ) ;
#3461=EDGE_LOOP ( 'NONE', ( #40962, #53372, #21110, #67620 ) ) ;
#3470=CARTESIAN_POINT ( 'NONE',  ( -3.094860106618432471, 136.5949999999999989, -9.525000000000000355 ) ) ;
#3474=CARTESIAN_POINT ( 'NONE',  ( -9.058813317711337021, 147.1549999999999727, -2.943386871421374895 ) ) ;
#3475=PRESENTATION_STYLE_ASSIGNMENT (( #62601 ) ) ;
#3476=DIRECTION ( 'NONE',  ( 0.000000000000000000, 0.000000000000000000, 1.000000000000000000 ) ) ;
#3478=CARTESIAN_POINT ( 'NONE',  ( -7.632228543268607446, 120.5429263765338135, -2.479861379858953718 ) ) ;
#3479=SURFACE_SIDE_STYLE ('',( #8483 ) ) ;
#3483=SURFACE_SIDE_STYLE ('',( #39823 ) ) ;
#3488=VERTEX_POINT ( 'NONE', #57791 ) ;
#3491=AXIS2_PLACEMENT_3D ( 'NONE', #49357, #65873, #28195 ) ;
#3493=ORIENTED_EDGE ( 'NONE', *, *, #19749, .T. ) ;
#3495=CARTESIAN_POINT ( 'NONE',  ( -60.00000000000000000, -2.024042244987997205E-14, -6.000000000000000000 ) ) ;
#3496=CARTESIAN_POINT ( 'NONE',  ( -2.607480562269116842, 152.4070736234661751, 8.024999999999970157 ) ) ;
#3497=CARTESIAN_POINT ( 'NONE',  ( 74.99999999999998579, 19.70845863561292433, 6.466567654930966746 ) ) ;
#3498=FILL_AREA_STYLE_COLOUR ( '', #46794 ) ;
#3500=FILL_AREA_STYLE ('',( #28615 ) ) ;
#3503=MECHANICAL_DESIGN_GEOMETRIC_PRESENTATION_REPRESENTATION('',(#107),#25976);
#3504=SURFACE_STYLE_USAGE ( .BOTH. , #62979 ) ;
#3506=ORIENTED_EDGE ( 'NONE', *, *, #62830, .F. ) ;
#3507=CARTESIAN_POINT ( 'NONE',  ( -74.99999999999998579, 50.00000000000000000, -11.50000000000000000 ) ) ;
#3509=MECHANICAL_DESIGN_GEOMETRIC_PRESENTATION_REPRESENTATION('',(#64204),#53021);
#3513=CARTESIAN_POINT ( 'NONE',  ( -75.00000000000001421, 8.253551290271408547, -5.607507417892254153 ) ) ;
#3514=( NAMED_UNIT ( * ) PLANE_ANGLE_UNIT ( ) SI_UNIT ( $, .RADIAN. ) );
#3516=CARTESIAN_POINT ( 'NONE',  ( -74.50000000000000000, -2.220952357103124294E-14, 10.00000000000000000 ) ) ;
#3517=AXIS2_PLACEMENT_3D ( 'NONE', #62193, #63245, #45718 ) ;
#3518=CARTESIAN_POINT ( 'NONE',  ( 3.094860106618431583, 135.0949999999999420, 9.525000000000000355 ) ) ;
#3521=EDGE_CURVE ( 'NONE', #51980, #58400, #24345, .T. ) ;
#3525=CIRCLE ( 'NONE', #32804, 0.5000000000000004441 ) ;
#3526=CARTESIAN_POINT ( 'NONE',  ( -41.16129102860537614, 107.5075374186653505, -3.372645969649438857 ) ) ;
#3529=( LENGTH_UNIT ( ) NAMED_UNIT ( * ) SI_UNIT ( .MILLI., .METRE. ) );
#3531=EDGE_CURVE ( 'NONE', #65093, #64724, #48018, .T. ) ;
#3532=PRESENTATION_STYLE_ASSIGNMENT (( #40197 ) ) ;
#3533=DIRECTION ( 'NONE',  ( 0.000000000000000000, 0.000000000000000000, 1.000000000000000000 ) ) ;
#3534=CARTESIAN_POINT ( 'NONE',  ( 9.827790563157511022E-16, 152.9999999999999716, -8.025000000000000355 ) ) ;
#3536=CARTESIAN_POINT ( 'NONE',  ( -6.826472737025120807, 129.9929263765338021, 4.959722759717906548 ) ) ;
#3539=EDGE_CURVE ( 'NONE', #21703, #45027, #67049, .T. ) ;
#3543=SURFACE_STYLE_USAGE ( .BOTH. , #24673 ) ;
#3547=CARTESIAN_POINT ( 'NONE',  ( -44.99999999999977973, 147.4999999999999716, -10.00000000000000000 ) ) ;
#3552=( NAMED_UNIT ( * ) SI_UNIT ( $, .STERADIAN. ) SOLID_ANGLE_UNIT ( ) );
#3557=( GEOMETRIC_REPRESENTATION_CONTEXT ( 3 ) GLOBAL_UNCERTAINTY_ASSIGNED_CONTEXT ( ( #39128 ) ) GLOBAL_UNIT_ASSIGNED_CONTEXT ( ( #54976, #34246, #15748 ) ) REPRESENTATION_CONTEXT ( 'NONE', 'WORKASPACE' ) );
#3559=CARTESIAN_POINT ( 'NONE',  ( -5.598654528085806881, 109.7449999999999761, -7.705886871421374629 ) ) ;
#3563=CARTESIAN_POINT ( 'NONE',  ( -5.598654528085808657, 114.7549999999999812, 7.705886871421373741 ) ) ;
#3567=CARTESIAN_POINT ( 'NONE',  ( 8.102448949553181734, 139.5049999999999955, 5.886773742842750679 ) ) ;
#3568=MECHANICAL_DESIGN_GEOMETRIC_PRESENTATION_REPRESENTATION('',(#13702),#12573);
#3569=VECTOR ( 'NONE', #13486, 1000.000000000000000 ) ;
#3570=CARTESIAN_POINT ( 'NONE',  ( 19.89974874213239886, 114.9999999999999574, 10.00000000000001421 ) ) ;
#3572=VERTEX_POINT ( 'NONE', #59496 ) ;
#3573=CARTESIAN_POINT ( 'NONE',  ( -60.00000000000000000, -2.024042244987997205E-14, 12.00000000000000000 ) ) ;
#3576=ORIENTED_EDGE ( 'NONE', *, *, #42630, .T. ) ;
#3577=CARTESIAN_POINT ( 'NONE',  ( 6.050614363280118368, 111.1366428633864558, 6.516612769276372674 ) ) ;
#3580=CARTESIAN_POINT ( 'NONE',  ( -45.50000000000000000, 7.768687147774684831, -6.500000000000004441 ) ) ;
#3583=PRESENTATION_STYLE_ASSIGNMENT (( #46943 ) ) ;
#3586=DIRECTION ( 'NONE',  ( 0.000000000000000000, 0.000000000000000000, 1.000000000000000000 ) ) ;
#3594=CARTESIAN_POINT ( 'NONE',  ( 8.102448949553181734, 153.9950000000000045, -5.886773742842746238 ) ) ;
#3598=ORIENTED_EDGE ( 'NONE', *, *, #48098, .F. ) ;
#3600=COLOUR_RGB ( '', 0.31764706, 0.68627451, 0.89019608) ;
#3604=CARTESIAN_POINT ( 'NONE',  ( -8.102448949553181734, 110.4949999999999903, 5.886773742842747126 ) ) ;
#3608=( GEOMETRIC_REPRESENTATION_CONTEXT ( 3 ) GLOBAL_UNCERTAINTY_ASSIGNED_CONTEXT ( ( #12330 ) ) GLOBAL_UNIT_ASSIGNED_CONTEXT ( ( #27814, #39478, #32416 ) ) REPRESENTATION_CONTEXT ( 'NONE', 'WORKASPACE' ) );
#3609=ORIENTED_EDGE ( 'NONE', *, *, #51785, .F. ) ;
#3610=EDGE_CURVE ( 'NONE', #58089, #67711, #1031, .T. ) ;
#3611=MECHANICAL_DESIGN_GEOMETRIC_PRESENTATION_REPRESENTATION('',(#55375),#35188);
#3612=( LENGTH_UNIT ( ) NAMED_UNIT ( * ) SI_UNIT ( .MILLI., .METRE. ) );
#3615=CARTESIAN_POINT ( 'NONE',  ( -75.50000000000000000, 64.49137674618943095, -6.499999999999999112 ) ) ;
#3620=AXIS2_PLACEMENT_3D ( 'NONE', #44009, #15872, #65052 ) ;
#3623=EDGE_CURVE ( 'NONE', #21703, #38944, #41935, .T. ) ;
#3627=ADVANCED_FACE ( 'NONE', ( #61922 ), #29577, .F. ) ;
#3629=( NAMED_UNIT ( * ) SI_UNIT ( $, .STERADIAN. ) SOLID_ANGLE_UNIT ( ) );
#3631=CARTESIAN_POINT ( 'NONE',  ( 71.50000000000000000, 99.99999999999998579, 7.500000000000000000 ) ) ;
#3633=EDGE_CURVE ( 'NONE', #27227, #18512, #29976, .T. ) ;
#3634=COLOUR_RGB ( '', 0.72549020, 0.75294118, 0.79215686) ;
#3637=AXIS2_PLACEMENT_3D ( 'NONE', #24629, #67567, #19364 ) ;
#3638=CARTESIAN_POINT ( 'NONE',  ( -24.21231517720798010, 117.4999999999999716, 7.500000000000000000 ) ) ;
#3641=SURFACE_STYLE_FILL_AREA ( #67709 ) ;
#3646=CARTESIAN_POINT ( 'NONE',  ( 7.632228543268607446, 129.1570736234661467, 2.479861379858954606 ) ) ;
#3649=ORIENTED_EDGE ( 'NONE', *, *, #32183, .F. ) ;
#3652=COLOUR_RGB ( '', 0.31764706, 0.68627451, 0.89019608) ;
#3653=ORIENTED_EDGE ( 'NONE', *, *, #17011, .T. ) ;
#3656=CARTESIAN_POINT ( 'NONE',  ( 1.105243736230485067E-15, 152.9999999999999716, -8.025000000000000355 ) ) ;
#3658=ORIENTED_EDGE ( 'NONE', *, *, #60547, .T. ) ;
#3660=PRESENTATION_STYLE_ASSIGNMENT (( #14607 ) ) ;
#3666=DIRECTION ( 'NONE',  ( 0.000000000000000000, 0.000000000000000000, 1.000000000000000000 ) ) ;
#3668=EDGE_LOOP ( 'NONE', ( #24495, #47254, #31737, #47537, #43305, #42607, #27015, #27738, #63125, #26671, #32245, #50776, #66537, #64016 ) ) ;
#3669=CARTESIAN_POINT ( 'NONE',  ( 45.00000000000000000, 10.69371294336137801, 10.00000000000000000 ) ) ;
#3675=ORIENTED_EDGE ( 'NONE', *, *, #39032, .F. ) ;
#3679=DIRECTION ( 'NONE',  ( 0.7071067811865549002, 8.659560562355024070E-17, -0.7071067811865401342 ) ) ;
#3681=AXIS2_PLACEMENT_3D ( 'NONE', #36306, #46521, #10233 ) ;
#3682=CARTESIAN_POINT ( 'NONE',  ( 8.437984349512095861, 113.1929263765338050, 1.550032578732816828E-15 ) ) ;
#3685=( NAMED_UNIT ( * ) PLANE_ANGLE_UNIT ( ) SI_UNIT ( $, .RADIAN. ) );
#3686=DIRECTION ( 'NONE',  ( 0.000000000000000000, 0.000000000000000000, -1.000000000000000000 ) ) ;
#3689=DIRECTION ( 'NONE',  ( 1.000000000000000000, 0.000000000000000000, 0.000000000000000000 ) ) ;
#3692=CARTESIAN_POINT ( 'NONE',  ( -75.00000000000000000, 9.585819622309035282, 6.373651444779978803 ) ) ;
#3693=CARTESIAN_POINT ( 'NONE',  ( 0.000000000000000000, 110.5741857357814553, -9.450814264218539762 ) ) ;
#3697=ORIENTED_EDGE ( 'NONE', *, *, #30630, .F. ) ;
#3698=ADVANCED_FACE ( 'NONE', ( #18349, #34508 ), #19360, .T. ) ;
#3701=CARTESIAN_POINT ( 'NONE',  ( -45.50000000000000000, 99.99999999999992895, -9.500000000000000000 ) ) ;
#3703=UNCERTAINTY_MEASURE_WITH_UNIT (LENGTH_MEASURE( 1.000000000000000082E-05 ), #703, 'distance_accuracy_value', 'NONE');
#3709=CARTESIAN_POINT ( 'NONE',  ( -3.094860106618432471, 155.7049999999999841, -9.525000000000000355 ) ) ;
#3710=DIRECTION ( 'NONE',  ( 0.000000000000000000, 0.000000000000000000, 1.000000000000000000 ) ) ;
#3719=CARTESIAN_POINT ( 'NONE',  ( -2.451748578458123784E-13, 110.8535625161535592, 9.171437483846442973 ) ) ;
#3725=ORIENTED_EDGE ( 'NONE', *, *, #64414, .T. ) ;
#3729=DIRECTION ( 'NONE',  ( -0.000000000000000000, -0.000000000000000000, -1.000000000000000000 ) ) ;
#3734=AXIS2_PLACEMENT_3D ( 'NONE', #51456, #40229, #68337 ) ;
#3736=CARTESIAN_POINT ( 'NONE',  ( -8.102448949553181734, 120.0049999999999955, -5.886773742842749790 ) ) ;
#3737=CARTESIAN_POINT ( 'NONE',  ( 34.99999999999992895, 113.4999999999999858, 7.000000000000000000 ) ) ;
#3741=ORIENTED_EDGE ( 'NONE', *, *, #67515, .F. ) ;
#3742=SURFACE_SIDE_STYLE ('',( #64165 ) ) ;
#3745=CYLINDRICAL_SURFACE ( 'NONE', #26085, 0.5000000000000004441 ) ;
#3749=CARTESIAN_POINT ( 'NONE',  ( 6.826472737025121695, 149.4929263765338021, -4.959722759717905660 ) ) ;
#3750=FILL_AREA_STYLE_COLOUR ( '', #52362 ) ;
#3751=ADVANCED_FACE ( 'NONE', ( #50021 ), #54716, .F. ) ;
#3752=CARTESIAN_POINT ( 'NONE',  ( 52.49999999999998579, 2.746146170318484607E-15, 12.00000000000000000 ) ) ;
#3753=COLOUR_RGB ( '', 0.72549020, 0.75294118, 0.79215686) ;
#3755=( LENGTH_UNIT ( ) NAMED_UNIT ( * ) SI_UNIT ( .MILLI., .METRE. ) );
#3760=CARTESIAN_POINT ( 'NONE',  ( 41.40613950039011826, 107.1008216811760718, -3.493724300021677553 ) ) ;
#3764=CARTESIAN_POINT ( 'NONE',  ( 21.02379604162863913, 154.9999999999999716, 10.50000000000000000 ) ) ;
#3766=COLOUR_RGB ( '', 0.09019608, 0.27058824, 0.51372549) ;
#3767=DIRECTION ( 'NONE',  ( -0.9486832980505138790, -0.3162277660168378857, 0.000000000000000000 ) ) ;
#3770=VERTEX_POINT ( 'NONE', #1758 ) ;
#3776=DIRECTION ( 'NONE',  ( 0.000000000000000000, 0.000000000000000000, -1.000000000000000000 ) ) ;
#3781=( NAMED_UNIT ( * ) SI_UNIT ( $, .STERADIAN. ) SOLID_ANGLE_UNIT ( ) );
#3782=LINE ( 'NONE', #36208, #38065 ) ;
#3789=EDGE_CURVE ( 'NONE', #30484, #46307, #42598, .T. ) ;
#3792=FACE_OUTER_BOUND ( 'NONE', #58558, .T. ) ;
#3794=CARTESIAN_POINT ( 'NONE',  ( 45.00000000000000000, -1.469576158976824618E-14, -4.000000000000000000 ) ) ;
#3795=ADVANCED_FACE ( 'NONE', ( #41545 ), #58389, .F. ) ;
#3796=( GEOMETRIC_REPRESENTATION_CONTEXT ( 3 ) GLOBAL_UNCERTAINTY_ASSIGNED_CONTEXT ( ( #36229 ) ) GLOBAL_UNIT_ASSIGNED_CONTEXT ( ( #22598, #43742, #64807 ) ) REPRESENTATION_CONTEXT ( 'NONE', 'WORKASPACE' ) );
#3798=CARTESIAN_POINT ( 'NONE',  ( -3.094860106618432471, 131.7049999999999557, -9.525000000000000355 ) ) ;
#3800=CARTESIAN_POINT ( 'NONE',  ( 71.50000000000000000, 14.49137674618942562, 7.000000000000000000 ) ) ;
#3805=UNCERTAINTY_MEASURE_WITH_UNIT (LENGTH_MEASURE( 1.000000000000000082E-05 ), #63707, 'distance_accuracy_value', 'NONE');
#3811=( LENGTH_UNIT ( ) NAMED_UNIT ( * ) SI_UNIT ( .MILLI., .METRE. ) );
#3815=DIRECTION ( 'NONE',  ( 0.000000000000000000, 0.000000000000000000, 1.000000000000000000 ) ) ;
#3817=VERTEX_POINT ( 'NONE', #51745 ) ;
#3818=CARTESIAN_POINT ( 'NONE',  ( 6.826472737025121695, 131.4929263765337737, -4.959722759717905660 ) ) ;
#3819=CIRCLE ( 'NONE', #59984, 0.5000000000000004441 ) ;
#3820=STYLED_ITEM ( 'NONE', ( #14603 ), #324 ) ;
#3823=CARTESIAN_POINT ( 'NONE',  ( -23.71231517720798010, 113.4999999999999858, 7.500000000000000000 ) ) ;
#3824=CARTESIAN_POINT ( 'NONE',  ( -19.89974874213240597, 115.4999999999999574, 10.50000000000000000 ) ) ;
#3828=AXIS2_PLACEMENT_3D ( 'NONE', #43776, #38513, #59906 ) ;
#3836=CARTESIAN_POINT ( 'NONE',  ( 0.000000000000000000, 148.4449999999999932, -9.525000000000000355 ) ) ;
#3839=ORIENTED_EDGE ( 'NONE', *, *, #57162, .T. ) ;
#3840=AXIS2_PLACEMENT_3D ( 'NONE', #54819, #18609, #17587 ) ;
#3841=CARTESIAN_POINT ( 'NONE',  ( 10.01517768586949408, 151.8049999999999784, 1.839758294383810543E-15 ) ) ;
#3844=CARTESIAN_POINT ( 'NONE',  ( 7.632228543268608334, 113.3429263765338106, -2.479861379858951942 ) ) ;
#3846=UNCERTAINTY_MEASURE_WITH_UNIT (LENGTH_MEASURE( 1.000000000000000082E-05 ), #56279, 'distance_accuracy_value', 'NONE');
#3847=( LENGTH_UNIT ( ) NAMED_UNIT ( * ) SI_UNIT ( .MILLI., .METRE. ) );
#3848=DIRECTION ( 'NONE',  ( -0.000000000000000000, -0.000000000000000000, -1.000000000000000000 ) ) ;
#3854=ORIENTED_EDGE ( 'NONE', *, *, #6986, .T. ) ;
#3862=UNCERTAINTY_MEASURE_WITH_UNIT (LENGTH_MEASURE( 1.000000000000000082E-05 ), #13227, 'distance_accuracy_value', 'NONE');
#3864=CARTESIAN_POINT ( 'NONE',  ( -61.49999999999998579, 50.00000000000000000, -9.500000000000000000 ) ) ;
#3867=CARTESIAN_POINT ( 'NONE',  ( 45.50000000000000000, 10.69371294336137979, -6.000000000000000000 ) ) ;
#3868=EDGE_LOOP ( 'NONE', ( #63158, #13657, #52185, #674 ) ) ;
#3869=AXIS2_PLACEMENT_3D ( 'NONE', #25001, #41557, #46510 ) ;
#3873=FILL_AREA_STYLE_COLOUR ( '', #20993 ) ;
#3877=ORIENTED_EDGE ( 'NONE', *, *, #31596, .T. ) ;
#3879=CARTESIAN_POINT ( 'NONE',  ( -74.99999999999998579, 50.00000000000000000, 6.499999999999999112 ) ) ;
#3883=STYLED_ITEM ( 'NONE', ( #47705 ), #56231 ) ;
#3887=DIRECTION ( 'NONE',  ( -0.000000000000000000, -0.000000000000000000, -1.000000000000000000 ) ) ;
#3891=CARTESIAN_POINT ( 'NONE',  ( 9.058813317711338797, 150.8449999999999989, -2.943386871421372675 ) ) ;
#3893=FACE_OUTER_BOUND ( 'NONE', #25998, .T. ) ;
#3894=CARTESIAN_POINT ( 'NONE',  ( -67.99999999999998579, -2.024042244987997205E-14, 10.50000000000000000 ) ) ;
#3895=UNCERTAINTY_MEASURE_WITH_UNIT (LENGTH_MEASURE( 1.000000000000000082E-05 ), #29993, 'distance_accuracy_value', 'NONE');
#3896=CIRCLE ( 'NONE', #26350, 0.5000000000000004441 ) ;
#3901=DIRECTION ( 'NONE',  ( -0.000000000000000000, -0.000000000000000000, -1.000000000000000000 ) ) ;
#3908=MECHANICAL_DESIGN_GEOMETRIC_PRESENTATION_REPRESENTATION('',(#24159),#36580);
#3911=ORIENTED_EDGE ( 'NONE', *, *, #52057, .T. ) ;
#3912=VERTEX_POINT ( 'NONE', #28067 ) ;
#3917=CARTESIAN_POINT ( 'NONE',  ( 7.632228543268607446, 119.0429263765338135, 2.479861379858954606 ) ) ;
#3918=CARTESIAN_POINT ( 'NONE',  ( -44.99999999999998579, 119.9999999999999716, 7.500000000000000000 ) ) ;
#3919=SURFACE_STYLE_USAGE ( .BOTH. , #10272 ) ;
#3920=ORIENTED_EDGE ( 'NONE', *, *, #26448, .T. ) ;
#3922=VECTOR ( 'NONE', #3925, 1000.000000000000000 ) ;
#3923=ORIENTED_EDGE ( 'NONE', *, *, #14706, .T. ) ;
#3924=DIRECTION ( 'NONE',  ( 0.000000000000000000, 1.000000000000000000, 0.000000000000000000 ) ) ;
#3925=DIRECTION ( 'NONE',  ( 1.000000000000000000, -0.000000000000000000, -0.000000000000000000 ) ) ;
#3927=CIRCLE ( 'NONE', #27518, 0.5000000000000004441 ) ;
#3930=CARTESIAN_POINT ( 'NONE',  ( 2.607480562269076430, 159.9070736234661183, -8.025000000000000355 ) ) ;
#3932=VERTEX_POINT ( 'NONE', #42956 ) ;
#3934=CARTESIAN_POINT ( 'NONE',  ( 3.094860106618435136, 116.4049999999999869, -9.525000000000000355 ) ) ;
#3940=CARTESIAN_POINT ( 'NONE',  ( -1.166476076187854022E-15, 139.0549999999999784, 9.525000000000000355 ) ) ;
#3942=( LENGTH_UNIT ( ) NAMED_UNIT ( * ) SI_UNIT ( .MILLI., .METRE. ) );
#3944=SURFACE_SIDE_STYLE ('',( #41287 ) ) ;
#3945=ADVANCED_FACE ( 'NONE', ( #27038 ), #55832, .T. ) ;
#3946=( NAMED_UNIT ( * ) PLANE_ANGLE_UNIT ( ) SI_UNIT ( $, .RADIAN. ) );
#3948=DIRECTION ( 'NONE',  ( -0.000000000000000000, -1.000000000000000000, -0.000000000000000000 ) ) ;
#3952=EDGE_CURVE ( 'NONE', #30747, #67303, #10949, .T. ) ;
#3957=VERTEX_POINT ( 'NONE', #43985 ) ;
#3964=MANIFOLD_SOLID_BREP ( 'Cut-Sweep4', #67724 ) ;
#3968=COLOUR_RGB ( '', 0.31764706, 0.68627451, 0.89019608) ;
#3970=FILL_AREA_STYLE_COLOUR ( '', #20653 ) ;
#3978=DIRECTION ( 'NONE',  ( 0.000000000000000000, 0.000000000000000000, 1.000000000000000000 ) ) ;
#3979=CARTESIAN_POINT ( 'NONE',  ( 10.01517768586949231, 117.6949999999999790, 1.839758294383810543E-15 ) ) ;
#3981=MECHANICAL_DESIGN_GEOMETRIC_PRESENTATION_REPRESENTATION('',(#6252),#60183);
#3982=CYLINDRICAL_SURFACE ( 'NONE', #54934, 0.5000000000000004441 ) ;
#3983=ORIENTED_EDGE ( 'NONE', *, *, #577, .T. ) ;
#3984=SURFACE_SIDE_STYLE ('',( #52224 ) ) ;
#3986=ORIENTED_EDGE ( 'NONE', *, *, #51406, .T. ) ;
#3988=CIRCLE ( 'NONE', #60194, 10.02500000000000568 ) ;
#3991=CARTESIAN_POINT ( 'NONE',  ( -44.99282180236183848, 9.603602307716927911, -3.208073701553950219 ) ) ;
#3999=SURFACE_SIDE_STYLE ('',( #8619 ) ) ;
#4001=( GEOMETRIC_REPRESENTATION_CONTEXT ( 3 ) GLOBAL_UNCERTAINTY_ASSIGNED_CONTEXT ( ( #42550 ) ) GLOBAL_UNIT_ASSIGNED_CONTEXT ( ( #56571, #14717, #66796 ) ) REPRESENTATION_CONTEXT ( 'NONE', 'WORKASPACE' ) );
#4003=ORIENTED_EDGE ( 'NONE', *, *, #6431, .T. ) ;
#4005=FACE_OUTER_BOUND ( 'NONE', #59870, .T. ) ;
#4006=SURFACE_STYLE_USAGE ( .BOTH. , #52250 ) ;
#4007=AXIS2_PLACEMENT_3D ( 'NONE', #13824, #35285, #44831 ) ;
#4008=ORIENTED_EDGE ( 'NONE', *, *, #51896, .T. ) ;
#4009=VECTOR ( 'NONE', #13286, 1000.000000000000000 ) ;
#4010=CARTESIAN_POINT ( 'NONE',  ( 71.49999999999998579, 64.07124727947029896, -7.500000000000000000 ) ) ;
#4011=CARTESIAN_POINT ( 'NONE',  ( -7.632228543268608334, 130.9570736234661581, 2.479861379858952830 ) ) ;
#4012=LINE ( 'NONE', #45339, #21419 ) ;
#4017=CARTESIAN_POINT ( 'NONE',  ( 75.15811388300841145, 19.52565835097472302, 6.500000000000000000 ) ) ;
#4019=SURFACE_SIDE_STYLE ('',( #41359 ) ) ;
#4023=EDGE_CURVE ( 'NONE', #21246, #47500, #57404, .T. ) ;
#4028=VERTEX_POINT ( 'NONE', #34749 ) ;
#4029=STYLED_ITEM ( 'NONE', ( #56903 ), #57326 ) ;
#4030=CARTESIAN_POINT ( 'NONE',  ( -72.00000000000000000, 35.92875272052971525, 10.00000000000000000 ) ) ;
#4037=ORIENTED_EDGE ( 'NONE', *, *, #35524, .T. ) ;
#4040=VERTEX_POINT ( 'NONE', #28418 ) ;
#4046=CARTESIAN_POINT ( 'NONE',  ( 0.000000000000000000, 121.4449999999999790, -9.525000000000000355 ) ) ;
#4053=CARTESIAN_POINT ( 'NONE',  ( 34.99999999999992895, 113.4999999999999858, -7.500000000000000000 ) ) ;
#4054=CARTESIAN_POINT ( 'NONE',  ( 72.00000000000000000, 35.92875272052971525, 7.500000000000000000 ) ) ;
#4055=AXIS2_PLACEMENT_3D ( 'NONE', #27393, #66075, #59770 ) ;
#4056=DIRECTION ( 'NONE',  ( 0.000000000000000000, 0.000000000000000000, -1.000000000000000000 ) ) ;
#4061=ORIENTED_EDGE ( 'NONE', *, *, #15514, .F. ) ;
#4064=CARTESIAN_POINT ( 'NONE',  ( -75.00000000000000000, 67.00000000000000000, -6.500000000000000000 ) ) ;
#4067=STYLED_ITEM ( 'NONE', ( #20999 ), #40143 ) ;
#4069=CARTESIAN_POINT ( 'NONE',  ( -3.094860106618434248, 153.9049999999999443, 9.525000000000000355 ) ) ;
#4073=SURFACE_STYLE_USAGE ( .BOTH. , #63537 ) ;
#4077=CARTESIAN_POINT ( 'NONE',  ( -23.71231517720798010, 118.4999999999999716, -7.000000000000000000 ) ) ;
#4079=( LENGTH_UNIT ( ) NAMED_UNIT ( * ) SI_UNIT ( .MILLI., .METRE. ) );
#4086=VERTEX_POINT ( 'NONE', #41822 ) ;
#4089=( NAMED_UNIT ( * ) PLANE_ANGLE_UNIT ( ) SI_UNIT ( $, .RADIAN. ) );
#4091=CARTESIAN_POINT ( 'NONE',  ( -3.094860106618432471, 116.7049999999999983, -9.525000000000000355 ) ) ;
#4097=ORIENTED_EDGE ( 'NONE', *, *, #11882, .F. ) ;
#4100=DIRECTION ( 'NONE',  ( 0.000000000000000000, 0.000000000000000000, 1.000000000000000000 ) ) ;
#4101=DIRECTION ( 'NONE',  ( 7.080503983578803083E-17, -1.000000000000000000, 0.000000000000000000 ) ) ;
#4103=CARTESIAN_POINT ( 'NONE',  ( 4.716976649647099507, 158.6429263765338078, -6.492361379858953008 ) ) ;
#4104=DIRECTION ( 'NONE',  ( 0.000000000000000000, -1.000000000000000000, 0.000000000000000000 ) ) ;
#4105=VECTOR ( 'NONE', #39127, 1000.000000000000000 ) ;
#4107=ORIENTED_EDGE ( 'NONE', *, *, #69561, .T. ) ;
#4108=CARTESIAN_POINT ( 'NONE',  ( 19.98431065987488608, 114.9999999999999574, -10.47133983857574613 ) ) ;
#4117=VECTOR ( 'NONE', #43882, 1000.000000000000000 ) ;
#4119=EDGE_CURVE ( 'NONE', #58118, #2414, #69489, .T. ) ;
#4124=EDGE_LOOP ( 'NONE', ( #19322, #63004, #28694, #64597 ) ) ;
#4125=CARTESIAN_POINT ( 'NONE',  ( -9.827790563157511022E-16, 151.4429263765338192, 8.025000000000000355 ) ) ;
#4130=FILL_AREA_STYLE_COLOUR ( '', #19150 ) ;
#4132=DIRECTION ( 'NONE',  ( 1.000000000000000000, 0.000000000000000000, 0.000000000000000000 ) ) ;
#4133=DIRECTION ( 'NONE',  ( 0.000000000000000000, 0.000000000000000000, 1.000000000000000000 ) ) ;
#4141=CARTESIAN_POINT ( 'NONE',  ( -74.55554437418339830, 36.39399965470389731, -10.00000000000000000 ) ) ;
#4142=AXIS2_PLACEMENT_3D ( 'NONE', #11061, #22674, #43817 ) ;
#4144=CARTESIAN_POINT ( 'NONE',  ( -1.166476076187854022E-15, 127.0549999999999784, 9.525000000000000355 ) ) ;
#4145=( GEOMETRIC_REPRESENTATION_CONTEXT ( 3 ) GLOBAL_UNCERTAINTY_ASSIGNED_CONTEXT ( ( #62776 ) ) GLOBAL_UNIT_ASSIGNED_CONTEXT ( ( #936, #10897, #59768 ) ) REPRESENTATION_CONTEXT ( 'NONE', 'WORKASPACE' ) );
#4147=CARTESIAN_POINT ( 'NONE',  ( -75.00000000000000000, 8.163938725409359165, -6.987118804072281364 ) ) ;
#4149=EDGE_CURVE ( 'NONE', #2048, #48570, #51113, .T. ) ;
#4150=SURFACE_STYLE_USAGE ( .BOTH. , #9485 ) ;
#4151=FACE_OUTER_BOUND ( 'NONE', #28866, .T. ) ;
#4155=CARTESIAN_POINT ( 'NONE',  ( -6.826472737025120807, 146.1070736234661354, 4.959722759717906548 ) ) ;
#4156=AXIS2_PLACEMENT_3D ( 'NONE', #55951, #17982, #66517 ) ;
#4157=CARTESIAN_POINT ( 'NONE',  ( 34.99999999999999289, 99.99999999999997158, -9.500000000000000000 ) ) ;
#4158=CARTESIAN_POINT ( 'NONE',  ( 0.000000000000000000, 136.0570736234661808, -8.025000000000000355 ) ) ;
#4159=SURFACE_SIDE_STYLE ('',( #9496 ) ) ;
#4160=ORIENTED_EDGE ( 'NONE', *, *, #23412, .F. ) ;
#4162=( LENGTH_UNIT ( ) NAMED_UNIT ( * ) SI_UNIT ( .MILLI., .METRE. ) );
#4166=DIRECTION ( 'NONE',  ( 1.000000000000000000, 0.000000000000000000, 0.000000000000000000 ) ) ;
#4168=ORIENTED_EDGE ( 'NONE', *, *, #36815, .T. ) ;
#4171=EDGE_CURVE ( 'NONE', #25674, #67533, #23431, .T. ) ;
#4174=EDGE_CURVE ( 'NONE', #27816, #36075, #3155, .T. ) ;
#4176=LINE ( 'NONE', #58044, #53811 ) ;
#4177=DIRECTION ( 'NONE',  ( 1.000000000000000000, 0.000000000000000000, 0.000000000000000000 ) ) ;
#4178=ORIENTED_EDGE ( 'NONE', *, *, #31616, .T. ) ;
#4179=CARTESIAN_POINT ( 'NONE',  ( 10.01517768586949231, 153.6949999999999932, 1.839758294383810543E-15 ) ) ;
#4181=( LENGTH_UNIT ( ) NAMED_UNIT ( * ) SI_UNIT ( .MILLI., .METRE. ) );
#4182=CARTESIAN_POINT ( 'NONE',  ( -9.058813317711337021, 150.1549999999999727, -2.943386871421374895 ) ) ;
#4184=CARTESIAN_POINT ( 'NONE',  ( -74.99999999999998579, 50.00000000000000000, 10.50000000000000000 ) ) ;
#4185=CARTESIAN_POINT ( 'NONE',  ( 24.21231517720798010, 112.9999999999999858, -7.500000000000000000 ) ) ;
#4187=CARTESIAN_POINT ( 'NONE',  ( -6.826472737025120807, 126.3929263765338220, -4.959722759717907437 ) ) ;
#4190=CARTESIAN_POINT ( 'NONE',  ( 45.00000000000000000, 10.69371294329215516, 6.262534692517949253 ) ) ;
#4196=ADVANCED_FACE ( 'NONE', ( #57255 ), #30504, .F. ) ;
#4199=FILL_AREA_STYLE_COLOUR ( '', #24398 ) ;
#4206=SPHERICAL_SURFACE ( 'NONE', #59513, 0.5000000000000000000 ) ;
#4207=CARTESIAN_POINT ( 'NONE',  ( 34.99999999999999289, 99.99999999999997158, 10.00000000000000000 ) ) ;
#4210=ORIENTED_EDGE ( 'NONE', *, *, #17806, .T. ) ;
#4214=ORIENTED_EDGE ( 'NONE', *, *, #46004, .T. ) ;
#4216=DIRECTION ( 'NONE',  ( 0.000000000000000000, 0.000000000000000000, 1.000000000000000000 ) ) ;
#4220=CARTESIAN_POINT ( 'NONE',  ( -75.00000000000000000, 8.380821545698800890, -5.549835146672132957 ) ) ;
#4224=CARTESIAN_POINT ( 'NONE',  ( 10.01517768586949231, 144.6949999999999932, 1.839758294383810543E-15 ) ) ;
#4227=CARTESIAN_POINT ( 'NONE',  ( 20.71231517720797655, 149.4999999999999716, -10.00000000000000000 ) ) ;
#4231=CIRCLE ( 'NONE', #8736, 5.500000000000005329 ) ;
#4233=DIRECTION ( 'NONE',  ( 1.000000000000000000, 0.000000000000000000, 0.000000000000000000 ) ) ;
#4236=STYLED_ITEM ( 'NONE', ( #55459 ), #65992 ) ;
#4240=AXIS2_PLACEMENT_3D ( 'NONE', #17111, #16430, #32541 ) ;
#4241=PRESENTATION_STYLE_ASSIGNMENT (( #25386 ) ) ;
#4243=CARTESIAN_POINT ( 'NONE',  ( 23.71231517720798010, 117.4999999999999716, 7.500000000000000000 ) ) ;
#4245=DIRECTION ( 'NONE',  ( 0.000000000000000000, 0.000000000000000000, -1.000000000000000000 ) ) ;
#4246=CARTESIAN_POINT ( 'NONE',  ( -45.89399618234750733, 9.348666914230159719, 6.164661031308989791 ) ) ;
#4248=MECHANICAL_DESIGN_GEOMETRIC_PRESENTATION_REPRESENTATION('',(#9927),#42487);
#4249=COLOUR_RGB ( '', 0.72549020, 0.75294118, 0.79215686) ;
#4250=VERTEX_POINT ( 'NONE', #31905 ) ;
#4256=CARTESIAN_POINT ( 'NONE',  ( 0.000000000000000000, 149.9999999999999716, 0.000000000000000000 ) ) ;
#4260=CARTESIAN_POINT ( 'NONE',  ( -8.102448949553181734, 125.4949999999999903, 5.886773742842747126 ) ) ;
#4263=CARTESIAN_POINT ( 'NONE',  ( 8.102448949553179958, 118.5049999999999955, 5.886773742842750679 ) ) ;
#4268=CARTESIAN_POINT ( 'NONE',  ( -1.166476076187854022E-15, 136.0549999999999784, 9.525000000000000355 ) ) ;
#4272=PRESENTATION_STYLE_ASSIGNMENT (( #47270 ) ) ;
#4273=( NAMED_UNIT ( * ) PLANE_ANGLE_UNIT ( ) SI_UNIT ( $, .RADIAN. ) );
#4275=VECTOR ( 'NONE', #12672, 1000.000000000000000 ) ;
#4278=CARTESIAN_POINT ( 'NONE',  ( -60.99999999999998579, 50.00000000000000000, 7.000000000000000000 ) ) ;
#4281=CARTESIAN_POINT ( 'NONE',  ( 2.139872436712063397, 110.9430683727271685, 8.842724602598599049 ) ) ;
#4283=SURFACE_SIDE_STYLE ('',( #25764 ) ) ;
#4284=CARTESIAN_POINT ( 'NONE',  ( -74.50000000000000000, -2.220952357103124925E-14, 6.999999999999999112 ) ) ;
#4285=ORIENTED_EDGE ( 'NONE', *, *, #60742, .F. ) ;
#4287=COLOUR_RGB ( '', 0.08235294, 0.09019608, 0.10196078) ;
#4289=SURFACE_STYLE_FILL_AREA ( #52198 ) ;
#4295=ADVANCED_FACE ( 'NONE', ( #42510 ), #53387, .F. ) ;
#4297=CARTESIAN_POINT ( 'NONE',  ( 3.094860106618431583, 150.0949999999999420, 9.525000000000000355 ) ) ;
#4300=ORIENTED_EDGE ( 'NONE', *, *, #67795, .F. ) ;
#4301=SURFACE_STYLE_FILL_AREA ( #62026 ) ;
#4303=MECHANICAL_DESIGN_GEOMETRIC_PRESENTATION_REPRESENTATION('',(#30121),#45937);
#4304=FILL_AREA_STYLE ('',( #46618 ) ) ;
#4305=CARTESIAN_POINT ( 'NONE',  ( -83.99999999999997158, 50.00000000000000000, -11.50000000000000000 ) ) ;
#4308=CARTESIAN_POINT ( 'NONE',  ( -9.058813317711337021, 122.0449999999999875, -2.943386871421374895 ) ) ;
#4312=ORIENTED_EDGE ( 'NONE', *, *, #59090, .T. ) ;
#4313=VECTOR ( 'NONE', #296, 1000.000000000000000 ) ;
#4316=CARTESIAN_POINT ( 'NONE',  ( -21.02379604162864268, 110.4999999999999858, -10.00000000000000000 ) ) ;
#4320=( GEOMETRIC_REPRESENTATION_CONTEXT ( 3 ) GLOBAL_UNCERTAINTY_ASSIGNED_CONTEXT ( ( #55336 ) ) GLOBAL_UNIT_ASSIGNED_CONTEXT ( ( #51582, #8338, #39325 ) ) REPRESENTATION_CONTEXT ( 'NONE', 'WORKASPACE' ) );
#4323=FILL_AREA_STYLE_COLOUR ( '', #4663 ) ;
#4324=VERTEX_POINT ( 'NONE', #63909 ) ;
#4329=SURFACE_STYLE_USAGE ( .BOTH. , #10689 ) ;
#4330=EDGE_CURVE ( 'NONE', #42106, #41694, #15761, .T. ) ;
#4336=ORIENTED_EDGE ( 'NONE', *, *, #68201, .F. ) ;
#4339=ORIENTED_EDGE ( 'NONE', *, *, #19213, .F. ) ;
#4341=CARTESIAN_POINT ( 'NONE',  ( -2.607480562269073765, 145.2070736234661581, -8.025000000000000355 ) ) ;
#4343=VECTOR ( 'NONE', #13492, 1000.000000000000000 ) ;
#4347=AXIS2_PLACEMENT_3D ( 'NONE', #57276, #56588, #31220 ) ;
#4350=DIRECTION ( 'NONE',  ( -0.9704308468600219006, -0.2413793103448194366, -0.000000000000000000 ) ) ;
#4352=CARTESIAN_POINT ( 'NONE',  ( 14.98999599679679662, 146.4999999999999716, -9.500000000000000000 ) ) ;
#4353=DIRECTION ( 'NONE',  ( -0.000000000000000000, -0.000000000000000000, -1.000000000000000000 ) ) ;
#4364=VERTEX_POINT ( 'NONE', #6909 ) ;
#4367=VECTOR ( 'NONE', #47374, 1000.000000000000000 ) ;
#4370=PRESENTATION_STYLE_ASSIGNMENT (( #32746 ) ) ;
#4374=MECHANICAL_DESIGN_GEOMETRIC_PRESENTATION_REPRESENTATION('',(#47131),#6647);
#4375=DIRECTION ( 'NONE',  ( -1.000000000000000000, 1.224646799147349509E-16, 0.000000000000000000 ) ) ;
#4376=FILL_AREA_STYLE ('',( #52624 ) ) ;
#4381=CARTESIAN_POINT ( 'NONE',  ( 5.598654528085809545, 127.1449999999999818, -7.705886871421373741 ) ) ;
#4382=STYLED_ITEM ( 'NONE', ( #40964 ), #4768 ) ;
#4384=TOROIDAL_SURFACE ( 'NONE', #35793, 22.50000000000000000, 0.5000000000000000000 ) ;
#4385=LINE ( 'NONE', #53320, #49353 ) ;
#4389=LINE ( 'NONE', #25864, #11037 ) ;
#4390=SURFACE_STYLE_USAGE ( .BOTH. , #47380 ) ;
#4391=PRESENTATION_STYLE_ASSIGNMENT (( #57907 ) ) ;
#4393=( NAMED_UNIT ( * ) SI_UNIT ( $, .STERADIAN. ) SOLID_ANGLE_UNIT ( ) );
#4394=CARTESIAN_POINT ( 'NONE',  ( -24.21231517720798010, 113.4999999999999858, -7.000000000000000000 ) ) ;
#4401=( NAMED_UNIT ( * ) SI_UNIT ( $, .STERADIAN. ) SOLID_ANGLE_UNIT ( ) );
#4402=FILL_AREA_STYLE_COLOUR ( '', #22626 ) ;
#4406=CARTESIAN_POINT ( 'NONE',  ( 3.094860106618431583, 160.2050000000000125, 9.525000000000000355 ) ) ;
#4407=DIRECTION ( 'NONE',  ( 0.000000000000000000, 1.000000000000000000, 0.000000000000000000 ) ) ;
#4408=ADVANCED_FACE ( 'NONE', ( #65998 ), #1911, .T. ) ;
#4410=UNCERTAINTY_MEASURE_WITH_UNIT (LENGTH_MEASURE( 1.000000000000000082E-05 ), #44545, 'distance_accuracy_value', 'NONE');
#4415=CARTESIAN_POINT ( 'NONE',  ( -40.99999999999998579, 107.7459666924148394, 3.500000000000000444 ) ) ;
#4416=SURFACE_STYLE_USAGE ( .BOTH. , #63198 ) ;
#4418=FACE_OUTER_BOUND ( 'NONE', #44325, .T. ) ;
#4423=AXIS2_PLACEMENT_3D ( 'NONE', #12087, #65915, #27565 ) ;
#4425=EDGE_CURVE ( 'NONE', #28436, #58801, #26822, .T. ) ;
#4428=EDGE_CURVE ( 'NONE', #52813, #19239, #29029, .T. ) ;
#4433=EDGE_LOOP ( 'NONE', ( #63202, #19737, #38622, #55162 ) ) ;
#4435=ADVANCED_FACE ( 'NONE', ( #55791 ), #33586, .T. ) ;
#4439=CARTESIAN_POINT ( 'NONE',  ( 10.01517768586949231, 118.8049999999999926, 1.839758294383810543E-15 ) ) ;
#4441=CARTESIAN_POINT ( 'NONE',  ( 45.00000000000000000, 10.25709351175097694, 7.000000000000000000 ) ) ;
#4443=DIRECTION ( 'NONE',  ( -0.000000000000000000, -1.000000000000000000, -0.000000000000000000 ) ) ;
#4445=ORIENTED_EDGE ( 'NONE', *, *, #26740, .F. ) ;
#4446=CIRCLE ( 'NONE', #40454, 0.5000000000000004441 ) ;
#4447=CARTESIAN_POINT ( 'NONE',  ( -20.57648123223228254, 114.4999999999999574, -10.27659574468085069 ) ) ;
#4448=CARTESIAN_POINT ( 'NONE',  ( 44.99999999999977973, 149.4999999999999716, -9.500000000000000000 ) ) ;
#4451=CARTESIAN_POINT ( 'NONE',  ( -6.826472737025120807, 153.9929263765338021, 4.959722759717906548 ) ) ;
#4456=CARTESIAN_POINT ( 'NONE',  ( 20.35573775503900151, 114.9974703310426634, -9.999999999999998224 ) ) ;
#4457=VERTEX_POINT ( 'NONE', #68106 ) ;
#4458=CARTESIAN_POINT ( 'NONE',  ( 19.89974874213240597, 115.4999999999999574, 10.00000000000000000 ) ) ;
#4460=SURFACE_STYLE_USAGE ( .BOTH. , #52695 ) ;
#4466=AXIS2_PLACEMENT_3D ( 'NONE', #25371, #57389, #30632 ) ;
#4467=FACE_OUTER_BOUND ( 'NONE', #47565, .T. ) ;
#4469=CARTESIAN_POINT ( 'NONE',  ( -2.607480562269020918, 120.0929263765338249, -8.025000000000037659 ) ) ;
#4474=CARTESIAN_POINT ( 'NONE',  ( -24.21231517720798010, 113.4999999999999858, 7.000000000000000000 ) ) ;
#4475=DIRECTION ( 'NONE',  ( 1.000000000000000000, 0.000000000000000000, 0.000000000000000000 ) ) ;
#4476=CARTESIAN_POINT ( 'NONE',  ( 74.59262096826685706, 19.64589727361706650, 6.500000000000000000 ) ) ;
#4486=VECTOR ( 'NONE', #1371, 1000.000000000000000 ) ;
#4492=SURFACE_STYLE_FILL_AREA ( #40801 ) ;
#4494=( NAMED_UNIT ( * ) SI_UNIT ( $, .STERADIAN. ) SOLID_ANGLE_UNIT ( ) );
#4496=CARTESIAN_POINT ( 'NONE',  ( 9.058813317711338797, 124.9549999999999841, -2.943386871421372675 ) ) ;
#4498=DIRECTION ( 'NONE',  ( 0.000000000000000000, 0.000000000000000000, 1.000000000000000000 ) ) ;
#4501=CIRCLE ( 'NONE', #42737, 4.999999999999997335 ) ;
#4504=UNCERTAINTY_MEASURE_WITH_UNIT (LENGTH_MEASURE( 1.000000000000000082E-05 ), #53360, 'distance_accuracy_value', 'NONE');
#4506=EDGE_CURVE ( 'NONE', #3957, #7058, #3316, .T. ) ;
#4509=ADVANCED_FACE ( 'NONE', ( #35735 ), #57893, .F. ) ;
#4510=ORIENTED_EDGE ( 'NONE', *, *, #43270, .T. ) ;
#4512=AXIS2_PLACEMENT_3D ( 'NONE', #51247, #68463, #52646 ) ;
#4513=EDGE_CURVE ( 'NONE', #44423, #631, #64997, .T. ) ;
#4517=DIRECTION ( 'NONE',  ( 1.000000000000000000, 0.000000000000000000, -0.000000000000000000 ) ) ;
#4518=CARTESIAN_POINT ( 'NONE',  ( -34.99999999999999289, 99.99999999999998579, -7.500000000000000000 ) ) ;
#4519=DIRECTION ( 'NONE',  ( 3.469446951953611033E-15, -1.000000000000000000, 0.000000000000000000 ) ) ;
#4523=MECHANICAL_DESIGN_GEOMETRIC_PRESENTATION_REPRESENTATION('',(#34872),#67443);
#4524=UNCERTAINTY_MEASURE_WITH_UNIT (LENGTH_MEASURE( 1.000000000000000082E-05 ), #59042, 'distance_accuracy_value', 'NONE');
#4526=ADVANCED_FACE ( 'NONE', ( #26546 ), #17073, .T. ) ;
#4527=AXIS2_PLACEMENT_3D ( 'NONE', #38819, #44106, #1779 ) ;
#4528=CARTESIAN_POINT ( 'NONE',  ( -9.827790563157511022E-16, 148.4429263765338476, 8.025000000000000355 ) ) ;
#4529=DIRECTION ( 'NONE',  ( -1.000000000000000000, 0.000000000000000000, 0.000000000000000000 ) ) ;
#4531=ORIENTED_EDGE ( 'NONE', *, *, #10269, .F. ) ;
#4533=ORIENTED_EDGE ( 'NONE', *, *, #35808, .T. ) ;
#4534=DIRECTION ( 'NONE',  ( -1.734723475976805714E-15, -5.782411586589310307E-16, -1.000000000000000000 ) ) ;
#4535=CARTESIAN_POINT ( 'NONE',  ( 6.826472737025119919, 129.0070736234661695, 4.959722759717908325 ) ) ;
#4537=FILL_AREA_STYLE ('',( #10874 ) ) ;
#4539=ORIENTED_EDGE ( 'NONE', *, *, #51635, .T. ) ;
#4540=( GEOMETRIC_REPRESENTATION_CONTEXT ( 3 ) GLOBAL_UNCERTAINTY_ASSIGNED_CONTEXT ( ( #1106 ) ) GLOBAL_UNIT_ASSIGNED_CONTEXT ( ( #415, #15315, #31425 ) ) REPRESENTATION_CONTEXT ( 'NONE', 'WORKASPACE' ) );
#4541=STYLED_ITEM ( 'NONE', ( #68895 ), #11453 ) ;
#4543=CARTESIAN_POINT ( 'NONE',  ( 3.094860106618435136, 148.2949999999999307, -9.525000000000000355 ) ) ;
#4544=DIRECTION ( 'NONE',  ( 0.000000000000000000, 0.000000000000000000, -1.000000000000000000 ) ) ;
#4547=CARTESIAN_POINT ( 'NONE',  ( -8.102448949553179958, 153.0049999999999955, -5.886773742842749790 ) ) ;
#4549=VECTOR ( 'NONE', #68476, 1000.000000000000000 ) ;
#4550=FACE_OUTER_BOUND ( 'NONE', #6117, .T. ) ;
#4552=CARTESIAN_POINT ( 'NONE',  ( 0.000000000000000000, 128.9429263765338192, -8.025000000000000355 ) ) ;
#4553=LINE ( 'NONE', #15166, #65991 ) ;
#4554=UNCERTAINTY_MEASURE_WITH_UNIT (LENGTH_MEASURE( 1.000000000000000082E-05 ), #42301, 'distance_accuracy_value', 'NONE');
#4555=CARTESIAN_POINT ( 'NONE',  ( -75.37259712596974737, 36.06274621594484842, -9.736487711843981430 ) ) ;
#4557=CARTESIAN_POINT ( 'NONE',  ( -44.50000000000000000, 99.99999999999998579, 3.500000000000000000 ) ) ;
#4558=DIRECTION ( 'NONE',  ( 0.7292845505553197105, 0.6842105263157864936, -0.000000000000000000 ) ) ;
#4560=COLOUR_RGB ( '', 0.08235294, 0.09019608, 0.10196078) ;
#4561=CARTESIAN_POINT ( 'NONE',  ( 0.000000000000000000, 87.30187232391182306, 0.000000000000000000 ) ) ;
#4562=ORIENTED_EDGE ( 'NONE', *, *, #29613, .T. ) ;
#4564=DIRECTION ( 'NONE',  ( 0.000000000000000000, 0.000000000000000000, 1.000000000000000000 ) ) ;
#4567=UNCERTAINTY_MEASURE_WITH_UNIT (LENGTH_MEASURE( 1.000000000000000082E-05 ), #18889, 'distance_accuracy_value', 'NONE');
#4572=DIRECTION ( 'NONE',  ( -1.000000000000000000, 0.000000000000000000, 0.000000000000000000 ) ) ;
#4573=ORIENTED_EDGE ( 'NONE', *, *, #67515, .T. ) ;
#4582=AXIS2_PLACEMENT_3D ( 'NONE', #31953, #27681, #43596 ) ;
#4583=DIRECTION ( 'NONE',  ( 0.000000000000000000, -1.000000000000000000, 0.000000000000000000 ) ) ;
#4587=DIRECTION ( 'NONE',  ( 0.000000000000000000, 1.000000000000000000, 0.000000000000000000 ) ) ;
#4588=DIRECTION ( 'NONE',  ( 1.000000000000000000, 0.000000000000000000, 0.000000000000000000 ) ) ;
#4590=LINE ( 'NONE', #62311, #16654 ) ;
#4591=FACE_OUTER_BOUND ( 'NONE', #13665, .T. ) ;
#4593=EDGE_CURVE ( 'NONE', #60087, #27592, #20945, .T. ) ;
#4595=CARTESIAN_POINT ( 'NONE',  ( -5.598654528085806881, 148.7449999999999761, -7.705886871421374629 ) ) ;
#4597=CIRCLE ( 'NONE', #42867, 0.4999999999999994449 ) ;
#4598=DIRECTION ( 'NONE',  ( 1.000000000000000000, 0.000000000000000000, 0.000000000000000000 ) ) ;
#4600=STYLED_ITEM ( 'NONE', ( #18140 ), #34863 ) ;
#4603=VECTOR ( 'NONE', #28377, 1000.000000000000000 ) ;
#4604=( NAMED_UNIT ( * ) PLANE_ANGLE_UNIT ( ) SI_UNIT ( $, .RADIAN. ) );
#4609=CIRCLE ( 'NONE', #13592, 26.99999999999999645 ) ;
#4615=ORIENTED_EDGE ( 'NONE', *, *, #39985, .T. ) ;
#4617=LINE ( 'NONE', #10267, #52135 ) ;
#4620=CARTESIAN_POINT ( 'NONE',  ( -45.00000000000000000, 9.027119726910822095, 6.778758691516320489 ) ) ;
#4624=ORIENTED_EDGE ( 'NONE', *, *, #16570, .T. ) ;
#4631=DIRECTION ( 'NONE',  ( -0.000000000000000000, -0.000000000000000000, -1.000000000000000000 ) ) ;
#4632=CARTESIAN_POINT ( 'NONE',  ( -5.598654528085806881, 118.7449999999999903, -7.705886871421374629 ) ) ;
#4633=( NAMED_UNIT ( * ) PLANE_ANGLE_UNIT ( ) SI_UNIT ( $, .RADIAN. ) );
#4634=ORIENTED_EDGE ( 'NONE', *, *, #25431, .T. ) ;
#4636=CARTESIAN_POINT ( 'NONE',  ( 45.00000000000000000, -1.469576158976824618E-14, 10.00000000000000000 ) ) ;
#4637=CARTESIAN_POINT ( 'NONE',  ( 5.598654528085809545, 119.2549999999999812, -7.705886871421373741 ) ) ;
#4638=MECHANICAL_DESIGN_GEOMETRIC_PRESENTATION_REPRESENTATION('',(#58576),#45116);
#4641=ORIENTED_EDGE ( 'NONE', *, *, #24134, .F. ) ;
#4642=CARTESIAN_POINT ( 'NONE',  ( -9.058813317711338797, 147.4550000000000125, 2.943386871421373563 ) ) ;
#4643=UNCERTAINTY_MEASURE_WITH_UNIT (LENGTH_MEASURE( 1.000000000000000082E-05 ), #54692, 'distance_accuracy_value', 'NONE');
#4645=CIRCLE ( 'NONE', #42913, 0.5000000000000004441 ) ;
#4646=CARTESIAN_POINT ( 'NONE',  ( 21.02379604162874926, 114.4999999999999574, 10.00000000000000000 ) ) ;
#4647=DIRECTION ( 'NONE',  ( 0.000000000000000000, 0.000000000000000000, -1.000000000000000000 ) ) ;
#4648=AXIS2_PLACEMENT_3D ( 'NONE', #64682, #59735, #11542 ) ;
#4654=VERTEX_POINT ( 'NONE', #10735 ) ;
#4655=CARTESIAN_POINT ( 'NONE',  ( -47.50000000000000000, 99.99999999999992895, -10.00000000000000000 ) ) ;
#4658=FACE_OUTER_BOUND ( 'NONE', #11839, .T. ) ;
#4662=DIRECTION ( 'NONE',  ( 0.000000000000000000, 0.000000000000000000, 1.000000000000000000 ) ) ;
#4663=COLOUR_RGB ( '', 0.09019608, 0.27058824, 0.51372549) ;
#4666=EDGE_LOOP ( 'NONE', ( #60747, #58132, #63138 ) ) ;
#4669=LINE ( 'NONE', #379, #14557 ) ;
#4672=CARTESIAN_POINT ( 'NONE',  ( 0.000000000000000000, 154.4449999999999932, -9.525000000000000355 ) ) ;
#4677=ORIENTED_EDGE ( 'NONE', *, *, #22574, .T. ) ;
#4680=ADVANCED_FACE ( 'NONE', ( #47743 ), #69139, .F. ) ;
#4682=EDGE_CURVE ( 'NONE', #67303, #37663, #2170, .T. ) ;
#4683=CARTESIAN_POINT ( 'NONE',  ( -8.102448949553181734, 116.4949999999999761, 5.886773742842747126 ) ) ;
#4688=AXIS2_PLACEMENT_3D ( 'NONE', #68085, #36068, #30068 ) ;
#4691=VECTOR ( 'NONE', #42992, 1000.000000000000000 ) ;
#4696=SURFACE_SIDE_STYLE ('',( #403 ) ) ;
#4701=CARTESIAN_POINT ( 'NONE',  ( 75.00000000000000000, -2.215169945516535778E-14, -9.500000000000000000 ) ) ;
#4703=STYLED_ITEM ( 'NONE', ( #50253 ), #35510 ) ;
#4708=EDGE_CURVE ( 'NONE', #25004, #599, #20167, .T. ) ;
#4710=CARTESIAN_POINT ( 'NONE',  ( -9.827790563157511022E-16, 149.5570736234661524, 8.025000000000000355 ) ) ;
#4711=VECTOR ( 'NONE', #29260, 1000.000000000000000 ) ;
#4713=AXIS2_PLACEMENT_3D ( 'NONE', #29838, #67131, #3767 ) ;
#4720=CARTESIAN_POINT ( 'NONE',  ( -2.607480562269075097, 146.4070736234661183, 8.025000000000000355 ) ) ;
#4721=MECHANICAL_DESIGN_GEOMETRIC_PRESENTATION_REPRESENTATION('',(#45237),#63181);
#4723=CARTESIAN_POINT ( 'NONE',  ( 45.00000000000000000, 10.69371294336137979, -4.000000000000000000 ) ) ;
#4726=AXIS2_PLACEMENT_3D ( 'NONE', #23546, #28458, #55569 ) ;
#4727=ORIENTED_EDGE ( 'NONE', *, *, #69644, .T. ) ;
#4730=CIRCLE ( 'NONE', #62020, 17.00000000000000000 ) ;
#4741=( LENGTH_UNIT ( ) NAMED_UNIT ( * ) SI_UNIT ( .MILLI., .METRE. ) );
#4742=DIRECTION ( 'NONE',  ( 0.000000000000000000, 0.000000000000000000, 1.000000000000000000 ) ) ;
#4744=COLOUR_RGB ( '', 0.08235294, 0.09019608, 0.10196078) ;
#4745=DIRECTION ( 'NONE',  ( 0.000000000000000000, 0.000000000000000000, 1.000000000000000000 ) ) ;
#4746=VERTEX_POINT ( 'NONE', #18086 ) ;
#4749=CARTESIAN_POINT ( 'NONE',  ( -41.84210526315788314, 107.2928455055531600, 4.000000000000000000 ) ) ;
#4751=CARTESIAN_POINT ( 'NONE',  ( 3.094860106618431583, 123.0949999999999704, 9.525000000000000355 ) ) ;
#4754=ADVANCED_FACE ( 'NONE', ( #34593 ), #56049, .F. ) ;
#4755=FILL_AREA_STYLE ('',( #46332 ) ) ;
#4761=DIRECTION ( 'NONE',  ( 0.000000000000000000, 0.000000000000000000, -1.000000000000000000 ) ) ;
#4766=CARTESIAN_POINT ( 'NONE',  ( 0.000000000000000000, 87.30187232391182306, 0.000000000000000000 ) ) ;
#4768=ADVANCED_FACE ( 'NONE', ( #68027 ), #30015, .T. ) ;
#4774=DIRECTION ( 'NONE',  ( 1.000000000000000000, 0.000000000000000000, 0.000000000000000000 ) ) ;
#4775=CARTESIAN_POINT ( 'NONE',  ( -83.49999999999997158, 50.00000000000000000, 11.50000000000000000 ) ) ;
#4779=CARTESIAN_POINT ( 'NONE',  ( -5.598654528085808657, 153.7549999999999670, 7.705886871421373741 ) ) ;
#4780=SURFACE_SIDE_STYLE ('',( #52987 ) ) ;
#4781=DIRECTION ( 'NONE',  ( 4.336808689941999001E-16, 1.000000000000000000, -0.000000000000000000 ) ) ;
#4782=MECHANICAL_DESIGN_GEOMETRIC_PRESENTATION_REPRESENTATION('',(#42058),#17174);
#4790=AXIS2_PLACEMENT_3D ( 'NONE', #19082, #39553, #40588 ) ;
#4791=PRESENTATION_STYLE_ASSIGNMENT (( #42477 ) ) ;
#4792=UNCERTAINTY_MEASURE_WITH_UNIT (LENGTH_MEASURE( 1.000000000000000082E-05 ), #53570, 'distance_accuracy_value', 'NONE');
#4793=EDGE_CURVE ( 'NONE', #23836, #26070, #31357, .T. ) ;
#4796=FACE_OUTER_BOUND ( 'NONE', #47006, .T. ) ;
#4798=VERTEX_POINT ( 'NONE', #52548 ) ;
#4802=CARTESIAN_POINT ( 'NONE',  ( 0.000000000000000000, 115.0570736234661666, -8.025000000000000355 ) ) ;
#4805=ORIENTED_EDGE ( 'NONE', *, *, #50791, .T. ) ;
#4806=CARTESIAN_POINT ( 'NONE',  ( 74.99999999999998579, 50.00000000000000000, -10.00000000000000000 ) ) ;
#4808=STYLED_ITEM ( 'NONE', ( #42621 ), #29206 ) ;
#4811=CARTESIAN_POINT ( 'NONE',  ( 8.102448949553183510, 116.1049999999999756, -5.886773742842746238 ) ) ;
#4812=( NAMED_UNIT ( * ) PLANE_ANGLE_UNIT ( ) SI_UNIT ( $, .RADIAN. ) );
#4813=CARTESIAN_POINT ( 'NONE',  ( -71.50000000000000000, 35.92875272052971525, -7.500000000000000000 ) ) ;
#4814=DIRECTION ( 'NONE',  ( -1.000000000000000000, 0.000000000000000000, 0.000000000000000000 ) ) ;
#4820=CARTESIAN_POINT ( 'NONE',  ( -4.716976649647097730, 153.2429263765338021, -6.492361379858953896 ) ) ;
#4826=ORIENTED_EDGE ( 'NONE', *, *, #50651, .T. ) ;
#4827=CARTESIAN_POINT ( 'NONE',  ( 20.17679519342876304, 115.4776649671489963, 10.00000000000000000 ) ) ;
#4829=DIRECTION ( 'NONE',  ( -1.000000000000000000, 0.000000000000000000, 0.000000000000000000 ) ) ;
#4830=( NAMED_UNIT ( * ) PLANE_ANGLE_UNIT ( ) SI_UNIT ( $, .RADIAN. ) );
#4833=( NAMED_UNIT ( * ) SI_UNIT ( $, .STERADIAN. ) SOLID_ANGLE_UNIT ( ) );
#4840=CARTESIAN_POINT ( 'NONE',  ( -71.99999999999998579, 119.9999999999997868, 9.500000000000000000 ) ) ;
#4844=FILL_AREA_STYLE_COLOUR ( '', #3968 ) ;
#4846=DIRECTION ( 'NONE',  ( 1.000000000000000000, 0.000000000000000000, 0.000000000000000000 ) ) ;
#4848=PRESENTATION_STYLE_ASSIGNMENT (( #53054 ) ) ;
#4856=VECTOR ( 'NONE', #67210, 1000.000000000000000 ) ;
#4859=AXIS2_PLACEMENT_3D ( 'NONE', #9505, #30925, #4166 ) ;
#4861=CARTESIAN_POINT ( 'NONE',  ( 9.489509921829204941, 154.5000000000000568, -0.9314843046822294248 ) ) ;
#4863=CARTESIAN_POINT ( 'NONE',  ( -74.58429712092500097, 36.42179758710307169, -9.999999998919950173 ) ) ;
#4867=CARTESIAN_POINT ( 'NONE',  ( 10.01517768586949231, 127.8050000000000068, 1.839758294383810543E-15 ) ) ;
#4868=DIRECTION ( 'NONE',  ( 1.000000000000000000, 0.000000000000000000, 0.000000000000000000 ) ) ;
#4873=FILL_AREA_STYLE ('',( #20355 ) ) ;
#4875=ORIENTED_EDGE ( 'NONE', *, *, #40850, .T. ) ;
#4876=CARTESIAN_POINT ( 'NONE',  ( 65.50000000000000000, 1.797044900979284448E-15, -6.500000000000000000 ) ) ;
#4878=CARTESIAN_POINT ( 'NONE',  ( 65.00000000000000000, 1.797044900979284448E-15, -12.00000000000000000 ) ) ;
#4883=CARTESIAN_POINT ( 'NONE',  ( -45.89269293898073698, 9.343722028457033701, -6.169771923672656477 ) ) ;
#4885=COLOUR_RGB ( '', 0.31764706, 0.68627451, 0.89019608) ;
#4887=PRESENTATION_STYLE_ASSIGNMENT (( #69272 ) ) ;
#4891=ORIENTED_EDGE ( 'NONE', *, *, #33979, .F. ) ;
#4893=CARTESIAN_POINT ( 'NONE',  ( 20.17806131642189271, 115.4772719928210876, -10.00000000000000178 ) ) ;
#4894=VERTEX_POINT ( 'NONE', #20143 ) ;
#4895=( NAMED_UNIT ( * ) SI_UNIT ( $, .STERADIAN. ) SOLID_ANGLE_UNIT ( ) );
#4896=( NAMED_UNIT ( * ) PLANE_ANGLE_UNIT ( ) SI_UNIT ( $, .RADIAN. ) );
#4899=CARTESIAN_POINT ( 'NONE',  ( 3.094860106618435136, 154.2949999999999875, -9.525000000000000355 ) ) ;
#4903=CARTESIAN_POINT ( 'NONE',  ( 3.094860106618435136, 149.4049999999999443, -9.525000000000000355 ) ) ;
#4904=CARTESIAN_POINT ( 'NONE',  ( -34.99999999999992895, 112.4999999999999858, 9.500000000000000000 ) ) ;
#4907=CARTESIAN_POINT ( 'NONE',  ( 7.632228543268608334, 128.3429263765338249, -2.479861379858951942 ) ) ;
#4908=CARTESIAN_POINT ( 'NONE',  ( -23.21231517720798010, 113.4999999999999858, -10.00000000000000000 ) ) ;
#4911=( GEOMETRIC_REPRESENTATION_CONTEXT ( 3 ) GLOBAL_UNCERTAINTY_ASSIGNED_CONTEXT ( ( #5327 ) ) GLOBAL_UNIT_ASSIGNED_CONTEXT ( ( #7640, #34034, #29072 ) ) REPRESENTATION_CONTEXT ( 'NONE', 'WORKASPACE' ) );
#4913=EDGE_CURVE ( 'NONE', #49132, #2827, #33629, .T. ) ;
#4921=DIRECTION ( 'NONE',  ( -0.000000000000000000, -0.000000000000000000, -1.000000000000000000 ) ) ;
#4923=AXIS2_PLACEMENT_3D ( 'NONE', #20250, #68118, #19899 ) ;
#4924=EDGE_CURVE ( 'NONE', #60894, #15891, #4669, .T. ) ;
#4925=CIRCLE ( 'NONE', #18448, 5.000000000000004441 ) ;
#4927=LINE ( 'NONE', #38377, #25958 ) ;
#4928=CARTESIAN_POINT ( 'NONE',  ( 41.39060477125153170, 107.1334711628775693, 3.500000000000000888 ) ) ;
#4932=ORIENTED_EDGE ( 'NONE', *, *, #12796, .F. ) ;
#4942=EDGE_CURVE ( 'NONE', #37991, #15417, #2055, .T. ) ;
#4944=EDGE_CURVE ( 'NONE', #23886, #64569, #56077, .T. ) ;
#4945=DIRECTION ( 'NONE',  ( 1.000000000000000000, 0.000000000000000000, 0.000000000000000000 ) ) ;
#4948=ADVANCED_FACE ( 'NONE', ( #69063 ), #32800, .T. ) ;
#4949=SURFACE_SIDE_STYLE ('',( #36667 ) ) ;
#4950=SURFACE_SIDE_STYLE ('',( #53155 ) ) ;
#4951=DIRECTION ( 'NONE',  ( 1.000000000000000000, 0.000000000000000000, 0.000000000000000000 ) ) ;
#4952=( NAMED_UNIT ( * ) PLANE_ANGLE_UNIT ( ) SI_UNIT ( $, .RADIAN. ) );
#4954=CARTESIAN_POINT ( 'NONE',  ( 0.000000000000000000, 151.4449999999999932, -9.525000000000000355 ) ) ;
#4956=CARTESIAN_POINT ( 'NONE',  ( -44.50000000000000000, 10.49999999999998224, -3.000000000000000444 ) ) ;
#4958=SURFACE_STYLE_USAGE ( .BOTH. , #64040 ) ;
#4960=ORIENTED_EDGE ( 'NONE', *, *, #64085, .T. ) ;
#4965=DIRECTION ( 'NONE',  ( 1.000000000000000000, 0.000000000000000000, 0.000000000000000000 ) ) ;
#4966=MECHANICAL_DESIGN_GEOMETRIC_PRESENTATION_REPRESENTATION('',(#35305),#52197);
#4969=( GEOMETRIC_REPRESENTATION_CONTEXT ( 3 ) GLOBAL_UNCERTAINTY_ASSIGNED_CONTEXT ( ( #35383 ) ) GLOBAL_UNIT_ASSIGNED_CONTEXT ( ( #51450, #50412, #23326 ) ) REPRESENTATION_CONTEXT ( 'NONE', 'WORKASPACE' ) );
#4971=FACE_OUTER_BOUND ( 'NONE', #45631, .T. ) ;
#4974=DIRECTION ( 'NONE',  ( -0.000000000000000000, -1.000000000000000000, 0.000000000000000000 ) ) ;
#4982=STYLED_ITEM ( 'NONE', ( #60675 ), #48567 ) ;
#4984=DIRECTION ( 'NONE',  ( -0.000000000000000000, -0.000000000000000000, 1.000000000000000000 ) ) ;
#4985=CARTESIAN_POINT ( 'NONE',  ( -9.058813317711338797, 116.3449999999999847, 2.943386871421373563 ) ) ;
#4989=CARTESIAN_POINT ( 'NONE',  ( 8.102448949553179958, 124.5049999999999812, 5.886773742842750679 ) ) ;
#4991=CARTESIAN_POINT ( 'NONE',  ( -41.39060477124900927, 107.1334711628759493, -3.500000000000001776 ) ) ;
#4992=ORIENTED_EDGE ( 'NONE', *, *, #29873, .F. ) ;
#4993=CARTESIAN_POINT ( 'NONE',  ( 0.000000000000000000, 146.5549999999999784, -9.525000000000000355 ) ) ;
#4997=PLANE ( 'NONE',  #46732 ) ;
#5000=ORIENTED_EDGE ( 'NONE', *, *, #32218, .T. ) ;
#5001=LINE ( 'NONE', #56469, #7491 ) ;
#5003=( LENGTH_UNIT ( ) NAMED_UNIT ( * ) SI_UNIT ( .MILLI., .METRE. ) );
#5007=EDGE_CURVE ( 'NONE', #62297, #47726, #47196, .T. ) ;
#5010=( NAMED_UNIT ( * ) PLANE_ANGLE_UNIT ( ) SI_UNIT ( $, .RADIAN. ) );
#5012=SURFACE_STYLE_FILL_AREA ( #43052 ) ;
#5015=CARTESIAN_POINT ( 'NONE',  ( -71.50000000000000000, 35.92875272052971525, -7.000000000000000000 ) ) ;
#5019=EDGE_CURVE ( 'NONE', #8109, #53103, #27557, .T. ) ;
#5023=CARTESIAN_POINT ( 'NONE',  ( -3.094860106618434248, 149.7949999999999875, 9.525000000000000355 ) ) ;
#5025=CIRCLE ( 'NONE', #16263, 0.5000000000000004441 ) ;
#5028=VERTEX_POINT ( 'NONE', #50617 ) ;
#5030=DIRECTION ( 'NONE',  ( 0.000000000000000000, 1.000000000000000000, 3.469446951953611033E-15 ) ) ;
#5031=CARTESIAN_POINT ( 'NONE',  ( 60.00000000000000000, 1.797044900979284448E-15, -12.00000000000000000 ) ) ;
#5033=AXIS2_PLACEMENT_3D ( 'NONE', #17269, #54161, #6318 ) ;
#5035=CARTESIAN_POINT ( 'NONE',  ( -3.094860106618432471, 121.5949999999999847, -9.525000000000000355 ) ) ;
#5037=AXIS2_PLACEMENT_3D ( 'NONE', #25994, #31624, #15484 ) ;
#5038=AXIS2_PLACEMENT_3D ( 'NONE', #18060, #66234, #1817 ) ;
#5040=( LENGTH_UNIT ( ) NAMED_UNIT ( * ) SI_UNIT ( .MILLI., .METRE. ) );
#5042=VERTEX_POINT ( 'NONE', #39747 ) ;
#5047=DIRECTION ( 'NONE',  ( 1.000000000000000000, 0.000000000000000000, 0.000000000000000000 ) ) ;
#5050=SURFACE_STYLE_FILL_AREA ( #10348 ) ;
#5055=EDGE_CURVE ( 'NONE', #53177, #60077, #55187, .T. ) ;
#5057=FILL_AREA_STYLE_COLOUR ( '', #15844 ) ;
#5061=EDGE_LOOP ( 'NONE', ( #58878, #33808, #753, #48582, #62588 ) ) ;
#5063=DIRECTION ( 'NONE',  ( 0.000000000000000000, 1.000000000000000000, -0.000000000000000000 ) ) ;
#5064=CARTESIAN_POINT ( 'NONE',  ( 6.826472737025121695, 141.6070736234661354, -4.959722759717905660 ) ) ;
#5065=STYLED_ITEM ( 'NONE', ( #64457 ), #27772 ) ;
#5070=CARTESIAN_POINT ( 'NONE',  ( -52.50000000000000000, -2.024042244987997205E-14, -12.00000000000000000 ) ) ;
#5073=( GEOMETRIC_REPRESENTATION_CONTEXT ( 3 ) GLOBAL_UNCERTAINTY_ASSIGNED_CONTEXT ( ( #64985 ) ) GLOBAL_UNIT_ASSIGNED_CONTEXT ( ( #6481, #12117, #27920 ) ) REPRESENTATION_CONTEXT ( 'NONE', 'WORKASPACE' ) );
#5079=STYLED_ITEM ( 'NONE', ( #33697 ), #49078 ) ;
#5081=AXIS2_PLACEMENT_3D ( 'NONE', #4474, #42201, #68191 ) ;
#5082=( NAMED_UNIT ( * ) SI_UNIT ( $, .STERADIAN. ) SOLID_ANGLE_UNIT ( ) );
#5084=VERTEX_POINT ( 'NONE', #55544 ) ;
#5086=EDGE_CURVE ( 'NONE', #42518, #26425, #60659, .T. ) ;
#5088=VERTEX_POINT ( 'NONE', #28796 ) ;
#5090=( LENGTH_UNIT ( ) NAMED_UNIT ( * ) SI_UNIT ( .MILLI., .METRE. ) );
#5091=MECHANICAL_DESIGN_GEOMETRIC_PRESENTATION_REPRESENTATION('',(#26388),#54501);
#5092=DIRECTION ( 'NONE',  ( 0.000000000000000000, 0.000000000000000000, 1.000000000000000000 ) ) ;
#5096=EDGE_CURVE ( 'NONE', #65582, #51799, #552, .T. ) ;
#5098=( NAMED_UNIT ( * ) SI_UNIT ( $, .STERADIAN. ) SOLID_ANGLE_UNIT ( ) );
#5101=CARTESIAN_POINT ( 'NONE',  ( 10.01517768586949408, 123.6949999999999790, 1.839758294383810543E-15 ) ) ;
#5105=VERTEX_POINT ( 'NONE', #58656 ) ;
#5108=SURFACE_STYLE_FILL_AREA ( #31836 ) ;
#5109=CARTESIAN_POINT ( 'NONE',  ( -8.437984349512095861, 130.8070736234661524, -5.166775262442723748E-16 ) ) ;
#5111=SURFACE_STYLE_USAGE ( .BOTH. , #38206 ) ;
#5116=DIRECTION ( 'NONE',  ( -1.000000000000000000, 0.000000000000000000, 0.000000000000000000 ) ) ;
#5118=UNCERTAINTY_MEASURE_WITH_UNIT (LENGTH_MEASURE( 1.000000000000000082E-05 ), #52629, 'distance_accuracy_value', 'NONE');
#5120=STYLED_ITEM ( 'NONE', ( #56923 ), #64489 ) ;
#5122=CARTESIAN_POINT ( 'NONE',  ( 60.00000000000000000, 1.797044900979284448E-15, 12.00000000000000000 ) ) ;
#5123=CIRCLE ( 'NONE', #14139, 13.99999999999999822 ) ;
#5127=ADVANCED_FACE ( 'NONE', ( #36202, #14727 ), #51657, .F. ) ;
#5130=AXIS2_PLACEMENT_3D ( 'NONE', #30224, #35545, #61538 ) ;
#5131=DIRECTION ( 'NONE',  ( 1.000000000000000000, -3.469446951953611033E-15, 0.000000000000000000 ) ) ;
#5134=PRESENTATION_STYLE_ASSIGNMENT (( #32224 ) ) ;
#5138=CARTESIAN_POINT ( 'NONE',  ( -4.716976649647097730, 118.3570736234661638, -6.492361379858953896 ) ) ;
#5140=STYLED_ITEM ( 'NONE', ( #47684 ), #32592 ) ;
#5142=CARTESIAN_POINT ( 'NONE',  ( -74.99999999999998579, 50.00000000000000000, 9.500000000000001776 ) ) ;
#5145=ORIENTED_EDGE ( 'NONE', *, *, #63847, .T. ) ;
#5147=EDGE_CURVE ( 'NONE', #20549, #29123, #21971, .T. ) ;
#5150=ADVANCED_FACE ( 'NONE', ( #52707 ), #25263, .F. ) ;
#5151=CARTESIAN_POINT ( 'NONE',  ( -10.01517768586949231, 117.3049999999999784, -6.132527647946036459E-16 ) ) ;
#5152=CARTESIAN_POINT ( 'NONE',  ( -74.99999999999998579, 119.9999999999997726, 10.00000000000000000 ) ) ;
#5155=ORIENTED_EDGE ( 'NONE', *, *, #5961, .F. ) ;
#5158=LINE ( 'NONE', #59927, #8138 ) ;
#5160=FILL_AREA_STYLE ('',( #69533 ) ) ;
#5162=CARTESIAN_POINT ( 'NONE',  ( -2.607480562269073765, 159.0929263765338533, -8.025000000000000355 ) ) ;
#5163=EDGE_CURVE ( 'NONE', #42076, #29454, #44462, .T. ) ;
#5165=ORIENTED_EDGE ( 'NONE', *, *, #38417, .F. ) ;
#5166=STYLED_ITEM ( 'NONE', ( #29290 ), #49897 ) ;
#5168=CARTESIAN_POINT ( 'NONE',  ( -71.99999999999998579, 63.67479433117734544, 9.500000000000000000 ) ) ;
#5169=DIRECTION ( 'NONE',  ( 0.000000000000000000, 0.000000000000000000, -1.000000000000000000 ) ) ;
#5174=CARTESIAN_POINT ( 'NONE',  ( 7.632228543268607446, 116.0429263765338277, 2.479861379858954606 ) ) ;
#5178=CARTESIAN_POINT ( 'NONE',  ( -45.89905495956738690, 9.405628579031729330, -6.500000000000000000 ) ) ;
#5181=CARTESIAN_POINT ( 'NONE',  ( 49.12162162162162105, 13.70805908423323594, -9.500000000000000000 ) ) ;
#5182=CIRCLE ( 'NONE', #13026, 0.5000000000000004441 ) ;
#5183=ORIENTED_EDGE ( 'NONE', *, *, #9856, .T. ) ;
#5184=SURFACE_SIDE_STYLE ('',( #36904 ) ) ;
#5186=SURFACE_STYLE_FILL_AREA ( #21032 ) ;
#5190=AXIS2_PLACEMENT_3D ( 'NONE', #68706, #36001, #52880 ) ;
#5201=CARTESIAN_POINT ( 'NONE',  ( 5.598654528085805993, 136.3550000000000182, 7.705886871421374629 ) ) ;
#5213=( NAMED_UNIT ( * ) PLANE_ANGLE_UNIT ( ) SI_UNIT ( $, .RADIAN. ) );
#5214=AXIS2_PLACEMENT_3D ( 'NONE', #35638, #25413, #36369 ) ;
#5216=EDGE_LOOP ( 'NONE', ( #33426, #59584, #42951, #9873 ) ) ;
#5217=CARTESIAN_POINT ( 'NONE',  ( -45.91547277936962246, 9.430195807687216103, -6.039972492249777503 ) ) ;
#5219=EDGE_CURVE ( 'NONE', #53591, #3129, #6239, .T. ) ;
#5227=LINE ( 'NONE', #37992, #8471 ) ;
#5229=CARTESIAN_POINT ( 'NONE',  ( 0.000000000000000000, 130.0570736234661524, -8.025000000000000355 ) ) ;
#5231=ORIENTED_EDGE ( 'NONE', *, *, #60605, .F. ) ;
#5232=LINE ( 'NONE', #26675, #52675 ) ;
#5235=CARTESIAN_POINT ( 'NONE',  ( -10.01517768586949231, 152.1949999999999932, -6.132527647946036459E-16 ) ) ;
#5236=( NAMED_UNIT ( * ) SI_UNIT ( $, .STERADIAN. ) SOLID_ANGLE_UNIT ( ) );
#5238=STYLED_ITEM ( 'NONE', ( #36868 ), #46 ) ;
#5240=DIRECTION ( 'NONE',  ( 0.000000000000000000, 0.000000000000000000, -1.000000000000000000 ) ) ;
#5243=CARTESIAN_POINT ( 'NONE',  ( -6.826472737025120807, 129.9929263765338021, 4.959722759717906548 ) ) ;
#5246=( GEOMETRIC_REPRESENTATION_CONTEXT ( 3 ) GLOBAL_UNCERTAINTY_ASSIGNED_CONTEXT ( ( #33976 ) ) GLOBAL_UNIT_ASSIGNED_CONTEXT ( ( #54648, #761, #59573 ) ) REPRESENTATION_CONTEXT ( 'NONE', 'WORKASPACE' ) );
#5247=EDGE_CURVE ( 'NONE', #48466, #40049, #62384, .T. ) ;
#5248=LINE ( 'NONE', #4557, #45252 ) ;
#5251=ORIENTED_EDGE ( 'NONE', *, *, #8824, .T. ) ;
#5253=( NAMED_UNIT ( * ) PLANE_ANGLE_UNIT ( ) SI_UNIT ( $, .RADIAN. ) );
#5256=( LENGTH_UNIT ( ) NAMED_UNIT ( * ) SI_UNIT ( .MILLI., .METRE. ) );
#5257=UNCERTAINTY_MEASURE_WITH_UNIT (LENGTH_MEASURE( 1.000000000000000082E-05 ), #33574, 'distance_accuracy_value', 'NONE');
#5262=ORIENTED_EDGE ( 'NONE', *, *, #60547, .F. ) ;
#5263=DIRECTION ( 'NONE',  ( 0.000000000000000000, 0.000000000000000000, -1.000000000000000000 ) ) ;
#5264=TOROIDAL_SURFACE ( 'NONE', #48017, 14.49999999999999822, 0.5000000000000000000 ) ;
#5266=EDGE_LOOP ( 'NONE', ( #16790, #8004, #9779, #12242, #66524, #59127 ) ) ;
#5275=ORIENTED_EDGE ( 'NONE', *, *, #15467, .F. ) ;
#5276=CARTESIAN_POINT ( 'NONE',  ( -60.00000000000000000, -2.024042244987997205E-14, 10.00000000000000000 ) ) ;
#5277=CARTESIAN_POINT ( 'NONE',  ( 15.98999599679679839, 117.9999999999999716, -7.000000000000000000 ) ) ;
#5279=CIRCLE ( 'NONE', #4156, 4.999999999999997335 ) ;
#5281=CARTESIAN_POINT ( 'NONE',  ( -5.598654528085806881, 157.7450000000000045, -7.705886871421374629 ) ) ;
#5283=CARTESIAN_POINT ( 'NONE',  ( -2.607480562269094637, 112.2070736234661439, -8.024999999999986144 ) ) ;
#5285=LINE ( 'NONE', #35684, #4691 ) ;
#5286=UNCERTAINTY_MEASURE_WITH_UNIT (LENGTH_MEASURE( 1.000000000000000082E-05 ), #37377, 'distance_accuracy_value', 'NONE');
#5299=CARTESIAN_POINT ( 'NONE',  ( -44.99999999999966604, 8.592356338113384950, 6.069948737345426615 ) ) ;
#5314=EDGE_CURVE ( 'NONE', #849, #69341, #17470, .T. ) ;
#5315=LINE ( 'NONE', #52856, #18568 ) ;
#5316=CARTESIAN_POINT ( 'NONE',  ( 3.094860106618431583, 120.0949999999999704, 9.525000000000000355 ) ) ;
#5317=LINE ( 'NONE', #58807, #21620 ) ;
#5320=CARTESIAN_POINT ( 'NONE',  ( 10.01517768586949408, 121.8049999999999642, 1.839758294383810543E-15 ) ) ;
#5325=ORIENTED_EDGE ( 'NONE', *, *, #52039, .T. ) ;
#5326=CARTESIAN_POINT ( 'NONE',  ( 3.094860106618435136, 152.4049999999999443, -9.525000000000000355 ) ) ;
#5327=UNCERTAINTY_MEASURE_WITH_UNIT (LENGTH_MEASURE( 1.000000000000000082E-05 ), #7640, 'distance_accuracy_value', 'NONE');
#5329=SURFACE_SIDE_STYLE ('',( #32407 ) ) ;
#5332=CARTESIAN_POINT ( 'NONE',  ( -74.99999999999998579, 50.00000000000000000, -12.00000000000000000 ) ) ;
#5333=FACE_BOUND ( 'NONE', #665, .T. ) ;
#5334=FILL_AREA_STYLE ('',( #358 ) ) ;
#5340=UNCERTAINTY_MEASURE_WITH_UNIT (LENGTH_MEASURE( 1.000000000000000082E-05 ), #45102, 'distance_accuracy_value', 'NONE');
#5341=DIRECTION ( 'NONE',  ( 0.000000000000000000, 0.000000000000000000, 1.000000000000000000 ) ) ;
#5342=CARTESIAN_POINT ( 'NONE',  ( -71.50000000000000000, 50.00000000000000000, 7.500000000000000000 ) ) ;
#5345=CARTESIAN_POINT ( 'NONE',  ( 60.00000000000000000, 149.4999999999999716, 9.500000000000000000 ) ) ;
#5351=CARTESIAN_POINT ( 'NONE',  ( -60.00000000000000000, -2.024042244987997205E-14, 7.000000000000000000 ) ) ;
#5353=TOROIDAL_SURFACE ( 'NONE', #45823, 1.000000000000000000, 0.5000000000000000000 ) ;
#5358=( NAMED_UNIT ( * ) PLANE_ANGLE_UNIT ( ) SI_UNIT ( $, .RADIAN. ) );
#5359=STYLED_ITEM ( 'NONE', ( #65322 ), #65984 ) ;
#5361=CARTESIAN_POINT ( 'NONE',  ( 5.598654528085809545, 124.1449999999999960, -7.705886871421373741 ) ) ;
#5363=DIRECTION ( 'NONE',  ( 0.000000000000000000, 0.000000000000000000, 1.000000000000000000 ) ) ;
#5364=SURFACE_STYLE_FILL_AREA ( #32126 ) ;
#5370=CYLINDRICAL_SURFACE ( 'NONE', #25347, 8.025000000000000355 ) ;
#5385=EDGE_LOOP ( 'NONE', ( #45720, #20459, #23660, #56399 ) ) ;
#5388=ADVANCED_FACE ( 'NONE', ( #54411, #194, #21718 ), #37949, .T. ) ;
#5389=DIRECTION ( 'NONE',  ( 0.000000000000000000, -1.000000000000000000, 0.000000000000000000 ) ) ;
#5392=SURFACE_SIDE_STYLE ('',( #59204 ) ) ;
#5393=CARTESIAN_POINT ( 'NONE',  ( -4.716976649647098618, 146.2570736234661410, 6.492361379858953008 ) ) ;
#5395=CARTESIAN_POINT ( 'NONE',  ( 45.00000000000000000, 10.69371294336137623, -3.707106781186547906 ) ) ;
#5396=ADVANCED_FACE ( 'NONE', ( #23792 ), #61074, .T. ) ;
#5398=UNCERTAINTY_MEASURE_WITH_UNIT (LENGTH_MEASURE( 1.000000000000000082E-05 ), #27204, 'distance_accuracy_value', 'NONE');
#5399=VERTEX_POINT ( 'NONE', #66714 ) ;
#5401=CARTESIAN_POINT ( 'NONE',  ( -23.21231517720797655, 117.4999999999999716, 7.000000000000000000 ) ) ;
#5402=DIRECTION ( 'NONE',  ( 0.000000000000000000, -1.000000000000000000, -0.000000000000000000 ) ) ;
#5406=STYLED_ITEM ( 'NONE', ( #66658 ), #14177 ) ;
#5414=( NAMED_UNIT ( * ) PLANE_ANGLE_UNIT ( ) SI_UNIT ( $, .RADIAN. ) );
#5416=EDGE_LOOP ( 'NONE', ( #48385, #30225, #52911, #20775 ) ) ;
#5423=CARTESIAN_POINT ( 'NONE',  ( -8.102448949553179958, 125.4949999999999903, 5.886773742842747126 ) ) ;
#5425=EDGE_CURVE ( 'NONE', #32302, #16942, #5123, .T. ) ;
#5426=MECHANICAL_DESIGN_GEOMETRIC_PRESENTATION_REPRESENTATION('',(#15576),#20052);
#5427=EDGE_LOOP ( 'NONE', ( #53029, #27977, #45709, #59570 ) ) ;
#5428=CARTESIAN_POINT ( 'NONE',  ( -84.49999999999997158, 50.00000000000000000, -10.49999999999999822 ) ) ;
#5431=CARTESIAN_POINT ( 'NONE',  ( -67.99999999999998579, -2.024042244987997205E-14, 12.00000000000000000 ) ) ;
#5443=CARTESIAN_POINT ( 'NONE',  ( -24.21231517720798010, 112.9999999999999858, 7.500000000000000000 ) ) ;
#5444=AXIS2_PLACEMENT_3D ( 'NONE', #15971, #59521, #33165 ) ;
#5445=EDGE_CURVE ( 'NONE', #40233, #30278, #42312, .T. ) ;
#5446=EDGE_CURVE ( 'NONE', #40883, #21177, #44503, .T. ) ;
#5447=SURFACE_STYLE_FILL_AREA ( #22352 ) ;
#5448=CARTESIAN_POINT ( 'NONE',  ( 2.607480562269030688, 152.7070736234661581, 8.025000000000034106 ) ) ;
#5449=AXIS2_PLACEMENT_3D ( 'NONE', #43447, #60250, #38502 ) ;
#5453=EDGE_CURVE ( 'NONE', #8394, #4028, #18654, .T. ) ;
#5462=CARTESIAN_POINT ( 'NONE',  ( 2.607480562269071989, 110.7070736234661723, 8.025000000000002132 ) ) ;
#5463=( GEOMETRIC_REPRESENTATION_CONTEXT ( 3 ) GLOBAL_UNCERTAINTY_ASSIGNED_CONTEXT ( ( #53121 ) ) GLOBAL_UNIT_ASSIGNED_CONTEXT ( ( #67493, #13322, #51674 ) ) REPRESENTATION_CONTEXT ( 'NONE', 'WORKASPACE' ) );
#5465=SURFACE_STYLE_FILL_AREA ( #37574 ) ;
#5466=FILL_AREA_STYLE_COLOUR ( '', #22934 ) ;
#5467=VERTEX_POINT ( 'NONE', #30794 ) ;
#5468=( GEOMETRIC_REPRESENTATION_CONTEXT ( 3 ) GLOBAL_UNCERTAINTY_ASSIGNED_CONTEXT ( ( #68603 ) ) GLOBAL_UNIT_ASSIGNED_CONTEXT ( ( #56852, #42114, #19550 ) ) REPRESENTATION_CONTEXT ( 'NONE', 'WORKASPACE' ) );
#5470=CARTESIAN_POINT ( 'NONE',  ( 65.00000000000000000, 1.797044900979284448E-15, -7.000000000000017764 ) ) ;
#5474=CARTESIAN_POINT ( 'NONE',  ( 5.598654528085805993, 133.3549999999999898, 7.705886871421374629 ) ) ;
#5476=CARTESIAN_POINT ( 'NONE',  ( 75.00000000000000000, 19.99999999999997868, -6.000000000000000000 ) ) ;
#5477=( GEOMETRIC_REPRESENTATION_CONTEXT ( 3 ) GLOBAL_UNCERTAINTY_ASSIGNED_CONTEXT ( ( #30606 ) ) GLOBAL_UNIT_ASSIGNED_CONTEXT ( ( #20747, #58717, #4895 ) ) REPRESENTATION_CONTEXT ( 'NONE', 'WORKASPACE' ) );
#5482=( BOUNDED_CURVE ( )  B_SPLINE_CURVE ( 2, ( #47867, #32641, #64677, #43942, #69267, #58698, #26324, #10523, #21063, #32301, #226 ),
 .UNSPECIFIED., .F., .F. ) 
 B_SPLINE_CURVE_WITH_KNOTS ( ( 3, 2, 2, 2, 2, 3 ),
 ( 0.5294117647058825815, 0.5352941176470590312, 0.5411764705882354809, 0.5470588235294120416, 0.5529411764705884913, 0.5588235294117649410 ),
 .UNSPECIFIED. ) 
 CURVE ( )  GEOMETRIC_REPRESENTATION_ITEM ( )  RATIONAL_B_SPLINE_CURVE ( ( 0.9999999999999981126, 0.9510565162951554186, 1.000000000000000000, 0.9510565162951535312, 1.000000000000000000, 0.9510565162951535312, 1.000000000000000000, 0.9510565162951535312, 1.000000000000000000, 0.9510565162951516438, 1.000000000000001776 ) ) 
 REPRESENTATION_ITEM ( '' )  );
#5485=CARTESIAN_POINT ( 'NONE',  ( -7.632228543268608334, 150.8429263765338249, 2.479861379858952830 ) ) ;
#5487=LINE ( 'NONE', #50432, #19449 ) ;
#5491=DIRECTION ( 'NONE',  ( -0.9486832980505138790, -0.3162277660168378857, 0.000000000000000000 ) ) ;
#5492=( NAMED_UNIT ( * ) PLANE_ANGLE_UNIT ( ) SI_UNIT ( $, .RADIAN. ) );
#5499=( NAMED_UNIT ( * ) SI_UNIT ( $, .STERADIAN. ) SOLID_ANGLE_UNIT ( ) );
#5501=DIRECTION ( 'NONE',  ( 0.000000000000000000, -1.000000000000000000, 0.000000000000000000 ) ) ;
#5504=AXIS2_PLACEMENT_3D ( 'NONE', #67675, #67322, #3978 ) ;
#5506=LINE ( 'NONE', #5178, #16056 ) ;
#5508=CARTESIAN_POINT ( 'NONE',  ( -40.78947368421051323, 108.1536491499103505, 10.00000000000000000 ) ) ;
#5517=AXIS2_PLACEMENT_3D ( 'NONE', #42433, #36083, #69132 ) ;
#5518=MECHANICAL_DESIGN_GEOMETRIC_PRESENTATION_REPRESENTATION('',(#28006),#44904);
#5519=ORIENTED_EDGE ( 'NONE', *, *, #3137, .F. ) ;
#5521=( GEOMETRIC_REPRESENTATION_CONTEXT ( 3 ) GLOBAL_UNCERTAINTY_ASSIGNED_CONTEXT ( ( #59975 ) ) GLOBAL_UNIT_ASSIGNED_CONTEXT ( ( #5040, #59178, #17000 ) ) REPRESENTATION_CONTEXT ( 'NONE', 'WORKASPACE' ) );
#5524=EDGE_CURVE ( 'NONE', #61802, #68002, #20871, .T. ) ;
#5526=CARTESIAN_POINT ( 'NONE',  ( 0.000000000000000000, 154.5000000000000000, -9.524999999999998579 ) ) ;
#5527=CARTESIAN_POINT ( 'NONE',  ( 21.02379604162863913, 110.4999999999999858, 10.00000000000000000 ) ) ;
#5528=CARTESIAN_POINT ( 'NONE',  ( -74.93847439803357702, 36.28117515973496410, -9.953338452613744280 ) ) ;
#5532=CARTESIAN_POINT ( 'NONE',  ( -8.102448949553181734, 141.6050000000000182, 5.886773742842747126 ) ) ;
#5533=CARTESIAN_POINT ( 'NONE',  ( 0.000000000000000000, 125.9429263765338192, -8.025000000000000355 ) ) ;
#5538=AXIS2_PLACEMENT_3D ( 'NONE', #67662, #35658, #8918 ) ;
#5542=VERTEX_POINT ( 'NONE', #53446 ) ;
#5544=CARTESIAN_POINT ( 'NONE',  ( 0.000000000000000000, 131.9429263765338192, -8.025000000000000355 ) ) ;
#5545=( GEOMETRIC_REPRESENTATION_CONTEXT ( 3 ) GLOBAL_UNCERTAINTY_ASSIGNED_CONTEXT ( ( #31326 ) ) GLOBAL_UNIT_ASSIGNED_CONTEXT ( ( #60743, #1623, #45325 ) ) REPRESENTATION_CONTEXT ( 'NONE', 'WORKASPACE' ) );
#5546=EDGE_CURVE ( 'NONE', #20411, #29207, #13420, .T. ) ;
#5552=COLOUR_RGB ( '', 0.08235294, 0.09019608, 0.10196078) ;
#5555=DIRECTION ( 'NONE',  ( -0.000000000000000000, -0.000000000000000000, -1.000000000000000000 ) ) ;
#5556=( LENGTH_UNIT ( ) NAMED_UNIT ( * ) SI_UNIT ( .MILLI., .METRE. ) );
#5557=CIRCLE ( 'NONE', #1045, 5.000000000000004441 ) ;
#5565=ORIENTED_EDGE ( 'NONE', *, *, #8239, .T. ) ;
#5568=VERTEX_POINT ( 'NONE', #59054 ) ;
#5569=( GEOMETRIC_REPRESENTATION_CONTEXT ( 3 ) GLOBAL_UNCERTAINTY_ASSIGNED_CONTEXT ( ( #32786 ) ) GLOBAL_UNIT_ASSIGNED_CONTEXT ( ( #39919, #8228, #44848 ) ) REPRESENTATION_CONTEXT ( 'NONE', 'WORKASPACE' ) );
#5573=CARTESIAN_POINT ( 'NONE',  ( 9.058813317711337021, 159.5449999999999875, 2.943386871421375783 ) ) ;
#5575=EDGE_LOOP ( 'NONE', ( #36664, #51264, #47555, #64857 ) ) ;
#5578=COLOUR_RGB ( '', 0.09019608, 0.27058824, 0.51372549) ;
#5581=CARTESIAN_POINT ( 'NONE',  ( 4.716976649647099507, 122.6429263765338220, -6.492361379858953008 ) ) ;
#5582=CARTESIAN_POINT ( 'NONE',  ( 74.99999999999998579, 50.00000000000000000, 7.000000000000000000 ) ) ;
#5584=CARTESIAN_POINT ( 'NONE',  ( 60.00000000000000000, 1.797044900979284448E-15, -11.50000000000000000 ) ) ;
#5589=ORIENTED_EDGE ( 'NONE', *, *, #48241, .T. ) ;
#5591=STYLED_ITEM ( 'NONE', ( #449 ), #10891 ) ;
#5596=DIRECTION ( 'NONE',  ( 1.000000000000000000, 0.000000000000000000, 0.000000000000000000 ) ) ;
#5597=CARTESIAN_POINT ( 'NONE',  ( -2.607480562269115509, 115.2070736234661865, -8.024999999999970157 ) ) ;
#5598=STYLED_ITEM ( 'NONE', ( #40907 ), #33046 ) ;
#5600=CARTESIAN_POINT ( 'NONE',  ( 41.21690152797561524, 107.8360404011451976, 3.444195824416762974 ) ) ;
#5601=VERTEX_POINT ( 'NONE', #242 ) ;
#5604=CARTESIAN_POINT ( 'NONE',  ( -40.99999999999998579, 108.0000000000000000, -3.000000000000000444 ) ) ;
#5606=ORIENTED_EDGE ( 'NONE', *, *, #31902, .F. ) ;
#5607=DIRECTION ( 'NONE',  ( 1.000000000000000000, 0.000000000000000000, 0.000000000000000000 ) ) ;
#5608=CARTESIAN_POINT ( 'NONE',  ( 71.99999999999998579, 119.9999999999997868, 7.500000000000000000 ) ) ;
#5609=LINE ( 'NONE', #65049, #1998 ) ;
#5610=FACE_OUTER_BOUND ( 'NONE', #10819, .T. ) ;
#5611=DIRECTION ( 'NONE',  ( 0.000000000000000000, -1.000000000000000000, -0.000000000000000000 ) ) ;
#5613=ORIENTED_EDGE ( 'NONE', *, *, #4428, .T. ) ;
#5614=EDGE_CURVE ( 'NONE', #5967, #2421, #31650, .T. ) ;
#5619=ADVANCED_FACE ( 'NONE', ( #26342 ), #17520, .T. ) ;
#5621=CARTESIAN_POINT ( 'NONE',  ( 0.000000000000000000, 160.4449999999999932, -9.525000000000000355 ) ) ;
#5623=( LENGTH_UNIT ( ) NAMED_UNIT ( * ) SI_UNIT ( .MILLI., .METRE. ) );
#5624=CARTESIAN_POINT ( 'NONE',  ( 20.12916642283592950, 109.9999999999999858, 10.05319148936170137 ) ) ;
#5626=DIRECTION ( 'NONE',  ( -1.000000000000000000, -6.938893903907221278E-15, -0.000000000000000000 ) ) ;
#5632=CARTESIAN_POINT ( 'NONE',  ( 23.71231517720798365, 112.9999999999999858, -9.500000000000000000 ) ) ;
#5633=EDGE_CURVE ( 'NONE', #50095, #15159, #11210, .T. ) ;
#5638=ORIENTED_EDGE ( 'NONE', *, *, #2960, .F. ) ;
#5639=TOROIDAL_SURFACE ( 'NONE', #2222, 9.500000000000005329, 0.5000000000000000000 ) ;
#5643=CARTESIAN_POINT ( 'NONE',  ( -15.98999599679679839, 118.4999999999999716, 10.00000000000000000 ) ) ;
#5644=DIRECTION ( 'NONE',  ( 0.000000000000000000, 0.000000000000000000, 1.000000000000000000 ) ) ;
#5646=( NAMED_UNIT ( * ) SI_UNIT ( $, .STERADIAN. ) SOLID_ANGLE_UNIT ( ) );
#5654=ORIENTED_EDGE ( 'NONE', *, *, #62423, .T. ) ;
#5655=VECTOR ( 'NONE', #11194, 1000.000000000000114 ) ;
#5658=EDGE_CURVE ( 'NONE', #39399, #54750, #12579, .T. ) ;
#5659=CARTESIAN_POINT ( 'NONE',  ( 9.058813317711338797, 120.8449999999999847, -2.943386871421372675 ) ) ;
#5660=DIRECTION ( 'NONE',  ( -1.000000000000000000, -0.000000000000000000, -0.000000000000000000 ) ) ;
#5664=CARTESIAN_POINT ( 'NONE',  ( -5.598654528085808657, 126.7549999999999812, 7.705886871421373741 ) ) ;
#5667=DIRECTION ( 'NONE',  ( -1.000000000000000000, 0.000000000000000000, 0.000000000000000000 ) ) ;
#5669=CARTESIAN_POINT ( 'NONE',  ( 0.000000000000000000, 152.5550000000000068, -9.525000000000000355 ) ) ;
#5670=FACE_OUTER_BOUND ( 'NONE', #59898, .T. ) ;
#5671=STYLED_ITEM ( 'NONE', ( #22012 ), #69676 ) ;
#5672=DIRECTION ( 'NONE',  ( 1.000000000000000000, 0.000000000000000000, 0.000000000000000000 ) ) ;
#5674=( NAMED_UNIT ( * ) SI_UNIT ( $, .STERADIAN. ) SOLID_ANGLE_UNIT ( ) );
#5678=MECHANICAL_DESIGN_GEOMETRIC_PRESENTATION_REPRESENTATION('',(#30420),#65243);
#5680=ORIENTED_EDGE ( 'NONE', *, *, #9323, .F. ) ;
#5682=DIRECTION ( 'NONE',  ( 0.000000000000000000, 0.000000000000000000, -1.000000000000000000 ) ) ;
#5683=VECTOR ( 'NONE', #61224, 1000.000000000000000 ) ;
#5684=AXIS2_PLACEMENT_3D ( 'NONE', #6657, #49605, #1338 ) ;
#5685=( LENGTH_UNIT ( ) NAMED_UNIT ( * ) SI_UNIT ( .MILLI., .METRE. ) );
#5686=CARTESIAN_POINT ( 'NONE',  ( -44.99283348780034686, 9.603717787655236648, 3.208807429303570657 ) ) ;
#5689=FACE_OUTER_BOUND ( 'NONE', #66185, .T. ) ;
#5691=ORIENTED_EDGE ( 'NONE', *, *, #14288, .T. ) ;
#5695=CARTESIAN_POINT ( 'NONE',  ( -6.422934014168760974, 111.9999999999999858, 4.811085495980506721 ) ) ;
#5696=CARTESIAN_POINT ( 'NONE',  ( 7.632228543268608334, 144.4570736234661581, -2.479861379858951942 ) ) ;
#5699=CIRCLE ( 'NONE', #24776, 5.499999999999976907 ) ;
#5700=( NAMED_UNIT ( * ) SI_UNIT ( $, .STERADIAN. ) SOLID_ANGLE_UNIT ( ) );
#5702=AXIS2_PLACEMENT_3D ( 'NONE', #19766, #61975, #14157 ) ;
#5704=( LENGTH_UNIT ( ) NAMED_UNIT ( * ) SI_UNIT ( .MILLI., .METRE. ) );
#5705=( LENGTH_UNIT ( ) NAMED_UNIT ( * ) SI_UNIT ( .MILLI., .METRE. ) );
#5708=CARTESIAN_POINT ( 'NONE',  ( 3.094860106618431583, 132.0949999999999989, 9.525000000000000355 ) ) ;
#5712=CIRCLE ( 'NONE', #34958, 0.5000000000000004441 ) ;
#5718=ADVANCED_FACE ( 'NONE', ( #50243 ), #38686, .F. ) ;
#5722=DIRECTION ( 'NONE',  ( 0.000000000000000000, 0.000000000000000000, -1.000000000000000000 ) ) ;
#5723=ORIENTED_EDGE ( 'NONE', *, *, #36515, .T. ) ;
#5727=CARTESIAN_POINT ( 'NONE',  ( 71.50000000000000000, 14.49137674618942562, 10.00000000000000000 ) ) ;
#5732=VECTOR ( 'NONE', #48870, 1000.000000000000000 ) ;
#5736=CYLINDRICAL_SURFACE ( 'NONE', #35435, 0.5000000000000004441 ) ;
#5739=CARTESIAN_POINT ( 'NONE',  ( 72.49999999999998579, 1.797044900979284448E-15, -9.500000000000000000 ) ) ;
#5742=CARTESIAN_POINT ( 'NONE',  ( -4.716976649647097730, 142.3570736234661638, -6.492361379858953896 ) ) ;
#5743=ORIENTED_EDGE ( 'NONE', *, *, #65281, .F. ) ;
#5746=ORIENTED_EDGE ( 'NONE', *, *, #65191, .T. ) ;
#5750=ORIENTED_EDGE ( 'NONE', *, *, #50209, .T. ) ;
#5755=SURFACE_SIDE_STYLE ('',( #32172 ) ) ;
#5756=LINE ( 'NONE', #59582, #8741 ) ;
#5757=CARTESIAN_POINT ( 'NONE',  ( -44.99999999999977973, 146.4999999999999716, -7.500000000000000000 ) ) ;
#5759=FILL_AREA_STYLE_COLOUR ( '', #42726 ) ;
#5768=SURFACE_STYLE_FILL_AREA ( #53966 ) ;
#5769=EDGE_CURVE ( 'NONE', #40899, #37680, #38922, .T. ) ;
#5774=AXIS2_PLACEMENT_3D ( 'NONE', #23642, #24334, #45511 ) ;
#5775=CARTESIAN_POINT ( 'NONE',  ( -8.102448949553179958, 131.4950000000000045, 5.886773742842747126 ) ) ;
#5779=CIRCLE ( 'NONE', #68740, 0.5000000000000004441 ) ;
#5780=SURFACE_STYLE_USAGE ( .BOTH. , #48073 ) ;
#5781=EDGE_LOOP ( 'NONE', ( #12875, #53569, #45873, #69234 ) ) ;
#5782=CYLINDRICAL_SURFACE ( 'NONE', #36350, 7.999999999999992895 ) ;
#5783=EDGE_CURVE ( 'NONE', #10407, #9536, #13269, .T. ) ;
#5784=( GEOMETRIC_REPRESENTATION_CONTEXT ( 3 ) GLOBAL_UNCERTAINTY_ASSIGNED_CONTEXT ( ( #44770 ) ) GLOBAL_UNIT_ASSIGNED_CONTEXT ( ( #20334, #21030, #31926 ) ) REPRESENTATION_CONTEXT ( 'NONE', 'WORKASPACE' ) );
#5788=DIRECTION ( 'NONE',  ( -0.000000000000000000, -0.000000000000000000, -1.000000000000000000 ) ) ;
#5790=( GEOMETRIC_REPRESENTATION_CONTEXT ( 3 ) GLOBAL_UNCERTAINTY_ASSIGNED_CONTEXT ( ( #58899 ) ) GLOBAL_UNIT_ASSIGNED_CONTEXT ( ( #3012, #67095, #40380 ) ) REPRESENTATION_CONTEXT ( 'NONE', 'WORKASPACE' ) );
#5794=TOROIDAL_SURFACE ( 'NONE', #33863, 9.499999999999996447, 0.5000000000000000000 ) ;
#5798=CARTESIAN_POINT ( 'NONE',  ( 45.30708737912519979, 10.10236245970838453, -3.219298532130920432 ) ) ;
#5799=SURFACE_SIDE_STYLE ('',( #61004 ) ) ;
#5800=ADVANCED_FACE ( 'NONE', ( #35788 ), #68154, .F. ) ;
#5801=UNCERTAINTY_MEASURE_WITH_UNIT (LENGTH_MEASURE( 1.000000000000000082E-05 ), #32473, 'distance_accuracy_value', 'NONE');
#5803=SURFACE_SIDE_STYLE ('',( #26568 ) ) ;
#5806=FACE_OUTER_BOUND ( 'NONE', #64115, .T. ) ;
#5809=DIRECTION ( 'NONE',  ( 1.000000000000000000, 1.156482317317866302E-16, 0.000000000000000000 ) ) ;
#5813=DIRECTION ( 'NONE',  ( 1.000000000000000000, 0.000000000000000000, 0.000000000000000000 ) ) ;
#5816=FILL_AREA_STYLE ('',( #54014 ) ) ;
#5821=DIRECTION ( 'NONE',  ( 1.000000000000000000, 0.000000000000000000, 0.000000000000000000 ) ) ;
#5822=ORIENTED_EDGE ( 'NONE', *, *, #21152, .F. ) ;
#5823=AXIS2_PLACEMENT_3D ( 'NONE', #15135, #36932, #67521 ) ;
#5824=CARTESIAN_POINT ( 'NONE',  ( -6.826472737025120807, 109.5070736234661695, -4.959722759717907437 ) ) ;
#5825=STYLED_ITEM ( 'NONE', ( #40161 ), #46256 ) ;
#5828=CARTESIAN_POINT ( 'NONE',  ( 74.65399860055316594, 19.87094859200031394, -6.130873952096200341 ) ) ;
#5830=FILL_AREA_STYLE ('',( #15730 ) ) ;
#5831=ORIENTED_EDGE ( 'NONE', *, *, #32300, .T. ) ;
#5836=CARTESIAN_POINT ( 'NONE',  ( 9.058813317711338797, 124.9549999999999841, -2.943386871421372675 ) ) ;
#5839=COLOUR_RGB ( '', 0.66274510, 0.83137255, 0.94901961) ;
#5840=STYLED_ITEM ( 'NONE', ( #24033 ), #35779 ) ;
#5843=ORIENTED_EDGE ( 'NONE', *, *, #29873, .T. ) ;
#5845=FACE_OUTER_BOUND ( 'NONE', #11804, .T. ) ;
#5848=SURFACE_STYLE_FILL_AREA ( #32957 ) ;
#5865=DIRECTION ( 'NONE',  ( 0.000000000000000000, -1.000000000000000000, 0.000000000000000000 ) ) ;
#5866=CARTESIAN_POINT ( 'NONE',  ( -8.003604573459423221, 153.4245184585901427, -2.762566347670349476 ) ) ;
#5870=DIRECTION ( 'NONE',  ( 0.000000000000000000, 1.000000000000000000, 0.000000000000000000 ) ) ;
#5871=( NAMED_UNIT ( * ) PLANE_ANGLE_UNIT ( ) SI_UNIT ( $, .RADIAN. ) );
#5873=( LENGTH_UNIT ( ) NAMED_UNIT ( * ) SI_UNIT ( .MILLI., .METRE. ) );
#5882=ORIENTED_EDGE ( 'NONE', *, *, #2484, .T. ) ;
#5883=DIRECTION ( 'NONE',  ( 0.000000000000000000, -1.000000000000000000, 0.000000000000000000 ) ) ;
#5884=COLOUR_RGB ( '', 0.09019608, 0.27058824, 0.51372549) ;
#5887=FILL_AREA_STYLE_COLOUR ( '', #56307 ) ;
#5890=AXIS2_PLACEMENT_3D ( 'NONE', #13200, #7933, #29375 ) ;
#5893=CARTESIAN_POINT ( 'NONE',  ( -9.058813317711338797, 135.4549999999999841, 2.943386871421373563 ) ) ;
#5895=( GEOMETRIC_REPRESENTATION_CONTEXT ( 3 ) GLOBAL_UNCERTAINTY_ASSIGNED_CONTEXT ( ( #34841 ) ) GLOBAL_UNIT_ASSIGNED_CONTEXT ( ( #5003, #37064, #10641 ) ) REPRESENTATION_CONTEXT ( 'NONE', 'WORKASPACE' ) );
#5897=UNCERTAINTY_MEASURE_WITH_UNIT (LENGTH_MEASURE( 1.000000000000000082E-05 ), #23210, 'distance_accuracy_value', 'NONE');
#5898=DIRECTION ( 'NONE',  ( 0.000000000000000000, 0.000000000000000000, 1.000000000000000000 ) ) ;
#5899=( NAMED_UNIT ( * ) PLANE_ANGLE_UNIT ( ) SI_UNIT ( $, .RADIAN. ) );
#5902=CIRCLE ( 'NONE', #14939, 22.49999999999999645 ) ;
#5904=DIRECTION ( 'NONE',  ( 0.000000000000000000, 0.000000000000000000, 1.000000000000000000 ) ) ;
#5906=( NAMED_UNIT ( * ) SI_UNIT ( $, .STERADIAN. ) SOLID_ANGLE_UNIT ( ) );
#5907=CARTESIAN_POINT ( 'NONE',  ( 24.21231517720798010, 117.4999999999999716, 7.000000000000000000 ) ) ;
#5908=EDGE_LOOP ( 'NONE', ( #57302, #33687, #65213, #35487 ) ) ;
#5914=STYLED_ITEM ( 'NONE', ( #34177 ), #24846 ) ;
#5915=CARTESIAN_POINT ( 'NONE',  ( -14.98999599679678951, 118.4999999999999716, -10.00000000000000000 ) ) ;
#5919=SURFACE_STYLE_FILL_AREA ( #15825 ) ;
#5923=ORIENTED_EDGE ( 'NONE', *, *, #39512, .T. ) ;
#5925=MECHANICAL_DESIGN_GEOMETRIC_PRESENTATION_REPRESENTATION('',(#55346),#26124);
#5926=FACE_OUTER_BOUND ( 'NONE', #66123, .T. ) ;
#5927=PRESENTATION_STYLE_ASSIGNMENT (( #12234 ) ) ;
#5930=ORIENTED_EDGE ( 'NONE', *, *, #21765, .T. ) ;
#5933=SURFACE_STYLE_FILL_AREA ( #59065 ) ;
#5935=DIRECTION ( 'NONE',  ( 1.000000000000000000, 0.000000000000000000, 0.000000000000000000 ) ) ;
#5937=CARTESIAN_POINT ( 'NONE',  ( -9.827790563157511022E-16, 133.4429263765338192, 8.025000000000000355 ) ) ;
#5938=CARTESIAN_POINT ( 'NONE',  ( 45.07697505292422591, 10.02565835097472480, -3.091949714863345910 ) ) ;
#5941=SURFACE_STYLE_FILL_AREA ( #21094 ) ;
#5948=CARTESIAN_POINT ( 'NONE',  ( -12.72792206135785698, 115.4999999999999574, 10.00000000000000000 ) ) ;
#5949=DIRECTION ( 'NONE',  ( -0.000000000000000000, -0.000000000000000000, -1.000000000000000000 ) ) ;
#5954=UNCERTAINTY_MEASURE_WITH_UNIT (LENGTH_MEASURE( 1.000000000000000082E-05 ), #24085, 'distance_accuracy_value', 'NONE');
#5959=ORIENTED_EDGE ( 'NONE', *, *, #66146, .F. ) ;
#5961=EDGE_CURVE ( 'NONE', #28720, #39204, #2736, .T. ) ;
#5963=MECHANICAL_DESIGN_GEOMETRIC_PRESENTATION_REPRESENTATION('',(#44229),#26194);
#5967=VERTEX_POINT ( 'NONE', #50086 ) ;
#5968=SURFACE_STYLE_USAGE ( .BOTH. , #44005 ) ;
#5969=DIRECTION ( 'NONE',  ( -0.000000000000000000, -1.000000000000000000, -0.000000000000000000 ) ) ;
#5975=ORIENTED_EDGE ( 'NONE', *, *, #39998, .F. ) ;
#5983=CARTESIAN_POINT ( 'NONE',  ( 8.102448949553183510, 113.1049999999999898, -5.886773742842746238 ) ) ;
#5989=UNCERTAINTY_MEASURE_WITH_UNIT (LENGTH_MEASURE( 1.000000000000000082E-05 ), #54474, 'distance_accuracy_value', 'NONE');
#5990=APPLICATION_CONTEXT ( 'automotive_design' ) ;
#6002=( GEOMETRIC_REPRESENTATION_CONTEXT ( 3 ) GLOBAL_UNCERTAINTY_ASSIGNED_CONTEXT ( ( #29918 ) ) GLOBAL_UNIT_ASSIGNED_CONTEXT ( ( #25578, #20316, #69219 ) ) REPRESENTATION_CONTEXT ( 'NONE', 'WORKASPACE' ) );
#6004=SURFACE_STYLE_USAGE ( .BOTH. , #17956 ) ;
#6006=EDGE_CURVE ( 'NONE', #41477, #65971, #64598, .T. ) ;
#6013=CARTESIAN_POINT ( 'NONE',  ( 60.00000000000000000, 1.797044900979284448E-15, 6.500000000000000000 ) ) ;
#6014=ORIENTED_EDGE ( 'NONE', *, *, #25812, .T. ) ;
#6018=ORIENTED_EDGE ( 'NONE', *, *, #37709, .F. ) ;
#6021=ORIENTED_EDGE ( 'NONE', *, *, #12022, .T. ) ;
#6022=VECTOR ( 'NONE', #22920, 1000.000000000000000 ) ;
#6025=CARTESIAN_POINT ( 'NONE',  ( 5.598654528085805993, 135.2450000000000045, 7.705886871421374629 ) ) ;
#6029=DIRECTION ( 'NONE',  ( -0.000000000000000000, -0.000000000000000000, -1.000000000000000000 ) ) ;
#6030=CARTESIAN_POINT ( 'NONE',  ( 9.058813317711338797, 133.9549999999999841, -2.943386871421372675 ) ) ;
#6035=CARTESIAN_POINT ( 'NONE',  ( 8.102448949553181734, 145.5049999999999670, 5.886773742842750679 ) ) ;
#6042=EDGE_CURVE ( 'NONE', #27715, #37052, #65613, .T. ) ;
#6044=AXIS2_PLACEMENT_3D ( 'NONE', #2045, #45435, #7414 ) ;
#6047=ORIENTED_EDGE ( 'NONE', *, *, #15552, .T. ) ;
#6052=FACE_OUTER_BOUND ( 'NONE', #57377, .T. ) ;
#6055=VERTEX_POINT ( 'NONE', #29286 ) ;
#6057=CARTESIAN_POINT ( 'NONE',  ( -45.20191651604595506, 8.361204532447573001, -3.290978531522150696 ) ) ;
#6059=CIRCLE ( 'NONE', #64463, 13.99999999999999822 ) ;
#6060=ORIENTED_EDGE ( 'NONE', *, *, #13815, .F. ) ;
#6061=CARTESIAN_POINT ( 'NONE',  ( -9.827790563157511022E-16, 112.4429263765338192, 8.025000000000000355 ) ) ;
#6064=STYLED_ITEM ( 'NONE', ( #64182 ), #55997 ) ;
#6065=DIRECTION ( 'NONE',  ( 0.000000000000000000, 0.000000000000000000, 1.000000000000000000 ) ) ;
#6067=CARTESIAN_POINT ( 'NONE',  ( 24.21231517720798010, 112.4999999999999858, 9.500000000000000000 ) ) ;
#6072=ADVANCED_FACE ( 'NONE', ( #44827 ), #53187, .T. ) ;
#6073=CARTESIAN_POINT ( 'NONE',  ( 8.102448949553183510, 126.9950000000000045, -5.886773742842746238 ) ) ;
#6076=EDGE_CURVE ( 'NONE', #4894, #12034, #13457, .T. ) ;
#6078=( NAMED_UNIT ( * ) PLANE_ANGLE_UNIT ( ) SI_UNIT ( $, .RADIAN. ) );
#6083=AXIS2_PLACEMENT_3D ( 'NONE', #28539, #39853, #12361 ) ;
#6084=FILL_AREA_STYLE_COLOUR ( '', #15298 ) ;
#6085=AXIS2_PLACEMENT_3D ( 'NONE', #43865, #22030, #65965 ) ;
#6086=( GEOMETRIC_REPRESENTATION_CONTEXT ( 3 ) GLOBAL_UNCERTAINTY_ASSIGNED_CONTEXT ( ( #58019 ) ) GLOBAL_UNIT_ASSIGNED_CONTEXT ( ( #44649, #23834, #61789 ) ) REPRESENTATION_CONTEXT ( 'NONE', 'WORKASPACE' ) );
#6089=FILL_AREA_STYLE ('',( #63101 ) ) ;
#6091=ORIENTED_EDGE ( 'NONE', *, *, #62437, .T. ) ;
#6097=VERTEX_POINT ( 'NONE', #41622 ) ;
#6100=ORIENTED_EDGE ( 'NONE', *, *, #60080, .F. ) ;
#6106=CIRCLE ( 'NONE', #44379, 12.50000000000000355 ) ;
#6108=CARTESIAN_POINT ( 'NONE',  ( 0.000000000000000000, 151.0570736234661524, -8.025000000000000355 ) ) ;
#6109=AXIS2_PLACEMENT_3D ( 'NONE', #4010, #9688, #63474 ) ;
#6110=ORIENTED_EDGE ( 'NONE', *, *, #33736, .F. ) ;
#6114=CIRCLE ( 'NONE', #39857, 23.00000000000000000 ) ;
#6117=EDGE_LOOP ( 'NONE', ( #63068, #22200, #15913, #23090, #48157 ) ) ;
#6121=FACE_OUTER_BOUND ( 'NONE', #6609, .T. ) ;
#6124=EDGE_LOOP ( 'NONE', ( #50786, #16577, #55238, #3019 ) ) ;
#6128=CARTESIAN_POINT ( 'NONE',  ( -74.99999999999998579, 50.00000000000000000, -6.500000000000000000 ) ) ;
#6130=DIRECTION ( 'NONE',  ( -1.000000000000000000, 0.000000000000000000, 0.000000000000000000 ) ) ;
#6132=ORIENTED_EDGE ( 'NONE', *, *, #22088, .F. ) ;
#6133=CYLINDRICAL_SURFACE ( 'NONE', #4423, 0.5000000000000004441 ) ;
#6138=LINE ( 'NONE', #48752, #44954 ) ;
#6143=FILL_AREA_STYLE ('',( #22320 ) ) ;
#6144=PRESENTATION_STYLE_ASSIGNMENT (( #54668 ) ) ;
#6148=CARTESIAN_POINT ( 'NONE',  ( -8.102448949553179958, 128.4950000000000045, 5.886773742842747126 ) ) ;
#6150=DIRECTION ( 'NONE',  ( 0.000000000000000000, 1.000000000000000000, -0.000000000000000000 ) ) ;
#6152=SURFACE_STYLE_FILL_AREA ( #43150 ) ;
#6157=CARTESIAN_POINT ( 'NONE',  ( -14.98999599679678951, 146.4999999999999716, -10.00000000000000000 ) ) ;
#6159=AXIS2_PLACEMENT_3D ( 'NONE', #22648, #17402, #38865 ) ;
#6161=ORIENTED_EDGE ( 'NONE', *, *, #46750, .F. ) ;
#6163=DIRECTION ( 'NONE',  ( 0.000000000000000000, 1.000000000000000000, 0.000000000000000000 ) ) ;
#6165=COLOUR_RGB ( '', 0.66274510, 0.83137255, 0.94901961) ;
#6167=FACE_OUTER_BOUND ( 'NONE', #41521, .T. ) ;
#6171=SURFACE_STYLE_FILL_AREA ( #21298 ) ;
#6172=( LENGTH_UNIT ( ) NAMED_UNIT ( * ) SI_UNIT ( .MILLI., .METRE. ) );
#6173=CARTESIAN_POINT ( 'NONE',  ( -74.99999999999998579, 50.00000000000000000, 12.00000000000000000 ) ) ;
#6177=FACE_OUTER_BOUND ( 'NONE', #18580, .T. ) ;
#6178=STYLED_ITEM ( 'NONE', ( #31908 ), #8013 ) ;
#6180=COLOUR_RGB ( '', 0.66274510, 0.83137255, 0.94901961) ;
#6182=ORIENTED_EDGE ( 'NONE', *, *, #8990, .F. ) ;
#6187=DIRECTION ( 'NONE',  ( -0.000000000000000000, -0.000000000000000000, 1.000000000000000000 ) ) ;
#6188=AXIS2_PLACEMENT_3D ( 'NONE', #62847, #14687, #8006 ) ;
#6189=CARTESIAN_POINT ( 'NONE',  ( -2.607480562269075097, 113.4070736234661609, 8.025000000000000355 ) ) ;
#6191=( NAMED_UNIT ( * ) SI_UNIT ( $, .STERADIAN. ) SOLID_ANGLE_UNIT ( ) );
#6200=EDGE_CURVE ( 'NONE', #20172, #58654, #54263, .T. ) ;
#6204=DIRECTION ( 'NONE',  ( -0.000000000000000000, -0.000000000000000000, -1.000000000000000000 ) ) ;
#6206=ORIENTED_EDGE ( 'NONE', *, *, #19056, .F. ) ;
#6209=ADVANCED_FACE ( 'NONE', ( #63729 ), #39556, .F. ) ;
#6211=AXIS2_PLACEMENT_3D ( 'NONE', #28285, #29344, #49790 ) ;
#6218=DIRECTION ( 'NONE',  ( -1.000000000000000000, -1.099520432716498821E-15, 0.000000000000000000 ) ) ;
#6219=ORIENTED_EDGE ( 'NONE', *, *, #37632, .F. ) ;
#6222=CARTESIAN_POINT ( 'NONE',  ( 45.00000000000000000, -1.469576158976824618E-14, 10.00000000000000000 ) ) ;
#6226=COLOUR_RGB ( '', 0.40784314, 0.44705882, 0.49803922) ;
#6228=CARTESIAN_POINT ( 'NONE',  ( -6.946753979098152953, 153.3272276288669502, -4.645043913640976463 ) ) ;
#6231=( NAMED_UNIT ( * ) SI_UNIT ( $, .STERADIAN. ) SOLID_ANGLE_UNIT ( ) );
#6232=AXIS2_PLACEMENT_3D ( 'NONE', #67676, #56417, #7541 ) ;
#6239=CIRCLE ( 'NONE', #39973, 0.5000000000000004441 ) ;
#6244=CARTESIAN_POINT ( 'NONE',  ( -4.716976649647098618, 151.1429263765338078, 6.492361379858953008 ) ) ;
#6246=PRESENTATION_STYLE_ASSIGNMENT (( #208 ) ) ;
#6248=CIRCLE ( 'NONE', #54549, 10.02500000000000568 ) ;
#6250=CARTESIAN_POINT ( 'NONE',  ( 10.01517768586949231, 133.8049999999999784, 1.839758294383810543E-15 ) ) ;
#6252=STYLED_ITEM ( 'NONE', ( #67208 ), #58207 ) ;
#6253=VECTOR ( 'NONE', #37780, 1000.000000000000000 ) ;
#6255=AXIS2_PLACEMENT_3D ( 'NONE', #15155, #47887, #63649 ) ;
#6258=ORIENTED_EDGE ( 'NONE', *, *, #36330, .F. ) ;
#6261=EDGE_CURVE ( 'NONE', #62586, #14708, #46492, .T. ) ;
#6262=PLANE ( 'NONE',  #58857 ) ;
#6265=VERTEX_POINT ( 'NONE', #10965 ) ;
#6270=DIRECTION ( 'NONE',  ( 1.000000000000000000, 2.304236466203155263E-14, 0.000000000000000000 ) ) ;
#6273=ORIENTED_EDGE ( 'NONE', *, *, #49262, .T. ) ;
#6274=AXIS2_PLACEMENT_3D ( 'NONE', #3764, #57622, #9442 ) ;
#6278=ORIENTED_EDGE ( 'NONE', *, *, #57839, .F. ) ;
#6280=COLOUR_RGB ( '', 0.66274510, 0.83137255, 0.94901961) ;
#6284=ORIENTED_EDGE ( 'NONE', *, *, #13251, .F. ) ;
#6286=( NAMED_UNIT ( * ) PLANE_ANGLE_UNIT ( ) SI_UNIT ( $, .RADIAN. ) );
#6287=EDGE_CURVE ( 'NONE', #62679, #30440, #37414, .T. ) ;
#6288=CARTESIAN_POINT ( 'NONE',  ( -45.00000000000000000, 9.708372675170618749, 3.611004237778676185 ) ) ;
#6290=CARTESIAN_POINT ( 'NONE',  ( 7.632228543268608334, 134.3429263765337964, -2.479861379858951942 ) ) ;
#6297=AXIS2_PLACEMENT_3D ( 'NONE', #65133, #38469, #32101 ) ;
#6299=CARTESIAN_POINT ( 'NONE',  ( 0.000000000000000000, 154.9999999999999716, 0.000000000000000000 ) ) ;
#6301=FILL_AREA_STYLE_COLOUR ( '', #51030 ) ;
#6303=ORIENTED_EDGE ( 'NONE', *, *, #67345, .T. ) ;
#6306=CARTESIAN_POINT ( 'NONE',  ( 41.49999999999998579, 106.9282032302754857, 3.500000000000000888 ) ) ;
#6307=ORIENTED_EDGE ( 'NONE', *, *, #64645, .T. ) ;
#6313=FACE_BOUND ( 'NONE', #50082, .T. ) ;
#6316=SURFACE_STYLE_FILL_AREA ( #31672 ) ;
#6317=DIRECTION ( 'NONE',  ( -0.000000000000000000, -0.000000000000000000, -1.000000000000000000 ) ) ;
#6318=DIRECTION ( 'NONE',  ( 0.000000000000000000, 0.000000000000000000, 1.000000000000000000 ) ) ;
#6327=VECTOR ( 'NONE', #48924, 1000.000000000000000 ) ;
#6329=CARTESIAN_POINT ( 'NONE',  ( 8.102448949553183510, 153.9950000000000045, -5.886773742842746238 ) ) ;
#6332=AXIS2_PLACEMENT_3D ( 'NONE', #38090, #6377, #5672 ) ;
#6337=VERTEX_POINT ( 'NONE', #33128 ) ;
#6347=ORIENTED_EDGE ( 'NONE', *, *, #5163, .T. ) ;
#6348=VERTEX_POINT ( 'NONE', #22565 ) ;
#6349=LINE ( 'NONE', #17633, #53906 ) ;
#6350=DIRECTION ( 'NONE',  ( 0.000000000000000000, 0.000000000000000000, 1.000000000000000000 ) ) ;
#6352=ADVANCED_FACE ( 'NONE', ( #48997 ), #36344, .F. ) ;
#6359=ORIENTED_EDGE ( 'NONE', *, *, #43353, .F. ) ;
#6360=ORIENTED_EDGE ( 'NONE', *, *, #65356, .F. ) ;
#6361=DIRECTION ( 'NONE',  ( -1.000000000000000000, -0.000000000000000000, -0.000000000000000000 ) ) ;
#6363=ORIENTED_EDGE ( 'NONE', *, *, #35427, .T. ) ;
#6364=EDGE_CURVE ( 'NONE', #67303, #33055, #53206, .T. ) ;
#6366=CARTESIAN_POINT ( 'NONE',  ( -8.102448949553181734, 133.8950000000000102, -5.886773742842749790 ) ) ;
#6369=CARTESIAN_POINT ( 'NONE',  ( -5.598654528085806881, 134.8549999999999898, -7.705886871421374629 ) ) ;
#6372=EDGE_CURVE ( 'NONE', #24214, #52342, #48649, .T. ) ;
#6373=CARTESIAN_POINT ( 'NONE',  ( -41.47746817312046375, 107.6230562796895356, -3.580135233559778030 ) ) ;
#6375=CARTESIAN_POINT ( 'NONE',  ( 5.598654528085809545, 155.2549999999999670, -7.705886871421373741 ) ) ;
#6377=DIRECTION ( 'NONE',  ( 0.000000000000000000, 0.000000000000000000, 1.000000000000000000 ) ) ;
#6385=FILL_AREA_STYLE_COLOUR ( '', #47554 ) ;
#6389=SURFACE_STYLE_FILL_AREA ( #28873 ) ;
#6390=DIRECTION ( 'NONE',  ( 0.000000000000000000, 0.000000000000000000, -1.000000000000000000 ) ) ;
#6392=ORIENTED_EDGE ( 'NONE', *, *, #50135, .F. ) ;
#6393=CARTESIAN_POINT ( 'NONE',  ( -45.00000000000000000, 8.062885781073934055, -3.611004237778684178 ) ) ;
#6397=ORIENTED_EDGE ( 'NONE', *, *, #34328, .T. ) ;
#6398=DIRECTION ( 'NONE',  ( 1.000000000000000000, 0.000000000000000000, 0.000000000000000000 ) ) ;
#6399=( LENGTH_UNIT ( ) NAMED_UNIT ( * ) SI_UNIT ( .MILLI., .METRE. ) );
#6400=CARTESIAN_POINT ( 'NONE',  ( 23.21231517720798010, 113.4999999999999858, -9.500000000000000000 ) ) ;
#6402=ADVANCED_FACE ( 'NONE', ( #50009 ), #44507, .F. ) ;
#6403=CARTESIAN_POINT ( 'NONE',  ( -74.23245021955101208, 8.860682567649762476, -6.389379348043731532 ) ) ;
#6406=SURFACE_STYLE_USAGE ( .BOTH. , #54600 ) ;
#6409=CARTESIAN_POINT ( 'NONE',  ( -9.058813317711338797, 134.3449999999999989, 2.943386871421373563 ) ) ;
#6412=DIRECTION ( 'NONE',  ( -0.000000000000000000, -1.000000000000000000, 0.000000000000000000 ) ) ;
#6426=DIRECTION ( 'NONE',  ( 0.000000000000000000, -0.000000000000000000, 1.000000000000000000 ) ) ;
#6428=VERTEX_POINT ( 'NONE', #50685 ) ;
#6431=EDGE_CURVE ( 'NONE', #29454, #5399, #17656, .T. ) ;
#6432=DIRECTION ( 'NONE',  ( 1.000000000000000000, 0.000000000000000000, 0.000000000000000000 ) ) ;
#6435=EDGE_CURVE ( 'NONE', #4028, #63980, #10504, .T. ) ;
#6437=STYLED_ITEM ( 'NONE', ( #14336 ), #41280 ) ;
#6438=EDGE_LOOP ( 'NONE', ( #28847, #35119, #36372, #63117 ) ) ;
#6440=ORIENTED_EDGE ( 'NONE', *, *, #32109, .F. ) ;
#6443=DIRECTION ( 'NONE',  ( 0.000000000000000000, 0.000000000000000000, 1.000000000000000000 ) ) ;
#6445=FILL_AREA_STYLE_COLOUR ( '', #34231 ) ;
#6446=CARTESIAN_POINT ( 'NONE',  ( 0.000000000000000000, 157.0570736234661524, -8.025000000000000355 ) ) ;
#6452=ORIENTED_EDGE ( 'NONE', *, *, #68201, .T. ) ;
#6454=ADVANCED_FACE ( 'NONE', ( #3116 ), #35555, .F. ) ;
#6457=FILL_AREA_STYLE_COLOUR ( '', #64911 ) ;
#6458=CARTESIAN_POINT ( 'NONE',  ( -45.88773363194338373, 9.324829141677650313, -6.185705318536817821 ) ) ;
#6459=STYLED_ITEM ( 'NONE', ( #7620 ), #67102 ) ;
#6460=EDGE_LOOP ( 'NONE', ( #15947, #53978, #55917, #25630 ) ) ;
#6465=CARTESIAN_POINT ( 'NONE',  ( -74.50000000000000000, 7.768687147774684831, 6.500000000000004441 ) ) ;
#6468=CARTESIAN_POINT ( 'NONE',  ( 12.34222745343792127, 114.9999999999999574, -10.18181818181818166 ) ) ;
#6469=FILL_AREA_STYLE ('',( #33228 ) ) ;
#6470=CIRCLE ( 'NONE', #24440, 0.5000000000000004441 ) ;
#6473=CARTESIAN_POINT ( 'NONE',  ( 5.598654528085805993, 129.2450000000000045, 7.705886871421374629 ) ) ;
#6477=AXIS2_PLACEMENT_3D ( 'NONE', #16063, #9743, #5116 ) ;
#6481=( LENGTH_UNIT ( ) NAMED_UNIT ( * ) SI_UNIT ( .MILLI., .METRE. ) );
#6489=( NAMED_UNIT ( * ) PLANE_ANGLE_UNIT ( ) SI_UNIT ( $, .RADIAN. ) );
#6491=EDGE_CURVE ( 'NONE', #28358, #31294, #57700, .T. ) ;
#6493=DIRECTION ( 'NONE',  ( 0.000000000000000000, 1.000000000000000000, -0.000000000000000000 ) ) ;
#6510=LINE ( 'NONE', #60338, #64495 ) ;
#6512=CARTESIAN_POINT ( 'NONE',  ( -9.827790563157511022E-16, 119.5570736234661524, 8.025000000000000355 ) ) ;
#6513=DIRECTION ( 'NONE',  ( -1.000000000000000000, 0.000000000000000000, 0.000000000000000000 ) ) ;
#6514=CARTESIAN_POINT ( 'NONE',  ( 75.00000000000000000, 19.90218225813118380, -6.307374275524009200 ) ) ;
#6515=CARTESIAN_POINT ( 'NONE',  ( -23.21231517720797655, 117.4999999999999716, -7.000000000000000000 ) ) ;
#6517=VERTEX_POINT ( 'NONE', #4185 ) ;
#6523=CARTESIAN_POINT ( 'NONE',  ( -60.00000000000000000, -2.024042244987997205E-14, 6.000000000000000888 ) ) ;
#6527=CARTESIAN_POINT ( 'NONE',  ( -20.05202421861157447, 114.9999999999999432, -10.44839000960907960 ) ) ;
#6536=ORIENTED_EDGE ( 'NONE', *, *, #886, .T. ) ;
#6539=DIRECTION ( 'NONE',  ( -0.000000000000000000, -0.000000000000000000, -1.000000000000000000 ) ) ;
#6540=AXIS2_PLACEMENT_3D ( 'NONE', #44742, #6361, #27791 ) ;
#6542=DIRECTION ( 'NONE',  ( -1.000000000000000000, 0.000000000000000000, 0.000000000000000000 ) ) ;
#6546=CARTESIAN_POINT ( 'NONE',  ( -1.518239866961766493, 153.0257666483763330, -7.925161578318726363 ) ) ;
#6548=CARTESIAN_POINT ( 'NONE',  ( -71.49999999999998579, 64.07124727947029896, -7.500000000000000000 ) ) ;
#6555=DIRECTION ( 'NONE',  ( 0.000000000000000000, -1.000000000000000000, 0.000000000000000000 ) ) ;
#6557=EDGE_CURVE ( 'NONE', #11851, #39381, #1490, .T. ) ;
#6565=FILL_AREA_STYLE ('',( #23450 ) ) ;
#6566=FACE_OUTER_BOUND ( 'NONE', #9078, .T. ) ;
#6571=ADVANCED_FACE ( 'NONE', ( #4550 ), #19368, .F. ) ;
#6573=CARTESIAN_POINT ( 'NONE',  ( 8.102448949553181734, 133.5049999999999670, 5.886773742842750679 ) ) ;
#6577=UNCERTAINTY_MEASURE_WITH_UNIT (LENGTH_MEASURE( 1.000000000000000082E-05 ), #46786, 'distance_accuracy_value', 'NONE');
#6580=VERTEX_POINT ( 'NONE', #42945 ) ;
#6582=DIRECTION ( 'NONE',  ( 1.000000000000000000, 0.000000000000000000, 0.000000000000000000 ) ) ;
#6584=AXIS2_PLACEMENT_3D ( 'NONE', #60726, #7619, #24477 ) ;
#6585=SURFACE_STYLE_FILL_AREA ( #17544 ) ;
#6586=DIRECTION ( 'NONE',  ( 0.000000000000000000, 0.000000000000000000, 1.000000000000000000 ) ) ;
#6589=VERTEX_POINT ( 'NONE', #15840 ) ;
#6590=DIRECTION ( 'NONE',  ( 1.000000000000000000, 0.000000000000000000, 0.000000000000000000 ) ) ;
#6591=COLOUR_RGB ( '', 0.40784314, 0.44705882, 0.49803922) ;
#6595=( GEOMETRIC_REPRESENTATION_CONTEXT ( 3 ) GLOBAL_UNCERTAINTY_ASSIGNED_CONTEXT ( ( #44548 ) ) GLOBAL_UNIT_ASSIGNED_CONTEXT ( ( #10763, #63530, #69167 ) ) REPRESENTATION_CONTEXT ( 'NONE', 'WORKASPACE' ) );
#6596=MECHANICAL_DESIGN_GEOMETRIC_PRESENTATION_REPRESENTATION('',(#65001),#38113);
#6602=FILL_AREA_STYLE_COLOUR ( '', #46772 ) ;
#6606=CARTESIAN_POINT ( 'NONE',  ( -8.102448949553181734, 158.4950000000000045, 5.886773742842747126 ) ) ;
#6608=( GEOMETRIC_REPRESENTATION_CONTEXT ( 3 ) GLOBAL_UNCERTAINTY_ASSIGNED_CONTEXT ( ( #4792 ) ) GLOBAL_UNIT_ASSIGNED_CONTEXT ( ( #53570, #48006, #26131 ) ) REPRESENTATION_CONTEXT ( 'NONE', 'WORKASPACE' ) );
#6609=EDGE_LOOP ( 'NONE', ( #43291, #37212, #3983, #55136 ) ) ;
#6611=CYLINDRICAL_SURFACE ( 'NONE', #61986, 0.5000000000000004441 ) ;
#6615=CARTESIAN_POINT ( 'NONE',  ( -4.716976649647098618, 136.1429263765338362, 6.492361379858953008 ) ) ;
#6616=DIRECTION ( 'NONE',  ( 0.000000000000000000, 1.000000000000000000, 0.000000000000000000 ) ) ;
#6619=CARTESIAN_POINT ( 'NONE',  ( 7.632228543268607446, 125.0429263765337993, 2.479861379858954606 ) ) ;
#6629=( LENGTH_UNIT ( ) NAMED_UNIT ( * ) SI_UNIT ( .MILLI., .METRE. ) );
#6630=UNCERTAINTY_MEASURE_WITH_UNIT (LENGTH_MEASURE( 1.000000000000000082E-05 ), #24819, 'distance_accuracy_value', 'NONE');
#6631=VERTEX_POINT ( 'NONE', #26007 ) ;
#6632=MECHANICAL_DESIGN_GEOMETRIC_PRESENTATION_REPRESENTATION('',(#50498),#13423);
#6633=CARTESIAN_POINT ( 'NONE',  ( -8.437984349512095861, 115.8070736234661524, -5.166775262442723748E-16 ) ) ;
#6636=ORIENTED_EDGE ( 'NONE', *, *, #65931, .F. ) ;
#6637=ORIENTED_EDGE ( 'NONE', *, *, #44912, .F. ) ;
#6647=( GEOMETRIC_REPRESENTATION_CONTEXT ( 3 ) GLOBAL_UNCERTAINTY_ASSIGNED_CONTEXT ( ( #64520 ) ) GLOBAL_UNIT_ASSIGNED_CONTEXT ( ( #33249, #59615, #26890 ) ) REPRESENTATION_CONTEXT ( 'NONE', 'WORKASPACE' ) );
#6649=AXIS2_PLACEMENT_3D ( 'NONE', #21948, #21222, #15998 ) ;
#6650=DIRECTION ( 'NONE',  ( -0.000000000000000000, 3.471511484687326312E-15, 1.000000000000000000 ) ) ;
#6651=AXIS2_PLACEMENT_3D ( 'NONE', #50442, #7863, #24051 ) ;
#6657=CARTESIAN_POINT ( 'NONE',  ( -12.72792206135785698, 149.9999999999999716, -10.50000000000000000 ) ) ;
#6659=LINE ( 'NONE', #54516, #38165 ) ;
#6660=STYLED_ITEM ( 'NONE', ( #24945 ), #51466 ) ;
#6661=CYLINDRICAL_SURFACE ( 'NONE', #3362, 0.5000000000000004441 ) ;
#6665=CARTESIAN_POINT ( 'NONE',  ( 9.058813317711337021, 159.5449999999999875, 2.943386871421375783 ) ) ;
#6667=EDGE_CURVE ( 'NONE', #60866, #29393, #28484, .T. ) ;
#6668=CARTESIAN_POINT ( 'NONE',  ( -2.607480562269048896, 113.4070736234661467, 8.025000000000019895 ) ) ;
#6669=( LENGTH_UNIT ( ) NAMED_UNIT ( * ) SI_UNIT ( .MILLI., .METRE. ) );
#6674=( NAMED_UNIT ( * ) PLANE_ANGLE_UNIT ( ) SI_UNIT ( $, .RADIAN. ) );
#6675=CARTESIAN_POINT ( 'NONE',  ( 44.99999999999977973, 146.9999999999999716, 9.500000000000000000 ) ) ;
#6676=ORIENTED_EDGE ( 'NONE', *, *, #8296, .F. ) ;
#6682=TOROIDAL_SURFACE ( 'NONE', #23499, 1.000000000000000000, 0.5000000000000000000 ) ;
#6686=VERTEX_POINT ( 'NONE', #13282 ) ;
#6688=AXIS2_PLACEMENT_3D ( 'NONE', #29751, #67736, #19533 ) ;
#6693=DIRECTION ( 'NONE',  ( 1.000000000000000000, 0.000000000000000000, 0.000000000000000000 ) ) ;
#6696=ORIENTED_EDGE ( 'NONE', *, *, #35648, .T. ) ;
#6701=CARTESIAN_POINT ( 'NONE',  ( 60.00000000000000000, 1.797044900979284448E-15, 12.00000000000000000 ) ) ;
#6707=CARTESIAN_POINT ( 'NONE',  ( 3.094860106618435136, 127.2949999999999875, -9.525000000000000355 ) ) ;
#6712=CARTESIAN_POINT ( 'NONE',  ( 0.000000000000000000, 128.5549999999999784, -9.525000000000000355 ) ) ;
#6717=CARTESIAN_POINT ( 'NONE',  ( -10.01517768586949231, 159.3049999999999784, -6.132527647946036459E-16 ) ) ;
#6718=UNCERTAINTY_MEASURE_WITH_UNIT (LENGTH_MEASURE( 1.000000000000000082E-05 ), #26995, 'distance_accuracy_value', 'NONE');
#6721=( NAMED_UNIT ( * ) SI_UNIT ( $, .STERADIAN. ) SOLID_ANGLE_UNIT ( ) );
#6723=( NAMED_UNIT ( * ) PLANE_ANGLE_UNIT ( ) SI_UNIT ( $, .RADIAN. ) );
#6724=VERTEX_POINT ( 'NONE', #65388 ) ;
#6727=FACE_OUTER_BOUND ( 'NONE', #35001, .T. ) ;
#6729=VERTEX_POINT ( 'NONE', #6288 ) ;
#6734=SURFACE_SIDE_STYLE ('',( #65129 ) ) ;
#6736=CARTESIAN_POINT ( 'NONE',  ( -44.99680003617404367, 9.646670402630480368, 3.411693126523581032 ) ) ;
#6737=ORIENTED_EDGE ( 'NONE', *, *, #34556, .T. ) ;
#6738=ORIENTED_EDGE ( 'NONE', *, *, #60732, .T. ) ;
#6739=CARTESIAN_POINT ( 'NONE',  ( -44.99626347754794153, 9.641092568915874850, -3.381901693660977593 ) ) ;
#6743=EDGE_CURVE ( 'NONE', #60681, #25577, #30057, .T. ) ;
#6744=CARTESIAN_POINT ( 'NONE',  ( 8.437984349512095861, 144.3070736234661524, 1.550032578732816828E-15 ) ) ;
#6753=CARTESIAN_POINT ( 'NONE',  ( -8.102448949553181734, 124.8949999999999960, -5.886773742842749790 ) ) ;
#6755=AXIS2_PLACEMENT_3D ( 'NONE', #4157, #21061, #42557 ) ;
#6756=EDGE_CURVE ( 'NONE', #13502, #24967, #54803, .T. ) ;
#6765=AXIS2_PLACEMENT_3D ( 'NONE', #28994, #1541, #54699 ) ;
#6774=AXIS2_PLACEMENT_3D ( 'NONE', #37977, #15802, #36603 ) ;
#6779=CARTESIAN_POINT ( 'NONE',  ( 44.91886116991580735, 9.999999999999980460, -3.201362207699240514 ) ) ;
#6788=( NAMED_UNIT ( * ) PLANE_ANGLE_UNIT ( ) SI_UNIT ( $, .RADIAN. ) );
#6789=CARTESIAN_POINT ( 'NONE',  ( -7.632228543268607446, 154.6570736234661467, -2.479861379858953718 ) ) ;
#6793=CARTESIAN_POINT ( 'NONE',  ( 6.826472737025121695, 137.4929263765338305, -4.959722759717905660 ) ) ;
#6803=ORIENTED_EDGE ( 'NONE', *, *, #63688, .F. ) ;
#6810=CARTESIAN_POINT ( 'NONE',  ( -45.91398438485168043, 9.424559774107503785, -6.049830996511076364 ) ) ;
#6812=SURFACE_STYLE_USAGE ( .BOTH. , #10724 ) ;
#6813=DIRECTION ( 'NONE',  ( 0.7071067811865543451, 8.659560562355015442E-17, -0.7071067811865408004 ) ) ;
#6815=ORIENTED_EDGE ( 'NONE', *, *, #40354, .T. ) ;
#6816=ADVANCED_FACE ( 'NONE', ( #34738 ), #50254, .F. ) ;
#6817=CARTESIAN_POINT ( 'NONE',  ( -74.33468449153457414, 8.455116999143504231, 6.464599779185707717 ) ) ;
#6823=AXIS2_PLACEMENT_3D ( 'NONE', #44358, #50970, #22508 ) ;
#6824=CARTESIAN_POINT ( 'NONE',  ( -75.00000000000000000, 67.00000000000000000, -6.500000000000000000 ) ) ;
#6830=CARTESIAN_POINT ( 'NONE',  ( 5.598654528085805993, 135.2450000000000045, 7.705886871421374629 ) ) ;
#6833=EDGE_CURVE ( 'NONE', #30766, #2723, #59937, .T. ) ;
#6840=FILL_AREA_STYLE ('',( #45213 ) ) ;
#6844=CARTESIAN_POINT ( 'NONE',  ( 21.02379604162863913, 109.9999999999999858, -9.500000000000000000 ) ) ;
#6850=CARTESIAN_POINT ( 'NONE',  ( 44.97464006314718432, 9.991546687716517994, -3.784415753861334331 ) ) ;
#6851=DIRECTION ( 'NONE',  ( 1.000000000000000000, 0.000000000000000000, 0.000000000000000000 ) ) ;
#6854=EDGE_CURVE ( 'NONE', #21703, #40244, #56550, .T. ) ;
#6856=SURFACE_STYLE_FILL_AREA ( #43843 ) ;
#6859=( NAMED_UNIT ( * ) PLANE_ANGLE_UNIT ( ) SI_UNIT ( $, .RADIAN. ) );
#6860=FACE_OUTER_BOUND ( 'NONE', #45436, .T. ) ;
#6863=AXIS2_PLACEMENT_3D ( 'NONE', #37132, #68769, #37492 ) ;
#6869=DIRECTION ( 'NONE',  ( -0.000000000000000000, 1.000000000000000000, -0.000000000000000000 ) ) ;
#6877=EDGE_LOOP ( 'NONE', ( #10533, #2815, #11339, #38314 ) ) ;
#6880=CARTESIAN_POINT ( 'NONE',  ( -6.826472737025120807, 128.1070736234661354, 4.959722759717906548 ) ) ;
#6881=DIRECTION ( 'NONE',  ( 1.000000000000000000, -0.000000000000000000, 0.000000000000000000 ) ) ;
#6882=( LENGTH_UNIT ( ) NAMED_UNIT ( * ) SI_UNIT ( .MILLI., .METRE. ) );
#6885=ORIENTED_EDGE ( 'NONE', *, *, #31606, .F. ) ;
#6890=LINE ( 'NONE', #17481, #13128 ) ;
#6892=DIRECTION ( 'NONE',  ( 0.000000000000000000, 0.000000000000000000, 1.000000000000000000 ) ) ;
#6894=VERTEX_POINT ( 'NONE', #62170 ) ;
#6895=CARTESIAN_POINT ( 'NONE',  ( -7.632228543268608334, 123.8429263765338249, 2.479861379858952830 ) ) ;
#6896=EDGE_CURVE ( 'NONE', #67189, #19250, #56194, .T. ) ;
#6901=EDGE_CURVE ( 'NONE', #51449, #52352, #53246, .T. ) ;
#6903=EDGE_CURVE ( 'NONE', #32066, #41197, #68170, .T. ) ;
#6904=DIRECTION ( 'NONE',  ( 1.000000000000000000, 0.000000000000000000, 0.000000000000000000 ) ) ;
#6905=ORIENTED_EDGE ( 'NONE', *, *, #58494, .F. ) ;
#6906=ADVANCED_FACE ( 'NONE', ( #50942 ), #68510, .F. ) ;
#6908=ORIENTED_EDGE ( 'NONE', *, *, #36890, .T. ) ;
#6909=CARTESIAN_POINT ( 'NONE',  ( 44.99999999999977973, 146.9999999999999716, -9.500000000000000000 ) ) ;
#6912=( GEOMETRIC_REPRESENTATION_CONTEXT ( 3 ) GLOBAL_UNCERTAINTY_ASSIGNED_CONTEXT ( ( #22222 ) ) GLOBAL_UNIT_ASSIGNED_CONTEXT ( ( #65194, #60590, #44493 ) ) REPRESENTATION_CONTEXT ( 'NONE', 'WORKASPACE' ) );
#6913=CARTESIAN_POINT ( 'NONE',  ( 15.98999599679679839, 118.4999999999999716, 7.000000000000000000 ) ) ;
#6917=CARTESIAN_POINT ( 'NONE',  ( -45.91547277936962246, 9.430195807687212550, -3.611004237778682402 ) ) ;
#6922=DIRECTION ( 'NONE',  ( 0.000000000000000000, 0.000000000000000000, 1.000000000000000000 ) ) ;
#6924=CARTESIAN_POINT ( 'NONE',  ( -71.50000000000000000, 14.49137674618942562, 7.500000000000000000 ) ) ;
#6925=ORIENTED_EDGE ( 'NONE', *, *, #67963, .T. ) ;
#6929=( GEOMETRIC_REPRESENTATION_CONTEXT ( 3 ) GLOBAL_UNCERTAINTY_ASSIGNED_CONTEXT ( ( #25047 ) ) GLOBAL_UNIT_ASSIGNED_CONTEXT ( ( #12026, #706, #16643 ) ) REPRESENTATION_CONTEXT ( 'NONE', 'WORKASPACE' ) );
#6932=ORIENTED_EDGE ( 'NONE', *, *, #61683, .F. ) ;
#6934=CARTESIAN_POINT ( 'NONE',  ( 45.00000000011531398, 10.00000000003077716, 3.953713388244146199 ) ) ;
#6935=CARTESIAN_POINT ( 'NONE',  ( -52.50000000000000000, -2.024042244987997205E-14, 12.00000000000000000 ) ) ;
#6941=CARTESIAN_POINT ( 'NONE',  ( 10.01517768586949231, 142.8049999999999500, 1.839758294383810543E-15 ) ) ;
#6944=AXIS2_PLACEMENT_3D ( 'NONE', #34807, #7044, #1719 ) ;
#6946=EDGE_CURVE ( 'NONE', #65906, #26318, #13802, .T. ) ;
#6947=SHAPE_REPRESENTATION ( '2. Support', ( #42840 ), #2244 ) ;
#6949=COLOUR_RGB ( '', 0.66274510, 0.83137255, 0.94901961) ;
#6957=ORIENTED_EDGE ( 'NONE', *, *, #42525, .T. ) ;
#6960=STYLED_ITEM ( 'NONE', ( #54967 ), #35309 ) ;
#6962=DIRECTION ( 'NONE',  ( 0.000000000000000000, 0.000000000000000000, 1.000000000000000000 ) ) ;
#6963=SURFACE_STYLE_FILL_AREA ( #22454 ) ;
#6964=AXIS2_PLACEMENT_3D ( 'NONE', #52577, #53922, #5722 ) ;
#6965=DIRECTION ( 'NONE',  ( 0.000000000000000000, 1.000000000000000000, -0.000000000000000000 ) ) ;
#6967=ORIENTED_EDGE ( 'NONE', *, *, #55908, .T. ) ;
#6971=CONICAL_SURFACE ( 'NONE', #49683, 5.000000000000004441, 0.7853981633974587151 ) ;
#6973=DIRECTION ( 'NONE',  ( 0.000000000000000000, 0.000000000000000000, -1.000000000000000000 ) ) ;
#6975=VERTEX_POINT ( 'NONE', #10465 ) ;
#6977=ADVANCED_FACE ( 'NONE', ( #32578 ), #43212, .T. ) ;
#6978=CARTESIAN_POINT ( 'NONE',  ( -41.49999999999997868, 10.49999999999998401, 3.000000000000000000 ) ) ;
#6980=EDGE_LOOP ( 'NONE', ( #49282, #34470, #11907, #17667 ) ) ;
#6983=CARTESIAN_POINT ( 'NONE',  ( -8.874979192299518260, 110.5000000000000142, -3.486497148140166313 ) ) ;
#6984=DIRECTION ( 'NONE',  ( 0.000000000000000000, 0.000000000000000000, 1.000000000000000000 ) ) ;
#6986=EDGE_CURVE ( 'NONE', #64475, #35776, #18283, .T. ) ;
#6987=CARTESIAN_POINT ( 'NONE',  ( -71.62068965517239860, 36.41396814395972115, -7.000000000000000000 ) ) ;
#6988=ORIENTED_EDGE ( 'NONE', *, *, #51155, .F. ) ;
#6989=CARTESIAN_POINT ( 'NONE',  ( -8.437984349512095861, 135.6929263765338192, -5.166775262442723748E-16 ) ) ;
#6992=STYLED_ITEM ( 'NONE', ( #59499 ), #24837 ) ;
#6997=ORIENTED_EDGE ( 'NONE', *, *, #4924, .F. ) ;
#6998=PRESENTATION_STYLE_ASSIGNMENT (( #45021 ) ) ;
#7000=DIRECTION ( 'NONE',  ( -0.000000000000000000, -1.000000000000000000, -0.000000000000000000 ) ) ;
#7002=CARTESIAN_POINT ( 'NONE',  ( -75.50000000000000000, 64.49137674618943095, -9.500000000000001776 ) ) ;
#7005=COLOUR_RGB ( '', 0.40784314, 0.44705882, 0.49803922) ;
#7008=CARTESIAN_POINT ( 'NONE',  ( -45.00000000000000000, 9.585819622309035282, -6.373651444779981468 ) ) ;
#7012=CARTESIAN_POINT ( 'NONE',  ( -71.99999999999998579, 64.07124727947029896, 7.000000000000000000 ) ) ;
#7016=DIRECTION ( 'NONE',  ( 0.000000000000000000, 0.000000000000000000, 1.000000000000000000 ) ) ;
#7022=COLOUR_RGB ( '', 0.31764706, 0.68627451, 0.89019608) ;
#7023=DIRECTION ( 'NONE',  ( -0.000000000000000000, -0.000000000000000000, 1.000000000000000000 ) ) ;
#7024=DIRECTION ( 'NONE',  ( -1.000000000000000000, 0.000000000000000000, 0.000000000000000000 ) ) ;
#7025=FACE_OUTER_BOUND ( 'NONE', #24268, .T. ) ;
#7027=CARTESIAN_POINT ( 'NONE',  ( 10.01517768586949231, 115.8049999999999784, 1.839758294383810543E-15 ) ) ;
#7032=CARTESIAN_POINT ( 'NONE',  ( 15.98999599679679839, 117.9999999999999716, -7.500000000000000000 ) ) ;
#7034=( NAMED_UNIT ( * ) SI_UNIT ( $, .STERADIAN. ) SOLID_ANGLE_UNIT ( ) );
#7036=ORIENTED_EDGE ( 'NONE', *, *, #50534, .F. ) ;
#7038=CIRCLE ( 'NONE', #232, 0.5000000000000004441 ) ;
#7042=AXIS2_PLACEMENT_3D ( 'NONE', #48577, #59774, #5596 ) ;
#7044=DIRECTION ( 'NONE',  ( 0.000000000000000000, 0.000000000000000000, 1.000000000000000000 ) ) ;
#7045=ORIENTED_EDGE ( 'NONE', *, *, #5633, .T. ) ;
#7048=STYLED_ITEM ( 'NONE', ( #5134 ), #60917 ) ;
#7050=STYLED_ITEM ( 'NONE', ( #63661 ), #46308 ) ;
#7051=CARTESIAN_POINT ( 'NONE',  ( 19.89974874213239886, 114.9999999999999574, 10.49999999999999645 ) ) ;
#7053=MECHANICAL_DESIGN_GEOMETRIC_PRESENTATION_REPRESENTATION('',(#46416),#47542);
#7054=CARTESIAN_POINT ( 'NONE',  ( -9.827790563157511022E-16, 143.5570736234661524, 8.025000000000000355 ) ) ;
#7058=VERTEX_POINT ( 'NONE', #15749 ) ;
#7059=ORIENTED_EDGE ( 'NONE', *, *, #46420, .T. ) ;
#7060=CARTESIAN_POINT ( 'NONE',  ( -44.99999999999977973, 146.9999999999999716, -7.500000000000000000 ) ) ;
#7061=DIRECTION ( 'NONE',  ( 1.000000000000000000, 0.000000000000000000, 0.000000000000000000 ) ) ;
#7062=MECHANICAL_DESIGN_GEOMETRIC_PRESENTATION_REPRESENTATION('',(#37457),#29553);
#7063=ORIENTED_EDGE ( 'NONE', *, *, #32733, .T. ) ;
#7067=( GEOMETRIC_REPRESENTATION_CONTEXT ( 3 ) GLOBAL_UNCERTAINTY_ASSIGNED_CONTEXT ( ( #55952 ) ) GLOBAL_UNIT_ASSIGNED_CONTEXT ( ( #56752, #35293, #13464 ) ) REPRESENTATION_CONTEXT ( 'NONE', 'WORKASPACE' ) );
#7068=( NAMED_UNIT ( * ) SI_UNIT ( $, .STERADIAN. ) SOLID_ANGLE_UNIT ( ) );
#7069=CARTESIAN_POINT ( 'NONE',  ( 5.598654528085805993, 132.2450000000000045, 7.705886871421374629 ) ) ;
#7071=COLOUR_RGB ( '', 0.31764706, 0.68627451, 0.89019608) ;
#7073=DIRECTION ( 'NONE',  ( -0.000000000000000000, -0.000000000000000000, -1.000000000000000000 ) ) ;
#7074=CARTESIAN_POINT ( 'NONE',  ( -8.102448949553179958, 126.6049999999999898, 5.886773742842747126 ) ) ;
#7076=CARTESIAN_POINT ( 'NONE',  ( 40.82708550458274033, 108.1272155206430483, -3.301554093733430228 ) ) ;
#7078=CARTESIAN_POINT ( 'NONE',  ( 8.102448949553181734, 160.5049999999999386, 5.886773742842750679 ) ) ;
#7080=ADVANCED_FACE ( 'NONE', ( #5845 ), #58755, .T. ) ;
#7082=AXIS2_PLACEMENT_3D ( 'NONE', #54041, #31188, #26934 ) ;
#7083=AXIS2_PLACEMENT_3D ( 'NONE', #10918, #59421, #960 ) ;
#7084=( NAMED_UNIT ( * ) PLANE_ANGLE_UNIT ( ) SI_UNIT ( $, .RADIAN. ) );
#7086=DIRECTION ( 'NONE',  ( -1.000000000000000000, 0.000000000000000000, 0.000000000000000000 ) ) ;
#7087=MECHANICAL_DESIGN_GEOMETRIC_PRESENTATION_REPRESENTATION('',(#43042),#66642);
#7088=ORIENTED_EDGE ( 'NONE', *, *, #23304, .T. ) ;
#7095=VERTEX_POINT ( 'NONE', #7590 ) ;
#7097=ADVANCED_FACE ( 'NONE', ( #60016 ), #34333, .F. ) ;
#7098=PRESENTATION_STYLE_ASSIGNMENT (( #27821 ) ) ;
#7099=DIRECTION ( 'NONE',  ( 0.000000000000000000, 1.000000000000000000, 0.000000000000000000 ) ) ;
#7104=DIRECTION ( 'NONE',  ( 0.000000000000000000, -1.000000000000000000, 0.000000000000000000 ) ) ;
#7109=MECHANICAL_DESIGN_GEOMETRIC_PRESENTATION_REPRESENTATION('',(#20555),#46462);
#7114=DIRECTION ( 'NONE',  ( 4.336808689941999001E-16, -1.000000000000000000, -0.000000000000000000 ) ) ;
#7116=AXIS2_PLACEMENT_3D ( 'NONE', #17019, #50395, #11366 ) ;
#7117=CARTESIAN_POINT ( 'NONE',  ( 5.598654528085805993, 129.2450000000000045, 7.705886871421374629 ) ) ;
#7119=AXIS2_PLACEMENT_3D ( 'NONE', #33717, #54486, #43318 ) ;
#7121=AXIS2_PLACEMENT_3D ( 'NONE', #4561, #26015, #47188 ) ;
#7123=( NAMED_UNIT ( * ) SI_UNIT ( $, .STERADIAN. ) SOLID_ANGLE_UNIT ( ) );
#7130=ORIENTED_EDGE ( 'NONE', *, *, #66467, .T. ) ;
#7132=ORIENTED_EDGE ( 'NONE', *, *, #65186, .F. ) ;
#7134=CARTESIAN_POINT ( 'NONE',  ( -45.79655366757389601, 8.974374905500285493, 6.364158535394770055 ) ) ;
#7135=DIRECTION ( 'NONE',  ( 1.000000000000000000, 0.000000000000000000, 0.000000000000000000 ) ) ;
#7136=AXIS2_PLACEMENT_3D ( 'NONE', #48851, #10141, #31574 ) ;
#7138=CARTESIAN_POINT ( 'NONE',  ( -44.99154893936433552, 9.591540374752312914, 3.000000000000000000 ) ) ;
#7140=DIRECTION ( 'NONE',  ( 1.000000000000000000, -0.000000000000000000, -0.000000000000000000 ) ) ;
#7146=DIRECTION ( 'NONE',  ( 0.7071067811865549002, 0.000000000000000000, 0.7071067811865402453 ) ) ;
#7147=CARTESIAN_POINT ( 'NONE',  ( 15.98999599679679839, 146.4999999999999716, -10.00000000000000000 ) ) ;
#7150=AXIS2_PLACEMENT_3D ( 'NONE', #56525, #41083, #35443 ) ;
#7152=PLANE ( 'NONE',  #28641 ) ;
#7153=CARTESIAN_POINT ( 'NONE',  ( 7.632228543268607446, 150.1570736234661751, 2.479861379858954606 ) ) ;
#7157=TOROIDAL_SURFACE ( 'NONE', #35229, 1.000000000000000000, 0.5000000000000000000 ) ;
#7160=CARTESIAN_POINT ( 'NONE',  ( 5.598654528085805993, 130.3549999999999898, 7.705886871421374629 ) ) ;
#7161=DIRECTION ( 'NONE',  ( -1.387778780781444413E-14, -1.000000000000000000, 0.000000000000000000 ) ) ;
#7162=FILL_AREA_STYLE ('',( #67290 ) ) ;
#7163=DIRECTION ( 'NONE',  ( -1.156482317317873451E-16, -1.000000000000000000, 0.000000000000000000 ) ) ;
#7164=( GEOMETRIC_REPRESENTATION_CONTEXT ( 3 ) GLOBAL_UNCERTAINTY_ASSIGNED_CONTEXT ( ( #45456 ) ) GLOBAL_UNIT_ASSIGNED_CONTEXT ( ( #56003, #29629, #52156 ) ) REPRESENTATION_CONTEXT ( 'NONE', 'WORKASPACE' ) );
#7165=CARTESIAN_POINT ( 'NONE',  ( 23.21231517720797655, 117.4999999999999716, 9.500000000000000000 ) ) ;
#7166=CYLINDRICAL_SURFACE ( 'NONE', #17562, 0.5000000000000004441 ) ;
#7168=SURFACE_STYLE_USAGE ( .BOTH. , #49736 ) ;
#7171=CYLINDRICAL_SURFACE ( 'NONE', #21664, 0.5000000000000004441 ) ;
#7175=SURFACE_STYLE_FILL_AREA ( #1124 ) ;
#7176=CARTESIAN_POINT ( 'NONE',  ( -44.99999999999999289, 8.382277537376673138, -5.549490760430606073 ) ) ;
#7178=CARTESIAN_POINT ( 'NONE',  ( 72.50000000000000000, 36.32520566882265456, 9.500000000000000000 ) ) ;
#7182=DIRECTION ( 'NONE',  ( 0.000000000000000000, 0.000000000000000000, 1.000000000000000000 ) ) ;
#7183=ORIENTED_EDGE ( 'NONE', *, *, #48140, .F. ) ;
#7185=STYLED_ITEM ( 'NONE', ( #48529 ), #29705 ) ;
#7186=DIRECTION ( 'NONE',  ( 1.156482317317873451E-16, 1.000000000000000000, -0.000000000000000000 ) ) ;
#7189=SURFACE_SIDE_STYLE ('',( #55364 ) ) ;
#7195=CARTESIAN_POINT ( 'NONE',  ( 3.094860106618431583, 135.0949999999999704, 9.525000000000000355 ) ) ;
#7197=COLOUR_RGB ( '', 0.31764706, 0.68627451, 0.89019608) ;
#7202=( LENGTH_UNIT ( ) NAMED_UNIT ( * ) SI_UNIT ( .MILLI., .METRE. ) );
#7206=( LENGTH_UNIT ( ) NAMED_UNIT ( * ) SI_UNIT ( .MILLI., .METRE. ) );
#7209=AXIS2_PLACEMENT_3D ( 'NONE', #66316, #28310, #18142 ) ;
#7213=EDGE_CURVE ( 'NONE', #33977, #15830, #5902, .T. ) ;
#7214=CARTESIAN_POINT ( 'NONE',  ( -65.49999999999998579, 50.00000000000000000, -9.999999999999998224 ) ) ;
#7217=DIRECTION ( 'NONE',  ( 0.000000000000000000, 0.000000000000000000, 1.000000000000000000 ) ) ;
#7219=FILL_AREA_STYLE_COLOUR ( '', #55650 ) ;
#7221=( LENGTH_UNIT ( ) NAMED_UNIT ( * ) SI_UNIT ( .MILLI., .METRE. ) );
#7224=CARTESIAN_POINT ( 'NONE',  ( 45.00000000000000000, 99.99999999999992895, -9.500000000000000000 ) ) ;
#7227=CARTESIAN_POINT ( 'NONE',  ( 0.000000000000000000, 87.30187232391182306, 0.000000000000000000 ) ) ;
#7228=VECTOR ( 'NONE', #17934, 1000.000000000000000 ) ;
#7230=CARTESIAN_POINT ( 'NONE',  ( -41.49999999999998579, 106.9282032302754999, 3.500000000000000000 ) ) ;
#7235=DIRECTION ( 'NONE',  ( 1.000000000000000000, 0.000000000000000000, 0.000000000000000000 ) ) ;
#7238=CARTESIAN_POINT ( 'NONE',  ( 2.607480562269071989, 119.7070736234661723, 8.025000000000002132 ) ) ;
#7241=EDGE_CURVE ( 'NONE', #22515, #35027, #2955, .T. ) ;
#7244=( LENGTH_UNIT ( ) NAMED_UNIT ( * ) SI_UNIT ( .MILLI., .METRE. ) );
#7245=ORIENTED_EDGE ( 'NONE', *, *, #42146, .T. ) ;
#7247=AXIS2_PLACEMENT_3D ( 'NONE', #38479, #60228, #48680 ) ;
#7249=VERTEX_POINT ( 'NONE', #2619 ) ;
#7251=SURFACE_STYLE_USAGE ( .BOTH. , #35011 ) ;
#7254=DIRECTION ( 'NONE',  ( 1.000000000000000000, 0.000000000000000000, 0.000000000000000000 ) ) ;
#7257=CARTESIAN_POINT ( 'NONE',  ( 0.8118891587097655238, 154.3723208332566514, -9.397320833256809891 ) ) ;
#7260=ORIENTED_EDGE ( 'NONE', *, *, #33659, .T. ) ;
#7263=AXIS2_PLACEMENT_3D ( 'NONE', #22758, #34346, #55451 ) ;
#7264=DIRECTION ( 'NONE',  ( 0.000000000000000000, 1.000000000000000000, 0.000000000000000000 ) ) ;
#7269=DIRECTION ( 'NONE',  ( -0.000000000000000000, -0.000000000000000000, 1.000000000000000000 ) ) ;
#7273=CARTESIAN_POINT ( 'NONE',  ( -44.50000000000000000, 10.49999999999998579, 3.000000000000000000 ) ) ;
#7275=AXIS2_PLACEMENT_3D ( 'NONE', #56677, #8830, #67576 ) ;
#7282=SURFACE_STYLE_USAGE ( .BOTH. , #29409 ) ;
#7284=( NAMED_UNIT ( * ) SI_UNIT ( $, .STERADIAN. ) SOLID_ANGLE_UNIT ( ) );
#7295=CARTESIAN_POINT ( 'NONE',  ( 71.50000000000000000, 35.92875272052971525, 7.000000000000000000 ) ) ;
#7298=CARTESIAN_POINT ( 'NONE',  ( 15.48999599679679662, 146.4999999999999716, 7.500000000000000000 ) ) ;
#7301=CARTESIAN_POINT ( 'NONE',  ( 9.058813317711337021, 148.6549999999999727, 2.943386871421375783 ) ) ;
#7303=CIRCLE ( 'NONE', #62382, 0.5000000000000004441 ) ;
#7306=CARTESIAN_POINT ( 'NONE',  ( 48.50000000000000000, 99.99999999999992895, -7.000000000000000000 ) ) ;
#7307=UNCERTAINTY_MEASURE_WITH_UNIT (LENGTH_MEASURE( 1.000000000000000082E-05 ), #37353, 'distance_accuracy_value', 'NONE');
#7314=DIRECTION ( 'NONE',  ( 1.000000000000000000, 0.000000000000000000, 0.000000000000000000 ) ) ;
#7315=EDGE_CURVE ( 'NONE', #30440, #42106, #68788, .T. ) ;
#7320=CARTESIAN_POINT ( 'NONE',  ( -2.607480562269115509, 135.0929263765338249, -8.024999999999970157 ) ) ;
#7322=EDGE_CURVE ( 'NONE', #9977, #60808, #58866, .T. ) ;
#7325=CYLINDRICAL_SURFACE ( 'NONE', #27413, 0.5000000000000004441 ) ;
#7332=CARTESIAN_POINT ( 'NONE',  ( 0.000000000000000000, 110.5549999999999926, -9.525000000000000355 ) ) ;
#7337=( GEOMETRIC_REPRESENTATION_CONTEXT ( 3 ) GLOBAL_UNCERTAINTY_ASSIGNED_CONTEXT ( ( #58818 ) ) GLOBAL_UNIT_ASSIGNED_CONTEXT ( ( #53224, #15952, #59504 ) ) REPRESENTATION_CONTEXT ( 'NONE', 'WORKASPACE' ) );
#7339=CARTESIAN_POINT ( 'NONE',  ( -74.13095319853044884, 9.253562910438322575, -6.241030289661791741 ) ) ;
#7341=PLANE ( 'NONE',  #2449 ) ;
#7345=CARTESIAN_POINT ( 'NONE',  ( 6.826472737025119919, 136.8929263765338362, 4.959722759717908325 ) ) ;
#7351=ORIENTED_EDGE ( 'NONE', *, *, #24941, .F. ) ;
#7356=( LENGTH_UNIT ( ) NAMED_UNIT ( * ) SI_UNIT ( .MILLI., .METRE. ) );
#7357=CARTESIAN_POINT ( 'NONE',  ( 0.000000000000000000, 87.30187232391182306, 8.025000000000000355 ) ) ;
#7360=DIRECTION ( 'NONE',  ( 1.000000000000000000, 0.000000000000000000, 0.000000000000000000 ) ) ;
#7364=CARTESIAN_POINT ( 'NONE',  ( -45.00000000000000000, 9.027015924850157802, -6.778771685250380763 ) ) ;
#7380=( GEOMETRIC_REPRESENTATION_CONTEXT ( 3 ) GLOBAL_UNCERTAINTY_ASSIGNED_CONTEXT ( ( #4643 ) ) GLOBAL_UNIT_ASSIGNED_CONTEXT ( ( #54692, #22017, #61357 ) ) REPRESENTATION_CONTEXT ( 'NONE', 'WORKASPACE' ) );
#7382=CARTESIAN_POINT ( 'NONE',  ( 4.630149463674436916, 154.5000000000001137, -8.335376919559424280 ) ) ;
#7386=CARTESIAN_POINT ( 'NONE',  ( -10.01517768586949231, 114.3049999999999926, -6.132527647946036459E-16 ) ) ;
#7392=UNCERTAINTY_MEASURE_WITH_UNIT (LENGTH_MEASURE( 1.000000000000000082E-05 ), #22652, 'distance_accuracy_value', 'NONE');
#7393=FACE_OUTER_BOUND ( 'NONE', #27656, .T. ) ;
#7401=AXIS2_PLACEMENT_3D ( 'NONE', #31331, #21135, #4233 ) ;
#7403=FILL_AREA_STYLE ('',( #12657 ) ) ;
#7404=STYLED_ITEM ( 'NONE', ( #41709 ), #49780 ) ;
#7405=FILL_AREA_STYLE ('',( #45757 ) ) ;
#7407=VERTEX_POINT ( 'NONE', #44510 ) ;
#7409=CARTESIAN_POINT ( 'NONE',  ( 24.21231517720798010, 99.99999999999998579, -7.000000000000000000 ) ) ;
#7410=CARTESIAN_POINT ( 'NONE',  ( 0.000000000000000000, 87.30187232391182306, 0.000000000000000000 ) ) ;
#7411=( LENGTH_UNIT ( ) NAMED_UNIT ( * ) SI_UNIT ( .MILLI., .METRE. ) );
#7412=CARTESIAN_POINT ( 'NONE',  ( -24.21231517720798010, 113.4999999999999858, 9.500000000000000000 ) ) ;
#7414=DIRECTION ( 'NONE',  ( 0.000000000000000000, 0.000000000000000000, 1.000000000000000000 ) ) ;
#7416=ADVANCED_FACE ( 'NONE', ( #11401 ), #3093, .T. ) ;
#7417=ORIENTED_EDGE ( 'NONE', *, *, #62251, .F. ) ;
#7420=MECHANICAL_DESIGN_GEOMETRIC_PRESENTATION_REPRESENTATION('',(#24220),#8530);
#7421=ORIENTED_EDGE ( 'NONE', *, *, #14706, .F. ) ;
#7423=DIRECTION ( 'NONE',  ( 1.000000000000000000, 0.000000000000000000, 0.000000000000000000 ) ) ;
#7424=EDGE_LOOP ( 'NONE', ( #63041, #68779, #10791, #8802 ) ) ;
#7425=CIRCLE ( 'NONE', #620, 0.5000000000000004441 ) ;
#7427=SURFACE_SIDE_STYLE ('',( #45445 ) ) ;
#7428=CARTESIAN_POINT ( 'NONE',  ( -5.598654528085808657, 134.6449999999999818, 7.705886871421373741 ) ) ;
#7433=CARTESIAN_POINT ( 'NONE',  ( -5.598654528085808657, 141.7549999999999955, 7.705886871421373741 ) ) ;
#7435=SURFACE_STYLE_FILL_AREA ( #2063 ) ;
#7436=VERTEX_POINT ( 'NONE', #19451 ) ;
#7437=CARTESIAN_POINT ( 'NONE',  ( 9.058813317711337021, 157.6550000000000011, 2.943386871421375783 ) ) ;
#7440=SURFACE_SIDE_STYLE ('',( #7758 ) ) ;
#7442=ORIENTED_EDGE ( 'NONE', *, *, #10436, .T. ) ;
#7450=SURFACE_STYLE_FILL_AREA ( #2082 ) ;
#7451=UNCERTAINTY_MEASURE_WITH_UNIT (LENGTH_MEASURE( 1.000000000000000082E-05 ), #28264, 'distance_accuracy_value', 'NONE');
#7452=CIRCLE ( 'NONE', #52405, 14.49999999999999822 ) ;
#7458=ORIENTED_EDGE ( 'NONE', *, *, #67795, .T. ) ;
#7459=DIRECTION ( 'NONE',  ( -0.000000000000000000, -1.000000000000000000, -0.000000000000000000 ) ) ;
#7462=ORIENTED_EDGE ( 'NONE', *, *, #36515, .F. ) ;
#7463=FILL_AREA_STYLE_COLOUR ( '', #3385 ) ;
#7464=FILL_AREA_STYLE_COLOUR ( '', #18818 ) ;
#7465=CARTESIAN_POINT ( 'NONE',  ( 12.72792206135785698, 149.9999999999999716, 10.00000000000000000 ) ) ;
#7466=CIRCLE ( 'NONE', #26526, 5.499999999999976907 ) ;
#7467=CARTESIAN_POINT ( 'NONE',  ( 3.094860106618431583, 141.0949999999999989, 9.525000000000000355 ) ) ;
#7477=ORIENTED_EDGE ( 'NONE', *, *, #28739, .T. ) ;
#7479=VERTEX_POINT ( 'NONE', #13837 ) ;
#7480=EDGE_CURVE ( 'NONE', #8394, #24181, #7515, .T. ) ;
#7486=CARTESIAN_POINT ( 'NONE',  ( -9.827790563157511022E-16, 143.5570736234661524, 8.025000000000000355 ) ) ;
#7487=VECTOR ( 'NONE', #58569, 1000.000000000000000 ) ;
#7488=EDGE_CURVE ( 'NONE', #37840, #1408, #4925, .T. ) ;
#7491=VECTOR ( 'NONE', #63051, 1000.000000000000000 ) ;
#7493=TOROIDAL_SURFACE ( 'NONE', #6332, 1.000000000000000000, 0.5000000000000000000 ) ;
#7495=CARTESIAN_POINT ( 'NONE',  ( 6.826472737025121695, 150.6070736234661069, -4.959722759717905660 ) ) ;
#7497=CARTESIAN_POINT ( 'NONE',  ( 8.102448949553179958, 112.5049999999999670, 5.886773742842750679 ) ) ;
#7499=SURFACE_SIDE_STYLE ('',( #18057 ) ) ;
#7500=CARTESIAN_POINT ( 'NONE',  ( -3.094860106618434248, 132.9050000000000011, 9.525000000000000355 ) ) ;
#7503=SURFACE_SIDE_STYLE ('',( #13460 ) ) ;
#7505=FILL_AREA_STYLE ('',( #65901 ) ) ;
#7507=DIRECTION ( 'NONE',  ( -0.2413793103448194644, -0.9704308468600220117, 0.000000000000000000 ) ) ;
#7509=SURFACE_STYLE_FILL_AREA ( #60958 ) ;
#7510=DIRECTION ( 'NONE',  ( -1.156482317317873451E-16, 1.000000000000000000, 0.000000000000000000 ) ) ;
#7513=CARTESIAN_POINT ( 'NONE',  ( -71.50000000000000000, 35.92875272052971525, -7.500000000000000000 ) ) ;
#7515=LINE ( 'NONE', #62370, #19526 ) ;
#7517=VERTEX_POINT ( 'NONE', #23690 ) ;
#7518=CYLINDRICAL_SURFACE ( 'NONE', #49417, 8.025000000000000355 ) ;
#7520=( NAMED_UNIT ( * ) PLANE_ANGLE_UNIT ( ) SI_UNIT ( $, .RADIAN. ) );
#7521=ORIENTED_EDGE ( 'NONE', *, *, #62499, .T. ) ;
#7522=CARTESIAN_POINT ( 'NONE',  ( -75.00000000000000000, 8.674606743306283008, 5.942398972768304866 ) ) ;
#7524=ORIENTED_EDGE ( 'NONE', *, *, #14362, .F. ) ;
#7525=DIRECTION ( 'NONE',  ( 0.000000000000000000, 0.000000000000000000, 1.000000000000000000 ) ) ;
#7529=CARTESIAN_POINT ( 'NONE',  ( -5.598654528085808657, 146.6450000000000102, 7.705886871421373741 ) ) ;
#7532=FACE_OUTER_BOUND ( 'NONE', #45004, .T. ) ;
#7535=SURFACE_SIDE_STYLE ('',( #60989 ) ) ;
#7541=DIRECTION ( 'NONE',  ( 0.000000000000000000, 0.000000000000000000, 1.000000000000000000 ) ) ;
#7543=EDGE_CURVE ( 'NONE', #42377, #35623, #33057, .T. ) ;
#7545=CARTESIAN_POINT ( 'NONE',  ( 45.00000000000000000, -1.469576158976824618E-14, -9.500000000000000000 ) ) ;
#7549=EDGE_CURVE ( 'NONE', #28212, #46059, #34581, .T. ) ;
#7555=EDGE_CURVE ( 'NONE', #63218, #16463, #44294, .T. ) ;
#7558=DIRECTION ( 'NONE',  ( 0.000000000000000000, 0.000000000000000000, 1.000000000000000000 ) ) ;
#7559=PRESENTATION_STYLE_ASSIGNMENT (( #23059 ) ) ;
#7566=FILL_AREA_STYLE ('',( #12482 ) ) ;
#7567=CARTESIAN_POINT ( 'NONE',  ( -40.99999999999998579, 108.0041655821620168, 3.000000000000000888 ) ) ;
#7572=DIRECTION ( 'NONE',  ( 0.000000000000000000, 0.000000000000000000, 1.000000000000000000 ) ) ;
#7575=CARTESIAN_POINT ( 'NONE',  ( -2.607480562269073765, 124.2070736234661581, -8.025000000000000355 ) ) ;
#7576=SURFACE_STYLE_USAGE ( .BOTH. , #38941 ) ;
#7578=TOROIDAL_SURFACE ( 'NONE', #56997, 8.500000000000012434, 0.5000000000000000000 ) ;
#7579=EDGE_LOOP ( 'NONE', ( #44012, #33343, #27416, #16439 ) ) ;
#7580=( GEOMETRIC_REPRESENTATION_CONTEXT ( 3 ) GLOBAL_UNCERTAINTY_ASSIGNED_CONTEXT ( ( #6577 ) ) GLOBAL_UNIT_ASSIGNED_CONTEXT ( ( #46786, #50618, #30173 ) ) REPRESENTATION_CONTEXT ( 'NONE', 'WORKASPACE' ) );
#7584=SURFACE_STYLE_FILL_AREA ( #12861 ) ;
#7588=EDGE_CURVE ( 'NONE', #19233, #45842, #15111, .T. ) ;
#7589=CARTESIAN_POINT ( 'NONE',  ( -6.826472737025120807, 123.3929263765338078, -4.959722759717907437 ) ) ;
#7590=CARTESIAN_POINT ( 'NONE',  ( 0.000000000000000000, 122.9429263765338192, -8.025000000000000355 ) ) ;
#7592=SPHERICAL_SURFACE ( 'NONE', #51602, 0.5000000000000000000 ) ;
#7595=DIRECTION ( 'NONE',  ( 0.000000000000000000, 0.000000000000000000, -1.000000000000000000 ) ) ;
#7597=CARTESIAN_POINT ( 'NONE',  ( -15.98999599679679839, 117.9999999999999716, -7.500000000000000000 ) ) ;
#7600=( NAMED_UNIT ( * ) SI_UNIT ( $, .STERADIAN. ) SOLID_ANGLE_UNIT ( ) );
#7608=DIRECTION ( 'NONE',  ( 0.000000000000000000, -1.000000000000000000, 0.000000000000000000 ) ) ;
#7610=ORIENTED_EDGE ( 'NONE', *, *, #51926, .F. ) ;
#7618=ADVANCED_FACE ( 'NONE', ( #54138 ), #273, .T. ) ;
#7619=DIRECTION ( 'NONE',  ( 0.000000000000000000, 0.000000000000000000, 1.000000000000000000 ) ) ;
#7620=PRESENTATION_STYLE_ASSIGNMENT (( #38300 ) ) ;
#7621=CIRCLE ( 'NONE', #63762, 0.5000000000000004441 ) ;
#7622=DIRECTION ( 'NONE',  ( -1.000000000000000000, -0.000000000000000000, -0.000000000000000000 ) ) ;
#7628=CARTESIAN_POINT ( 'NONE',  ( -5.598654528085806881, 143.8549999999999898, -7.705886871421374629 ) ) ;
#7631=( GEOMETRIC_REPRESENTATION_CONTEXT ( 3 ) GLOBAL_UNCERTAINTY_ASSIGNED_CONTEXT ( ( #53795 ) ) GLOBAL_UNIT_ASSIGNED_CONTEXT ( ( #32214, #47404, #11093 ) ) REPRESENTATION_CONTEXT ( 'NONE', 'WORKASPACE' ) );
#7634=PRESENTATION_STYLE_ASSIGNMENT (( #1260 ) ) ;
#7636=SURFACE_STYLE_USAGE ( .BOTH. , #50911 ) ;
#7637=COLOUR_RGB ( '', 0.08235294, 0.09019608, 0.10196078) ;
#7639=DIRECTION ( 'NONE',  ( 1.000000000000000000, 0.000000000000000000, 0.000000000000000000 ) ) ;
#7640=( LENGTH_UNIT ( ) NAMED_UNIT ( * ) SI_UNIT ( .MILLI., .METRE. ) );
#7641=CARTESIAN_POINT ( 'NONE',  ( -14.98999599679679662, 146.4999999999999716, 9.500000000000000000 ) ) ;
#7643=VERTEX_POINT ( 'NONE', #69307 ) ;
#7648=FILL_AREA_STYLE_COLOUR ( '', #20817 ) ;
#7651=CARTESIAN_POINT ( 'NONE',  ( -1.166476076187854022E-15, 112.0549999999999926, 9.525000000000000355 ) ) ;
#7652=DIRECTION ( 'NONE',  ( 1.000000000000000000, 0.000000000000000000, 0.000000000000000000 ) ) ;
#7655=( NAMED_UNIT ( * ) PLANE_ANGLE_UNIT ( ) SI_UNIT ( $, .RADIAN. ) );
#7663=LINE ( 'NONE', #60771, #40735 ) ;
#7667=CARTESIAN_POINT ( 'NONE',  ( 4.716976649647096842, 142.7429263765338305, 6.492361379858953896 ) ) ;
#7668=( LENGTH_UNIT ( ) NAMED_UNIT ( * ) SI_UNIT ( .MILLI., .METRE. ) );
#7669=FILL_AREA_STYLE ('',( #3750 ) ) ;
#7671=DIRECTION ( 'NONE',  ( 1.000000000000000000, 0.000000000000000000, 0.000000000000000000 ) ) ;
#7674=ORIENTED_EDGE ( 'NONE', *, *, #17439, .T. ) ;
#7675=CARTESIAN_POINT ( 'NONE',  ( -72.00000000000000000, 14.49137674618942562, 7.000000000000000000 ) ) ;
#7676=CARTESIAN_POINT ( 'NONE',  ( 41.45364736693642982, 107.0151787721003842, -3.500000000000000444 ) ) ;
#7679=( LENGTH_UNIT ( ) NAMED_UNIT ( * ) SI_UNIT ( .MILLI., .METRE. ) );
#7681=EDGE_LOOP ( 'NONE', ( #50539, #17231, #26337, #65318 ) ) ;
#7688=VERTEX_POINT ( 'NONE', #42960 ) ;
#7689=( NAMED_UNIT ( * ) PLANE_ANGLE_UNIT ( ) SI_UNIT ( $, .RADIAN. ) );
#7691=FACE_OUTER_BOUND ( 'NONE', #12900, .T. ) ;
#7692=EDGE_CURVE ( 'NONE', #39893, #197, #2719, .T. ) ;
#7697=( NAMED_UNIT ( * ) PLANE_ANGLE_UNIT ( ) SI_UNIT ( $, .RADIAN. ) );
#7700=( NAMED_UNIT ( * ) PLANE_ANGLE_UNIT ( ) SI_UNIT ( $, .RADIAN. ) );
#7704=DIRECTION ( 'NONE',  ( -0.000000000000000000, -0.000000000000000000, -1.000000000000000000 ) ) ;
#7705=CONICAL_SURFACE ( 'NONE', #62729, 8.025000000000000355, 0.7853981633974421728 ) ;
#7706=CARTESIAN_POINT ( 'NONE',  ( 8.437984349512095861, 117.3070736234661666, 1.550032578732816828E-15 ) ) ;
#7708=CARTESIAN_POINT ( 'NONE',  ( 0.8807004131023399296, 154.4999999999999716, -9.494441468940317819 ) ) ;
#7711=EDGE_CURVE ( 'NONE', #16182, #41197, #5025, .T. ) ;
#7713=CARTESIAN_POINT ( 'NONE',  ( 9.058813317711338797, 118.9549999999999983, -2.943386871421372675 ) ) ;
#7716=EDGE_CURVE ( 'NONE', #52417, #1012, #57816, .T. ) ;
#7720=VECTOR ( 'NONE', #62787, 1000.000000000000000 ) ;
#7730=SURFACE_STYLE_FILL_AREA ( #7403 ) ;
#7734=SURFACE_STYLE_USAGE ( .BOTH. , #42147 ) ;
#7742=ORIENTED_EDGE ( 'NONE', *, *, #16175, .T. ) ;
#7746=EDGE_LOOP ( 'NONE', ( #15675, #60966, #50918, #12535 ) ) ;
#7748=CYLINDRICAL_SURFACE ( 'NONE', #41085, 8.025000000000000355 ) ;
#7749=CARTESIAN_POINT ( 'NONE',  ( -1.166476076187854022E-15, 143.9449999999999932, 9.525000000000000355 ) ) ;
#7750=ORIENTED_EDGE ( 'NONE', *, *, #25353, .T. ) ;
#7751=CARTESIAN_POINT ( 'NONE',  ( -3.094860106618434248, 144.9050000000000011, 9.525000000000000355 ) ) ;
#7753=STYLED_ITEM ( 'NONE', ( #61856 ), #43560 ) ;
#7754=CARTESIAN_POINT ( 'NONE',  ( 41.03152803655225966, 107.9804733857993284, -3.206774974533878719 ) ) ;
#7755=VERTEX_POINT ( 'NONE', #23866 ) ;
#7756=CARTESIAN_POINT ( 'NONE',  ( 6.826472737025121695, 116.4929263765338021, -4.959722759717905660 ) ) ;
#7758=SURFACE_STYLE_FILL_AREA ( #55954 ) ;
#7759=FILL_AREA_STYLE_COLOUR ( '', #6949 ) ;
#7762=LINE ( 'NONE', #12695, #29513 ) ;
#7764=CARTESIAN_POINT ( 'NONE',  ( 12.72792206135785698, 115.4999999999999574, 10.50000000000000000 ) ) ;
#7765=( GEOMETRIC_REPRESENTATION_CONTEXT ( 3 ) GLOBAL_UNCERTAINTY_ASSIGNED_CONTEXT ( ( #50356 ) ) GLOBAL_UNIT_ASSIGNED_CONTEXT ( ( #50179, #40318, #18833 ) ) REPRESENTATION_CONTEXT ( 'NONE', 'WORKASPACE' ) );
#7771=( NAMED_UNIT ( * ) SI_UNIT ( $, .STERADIAN. ) SOLID_ANGLE_UNIT ( ) );
#7773=( BOUNDED_CURVE ( )  B_SPLINE_CURVE ( 3, ( #50054, #11350, #54258, #27512 ),
 .UNSPECIFIED., .F., .F. ) 
 B_SPLINE_CURVE_WITH_KNOTS ( ( 4, 4 ),
 ( 3.141592653589794004, 4.280198172320947236 ),
 .UNSPECIFIED. ) 
 CURVE ( )  GEOMETRIC_REPRESENTATION_ITEM ( )  RATIONAL_B_SPLINE_CURVE ( ( 1.000000000000000000, 0.8948513492540270953, 0.8948513492540270953, 1.000000000000000000 ) ) 
 REPRESENTATION_ITEM ( '' )  );
#7774=ADVANCED_FACE ( 'NONE', ( #49934 ), #18492, .T. ) ;
#7775=DIRECTION ( 'NONE',  ( -0.000000000000000000, -0.000000000000000000, 1.000000000000000000 ) ) ;
#7777=SURFACE_SIDE_STYLE ('',( #45118 ) ) ;
#7790=CARTESIAN_POINT ( 'NONE',  ( -75.00000000000000000, 7.967232421023206612, -7.000000003139141391 ) ) ;
#7791=EDGE_LOOP ( 'NONE', ( #34712, #52892, #44410, #41643 ) ) ;
#7792=SURFACE_SIDE_STYLE ('',( #17690 ) ) ;
#7793=AXIS2_PLACEMENT_3D ( 'NONE', #33579, #55735, #28267 ) ;
#7795=ADVANCED_FACE ( 'NONE', ( #60121 ), #19582, .T. ) ;
#7796=CARTESIAN_POINT ( 'NONE',  ( -3.094860106618432471, 136.5949999999999989, -9.525000000000000355 ) ) ;
#7801=FILL_AREA_STYLE_COLOUR ( '', #60456 ) ;
#7802=SURFACE_STYLE_FILL_AREA ( #59179 ) ;
#7806=ADVANCED_FACE ( 'NONE', ( #1990 ), #61823, .F. ) ;
#7808=AXIS2_PLACEMENT_3D ( 'NONE', #55923, #19317, #13704 ) ;
#7813=VERTEX_POINT ( 'NONE', #33720 ) ;
#7816=CARTESIAN_POINT ( 'NONE',  ( -74.50000000000001421, 1.735173206890468129E-14, 9.500000000000000000 ) ) ;
#7818=MECHANICAL_DESIGN_GEOMETRIC_PRESENTATION_REPRESENTATION('',(#61726),#69480);
#7819=CARTESIAN_POINT ( 'NONE',  ( -9.827790563157511022E-16, 119.5570736234661524, 8.025000000000000355 ) ) ;
#7823=CARTESIAN_POINT ( 'NONE',  ( -4.716976649647098618, 143.2570736234661410, 6.492361379858953008 ) ) ;
#7824=ORIENTED_EDGE ( 'NONE', *, *, #21352, .F. ) ;
#7827=CARTESIAN_POINT ( 'NONE',  ( -20.17679519342876304, 115.4776649671489963, -10.00000000000000000 ) ) ;
#7828=PRESENTATION_STYLE_ASSIGNMENT (( #33861 ) ) ;
#7831=SURFACE_STYLE_USAGE ( .BOTH. , #66945 ) ;
#7832=CARTESIAN_POINT ( 'NONE',  ( -3.094860106618434248, 113.7950000000000017, 9.525000000000000355 ) ) ;
#7833=MECHANICAL_DESIGN_GEOMETRIC_PRESENTATION_REPRESENTATION('',(#29158),#2134);
#7834=VERTEX_POINT ( 'NONE', #46408 ) ;
#7836=CARTESIAN_POINT ( 'NONE',  ( 5.598654528085805993, 115.3549999999999898, 7.705886871421374629 ) ) ;
#7838=CARTESIAN_POINT ( 'NONE',  ( 0.000000000000000000, 125.5550000000000068, -9.525000000000000355 ) ) ;
#7839=STYLED_ITEM ( 'NONE', ( #68207 ), #69257 ) ;
#7840=FACE_OUTER_BOUND ( 'NONE', #35722, .T. ) ;
#7841=CARTESIAN_POINT ( 'NONE',  ( 20.86663389611626229, 115.0293260623345475, 10.00000000000000000 ) ) ;
#7844=CARTESIAN_POINT ( 'NONE',  ( -71.49999999999998579, 64.07124727947029896, -9.500000000000000000 ) ) ;
#7845=ORIENTED_EDGE ( 'NONE', *, *, #42603, .T. ) ;
#7853=DIRECTION ( 'NONE',  ( 1.000000000000000000, 0.000000000000000000, 0.000000000000000000 ) ) ;
#7856=EDGE_LOOP ( 'NONE', ( #6967, #21600, #52062, #20675 ) ) ;
#7857=CARTESIAN_POINT ( 'NONE',  ( -75.00000000000000000, 9.025366258634575090, 6.779481487458411060 ) ) ;
#7858=ADVANCED_FACE ( 'NONE', ( #41127 ), #62869, .F. ) ;
#7860=VERTEX_POINT ( 'NONE', #8400 ) ;
#7861=( LENGTH_UNIT ( ) NAMED_UNIT ( * ) SI_UNIT ( .MILLI., .METRE. ) );
#7863=DIRECTION ( 'NONE',  ( 0.000000000000000000, 1.000000000000000000, 0.000000000000000000 ) ) ;
#7865=AXIS2_PLACEMENT_3D ( 'NONE', #11597, #27054, #289 ) ;
#7867=CIRCLE ( 'NONE', #52840, 26.99999999999999645 ) ;
#7868=FILL_AREA_STYLE ('',( #18444 ) ) ;
#7869=CARTESIAN_POINT ( 'NONE',  ( -8.102448949553179958, 142.8949999999999818, -5.886773742842749790 ) ) ;
#7871=AXIS2_PLACEMENT_3D ( 'NONE', #23465, #49885, #40727 ) ;
#7873=FILL_AREA_STYLE_COLOUR ( '', #50750 ) ;
#7876=CARTESIAN_POINT ( 'NONE',  ( -21.02379604162864268, 1.797044900979284448E-15, 10.00000000000000000 ) ) ;
#7877=DIRECTION ( 'NONE',  ( 0.000000000000000000, 0.000000000000000000, 1.000000000000000000 ) ) ;
#7878=ADVANCED_FACE ( 'NONE', ( #31202, #56567 ), #29835, .F. ) ;
#7880=DIRECTION ( 'NONE',  ( -0.000000000000000000, -0.000000000000000000, -1.000000000000000000 ) ) ;
#7881=FACE_OUTER_BOUND ( 'NONE', #40422, .T. ) ;
#7882=CARTESIAN_POINT ( 'NONE',  ( 8.102448949553183510, 114.9949999999999903, -5.886773742842746238 ) ) ;
#7892=CARTESIAN_POINT ( 'NONE',  ( -75.48275862068965125, 36.00832590023089352, -6.499999999999999112 ) ) ;
#7899=DIRECTION ( 'NONE',  ( -0.000000000000000000, -1.000000000000000000, 0.000000000000000000 ) ) ;
#7905=DIRECTION ( 'NONE',  ( 0.000000000000000000, -1.000000000000000000, 0.000000000000000000 ) ) ;
#7906=( GEOMETRIC_REPRESENTATION_CONTEXT ( 3 ) GLOBAL_UNCERTAINTY_ASSIGNED_CONTEXT ( ( #33253 ) ) GLOBAL_UNIT_ASSIGNED_CONTEXT ( ( #49269, #28822, #34457 ) ) REPRESENTATION_CONTEXT ( 'NONE', 'WORKASPACE' ) );
#7908=( NAMED_UNIT ( * ) SI_UNIT ( $, .STERADIAN. ) SOLID_ANGLE_UNIT ( ) );
#7909=CARTESIAN_POINT ( 'NONE',  ( -40.95793942983048197, 108.0317815798968866, 3.561444987364583259 ) ) ;
#7910=CARTESIAN_POINT ( 'NONE',  ( 60.00000000000000000, 1.797044900979284448E-15, 10.00000000000000000 ) ) ;
#7914=TOROIDAL_SURFACE ( 'NONE', #11332, 8.499999999999998224, 0.5000000000000000000 ) ;
#7916=( GEOMETRIC_REPRESENTATION_CONTEXT ( 3 ) GLOBAL_UNCERTAINTY_ASSIGNED_CONTEXT ( ( #12345 ) ) GLOBAL_UNIT_ASSIGNED_CONTEXT ( ( #30522, #47836, #42206 ) ) REPRESENTATION_CONTEXT ( 'NONE', 'WORKASPACE' ) );
#7917=ORIENTED_EDGE ( 'NONE', *, *, #46184, .F. ) ;
#7920=CARTESIAN_POINT ( 'NONE',  ( 7.632228543268608334, 132.4570736234661581, -2.479861379858951942 ) ) ;
#7922=AXIS2_PLACEMENT_3D ( 'NONE', #61108, #62138, #13252 ) ;
#7923=CARTESIAN_POINT ( 'NONE',  ( -15.98999599679679839, 146.4999999999999716, -7.000000000000000000 ) ) ;
#7924=AXIS2_PLACEMENT_3D ( 'NONE', #18037, #64836, #39522 ) ;
#7928=DIRECTION ( 'NONE',  ( -0.000000000000000000, -0.000000000000000000, 1.000000000000000000 ) ) ;
#7930=FILL_AREA_STYLE ('',( #18500 ) ) ;
#7931=MECHANICAL_DESIGN_GEOMETRIC_PRESENTATION_REPRESENTATION('',(#19164),#65224);
#7933=DIRECTION ( 'NONE',  ( -1.000000000000000000, 0.000000000000000000, -0.000000000000000000 ) ) ;
#7936=VECTOR ( 'NONE', #21055, 1000.000000000000000 ) ;
#7941=UNCERTAINTY_MEASURE_WITH_UNIT (LENGTH_MEASURE( 1.000000000000000082E-05 ), #36733, 'distance_accuracy_value', 'NONE');
#7942=VERTEX_POINT ( 'NONE', #10813 ) ;
#7951=( NAMED_UNIT ( * ) PLANE_ANGLE_UNIT ( ) SI_UNIT ( $, .RADIAN. ) );
#7958=VECTOR ( 'NONE', #21156, 1000.000000000000000 ) ;
#7969=CARTESIAN_POINT ( 'NONE',  ( -8.300844275602472067, 111.4071313305642263, -2.350466666536774607 ) ) ;
#7970=COLOUR_RGB ( '', 0.09019608, 0.27058824, 0.51372549) ;
#7973=AXIS2_PLACEMENT_3D ( 'NONE', #11810, #17130, #6513 ) ;
#7974=ORIENTED_EDGE ( 'NONE', *, *, #37047, .T. ) ;
#7975=STYLED_ITEM ( 'NONE', ( #57572 ), #53924 ) ;
#7976=DIRECTION ( 'NONE',  ( -1.000000000000000000, 0.000000000000000000, 0.000000000000000000 ) ) ;
#7978=( LENGTH_UNIT ( ) NAMED_UNIT ( * ) SI_UNIT ( .MILLI., .METRE. ) );
#7984=CARTESIAN_POINT ( 'NONE',  ( -1.166476076187854022E-15, 142.0549999999999784, 9.525000000000000355 ) ) ;
#7985=PLANE ( 'NONE',  #14057 ) ;
#7988=UNCERTAINTY_MEASURE_WITH_UNIT (LENGTH_MEASURE( 1.000000000000000082E-05 ), #17776, 'distance_accuracy_value', 'NONE');
#7989=FILL_AREA_STYLE_COLOUR ( '', #45096 ) ;
#7994=CARTESIAN_POINT ( 'NONE',  ( -74.99999999999998579, 50.00000000000000000, 12.00000000000000000 ) ) ;
#7995=PRESENTATION_STYLE_ASSIGNMENT (( #12213 ) ) ;
#7999=STYLED_ITEM ( 'NONE', ( #30445 ), #12707 ) ;
#8004=ORIENTED_EDGE ( 'NONE', *, *, #58882, .F. ) ;
#8005=( NAMED_UNIT ( * ) PLANE_ANGLE_UNIT ( ) SI_UNIT ( $, .RADIAN. ) );
#8006=DIRECTION ( 'NONE',  ( 1.000000000000000000, 0.000000000000000000, 0.000000000000000000 ) ) ;
#8009=CARTESIAN_POINT ( 'NONE',  ( -3.094860106618432471, 113.7049999999999699, -9.525000000000000355 ) ) ;
#8011=ORIENTED_EDGE ( 'NONE', *, *, #42771, .T. ) ;
#8012=AXIS2_PLACEMENT_3D ( 'NONE', #65366, #6962, #33015 ) ;
#8013=ADVANCED_FACE ( 'NONE', ( #21020 ), #43225, .T. ) ;
#8014=DIRECTION ( 'NONE',  ( -1.000000000000000000, 0.000000000000000000, 0.000000000000000000 ) ) ;
#8015=LINE ( 'NONE', #2693, #61978 ) ;
#8020=CARTESIAN_POINT ( 'NONE',  ( 72.49999999999998579, 119.9999999999997868, 10.00000000000000000 ) ) ;
#8022=CARTESIAN_POINT ( 'NONE',  ( -75.00000000000000000, -2.215169945516535778E-14, 6.999999999999999112 ) ) ;
#8023=ORIENTED_EDGE ( 'NONE', *, *, #42401, .T. ) ;
#8024=CARTESIAN_POINT ( 'NONE',  ( 6.826472737025119919, 145.8929263765338362, 4.959722759717908325 ) ) ;
#8025=( NAMED_UNIT ( * ) SI_UNIT ( $, .STERADIAN. ) SOLID_ANGLE_UNIT ( ) );
#8026=CIRCLE ( 'NONE', #27085, 0.5000000000000004441 ) ;
#8035=CARTESIAN_POINT ( 'NONE',  ( -2.607480562269200330, 140.4070736234661751, 8.024999999999911537 ) ) ;
#8039=CYLINDRICAL_SURFACE ( 'NONE', #33885, 5.000000000000004441 ) ;
#8041=CARTESIAN_POINT ( 'NONE',  ( -44.99999999999977973, 149.9999999999999716, 10.00000000000000000 ) ) ;
#8047=MECHANICAL_DESIGN_GEOMETRIC_PRESENTATION_REPRESENTATION('',(#30464),#9174);
#8050=SURFACE_STYLE_USAGE ( .BOTH. , #56583 ) ;
#8051=ORIENTED_EDGE ( 'NONE', *, *, #54693, .T. ) ;
#8061=DIRECTION ( 'NONE',  ( 0.000000000000000000, 0.000000000000000000, 1.000000000000000000 ) ) ;
#8065=AXIS2_PLACEMENT_3D ( 'NONE', #15741, #4814, #47077 ) ;
#8069=CARTESIAN_POINT ( 'NONE',  ( 5.598654528085805993, 118.3549999999999898, 7.705886871421374629 ) ) ;
#8071=MECHANICAL_DESIGN_GEOMETRIC_PRESENTATION_REPRESENTATION('',(#17036),#65306);
#8073=CARTESIAN_POINT ( 'NONE',  ( -2.607480562268949420, 142.2929263765338135, 8.025000000000090949 ) ) ;
#8074=DIRECTION ( 'NONE',  ( 0.000000000000000000, 1.000000000000000000, 0.000000000000000000 ) ) ;
#8075=TOROIDAL_SURFACE ( 'NONE', #40687, 8.499999999999994671, 0.5000000000000000000 ) ;
#8078=MECHANICAL_DESIGN_GEOMETRIC_PRESENTATION_REPRESENTATION('',(#13697),#21538);
#8079=CARTESIAN_POINT ( 'NONE',  ( -75.50000000000000000, 64.49137674618943095, -41.30495168499704306 ) ) ;
#8080=CARTESIAN_POINT ( 'NONE',  ( -14.98999599679679662, 117.9999999999999716, 10.00000000000000000 ) ) ;
#8086=CARTESIAN_POINT ( 'NONE',  ( 45.50000000000000000, 99.99999999999992895, 9.500000000000000000 ) ) ;
#8088=DIRECTION ( 'NONE',  ( 0.000000000000000000, 0.000000000000000000, 1.000000000000000000 ) ) ;
#8094=VECTOR ( 'NONE', #18441, 1000.000000000000000 ) ;
#8096=FACE_OUTER_BOUND ( 'NONE', #15808, .T. ) ;
#8097=CIRCLE ( 'NONE', #4726, 8.000000000000000000 ) ;
#8098=FACE_OUTER_BOUND ( 'NONE', #67364, .T. ) ;
#8101=ORIENTED_EDGE ( 'NONE', *, *, #67820, .F. ) ;
#8102=EDGE_CURVE ( 'NONE', #18929, #13202, #36037, .T. ) ;
#8103=CARTESIAN_POINT ( 'NONE',  ( -44.99999999999977973, 146.9999999999999716, 9.500000000000000000 ) ) ;
#8108=FILL_AREA_STYLE_COLOUR ( '', #34323 ) ;
#8109=VERTEX_POINT ( 'NONE', #4316 ) ;
#8110=AXIS2_PLACEMENT_3D ( 'NONE', #66746, #1949, #39690 ) ;
#8113=CARTESIAN_POINT ( 'NONE',  ( -8.102448949553181734, 139.8950000000000102, -5.886773742842749790 ) ) ;
#8115=EDGE_LOOP ( 'NONE', ( #17394, #24792, #34954, #32266 ) ) ;
#8116=COLOUR_RGB ( '', 0.09019608, 0.27058824, 0.51372549) ;
#8117=CARTESIAN_POINT ( 'NONE',  ( 8.102448949553179958, 136.5049999999999670, 5.886773742842750679 ) ) ;
#8121=SURFACE_SIDE_STYLE ('',( #7435 ) ) ;
#8123=CARTESIAN_POINT ( 'NONE',  ( 2.607480562269076430, 113.7929263765338277, -8.025000000000000355 ) ) ;
#8124=CARTESIAN_POINT ( 'NONE',  ( -34.99999999999992895, 112.9999999999999858, -9.500000000000000000 ) ) ;
#8128=FILL_AREA_STYLE ('',( #1404 ) ) ;
#8130=CIRCLE ( 'NONE', #13693, 0.5000000000000004441 ) ;
#8133=ORIENTED_EDGE ( 'NONE', *, *, #7549, .T. ) ;
#8134=DIRECTION ( 'NONE',  ( 0.000000000000000000, 0.000000000000000000, 1.000000000000000000 ) ) ;
#8138=VECTOR ( 'NONE', #26605, 1000.000000000000000 ) ;
#8139=VERTEX_POINT ( 'NONE', #26146 ) ;
#8142=VECTOR ( 'NONE', #16540, 1000.000000000000000 ) ;
#8143=CARTESIAN_POINT ( 'NONE',  ( -60.00000000000000000, -2.024042244987997205E-14, -9.500000000000000000 ) ) ;
#8148=ORIENTED_EDGE ( 'NONE', *, *, #25372, .F. ) ;
#8152=DIRECTION ( 'NONE',  ( 0.000000000000000000, 0.000000000000000000, 1.000000000000000000 ) ) ;
#8153=AXIS2_PLACEMENT_3D ( 'NONE', #32801, #21552, #33487 ) ;
#8155=ORIENTED_EDGE ( 'NONE', *, *, #15916, .T. ) ;
#8160=ORIENTED_EDGE ( 'NONE', *, *, #29739, .T. ) ;
#8164=CARTESIAN_POINT ( 'NONE',  ( -8.102448949553181734, 137.4950000000000045, 5.886773742842747126 ) ) ;
#8166=VECTOR ( 'NONE', #36516, 1000.000000000000000 ) ;
#8168=UNCERTAINTY_MEASURE_WITH_UNIT (LENGTH_MEASURE( 1.000000000000000082E-05 ), #54097, 'distance_accuracy_value', 'NONE');
#8170=CARTESIAN_POINT ( 'NONE',  ( -9.827790563157511022E-16, 148.4429263765338476, 8.025000000000000355 ) ) ;
#8175=( GEOMETRIC_REPRESENTATION_CONTEXT ( 3 ) GLOBAL_UNCERTAINTY_ASSIGNED_CONTEXT ( ( #53284 ) ) GLOBAL_UNIT_ASSIGNED_CONTEXT ( ( #23336, #44838, #2878 ) ) REPRESENTATION_CONTEXT ( 'NONE', 'WORKASPACE' ) );
#8178=VECTOR ( 'NONE', #20837, 999.9999999999998863 ) ;
#8183=STYLED_ITEM ( 'NONE', ( #16633 ), #35959 ) ;
#8186=SURFACE_STYLE_USAGE ( .BOTH. , #14483 ) ;
#8188=CARTESIAN_POINT ( 'NONE',  ( -4.716976649647097730, 142.3570736234661638, -6.492361379858953896 ) ) ;
#8189=EDGE_LOOP ( 'NONE', ( #16874, #29935, #62768 ) ) ;
#8195=CARTESIAN_POINT ( 'NONE',  ( -20.04013953308945162, 115.4999999999999432, -10.00000000000000000 ) ) ;
#8196=( LENGTH_UNIT ( ) NAMED_UNIT ( * ) SI_UNIT ( .MILLI., .METRE. ) );
#8200=CARTESIAN_POINT ( 'NONE',  ( -4.716976649647098618, 158.2570736234661695, 6.492361379858953008 ) ) ;
#8202=STYLED_ITEM ( 'NONE', ( #30976 ), #26115 ) ;
#8203=ORIENTED_EDGE ( 'NONE', *, *, #38980, .T. ) ;
#8205=CARTESIAN_POINT ( 'NONE',  ( -5.598654528085806881, 110.8549999999999756, -7.705886871421374629 ) ) ;
#8206=EDGE_CURVE ( 'NONE', #24259, #8394, #51137, .T. ) ;
#8208=( NAMED_UNIT ( * ) PLANE_ANGLE_UNIT ( ) SI_UNIT ( $, .RADIAN. ) );
#8209=CARTESIAN_POINT ( 'NONE',  ( 3.094860106618435136, 134.4049999999999443, -9.525000000000000355 ) ) ;
#8210=UNCERTAINTY_MEASURE_WITH_UNIT (LENGTH_MEASURE( 1.000000000000000082E-05 ), #25308, 'distance_accuracy_value', 'NONE');
#8214=CARTESIAN_POINT ( 'NONE',  ( 0.000000000000000000, 115.4999999999999574, 10.50000000000000000 ) ) ;
#8215=EDGE_LOOP ( 'NONE', ( #29141, #57818, #15672, #62002, #29969 ) ) ;
#8223=CARTESIAN_POINT ( 'NONE',  ( -21.02379604162863558, 114.4999999999999574, -10.50000000000000000 ) ) ;
#8224=DIRECTION ( 'NONE',  ( -0.000000000000000000, -1.000000000000000000, -0.000000000000000000 ) ) ;
#8225=EDGE_LOOP ( 'NONE', ( #62327, #58215, #58624 ) ) ;
#8226=DIRECTION ( 'NONE',  ( -0.000000000000000000, 1.000000000000000000, -0.000000000000000000 ) ) ;
#8228=( NAMED_UNIT ( * ) PLANE_ANGLE_UNIT ( ) SI_UNIT ( $, .RADIAN. ) );
#8230=DIRECTION ( 'NONE',  ( -0.000000000000000000, -0.000000000000000000, -1.000000000000000000 ) ) ;
#8233=ADVANCED_FACE ( 'NONE', ( #34769 ), #23203, .F. ) ;
#8235=AXIS2_PLACEMENT_3D ( 'NONE', #23171, #16873, #38347 ) ;
#8236=DIRECTION ( 'NONE',  ( -0.000000000000000000, -1.000000000000000000, -0.000000000000000000 ) ) ;
#8238=MECHANICAL_DESIGN_GEOMETRIC_PRESENTATION_REPRESENTATION('',(#13849),#19463);
#8239=EDGE_CURVE ( 'NONE', #30440, #35956, #69111, .T. ) ;
#8240=DIRECTION ( 'NONE',  ( -0.000000000000000000, -1.000000000000000000, 0.000000000000000000 ) ) ;
#8241=CARTESIAN_POINT ( 'NONE',  ( -8.102448949553179958, 145.8949999999999818, -5.886773742842749790 ) ) ;
#8244=( LENGTH_UNIT ( ) NAMED_UNIT ( * ) SI_UNIT ( .MILLI., .METRE. ) );
#8245=COLOUR_RGB ( '', 0.66274510, 0.83137255, 0.94901961) ;
#8247=SURFACE_SIDE_STYLE ('',( #2182 ) ) ;
#8248=CARTESIAN_POINT ( 'NONE',  ( 6.826472737025121695, 120.6070736234661354, -4.959722759717905660 ) ) ;
#8252=CARTESIAN_POINT ( 'NONE',  ( 5.598654528085809545, 112.1449999999999818, -7.705886871421373741 ) ) ;
#8262=CARTESIAN_POINT ( 'NONE',  ( 0.000000000000000000, 115.4999999999999574, 10.50000000000000000 ) ) ;
#8264=( GEOMETRIC_REPRESENTATION_CONTEXT ( 3 ) GLOBAL_UNCERTAINTY_ASSIGNED_CONTEXT ( ( #52981 ) ) GLOBAL_UNIT_ASSIGNED_CONTEXT ( ( #22403, #1230, #5499 ) ) REPRESENTATION_CONTEXT ( 'NONE', 'WORKASPACE' ) );
#8266=AXIS2_PLACEMENT_3D ( 'NONE', #33878, #45181, #44834 ) ;
#8269=ORIENTED_EDGE ( 'NONE', *, *, #27286, .T. ) ;
#8271=SURFACE_SIDE_STYLE ('',( #14963 ) ) ;
#8275=EDGE_CURVE ( 'NONE', #16942, #53214, #35417, .T. ) ;
#8279=( NAMED_UNIT ( * ) SI_UNIT ( $, .STERADIAN. ) SOLID_ANGLE_UNIT ( ) );
#8280=EDGE_CURVE ( 'NONE', #56786, #50847, #15324, .T. ) ;
#8285=CARTESIAN_POINT ( 'NONE',  ( -2.607480562269115509, 133.2070736234661581, -8.024999999999970157 ) ) ;
#8286=VECTOR ( 'NONE', #61153, 1000.000000000000000 ) ;
#8287=CARTESIAN_POINT ( 'NONE',  ( 6.826472737025121695, 135.6070736234661638, -4.959722759717905660 ) ) ;
#8290=AXIS2_PLACEMENT_3D ( 'NONE', #54785, #17216, #236 ) ;
#8294=MECHANICAL_DESIGN_GEOMETRIC_PRESENTATION_REPRESENTATION('',(#42034),#2604);
#8295=CARTESIAN_POINT ( 'NONE',  ( -15.98999599679679839, 146.4999999999999716, 7.500000000000000000 ) ) ;
#8296=EDGE_CURVE ( 'NONE', #38837, #60182, #537, .T. ) ;
#8300=DIRECTION ( 'NONE',  ( 1.000000000000000000, 0.000000000000000000, 0.000000000000000000 ) ) ;
#8301=STYLED_ITEM ( 'NONE', ( #25657 ), #2910 ) ;
#8310=CARTESIAN_POINT ( 'NONE',  ( 23.21231517720797655, 117.9999999999999716, 9.500000000000000000 ) ) ;
#8313=ORIENTED_EDGE ( 'NONE', *, *, #65772, .T. ) ;
#8314=FACE_OUTER_BOUND ( 'NONE', #52578, .T. ) ;
#8319=AXIS2_PLACEMENT_3D ( 'NONE', #33282, #32939, #505 ) ;
#8322=CARTESIAN_POINT ( 'NONE',  ( 5.598654528085809545, 115.1449999999999818, -7.705886871421373741 ) ) ;
#8324=COLOUR_RGB ( '', 0.40784314, 0.44705882, 0.49803922) ;
#8327=ORIENTED_EDGE ( 'NONE', *, *, #23731, .T. ) ;
#8329=CARTESIAN_POINT ( 'NONE',  ( 60.00000000000000000, 1.797044900979284448E-15, 10.00000000000000000 ) ) ;
#8330=CARTESIAN_POINT ( 'NONE',  ( 68.00000000000000000, 2.776762340297169183E-15, -10.49999999999999822 ) ) ;
#8334=TOROIDAL_SURFACE ( 'NONE', #58891, 14.49999999999999822, 0.5000000000000000000 ) ;
#8337=AXIS2_PLACEMENT_3D ( 'NONE', #36087, #4745, #26200 ) ;
#8338=( NAMED_UNIT ( * ) PLANE_ANGLE_UNIT ( ) SI_UNIT ( $, .RADIAN. ) );
#8344=LINE ( 'NONE', #44961, #34732 ) ;
#8347=CARTESIAN_POINT ( 'NONE',  ( -5.598654528085808657, 147.7549999999999955, 7.705886871421373741 ) ) ;
#8349=EDGE_CURVE ( 'NONE', #31691, #5568, #42260, .T. ) ;
#8357=SURFACE_STYLE_FILL_AREA ( #1624 ) ;
#8359=SURFACE_STYLE_FILL_AREA ( #67423 ) ;
#8360=ADVANCED_FACE ( 'NONE', ( #8747 ), #27543, .T. ) ;
#8361=EDGE_CURVE ( 'NONE', #62857, #4894, #34302, .T. ) ;
#8368=SURFACE_STYLE_USAGE ( .BOTH. , #67792 ) ;
#8369=EDGE_CURVE ( 'NONE', #57600, #60182, #62417, .T. ) ;
#8371=EDGE_CURVE ( 'NONE', #23306, #54975, #24189, .T. ) ;
#8373=EDGE_LOOP ( 'NONE', ( #67523, #10531, #1458, #56323 ) ) ;
#8374=DIRECTION ( 'NONE',  ( -0.000000000000000000, -1.000000000000000000, -0.000000000000000000 ) ) ;
#8375=ADVANCED_FACE ( 'NONE', ( #59011 ), #26959, .F. ) ;
#8378=CARTESIAN_POINT ( 'NONE',  ( -9.058813317711337021, 114.1549999999999869, -2.943386871421374895 ) ) ;
#8383=ORIENTED_EDGE ( 'NONE', *, *, #27452, .T. ) ;
#8384=CARTESIAN_POINT ( 'NONE',  ( -9.190687389602119950, 110.4999999999999858, 2.539151240794934150 ) ) ;
#8387=FILL_AREA_STYLE_COLOUR ( '', #7022 ) ;
#8390=CARTESIAN_POINT ( 'NONE',  ( -2.607480562269075097, 148.2929263765338419, 8.025000000000000355 ) ) ;
#8392=CARTESIAN_POINT ( 'NONE',  ( 48.00000000000000000, 14.49137674618942562, 7.000000000000000000 ) ) ;
#8394=VERTEX_POINT ( 'NONE', #54413 ) ;
#8395=VERTEX_POINT ( 'NONE', #59326 ) ;
#8400=CARTESIAN_POINT ( 'NONE',  ( 23.71231517720798010, 117.4999999999999716, 7.500000000000000000 ) ) ;
#8404=STYLED_ITEM ( 'NONE', ( #40086 ), #7806 ) ;
#8406=SURFACE_STYLE_USAGE ( .BOTH. , #56575 ) ;
#8410=CARTESIAN_POINT ( 'NONE',  ( -19.89974874213240597, 115.4999999999999574, 10.00000000000000000 ) ) ;
#8412=VECTOR ( 'NONE', #5611, 1000.000000000000000 ) ;
#8413=PRESENTATION_STYLE_ASSIGNMENT (( #8050 ) ) ;
#8416=FILL_AREA_STYLE_COLOUR ( '', #11651 ) ;
#8421=COLOUR_RGB ( '', 0.31764706, 0.68627451, 0.89019608) ;
#8432=AXIS2_PLACEMENT_3D ( 'NONE', #7273, #6542, #16218 ) ;
#8435=CARTESIAN_POINT ( 'NONE',  ( -3.094860106618434248, 114.9049999999999727, 9.525000000000000355 ) ) ;
#8437=LINE ( 'NONE', #55568, #10647 ) ;
#8441=STYLED_ITEM ( 'NONE', ( #29278 ), #56464 ) ;
#8448=ADVANCED_FACE ( 'NONE', ( #32976 ), #1237, .T. ) ;
#8457=EDGE_CURVE ( 'NONE', #5084, #41694, #26462, .T. ) ;
#8458=FACE_OUTER_BOUND ( 'NONE', #2778, .T. ) ;
#8462=VERTEX_POINT ( 'NONE', #23794 ) ;
#8469=CARTESIAN_POINT ( 'NONE',  ( 12.72792206135785698, 114.9999999999999574, -10.50000000000000000 ) ) ;
#8470=EDGE_LOOP ( 'NONE', ( #56009, #36635, #19947 ) ) ;
#8471=VECTOR ( 'NONE', #15149, 1000.000000000000114 ) ;
#8474=CARTESIAN_POINT ( 'NONE',  ( -9.058813317711338797, 137.3449999999999989, 2.943386871421373563 ) ) ;
#8476=ORIENTED_EDGE ( 'NONE', *, *, #68395, .T. ) ;
#8477=DIRECTION ( 'NONE',  ( -1.000000000000000000, 1.156482317317866302E-16, 0.000000000000000000 ) ) ;
#8478=CARTESIAN_POINT ( 'NONE',  ( 10.01517768586949408, 136.8049999999999500, 1.839758294383810543E-15 ) ) ;
#8480=CARTESIAN_POINT ( 'NONE',  ( 0.000000000000000000, 115.4999999999999574, 0.000000000000000000 ) ) ;
#8482=CARTESIAN_POINT ( 'NONE',  ( 4.716976649647096842, 112.7429263765338163, 6.492361379858953896 ) ) ;
#8483=SURFACE_STYLE_FILL_AREA ( #40854 ) ;
#8485=( LENGTH_UNIT ( ) NAMED_UNIT ( * ) SI_UNIT ( .MILLI., .METRE. ) );
#8486=DIRECTION ( 'NONE',  ( 1.000000000000000000, 0.000000000000000000, -0.000000000000000000 ) ) ;
#8490=ORIENTED_EDGE ( 'NONE', *, *, #16704, .T. ) ;
#8492=DIRECTION ( 'NONE',  ( 1.000000000000000000, 0.000000000000000000, -0.000000000000000000 ) ) ;
#8496=FILL_AREA_STYLE ('',( #52110 ) ) ;
#8499=STYLED_ITEM ( 'NONE', ( #43174 ), #32251 ) ;
#8501=CARTESIAN_POINT ( 'NONE',  ( 75.00000000000000000, 19.30628705663858113, 6.500000000000000888 ) ) ;
#8503=DIRECTION ( 'NONE',  ( -0.000000000000000000, 1.000000000000000000, -0.000000000000000000 ) ) ;
#8504=ORIENTED_EDGE ( 'NONE', *, *, #32354, .F. ) ;
#8508=( NAMED_UNIT ( * ) SI_UNIT ( $, .STERADIAN. ) SOLID_ANGLE_UNIT ( ) );
#8512=DIRECTION ( 'NONE',  ( -0.000000000000000000, -0.000000000000000000, 1.000000000000000000 ) ) ;
#8517=CARTESIAN_POINT ( 'NONE',  ( 8.102448949553183510, 135.9950000000000045, -5.886773742842746238 ) ) ;
#8524=CARTESIAN_POINT ( 'NONE',  ( 15.48999599679679662, 117.4999999999999716, 10.00000000000000000 ) ) ;
#8528=FILL_AREA_STYLE ('',( #61961 ) ) ;
#8530=( GEOMETRIC_REPRESENTATION_CONTEXT ( 3 ) GLOBAL_UNCERTAINTY_ASSIGNED_CONTEXT ( ( #63659 ) ) GLOBAL_UNIT_ASSIGNED_CONTEXT ( ( #52851, #47617, #15569 ) ) REPRESENTATION_CONTEXT ( 'NONE', 'WORKASPACE' ) );
#8531=SURFACE_SIDE_STYLE ('',( #51783 ) ) ;
#8533=EDGE_CURVE ( 'NONE', #30209, #27227, #55460, .T. ) ;
#8536=CARTESIAN_POINT ( 'NONE',  ( -2.607480562269053781, 128.4070736234661467, 8.025000000000016342 ) ) ;
#8537=ORIENTED_EDGE ( 'NONE', *, *, #47730, .F. ) ;
#8542=DIRECTION ( 'NONE',  ( -1.000000000000000000, 0.000000000000000000, 0.000000000000000000 ) ) ;
#8546=VERTEX_POINT ( 'NONE', #47034 ) ;
#8547=( LENGTH_UNIT ( ) NAMED_UNIT ( * ) SI_UNIT ( .MILLI., .METRE. ) );
#8550=CARTESIAN_POINT ( 'NONE',  ( 8.102448949553181734, 114.3949999999999676, 5.886773742842750679 ) ) ;
#8557=EDGE_LOOP ( 'NONE', ( #24973, #11217, #8707, #48937 ) ) ;
#8558=CARTESIAN_POINT ( 'NONE',  ( 0.000000000000000000, 140.5549999999999784, -9.525000000000000355 ) ) ;
#8559=DIRECTION ( 'NONE',  ( 1.000000000000000000, 0.000000000000000000, 0.000000000000000000 ) ) ;
#8561=AXIS2_PLACEMENT_3D ( 'NONE', #60118, #5949, #32683 ) ;
#8562=FILL_AREA_STYLE_COLOUR ( '', #11819 ) ;
#8563=AXIS2_PLACEMENT_3D ( 'NONE', #26449, #53210, #57432 ) ;
#8564=CIRCLE ( 'NONE', #44554, 0.5000000000000004441 ) ;
#8567=FILL_AREA_STYLE ('',( #45183 ) ) ;
#8571=ADVANCED_FACE ( 'NONE', ( #56858 ), #28703, .F. ) ;
#8583=CARTESIAN_POINT ( 'NONE',  ( -72.50000000000000000, 36.32520566882265456, 10.00000000000000000 ) ) ;
#8584=CARTESIAN_POINT ( 'NONE',  ( 3.094860106618431583, 138.0949999999999989, 9.525000000000000355 ) ) ;
#8585=COLOUR_RGB ( '', 0.66274510, 0.83137255, 0.94901961) ;
#8592=EDGE_CURVE ( 'NONE', #20703, #16182, #586, .T. ) ;
#8594=EDGE_CURVE ( 'NONE', #58540, #62495, #35515, .T. ) ;
#8596=CARTESIAN_POINT ( 'NONE',  ( 3.094860106618431583, 111.0949999999999704, 9.525000000000000355 ) ) ;
#8599=FILL_AREA_STYLE ('',( #56785 ) ) ;
#8600=VERTEX_POINT ( 'NONE', #68449 ) ;
#8602=EDGE_CURVE ( 'NONE', #41301, #14677, #16416, .T. ) ;
#8606=EDGE_CURVE ( 'NONE', #29207, #54497, #20625, .T. ) ;
#8609=CARTESIAN_POINT ( 'NONE',  ( -4.716976649647097730, 124.3570736234661496, -6.492361379858953896 ) ) ;
#8612=CARTESIAN_POINT ( 'NONE',  ( -19.89974874213240597, 115.4999999999999574, 10.00000000000000000 ) ) ;
#8616=( BOUNDED_CURVE ( )  B_SPLINE_CURVE ( 2, ( #39963, #50831, #37821, #57854, #68755, #20546, #41691, #25469, #64140, #69099, #52918 ),
 .UNSPECIFIED., .F., .F. ) 
 B_SPLINE_CURVE_WITH_KNOTS ( ( 3, 2, 2, 2, 2, 3 ),
 ( 0.7941176470588233727, 0.7999999999999999334, 0.8058823529411763831, 0.8117647058823528328, 0.8176470588235292825, 0.8235294117647057321 ),
 .UNSPECIFIED. ) 
 CURVE ( )  GEOMETRIC_REPRESENTATION_ITEM ( )  RATIONAL_B_SPLINE_CURVE ( ( 1.000000000000000888, 0.9510565162951526430, 1.000000000000000000, 0.9510565162951535312, 1.000000000000000000, 0.9510565162951535312, 1.000000000000000000, 0.9510565162951535312, 1.000000000000000000, 0.9510565162951544194, 0.9999999999999991118 ) ) 
 REPRESENTATION_ITEM ( '' )  );
#8619=SURFACE_STYLE_FILL_AREA ( #30376 ) ;
#8627=FILL_AREA_STYLE_COLOUR ( '', #42126 ) ;
#8628=CARTESIAN_POINT ( 'NONE',  ( 8.437984349512095861, 129.3070736234661524, 1.550032578732817026E-15 ) ) ;
#8633=CARTESIAN_POINT ( 'NONE',  ( 74.99999999999998579, 19.62820054891026444, -6.498343828034972347 ) ) ;
#8638=LINE ( 'NONE', #62074, #44013 ) ;
#8640=( NAMED_UNIT ( * ) SI_UNIT ( $, .STERADIAN. ) SOLID_ANGLE_UNIT ( ) );
#8649=PRESENTATION_STYLE_ASSIGNMENT (( #18834 ) ) ;
#8650=( GEOMETRIC_REPRESENTATION_CONTEXT ( 3 ) GLOBAL_UNCERTAINTY_ASSIGNED_CONTEXT ( ( #43932 ) ) GLOBAL_UNIT_ASSIGNED_CONTEXT ( ( #17754, #30261, #45806 ) ) REPRESENTATION_CONTEXT ( 'NONE', 'WORKASPACE' ) );
#8653=DIRECTION ( 'NONE',  ( 0.000000000000000000, 0.000000000000000000, 1.000000000000000000 ) ) ;
#8660=CARTESIAN_POINT ( 'NONE',  ( -9.058813317711338797, 116.3449999999999847, 2.943386871421373563 ) ) ;
#8662=ADVANCED_FACE ( 'NONE', ( #469 ), #59962, .T. ) ;
#8663=FILL_AREA_STYLE_COLOUR ( '', #31794 ) ;
#8673=EDGE_CURVE ( 'NONE', #40899, #41694, #36665, .T. ) ;
#8675=CARTESIAN_POINT ( 'NONE',  ( -75.00000000000000000, 9.372904743120718862, 6.583929160757660881 ) ) ;
#8683=CARTESIAN_POINT ( 'NONE',  ( 2.786071468060228170E-15, 154.9999999999999716, 22.49999999999999645 ) ) ;
#8686=CARTESIAN_POINT ( 'NONE',  ( 8.102448949553183510, 158.1049999999999898, -5.886773742842746238 ) ) ;
#8687=CARTESIAN_POINT ( 'NONE',  ( -60.00000000000000000, -2.024042244987997205E-14, -6.500000000000000000 ) ) ;
#8688=DIRECTION ( 'NONE',  ( 0.000000000000000000, 0.000000000000000000, 1.000000000000000000 ) ) ;
#8689=UNCERTAINTY_MEASURE_WITH_UNIT (LENGTH_MEASURE( 1.000000000000000082E-05 ), #38219, 'distance_accuracy_value', 'NONE');
#8690=CARTESIAN_POINT ( 'NONE',  ( -80.49999999999995737, 50.00000000000000000, -12.00000000000000000 ) ) ;
#8692=CARTESIAN_POINT ( 'NONE',  ( 23.71231517720798010, 117.4999999999999716, -7.000000000000000000 ) ) ;
#8694=COLOUR_RGB ( '', 0.72549020, 0.75294118, 0.79215686) ;
#8695=STYLED_ITEM ( 'NONE', ( #47551 ), #3795 ) ;
#8696=EDGE_CURVE ( 'NONE', #6724, #16463, #43830, .T. ) ;
#8702=EDGE_CURVE ( 'NONE', #7479, #65906, #1708, .T. ) ;
#8703=CARTESIAN_POINT ( 'NONE',  ( 0.000000000000000000, 109.0570736234661524, -8.025000000000000355 ) ) ;
#8704=DIRECTION ( 'NONE',  ( -0.7833176619561783571, -0.6216216216216310375, 0.000000000000000000 ) ) ;
#8705=CIRCLE ( 'NONE', #45837, 0.5000000000000004441 ) ;
#8707=ORIENTED_EDGE ( 'NONE', *, *, #13658, .F. ) ;
#8709=VERTEX_POINT ( 'NONE', #37531 ) ;
#8710=CARTESIAN_POINT ( 'NONE',  ( -3.094860106618432471, 110.7049999999999983, -9.525000000000000355 ) ) ;
#8713=CARTESIAN_POINT ( 'NONE',  ( -15.48999599679679662, 118.4999999999999716, -9.500000000000000000 ) ) ;
#8716=EDGE_LOOP ( 'NONE', ( #36734, #49457, #48984, #32874 ) ) ;
#8718=CARTESIAN_POINT ( 'NONE',  ( -72.49999999999998579, 119.9999999999997868, 9.500000000000000000 ) ) ;
#8719=DIRECTION ( 'NONE',  ( 0.000000000000000000, 0.000000000000000000, 1.000000000000000000 ) ) ;
#8720=VERTEX_POINT ( 'NONE', #17089 ) ;
#8721=CARTESIAN_POINT ( 'NONE',  ( -8.437984349512095861, 141.6929263765338476, -5.166775262442723748E-16 ) ) ;
#8726=EDGE_CURVE ( 'NONE', #8546, #45132, #53644, .T. ) ;
#8729=CARTESIAN_POINT ( 'NONE',  ( 0.000000000000000000, 128.9429263765338192, -8.025000000000000355 ) ) ;
#8730=DIRECTION ( 'NONE',  ( -0.000000000000000000, 1.000000000000000000, -0.000000000000000000 ) ) ;
#8731=CARTESIAN_POINT ( 'NONE',  ( 24.21231517720798010, 113.4999999999999858, 9.500000000000000000 ) ) ;
#8736=AXIS2_PLACEMENT_3D ( 'NONE', #46530, #68992, #4951 ) ;
#8738=LINE ( 'NONE', #40778, #40702 ) ;
#8741=VECTOR ( 'NONE', #27894, 1000.000000000000114 ) ;
#8742=ORIENTED_EDGE ( 'NONE', *, *, #44817, .T. ) ;
#8747=FACE_OUTER_BOUND ( 'NONE', #26161, .T. ) ;
#8748=ORIENTED_EDGE ( 'NONE', *, *, #101, .F. ) ;
#8758=FACE_OUTER_BOUND ( 'NONE', #35653, .T. ) ;
#8759=ADVANCED_FACE ( 'NONE', ( #17436 ), #55380, .T. ) ;
#8760=CARTESIAN_POINT ( 'NONE',  ( 21.02379604162863913, 109.9999999999999858, 9.500000000000000000 ) ) ;
#8761=CARTESIAN_POINT ( 'NONE',  ( -75.00000000000000000, -2.215169945516535778E-14, 10.00000000000000000 ) ) ;
#8763=PLANE ( 'NONE',  #13459 ) ;
#8768=CARTESIAN_POINT ( 'NONE',  ( 5.598654528085805993, 130.3549999999999898, 7.705886871421374629 ) ) ;
#8770=CARTESIAN_POINT ( 'NONE',  ( 20.46171737063437845, 114.7896496367841905, -10.31361660310133388 ) ) ;
#8773=UNCERTAINTY_MEASURE_WITH_UNIT (LENGTH_MEASURE( 1.000000000000000082E-05 ), #41209, 'distance_accuracy_value', 'NONE');
#8774=( NAMED_UNIT ( * ) SI_UNIT ( $, .STERADIAN. ) SOLID_ANGLE_UNIT ( ) );
#8783=ORIENTED_EDGE ( 'NONE', *, *, #53794, .T. ) ;
#8786=TOROIDAL_SURFACE ( 'NONE', #26738, 1.000000000000000000, 0.5000000000000000000 ) ;
#8788=VECTOR ( 'NONE', #34274, 1000.000000000000000 ) ;
#8795=ORIENTED_EDGE ( 'NONE', *, *, #23574, .T. ) ;
#8797=DIRECTION ( 'NONE',  ( 1.000000000000000000, -0.000000000000000000, 0.000000000000000000 ) ) ;
#8798=EDGE_LOOP ( 'NONE', ( #58053, #18258, #28147, #23483 ) ) ;
#8799=AXIS2_PLACEMENT_3D ( 'NONE', #33597, #55036, #1531 ) ;
#8801=CARTESIAN_POINT ( 'NONE',  ( -8.102448949553181734, 137.4950000000000045, 5.886773742842747126 ) ) ;
#8802=ORIENTED_EDGE ( 'NONE', *, *, #15538, .F. ) ;
#8803=CARTESIAN_POINT ( 'NONE',  ( 3.094860106618435136, 140.4050000000000011, -9.525000000000000355 ) ) ;
#8805=( NAMED_UNIT ( * ) SI_UNIT ( $, .STERADIAN. ) SOLID_ANGLE_UNIT ( ) );
#8807=CARTESIAN_POINT ( 'NONE',  ( 2.607480562269076430, 116.7929263765337851, -8.025000000000000355 ) ) ;
#8810=DIRECTION ( 'NONE',  ( 0.000000000000000000, -0.000000000000000000, 1.000000000000000000 ) ) ;
#8811=SURFACE_STYLE_USAGE ( .BOTH. , #24617 ) ;
#8812=ORIENTED_EDGE ( 'NONE', *, *, #18916, .F. ) ;
#8813=EDGE_CURVE ( 'NONE', #40233, #47726, #8847, .T. ) ;
#8816=DIRECTION ( 'NONE',  ( 0.000000000000000000, 0.000000000000000000, 1.000000000000000000 ) ) ;
#8817=CARTESIAN_POINT ( 'NONE',  ( -44.50000000000000000, 10.49999999999998579, 3.000000000000000000 ) ) ;
#8823=UNCERTAINTY_MEASURE_WITH_UNIT (LENGTH_MEASURE( 1.000000000000000082E-05 ), #25529, 'distance_accuracy_value', 'NONE');
#8824=EDGE_CURVE ( 'NONE', #9835, #68674, #13058, .T. ) ;
#8825=EDGE_CURVE ( 'NONE', #36852, #41467, #13353, .T. ) ;
#8826=CARTESIAN_POINT ( 'NONE',  ( -9.827790563157511022E-16, 152.5570736234661524, 8.025000000000000355 ) ) ;
#8827=CARTESIAN_POINT ( 'NONE',  ( 75.00000000000000000, 19.99999999996226663, 6.081205180447340375 ) ) ;
#8829=ORIENTED_EDGE ( 'NONE', *, *, #35683, .F. ) ;
#8830=DIRECTION ( 'NONE',  ( -1.156482317317873451E-16, -1.000000000000000000, 0.000000000000000000 ) ) ;
#8833=AXIS2_PLACEMENT_3D ( 'NONE', #38472, #12027, #33483 ) ;
#8836=EDGE_CURVE ( 'NONE', #35776, #18929, #7452, .T. ) ;
#8837=( LENGTH_UNIT ( ) NAMED_UNIT ( * ) SI_UNIT ( .MILLI., .METRE. ) );
#8839=TOROIDAL_SURFACE ( 'NONE', #33532, 27.49999999999999645, 0.5000000000000000000 ) ;
#8843=AXIS2_PLACEMENT_3D ( 'NONE', #22397, #5491, #64263 ) ;
#8846=CARTESIAN_POINT ( 'NONE',  ( -75.00000000000000000, 9.701644063436951626, -6.099264075924416773 ) ) ;
#8847=LINE ( 'NONE', #7409, #16460 ) ;
#8852=CARTESIAN_POINT ( 'NONE',  ( -8.102448949553181734, 139.8950000000000102, -5.886773742842749790 ) ) ;
#8854=DIRECTION ( 'NONE',  ( 0.000000000000000000, -1.712231188808094676E-15, -1.000000000000000000 ) ) ;
#8856=CARTESIAN_POINT ( 'NONE',  ( -8.437984349512095861, 144.6929263765337623, -5.166775262442723748E-16 ) ) ;
#8859=FILL_AREA_STYLE ('',( #7219 ) ) ;
#8865=CARTESIAN_POINT ( 'NONE',  ( -6.826472737025120807, 127.5070736234661695, -4.959722759717907437 ) ) ;
#8867=DIRECTION ( 'NONE',  ( 1.156482317317873451E-16, 1.000000000000000000, -0.000000000000000000 ) ) ;
#8871=CARTESIAN_POINT ( 'NONE',  ( 44.48136104367662114, 9.999999999999978684, 3.378068172219622856 ) ) ;
#8875=VERTEX_POINT ( 'NONE', #29538 ) ;
#8878=ORIENTED_EDGE ( 'NONE', *, *, #37858, .F. ) ;
#8879=FILL_AREA_STYLE ('',( #40570 ) ) ;
#8881=CARTESIAN_POINT ( 'NONE',  ( 10.01517768586949231, 111.6949999999999932, 1.839758294383810543E-15 ) ) ;
#8884=CARTESIAN_POINT ( 'NONE',  ( 9.058813317711337021, 112.6549999999999869, 2.943386871421375783 ) ) ;
#8887=( BOUNDED_CURVE ( )  B_SPLINE_CURVE ( 2, ( #32948, #38259, #27969, #33968, #65640, #60352, #43884, #516, #55429, #38611, #59296 ),
 .UNSPECIFIED., .F., .F. ) 
 B_SPLINE_CURVE_WITH_KNOTS ( ( 3, 2, 2, 2, 2, 3 ),
 ( 0.7352941176470590978, 0.7411764705882355475, 0.7470588235294121082, 0.7529411764705885579, 0.7588235294117651186, 0.7647058823529415683 ),
 .UNSPECIFIED. ) 
 CURVE ( )  GEOMETRIC_REPRESENTATION_ITEM ( )  RATIONAL_B_SPLINE_CURVE ( ( 0.9999999999999981126, 0.9510565162951554186, 1.000000000000000000, 0.9510565162951535312, 1.000000000000000000, 0.9510565162951535312, 1.000000000000000000, 0.9510565162951535312, 1.000000000000000000, 0.9510565162951498674, 1.000000000000003775 ) ) 
 REPRESENTATION_ITEM ( '' )  );
#8889=CARTESIAN_POINT ( 'NONE',  ( -9.058813317711337021, 138.1550000000000011, -2.943386871421374895 ) ) ;
#8890=UNCERTAINTY_MEASURE_WITH_UNIT (LENGTH_MEASURE( 1.000000000000000082E-05 ), #64027, 'distance_accuracy_value', 'NONE');
#8891=FILL_AREA_STYLE ('',( #20118 ) ) ;
#8894=CARTESIAN_POINT ( 'NONE',  ( 19.89974874213239886, 115.4999999999999574, 10.00000000000000000 ) ) ;
#8896=FACE_OUTER_BOUND ( 'NONE', #54449, .T. ) ;
#8898=ORIENTED_EDGE ( 'NONE', *, *, #12514, .T. ) ;
#8900=DIRECTION ( 'NONE',  ( -1.000000000000000000, 0.000000000000000000, 0.000000000000000000 ) ) ;
#8903=VERTEX_POINT ( 'NONE', #51007 ) ;
#8904=CARTESIAN_POINT ( 'NONE',  ( 3.648904307674076808, 111.0119688737778318, 8.259051035474742619 ) ) ;
#8906=ADVANCED_FACE ( 'NONE', ( #4418 ), #56597, .F. ) ;
#8908=CARTESIAN_POINT ( 'NONE',  ( -45.00000000000000000, 7.768687147774684831, -7.000000000000003553 ) ) ;
#8910=ORIENTED_EDGE ( 'NONE', *, *, #37585, .F. ) ;
#8913=CIRCLE ( 'NONE', #65075, 0.5000000000000004441 ) ;
#8916=DIRECTION ( 'NONE',  ( 0.000000000000000000, 0.000000000000000000, -1.000000000000000000 ) ) ;
#8918=DIRECTION ( 'NONE',  ( 1.000000000000000000, 9.570888143320315888E-16, 0.000000000000000000 ) ) ;
#8920=CARTESIAN_POINT ( 'NONE',  ( 3.094860106618435136, 145.2949999999999875, -9.525000000000000355 ) ) ;
#8924=DIRECTION ( 'NONE',  ( 0.000000000000000000, 0.000000000000000000, 1.000000000000000000 ) ) ;
#8926=CARTESIAN_POINT ( 'NONE',  ( -71.99999999999998579, 63.67479433117734544, -7.500000000000000000 ) ) ;
#8932=FILL_AREA_STYLE_COLOUR ( '', #24650 ) ;
#8933=CARTESIAN_POINT ( 'NONE',  ( -10.01517768586949231, 110.1949999999999648, -6.132527647946036459E-16 ) ) ;
#8940=MECHANICAL_DESIGN_GEOMETRIC_PRESENTATION_REPRESENTATION('',(#11181),#25741);
#8949=CARTESIAN_POINT ( 'NONE',  ( -45.00000000000000000, 9.708372675170618749, -3.611004237778681514 ) ) ;
#8950=AXIS2_PLACEMENT_3D ( 'NONE', #43344, #32359, #47219 ) ;
#8951=DIRECTION ( 'NONE',  ( -1.000000000000000000, 0.000000000000000000, 0.000000000000000000 ) ) ;
#8959=DIRECTION ( 'NONE',  ( -0.000000000000000000, -1.000000000000000000, -0.000000000000000000 ) ) ;
#8962=EDGE_CURVE ( 'NONE', #26613, #36186, #37567, .T. ) ;
#8966=DIRECTION ( 'NONE',  ( 1.000000000000000000, 0.000000000000000000, 0.000000000000000000 ) ) ;
#8970=SPHERICAL_SURFACE ( 'NONE', #6109, 0.5000000000000000000 ) ;
#8971=CARTESIAN_POINT ( 'NONE',  ( -2.607480562269073765, 130.2070736234661581, -8.025000000000000355 ) ) ;
#8972=SURFACE_STYLE_FILL_AREA ( #35710 ) ;
#8973=ORIENTED_EDGE ( 'NONE', *, *, #36353, .F. ) ;
#8976=DIRECTION ( 'NONE',  ( 0.000000000000000000, 1.000000000000000000, 0.000000000000000000 ) ) ;
#8977=EDGE_LOOP ( 'NONE', ( #38173, #64914, #27062, #23867 ) ) ;
#8981=EDGE_CURVE ( 'NONE', #69362, #44405, #31829, .T. ) ;
#8988=AXIS2_PLACEMENT_3D ( 'NONE', #36699, #56723, #8542 ) ;
#8990=EDGE_CURVE ( 'NONE', #19860, #40912, #22900, .T. ) ;
#8992=COLOUR_RGB ( '', 0.40784314, 0.44705882, 0.49803922) ;
#8994=DIRECTION ( 'NONE',  ( 1.000000000000000000, -0.000000000000000000, 0.000000000000000000 ) ) ;
#8995=( NAMED_UNIT ( * ) PLANE_ANGLE_UNIT ( ) SI_UNIT ( $, .RADIAN. ) );
#8998=DIRECTION ( 'NONE',  ( 1.000000000000000000, 0.000000000000000000, 0.000000000000000000 ) ) ;
#8999=DIRECTION ( 'NONE',  ( 1.000000000000000000, 0.000000000000000000, 3.469446951953610639E-15 ) ) ;
#9001=( NAMED_UNIT ( * ) PLANE_ANGLE_UNIT ( ) SI_UNIT ( $, .RADIAN. ) );
#9002=ORIENTED_EDGE ( 'NONE', *, *, #6076, .T. ) ;
#9006=DIRECTION ( 'NONE',  ( 0.000000000000000000, 0.000000000000000000, 1.000000000000000000 ) ) ;
#9008=CARTESIAN_POINT ( 'NONE',  ( 5.598654528085805993, 114.2449999999999903, 7.705886871421374629 ) ) ;
#9012=DIRECTION ( 'NONE',  ( 0.000000000000000000, 1.000000000000000000, 0.000000000000000000 ) ) ;
#9019=CARTESIAN_POINT ( 'NONE',  ( -6.611298881745738321, 111.1103466397262025, -5.993574246798706540 ) ) ;
#9023=ORIENTED_EDGE ( 'NONE', *, *, #52605, .F. ) ;
#9027=AXIS2_PLACEMENT_3D ( 'NONE', #62564, #30905, #46447 ) ;
#9033=CARTESIAN_POINT ( 'NONE',  ( 8.102448949553183510, 161.1049999999999613, -5.886773742842746238 ) ) ;
#9037=( GEOMETRIC_REPRESENTATION_CONTEXT ( 3 ) GLOBAL_UNCERTAINTY_ASSIGNED_CONTEXT ( ( #49654 ) ) GLOBAL_UNIT_ASSIGNED_CONTEXT ( ( #46465, #58034, #10528 ) ) REPRESENTATION_CONTEXT ( 'NONE', 'WORKASPACE' ) );
#9040=EDGE_CURVE ( 'NONE', #68346, #39893, #43187, .T. ) ;
#9042=CARTESIAN_POINT ( 'NONE',  ( -2.879676287999554329, 110.7340786399931005, 8.840802594141578652 ) ) ;
#9048=ORIENTED_EDGE ( 'NONE', *, *, #40198, .T. ) ;
#9058=VERTEX_POINT ( 'NONE', #29358 ) ;
#9059=ORIENTED_EDGE ( 'NONE', *, *, #9603, .T. ) ;
#9060=( NAMED_UNIT ( * ) SI_UNIT ( $, .STERADIAN. ) SOLID_ANGLE_UNIT ( ) );
#9061=SURFACE_STYLE_FILL_AREA ( #56181 ) ;
#9065=CARTESIAN_POINT ( 'NONE',  ( 5.598654528085809545, 119.2549999999999812, -7.705886871421373741 ) ) ;
#9066=CARTESIAN_POINT ( 'NONE',  ( 0.000000000000000000, 149.9999999999999716, 16.00000000000000000 ) ) ;
#9070=DIRECTION ( 'NONE',  ( 1.000000000000000000, 0.000000000000000000, 0.000000000000000000 ) ) ;
#9072=VERTEX_POINT ( 'NONE', #49458 ) ;
#9078=EDGE_LOOP ( 'NONE', ( #33049, #59682, #17408, #7260, #19323, #4634, #8133 ) ) ;
#9079=CARTESIAN_POINT ( 'NONE',  ( 6.826472737025119919, 148.8929263765338078, 4.959722759717908325 ) ) ;
#9082=DIRECTION ( 'NONE',  ( 0.000000000000000000, -2.430666987507993885E-16, 1.000000000000000000 ) ) ;
#9085=PRESENTATION_STYLE_ASSIGNMENT (( #57252 ) ) ;
#9087=FILL_AREA_STYLE_COLOUR ( '', #23747 ) ;
#9088=CARTESIAN_POINT ( 'NONE',  ( -45.90208486430518064, 9.410172310978721200, 3.203880287027108142 ) ) ;
#9095=CARTESIAN_POINT ( 'NONE',  ( -72.00000000000000000, 35.92875272052971525, -7.500000000000000000 ) ) ;
#9097=CARTESIAN_POINT ( 'NONE',  ( -74.61075306680825747, 36.39434226735735223, 9.999999999999996447 ) ) ;
#9098=ORIENTED_EDGE ( 'NONE', *, *, #66262, .F. ) ;
#9101=DIRECTION ( 'NONE',  ( -1.000000000000000000, 0.000000000000000000, 0.000000000000000000 ) ) ;
#9103=LINE ( 'NONE', #40427, #9866 ) ;
#9104=CARTESIAN_POINT ( 'NONE',  ( 7.632228543268608334, 114.4570736234661581, -2.479861379858951942 ) ) ;
#9115=ORIENTED_EDGE ( 'NONE', *, *, #35707, .T. ) ;
#9116=VECTOR ( 'NONE', #31916, 1000.000000000000000 ) ;
#9117=FILL_AREA_STYLE_COLOUR ( '', #56055 ) ;
#9119=DIRECTION ( 'NONE',  ( 0.000000000000000000, 0.000000000000000000, 1.000000000000000000 ) ) ;
#9123=CARTESIAN_POINT ( 'NONE',  ( -9.058813317711337021, 132.1550000000000011, -2.943386871421374895 ) ) ;
#9126=DIRECTION ( 'NONE',  ( 0.000000000000000000, 0.000000000000000000, 1.000000000000000000 ) ) ;
#9130=CIRCLE ( 'NONE', #21469, 1.000000000000000000 ) ;
#9135=FILL_AREA_STYLE_COLOUR ( '', #44883 ) ;
#9140=CARTESIAN_POINT ( 'NONE',  ( -15.98999599679679839, 118.4999999999999716, 7.500000000000000000 ) ) ;
#9141=CARTESIAN_POINT ( 'NONE',  ( 60.00000000000000000, -2.024042244987997205E-14, -7.500000000000000000 ) ) ;
#9145=FILL_AREA_STYLE ('',( #19679 ) ) ;
#9146=CIRCLE ( 'NONE', #24829, 0.5000000000000004441 ) ;
#9150=STYLED_ITEM ( 'NONE', ( #5927 ), #52916 ) ;
#9155=ORIENTED_EDGE ( 'NONE', *, *, #17893, .T. ) ;
#9156=DIRECTION ( 'NONE',  ( 0.000000000000000000, 1.000000000000000000, 0.000000000000000000 ) ) ;
#9159=ORIENTED_EDGE ( 'NONE', *, *, #26, .T. ) ;
#9165=CARTESIAN_POINT ( 'NONE',  ( 8.102448949553181734, 150.3949999999999818, 5.886773742842750679 ) ) ;
#9168=CARTESIAN_POINT ( 'NONE',  ( -3.094860106618432471, 146.7049999999999841, -9.525000000000000355 ) ) ;
#9169=FILL_AREA_STYLE_COLOUR ( '', #27134 ) ;
#9170=VERTEX_POINT ( 'NONE', #51187 ) ;
#9171=CARTESIAN_POINT ( 'NONE',  ( -2.607480562269073765, 114.0929263765338106, -8.025000000000000355 ) ) ;
#9174=( GEOMETRIC_REPRESENTATION_CONTEXT ( 3 ) GLOBAL_UNCERTAINTY_ASSIGNED_CONTEXT ( ( #37054 ) ) GLOBAL_UNIT_ASSIGNED_CONTEXT ( ( #10221, #48930, #36985 ) ) REPRESENTATION_CONTEXT ( 'NONE', 'WORKASPACE' ) );
#9175=CARTESIAN_POINT ( 'NONE',  ( 44.99999999999998579, 119.9999999999999716, 10.00000000000000000 ) ) ;
#9177=CARTESIAN_POINT ( 'NONE',  ( -15.98999599679679839, 118.4999999999999716, 7.000000000000000000 ) ) ;
#9182=DIRECTION ( 'NONE',  ( -0.000000000000000000, -0.000000000000000000, -1.000000000000000000 ) ) ;
#9183=SURFACE_STYLE_FILL_AREA ( #46862 ) ;
#9184=STYLED_ITEM ( 'NONE', ( #42323 ), #60270 ) ;
#9187=AXIS2_PLACEMENT_3D ( 'NONE', #59923, #11739, #54646 ) ;
#9188=CARTESIAN_POINT ( 'NONE',  ( -45.00000000000000000, -2.024041941016019177E-14, -6.999999999999999112 ) ) ;
#9190=CARTESIAN_POINT ( 'NONE',  ( 74.57962914963242440, 19.59826060529047709, 6.436893197989940418 ) ) ;
#9191=DIRECTION ( 'NONE',  ( 0.000000000000000000, -0.000000000000000000, -1.000000000000000000 ) ) ;
#9193=( LENGTH_UNIT ( ) NAMED_UNIT ( * ) SI_UNIT ( .MILLI., .METRE. ) );
#9194=ORIENTED_EDGE ( 'NONE', *, *, #25012, .T. ) ;
#9197=FILL_AREA_STYLE ('',( #3873 ) ) ;
#9200=CARTESIAN_POINT ( 'NONE',  ( -65.00000000000000000, -1.962809905030629631E-14, -12.00000000000000000 ) ) ;
#9206=STYLED_ITEM ( 'NONE', ( #47687 ), #53301 ) ;
#9209=VECTOR ( 'NONE', #58309, 1000.000000000000000 ) ;
#9210=CARTESIAN_POINT ( 'NONE',  ( 9.058813317711338797, 147.8449999999999989, -2.943386871421372675 ) ) ;
#9213=DIRECTION ( 'NONE',  ( -1.000000000000000000, 0.000000000000000000, 0.000000000000000000 ) ) ;
#9216=CARTESIAN_POINT ( 'NONE',  ( -4.716976649647097730, 144.2429263765338305, -6.492361379858953896 ) ) ;
#9219=DIRECTION ( 'NONE',  ( 1.000000000000000000, 1.554312234475218841E-14, 0.000000000000000000 ) ) ;
#9226=SURFACE_STYLE_USAGE ( .BOTH. , #27347 ) ;
#9227=ORIENTED_EDGE ( 'NONE', *, *, #18809, .F. ) ;
#9233=AXIS2_PLACEMENT_3D ( 'NONE', #52345, #4443, #63564 ) ;
#9237=EDGE_CURVE ( 'NONE', #4798, #67711, #30248, .T. ) ;
#9239=DIRECTION ( 'NONE',  ( -0.000000000000000000, -0.000000000000000000, 1.000000000000000000 ) ) ;
#9241=STYLED_ITEM ( 'NONE', ( #65968 ), #22340 ) ;
#9245=AXIS2_PLACEMENT_3D ( 'NONE', #69532, #21335, #42858 ) ;
#9247=DIRECTION ( 'NONE',  ( 0.000000000000000000, 0.000000000000000000, -1.000000000000000000 ) ) ;
#9248=CARTESIAN_POINT ( 'NONE',  ( -3.094860106618434248, 110.7949999999999733, 9.525000000000000355 ) ) ;
#9251=SURFACE_STYLE_USAGE ( .BOTH. , #21161 ) ;
#9252=CARTESIAN_POINT ( 'NONE',  ( 5.598654528085805993, 124.3549999999999898, 7.705886871421374629 ) ) ;
#9255=DIRECTION ( 'NONE',  ( 0.2413793103448194644, 0.9704308468600220117, 0.000000000000000000 ) ) ;
#9257=CARTESIAN_POINT ( 'NONE',  ( 10.01517768586949231, 139.8050000000000068, 1.839758294383810543E-15 ) ) ;
#9258=SPHERICAL_SURFACE ( 'NONE', #25119, 0.5000000000000000000 ) ;
#9260=AXIS2_PLACEMENT_3D ( 'NONE', #43741, #65143, #64806 ) ;
#9261=DIRECTION ( 'NONE',  ( 0.000000000000000000, 0.000000000000000000, 1.000000000000000000 ) ) ;
#9262=AXIS2_PLACEMENT_3D ( 'NONE', #56930, #29842, #3054 ) ;
#9263=PRESENTATION_STYLE_ASSIGNMENT (( #25075 ) ) ;
#9265=( NAMED_UNIT ( * ) SI_UNIT ( $, .STERADIAN. ) SOLID_ANGLE_UNIT ( ) );
#9268=EDGE_LOOP ( 'NONE', ( #63884, #42354, #40070, #23487 ) ) ;
#9269=CARTESIAN_POINT ( 'NONE',  ( 0.5396081309076795618, 110.8751430657346617, 9.149856934265335084 ) ) ;
#9271=FILL_AREA_STYLE_COLOUR ( '', #53511 ) ;
#9272=VERTEX_POINT ( 'NONE', #24767 ) ;
#9275=VERTEX_POINT ( 'NONE', #63118 ) ;
#9280=CARTESIAN_POINT ( 'NONE',  ( 3.094860106618431583, 153.0949999999999989, 9.525000000000000355 ) ) ;
#9285=LINE ( 'NONE', #46957, #64195 ) ;
#9287=CARTESIAN_POINT ( 'NONE',  ( 12.72792206135785698, 115.4999999999999574, -10.50000000000000000 ) ) ;
#9290=( NAMED_UNIT ( * ) PLANE_ANGLE_UNIT ( ) SI_UNIT ( $, .RADIAN. ) );
#9291=CARTESIAN_POINT ( 'NONE',  ( -3.094860106618432471, 115.5949999999999704, -9.525000000000000355 ) ) ;
#9292=VECTOR ( 'NONE', #53530, 1000.000000000000000 ) ;
#9295=COLOUR_RGB ( '', 0.66274510, 0.83137255, 0.94901961) ;
#9296=FILL_AREA_STYLE ('',( #14932 ) ) ;
#9297=FACE_OUTER_BOUND ( 'NONE', #59587, .T. ) ;
#9302=CARTESIAN_POINT ( 'NONE',  ( -71.49999999999998579, 119.9999999999997868, -7.000000000000000000 ) ) ;
#9304=( GEOMETRIC_REPRESENTATION_CONTEXT ( 3 ) GLOBAL_UNCERTAINTY_ASSIGNED_CONTEXT ( ( #8890 ) ) GLOBAL_UNIT_ASSIGNED_CONTEXT ( ( #64027, #27060, #21825 ) ) REPRESENTATION_CONTEXT ( 'NONE', 'WORKASPACE' ) );
#9310=ORIENTED_EDGE ( 'NONE', *, *, #24946, .F. ) ;
#9313=CARTESIAN_POINT ( 'NONE',  ( -72.50000000000000000, 35.92875272052971525, 9.500000000000000000 ) ) ;
#9316=STYLED_ITEM ( 'NONE', ( #40527 ), #25881 ) ;
#9318=CARTESIAN_POINT ( 'NONE',  ( 0.000000000000000000, 87.30187232391182306, 0.000000000000000000 ) ) ;
#9319=MECHANICAL_DESIGN_GEOMETRIC_PRESENTATION_REPRESENTATION('',(#235),#29530);
#9320=FILL_AREA_STYLE ('',( #67019 ) ) ;
#9323=EDGE_CURVE ( 'NONE', #52417, #29181, #13395, .T. ) ;
#9326=AXIS2_PLACEMENT_3D ( 'NONE', #38597, #59993, #60336 ) ;
#9327=CARTESIAN_POINT ( 'NONE',  ( 4.716976649647099507, 135.7570736234661695, -6.492361379858953008 ) ) ;
#9329=EDGE_LOOP ( 'NONE', ( #22080, #40183, #38140 ) ) ;
#9333=CARTESIAN_POINT ( 'NONE',  ( 71.74137931034479720, 63.10081643261027295, -10.00000000000000000 ) ) ;
#9334=ORIENTED_EDGE ( 'NONE', *, *, #3521, .T. ) ;
#9337=SURFACE_STYLE_USAGE ( .BOTH. , #48297 ) ;
#9338=DIRECTION ( 'NONE',  ( 1.000000000000000000, 0.000000000000000000, 0.000000000000000000 ) ) ;
#9341=CIRCLE ( 'NONE', #55412, 1.000000000000000888 ) ;
#9346=UNCERTAINTY_MEASURE_WITH_UNIT (LENGTH_MEASURE( 1.000000000000000082E-05 ), #18697, 'distance_accuracy_value', 'NONE');
#9347=VERTEX_POINT ( 'NONE', #20550 ) ;
#9348=LINE ( 'NONE', #52276, #61669 ) ;
#9350=( GEOMETRIC_REPRESENTATION_CONTEXT ( 3 ) GLOBAL_UNCERTAINTY_ASSIGNED_CONTEXT ( ( #31113 ) ) GLOBAL_UNIT_ASSIGNED_CONTEXT ( ( #40578, #8208, #66594 ) ) REPRESENTATION_CONTEXT ( 'NONE', 'WORKASPACE' ) );
#9351=COLOUR_RGB ( '', 0.66274510, 0.83137255, 0.94901961) ;
#9352=SURFACE_STYLE_USAGE ( .BOTH. , #57526 ) ;
#9353=( NAMED_UNIT ( * ) SI_UNIT ( $, .STERADIAN. ) SOLID_ANGLE_UNIT ( ) );
#9355=COLOUR_RGB ( '', 0.72549020, 0.75294118, 0.79215686) ;
#9358=FILL_AREA_STYLE ('',( #52283 ) ) ;
#9362=UNCERTAINTY_MEASURE_WITH_UNIT (LENGTH_MEASURE( 1.000000000000000082E-05 ), #24393, 'distance_accuracy_value', 'NONE');
#9363=CARTESIAN_POINT ( 'NONE',  ( 9.058813317711338797, 126.8449999999999847, -2.943386871421372675 ) ) ;
#9370=DIRECTION ( 'NONE',  ( -0.000000000000000000, 1.000000000000000000, -0.000000000000000000 ) ) ;
#9371=DIRECTION ( 'NONE',  ( -0.000000000000000000, -0.000000000000000000, -1.000000000000000000 ) ) ;
#9372=CARTESIAN_POINT ( 'NONE',  ( 2.816687638038912352E-15, 154.9999999999999716, 23.00000000000000000 ) ) ;
#9373=CARTESIAN_POINT ( 'NONE',  ( 60.00000000000000000, 1.797044900979284448E-15, 6.999999999999988454 ) ) ;
#9375=CARTESIAN_POINT ( 'NONE',  ( -75.00000000000000000, 9.519990751839809917, 6.451194676399506278 ) ) ;
#9376=CARTESIAN_POINT ( 'NONE',  ( -8.255262359011400264, 111.6843284473704472, 1.256501419248624352 ) ) ;
#9379=VECTOR ( 'NONE', #8810, 1000.000000000000000 ) ;
#9393=EDGE_CURVE ( 'NONE', #61842, #3021, #40378, .T. ) ;
#9394=CARTESIAN_POINT ( 'NONE',  ( 9.058813317711337021, 160.6550000000000011, 2.943386871421375783 ) ) ;
#9395=( LENGTH_UNIT ( ) NAMED_UNIT ( * ) SI_UNIT ( .MILLI., .METRE. ) );
#9400=( NAMED_UNIT ( * ) PLANE_ANGLE_UNIT ( ) SI_UNIT ( $, .RADIAN. ) );
#9408=FILL_AREA_STYLE ('',( #41425 ) ) ;
#9410=ORIENTED_EDGE ( 'NONE', *, *, #18695, .F. ) ;
#9413=CARTESIAN_POINT ( 'NONE',  ( -20.68718488045382742, 114.6829008731431543, 10.00000000000011724 ) ) ;
#9417=VERTEX_POINT ( 'NONE', #43461 ) ;
#9422=CARTESIAN_POINT ( 'NONE',  ( -5.598654528085808657, 117.7549999999999812, 7.705886871421373741 ) ) ;
#9425=( NAMED_UNIT ( * ) SI_UNIT ( $, .STERADIAN. ) SOLID_ANGLE_UNIT ( ) );
#9428=CARTESIAN_POINT ( 'NONE',  ( 74.99999999999998579, 50.00000000000000000, 7.500000000000000000 ) ) ;
#9431=CARTESIAN_POINT ( 'NONE',  ( 8.437984349512095861, 155.1929263765338192, 1.550032578732817026E-15 ) ) ;
#9433=EDGE_LOOP ( 'NONE', ( #18884, #22184, #45088, #43483 ) ) ;
#9434=CARTESIAN_POINT ( 'NONE',  ( 19.89974874213240241, 114.9999999999999574, -10.49999999999999822 ) ) ;
#9435=ORIENTED_EDGE ( 'NONE', *, *, #68041, .T. ) ;
#9436=SURFACE_SIDE_STYLE ('',( #14712 ) ) ;
#9437=DIRECTION ( 'NONE',  ( 0.000000000000000000, 0.000000000000000000, 1.000000000000000000 ) ) ;
#9439=( GEOMETRIC_REPRESENTATION_CONTEXT ( 3 ) GLOBAL_UNCERTAINTY_ASSIGNED_CONTEXT ( ( #44071 ) ) GLOBAL_UNIT_ASSIGNED_CONTEXT ( ( #62098, #29395, #13562 ) ) REPRESENTATION_CONTEXT ( 'NONE', 'WORKASPACE' ) );
#9441=CARTESIAN_POINT ( 'NONE',  ( -71.99999999999998579, 64.07124727947029896, -10.00000000000000000 ) ) ;
#9442=DIRECTION ( 'NONE',  ( 0.000000000000000000, 0.000000000000000000, -1.000000000000000000 ) ) ;
#9445=SURFACE_SIDE_STYLE ('',( #25585 ) ) ;
#9446=AXIS2_PLACEMENT_3D ( 'NONE', #10250, #57388, #30990 ) ;
#9450=ORIENTED_EDGE ( 'NONE', *, *, #44371, .T. ) ;
#9451=DIRECTION ( 'NONE',  ( -0.000000000000000000, -0.000000000000000000, -1.000000000000000000 ) ) ;
#9452=AXIS2_PLACEMENT_3D ( 'NONE', #59388, #53457, #5935 ) ;
#9453=CARTESIAN_POINT ( 'NONE',  ( 74.65811388300841145, 19.88603796100278487, 6.292893218813452094 ) ) ;
#9457=LINE ( 'NONE', #43239, #50976 ) ;
#9460=( GEOMETRIC_REPRESENTATION_CONTEXT ( 3 ) GLOBAL_UNCERTAINTY_ASSIGNED_CONTEXT ( ( #52274 ) ) GLOBAL_UNIT_ASSIGNED_CONTEXT ( ( #4181, #14791, #9524 ) ) REPRESENTATION_CONTEXT ( 'NONE', 'WORKASPACE' ) );
#9465=VECTOR ( 'NONE', #41722, 1000.000000000000000 ) ;
#9467=( LENGTH_UNIT ( ) NAMED_UNIT ( * ) SI_UNIT ( .MILLI., .METRE. ) );
#9472=FILL_AREA_STYLE ('',( #14746 ) ) ;
#9477=CARTESIAN_POINT ( 'NONE',  ( -3.094860106618434248, 129.9050000000000011, 9.525000000000000355 ) ) ;
#9479=CARTESIAN_POINT ( 'NONE',  ( 19.89974874213239886, 114.9999999999999574, -10.49999999999999645 ) ) ;
#9484=UNCERTAINTY_MEASURE_WITH_UNIT (LENGTH_MEASURE( 1.000000000000000082E-05 ), #29945, 'distance_accuracy_value', 'NONE');
#9485=SURFACE_SIDE_STYLE ('',( #3434 ) ) ;
#9491=EDGE_CURVE ( 'NONE', #29106, #65770, #1095, .T. ) ;
#9496=SURFACE_STYLE_FILL_AREA ( #19321 ) ;
#9498=EDGE_LOOP ( 'NONE', ( #45602, #26466, #13212, #57136 ) ) ;
#9499=SURFACE_STYLE_USAGE ( .BOTH. , #58701 ) ;
#9500=AXIS2_PLACEMENT_3D ( 'NONE', #49289, #28126, #999 ) ;
#9501=( GEOMETRIC_REPRESENTATION_CONTEXT ( 3 ) GLOBAL_UNCERTAINTY_ASSIGNED_CONTEXT ( ( #65069 ) ) GLOBAL_UNIT_ASSIGNED_CONTEXT ( ( #67715, #52593, #3286 ) ) REPRESENTATION_CONTEXT ( 'NONE', 'WORKASPACE' ) );
#9502=UNCERTAINTY_MEASURE_WITH_UNIT (LENGTH_MEASURE( 1.000000000000000082E-05 ), #1539, 'distance_accuracy_value', 'NONE');
#9505=CARTESIAN_POINT ( 'NONE',  ( 23.21231517720797655, 117.4999999999999716, -7.500000000000000000 ) ) ;
#9513=VERTEX_POINT ( 'NONE', #17386 ) ;
#9514=CARTESIAN_POINT ( 'NONE',  ( 44.99999999999977973, 146.4999999999999716, 7.000000000000000000 ) ) ;
#9519=CARTESIAN_POINT ( 'NONE',  ( -9.058813317711337021, 149.0449999999999875, -2.943386871421374895 ) ) ;
#9520=SURFACE_STYLE_USAGE ( .BOTH. , #16536 ) ;
#9523=AXIS2_PLACEMENT_3D ( 'NONE', #63240, #36192, #9793 ) ;
#9524=( NAMED_UNIT ( * ) SI_UNIT ( $, .STERADIAN. ) SOLID_ANGLE_UNIT ( ) );
#9525=CARTESIAN_POINT ( 'NONE',  ( -3.094860106618434248, 147.9049999999999443, 9.525000000000000355 ) ) ;
#9527=CARTESIAN_POINT ( 'NONE',  ( -6.826472737025120807, 123.3929263765337936, -4.959722759717907437 ) ) ;
#9528=DIRECTION ( 'NONE',  ( 1.000000000000000000, 0.000000000000000000, 0.000000000000000000 ) ) ;
#9529=UNCERTAINTY_MEASURE_WITH_UNIT (LENGTH_MEASURE( 1.000000000000000082E-05 ), #15602, 'distance_accuracy_value', 'NONE');
#9530=SURFACE_SIDE_STYLE ('',( #31283 ) ) ;
#9531=CIRCLE ( 'NONE', #39873, 1.000000000000000888 ) ;
#9534=EDGE_LOOP ( 'NONE', ( #49471, #54439, #1183, #43572 ) ) ;
#9535=CARTESIAN_POINT ( 'NONE',  ( 41.03386404901051776, 107.6974965691264856, 3.186685921634084817 ) ) ;
#9536=VERTEX_POINT ( 'NONE', #23320 ) ;
#9538=( GEOMETRIC_REPRESENTATION_CONTEXT ( 3 ) GLOBAL_UNCERTAINTY_ASSIGNED_CONTEXT ( ( #25530 ) ) GLOBAL_UNIT_ASSIGNED_CONTEXT ( ( #48368, #33531, #28214 ) ) REPRESENTATION_CONTEXT ( 'NONE', 'WORKASPACE' ) );
#9544=SURFACE_STYLE_USAGE ( .BOTH. , #41917 ) ;
#9545=UNCERTAINTY_MEASURE_WITH_UNIT (LENGTH_MEASURE( 1.000000000000000082E-05 ), #47755, 'distance_accuracy_value', 'NONE');
#9547=CARTESIAN_POINT ( 'NONE',  ( -7.632228543268608334, 151.9570736234661581, 2.479861379858952830 ) ) ;
#9549=CARTESIAN_POINT ( 'NONE',  ( 7.632228543268608334, 146.3429263765338249, -2.479861379858951942 ) ) ;
#9551=( GEOMETRIC_REPRESENTATION_CONTEXT ( 3 ) GLOBAL_UNCERTAINTY_ASSIGNED_CONTEXT ( ( #2956 ) ) GLOBAL_UNIT_ASSIGNED_CONTEXT ( ( #69313, #37692, #48228 ) ) REPRESENTATION_CONTEXT ( 'NONE', 'WORKASPACE' ) );
#9555=EDGE_LOOP ( 'NONE', ( #319, #51133, #25862, #12313 ) ) ;
#9562=ORIENTED_EDGE ( 'NONE', *, *, #11594, .F. ) ;
#9564=LINE ( 'NONE', #61580, #3138 ) ;
#9566=DIRECTION ( 'NONE',  ( 0.000000000000000000, 0.000000000000000000, 1.000000000000000000 ) ) ;
#9569=ADVANCED_FACE ( 'NONE', ( #28576 ), #4384, .T. ) ;
#9570=CARTESIAN_POINT ( 'NONE',  ( -8.102448949553181734, 148.8950000000000102, -5.886773742842749790 ) ) ;
#9579=CARTESIAN_POINT ( 'NONE',  ( 34.99999999999999289, 99.99999999999998579, -10.00000000000000000 ) ) ;
#9581=PRESENTATION_STYLE_ASSIGNMENT (( #56085 ) ) ;
#9582=ADVANCED_FACE ( 'NONE', ( #2128 ), #47038, .F. ) ;
#9585=( GEOMETRIC_REPRESENTATION_CONTEXT ( 3 ) GLOBAL_UNCERTAINTY_ASSIGNED_CONTEXT ( ( #54347 ) ) GLOBAL_UNIT_ASSIGNED_CONTEXT ( ( #13982, #41096, #29809 ) ) REPRESENTATION_CONTEXT ( 'NONE', 'WORKASPACE' ) );
#9590=DIRECTION ( 'NONE',  ( 0.000000000000000000, 1.000000000000000000, 0.000000000000000000 ) ) ;
#9592=CARTESIAN_POINT ( 'NONE',  ( -51.50000000000000000, -2.024042244987997205E-14, -10.49999999999999822 ) ) ;
#9593=CARTESIAN_POINT ( 'NONE',  ( -45.00000000000000000, 9.581381838473474133, 6.370847823861928383 ) ) ;
#9596=ORIENTED_EDGE ( 'NONE', *, *, #64102, .F. ) ;
#9599=ORIENTED_EDGE ( 'NONE', *, *, #21765, .F. ) ;
#9601=FILL_AREA_STYLE_COLOUR ( '', #67987 ) ;
#9602=ORIENTED_EDGE ( 'NONE', *, *, #68459, .F. ) ;
#9603=EDGE_CURVE ( 'NONE', #42377, #39893, #22987, .T. ) ;
#9605=CARTESIAN_POINT ( 'NONE',  ( 0.000000000000000000, 118.4449999999999932, -9.525000000000000355 ) ) ;
#9606=ORIENTED_EDGE ( 'NONE', *, *, #16783, .F. ) ;
#9608=CARTESIAN_POINT ( 'NONE',  ( -9.058813317711337021, 123.1549999999999869, -2.943386871421374895 ) ) ;
#9612=CARTESIAN_POINT ( 'NONE',  ( 8.102448949553183510, 140.1049999999999898, -5.886773742842746238 ) ) ;
#9613=UNCERTAINTY_MEASURE_WITH_UNIT (LENGTH_MEASURE( 1.000000000000000082E-05 ), #60216, 'distance_accuracy_value', 'NONE');
#9616=( NAMED_UNIT ( * ) PLANE_ANGLE_UNIT ( ) SI_UNIT ( $, .RADIAN. ) );
#9617=( LENGTH_UNIT ( ) NAMED_UNIT ( * ) SI_UNIT ( .MILLI., .METRE. ) );
#9618=ORIENTED_EDGE ( 'NONE', *, *, #42500, .F. ) ;
#9620=CARTESIAN_POINT ( 'NONE',  ( 23.71231517720798010, 117.9999999999999716, -7.000000000000000000 ) ) ;
#9624=CARTESIAN_POINT ( 'NONE',  ( 7.239872073591122614, 111.2187526276816669, 5.042250455018136179 ) ) ;
#9629=VERTEX_POINT ( 'NONE', #34912 ) ;
#9636=( LENGTH_UNIT ( ) NAMED_UNIT ( * ) SI_UNIT ( .MILLI., .METRE. ) );
#9640=SURFACE_SIDE_STYLE ('',( #25441 ) ) ;
#9648=CIRCLE ( 'NONE', #18621, 7.500000000000000000 ) ;
#9652=CARTESIAN_POINT ( 'NONE',  ( -5.598654528085808657, 119.6449999999999818, 7.705886871421373741 ) ) ;
#9654=CIRCLE ( 'NONE', #41312, 13.00000000000000178 ) ;
#9659=DIRECTION ( 'NONE',  ( 0.000000000000000000, 1.000000000000000000, 0.000000000000000000 ) ) ;
#9663=DIRECTION ( 'NONE',  ( 0.7833176619561879050, -0.6216216216216192691, 0.000000000000000000 ) ) ;
#9666=EDGE_CURVE ( 'NONE', #12229, #53118, #56012, .T. ) ;
#9667=CARTESIAN_POINT ( 'NONE',  ( -4.716976649647098618, 125.2570736234661695, 6.492361379858953008 ) ) ;
#9668=CARTESIAN_POINT ( 'NONE',  ( -20.06812647026248086, 114.9888238951376991, -10.44321692355803144 ) ) ;
#9675=AXIS2_PLACEMENT_3D ( 'NONE', #47382, #36108, #57545 ) ;
#9677=DIRECTION ( 'NONE',  ( 0.000000000000000000, 0.000000000000000000, 1.000000000000000000 ) ) ;
#9680=ORIENTED_EDGE ( 'NONE', *, *, #7315, .T. ) ;
#9682=FACE_OUTER_BOUND ( 'NONE', #28906, .T. ) ;
#9687=AXIS2_PLACEMENT_3D ( 'NONE', #18530, #6922, #17835 ) ;
#9688=DIRECTION ( 'NONE',  ( 0.000000000000000000, 1.000000000000000000, 0.000000000000000000 ) ) ;
#9689=CARTESIAN_POINT ( 'NONE',  ( 8.437984349512095861, 144.3070736234661240, 1.550032578732817026E-15 ) ) ;
#9697=CARTESIAN_POINT ( 'NONE',  ( 0.000000000000000000, 143.9429263765338192, -8.025000000000000355 ) ) ;
#9699=MECHANICAL_DESIGN_GEOMETRIC_PRESENTATION_REPRESENTATION('',(#55720),#42160);
#9700=ORIENTED_EDGE ( 'NONE', *, *, #52765, .T. ) ;
#9703=FACE_BOUND ( 'NONE', #53458, .T. ) ;
#9705=ORIENTED_EDGE ( 'NONE', *, *, #23823, .F. ) ;
#9707=FILL_AREA_STYLE ('',( #31464 ) ) ;
#9708=SURFACE_SIDE_STYLE ('',( #63498 ) ) ;
#9709=SURFACE_STYLE_FILL_AREA ( #57527 ) ;
#9712=ADVANCED_FACE ( 'NONE', ( #19425 ), #8839, .T. ) ;
#9714=CARTESIAN_POINT ( 'NONE',  ( 72.00000000000000000, 36.32520566882265456, 7.000000000000000000 ) ) ;
#9716=SURFACE_STYLE_USAGE ( .BOTH. , #68802 ) ;
#9718=CARTESIAN_POINT ( 'NONE',  ( -5.598654528085806881, 121.7449999999999903, -7.705886871421374629 ) ) ;
#9719=ADVANCED_FACE ( 'NONE', ( #41270 ), #35968, .T. ) ;
#9723=PRESENTATION_STYLE_ASSIGNMENT (( #42113 ) ) ;
#9726=ORIENTED_EDGE ( 'NONE', *, *, #55771, .T. ) ;
#9727=FILL_AREA_STYLE ('',( #20954 ) ) ;
#9728=EDGE_CURVE ( 'NONE', #24181, #39125, #53706, .T. ) ;
#9729=CARTESIAN_POINT ( 'NONE',  ( 44.36184162591896296, 10.11502268137275351, 3.500000000000000000 ) ) ;
#9731=CONICAL_SURFACE ( 'NONE', #23162, 4.999999999999997335, 0.7853981633974587151 ) ;
#9734=PRESENTATION_STYLE_ASSIGNMENT (( #35049 ) ) ;
#9736=DIRECTION ( 'NONE',  ( 0.000000000000000000, 0.000000000000000000, 1.000000000000000000 ) ) ;
#9738=ADVANCED_FACE ( 'NONE', ( #53525 ), #57122, .T. ) ;
#9739=AXIS2_PLACEMENT_3D ( 'NONE', #18992, #50014, #39470 ) ;
#9743=DIRECTION ( 'NONE',  ( -0.000000000000000000, -0.000000000000000000, -1.000000000000000000 ) ) ;
#9746=CARTESIAN_POINT ( 'NONE',  ( -1.166476076187854022E-15, 154.0550000000000068, 9.525000000000000355 ) ) ;
#9749=SURFACE_STYLE_USAGE ( .BOTH. , #57930 ) ;
#9751=SPHERICAL_SURFACE ( 'NONE', #30404, 0.5000000000000000000 ) ;
#9754=DIRECTION ( 'NONE',  ( 0.9704308468600219006, -0.2413793103448194921, 0.000000000000000000 ) ) ;
#9763=SURFACE_STYLE_FILL_AREA ( #31172 ) ;
#9766=STYLED_ITEM ( 'NONE', ( #26865 ), #65246 ) ;
#9767=CARTESIAN_POINT ( 'NONE',  ( -72.00000000000000000, 14.49137674618942562, -7.500000000000000000 ) ) ;
#9770=CARTESIAN_POINT ( 'NONE',  ( 8.102448949553181734, 115.5049999999999812, 5.886773742842750679 ) ) ;
#9773=CARTESIAN_POINT ( 'NONE',  ( 34.99999999999992895, 113.4999999999999858, -7.500000000000000000 ) ) ;
#9774=FILL_AREA_STYLE_COLOUR ( '', #53175 ) ;
#9778=PRESENTATION_STYLE_ASSIGNMENT (( #36545 ) ) ;
#9779=ORIENTED_EDGE ( 'NONE', *, *, #5425, .T. ) ;
#9780=CARTESIAN_POINT ( 'NONE',  ( -2.607480562269073765, 153.0929263765338249, -8.025000000000000355 ) ) ;
#9784=DIRECTION ( 'NONE',  ( 0.000000000000000000, 0.000000000000000000, 1.000000000000000000 ) ) ;
#9786=ORIENTED_EDGE ( 'NONE', *, *, #69206, .F. ) ;
#9787=CARTESIAN_POINT ( 'NONE',  ( 20.56511377093078252, 115.3174848394179435, -10.00000000000000000 ) ) ;
#9789=CARTESIAN_POINT ( 'NONE',  ( 20.56323889998346388, 115.3189275942976337, 10.00000000000000000 ) ) ;
#9791=( LENGTH_UNIT ( ) NAMED_UNIT ( * ) SI_UNIT ( .MILLI., .METRE. ) );
#9792=DIRECTION ( 'NONE',  ( 0.000000000000000000, 0.000000000000000000, -1.000000000000000000 ) ) ;
#9793=DIRECTION ( 'NONE',  ( 0.000000000000000000, 0.000000000000000000, 1.000000000000000000 ) ) ;
#9802=CARTESIAN_POINT ( 'NONE',  ( -60.00000000000000000, -2.024042244987997205E-14, -12.00000000000000000 ) ) ;
#9805=CARTESIAN_POINT ( 'NONE',  ( 6.826472737025119919, 114.0070736234661553, 4.959722759717908325 ) ) ;
#9807=PLANE ( 'NONE',  #49516 ) ;
#9814=ORIENTED_EDGE ( 'NONE', *, *, #48419, .F. ) ;
#9821=SURFACE_STYLE_USAGE ( .BOTH. , #13328 ) ;
#9823=CARTESIAN_POINT ( 'NONE',  ( 9.058813317711337021, 130.6550000000000011, 2.943386871421375783 ) ) ;
#9833=PRESENTATION_STYLE_ASSIGNMENT (( #21062 ) ) ;
#9835=VERTEX_POINT ( 'NONE', #26429 ) ;
#9837=CARTESIAN_POINT ( 'NONE',  ( -45.91547277936962956, 9.430195807687216103, -6.000000000000000000 ) ) ;
#9838=CARTESIAN_POINT ( 'NONE',  ( -15.98999599679679839, 117.4999999999999716, 10.00000000000000000 ) ) ;
#9840=CARTESIAN_POINT ( 'NONE',  ( -2.607480562268991608, 148.2929263765338703, 8.025000000000060751 ) ) ;
#9841=CARTESIAN_POINT ( 'NONE',  ( -74.99999999999998579, 146.4999999999999716, 7.500000000000000000 ) ) ;
#9842=FACE_OUTER_BOUND ( 'NONE', #14780, .T. ) ;
#9847=DIRECTION ( 'NONE',  ( 0.000000000000000000, 0.7071067811865517916, 0.7071067811865431318 ) ) ;
#9848=CARTESIAN_POINT ( 'NONE',  ( 21.02379604162863913, 114.4999999999999574, -10.00000000000000000 ) ) ;
#9849=ORIENTED_EDGE ( 'NONE', *, *, #65370, .T. ) ;
#9853=CARTESIAN_POINT ( 'NONE',  ( -5.598654528085806881, 148.7449999999999761, -7.705886871421374629 ) ) ;
#9854=( NAMED_UNIT ( * ) PLANE_ANGLE_UNIT ( ) SI_UNIT ( $, .RADIAN. ) );
#9856=EDGE_CURVE ( 'NONE', #41276, #28244, #38072, .T. ) ;
#9858=CARTESIAN_POINT ( 'NONE',  ( -1.166476076187854022E-15, 151.0550000000000068, 9.525000000000000355 ) ) ;
#9860=ORIENTED_EDGE ( 'NONE', *, *, #17277, .T. ) ;
#9861=CARTESIAN_POINT ( 'NONE',  ( 4.716976649647096842, 124.7429263765338163, 6.492361379858953896 ) ) ;
#9864=AXIS2_PLACEMENT_3D ( 'NONE', #69212, #42184, #25923 ) ;
#9866=VECTOR ( 'NONE', #13309, 1000.000000000000000 ) ;
#9867=EDGE_CURVE ( 'NONE', #9629, #45776, #42562, .T. ) ;
#9868=( LENGTH_UNIT ( ) NAMED_UNIT ( * ) SI_UNIT ( .MILLI., .METRE. ) );
#9869=FILL_AREA_STYLE_COLOUR ( '', #17534 ) ;
#9870=EDGE_CURVE ( 'NONE', #17642, #61023, #32752, .T. ) ;
#9872=CYLINDRICAL_SURFACE ( 'NONE', #7121, 8.025000000000000355 ) ;
#9873=ORIENTED_EDGE ( 'NONE', *, *, #37497, .T. ) ;
#9875=SURFACE_STYLE_FILL_AREA ( #57005 ) ;
#9876=CARTESIAN_POINT ( 'NONE',  ( 23.21231517720797655, 117.9999999999999716, -7.500000000000000000 ) ) ;
#9880=CARTESIAN_POINT ( 'NONE',  ( -74.99999999999998579, 50.00000000000000000, -6.500000000000000000 ) ) ;
#9885=SURFACE_STYLE_USAGE ( .BOTH. , #31301 ) ;
#9886=ORIENTED_EDGE ( 'NONE', *, *, #16377, .F. ) ;
#9889=EDGE_CURVE ( 'NONE', #42152, #6348, #34191, .T. ) ;
#9895=DIRECTION ( 'NONE',  ( 1.000000000000000000, 0.000000000000000000, 0.000000000000000000 ) ) ;
#9897=EDGE_CURVE ( 'NONE', #44738, #31646, #38435, .T. ) ;
#9898=CARTESIAN_POINT ( 'NONE',  ( 71.49999999999998579, 119.9999999999997868, -7.500000000000000000 ) ) ;
#9902=EDGE_CURVE ( 'NONE', #34864, #34213, #36934, .T. ) ;
#9906=CARTESIAN_POINT ( 'NONE',  ( -5.598654528085806881, 145.7449999999999761, -7.705886871421374629 ) ) ;
#9910=( NAMED_UNIT ( * ) SI_UNIT ( $, .STERADIAN. ) SOLID_ANGLE_UNIT ( ) );
#9916=CARTESIAN_POINT ( 'NONE',  ( 71.49999999999998579, 64.07124727947029896, 9.500000000000000000 ) ) ;
#9918=SURFACE_STYLE_FILL_AREA ( #58107 ) ;
#9922=MECHANICAL_DESIGN_GEOMETRIC_PRESENTATION_REPRESENTATION('',(#18865),#7631);
#9923=ORIENTED_EDGE ( 'NONE', *, *, #68041, .F. ) ;
#9927=STYLED_ITEM ( 'NONE', ( #20170 ), #67540 ) ;
#9935=CARTESIAN_POINT ( 'NONE',  ( 8.102448949553183510, 120.9949999999999761, -5.886773742842746238 ) ) ;
#9936=PLANE ( 'NONE',  #1330 ) ;
#9939=CARTESIAN_POINT ( 'NONE',  ( 5.598654528085809545, 116.2549999999999812, -7.705886871421373741 ) ) ;
#9943=CARTESIAN_POINT ( 'NONE',  ( -8.102448949553181734, 144.6049999999999613, 5.886773742842747126 ) ) ;
#9946=EDGE_CURVE ( 'NONE', #69681, #23161, #856, .T. ) ;
#9947=CARTESIAN_POINT ( 'NONE',  ( 20.71462257909523075, 114.5925267038606563, 10.00000000000000000 ) ) ;
#9948=( NAMED_UNIT ( * ) SI_UNIT ( $, .STERADIAN. ) SOLID_ANGLE_UNIT ( ) );
#9949=SURFACE_STYLE_USAGE ( .BOTH. , #21530 ) ;
#9957=CARTESIAN_POINT ( 'NONE',  ( -2.451748578458123784E-13, 110.8535625161535592, 9.171437483846442973 ) ) ;
#9958=STYLED_ITEM ( 'NONE', ( #10473 ), #4196 ) ;
#9961=ORIENTED_EDGE ( 'NONE', *, *, #8813, .F. ) ;
#9963=ORIENTED_EDGE ( 'NONE', *, *, #30898, .T. ) ;
#9967=( NAMED_UNIT ( * ) SI_UNIT ( $, .STERADIAN. ) SOLID_ANGLE_UNIT ( ) );
#9972=CIRCLE ( 'NONE', #23396, 0.5000000000000004441 ) ;
#9975=CARTESIAN_POINT ( 'NONE',  ( -8.102448949553179958, 152.4949999999999761, 5.886773742842747126 ) ) ;
#9977=VERTEX_POINT ( 'NONE', #7060 ) ;
#9985=CARTESIAN_POINT ( 'NONE',  ( 5.598654528085805993, 117.2449999999999903, 7.705886871421374629 ) ) ;
#9989=ORIENTED_EDGE ( 'NONE', *, *, #5247, .F. ) ;
#9996=AXIS2_PLACEMENT_3D ( 'NONE', #25997, #68243, #20384 ) ;
#9997=CARTESIAN_POINT ( 'NONE',  ( -48.81081081081080697, 14.09971791521132900, 9.500000000000000000 ) ) ;
#9998=CARTESIAN_POINT ( 'NONE',  ( -71.99999999999998579, 119.9999999999997868, -7.000000000000000000 ) ) ;
#10000=ORIENTED_EDGE ( 'NONE', *, *, #66561, .T. ) ;
#10004=DIRECTION ( 'NONE',  ( -1.000000000000000000, 4.336808689941999001E-16, 0.000000000000000000 ) ) ;
#10007=CIRCLE ( 'NONE', #5444, 8.500000000000000000 ) ;
#10012=EDGE_CURVE ( 'NONE', #58922, #25661, #17009, .T. ) ;
#10018=CARTESIAN_POINT ( 'NONE',  ( 7.632228543268608334, 141.4570736234661581, -2.479861379858951942 ) ) ;
#10030=ORIENTED_EDGE ( 'NONE', *, *, #13048, .F. ) ;
#10031=DIRECTION ( 'NONE',  ( -0.000000000000000000, 1.000000000000000000, -0.000000000000000000 ) ) ;
#10040=DIRECTION ( 'NONE',  ( 0.000000000000000000, 0.000000000000000000, 1.000000000000000000 ) ) ;
#10045=ORIENTED_EDGE ( 'NONE', *, *, #26039, .T. ) ;
#10046=CIRCLE ( 'NONE', #35898, 18.00000000000000355 ) ;
#10047=( NAMED_UNIT ( * ) SI_UNIT ( $, .STERADIAN. ) SOLID_ANGLE_UNIT ( ) );
#10051=AXIS2_PLACEMENT_3D ( 'NONE', #48362, #17027, #21585 ) ;
#10052=CARTESIAN_POINT ( 'NONE',  ( 8.102448949553179958, 120.3949999999999818, 5.886773742842750679 ) ) ;
#10059=AXIS2_PLACEMENT_3D ( 'NONE', #660, #31695, #4965 ) ;
#10060=CYLINDRICAL_SURFACE ( 'NONE', #64380, 0.5000000000000004441 ) ;
#10064=DIRECTION ( 'NONE',  ( 0.000000000000000000, 0.000000000000000000, 1.000000000000000000 ) ) ;
#10072=CARTESIAN_POINT ( 'NONE',  ( 20.71938756518089875, 149.6378529145318907, -9.985383568374002650 ) ) ;
#10073=UNCERTAINTY_MEASURE_WITH_UNIT (LENGTH_MEASURE( 1.000000000000000082E-05 ), #1753, 'distance_accuracy_value', 'NONE');
#10075=CARTESIAN_POINT ( 'NONE',  ( 3.094860106618431583, 154.2049999999999272, 9.525000000000000355 ) ) ;
#10077=CARTESIAN_POINT ( 'NONE',  ( -71.50000000000000000, 14.49137674618942562, 7.500000000000000000 ) ) ;
#10080=UNCERTAINTY_MEASURE_WITH_UNIT (LENGTH_MEASURE( 1.000000000000000082E-05 ), #7202, 'distance_accuracy_value', 'NONE');
#10084=CIRCLE ( 'NONE', #34765, 18.00000000000000355 ) ;
#10094=CARTESIAN_POINT ( 'NONE',  ( 6.826472737025121695, 117.6070736234661638, -4.959722759717905660 ) ) ;
#10097=CIRCLE ( 'NONE', #64012, 13.49999999999999822 ) ;
#10098=SURFACE_STYLE_USAGE ( .BOTH. , #36856 ) ;
#10099=COLOUR_RGB ( '', 0.66274510, 0.83137255, 0.94901961) ;
#10107=CARTESIAN_POINT ( 'NONE',  ( 3.094860106618435136, 122.4049999999999727, -9.525000000000000355 ) ) ;
#10109=FILL_AREA_STYLE_COLOUR ( '', #32219 ) ;
#10117=CARTESIAN_POINT ( 'NONE',  ( 5.203376869638292490, 154.0320170787420579, -7.424028789300809450 ) ) ;
#10121=CARTESIAN_POINT ( 'NONE',  ( 4.716976649647096842, 157.7429263765338021, 6.492361379858953896 ) ) ;
#10122=CARTESIAN_POINT ( 'NONE',  ( 45.50000000000000000, -1.414600137340999687E-14, 9.500000000000000000 ) ) ;
#10127=DIRECTION ( 'NONE',  ( -1.000000000000000000, 0.000000000000000000, 0.000000000000000000 ) ) ;
#10128=COLOUR_RGB ( '', 0.09019608, 0.27058824, 0.51372549) ;
#10130=CIRCLE ( 'NONE', #14653, 1.000000000000000888 ) ;
#10131=CARTESIAN_POINT ( 'NONE',  ( -74.42860156060436339, 8.073466093857248893, 6.500000000000083489 ) ) ;
#10134=ORIENTED_EDGE ( 'NONE', *, *, #14692, .T. ) ;
#10135=EDGE_LOOP ( 'NONE', ( #69350, #29921 ) ) ;
#10136=DIRECTION ( 'NONE',  ( 1.000000000000000000, 0.000000000000000000, -0.000000000000000000 ) ) ;
#10141=DIRECTION ( 'NONE',  ( -0.000000000000000000, -0.000000000000000000, -1.000000000000000000 ) ) ;
#10145=VECTOR ( 'NONE', #22158, 1000.000000000000000 ) ;
#10147=MECHANICAL_DESIGN_GEOMETRIC_PRESENTATION_REPRESENTATION('',(#55055),#42777);
#10151=AXIS2_PLACEMENT_3D ( 'NONE', #22099, #33345, #54769 ) ;
#10154=( NAMED_UNIT ( * ) SI_UNIT ( $, .STERADIAN. ) SOLID_ANGLE_UNIT ( ) );
#10156=CARTESIAN_POINT ( 'NONE',  ( -75.43856457103669300, 36.03011512829429819, -9.655596932504062480 ) ) ;
#10158=CARTESIAN_POINT ( 'NONE',  ( -8.102448949553181734, 129.6049999999999613, 5.886773742842747126 ) ) ;
#10162=UNCERTAINTY_MEASURE_WITH_UNIT (LENGTH_MEASURE( 1.000000000000000082E-05 ), #41249, 'distance_accuracy_value', 'NONE');
#10163=CIRCLE ( 'NONE', #6774, 0.5000000000000004441 ) ;
#10173=ORIENTED_EDGE ( 'NONE', *, *, #5445, .T. ) ;
#10175=VECTOR ( 'NONE', #42880, 1000.000000000000000 ) ;
#10176=( LENGTH_UNIT ( ) NAMED_UNIT ( * ) SI_UNIT ( .MILLI., .METRE. ) );
#10177=ADVANCED_FACE ( 'NONE', ( #29183 ), #59056, .T. ) ;
#10181=VERTEX_POINT ( 'NONE', #50671 ) ;
#10183=ORIENTED_EDGE ( 'NONE', *, *, #58138, .T. ) ;
#10185=CARTESIAN_POINT ( 'NONE',  ( -9.827790563157511022E-16, 128.5570736234661524, 8.025000000000000355 ) ) ;
#10193=CARTESIAN_POINT ( 'NONE',  ( 0.000000000000000000, 154.4449999999999932, -9.525000000000000355 ) ) ;
#10195=AXIS2_PLACEMENT_3D ( 'NONE', #54944, #1079, #59542 ) ;
#10197=SURFACE_SIDE_STYLE ('',( #52089 ) ) ;
#10198=CARTESIAN_POINT ( 'NONE',  ( 3.094860106618435136, 146.4050000000000011, -9.525000000000000355 ) ) ;
#10203=CARTESIAN_POINT ( 'NONE',  ( 2.607480562269076430, 125.7929263765338277, -8.025000000000000355 ) ) ;
#10205=UNCERTAINTY_MEASURE_WITH_UNIT (LENGTH_MEASURE( 1.000000000000000082E-05 ), #8244, 'distance_accuracy_value', 'NONE');
#10208=( NAMED_UNIT ( * ) SI_UNIT ( $, .STERADIAN. ) SOLID_ANGLE_UNIT ( ) );
#10212=VERTEX_POINT ( 'NONE', #9514 ) ;
#10214=DIRECTION ( 'NONE',  ( -1.000000000000000000, 0.000000000000000000, 0.000000000000000000 ) ) ;
#10216=FILL_AREA_STYLE ('',( #6301 ) ) ;
#10219=MECHANICAL_DESIGN_GEOMETRIC_PRESENTATION_REPRESENTATION('',(#60740),#61851);
#10220=DIRECTION ( 'NONE',  ( 1.000000000000000000, 0.000000000000000000, 0.000000000000000000 ) ) ;
#10221=( LENGTH_UNIT ( ) NAMED_UNIT ( * ) SI_UNIT ( .MILLI., .METRE. ) );
#10223=FACE_OUTER_BOUND ( 'NONE', #35482, .T. ) ;
#10224=VERTEX_POINT ( 'NONE', #36625 ) ;
#10225=COLOUR_RGB ( '', 0.31764706, 0.68627451, 0.89019608) ;
#10233=DIRECTION ( 'NONE',  ( 0.000000000000000000, 0.000000000000000000, -1.000000000000000000 ) ) ;
#10239=AXIS2_PLACEMENT_3D ( 'NONE', #60938, #12756, #56362 ) ;
#10240=DIRECTION ( 'NONE',  ( 1.000000000000000000, 0.000000000000000000, 0.000000000000000000 ) ) ;
#10241=CARTESIAN_POINT ( 'NONE',  ( -44.50000000000000000, 10.49999999999998579, 3.500000000000000000 ) ) ;
#10243=LINE ( 'NONE', #30626, #48099 ) ;
#10247=CARTESIAN_POINT ( 'NONE',  ( 10.01517768586949231, 150.6949999999999648, 1.839758294383810543E-15 ) ) ;
#10249=VECTOR ( 'NONE', #19326, 1000.000000000000000 ) ;
#10250=CARTESIAN_POINT ( 'NONE',  ( 60.00000000000000000, 1.797044900979284448E-15, -11.50000000000000000 ) ) ;
#10253=UNCERTAINTY_MEASURE_WITH_UNIT (LENGTH_MEASURE( 1.000000000000000082E-05 ), #65487, 'distance_accuracy_value', 'NONE');
#10261=EDGE_CURVE ( 'NONE', #15159, #15321, #69526, .T. ) ;
#10262=EDGE_CURVE ( 'NONE', #67533, #33857, #5232, .T. ) ;
#10264=ORIENTED_EDGE ( 'NONE', *, *, #50830, .T. ) ;
#10265=ORIENTED_EDGE ( 'NONE', *, *, #67353, .F. ) ;
#10267=CARTESIAN_POINT ( 'NONE',  ( 45.50000000000000000, 1.797044900979284448E-15, 6.500000000000000000 ) ) ;
#10269=EDGE_CURVE ( 'NONE', #68002, #55126, #4176, .T. ) ;
#10270=CARTESIAN_POINT ( 'NONE',  ( -45.00000000000000000, -2.024042244987997205E-14, 6.999999999999999112 ) ) ;
#10272=SURFACE_SIDE_STYLE ('',( #47249 ) ) ;
#10275=ORIENTED_EDGE ( 'NONE', *, *, #31275, .F. ) ;
#10277=DIRECTION ( 'NONE',  ( 0.000000000000000000, 1.000000000000000000, -0.000000000000000000 ) ) ;
#10280=STYLED_ITEM ( 'NONE', ( #18390 ), #60190 ) ;
#10283=CARTESIAN_POINT ( 'NONE',  ( 9.058813317711337021, 117.5449999999999875, 2.943386871421375783 ) ) ;
#10284=CARTESIAN_POINT ( 'NONE',  ( 34.99999999999992895, 113.4999999999999858, 7.500000000000000000 ) ) ;
#10286=( NAMED_UNIT ( * ) PLANE_ANGLE_UNIT ( ) SI_UNIT ( $, .RADIAN. ) );
#10287=CARTESIAN_POINT ( 'NONE',  ( -3.094860106618434248, 123.9049999999999727, 9.525000000000000355 ) ) ;
#10290=DIRECTION ( 'NONE',  ( 0.000000000000000000, 0.000000000000000000, -1.000000000000000000 ) ) ;
#10293=CARTESIAN_POINT ( 'NONE',  ( 5.598654528085809545, 146.2549999999999955, -7.705886871421373741 ) ) ;
#10297=SURFACE_STYLE_FILL_AREA ( #357 ) ;
#10300=ORIENTED_EDGE ( 'NONE', *, *, #2888, .F. ) ;
#10302=DIRECTION ( 'NONE',  ( -1.000000000000000000, 0.000000000000000000, 0.000000000000000000 ) ) ;
#10304=ORIENTED_EDGE ( 'NONE', *, *, #63722, .F. ) ;
#10308=VERTEX_POINT ( 'NONE', #65008 ) ;
#10309=SURFACE_SIDE_STYLE ('',( #5012 ) ) ;
#10312=VERTEX_POINT ( 'NONE', #33024 ) ;
#10316=ORIENTED_EDGE ( 'NONE', *, *, #44817, .F. ) ;
#10321=CARTESIAN_POINT ( 'NONE',  ( -3.094860106618434248, 152.7949999999999591, 9.525000000000000355 ) ) ;
#10325=SURFACE_STYLE_USAGE ( .BOTH. , #384 ) ;
#10326=ORIENTED_EDGE ( 'NONE', *, *, #7315, .F. ) ;
#10328=FACE_OUTER_BOUND ( 'NONE', #49921, .T. ) ;
#10330=CARTESIAN_POINT ( 'NONE',  ( -3.094860106618432471, 118.5949999999999847, -9.525000000000000355 ) ) ;
#10333=DIRECTION ( 'NONE',  ( 0.000000000000000000, 0.000000000000000000, -1.000000000000000000 ) ) ;
#10338=CIRCLE ( 'NONE', #49649, 1.000000000000000888 ) ;
#10348=FILL_AREA_STYLE ('',( #4323 ) ) ;
#10350=CIRCLE ( 'NONE', #67627, 0.5000000000000004441 ) ;
#10355=EDGE_CURVE ( 'NONE', #24259, #63980, #24573, .T. ) ;
#10356=SURFACE_STYLE_FILL_AREA ( #10691 ) ;
#10357=CARTESIAN_POINT ( 'NONE',  ( 2.607480562268988500, 146.7070736234661581, 8.025000000000062528 ) ) ;
#10359=CIRCLE ( 'NONE', #10195, 0.5000000000000004441 ) ;
#10360=EDGE_CURVE ( 'NONE', #15634, #20172, #33582, .T. ) ;
#10362=( GEOMETRIC_REPRESENTATION_CONTEXT ( 3 ) GLOBAL_UNCERTAINTY_ASSIGNED_CONTEXT ( ( #19439 ) ) GLOBAL_UNIT_ASSIGNED_CONTEXT ( ( #37249, #49763, #23029 ) ) REPRESENTATION_CONTEXT ( 'NONE', 'WORKASPACE' ) );
#10363=VERTEX_POINT ( 'NONE', #27366 ) ;
#10367=LINE ( 'NONE', #37486, #37488 ) ;
#10368=DIRECTION ( 'NONE',  ( -0.000000000000000000, -0.000000000000000000, -1.000000000000000000 ) ) ;
#10371=CARTESIAN_POINT ( 'NONE',  ( -6.826472737025120807, 142.5070736234661410, -4.959722759717907437 ) ) ;
#10376=UNCERTAINTY_MEASURE_WITH_UNIT (LENGTH_MEASURE( 1.000000000000000082E-05 ), #14979, 'distance_accuracy_value', 'NONE');
#10378=CARTESIAN_POINT ( 'NONE',  ( 6.826472737025119919, 132.0070736234661695, 4.959722759717908325 ) ) ;
#10379=EDGE_LOOP ( 'NONE', ( #1366, #21730, #54317, #47809 ) ) ;
#10382=ADVANCED_FACE ( 'NONE', ( #22820, #59376 ), #11212, .T. ) ;
#10385=DIRECTION ( 'NONE',  ( 0.000000000000000000, 0.000000000000000000, 1.000000000000000000 ) ) ;
#10389=DIRECTION ( 'NONE',  ( -1.000000000000000000, 0.000000000000000000, 0.000000000000000000 ) ) ;
#10390=DIRECTION ( 'NONE',  ( 1.000000000000000000, 0.000000000000000000, 0.000000000000000000 ) ) ;
#10391=ORIENTED_EDGE ( 'NONE', *, *, #21060, .T. ) ;
#10394=AXIS2_PLACEMENT_3D ( 'NONE', #47724, #15339, #69457 ) ;
#10398=CIRCLE ( 'NONE', #33966, 0.5000000000000004441 ) ;
#10400=LINE ( 'NONE', #21624, #15138 ) ;
#10401=CARTESIAN_POINT ( 'NONE',  ( -74.49999999999998579, 64.49137674618943095, -10.00000000000000000 ) ) ;
#10403=MECHANICAL_DESIGN_GEOMETRIC_PRESENTATION_REPRESENTATION('',(#17138),#35078);
#10404=CARTESIAN_POINT ( 'NONE',  ( -8.102448949553179958, 118.8949999999999676, -5.886773742842749790 ) ) ;
#10407=VERTEX_POINT ( 'NONE', #67804 ) ;
#10408=CARTESIAN_POINT ( 'NONE',  ( -44.99999999999977973, 146.9999999999999716, -7.000000000000000000 ) ) ;
#10409=( NAMED_UNIT ( * ) SI_UNIT ( $, .STERADIAN. ) SOLID_ANGLE_UNIT ( ) );
#10410=AXIS2_PLACEMENT_3D ( 'NONE', #61944, #2461, #28883 ) ;
#10421=CYLINDRICAL_SURFACE ( 'NONE', #65989, 0.5000000000000004441 ) ;
#10422=EDGE_CURVE ( 'NONE', #66072, #46073, #19000, .T. ) ;
#10423=SURFACE_STYLE_FILL_AREA ( #58593 ) ;
#10425=COLOUR_RGB ( '', 0.09019608, 0.27058824, 0.51372549) ;
#10426=ADVANCED_FACE ( 'NONE', ( #55507 ), #17955, .T. ) ;
#10428=DIRECTION ( 'NONE',  ( 0.7833176619561877940, -0.6216216216216191581, -4.313366480807175060E-15 ) ) ;
#10431=CARTESIAN_POINT ( 'NONE',  ( 41.49999999999998579, 99.99999999999998579, 3.500000000000000000 ) ) ;
#10436=EDGE_CURVE ( 'NONE', #41309, #60166, #33634, .T. ) ;
#10437=FACE_OUTER_BOUND ( 'NONE', #50232, .T. ) ;
#10439=DIRECTION ( 'NONE',  ( 0.000000000000000000, 1.000000000000000000, -0.000000000000000000 ) ) ;
#10440=FACE_OUTER_BOUND ( 'NONE', #45474, .T. ) ;
#10442=STYLED_ITEM ( 'NONE', ( #42692 ), #35833 ) ;
#10443=CARTESIAN_POINT ( 'NONE',  ( -6.826472737025120807, 110.1070736234661496, 4.959722759717906548 ) ) ;
#10444=AXIS2_PLACEMENT_3D ( 'NONE', #34167, #39134, #44078 ) ;
#10447=SURFACE_STYLE_FILL_AREA ( #48112 ) ;
#10449=ORIENTED_EDGE ( 'NONE', *, *, #13993, .T. ) ;
#10453=ORIENTED_EDGE ( 'NONE', *, *, #12062, .F. ) ;
#10454=CARTESIAN_POINT ( 'NONE',  ( -5.598654528085806881, 122.8549999999999898, -7.705886871421374629 ) ) ;
#10455=DIRECTION ( 'NONE',  ( 0.000000000000000000, 0.000000000000000000, -1.000000000000000000 ) ) ;
#10456=( NAMED_UNIT ( * ) PLANE_ANGLE_UNIT ( ) SI_UNIT ( $, .RADIAN. ) );
#10457=AXIS2_PLACEMENT_3D ( 'NONE', #1149, #53980, #21272 ) ;
#10465=CARTESIAN_POINT ( 'NONE',  ( -48.00000000000000000, 14.49137674618942562, 9.500000000000000000 ) ) ;
#10467=CARTESIAN_POINT ( 'NONE',  ( -4.716976649647098618, 151.1429263765338078, 6.492361379858953008 ) ) ;
#10471=CARTESIAN_POINT ( 'NONE',  ( 20.06856914206998610, 114.9886858359306814, -10.44306996520268527 ) ) ;
#10472=ORIENTED_EDGE ( 'NONE', *, *, #43855, .F. ) ;
#10473=PRESENTATION_STYLE_ASSIGNMENT (( #30866 ) ) ;
#10474=AXIS2_PLACEMENT_3D ( 'NONE', #42243, #59046, #25983 ) ;
#10475=SURFACE_STYLE_USAGE ( .BOTH. , #42513 ) ;
#10477=COLOUR_RGB ( '', 0.08235294, 0.09019608, 0.10196078) ;
#10478=SURFACE_STYLE_USAGE ( .BOTH. , #9445 ) ;
#10479=DIRECTION ( 'NONE',  ( 0.000000000000000000, 0.000000000000000000, 1.000000000000000000 ) ) ;
#10482=ORIENTED_EDGE ( 'NONE', *, *, #8962, .F. ) ;
#10484=DIRECTION ( 'NONE',  ( 0.000000000000000000, -1.000000000000000000, 0.000000000000000000 ) ) ;
#10487=PRESENTATION_STYLE_ASSIGNMENT (( #53719 ) ) ;
#10488=ORIENTED_EDGE ( 'NONE', *, *, #42742, .T. ) ;
#10498=PRESENTATION_STYLE_ASSIGNMENT (( #69567 ) ) ;
#10499=CARTESIAN_POINT ( 'NONE',  ( 2.816687638038913141E-15, 149.9999999999999716, 23.00000000000000355 ) ) ;
#10503=CARTESIAN_POINT ( 'NONE',  ( -74.96321444755994889, 35.57983959226599779, -9.691745531186823470 ) ) ;
#10504=CIRCLE ( 'NONE', #29569, 29.50000000000000000 ) ;
#10507=CARTESIAN_POINT ( 'NONE',  ( -1.166476076187854022E-15, 139.0549999999999784, 9.525000000000000355 ) ) ;
#10509=CARTESIAN_POINT ( 'NONE',  ( -6.826472737025120807, 126.9929263765338163, 4.959722759717906548 ) ) ;
#10516=ORIENTED_EDGE ( 'NONE', *, *, #62562, .T. ) ;
#10517=EDGE_CURVE ( 'NONE', #16804, #53241, #54941, .T. ) ;
#10520=MECHANICAL_DESIGN_GEOMETRIC_PRESENTATION_REPRESENTATION('',(#65688),#50000);
#10523=CARTESIAN_POINT ( 'NONE',  ( -6.826472737025120807, 137.1070736234661638, 4.959722759717906548 ) ) ;
#10528=( NAMED_UNIT ( * ) SI_UNIT ( $, .STERADIAN. ) SOLID_ANGLE_UNIT ( ) );
#10531=ORIENTED_EDGE ( 'NONE', *, *, #29644, .T. ) ;
#10533=ORIENTED_EDGE ( 'NONE', *, *, #8702, .T. ) ;
#10542=CARTESIAN_POINT ( 'NONE',  ( -9.058813317711338797, 149.3449999999999989, 2.943386871421373563 ) ) ;
#10543=( GEOMETRIC_REPRESENTATION_CONTEXT ( 3 ) GLOBAL_UNCERTAINTY_ASSIGNED_CONTEXT ( ( #2383 ) ) GLOBAL_UNIT_ASSIGNED_CONTEXT ( ( #3755, #31195, #14710 ) ) REPRESENTATION_CONTEXT ( 'NONE', 'WORKASPACE' ) );
#10546=SURFACE_SIDE_STYLE ('',( #37319 ) ) ;
#10547=DIRECTION ( 'NONE',  ( 1.000000000000000000, 0.000000000000000000, 0.000000000000000000 ) ) ;
#10549=CARTESIAN_POINT ( 'NONE',  ( 4.716976649647096842, 127.7429263765338163, 6.492361379858953896 ) ) ;
#10550=DIRECTION ( 'NONE',  ( 1.000000000000000000, -0.000000000000000000, -0.000000000000000000 ) ) ;
#10552=( GEOMETRIC_REPRESENTATION_CONTEXT ( 3 ) GLOBAL_UNCERTAINTY_ASSIGNED_CONTEXT ( ( #49671 ) ) GLOBAL_UNIT_ASSIGNED_CONTEXT ( ( #14794, #46487, #8805 ) ) REPRESENTATION_CONTEXT ( 'NONE', 'WORKASPACE' ) );
#10556=LINE ( 'NONE', #59398, #68903 ) ;
#10560=DIRECTION ( 'NONE',  ( 0.000000000000000000, 0.000000000000000000, -1.000000000000000000 ) ) ;
#10562=DIRECTION ( 'NONE',  ( 1.000000000000000000, 0.000000000000000000, 0.000000000000000000 ) ) ;
#10567=( NAMED_UNIT ( * ) SI_UNIT ( $, .STERADIAN. ) SOLID_ANGLE_UNIT ( ) );
#10570=EDGE_LOOP ( 'NONE', ( #34245, #56523, #58816, #37845 ) ) ;
#10576=CARTESIAN_POINT ( 'NONE',  ( -74.99999999999998579, 50.00000000000000000, 11.50000000000003730 ) ) ;
#10580=STYLED_ITEM ( 'NONE', ( #54962 ), #48654 ) ;
#10581=ORIENTED_EDGE ( 'NONE', *, *, #38505, .F. ) ;
#10583=SURFACE_STYLE_USAGE ( .BOTH. , #4949 ) ;
#10584=CARTESIAN_POINT ( 'NONE',  ( -48.50000000000000000, 14.49137674618942562, -7.500000000000000000 ) ) ;
#10588=CARTESIAN_POINT ( 'NONE',  ( 5.598654528085805993, 153.2450000000000045, 7.705886871421374629 ) ) ;
#10590=ADVANCED_FACE ( 'NONE', ( #22747 ), #2077, .T. ) ;
#10592=MECHANICAL_DESIGN_GEOMETRIC_PRESENTATION_REPRESENTATION('',(#39791),#9439);
#10598=ADVANCED_FACE ( 'NONE', ( #28328 ), #7592, .T. ) ;
#10600=( GEOMETRIC_REPRESENTATION_CONTEXT ( 3 ) GLOBAL_UNCERTAINTY_ASSIGNED_CONTEXT ( ( #13823 ) ) GLOBAL_UNIT_ASSIGNED_CONTEXT ( ( #52497, #47602, #36691 ) ) REPRESENTATION_CONTEXT ( 'NONE', 'WORKASPACE' ) );
#10606=COLOUR_RGB ( '', 0.66274510, 0.83137255, 0.94901961) ;
#10609=CARTESIAN_POINT ( 'NONE',  ( 0.000000000000000000, 116.9429263765338192, -8.025000000000000355 ) ) ;
#10610=CARTESIAN_POINT ( 'NONE',  ( -45.91400648542629170, 9.424643574460597861, 6.049632038801588507 ) ) ;
#10613=VERTEX_POINT ( 'NONE', #13206 ) ;
#10616=VERTEX_POINT ( 'NONE', #40675 ) ;
#10620=COLOUR_RGB ( '', 0.08235294, 0.09019608, 0.10196078) ;
#10622=CARTESIAN_POINT ( 'NONE',  ( 8.102448949553183510, 117.9949999999999761, -5.886773742842746238 ) ) ;
#10623=DIRECTION ( 'NONE',  ( -0.000000000000000000, -0.000000000000000000, -1.000000000000000000 ) ) ;
#10627=CARTESIAN_POINT ( 'NONE',  ( -3.094860106618434248, 117.9049999999999727, 9.525000000000000355 ) ) ;
#10630=CARTESIAN_POINT ( 'NONE',  ( -41.68184459379065032, 107.4432011401341640, -3.569690802414609010 ) ) ;
#10631=ORIENTED_EDGE ( 'NONE', *, *, #2008, .T. ) ;
#10632=CARTESIAN_POINT ( 'NONE',  ( 5.598654528085809545, 149.2549999999999955, -7.705886871421373741 ) ) ;
#10633=DIRECTION ( 'NONE',  ( 1.000000000000000000, 0.000000000000000000, 0.000000000000000000 ) ) ;
#10634=CARTESIAN_POINT ( 'NONE',  ( 45.00000000000000000, 99.99999999999992895, 4.000000000000000000 ) ) ;
#10636=( LENGTH_UNIT ( ) NAMED_UNIT ( * ) SI_UNIT ( .MILLI., .METRE. ) );
#10637=CARTESIAN_POINT ( 'NONE',  ( -15.98999599679679839, 146.4999999999999716, -7.500000000000000000 ) ) ;
#10638=VERTEX_POINT ( 'NONE', #8310 ) ;
#10641=( NAMED_UNIT ( * ) SI_UNIT ( $, .STERADIAN. ) SOLID_ANGLE_UNIT ( ) );
#10645=AXIS2_PLACEMENT_3D ( 'NONE', #15325, #41008, #36783 ) ;
#10646=CARTESIAN_POINT ( 'NONE',  ( -48.50000000000000000, 14.49137674618942562, -9.500000000000000000 ) ) ;
#10647=VECTOR ( 'NONE', #18290, 1000.000000000000000 ) ;
#10648=FACE_OUTER_BOUND ( 'NONE', #53815, .T. ) ;
#10649=EDGE_LOOP ( 'NONE', ( #6091, #42013, #57786, #61439 ) ) ;
#10652=ORIENTED_EDGE ( 'NONE', *, *, #9040, .T. ) ;
#10655=CARTESIAN_POINT ( 'NONE',  ( 60.00000000000000000, 1.797044900979284448E-15, 12.00000000000000000 ) ) ;
#10657=DIRECTION ( 'NONE',  ( 1.000000000000000000, 0.000000000000000000, 0.000000000000000000 ) ) ;
#10658=SURFACE_STYLE_USAGE ( .BOTH. , #9640 ) ;
#10660=EDGE_CURVE ( 'NONE', #25577, #26262, #26192, .T. ) ;
#10661=AXIS2_PLACEMENT_3D ( 'NONE', #58328, #9119, #19295 ) ;
#10662=COLOUR_RGB ( '', 0.31764706, 0.68627451, 0.89019608) ;
#10664=ORIENTED_EDGE ( 'NONE', *, *, #39558, .T. ) ;
#10667=CARTESIAN_POINT ( 'NONE',  ( 10.01517768586949231, 123.6949999999999932, 1.839758294383810543E-15 ) ) ;
#10679=AXIS2_PLACEMENT_3D ( 'NONE', #43279, #18486, #64681 ) ;
#10681=CIRCLE ( 'NONE', #17482, 0.5000000000000004441 ) ;
#10682=CARTESIAN_POINT ( 'NONE',  ( -20.51914007124930706, 114.9043000146497207, -10.00000000000000000 ) ) ;
#10684=ORIENTED_EDGE ( 'NONE', *, *, #9889, .F. ) ;
#10687=MECHANICAL_DESIGN_GEOMETRIC_PRESENTATION_REPRESENTATION('',(#61249),#56737);
#10688=DIRECTION ( 'NONE',  ( 0.000000000000000000, 1.000000000000000000, 0.000000000000000000 ) ) ;
#10689=SURFACE_SIDE_STYLE ('',( #14578 ) ) ;
#10691=FILL_AREA_STYLE ('',( #5057 ) ) ;
#10692=FACE_OUTER_BOUND ( 'NONE', #57781, .T. ) ;
#10695=VERTEX_POINT ( 'NONE', #68098 ) ;
#10698=FILL_AREA_STYLE ('',( #64150 ) ) ;
#10699=CARTESIAN_POINT ( 'NONE',  ( 0.000000000000000000, 139.0570736234661808, -8.025000000000000355 ) ) ;
#10701=CIRCLE ( 'NONE', #42245, 0.5000000000000000000 ) ;
#10704=CARTESIAN_POINT ( 'NONE',  ( 40.99999999999997868, 9.999999999999978684, -3.000000000000000444 ) ) ;
#10707=CARTESIAN_POINT ( 'NONE',  ( 75.00000000000000000, 19.30628705663858113, -6.999999999999999112 ) ) ;
#10709=CARTESIAN_POINT ( 'NONE',  ( 7.632228543268608334, 143.3429263765338249, -2.479861379858951942 ) ) ;
#10711=SURFACE_STYLE_USAGE ( .BOTH. , #32487 ) ;
#10720=FACE_OUTER_BOUND ( 'NONE', #4124, .T. ) ;
#10722=EDGE_CURVE ( 'NONE', #62143, #15151, #56071, .T. ) ;
#10723=ORIENTED_EDGE ( 'NONE', *, *, #26813, .F. ) ;
#10724=SURFACE_SIDE_STYLE ('',( #48747 ) ) ;
#10726=DIRECTION ( 'NONE',  ( -0.000000000000000000, -0.000000000000000000, -1.000000000000000000 ) ) ;
#10727=STYLED_ITEM ( 'NONE', ( #56358 ), #39122 ) ;
#10728=PRESENTATION_STYLE_ASSIGNMENT (( #42436 ) ) ;
#10733=AXIS2_PLACEMENT_3D ( 'NONE', #15582, #49314, #10975 ) ;
#10735=CARTESIAN_POINT ( 'NONE',  ( -44.99999999999977973, 149.4999999999999716, 10.00000000000000000 ) ) ;
#10736=( NAMED_UNIT ( * ) PLANE_ANGLE_UNIT ( ) SI_UNIT ( $, .RADIAN. ) );
#10737=( NAMED_UNIT ( * ) SI_UNIT ( $, .STERADIAN. ) SOLID_ANGLE_UNIT ( ) );
#10739=CARTESIAN_POINT ( 'NONE',  ( 3.094860106618435136, 124.2949999999999733, -9.525000000000000355 ) ) ;
#10740=AXIS2_PLACEMENT_3D ( 'NONE', #28850, #2418, #17648 ) ;
#10742=EDGE_CURVE ( 'NONE', #69397, #2052, #9348, .T. ) ;
#10743=AXIS2_PLACEMENT_3D ( 'NONE', #23381, #61686, #66655 ) ;
#10750=CARTESIAN_POINT ( 'NONE',  ( -4.716976649647097730, 130.3570736234661638, -6.492361379858953896 ) ) ;
#10754=CARTESIAN_POINT ( 'NONE',  ( 41.06069799967658440, 107.9552192246431730, 3.682425535826294727 ) ) ;
#10758=FILL_AREA_STYLE_COLOUR ( '', #15676 ) ;
#10759=CARTESIAN_POINT ( 'NONE',  ( -74.99999999999998579, 50.00000000000000000, 7.000000000000000000 ) ) ;
#10763=( LENGTH_UNIT ( ) NAMED_UNIT ( * ) SI_UNIT ( .MILLI., .METRE. ) );
#10764=DIRECTION ( 'NONE',  ( 0.000000000000000000, 0.000000000000000000, 1.000000000000000000 ) ) ;
#10765=AXIS2_PLACEMENT_3D ( 'NONE', #4806, #42844, #42491 ) ;
#10770=( BOUNDED_CURVE ( )  B_SPLINE_CURVE ( 2, ( #23213, #44707, #17927, #39416, #52035, #7706, #62551, #34445, #30184, #24236, #51325 ),
 .UNSPECIFIED., .F., .F. ) 
 B_SPLINE_CURVE_WITH_KNOTS ( ( 3, 2, 2, 2, 2, 3 ),
 ( 0.1470588235294118806, 0.1529411764705883026, 0.1588235294117646967, 0.1647058823529411464, 0.1705882352941175684, 0.1764705882352939903 ),
 .UNSPECIFIED. ) 
 CURVE ( )  GEOMETRIC_REPRESENTATION_ITEM ( )  RATIONAL_B_SPLINE_CURVE ( ( 0.9999999999999991118, 0.9510565162951544194, 1.000000000000000000, 0.9510565162951535312, 1.000000000000000000, 0.9510565162951535312, 1.000000000000000000, 0.9510565162951535312, 1.000000000000000000, 0.9510565162951546414, 0.9999999999999988898 ) ) 
 REPRESENTATION_ITEM ( '' )  );
#10772=( NAMED_UNIT ( * ) SI_UNIT ( $, .STERADIAN. ) SOLID_ANGLE_UNIT ( ) );
#10775=MECHANICAL_DESIGN_GEOMETRIC_PRESENTATION_REPRESENTATION('',(#1732),#17530);
#10777=CARTESIAN_POINT ( 'NONE',  ( -74.99999999999998579, 50.00000000000000000, 10.50000000000000000 ) ) ;
#10778=FACE_OUTER_BOUND ( 'NONE', #22050, .T. ) ;
#10779=VECTOR ( 'NONE', #30254, 1000.000000000000000 ) ;
#10780=EDGE_LOOP ( 'NONE', ( #28332, #4960, #53302 ) ) ;
#10782=( GEOMETRIC_REPRESENTATION_CONTEXT ( 3 ) GLOBAL_UNCERTAINTY_ASSIGNED_CONTEXT ( ( #33422 ) ) GLOBAL_UNIT_ASSIGNED_CONTEXT ( ( #49212, #7655, #17227 ) ) REPRESENTATION_CONTEXT ( 'NONE', 'WORKASPACE' ) );
#10783=CARTESIAN_POINT ( 'NONE',  ( -6.826472737025120807, 112.5070736234661410, -4.959722759717907437 ) ) ;
#10784=B_SPLINE_CURVE_WITH_KNOTS ( 'NONE', 3,
 ( #28768, #1657, #44664, #29094, #65726, #54801, #7339, #39371, #18587, #33706, #55860, #34407 ),
 .UNSPECIFIED., .F., .F.,
 ( 4, 2, 2, 2, 2, 4 ),
 ( 0.000000000000000000, 0.0009366607938385700409, 0.001404991190757859994, 0.001639156389217507953, 0.001756238988447332908, 0.001873321587677158296 ),
 .UNSPECIFIED. ) ;
#10786=SURFACE_STYLE_USAGE ( .BOTH. , #22371 ) ;
#10787=ORIENTED_EDGE ( 'NONE', *, *, #53929, .F. ) ;
#10791=ORIENTED_EDGE ( 'NONE', *, *, #39502, .T. ) ;
#10792=CARTESIAN_POINT ( 'NONE',  ( 9.058813317711338797, 130.9549999999999841, -2.943386871421372675 ) ) ;
#10793=PLANE ( 'NONE',  #25433 ) ;
#10798=AXIS2_PLACEMENT_3D ( 'NONE', #40134, #66848, #12661 ) ;
#10799=CARTESIAN_POINT ( 'NONE',  ( 8.459058532691745569, 153.5028685191038562, -1.153563530786663405 ) ) ;
#10801=ORIENTED_EDGE ( 'NONE', *, *, #52222, .F. ) ;
#10802=CARTESIAN_POINT ( 'NONE',  ( 6.826472737025121695, 152.4929263765338590, -4.959722759717905660 ) ) ;
#10804=DIRECTION ( 'NONE',  ( 0.000000000000000000, 0.000000000000000000, 1.000000000000000000 ) ) ;
#10806=CARTESIAN_POINT ( 'NONE',  ( -20.74185979783655043, 149.7721295005298714, -9.939118314201632387 ) ) ;
#10808=VERTEX_POINT ( 'NONE', #41373 ) ;
#10809=DIRECTION ( 'NONE',  ( 1.000000000000000000, 0.000000000000000000, 0.000000000000000000 ) ) ;
#10810=STYLED_ITEM ( 'NONE', ( #13118 ), #49883 ) ;
#10813=CARTESIAN_POINT ( 'NONE',  ( -23.21231517720797655, 117.9999999999999716, -7.500000000000000000 ) ) ;
#10815=FILL_AREA_STYLE_COLOUR ( '', #22878 ) ;
#10816=CARTESIAN_POINT ( 'NONE',  ( 23.21231517720797655, 112.9999999999999858, 9.500000000000000000 ) ) ;
#10818=CARTESIAN_POINT ( 'NONE',  ( -7.239872073591128832, 153.7812473723182904, 5.042250455018151278 ) ) ;
#10819=EDGE_LOOP ( 'NONE', ( #51073, #63855, #44445, #30515 ) ) ;
#10820=ORIENTED_EDGE ( 'NONE', *, *, #42468, .T. ) ;
#10823=EDGE_CURVE ( 'NONE', #68013, #66131, #37099, .T. ) ;
#10825=STYLED_ITEM ( 'NONE', ( #20385 ), #39675 ) ;
#10827=FILL_AREA_STYLE ('',( #50803 ) ) ;
#10835=CARTESIAN_POINT ( 'NONE',  ( -23.21231517720797655, 117.4999999999999716, 9.500000000000000000 ) ) ;
#10841=CARTESIAN_POINT ( 'NONE',  ( -74.99506141310581597, 35.51815782338716332, -9.580134848897966293 ) ) ;
#10843=CARTESIAN_POINT ( 'NONE',  ( -8.102448949553181734, 135.0050000000000239, -5.886773742842749790 ) ) ;
#10845=CARTESIAN_POINT ( 'NONE',  ( -4.716976649647098618, 127.1429263765338220, 6.492361379858953008 ) ) ;
#10848=ADVANCED_FACE ( 'NONE', ( #15667 ), #6133, .T. ) ;
#10851=DIRECTION ( 'NONE',  ( 0.000000000000000000, 0.000000000000000000, 1.000000000000000000 ) ) ;
#10853=MECHANICAL_DESIGN_GEOMETRIC_PRESENTATION_REPRESENTATION('',(#36762),#69260);
#10854=FILL_AREA_STYLE_COLOUR ( '', #50661 ) ;
#10857=( NAMED_UNIT ( * ) PLANE_ANGLE_UNIT ( ) SI_UNIT ( $, .RADIAN. ) );
#10858=DIRECTION ( 'NONE',  ( 0.000000000000000000, 0.000000000000000000, -1.000000000000000000 ) ) ;
#10860=VERTEX_POINT ( 'NONE', #54988 ) ;
#10862=CYLINDRICAL_SURFACE ( 'NONE', #34053, 0.5000000000000004441 ) ;
#10863=CARTESIAN_POINT ( 'NONE',  ( 7.632228543268608334, 131.3429263765338249, -2.479861379858951942 ) ) ;
#10864=( BOUNDED_CURVE ( )  B_SPLINE_CURVE ( 2, ( #52702, #4469, #25936, #67132, #46058, #19268, #62194, #56927, #63918, #64272, #188 ),
 .UNSPECIFIED., .F., .F. ) 
 B_SPLINE_CURVE_WITH_KNOTS ( ( 3, 2, 2, 2, 2, 3 ),
 ( 0.1764705882352939903, 0.1823529411764704400, 0.1882352941176469174, 0.1941176470588234226, 0.1999999999999999001, 0.2058823529411763498 ),
 .UNSPECIFIED. ) 
 CURVE ( )  GEOMETRIC_REPRESENTATION_ITEM ( )  RATIONAL_B_SPLINE_CURVE ( ( 1.000000000000001110, 0.9510565162951523099, 1.000000000000000000, 0.9510565162951535312, 1.000000000000000000, 0.9510565162951535312, 1.000000000000000000, 0.9510565162951535312, 1.000000000000000000, 0.9510565162951544194, 0.9999999999999991118 ) ) 
 REPRESENTATION_ITEM ( '' )  );
#10865=CARTESIAN_POINT ( 'NONE',  ( 0.000000000000000000, 87.30187232391182306, 0.000000000000000000 ) ) ;
#10872=DIRECTION ( 'NONE',  ( 0.000000000000000000, 0.000000000000000000, 1.000000000000000000 ) ) ;
#10873=ORIENTED_EDGE ( 'NONE', *, *, #27339, .T. ) ;
#10874=FILL_AREA_STYLE_COLOUR ( '', #35850 ) ;
#10876=EDGE_LOOP ( 'NONE', ( #28210, #6737, #22634, #42000 ) ) ;
#10877=EDGE_CURVE ( 'NONE', #32066, #69681, #47191, .T. ) ;
#10879=CARTESIAN_POINT ( 'NONE',  ( 8.102448949553181734, 159.3949999999999534, 5.886773742842750679 ) ) ;
#10880=CARTESIAN_POINT ( 'NONE',  ( 24.21231517720798010, 113.4999999999999858, -7.000000000000000000 ) ) ;
#10881=ORIENTED_EDGE ( 'NONE', *, *, #61431, .T. ) ;
#10883=PRESENTATION_STYLE_ASSIGNMENT (( #31985 ) ) ;
#10884=FILL_AREA_STYLE ('',( #63989 ) ) ;
#10886=ORIENTED_EDGE ( 'NONE', *, *, #55288, .T. ) ;
#10887=CARTESIAN_POINT ( 'NONE',  ( -4.716976649647097730, 123.2429263765338163, -6.492361379858953896 ) ) ;
#10891=ADVANCED_FACE ( 'NONE', ( #38543 ), #38193, .T. ) ;
#10897=( NAMED_UNIT ( * ) PLANE_ANGLE_UNIT ( ) SI_UNIT ( $, .RADIAN. ) );
#10900=ADVANCED_FACE ( 'NONE', ( #49084 ), #7518, .F. ) ;
#10901=DIRECTION ( 'NONE',  ( 1.000000000000000000, 0.000000000000000000, -0.000000000000000000 ) ) ;
#10904=CARTESIAN_POINT ( 'NONE',  ( -65.00000000000000000, -1.962809905030629631E-14, 11.50000000000003020 ) ) ;
#10917=DIRECTION ( 'NONE',  ( 1.000000000000000000, 0.000000000000000000, -0.000000000000000000 ) ) ;
#10918=CARTESIAN_POINT ( 'NONE',  ( -60.00000000000000000, -2.024042244987997205E-14, 6.000000000000000888 ) ) ;
#10921=SPHERICAL_SURFACE ( 'NONE', #23415, 0.5000000000000000000 ) ;
#10922=DIRECTION ( 'NONE',  ( 0.000000000000000000, 1.000000000000000000, 0.000000000000000000 ) ) ;
#10923=PLANE ( 'NONE',  #8950 ) ;
#10924=MECHANICAL_DESIGN_GEOMETRIC_PRESENTATION_REPRESENTATION('',(#52485),#28877);
#10926=CARTESIAN_POINT ( 'NONE',  ( -1.166476076187854022E-15, 155.9449999999999932, 9.525000000000000355 ) ) ;
#10928=CARTESIAN_POINT ( 'NONE',  ( -4.716976649647097730, 112.3570736234661496, -6.492361379858953896 ) ) ;
#10930=DIRECTION ( 'NONE',  ( 0.000000000000000000, 0.000000000000000000, 1.000000000000000000 ) ) ;
#10933=ORIENTED_EDGE ( 'NONE', *, *, #21200, .F. ) ;
#10936=CARTESIAN_POINT ( 'NONE',  ( -71.50000000000000000, 36.32520566882265456, -7.500000000000000000 ) ) ;
#10940=ORIENTED_EDGE ( 'NONE', *, *, #2822, .F. ) ;
#10943=CARTESIAN_POINT ( 'NONE',  ( -45.00000000000000000, 8.092291901770513718, 5.807866024088225387 ) ) ;
#10949=CIRCLE ( 'NONE', #50285, 17.00000000000000000 ) ;
#10950=ORIENTED_EDGE ( 'NONE', *, *, #62566, .T. ) ;
#10952=VERTEX_POINT ( 'NONE', #22901 ) ;
#10954=CARTESIAN_POINT ( 'NONE',  ( -45.00000000000000000, -2.024042244987997205E-14, 10.00000000000000000 ) ) ;
#10955=CARTESIAN_POINT ( 'NONE',  ( 21.02379604162863913, 114.4999999999999574, -10.50000000000000000 ) ) ;
#10956=CARTESIAN_POINT ( 'NONE',  ( 3.094860106618431583, 123.0949999999999704, 9.525000000000000355 ) ) ;
#10957=FILL_AREA_STYLE ('',( #31356 ) ) ;
#10958=ADVANCED_FACE ( 'NONE', ( #12304 ), #52789, .F. ) ;
#10962=CARTESIAN_POINT ( 'NONE',  ( -10.01517768586949408, 129.3050000000000068, -6.132527647946036459E-16 ) ) ;
#10965=CARTESIAN_POINT ( 'NONE',  ( -71.62068965517239860, 36.41396814395972115, 9.500000000000000000 ) ) ;
#10967=CARTESIAN_POINT ( 'NONE',  ( -10.01517768586949231, 144.3049999999999784, -6.132527647946036459E-16 ) ) ;
#10969=UNCERTAINTY_MEASURE_WITH_UNIT (LENGTH_MEASURE( 1.000000000000000082E-05 ), #60412, 'distance_accuracy_value', 'NONE');
#10970=ADVANCED_FACE ( 'NONE', ( #32376 ), #30283, .F. ) ;
#10973=DIRECTION ( 'NONE',  ( 1.000000000000000000, 0.000000000000000000, 0.000000000000000000 ) ) ;
#10975=DIRECTION ( 'NONE',  ( 1.000000000000000000, 0.000000000000000000, 0.000000000000000000 ) ) ;
#10976=EDGE_CURVE ( 'NONE', #10695, #67841, #17970, .T. ) ;
#10977=CARTESIAN_POINT ( 'NONE',  ( -34.99999999999999289, 99.99999999999998579, 9.500000000000000000 ) ) ;
#10984=UNCERTAINTY_MEASURE_WITH_UNIT (LENGTH_MEASURE( 1.000000000000000082E-05 ), #41811, 'distance_accuracy_value', 'NONE');
#10986=SURFACE_SIDE_STYLE ('',( #47281 ) ) ;
#10987=DIRECTION ( 'NONE',  ( 0.000000000000000000, -1.000000000000000000, 0.000000000000000000 ) ) ;
#10988=CARTESIAN_POINT ( 'NONE',  ( -65.99999999999998579, 50.00000000000000000, 12.00000000000000000 ) ) ;
#10991=DIRECTION ( 'NONE',  ( 0.000000000000000000, 0.000000000000000000, -1.000000000000000000 ) ) ;
#10993=EDGE_LOOP ( 'NONE', ( #22972, #60205, #5155, #48683 ) ) ;
#10995=MECHANICAL_DESIGN_GEOMETRIC_PRESENTATION_REPRESENTATION('',(#1932),#61501);
#10999=( GEOMETRIC_REPRESENTATION_CONTEXT ( 3 ) GLOBAL_UNCERTAINTY_ASSIGNED_CONTEXT ( ( #46892 ) ) GLOBAL_UNIT_ASSIGNED_CONTEXT ( ( #57520, #36461, #15665 ) ) REPRESENTATION_CONTEXT ( 'NONE', 'WORKASPACE' ) );
#11000=FACE_OUTER_BOUND ( 'NONE', #38211, .T. ) ;
#11001=FILL_AREA_STYLE ('',( #26133 ) ) ;
#11003=CARTESIAN_POINT ( 'NONE',  ( 5.598654528085809545, 130.1449999999999818, -7.705886871421373741 ) ) ;
#11010=AXIS2_PLACEMENT_3D ( 'NONE', #57164, #8999, #30414 ) ;
#11020=PRESENTATION_STYLE_ASSIGNMENT (( #15640 ) ) ;
#11024=ORIENTED_EDGE ( 'NONE', *, *, #2394, .T. ) ;
#11025=DIRECTION ( 'NONE',  ( -0.000000000000000000, -0.000000000000000000, -1.000000000000000000 ) ) ;
#11026=MECHANICAL_DESIGN_GEOMETRIC_PRESENTATION_REPRESENTATION('',(#24514),#63852);
#11028=CARTESIAN_POINT ( 'NONE',  ( -9.827790563157511022E-16, 143.5570736234661524, 8.025000000000000355 ) ) ;
#11030=ORIENTED_EDGE ( 'NONE', *, *, #45504, .T. ) ;
#11031=CARTESIAN_POINT ( 'NONE',  ( 2.607480562269155921, 136.5929263765337964, 8.024999999999941735 ) ) ;
#11035=CIRCLE ( 'NONE', #35761, 0.5000000000000004441 ) ;
#11037=VECTOR ( 'NONE', #47379, 1000.000000000000000 ) ;
#11038=SURFACE_STYLE_USAGE ( .BOTH. , #33206 ) ;
#11040=SURFACE_SIDE_STYLE ('',( #26842 ) ) ;
#11042=EDGE_CURVE ( 'NONE', #23699, #6580, #6349, .T. ) ;
#11047=SURFACE_STYLE_USAGE ( .BOTH. , #21610 ) ;
#11053=ORIENTED_EDGE ( 'NONE', *, *, #12286, .T. ) ;
#11054=COLOUR_RGB ( '', 0.08235294, 0.09019608, 0.10196078) ;
#11059=ORIENTED_EDGE ( 'NONE', *, *, #53376, .T. ) ;
#11061=CARTESIAN_POINT ( 'NONE',  ( 45.50000000000000000, 99.99999999999992895, -9.500000000000000000 ) ) ;
#11063=CARTESIAN_POINT ( 'NONE',  ( -5.598654528085808657, 128.6449999999999818, 7.705886871421373741 ) ) ;
#11065=CIRCLE ( 'NONE', #34658, 8.500000000000000000 ) ;
#11066=LINE ( 'NONE', #43498, #26810 ) ;
#11068=( LENGTH_UNIT ( ) NAMED_UNIT ( * ) SI_UNIT ( .MILLI., .METRE. ) );
#11069=CARTESIAN_POINT ( 'NONE',  ( 40.99999999999998579, 107.7459666924148252, 3.000000000000000000 ) ) ;
#11073=PRESENTATION_STYLE_ASSIGNMENT (( #62470 ) ) ;
#11075=FILL_AREA_STYLE_COLOUR ( '', #35423 ) ;
#11085=SURFACE_STYLE_FILL_AREA ( #32916 ) ;
#11088=( GEOMETRIC_REPRESENTATION_CONTEXT ( 3 ) GLOBAL_UNCERTAINTY_ASSIGNED_CONTEXT ( ( #12124 ) ) GLOBAL_UNIT_ASSIGNED_CONTEXT ( ( #30999, #61685, #18470 ) ) REPRESENTATION_CONTEXT ( 'NONE', 'WORKASPACE' ) );
#11089=MECHANICAL_DESIGN_GEOMETRIC_PRESENTATION_REPRESENTATION('',(#58161),#50320);
#11091=LINE ( 'NONE', #68467, #61636 ) ;
#11093=( NAMED_UNIT ( * ) SI_UNIT ( $, .STERADIAN. ) SOLID_ANGLE_UNIT ( ) );
#11096=DIRECTION ( 'NONE',  ( 0.000000000000000000, 0.000000000000000000, -1.000000000000000000 ) ) ;
#11097=DIRECTION ( 'NONE',  ( 1.000000000000000000, 0.000000000000000000, 0.000000000000000000 ) ) ;
#11098=EDGE_CURVE ( 'NONE', #62495, #58540, #39386, .T. ) ;
#11100=EDGE_CURVE ( 'NONE', #47666, #6055, #20212, .T. ) ;
#11102=CARTESIAN_POINT ( 'NONE',  ( -4.716976649647097730, 138.2429263765338305, -6.492361379858953896 ) ) ;
#11105=B_SPLINE_CURVE_WITH_KNOTS ( 'NONE', 3,
 ( #61859, #13686, #7708, #18279, #51327, #35145, #60816, #45050, #7382, #23214, #17928, #39417, #12637, #29148, #50634, #2372, #14744, #35503, #57644, #42219, #4861, #46077, #25281, #63609, #19657, #36588, #62553, #41153, #36917, #67495, #36220, #14371 ),
 .UNSPECIFIED., .F., .F.,
 ( 4, 2, 2, 2, 2, 2, 2, 2, 2, 2, 2, 2, 2, 2, 2, 4 ),
 ( 0.001113530544794672211, 0.002431556489591745265, 0.003749582434388818754, 0.005067608379185892242, 0.006385634323982964863, 0.007703660268780037484, 0.009021686213577111840, 0.01165773810317125535, 0.01297576404796832797, 0.01429378999276540059, 0.01561181593756247668, 0.01692984188235954757, 0.01824786782715661845, 0.01956589377195369281, 0.02088391971675076370, 0.02220194566154783458 ),
 .UNSPECIFIED. ) ;
#11106=CARTESIAN_POINT ( 'NONE',  ( -6.826472737025120807, 115.5070736234661553, -4.959722759717907437 ) ) ;
#11108=VECTOR ( 'NONE', #2192, 1000.000000000000000 ) ;
#11110=CARTESIAN_POINT ( 'NONE',  ( -9.827790563157511022E-16, 137.5570736234661808, 8.025000000000000355 ) ) ;
#11119=CARTESIAN_POINT ( 'NONE',  ( -3.094860106618432471, 128.7049999999999841, -9.525000000000000355 ) ) ;
#11121=LINE ( 'NONE', #5476, #58705 ) ;
#11126=ORIENTED_EDGE ( 'NONE', *, *, #20724, .F. ) ;
#11127=VECTOR ( 'NONE', #18160, 1000.000000000000000 ) ;
#11128=DIRECTION ( 'NONE',  ( -1.000000000000000000, 0.000000000000000000, 0.000000000000000000 ) ) ;
#11132=( BOUNDED_CURVE ( )  B_SPLINE_CURVE ( 2, ( #62619, #14436, #46149, #67937, #67572, #40873, #9547, #41922, #57011, #3496, #8826 ),
 .UNSPECIFIED., .F., .T. ) 
 B_SPLINE_CURVE_WITH_KNOTS ( ( 3, 2, 2, 2, 2, 3 ),
 ( 0.8235294117647057321, 0.8294117647058822929, 0.8352941176470587425, 0.8411764705882351922, 0.8470588235294116419, 0.8529411764705880916 ),
 .UNSPECIFIED. ) 
 CURVE ( )  GEOMETRIC_REPRESENTATION_ITEM ( )  RATIONAL_B_SPLINE_CURVE ( ( 1.000000000000000888, 0.9510565162951526430, 1.000000000000000000, 0.9510565162951535312, 1.000000000000000000, 0.9510565162951535312, 1.000000000000000000, 0.9510565162951535312, 1.000000000000000000, 0.9510565162951544194, 0.9999999999999991118 ) ) 
 REPRESENTATION_ITEM ( '' )  );
#11133=CARTESIAN_POINT ( 'NONE',  ( 45.50000000000000000, -1.469576158976824618E-14, 6.500000000000000000 ) ) ;
#11137=CARTESIAN_POINT ( 'NONE',  ( -60.00000000000000000, -2.024042244987997205E-14, 10.50000000000000000 ) ) ;
#11140=DIRECTION ( 'NONE',  ( 0.000000000000000000, -1.000000000000000000, -0.000000000000000000 ) ) ;
#11141=DIRECTION ( 'NONE',  ( -0.000000000000000000, -1.000000000000000000, 0.000000000000000000 ) ) ;
#11143=COLOUR_RGB ( '', 0.66274510, 0.83137255, 0.94901961) ;
#11145=AXIS2_PLACEMENT_3D ( 'NONE', #17606, #12276, #5030 ) ;
#11149=CARTESIAN_POINT ( 'NONE',  ( -3.607123150363804154, 153.1289957264864938, -7.332553890433554322 ) ) ;
#11151=MECHANICAL_DESIGN_GEOMETRIC_PRESENTATION_REPRESENTATION('',(#56096),#62814);
#11152=ORIENTED_EDGE ( 'NONE', *, *, #13182, .T. ) ;
#11155=( NAMED_UNIT ( * ) PLANE_ANGLE_UNIT ( ) SI_UNIT ( $, .RADIAN. ) );
#11156=DIRECTION ( 'NONE',  ( -0.7833176619561877940, -0.6216216216216191581, 4.313366480807175060E-15 ) ) ;
#11157=ORIENTED_EDGE ( 'NONE', *, *, #33102, .T. ) ;
#11163=( GEOMETRIC_REPRESENTATION_CONTEXT ( 3 ) GLOBAL_UNCERTAINTY_ASSIGNED_CONTEXT ( ( #47445 ) ) GLOBAL_UNIT_ASSIGNED_CONTEXT ( ( #46314, #8995, #61394 ) ) REPRESENTATION_CONTEXT ( 'NONE', 'WORKASPACE' ) );
#11164=AXIS2_PLACEMENT_3D ( 'NONE', #41728, #20226, #37513 ) ;
#11167=EDGE_CURVE ( 'NONE', #6975, #61023, #36305, .T. ) ;
#11168=FACE_OUTER_BOUND ( 'NONE', #33698, .T. ) ;
#11169=CIRCLE ( 'NONE', #67315, 0.5000000000000004441 ) ;
#11170=CARTESIAN_POINT ( 'NONE',  ( -71.50000000000000000, 35.92875272052971525, 9.500000000000000000 ) ) ;
#11171=CARTESIAN_POINT ( 'NONE',  ( 0.000000000000000000, 114.9999999999999574, 0.000000000000000000 ) ) ;
#11173=CARTESIAN_POINT ( 'NONE',  ( -75.00000000000000000, 9.708372675170620525, 10.00000000000000000 ) ) ;
#11176=CARTESIAN_POINT ( 'NONE',  ( -5.598654528085808657, 138.7549999999999955, 7.705886871421373741 ) ) ;
#11181=STYLED_ITEM ( 'NONE', ( #44174 ), #4754 ) ;
#11188=( NAMED_UNIT ( * ) PLANE_ANGLE_UNIT ( ) SI_UNIT ( $, .RADIAN. ) );
#11192=EDGE_CURVE ( 'NONE', #2160, #32455, #20266, .T. ) ;
#11194=DIRECTION ( 'NONE',  ( 0.7071067811865543451, 0.000000000000000000, 0.7071067811865408004 ) ) ;
#11199=SURFACE_STYLE_USAGE ( .BOTH. , #45245 ) ;
#11200=EDGE_CURVE ( 'NONE', #52429, #45842, #34091, .T. ) ;
#11202=SURFACE_STYLE_FILL_AREA ( #31252 ) ;
#11203=CIRCLE ( 'NONE', #55030, 0.5000000000000004441 ) ;
#11204=DIRECTION ( 'NONE',  ( 0.000000000000000000, 0.000000000000000000, -1.000000000000000000 ) ) ;
#11205=ADVANCED_FACE ( 'NONE', ( #6313, #38030 ), #55182, .F. ) ;
#11210=LINE ( 'NONE', #37659, #23129 ) ;
#11212=PLANE ( 'NONE',  #34713 ) ;
#11213=ORIENTED_EDGE ( 'NONE', *, *, #36591, .T. ) ;
#11215=CARTESIAN_POINT ( 'NONE',  ( -9.058813317711337021, 155.0449999999999875, -2.943386871421374895 ) ) ;
#11216=VERTEX_POINT ( 'NONE', #66091 ) ;
#11217=ORIENTED_EDGE ( 'NONE', *, *, #23412, .T. ) ;
#11220=CIRCLE ( 'NONE', #4466, 0.5000000000000004441 ) ;
#11223=CARTESIAN_POINT ( 'NONE',  ( -7.632228543268607446, 132.5429263765338135, -2.479861379858953718 ) ) ;
#11224=CARTESIAN_POINT ( 'NONE',  ( -45.50000000000000000, -2.024042244987997205E-14, -6.500000000000000000 ) ) ;
#11225=CARTESIAN_POINT ( 'NONE',  ( -75.16423876665271564, 36.16671995880537338, -9.876590145901744222 ) ) ;
#11226=CARTESIAN_POINT ( 'NONE',  ( 2.607480562269075985, 125.7929263765338277, -8.025000000000000355 ) ) ;
#11227=CARTESIAN_POINT ( 'NONE',  ( -41.49999999999998579, 106.9282032302754999, -4.000000000000000000 ) ) ;
#11228=EDGE_CURVE ( 'NONE', #66508, #35623, #54832, .T. ) ;
#11230=STYLED_ITEM ( 'NONE', ( #57831 ), #20656 ) ;
#11236=FILL_AREA_STYLE_COLOUR ( '', #54625 ) ;
#11238=EDGE_CURVE ( 'NONE', #15151, #36166, #22507, .T. ) ;
#11240=CARTESIAN_POINT ( 'NONE',  ( -9.827790563157511022E-16, 116.5570736234661666, 8.025000000000000355 ) ) ;
#11241=( GEOMETRIC_REPRESENTATION_CONTEXT ( 3 ) GLOBAL_UNCERTAINTY_ASSIGNED_CONTEXT ( ( #27805 ) ) GLOBAL_UNIT_ASSIGNED_CONTEXT ( ( #222, #49193, #59720 ) ) REPRESENTATION_CONTEXT ( 'NONE', 'WORKASPACE' ) );
#11242=CARTESIAN_POINT ( 'NONE',  ( 41.36494435661962399, 107.7173713599237601, 3.929015280518105335 ) ) ;
#11244=AXIS2_PLACEMENT_3D ( 'NONE', #26905, #52993, #52650 ) ;
#11246=DIRECTION ( 'NONE',  ( 0.000000000000000000, 0.000000000000000000, -1.000000000000000000 ) ) ;
#11252=LINE ( 'NONE', #955, #22807 ) ;
#11254=AXIS2_PLACEMENT_3D ( 'NONE', #41173, #31959, #53433 ) ;
#11257=CARTESIAN_POINT ( 'NONE',  ( -83.49999999999997158, 50.00000000000000000, -11.50000000000000000 ) ) ;
#11259=VERTEX_POINT ( 'NONE', #21819 ) ;
#11260=FACE_OUTER_BOUND ( 'NONE', #3025, .T. ) ;
#11263=CARTESIAN_POINT ( 'NONE',  ( -5.598654528085806881, 154.7450000000000045, -7.705886871421374629 ) ) ;
#11269=CARTESIAN_POINT ( 'NONE',  ( -71.49999999999998579, 119.9999999999997868, -7.000000000000000000 ) ) ;
#11272=VECTOR ( 'NONE', #44026, 1000.000000000000000 ) ;
#11277=LINE ( 'NONE', #5632, #59429 ) ;
#11278=EDGE_CURVE ( 'NONE', #54731, #23185, #19100, .T. ) ;
#11281=SURFACE_STYLE_FILL_AREA ( #44038 ) ;
#11283=ORIENTED_EDGE ( 'NONE', *, *, #6435, .F. ) ;
#11286=STYLED_ITEM ( 'NONE', ( #12483 ), #33509 ) ;
#11288=SURFACE_STYLE_FILL_AREA ( #34130 ) ;
#11291=FACE_OUTER_BOUND ( 'NONE', #54414, .T. ) ;
#11295=VERTEX_POINT ( 'NONE', #54503 ) ;
#11298=CARTESIAN_POINT ( 'NONE',  ( 0.000000000000000000, 87.30187232391182306, 0.000000000000000000 ) ) ;
#11303=CARTESIAN_POINT ( 'NONE',  ( 3.094860106618435136, 133.2950000000000159, -9.525000000000000355 ) ) ;
#11306=ORIENTED_EDGE ( 'NONE', *, *, #69031, .T. ) ;
#11308=CARTESIAN_POINT ( 'NONE',  ( -3.094860106618432471, 131.7049999999999557, -9.525000000000000355 ) ) ;
#11311=CARTESIAN_POINT ( 'NONE',  ( 71.50000000000000000, 35.92875272052971525, 7.500000000000000000 ) ) ;
#11313=CARTESIAN_POINT ( 'NONE',  ( 8.102448949553183510, 149.1049999999999898, -5.886773742842746238 ) ) ;
#11315=STYLED_ITEM ( 'NONE', ( #13161 ), #14448 ) ;
#11317=CARTESIAN_POINT ( 'NONE',  ( -48.50000000000000000, 14.49137674618942562, -9.500000000000000000 ) ) ;
#11321=( LENGTH_UNIT ( ) NAMED_UNIT ( * ) SI_UNIT ( .MILLI., .METRE. ) );
#11324=MECHANICAL_DESIGN_GEOMETRIC_PRESENTATION_REPRESENTATION('',(#48469),#42860);
#11326=DIRECTION ( 'NONE',  ( 1.000000000000000000, 0.000000000000000000, 0.000000000000000000 ) ) ;
#11327=CARTESIAN_POINT ( 'NONE',  ( 54.49999999999999289, 1.797044900979284448E-15, 6.500000000000000000 ) ) ;
#11329=CARTESIAN_POINT ( 'NONE',  ( -44.99742019440035534, 9.654572671137946926, -3.431488482060549128 ) ) ;
#11332=AXIS2_PLACEMENT_3D ( 'NONE', #31789, #48713, #32835 ) ;
#11335=CARTESIAN_POINT ( 'NONE',  ( 4.716976649647099507, 144.7570736234661410, -6.492361379858953008 ) ) ;
#11339=ORIENTED_EDGE ( 'NONE', *, *, #20275, .F. ) ;
#11341=FILL_AREA_STYLE_COLOUR ( '', #45972 ) ;
#11342=( NAMED_UNIT ( * ) PLANE_ANGLE_UNIT ( ) SI_UNIT ( $, .RADIAN. ) );
#11344=CARTESIAN_POINT ( 'NONE',  ( -10.01517768586949231, 134.1949999999999932, -6.132527647946036459E-16 ) ) ;
#11348=STYLED_ITEM ( 'NONE', ( #55043 ), #17033 ) ;
#11350=CARTESIAN_POINT ( 'NONE',  ( 45.65811388300841855, 10.21937129433613478, 3.598410089384283417 ) ) ;
#11356=( NAMED_UNIT ( * ) PLANE_ANGLE_UNIT ( ) SI_UNIT ( $, .RADIAN. ) );
#11358=VERTEX_POINT ( 'NONE', #23878 ) ;
#11366=DIRECTION ( 'NONE',  ( 0.000000000000000000, 0.000000000000000000, 1.000000000000000000 ) ) ;
#11367=DIRECTION ( 'NONE',  ( 1.000000000000000000, 0.000000000000000000, 0.000000000000000000 ) ) ;
#11370=MECHANICAL_DESIGN_GEOMETRIC_PRESENTATION_REPRESENTATION('',(#41744),#17024);
#11371=( LENGTH_UNIT ( ) NAMED_UNIT ( * ) SI_UNIT ( .MILLI., .METRE. ) );
#11372=DIRECTION ( 'NONE',  ( 0.000000000000000000, 0.000000000000000000, 1.000000000000000000 ) ) ;
#11377=ORIENTED_EDGE ( 'NONE', *, *, #58298, .F. ) ;
#11382=SURFACE_SIDE_STYLE ('',( #58890 ) ) ;
#11383=CARTESIAN_POINT ( 'NONE',  ( 7.632228543268607446, 153.1570736234661751, 2.479861379858954606 ) ) ;
#11385=CARTESIAN_POINT ( 'NONE',  ( 7.632228543268608334, 137.3429263765337964, -2.479861379858951942 ) ) ;
#11387=MECHANICAL_DESIGN_GEOMETRIC_PRESENTATION_REPRESENTATION('',(#42925),#25988);
#11389=ORIENTED_EDGE ( 'NONE', *, *, #63688, .T. ) ;
#11391=MECHANICAL_DESIGN_GEOMETRIC_PRESENTATION_REPRESENTATION('',(#58598),#6929);
#11397=CIRCLE ( 'NONE', #2347, 0.5000000000000004441 ) ;
#11398=FILL_AREA_STYLE ('',( #27561 ) ) ;
#11399=AXIS2_PLACEMENT_3D ( 'NONE', #41128, #62533, #14348 ) ;
#11401=FACE_OUTER_BOUND ( 'NONE', #59850, .T. ) ;
#11403=( LENGTH_UNIT ( ) NAMED_UNIT ( * ) SI_UNIT ( .MILLI., .METRE. ) );
#11405=ORIENTED_EDGE ( 'NONE', *, *, #6903, .F. ) ;
#11409=ORIENTED_EDGE ( 'NONE', *, *, #16967, .T. ) ;
#11415=TOROIDAL_SURFACE ( 'NONE', #18193, 22.50000000000000000, 0.5000000000000000000 ) ;
#11416=CARTESIAN_POINT ( 'NONE',  ( -8.102448949553179958, 136.8949999999999534, -5.886773742842749790 ) ) ;
#11419=SURFACE_STYLE_FILL_AREA ( #43148 ) ;
#11421=( GEOMETRIC_REPRESENTATION_CONTEXT ( 3 ) GLOBAL_UNCERTAINTY_ASSIGNED_CONTEXT ( ( #37134 ) ) GLOBAL_UNIT_ASSIGNED_CONTEXT ( ( #37584, #20296, #9425 ) ) REPRESENTATION_CONTEXT ( 'NONE', 'WORKASPACE' ) );
#11423=MECHANICAL_DESIGN_GEOMETRIC_PRESENTATION_REPRESENTATION('',(#40631),#39526);
#11424=SURFACE_STYLE_FILL_AREA ( #42451 ) ;
#11426=DIRECTION ( 'NONE',  ( 0.000000000000000000, -1.000000000000000000, -0.000000000000000000 ) ) ;
#11428=DIRECTION ( 'NONE',  ( 0.000000000000000000, -0.000000000000000000, 1.000000000000000000 ) ) ;
#11433=ORIENTED_EDGE ( 'NONE', *, *, #40790, .F. ) ;
#11434=EDGE_CURVE ( 'NONE', #30747, #49901, #16133, .T. ) ;
#11435=STYLED_ITEM ( 'NONE', ( #15163 ), #54541 ) ;
#11436=UNCERTAINTY_MEASURE_WITH_UNIT (LENGTH_MEASURE( 1.000000000000000082E-05 ), #1647, 'distance_accuracy_value', 'NONE');
#11438=FILL_AREA_STYLE ('',( #53658 ) ) ;
#11439=CIRCLE ( 'NONE', #14835, 17.50000000000000000 ) ;
#11441=AXIS2_PLACEMENT_3D ( 'NONE', #29316, #19464, #18775 ) ;
#11442=CYLINDRICAL_SURFACE ( 'NONE', #32049, 0.5000000000000004441 ) ;
#11444=CYLINDRICAL_SURFACE ( 'NONE', #51172, 8.025000000000000355 ) ;
#11445=CIRCLE ( 'NONE', #41819, 16.00000000000000000 ) ;
#11447=LINE ( 'NONE', #60656, #23354 ) ;
#11448=DIRECTION ( 'NONE',  ( -0.000000000000000000, -0.000000000000000000, -1.000000000000000000 ) ) ;
#11453=ADVANCED_FACE ( 'NONE', ( #25597 ), #9807, .T. ) ;
#11458=ORIENTED_EDGE ( 'NONE', *, *, #21858, .T. ) ;
#11460=DIRECTION ( 'NONE',  ( -1.000000000000000000, 0.000000000000000000, 0.000000000000000000 ) ) ;
#11462=CARTESIAN_POINT ( 'NONE',  ( 4.716976649647096842, 113.8570736234661638, 6.492361379858953896 ) ) ;
#11463=AXIS2_PLACEMENT_3D ( 'NONE', #67556, #18994, #18343 ) ;
#11465=CARTESIAN_POINT ( 'NONE',  ( -45.50000000000000000, 99.99999999999992895, 9.500000000000000000 ) ) ;
#11466=CARTESIAN_POINT ( 'NONE',  ( 75.00000000000000000, 20.36037961002804408, -6.000000000000000000 ) ) ;
#11468=ADVANCED_FACE ( 'NONE', ( #63253 ), #34271, .F. ) ;
#11469=ORIENTED_EDGE ( 'NONE', *, *, #10012, .T. ) ;
#11474=( NAMED_UNIT ( * ) SI_UNIT ( $, .STERADIAN. ) SOLID_ANGLE_UNIT ( ) );
#11483=( NAMED_UNIT ( * ) SI_UNIT ( $, .STERADIAN. ) SOLID_ANGLE_UNIT ( ) );
#11487=DIRECTION ( 'NONE',  ( 1.000000000000000000, -7.080503983578803083E-17, 0.000000000000000000 ) ) ;
#11489=MECHANICAL_DESIGN_GEOMETRIC_PRESENTATION_REPRESENTATION('',(#55280),#51935);
#11491=ORIENTED_EDGE ( 'NONE', *, *, #62437, .F. ) ;
#11493=CARTESIAN_POINT ( 'NONE',  ( -71.99999999999998579, 64.07124727947029896, -9.500000000000000000 ) ) ;
#11497=CARTESIAN_POINT ( 'NONE',  ( 45.07697505292422591, 10.02565835097472480, 3.091949714863343246 ) ) ;
#11500=CARTESIAN_POINT ( 'NONE',  ( -8.601545703395441222, 153.5693124935650360, 0.4166762051479260820 ) ) ;
#11501=EDGE_LOOP ( 'NONE', ( #52432, #11213, #4097, #7421, #22501, #44492, #24691, #1755 ) ) ;
#11503=PRESENTATION_STYLE_ASSIGNMENT (( #27311 ) ) ;
#11504=CARTESIAN_POINT ( 'NONE',  ( 60.00000000000000000, 1.797044900979284448E-15, 11.50000000000003730 ) ) ;
#11506=VERTEX_POINT ( 'NONE', #23711 ) ;
#11507=PRESENTATION_STYLE_ASSIGNMENT (( #22073 ) ) ;
#11509=ADVANCED_FACE ( 'NONE', ( #7532 ), #38641, .T. ) ;
#11513=MECHANICAL_DESIGN_GEOMETRIC_PRESENTATION_REPRESENTATION('',(#18408),#57734);
#11518=CARTESIAN_POINT ( 'NONE',  ( 45.30708737912571848, 10.10236245970856750, 3.219298532130914658 ) ) ;
#11524=CARTESIAN_POINT ( 'NONE',  ( 5.598654528085809545, 140.2549999999999955, -7.705886871421373741 ) ) ;
#11530=UNCERTAINTY_MEASURE_WITH_UNIT (LENGTH_MEASURE( 1.000000000000000082E-05 ), #69140, 'distance_accuracy_value', 'NONE');
#11533=ADVANCED_FACE ( 'NONE', ( #21722 ), #66987, .F. ) ;
#11534=CARTESIAN_POINT ( 'NONE',  ( -4.716976649647097730, 132.2429263765338021, -6.492361379858953896 ) ) ;
#11536=AXIS2_PLACEMENT_3D ( 'NONE', #165, #64617, #43552 ) ;
#11540=ORIENTED_EDGE ( 'NONE', *, *, #49675, .F. ) ;
#11541=( LENGTH_UNIT ( ) NAMED_UNIT ( * ) SI_UNIT ( .MILLI., .METRE. ) );
#11542=DIRECTION ( 'NONE',  ( 1.000000000000000000, 0.000000000000000000, 0.000000000000000000 ) ) ;
#11543=DIRECTION ( 'NONE',  ( -0.000000000000000000, -0.000000000000000000, -1.000000000000000000 ) ) ;
#11547=VERTEX_POINT ( 'NONE', #67316 ) ;
#11550=( NAMED_UNIT ( * ) SI_UNIT ( $, .STERADIAN. ) SOLID_ANGLE_UNIT ( ) );
#11552=VERTEX_POINT ( 'NONE', #25786 ) ;
#11556=AXIS2_PLACEMENT_3D ( 'NONE', #68271, #68973, #10220 ) ;
#11557=STYLED_ITEM ( 'NONE', ( #42754 ), #61368 ) ;
#11558=CARTESIAN_POINT ( 'NONE',  ( 15.98999599679679839, 146.9999999999999716, 7.500000000000000000 ) ) ;
#11559=FILL_AREA_STYLE ('',( #39029 ) ) ;
#11565=DIRECTION ( 'NONE',  ( 0.000000000000000000, 0.000000000000000000, 1.000000000000000000 ) ) ;
#11567=ORIENTED_EDGE ( 'NONE', *, *, #61128, .F. ) ;
#11568=CARTESIAN_POINT ( 'NONE',  ( 7.632228543268608334, 137.3429263765337964, -2.479861379858951942 ) ) ;
#11574=ORIENTED_EDGE ( 'NONE', *, *, #63383, .F. ) ;
#11577=DIRECTION ( 'NONE',  ( -0.000000000000000000, 1.000000000000000000, -0.000000000000000000 ) ) ;
#11579=CIRCLE ( 'NONE', #36335, 0.5000000000000004441 ) ;
#11581=CARTESIAN_POINT ( 'NONE',  ( -71.62068965517239860, 36.41396814395972115, -9.500000000000000000 ) ) ;
#11583=ORIENTED_EDGE ( 'NONE', *, *, #7711, .F. ) ;
#11589=CARTESIAN_POINT ( 'NONE',  ( 41.68184459379349249, 107.4432011401419516, 3.569690802405922625 ) ) ;
#11590=ORIENTED_EDGE ( 'NONE', *, *, #24200, .F. ) ;
#11593=AXIS2_PLACEMENT_3D ( 'NONE', #66231, #29655, #24357 ) ;
#11594=EDGE_CURVE ( 'NONE', #65459, #47666, #9285, .T. ) ;
#11596=ORIENTED_EDGE ( 'NONE', *, *, #5633, .F. ) ;
#11597=CARTESIAN_POINT ( 'NONE',  ( -74.99999999999998579, 50.00000000000000000, -12.00000000000000000 ) ) ;
#11601=DIRECTION ( 'NONE',  ( 0.000000000000000000, -0.000000000000000000, 1.000000000000000000 ) ) ;
#11602=DIRECTION ( 'NONE',  ( 0.000000000000000000, 1.000000000000000000, -0.000000000000000000 ) ) ;
#11608=CARTESIAN_POINT ( 'NONE',  ( 12.72792206135785875, 115.4999999999999574, -10.00000000000000000 ) ) ;
#11610=DIRECTION ( 'NONE',  ( -0.000000000000000000, -0.000000000000000000, 1.000000000000000000 ) ) ;
#11615=CARTESIAN_POINT ( 'NONE',  ( 8.102448949553183510, 156.9949999999999761, -5.886773742842746238 ) ) ;
#11617=CARTESIAN_POINT ( 'NONE',  ( -6.826472737025120807, 113.1070736234661496, 4.959722759717906548 ) ) ;
#11621=LINE ( 'NONE', #22882, #35068 ) ;
#11622=UNCERTAINTY_MEASURE_WITH_UNIT (LENGTH_MEASURE( 1.000000000000000082E-05 ), #21426, 'distance_accuracy_value', 'NONE');
#11624=( GEOMETRIC_REPRESENTATION_CONTEXT ( 3 ) GLOBAL_UNCERTAINTY_ASSIGNED_CONTEXT ( ( #67771 ) ) GLOBAL_UNIT_ASSIGNED_CONTEXT ( ( #63060, #52538, #43051 ) ) REPRESENTATION_CONTEXT ( 'NONE', 'WORKASPACE' ) );
#11630=( NAMED_UNIT ( * ) SI_UNIT ( $, .STERADIAN. ) SOLID_ANGLE_UNIT ( ) );
#11633=COLOUR_RGB ( '', 0.31764706, 0.68627451, 0.89019608) ;
#11634=EDGE_CURVE ( 'NONE', #1012, #65204, #18156, .T. ) ;
#11636=CARTESIAN_POINT ( 'NONE',  ( -60.00000000000000000, -2.024042244987997205E-14, 10.50000000000000000 ) ) ;
#11638=SURFACE_STYLE_USAGE ( .BOTH. , #26750 ) ;
#11641=EDGE_LOOP ( 'NONE', ( #19200, #46554, #38379, #45358 ) ) ;
#11643=ORIENTED_EDGE ( 'NONE', *, *, #26932, .T. ) ;
#11645=VERTEX_POINT ( 'NONE', #52554 ) ;
#11646=DIRECTION ( 'NONE',  ( 0.000000000000000000, 1.000000000000000000, 0.000000000000000000 ) ) ;
#11650=CARTESIAN_POINT ( 'NONE',  ( -9.058813317711337021, 128.0449999999999875, -2.943386871421374895 ) ) ;
#11651=COLOUR_RGB ( '', 0.08235294, 0.09019608, 0.10196078) ;
#11655=CARTESIAN_POINT ( 'NONE',  ( -8.102448949553179958, 129.0049999999999670, -5.886773742842749790 ) ) ;
#11658=CARTESIAN_POINT ( 'NONE',  ( -41.12443333818656299, 107.5641524110674112, -3.336502945398625908 ) ) ;
#11659=ORIENTED_EDGE ( 'NONE', *, *, #34541, .F. ) ;
#11660=CARTESIAN_POINT ( 'NONE',  ( 9.058813317711338797, 160.9549999999999841, -2.943386871421372675 ) ) ;
#11662=UNCERTAINTY_MEASURE_WITH_UNIT (LENGTH_MEASURE( 1.000000000000000082E-05 ), #11321, 'distance_accuracy_value', 'NONE');
#11663=AXIS2_PLACEMENT_3D ( 'NONE', #535, #59677, #17159 ) ;
#11664=ADVANCED_FACE ( 'NONE', ( #18779 ), #62713, .F. ) ;
#11666=ORIENTED_EDGE ( 'NONE', *, *, #38361, .F. ) ;
#11667=AXIS2_PLACEMENT_3D ( 'NONE', #58969, #47419, #30472 ) ;
#11673=UNCERTAINTY_MEASURE_WITH_UNIT (LENGTH_MEASURE( 1.000000000000000082E-05 ), #5090, 'distance_accuracy_value', 'NONE');
#11674=FILL_AREA_STYLE_COLOUR ( '', #15599 ) ;
#11675=EDGE_CURVE ( 'NONE', #51271, #34471, #57104, .T. ) ;
#11676=CARTESIAN_POINT ( 'NONE',  ( -20.71231517720798010, 147.4999999999999716, 9.500000000000000000 ) ) ;
#11677=FILL_AREA_STYLE ('',( #1415 ) ) ;
#11678=ORIENTED_EDGE ( 'NONE', *, *, #39501, .T. ) ;
#11679=FACE_OUTER_BOUND ( 'NONE', #64029, .T. ) ;
#11683=AXIS2_PLACEMENT_3D ( 'NONE', #1724, #1368, #49630 ) ;
#11684=VERTEX_POINT ( 'NONE', #19822 ) ;
#11687=SURFACE_SIDE_STYLE ('',( #59873 ) ) ;
#11688=FACE_OUTER_BOUND ( 'NONE', #1674, .T. ) ;
#11690=( GEOMETRIC_REPRESENTATION_CONTEXT ( 3 ) GLOBAL_UNCERTAINTY_ASSIGNED_CONTEXT ( ( #40453 ) ) GLOBAL_UNIT_ASSIGNED_CONTEXT ( ( #22319, #28246, #54667 ) ) REPRESENTATION_CONTEXT ( 'NONE', 'WORKASPACE' ) );
#11693=ORIENTED_EDGE ( 'NONE', *, *, #22167, .F. ) ;
#11695=DIRECTION ( 'NONE',  ( 0.000000000000000000, 0.000000000000000000, -1.000000000000000000 ) ) ;
#11699=CARTESIAN_POINT ( 'NONE',  ( -8.102448949553181734, 133.8950000000000102, -5.886773742842749790 ) ) ;
#11701=AXIS2_PLACEMENT_3D ( 'NONE', #56018, #18743, #56739 ) ;
#11702=DIRECTION ( 'NONE',  ( 1.000000000000000000, 0.000000000000000000, 0.000000000000000000 ) ) ;
#11712=AXIS2_PLACEMENT_3D ( 'NONE', #48037, #10368, #14589 ) ;
#11715=( LENGTH_UNIT ( ) NAMED_UNIT ( * ) SI_UNIT ( .MILLI., .METRE. ) );
#11718=EDGE_CURVE ( 'NONE', #61535, #35366, #4645, .T. ) ;
#11722=DIRECTION ( 'NONE',  ( 0.000000000000000000, 0.000000000000000000, -1.000000000000000000 ) ) ;
#11724=LINE ( 'NONE', #69181, #45439 ) ;
#11730=FACE_OUTER_BOUND ( 'NONE', #54729, .T. ) ;
#11732=DIRECTION ( 'NONE',  ( -0.000000000000000000, -0.000000000000000000, 1.000000000000000000 ) ) ;
#11733=CARTESIAN_POINT ( 'NONE',  ( -7.632228543268608334, 151.9570736234661581, 2.479861379858952830 ) ) ;
#11735=ORIENTED_EDGE ( 'NONE', *, *, #44451, .F. ) ;
#11739=DIRECTION ( 'NONE',  ( 0.000000000000000000, -1.000000000000000000, 0.000000000000000000 ) ) ;
#11742=ORIENTED_EDGE ( 'NONE', *, *, #24126, .F. ) ;
#11749=CARTESIAN_POINT ( 'NONE',  ( -45.00000000000000000, 9.517485987480714726, -6.449082597785445792 ) ) ;
#11750=ORIENTED_EDGE ( 'NONE', *, *, #69176, .T. ) ;
#11751=DIRECTION ( 'NONE',  ( -0.000000000000000000, -1.000000000000000000, -0.000000000000000000 ) ) ;
#11753=ORIENTED_EDGE ( 'NONE', *, *, #23147, .F. ) ;
#11755=CARTESIAN_POINT ( 'NONE',  ( 44.99999999999999289, 10.00000000017111290, -6.065867531378238198 ) ) ;
#11756=CARTESIAN_POINT ( 'NONE',  ( -74.45892860114929590, 7.944008872641778574, 6.500000000000004441 ) ) ;
#11763=SURFACE_STYLE_FILL_AREA ( #43816 ) ;
#11769=CARTESIAN_POINT ( 'NONE',  ( -10.01517768586949408, 131.1949999999999363, -6.132527647946036459E-16 ) ) ;
#11772=LINE ( 'NONE', #38200, #66155 ) ;
#11775=COLOUR_RGB ( '', 0.08235294, 0.09019608, 0.10196078) ;
#11776=CARTESIAN_POINT ( 'NONE',  ( 51.99999999999998579, 1.797044900979284448E-15, 12.00000000000000000 ) ) ;
#11778=CARTESIAN_POINT ( 'NONE',  ( -7.632228543268607446, 130.6570736234661467, -2.479861379858953718 ) ) ;
#11782=DIRECTION ( 'NONE',  ( 0.000000000000000000, 0.000000000000000000, 1.000000000000000000 ) ) ;
#11786=CONICAL_SURFACE ( 'NONE', #26395, 5.500000000000005329, 0.7853981633974309595 ) ;
#11787=FILL_AREA_STYLE ('',( #10758 ) ) ;
#11788=DIRECTION ( 'NONE',  ( 0.000000000000000000, 0.000000000000000000, -1.000000000000000000 ) ) ;
#11789=AXIS2_PLACEMENT_3D ( 'NONE', #62819, #67776, #19576 ) ;
#11792=DIRECTION ( 'NONE',  ( 1.000000000000000000, 0.000000000000000000, 0.000000000000000000 ) ) ;
#11794=DIRECTION ( 'NONE',  ( 0.6216216216216191581, 0.7833176619561879050, 0.000000000000000000 ) ) ;
#11800=DIRECTION ( 'NONE',  ( 0.000000000000000000, 0.000000000000000000, 1.000000000000000000 ) ) ;
#11802=COLOUR_RGB ( '', 0.31764706, 0.68627451, 0.89019608) ;
#11804=EDGE_LOOP ( 'NONE', ( #27389, #46415, #30759, #13612 ) ) ;
#11808=AXIS2_PLACEMENT_3D ( 'NONE', #52375, #42523, #25593 ) ;
#11809=CARTESIAN_POINT ( 'NONE',  ( -2.607480562269073765, 127.2070736234661723, -8.025000000000000355 ) ) ;
#11810=CARTESIAN_POINT ( 'NONE',  ( 15.98999599679679839, 118.4999999999999716, 7.500000000000000000 ) ) ;
#11811=DIRECTION ( 'NONE',  ( 1.000000000000000000, 0.000000000000000000, -0.000000000000000000 ) ) ;
#11812=ORIENTED_EDGE ( 'NONE', *, *, #66553, .T. ) ;
#11813=ORIENTED_EDGE ( 'NONE', *, *, #34019, .T. ) ;
#11819=COLOUR_RGB ( '', 0.08235294, 0.09019608, 0.10196078) ;
#11821=CARTESIAN_POINT ( 'NONE',  ( 2.607480562269113733, 133.5929263765338249, 8.024999999999973710 ) ) ;
#11823=ORIENTED_EDGE ( 'NONE', *, *, #35897, .F. ) ;
#11825=EDGE_CURVE ( 'NONE', #35623, #41276, #25878, .T. ) ;
#11827=CARTESIAN_POINT ( 'NONE',  ( 45.00000000000000000, 9.639620389971918613, 7.000000000000000888 ) ) ;
#11836=ORIENTED_EDGE ( 'NONE', *, *, #45924, .F. ) ;
#11839=EDGE_LOOP ( 'NONE', ( #20965, #44004, #28833, #54101 ) ) ;
#11845=CARTESIAN_POINT ( 'NONE',  ( 34.99999999999992895, 110.4999999999999858, 10.00000000000000000 ) ) ;
#11848=DIRECTION ( 'NONE',  ( 0.000000000000000000, 0.000000000000000000, -1.000000000000000000 ) ) ;
#11851=VERTEX_POINT ( 'NONE', #39859 ) ;
#11854=FILL_AREA_STYLE_COLOUR ( '', #54808 ) ;
#11858=( NAMED_UNIT ( * ) SI_UNIT ( $, .STERADIAN. ) SOLID_ANGLE_UNIT ( ) );
#11861=DIRECTION ( 'NONE',  ( 1.000000000000000000, 0.000000000000000000, 0.000000000000000000 ) ) ;
#11866=EDGE_LOOP ( 'NONE', ( #57914, #42930 ) ) ;
#11867=SPHERICAL_SURFACE ( 'NONE', #69525, 0.5000000000000000000 ) ;
#11869=CARTESIAN_POINT ( 'NONE',  ( 0.000000000000000000, 149.9429263765338476, -8.025000000000000355 ) ) ;
#11875=CARTESIAN_POINT ( 'NONE',  ( -9.058813317711337021, 141.1549999999999727, -2.943386871421374895 ) ) ;
#11877=CIRCLE ( 'NONE', #29851, 0.5000000000000004441 ) ;
#11878=AXIS2_PLACEMENT_3D ( 'NONE', #55273, #66536, #28529 ) ;
#11882=EDGE_CURVE ( 'NONE', #39909, #4746, #55256, .T. ) ;
#11886=DIRECTION ( 'NONE',  ( 1.000000000000000000, 0.000000000000000000, 0.000000000000000000 ) ) ;
#11887=FACE_OUTER_BOUND ( 'NONE', #58265, .T. ) ;
#11891=ORIENTED_EDGE ( 'NONE', *, *, #12796, .T. ) ;
#11892=ORIENTED_EDGE ( 'NONE', *, *, #37850, .F. ) ;
#11893=DIRECTION ( 'NONE',  ( 0.000000000000000000, 0.000000000000000000, -1.000000000000000000 ) ) ;
#11894=VECTOR ( 'NONE', #32899, 1000.000000000000000 ) ;
#11898=ORIENTED_EDGE ( 'NONE', *, *, #21755, .F. ) ;
#11901=( GEOMETRIC_REPRESENTATION_CONTEXT ( 3 ) GLOBAL_UNCERTAINTY_ASSIGNED_CONTEXT ( ( #15798 ) ) GLOBAL_UNIT_ASSIGNED_CONTEXT ( ( #28420, #23189, #38014 ) ) REPRESENTATION_CONTEXT ( 'NONE', 'WORKASPACE' ) );
#11902=CARTESIAN_POINT ( 'NONE',  ( -45.50000000000000000, 99.99999999999992895, 10.00000000000000000 ) ) ;
#11904=ORIENTED_EDGE ( 'NONE', *, *, #37705, .T. ) ;
#11906=CARTESIAN_POINT ( 'NONE',  ( 0.000000000000000000, 109.9999999999999858, -10.02500000000000568 ) ) ;
#11907=ORIENTED_EDGE ( 'NONE', *, *, #35606, .F. ) ;
#11909=AXIS2_PLACEMENT_3D ( 'NONE', #12181, #18845, #55804 ) ;
#11911=CARTESIAN_POINT ( 'NONE',  ( 10.01517768586949231, 159.6949999999999648, 1.839758294383810543E-15 ) ) ;
#11914=ORIENTED_EDGE ( 'NONE', *, *, #34880, .T. ) ;
#11916=FILL_AREA_STYLE_COLOUR ( '', #59731 ) ;
#11920=CARTESIAN_POINT ( 'NONE',  ( 2.607480562269076430, 131.7929263765337851, -8.025000000000000355 ) ) ;
#11921=CYLINDRICAL_SURFACE ( 'NONE', #35690, 8.025000000000000355 ) ;
#11923=CARTESIAN_POINT ( 'NONE',  ( 8.437984349512095861, 125.1929263765338192, 1.550032578732816828E-15 ) ) ;
#11926=VERTEX_POINT ( 'NONE', #39497 ) ;
#11929=VERTEX_POINT ( 'NONE', #65859 ) ;
#11932=FILL_AREA_STYLE_COLOUR ( '', #28902 ) ;
#11936=CARTESIAN_POINT ( 'NONE',  ( -65.00000000000000000, -2.024042244987997205E-14, 6.999999999999995559 ) ) ;
#11940=EDGE_CURVE ( 'NONE', #44352, #24951, #55647, .T. ) ;
#11944=CARTESIAN_POINT ( 'NONE',  ( -44.99626276708967509, 9.641083881037339154, 3.381873653971033455 ) ) ;
#11949=CARTESIAN_POINT ( 'NONE',  ( 60.00000000000000000, 112.4999999999999858, -9.500000000000000000 ) ) ;
#11957=CARTESIAN_POINT ( 'NONE',  ( -44.99999999999977973, 146.4999999999999716, 7.000000000000000000 ) ) ;
#11958=AXIS2_PLACEMENT_3D ( 'NONE', #55082, #6539, #27988 ) ;
#11960=CARTESIAN_POINT ( 'NONE',  ( -3.094860106618434248, 158.7949999999999875, 9.525000000000000355 ) ) ;
#11963=CARTESIAN_POINT ( 'NONE',  ( -21.02379604162863913, 110.4999999999999858, 9.500000000000000000 ) ) ;
#11966=ADVANCED_FACE ( 'NONE', ( #33164 ), #5, .T. ) ;
#11968=FACE_OUTER_BOUND ( 'NONE', #37854, .T. ) ;
#11979=CARTESIAN_POINT ( 'NONE',  ( -45.50000000000000000, -2.024042244987997205E-14, -6.999999999999999112 ) ) ;
#11980=DIRECTION ( 'NONE',  ( 0.000000000000000000, -1.000000000000000000, 0.000000000000000000 ) ) ;
#11981=MECHANICAL_DESIGN_GEOMETRIC_PRESENTATION_REPRESENTATION('',(#54660),#5246);
#11987=ADVANCED_FACE ( 'NONE', ( #60232 ), #66186, .F. ) ;
#11988=EDGE_CURVE ( 'NONE', #67189, #3488, #19141, .T. ) ;
#11991=DIRECTION ( 'NONE',  ( 0.000000000000000000, 0.000000000000000000, 1.000000000000000000 ) ) ;
#11994=PRESENTATION_STYLE_ASSIGNMENT (( #50003 ) ) ;
#11995=CARTESIAN_POINT ( 'NONE',  ( 3.094860106618431583, 135.0949999999999420, 9.525000000000000355 ) ) ;
#11997=EDGE_LOOP ( 'NONE', ( #57151, #9002, #66716, #66268 ) ) ;
#11999=CARTESIAN_POINT ( 'NONE',  ( -3.094860106618432471, 134.7049999999999841, -9.525000000000000355 ) ) ;
#12004=CARTESIAN_POINT ( 'NONE',  ( -9.058813317711337021, 156.1550000000000011, -2.943386871421374895 ) ) ;
#12012=DIRECTION ( 'NONE',  ( -1.000000000000000000, 0.000000000000000000, -0.000000000000000000 ) ) ;
#12015=DIRECTION ( 'NONE',  ( 1.000000000000000000, 0.000000000000000000, 0.000000000000000000 ) ) ;
#12019=( NAMED_UNIT ( * ) PLANE_ANGLE_UNIT ( ) SI_UNIT ( $, .RADIAN. ) );
#12020=PRESENTATION_STYLE_ASSIGNMENT (( #60214 ) ) ;
#12021=CARTESIAN_POINT ( 'NONE',  ( 20.71231517720798010, 146.4999999999999716, -7.500000000000000000 ) ) ;
#12022=EDGE_CURVE ( 'NONE', #48570, #26152, #13775, .T. ) ;
#12026=( LENGTH_UNIT ( ) NAMED_UNIT ( * ) SI_UNIT ( .MILLI., .METRE. ) );
#12027=DIRECTION ( 'NONE',  ( 0.000000000000000000, 1.000000000000000000, 0.000000000000000000 ) ) ;
#12031=CARTESIAN_POINT ( 'NONE',  ( 4.716976649647096842, 143.8570736234661638, 6.492361379858953896 ) ) ;
#12034=VERTEX_POINT ( 'NONE', #41234 ) ;
#12035=SURFACE_STYLE_FILL_AREA ( #49692 ) ;
#12036=CARTESIAN_POINT ( 'NONE',  ( -1.166476076187854022E-15, 128.9449999999999648, 9.525000000000000355 ) ) ;
#12042=COLOUR_RGB ( '', 0.09019608, 0.27058824, 0.51372549) ;
#12052=DIRECTION ( 'NONE',  ( -1.000000000000000000, 0.000000000000000000, 0.000000000000000000 ) ) ;
#12055=DIRECTION ( 'NONE',  ( -0.7713892158398705234, 0.000000000000000000, -0.6363636363636357984 ) ) ;
#12056=CARTESIAN_POINT ( 'NONE',  ( 44.86929803721407239, 9.999999999999982236, -3.235899272506259639 ) ) ;
#12060=ORIENTED_EDGE ( 'NONE', *, *, #20834, .F. ) ;
#12062=EDGE_CURVE ( 'NONE', #38434, #34665, #32358, .T. ) ;
#12063=ORIENTED_EDGE ( 'NONE', *, *, #37047, .F. ) ;
#12064=EDGE_CURVE ( 'NONE', #29393, #8546, #24761, .T. ) ;
#12067=CARTESIAN_POINT ( 'NONE',  ( -60.00000000000000000, -2.024042244987997205E-14, 11.50000000000000000 ) ) ;
#12068=( LENGTH_UNIT ( ) NAMED_UNIT ( * ) SI_UNIT ( .MILLI., .METRE. ) );
#12069=CARTESIAN_POINT ( 'NONE',  ( 6.826472737025119919, 153.0070736234661126, 4.959722759717908325 ) ) ;
#12075=PRESENTATION_STYLE_ASSIGNMENT (( #48048 ) ) ;
#12076=DIRECTION ( 'NONE',  ( -0.000000000000000000, -0.000000000000000000, 1.000000000000000000 ) ) ;
#12082=PRESENTATION_STYLE_ASSIGNMENT (( #11047 ) ) ;
#12087=CARTESIAN_POINT ( 'NONE',  ( -72.49999999999998579, 1.797044900979284448E-15, -9.500000000000000000 ) ) ;
#12088=CARTESIAN_POINT ( 'NONE',  ( 65.00000000000000000, 1.797044900979284448E-15, -11.50000000000001066 ) ) ;
#12090=CIRCLE ( 'NONE', #67179, 22.50000000000000000 ) ;
#12095=DIRECTION ( 'NONE',  ( -0.000000000000000000, 1.000000000000000000, -0.000000000000000000 ) ) ;
#12096=PRESENTATION_STYLE_ASSIGNMENT (( #22671 ) ) ;
#12097=DIRECTION ( 'NONE',  ( -1.000000000000000000, 0.000000000000000000, 0.000000000000000000 ) ) ;
#12103=CARTESIAN_POINT ( 'NONE',  ( 3.094860106618431583, 129.0949999999999704, 9.525000000000000355 ) ) ;
#12105=AXIS2_PLACEMENT_3D ( 'NONE', #41535, #23678, #50423 ) ;
#12107=VERTEX_POINT ( 'NONE', #10241 ) ;
#12108=PRESENTATION_STYLE_ASSIGNMENT (( #2903 ) ) ;
#12112=FILL_AREA_STYLE ('',( #60306 ) ) ;
#12115=DIRECTION ( 'NONE',  ( 0.000000000000000000, -1.000000000000000000, 0.000000000000000000 ) ) ;
#12116=DIRECTION ( 'NONE',  ( 0.000000000000000000, -1.000000000000000000, 0.000000000000000000 ) ) ;
#12117=( NAMED_UNIT ( * ) PLANE_ANGLE_UNIT ( ) SI_UNIT ( $, .RADIAN. ) );
#12124=UNCERTAINTY_MEASURE_WITH_UNIT (LENGTH_MEASURE( 1.000000000000000082E-05 ), #30999, 'distance_accuracy_value', 'NONE');
#12129=LINE ( 'NONE', #28288, #32731 ) ;
#12133=FILL_AREA_STYLE ('',( #48789 ) ) ;
#12135=CARTESIAN_POINT ( 'NONE',  ( -41.12389261647926730, 107.5649728523252833, 3.335908204272032940 ) ) ;
#12137=CIRCLE ( 'NONE', #48102, 0.5000000000000004441 ) ;
#12139=ADVANCED_FACE ( 'NONE', ( #64736 ), #68990, .T. ) ;
#12143=EDGE_LOOP ( 'NONE', ( #30857, #17974, #36155, #37342 ) ) ;
#12145=AXIS2_PLACEMENT_3D ( 'NONE', #67695, #40993, #39609 ) ;
#12146=CARTESIAN_POINT ( 'NONE',  ( -4.716976649647097730, 121.3570736234661638, -6.492361379858953896 ) ) ;
#12147=CARTESIAN_POINT ( 'NONE',  ( 2.607480562269155921, 137.7070736234661297, 8.024999999999941735 ) ) ;
#12153=ORIENTED_EDGE ( 'NONE', *, *, #60605, .T. ) ;
#12157=VERTEX_POINT ( 'NONE', #69329 ) ;
#12158=CARTESIAN_POINT ( 'NONE',  ( 45.00000000000000711, 9.639620389971920389, 6.500000000000007105 ) ) ;
#12164=CARTESIAN_POINT ( 'NONE',  ( 12.72792206135785698, 115.4999999999999574, 10.50000000000000000 ) ) ;
#12165=VERTEX_POINT ( 'NONE', #58766 ) ;
#12171=AXIS2_PLACEMENT_3D ( 'NONE', #66137, #11646, #60180 ) ;
#12179=( NAMED_UNIT ( * ) PLANE_ANGLE_UNIT ( ) SI_UNIT ( $, .RADIAN. ) );
#12181=CARTESIAN_POINT ( 'NONE',  ( 24.21231517720798010, 113.4999999999999858, -7.500000000000000000 ) ) ;
#12182=SURFACE_SIDE_STYLE ('',( #48845 ) ) ;
#12184=VERTEX_POINT ( 'NONE', #47928 ) ;
#12190=ORIENTED_EDGE ( 'NONE', *, *, #23461, .F. ) ;
#12192=CARTESIAN_POINT ( 'NONE',  ( 45.61109309484437802, 10.20369769828145579, 3.650011426053806574 ) ) ;
#12198=CARTESIAN_POINT ( 'NONE',  ( 9.058813317711337021, 145.6549999999999727, 2.943386871421375783 ) ) ;
#12201=UNCERTAINTY_MEASURE_WITH_UNIT (LENGTH_MEASURE( 1.000000000000000082E-05 ), #15648, 'distance_accuracy_value', 'NONE');
#12202=FACE_OUTER_BOUND ( 'NONE', #39790, .T. ) ;
#12205=DIRECTION ( 'NONE',  ( 0.000000000000000000, 0.000000000000000000, 1.000000000000000000 ) ) ;
#12207=STYLED_ITEM ( 'NONE', ( #19890 ), #42555 ) ;
#12208=CARTESIAN_POINT ( 'NONE',  ( 20.57648123223228254, 114.4999999999999574, -10.27659574468085069 ) ) ;
#12213=SURFACE_STYLE_USAGE ( .BOTH. , #61438 ) ;
#12216=EDGE_LOOP ( 'NONE', ( #20202, #29225, #20468, #18400 ) ) ;
#12217=FILL_AREA_STYLE ('',( #60749 ) ) ;
#12218=EDGE_CURVE ( 'NONE', #31971, #44642, #61876, .T. ) ;
#12219=AXIS2_PLACEMENT_3D ( 'NONE', #66339, #28337, #34670 ) ;
#12221=CARTESIAN_POINT ( 'NONE',  ( 21.02379604162863913, 110.4999999999999858, -10.50000000000000000 ) ) ;
#12227=SURFACE_SIDE_STYLE ('',( #911 ) ) ;
#12229=VERTEX_POINT ( 'NONE', #12636 ) ;
#12230=DIRECTION ( 'NONE',  ( 0.000000000000000000, 0.000000000000000000, 1.000000000000000000 ) ) ;
#12231=CARTESIAN_POINT ( 'NONE',  ( 15.98999599679679839, 118.4999999999999716, -7.500000000000000000 ) ) ;
#12234=SURFACE_STYLE_USAGE ( .BOTH. , #60427 ) ;
#12236=ORIENTED_EDGE ( 'NONE', *, *, #57961, .T. ) ;
#12239=CARTESIAN_POINT ( 'NONE',  ( -8.313367756837561018, 110.4999999999999858, -4.669448307627880546 ) ) ;
#12241=FILL_AREA_STYLE_COLOUR ( '', #30760 ) ;
#12242=ORIENTED_EDGE ( 'NONE', *, *, #8275, .T. ) ;
#12243=CARTESIAN_POINT ( 'NONE',  ( -2.607480562269075097, 139.2929263765338419, 8.025000000000000355 ) ) ;
#12247=LINE ( 'NONE', #38359, #57567 ) ;
#12253=CARTESIAN_POINT ( 'NONE',  ( -75.46551724137930250, 63.49197145334878201, 9.500000000000001776 ) ) ;
#12255=VERTEX_POINT ( 'NONE', #11608 ) ;
#12257=CARTESIAN_POINT ( 'NONE',  ( 0.000000000000000000, 115.0570736234661666, -8.025000000000000355 ) ) ;
#12264=ORIENTED_EDGE ( 'NONE', *, *, #20898, .F. ) ;
#12265=( LENGTH_UNIT ( ) NAMED_UNIT ( * ) SI_UNIT ( .MILLI., .METRE. ) );
#12266=( NAMED_UNIT ( * ) PLANE_ANGLE_UNIT ( ) SI_UNIT ( $, .RADIAN. ) );
#12268=VECTOR ( 'NONE', #52978, 1000.000000000000000 ) ;
#12276=DIRECTION ( 'NONE',  ( 0.000000000000000000, 3.118022522272251586E-15, -1.000000000000000000 ) ) ;
#12283=CARTESIAN_POINT ( 'NONE',  ( -9.058813317711337021, 111.1549999999999869, -2.943386871421374895 ) ) ;
#12286=EDGE_CURVE ( 'NONE', #6589, #6975, #22870, .T. ) ;
#12288=SURFACE_STYLE_FILL_AREA ( #28460 ) ;
#12290=UNCERTAINTY_MEASURE_WITH_UNIT (LENGTH_MEASURE( 1.000000000000000082E-05 ), #56295, 'distance_accuracy_value', 'NONE');
#12293=CARTESIAN_POINT ( 'NONE',  ( -24.21231517720798010, 112.9999999999999858, 7.000000000000000000 ) ) ;
#12294=ORIENTED_EDGE ( 'NONE', *, *, #12064, .T. ) ;
#12297=VECTOR ( 'NONE', #12116, 1000.000000000000000 ) ;
#12304=FACE_OUTER_BOUND ( 'NONE', #58519, .T. ) ;
#12308=( LENGTH_UNIT ( ) NAMED_UNIT ( * ) SI_UNIT ( .MILLI., .METRE. ) );
#12313=ORIENTED_EDGE ( 'NONE', *, *, #13321, .F. ) ;
#12314=DIRECTION ( 'NONE',  ( 1.000000000000000000, 0.000000000000000000, 0.000000000000000000 ) ) ;
#12315=FACE_OUTER_BOUND ( 'NONE', #27209, .T. ) ;
#12316=VERTEX_POINT ( 'NONE', #55559 ) ;
#12320=CARTESIAN_POINT ( 'NONE',  ( 5.598654528085809545, 130.1449999999999818, -7.705886871421373741 ) ) ;
#12321=FILL_AREA_STYLE_COLOUR ( '', #36282 ) ;
#12324=CARTESIAN_POINT ( 'NONE',  ( 5.598654528085805993, 130.3549999999999898, 7.705886871421374629 ) ) ;
#12328=CARTESIAN_POINT ( 'NONE',  ( -3.094860106618434248, 159.9050000000000011, 9.525000000000000355 ) ) ;
#12329=CARTESIAN_POINT ( 'NONE',  ( 34.99999999999992895, 109.9999999999999858, 9.500000000000000000 ) ) ;
#12330=UNCERTAINTY_MEASURE_WITH_UNIT (LENGTH_MEASURE( 1.000000000000000082E-05 ), #27814, 'distance_accuracy_value', 'NONE');
#12331=AXIS2_PLACEMENT_3D ( 'NONE', #60069, #54440, #11886 ) ;
#12332=EDGE_CURVE ( 'NONE', #38874, #11216, #51813, .T. ) ;
#12336=EDGE_LOOP ( 'NONE', ( #29496, #27081, #38362, #7674 ) ) ;
#12337=PRESENTATION_STYLE_ASSIGNMENT (( #60524 ) ) ;
#12338=EDGE_LOOP ( 'NONE', ( #29419, #59590, #11126, #32841 ) ) ;
#12344=DIRECTION ( 'NONE',  ( 0.000000000000000000, 0.000000000000000000, -1.000000000000000000 ) ) ;
#12345=UNCERTAINTY_MEASURE_WITH_UNIT (LENGTH_MEASURE( 1.000000000000000082E-05 ), #30522, 'distance_accuracy_value', 'NONE');
#12346=STYLED_ITEM ( 'NONE', ( #15544 ), #16264 ) ;
#12347=EDGE_CURVE ( 'NONE', #29858, #43604, #10770, .T. ) ;
#12351=ORIENTED_EDGE ( 'NONE', *, *, #11940, .F. ) ;
#12353=ORIENTED_EDGE ( 'NONE', *, *, #66305, .F. ) ;
#12358=LINE ( 'NONE', #55283, #41940 ) ;
#12359=AXIS2_PLACEMENT_3D ( 'NONE', #66801, #17594, #40091 ) ;
#12361=DIRECTION ( 'NONE',  ( 1.000000000000000000, 0.000000000000000000, 0.000000000000000000 ) ) ;
#12365=SURFACE_STYLE_USAGE ( .BOTH. , #50372 ) ;
#12370=CARTESIAN_POINT ( 'NONE',  ( 9.058813317711338797, 126.8449999999999847, -2.943386871421372675 ) ) ;
#12375=VECTOR ( 'NONE', #47158, 1000.000000000000000 ) ;
#12376=CARTESIAN_POINT ( 'NONE',  ( -20.71231517720798010, 149.9999999999999716, 9.500000000000000000 ) ) ;
#12380=CIRCLE ( 'NONE', #37151, 8.000000000000007105 ) ;
#12385=VERTEX_POINT ( 'NONE', #14040 ) ;
#12389=CARTESIAN_POINT ( 'NONE',  ( -45.75849432247279935, 8.825695369645321975, 6.400617768950438879 ) ) ;
#12395=CARTESIAN_POINT ( 'NONE',  ( 44.48123910951614590, 9.999999999999978684, -3.378119344631853149 ) ) ;
#12402=DIRECTION ( 'NONE',  ( 0.000000000000000000, 1.000000000000000000, -0.000000000000000000 ) ) ;
#12404=VECTOR ( 'NONE', #5865, 1000.000000000000000 ) ;
#12405=FACE_BOUND ( 'NONE', #55139, .T. ) ;
#12406=CARTESIAN_POINT ( 'NONE',  ( -7.632228543268607446, 148.6570736234661751, -2.479861379858953718 ) ) ;
#12407=ORIENTED_EDGE ( 'NONE', *, *, #63722, .T. ) ;
#12410=CARTESIAN_POINT ( 'NONE',  ( -4.716976649647098618, 122.2570736234661553, 6.492361379858953008 ) ) ;
#12411=CARTESIAN_POINT ( 'NONE',  ( 9.058813317711337021, 130.6550000000000011, 2.943386871421375783 ) ) ;
#12414=FACE_OUTER_BOUND ( 'NONE', #47618, .T. ) ;
#12417=COLOUR_RGB ( '', 0.66274510, 0.83137255, 0.94901961) ;
#12421=VERTEX_POINT ( 'NONE', #61498 ) ;
#12425=DIRECTION ( 'NONE',  ( 0.000000000000000000, 0.000000000000000000, 1.000000000000000000 ) ) ;
#12426=CARTESIAN_POINT ( 'NONE',  ( -44.99999999999998579, 8.254931070086806599, -5.606557580296886556 ) ) ;
#12433=CARTESIAN_POINT ( 'NONE',  ( -74.11226636805670864, 9.324829141677559718, 6.185705318536756536 ) ) ;
#12435=ORIENTED_EDGE ( 'NONE', *, *, #10722, .F. ) ;
#12436=CARTESIAN_POINT ( 'NONE',  ( -6.826472737025120807, 119.1070736234661496, 4.959722759717906548 ) ) ;
#12437=DIRECTION ( 'NONE',  ( 1.000000000000000000, 0.000000000000000000, 0.000000000000000000 ) ) ;
#12438=( LENGTH_UNIT ( ) NAMED_UNIT ( * ) SI_UNIT ( .MILLI., .METRE. ) );
#12440=PRESENTATION_STYLE_ASSIGNMENT (( #62299 ) ) ;
#12442=DIRECTION ( 'NONE',  ( 1.000000000000000000, 0.000000000000000000, 0.000000000000000000 ) ) ;
#12443=CIRCLE ( 'NONE', #31524, 23.00000000000000000 ) ;
#12444=CARTESIAN_POINT ( 'NONE',  ( 9.058813317711337021, 132.5449999999999875, 2.943386871421375783 ) ) ;
#12447=EDGE_CURVE ( 'NONE', #46073, #41197, #39764, .T. ) ;
#12455=PLANE ( 'NONE',  #26837 ) ;
#12459=DIRECTION ( 'NONE',  ( -0.000000000000000000, -0.000000000000000000, 1.000000000000000000 ) ) ;
#12460=ORIENTED_EDGE ( 'NONE', *, *, #45772, .T. ) ;
#12462=PRESENTATION_STYLE_ASSIGNMENT (( #27243 ) ) ;
#12465=FACE_OUTER_BOUND ( 'NONE', #17211, .T. ) ;
#12466=VECTOR ( 'NONE', #28809, 1000.000000000000000 ) ;
#12472=CARTESIAN_POINT ( 'NONE',  ( 51.99999999999998579, 1.797044900979284448E-15, -10.49999999999999822 ) ) ;
#12473=( NAMED_UNIT ( * ) SI_UNIT ( $, .STERADIAN. ) SOLID_ANGLE_UNIT ( ) );
#12474=( NAMED_UNIT ( * ) PLANE_ANGLE_UNIT ( ) SI_UNIT ( $, .RADIAN. ) );
#12480=TOROIDAL_SURFACE ( 'NONE', #19246, 8.500000000000012434, 0.5000000000000000000 ) ;
#12482=FILL_AREA_STYLE_COLOUR ( '', #38239 ) ;
#12483=PRESENTATION_STYLE_ASSIGNMENT (( #2212 ) ) ;
#12484=CARTESIAN_POINT ( 'NONE',  ( 60.00000000000000000, 1.797044900979284448E-15, 10.50000000000000000 ) ) ;
#12489=LINE ( 'NONE', #33950, #18310 ) ;
#12491=ADVANCED_FACE ( 'NONE', ( #48161 ), #14742, .T. ) ;
#12493=CARTESIAN_POINT ( 'NONE',  ( -2.607480562269075097, 125.4070736234661609, 8.025000000000000355 ) ) ;
#12494=SURFACE_STYLE_FILL_AREA ( #27623 ) ;
#12498=LINE ( 'NONE', #2231, #59661 ) ;
#12503=ORIENTED_EDGE ( 'NONE', *, *, #44371, .F. ) ;
#12505=STYLED_ITEM ( 'NONE', ( #57511 ), #45698 ) ;
#12507=MECHANICAL_DESIGN_GEOMETRIC_PRESENTATION_REPRESENTATION('',(#65298),#38395);
#12508=SURFACE_STYLE_USAGE ( .BOTH. , #33298 ) ;
#12513=VERTEX_POINT ( 'NONE', #6935 ) ;
#12514=EDGE_CURVE ( 'NONE', #7755, #18998, #37312, .T. ) ;
#12515=CIRCLE ( 'NONE', #8012, 0.5000000000000004441 ) ;
#12516=DIRECTION ( 'NONE',  ( -1.099520432716498623E-15, 1.000000000000000000, 1.099520432716496848E-15 ) ) ;
#12520=CARTESIAN_POINT ( 'NONE',  ( 60.00000000000000000, 1.797044900979284448E-15, -7.000000000000017764 ) ) ;
#12522=MECHANICAL_DESIGN_GEOMETRIC_PRESENTATION_REPRESENTATION('',(#6960),#6912);
#12523=CARTESIAN_POINT ( 'NONE',  ( 21.02379604162863913, 109.9999999999999858, -10.50000000000000000 ) ) ;
#12524=DIRECTION ( 'NONE',  ( 0.000000000000000000, 0.000000000000000000, 1.000000000000000000 ) ) ;
#12527=ADVANCED_FACE ( 'NONE', ( #6566 ), #17526, .F. ) ;
#12531=CARTESIAN_POINT ( 'NONE',  ( -9.827790563157511022E-16, 121.4429263765338050, 8.025000000000000355 ) ) ;
#12532=SURFACE_SIDE_STYLE ('',( #66009 ) ) ;
#12533=FACE_OUTER_BOUND ( 'NONE', #57687, .T. ) ;
#12534=CARTESIAN_POINT ( 'NONE',  ( -71.49999999999998579, 64.07124727947029896, 9.500000000000000000 ) ) ;
#12535=ORIENTED_EDGE ( 'NONE', *, *, #41702, .F. ) ;
#12537=MECHANICAL_DESIGN_GEOMETRIC_PRESENTATION_REPRESENTATION('',(#64210),#10362);
#12546=CARTESIAN_POINT ( 'NONE',  ( 45.65811388300841855, 10.21937129433613478, 4.000000000000000000 ) ) ;
#12552=CARTESIAN_POINT ( 'NONE',  ( 8.102448949553181734, 145.5049999999999670, 5.886773742842750679 ) ) ;
#12556=CIRCLE ( 'NONE', #14857, 5.499999999999976907 ) ;
#12557=CIRCLE ( 'NONE', #39580, 1.000000000000000888 ) ;
#12558=DIRECTION ( 'NONE',  ( -1.000000000000000000, 0.000000000000000000, 0.000000000000000000 ) ) ;
#12561=AXIS2_PLACEMENT_3D ( 'NONE', #66393, #62501, #46018 ) ;
#12562=CARTESIAN_POINT ( 'NONE',  ( 0.000000000000000000, 114.9999999999999574, 0.000000000000000000 ) ) ;
#12563=SURFACE_STYLE_FILL_AREA ( #45675 ) ;
#12565=ORIENTED_EDGE ( 'NONE', *, *, #6006, .T. ) ;
#12566=CARTESIAN_POINT ( 'NONE',  ( -4.716976649647097730, 135.2429263765338305, -6.492361379858953896 ) ) ;
#12571=CARTESIAN_POINT ( 'NONE',  ( 15.98999599679679839, 99.99999999999998579, -7.000000000000000000 ) ) ;
#12572=CARTESIAN_POINT ( 'NONE',  ( 34.99999999999999289, 99.99999999999997158, 4.000000000000000000 ) ) ;
#12573=( GEOMETRIC_REPRESENTATION_CONTEXT ( 3 ) GLOBAL_UNCERTAINTY_ASSIGNED_CONTEXT ( ( #8168 ) ) GLOBAL_UNIT_ASSIGNED_CONTEXT ( ( #54097, #68312, #59041 ) ) REPRESENTATION_CONTEXT ( 'NONE', 'WORKASPACE' ) );
#12577=ORIENTED_EDGE ( 'NONE', *, *, #21455, .F. ) ;
#12579=LINE ( 'NONE', #11902, #32113 ) ;
#12584=ORIENTED_EDGE ( 'NONE', *, *, #41201, .T. ) ;
#12588=VERTEX_POINT ( 'NONE', #40714 ) ;
#12592=SURFACE_STYLE_USAGE ( .BOTH. , #65387 ) ;
#12595=CARTESIAN_POINT ( 'NONE',  ( -7.632228543268608334, 135.8429263765337964, 2.479861379858952830 ) ) ;
#12596=DIRECTION ( 'NONE',  ( -0.000000000000000000, 1.000000000000000000, -0.000000000000000000 ) ) ;
#12599=DIRECTION ( 'NONE',  ( -0.000000000000000000, -0.000000000000000000, -1.000000000000000000 ) ) ;
#12600=CARTESIAN_POINT ( 'NONE',  ( 72.50000000000000000, 36.32520566882265456, -10.00000000000000000 ) ) ;
#12606=CARTESIAN_POINT ( 'NONE',  ( -4.716976649647097730, 139.3570736234661638, -6.492361379858953896 ) ) ;
#12616=VERTEX_POINT ( 'NONE', #13950 ) ;
#12617=CIRCLE ( 'NONE', #32875, 0.5000000000000004441 ) ;
#12619=SURFACE_STYLE_USAGE ( .BOTH. , #61485 ) ;
#12625=CARTESIAN_POINT ( 'NONE',  ( -45.00000000000000000, 9.708372675170618749, 10.00000000000000000 ) ) ;
#12629=ADVANCED_FACE ( 'NONE', ( #34368, #35419 ), #29057, .F. ) ;
#12634=EDGE_CURVE ( 'NONE', #49593, #40233, #1934, .T. ) ;
#12636=CARTESIAN_POINT ( 'NONE',  ( 0.000000000000000000, 134.9429263765338192, -8.025000000000000355 ) ) ;
#12637=CARTESIAN_POINT ( 'NONE',  ( 6.724456118907052193, 154.5000000000000853, -6.760243897016276371 ) ) ;
#12638=CARTESIAN_POINT ( 'NONE',  ( 52.49999999999998579, 2.715530000339800426E-15, 11.50000000000000000 ) ) ;
#12641=CONICAL_SURFACE ( 'NONE', #17205, 5.499999999999976907, 0.7853981633974300713 ) ;
#12643=CARTESIAN_POINT ( 'NONE',  ( 10.01517768586949231, 121.8049999999999784, 1.839758294383810543E-15 ) ) ;
#12645=CIRCLE ( 'NONE', #41934, 0.5000000000000004441 ) ;
#12646=CARTESIAN_POINT ( 'NONE',  ( 0.9728900412908074724, 111.9999999999999858, -7.965808808122197604 ) ) ;
#12651=ORIENTED_EDGE ( 'NONE', *, *, #18019, .F. ) ;
#12653=MECHANICAL_DESIGN_GEOMETRIC_PRESENTATION_REPRESENTATION('',(#43050),#37432);
#12656=( GEOMETRIC_REPRESENTATION_CONTEXT ( 3 ) GLOBAL_UNCERTAINTY_ASSIGNED_CONTEXT ( ( #23001 ) ) GLOBAL_UNIT_ASSIGNED_CONTEXT ( ( #60531, #54903, #7771 ) ) REPRESENTATION_CONTEXT ( 'NONE', 'WORKASPACE' ) );
#12657=FILL_AREA_STYLE_COLOUR ( '', #9351 ) ;
#12661=DIRECTION ( 'NONE',  ( 0.000000000000000000, 0.000000000000000000, 1.000000000000000000 ) ) ;
#12663=FILL_AREA_STYLE_COLOUR ( '', #7970 ) ;
#12665=STYLED_ITEM ( 'NONE', ( #1826 ), #23821 ) ;
#12670=ORIENTED_EDGE ( 'NONE', *, *, #65724, .F. ) ;
#12672=DIRECTION ( 'NONE',  ( -0.000000000000000000, -1.000000000000000000, -0.000000000000000000 ) ) ;
#12673=( NAMED_UNIT ( * ) SI_UNIT ( $, .STERADIAN. ) SOLID_ANGLE_UNIT ( ) );
#12674=AXIS2_PLACEMENT_3D ( 'NONE', #10880, #69612, #41891 ) ;
#12677=CARTESIAN_POINT ( 'NONE',  ( -9.058813317711338797, 131.3449999999999989, 2.943386871421373563 ) ) ;
#12681=CARTESIAN_POINT ( 'NONE',  ( 9.058813317711337021, 142.6549999999999727, 2.943386871421375783 ) ) ;
#12683=CARTESIAN_POINT ( 'NONE',  ( 41.68104242135559190, 107.4439537334017984, -3.570039632082178116 ) ) ;
#12685=CARTESIAN_POINT ( 'NONE',  ( 10.01517768586949231, 160.8049999999999216, 1.839758294383810543E-15 ) ) ;
#12692=STYLED_ITEM ( 'NONE', ( #32193 ), #19531 ) ;
#12695=CARTESIAN_POINT ( 'NONE',  ( 23.71231517720798365, 117.4999999999999716, -10.00000000000000000 ) ) ;
#12703=CONICAL_SURFACE ( 'NONE', #21695, 5.500000000000005329, 0.7853981633974579379 ) ;
#12704=PRESENTATION_STYLE_ASSIGNMENT (( #49676 ) ) ;
#12705=FILL_AREA_STYLE_COLOUR ( '', #19757 ) ;
#12707=ADVANCED_FACE ( 'NONE', ( #29785 ), #37184, .F. ) ;
#12710=CARTESIAN_POINT ( 'NONE',  ( -45.91547277936962956, 9.430195807687217879, -3.508932040081443660 ) ) ;
#12713=EDGE_CURVE ( 'NONE', #6337, #31668, #21514, .T. ) ;
#12714=EDGE_CURVE ( 'NONE', #11684, #22849, #60813, .T. ) ;
#12715=COLOUR_RGB ( '', 0.72549020, 0.75294118, 0.79215686) ;
#12720=MECHANICAL_DESIGN_GEOMETRIC_PRESENTATION_REPRESENTATION('',(#311),#11624);
#12724=FILL_AREA_STYLE ('',( #45133 ) ) ;
#12725=DIRECTION ( 'NONE',  ( -1.000000000000000000, 0.000000000000000000, 0.000000000000000000 ) ) ;
#12728=CARTESIAN_POINT ( 'NONE',  ( -5.598654528085808657, 140.6449999999999818, 7.705886871421373741 ) ) ;
#12732=DIRECTION ( 'NONE',  ( 6.938893903907222067E-15, 0.000000000000000000, 1.000000000000000000 ) ) ;
#12733=( LENGTH_UNIT ( ) NAMED_UNIT ( * ) SI_UNIT ( .MILLI., .METRE. ) );
#12738=VECTOR ( 'NONE', #48294, 1000.000000000000000 ) ;
#12748=DIRECTION ( 'NONE',  ( 1.000000000000000000, 0.000000000000000000, 0.000000000000000000 ) ) ;
#12753=CARTESIAN_POINT ( 'NONE',  ( 20.57648123223228254, 114.4999999999999574, 10.27659574468085069 ) ) ;
#12754=MECHANICAL_DESIGN_GEOMETRIC_PRESENTATION_REPRESENTATION('',(#54341),#2630);
#12755=VECTOR ( 'NONE', #68581, 1000.000000000000000 ) ;
#12756=DIRECTION ( 'NONE',  ( -1.000000000000000000, 0.000000000000000000, 0.000000000000000000 ) ) ;
#12757=SURFACE_SIDE_STYLE ('',( #28922 ) ) ;
#12758=CARTESIAN_POINT ( 'NONE',  ( 4.716976649647096842, 149.8570736234661638, 6.492361379858953896 ) ) ;
#12759=( GEOMETRIC_REPRESENTATION_CONTEXT ( 3 ) GLOBAL_UNCERTAINTY_ASSIGNED_CONTEXT ( ( #3703 ) ) GLOBAL_UNIT_ASSIGNED_CONTEXT ( ( #703, #1041, #38802 ) ) REPRESENTATION_CONTEXT ( 'NONE', 'WORKASPACE' ) );
#12760=ORIENTED_EDGE ( 'NONE', *, *, #23132, .T. ) ;
#12761=AXIS2_PLACEMENT_3D ( 'NONE', #60943, #28583, #29986 ) ;
#12762=DIRECTION ( 'NONE',  ( -0.9704308468600219006, -0.2413793103448194366, 0.000000000000000000 ) ) ;
#12765=CARTESIAN_POINT ( 'NONE',  ( -4.716976649647097730, 121.3570736234661638, -6.492361379858953896 ) ) ;
#12766=CARTESIAN_POINT ( 'NONE',  ( -1.166476076187854022E-15, 130.0549999999999784, 9.525000000000000355 ) ) ;
#12769=EDGE_CURVE ( 'NONE', #44423, #14638, #66392, .T. ) ;
#12776=ORIENTED_EDGE ( 'NONE', *, *, #68555, .T. ) ;
#12778=CARTESIAN_POINT ( 'NONE',  ( -74.99999999999998579, 50.00000000000000000, 6.500000000000000000 ) ) ;
#12783=EDGE_CURVE ( 'NONE', #197, #37399, #68823, .T. ) ;
#12789=ORIENTED_EDGE ( 'NONE', *, *, #8990, .T. ) ;
#12791=AXIS2_PLACEMENT_3D ( 'NONE', #54446, #897, #43941 ) ;
#12792=CARTESIAN_POINT ( 'NONE',  ( -75.00000000000000000, 9.581012678897810275, 6.371410634540560558 ) ) ;
#12795=SURFACE_STYLE_USAGE ( .BOTH. , #7189 ) ;
#12796=EDGE_CURVE ( 'NONE', #58139, #44514, #58712, .T. ) ;
#12797=FILL_AREA_STYLE ('',( #45202 ) ) ;
#12801=CARTESIAN_POINT ( 'NONE',  ( 5.598654528085805993, 138.2449999999999761, 7.705886871421374629 ) ) ;
#12804=ADVANCED_FACE ( 'NONE', ( #42463 ), #63860, .T. ) ;
#12806=ORIENTED_EDGE ( 'NONE', *, *, #26813, .T. ) ;
#12808=( LENGTH_UNIT ( ) NAMED_UNIT ( * ) SI_UNIT ( .MILLI., .METRE. ) );
#12810=CIRCLE ( 'NONE', #49887, 1.000000000000000888 ) ;
#12816=( GEOMETRIC_REPRESENTATION_CONTEXT ( 3 ) GLOBAL_UNCERTAINTY_ASSIGNED_CONTEXT ( ( #57921 ) ) GLOBAL_UNIT_ASSIGNED_CONTEXT ( ( #61028, #26514, #20195 ) ) REPRESENTATION_CONTEXT ( 'NONE', 'WORKASPACE' ) );
#12820=CARTESIAN_POINT ( 'NONE',  ( 71.99999999999998579, 119.9999999999997868, -7.500000000000000000 ) ) ;
#12822=( NAMED_UNIT ( * ) SI_UNIT ( $, .STERADIAN. ) SOLID_ANGLE_UNIT ( ) );
#12829=AXIS2_PLACEMENT_3D ( 'NONE', #12520, #7269, #28696 ) ;
#12830=DIRECTION ( 'NONE',  ( -0.000000000000000000, 1.000000000000000000, 0.000000000000000000 ) ) ;
#12831=CARTESIAN_POINT ( 'NONE',  ( 21.02379604162863913, 110.4999999999999858, 10.50000000000000000 ) ) ;
#12839=DIRECTION ( 'NONE',  ( -0.000000000000000000, 0.000000000000000000, 1.000000000000000000 ) ) ;
#12840=CARTESIAN_POINT ( 'NONE',  ( -40.82708550458224295, 108.1272155206434320, 3.301554093733328088 ) ) ;
#12844=FILL_AREA_STYLE_COLOUR ( '', #44429 ) ;
#12845=( NAMED_UNIT ( * ) PLANE_ANGLE_UNIT ( ) SI_UNIT ( $, .RADIAN. ) );
#12847=SURFACE_SIDE_STYLE ('',( #29728 ) ) ;
#12848=CARTESIAN_POINT ( 'NONE',  ( -6.826472737025120807, 122.1070736234661780, 4.959722759717906548 ) ) ;
#12850=COLOUR_RGB ( '', 0.31764706, 0.68627451, 0.89019608) ;
#12852=FACE_OUTER_BOUND ( 'NONE', #14407, .T. ) ;
#12853=CARTESIAN_POINT ( 'NONE',  ( 74.52070078832288402, 19.38218994716114452, -6.500000000000000888 ) ) ;
#12861=FILL_AREA_STYLE ('',( #61039 ) ) ;
#12870=EDGE_CURVE ( 'NONE', #31971, #11259, #18198, .T. ) ;
#12872=AXIS2_PLACEMENT_3D ( 'NONE', #67352, #19148, #8966 ) ;
#12875=ORIENTED_EDGE ( 'NONE', *, *, #64581, .T. ) ;
#12877=FILL_AREA_STYLE ('',( #60706 ) ) ;
#12882=DIRECTION ( 'NONE',  ( 0.000000000000000000, 0.000000000000000000, 1.000000000000000000 ) ) ;
#12883=CARTESIAN_POINT ( 'NONE',  ( 10.01517768586949408, 114.6949999999999932, 1.839758294383810543E-15 ) ) ;
#12884=CIRCLE ( 'NONE', #52240, 0.5000000000000000000 ) ;
#12890=CARTESIAN_POINT ( 'NONE',  ( 4.716976649647096842, 121.7429263765338163, 6.492361379858953896 ) ) ;
#12891=CARTESIAN_POINT ( 'NONE',  ( -74.99999999999998579, 50.00000000000000000, 6.499999999999999112 ) ) ;
#12900=EDGE_LOOP ( 'NONE', ( #18132, #47650, #33075, #4210, #18755, #68254, #14777, #45590, #21371, #55290 ) ) ;
#12902=DIRECTION ( 'NONE',  ( -0.000000000000000000, -0.000000000000000000, -1.000000000000000000 ) ) ;
#12903=SURFACE_STYLE_USAGE ( .BOTH. , #45985 ) ;
#12907=AXIS2_PLACEMENT_3D ( 'NONE', #26882, #19978, #41476 ) ;
#12909=CARTESIAN_POINT ( 'NONE',  ( -9.058813317711337021, 144.1549999999999727, -2.943386871421374895 ) ) ;
#12910=SURFACE_STYLE_FILL_AREA ( #55824 ) ;
#12915=PRESENTATION_STYLE_ASSIGNMENT (( #18561 ) ) ;
#12916=PRESENTATION_STYLE_ASSIGNMENT (( #7636 ) ) ;
#12917=STYLED_ITEM ( 'NONE', ( #38519 ), #38903 ) ;
#12928=( NAMED_UNIT ( * ) SI_UNIT ( $, .STERADIAN. ) SOLID_ANGLE_UNIT ( ) );
#12932=ORIENTED_EDGE ( 'NONE', *, *, #801, .F. ) ;
#12933=( LENGTH_UNIT ( ) NAMED_UNIT ( * ) SI_UNIT ( .MILLI., .METRE. ) );
#12934=DIRECTION ( 'NONE',  ( 0.000000000000000000, 0.000000000000000000, 1.000000000000000000 ) ) ;
#12937=CARTESIAN_POINT ( 'NONE',  ( 3.094860106618435136, 113.4050000000000011, -9.525000000000000355 ) ) ;
#12938=DIRECTION ( 'NONE',  ( -0.000000000000000000, 1.000000000000000000, -0.000000000000000000 ) ) ;
#12943=AXIS2_PLACEMENT_3D ( 'NONE', #11676, #11326, #32790 ) ;
#12948=VERTEX_POINT ( 'NONE', #18110 ) ;
#12949=CARTESIAN_POINT ( 'NONE',  ( -7.632228543268607446, 141.5429263765338135, -2.479861379858953718 ) ) ;
#12953=( GEOMETRIC_REPRESENTATION_CONTEXT ( 3 ) GLOBAL_UNCERTAINTY_ASSIGNED_CONTEXT ( ( #36925 ) ) GLOBAL_UNIT_ASSIGNED_CONTEXT ( ( #56067, #57109, #66992 ) ) REPRESENTATION_CONTEXT ( 'NONE', 'WORKASPACE' ) );
#12954=CARTESIAN_POINT ( 'NONE',  ( -34.99999999999999289, 99.99999999999998579, -7.000000000000000000 ) ) ;
#12966=ORIENTED_EDGE ( 'NONE', *, *, #12514, .F. ) ;
#12969=CARTESIAN_POINT ( 'NONE',  ( -45.00000000000000000, 8.749900610107136600, -6.882725987574755955 ) ) ;
#12972=( LENGTH_UNIT ( ) NAMED_UNIT ( * ) SI_UNIT ( .MILLI., .METRE. ) );
#12973=CARTESIAN_POINT ( 'NONE',  ( -20.44164625062140317, 115.3859073845563756, 10.00000000000000000 ) ) ;
#12976=AXIS2_PLACEMENT_3D ( 'NONE', #40837, #29184, #24966 ) ;
#12977=VERTEX_POINT ( 'NONE', #45225 ) ;
#12979=SURFACE_SIDE_STYLE ('',( #29132 ) ) ;
#12982=DIRECTION ( 'NONE',  ( -0.2413793103448194644, -0.9704308468600220117, 0.000000000000000000 ) ) ;
#12992=CARTESIAN_POINT ( 'NONE',  ( 0.000000000000000000, 143.9429263765338192, -8.025000000000000355 ) ) ;
#12996=CARTESIAN_POINT ( 'NONE',  ( 0.000000000000000000, 113.5549999999999926, -9.525000000000000355 ) ) ;
#13000=UNCERTAINTY_MEASURE_WITH_UNIT (LENGTH_MEASURE( 1.000000000000000082E-05 ), #34505, 'distance_accuracy_value', 'NONE');
#13001=CARTESIAN_POINT ( 'NONE',  ( 60.00000000000000000, 1.797044900979284448E-15, -12.00000000000000000 ) ) ;
#13003=CARTESIAN_POINT ( 'NONE',  ( 41.06080360525773187, 107.9551383427286737, -3.682527553402531240 ) ) ;
#13008=TOROIDAL_SURFACE ( 'NONE', #22014, 9.499999999999998224, 0.5000000000000000000 ) ;
#13010=ADVANCED_FACE ( 'NONE', ( #12465 ), #66999, .T. ) ;
#13013=VERTEX_POINT ( 'NONE', #56427 ) ;
#13014=ORIENTED_EDGE ( 'NONE', *, *, #31756, .T. ) ;
#13015=( GEOMETRIC_REPRESENTATION_CONTEXT ( 3 ) GLOBAL_UNCERTAINTY_ASSIGNED_CONTEXT ( ( #27818 ) ) GLOBAL_UNIT_ASSIGNED_CONTEXT ( ( #43958, #54791, #43613 ) ) REPRESENTATION_CONTEXT ( 'NONE', 'WORKASPACE' ) );
#13019=( LENGTH_UNIT ( ) NAMED_UNIT ( * ) SI_UNIT ( .MILLI., .METRE. ) );
#13021=DIRECTION ( 'NONE',  ( 0.000000000000000000, 0.000000000000000000, -1.000000000000000000 ) ) ;
#13023=ORIENTED_EDGE ( 'NONE', *, *, #44208, .T. ) ;
#13026=AXIS2_PLACEMENT_3D ( 'NONE', #18224, #40388, #61126 ) ;
#13030=FACE_BOUND ( 'NONE', #68660, .T. ) ;
#13033=PRESENTATION_STYLE_ASSIGNMENT (( #20291 ) ) ;
#13034=EDGE_CURVE ( 'NONE', #31626, #67110, #13159, .T. ) ;
#13035=DIRECTION ( 'NONE',  ( 0.000000000000000000, 0.000000000000000000, 1.000000000000000000 ) ) ;
#13036=CARTESIAN_POINT ( 'NONE',  ( 8.102448949553183510, 135.9950000000000045, -5.886773742842746238 ) ) ;
#13037=CARTESIAN_POINT ( 'NONE',  ( -72.50000000000000000, 14.49137674618942562, 9.500000000000000000 ) ) ;
#13039=ORIENTED_EDGE ( 'NONE', *, *, #15916, .F. ) ;
#13040=CARTESIAN_POINT ( 'NONE',  ( -8.102448949553179958, 144.6049999999999613, 5.886773742842747126 ) ) ;
#13042=CARTESIAN_POINT ( 'NONE',  ( 41.05030025768302693, 107.9631293162027674, -3.671816393059894157 ) ) ;
#13044=CARTESIAN_POINT ( 'NONE',  ( 10.01517768586949231, 154.8050000000000352, 1.839758294383810543E-15 ) ) ;
#13048=EDGE_CURVE ( 'NONE', #53214, #6337, #45580, .T. ) ;
#13049=CARTESIAN_POINT ( 'NONE',  ( 20.71231517720798010, 149.4999999999999716, 10.00000000000000000 ) ) ;
#13053=DIRECTION ( 'NONE',  ( 0.6216216216216311485, -0.7833176619561784682, 0.000000000000000000 ) ) ;
#13057=UNCERTAINTY_MEASURE_WITH_UNIT (LENGTH_MEASURE( 1.000000000000000082E-05 ), #23975, 'distance_accuracy_value', 'NONE');
#13058=CIRCLE ( 'NONE', #10798, 0.5000000000000004441 ) ;
#13059=DIRECTION ( 'NONE',  ( 0.000000000000000000, 0.000000000000000000, 1.000000000000000000 ) ) ;
#13060=CARTESIAN_POINT ( 'NONE',  ( 45.64107345563247975, 10.15688972729190809, -6.260993343996352323 ) ) ;
#13061=( LENGTH_UNIT ( ) NAMED_UNIT ( * ) SI_UNIT ( .MILLI., .METRE. ) );
#13063=VERTEX_POINT ( 'NONE', #7892 ) ;
#13064=AXIS2_PLACEMENT_3D ( 'NONE', #34421, #67830, #29485 ) ;
#13072=ORIENTED_EDGE ( 'NONE', *, *, #31533, .T. ) ;
#13073=DIRECTION ( 'NONE',  ( 0.000000000000000000, 0.000000000000000000, 1.000000000000000000 ) ) ;
#13077=CARTESIAN_POINT ( 'NONE',  ( 5.598654528085805993, 138.2449999999999761, 7.705886871421374629 ) ) ;
#13080=FACE_OUTER_BOUND ( 'NONE', #54613, .T. ) ;
#13086=EDGE_LOOP ( 'NONE', ( #49086, #33712, #61373, #25009, #50648, #38751, #24465, #27619, #57415, #43543, #18168, #44083, #3059, #65308 ) ) ;
#13087=CARTESIAN_POINT ( 'NONE',  ( -2.607480562269053781, 130.2929263765338135, 8.025000000000016342 ) ) ;
#13088=ORIENTED_EDGE ( 'NONE', *, *, #2240, .F. ) ;
#13089=FACE_OUTER_BOUND ( 'NONE', #65755, .T. ) ;
#13090=EDGE_CURVE ( 'NONE', #50571, #43604, #40270, .T. ) ;
#13092=CARTESIAN_POINT ( 'NONE',  ( 60.00000000000000000, 149.4999999999999716, 9.500000000000000000 ) ) ;
#13093=CARTESIAN_POINT ( 'NONE',  ( 0.000000000000000000, 148.0570736234661524, -8.025000000000000355 ) ) ;
#13094=DIRECTION ( 'NONE',  ( -1.000000000000000000, 0.000000000000000000, 0.000000000000000000 ) ) ;
#13095=MECHANICAL_DESIGN_GEOMETRIC_PRESENTATION_REPRESENTATION('',(#33346),#17613);
#13098=EDGE_CURVE ( 'NONE', #46060, #62390, #5285, .T. ) ;
#13100=ORIENTED_EDGE ( 'NONE', *, *, #49026, .T. ) ;
#13101=PRESENTATION_STYLE_ASSIGNMENT (( #23661 ) ) ;
#13102=FILL_AREA_STYLE ('',( #27868 ) ) ;
#13105=MECHANICAL_DESIGN_GEOMETRIC_PRESENTATION_REPRESENTATION('',(#36721),#58086);
#13108=( LENGTH_UNIT ( ) NAMED_UNIT ( * ) SI_UNIT ( .MILLI., .METRE. ) );
#13109=CARTESIAN_POINT ( 'NONE',  ( 8.437984349512095861, 159.3070736234661240, 1.550032578732817026E-15 ) ) ;
#13112=SURFACE_STYLE_USAGE ( .BOTH. , #35277 ) ;
#13113=CARTESIAN_POINT ( 'NONE',  ( -1.166476076187854022E-15, 115.0549999999999926, 9.525000000000000355 ) ) ;
#13116=CARTESIAN_POINT ( 'NONE',  ( -1.166476076187854022E-15, 124.0549999999999784, 9.525000000000000355 ) ) ;
#13118=PRESENTATION_STYLE_ASSIGNMENT (( #51457 ) ) ;
#13119=CARTESIAN_POINT ( 'NONE',  ( 20.51914007124930706, 114.9043000146497207, 10.00000000000000000 ) ) ;
#13120=DIRECTION ( 'NONE',  ( 1.000000000000000000, 3.469446951953611033E-15, 0.000000000000000000 ) ) ;
#13124=FILL_AREA_STYLE_COLOUR ( '', #37452 ) ;
#13128=VECTOR ( 'NONE', #839, 1000.000000000000000 ) ;
#13129=CARTESIAN_POINT ( 'NONE',  ( -45.58243994668686838, 8.116436936526458368, -6.493641663363978189 ) ) ;
#13131=VERTEX_POINT ( 'NONE', #62403 ) ;
#13136=CARTESIAN_POINT ( 'NONE',  ( -74.09581123568146666, 9.387410786201540347, 6.121260521433846691 ) ) ;
#13138=EDGE_LOOP ( 'NONE', ( #51739, #1308, #12577, #12565 ) ) ;
#13139=( NAMED_UNIT ( * ) PLANE_ANGLE_UNIT ( ) SI_UNIT ( $, .RADIAN. ) );
#13142=SURFACE_SIDE_STYLE ('',( #39929 ) ) ;
#13143=CARTESIAN_POINT ( 'NONE',  ( -5.598654528085808657, 140.6449999999999818, 7.705886871421373741 ) ) ;
#13147=PRESENTATION_STYLE_ASSIGNMENT (( #39937 ) ) ;
#13148=CIRCLE ( 'NONE', #22154, 0.5000000000000004441 ) ;
#13151=LINE ( 'NONE', #68370, #50487 ) ;
#13152=CARTESIAN_POINT ( 'NONE',  ( 9.058813317711338797, 114.8449999999999847, -2.943386871421372675 ) ) ;
#13156=ORIENTED_EDGE ( 'NONE', *, *, #4119, .T. ) ;
#13159=LINE ( 'NONE', #30037, #42964 ) ;
#13161=PRESENTATION_STYLE_ASSIGNMENT (( #22700 ) ) ;
#13163=MECHANICAL_DESIGN_GEOMETRIC_PRESENTATION_REPRESENTATION('',(#58136),#28915);
#13167=EDGE_CURVE ( 'NONE', #58485, #26613, #20416, .T. ) ;
#13168=DIRECTION ( 'NONE',  ( -0.000000000000000000, -0.000000000000000000, -1.000000000000000000 ) ) ;
#13169=CARTESIAN_POINT ( 'NONE',  ( -34.99999999999999289, 99.99999999999998579, -10.00000000000000000 ) ) ;
#13172=FACE_OUTER_BOUND ( 'NONE', #64316, .T. ) ;
#13174=FACE_OUTER_BOUND ( 'NONE', #11997, .T. ) ;
#13176=CARTESIAN_POINT ( 'NONE',  ( -69.99999999999998579, 50.00000000000000000, -11.50000000000001066 ) ) ;
#13179=ORIENTED_EDGE ( 'NONE', *, *, #24928, .F. ) ;
#13182=EDGE_CURVE ( 'NONE', #33055, #10616, #5779, .T. ) ;
#13186=CARTESIAN_POINT ( 'NONE',  ( 0.000000000000000000, 124.0570736234661524, -8.025000000000000355 ) ) ;
#13187=DIRECTION ( 'NONE',  ( -1.000000000000000000, 0.000000000000000000, 0.000000000000000000 ) ) ;
#13188=EDGE_CURVE ( 'NONE', #38790, #60581, #10338, .T. ) ;
#13190=AXIS2_PLACEMENT_3D ( 'NONE', #41454, #30862, #46400 ) ;
#13193=DIRECTION ( 'NONE',  ( 1.156482317317873451E-16, -1.000000000000000000, 0.000000000000000000 ) ) ;
#13194=DIRECTION ( 'NONE',  ( -1.000000000000000000, 0.000000000000000000, 0.000000000000000000 ) ) ;
#13198=DIRECTION ( 'NONE',  ( 0.000000000000000000, 0.000000000000000000, 1.000000000000000000 ) ) ;
#13200=CARTESIAN_POINT ( 'NONE',  ( -15.98999599679679839, 117.4999999999999716, -9.500000000000000000 ) ) ;
#13202=VERTEX_POINT ( 'NONE', #11269 ) ;
#13206=CARTESIAN_POINT ( 'NONE',  ( -9.827790563157511022E-16, 121.4429263765338050, 8.025000000000000355 ) ) ;
#13208=( GEOMETRIC_REPRESENTATION_CONTEXT ( 3 ) GLOBAL_UNCERTAINTY_ASSIGNED_CONTEXT ( ( #50221 ) ) GLOBAL_UNIT_ASSIGNED_CONTEXT ( ( #55025, #32531, #64898 ) ) REPRESENTATION_CONTEXT ( 'NONE', 'WORKASPACE' ) );
#13209=AXIS2_PLACEMENT_3D ( 'NONE', #16882, #66063, #38357 ) ;
#13212=ORIENTED_EDGE ( 'NONE', *, *, #8533, .T. ) ;
#13214=SURFACE_SIDE_STYLE ('',( #40005 ) ) ;
#13215=( LENGTH_UNIT ( ) NAMED_UNIT ( * ) SI_UNIT ( .MILLI., .METRE. ) );
#13218=CARTESIAN_POINT ( 'NONE',  ( -3.094860106618432471, 115.5949999999999704, -9.525000000000000355 ) ) ;
#13220=EDGE_CURVE ( 'NONE', #34097, #46742, #55248, .T. ) ;
#13222=DIRECTION ( 'NONE',  ( -1.000000000000000000, 1.224646799147349509E-16, 0.000000000000000000 ) ) ;
#13225=FILL_AREA_STYLE_COLOUR ( '', #1722 ) ;
#13226=CARTESIAN_POINT ( 'NONE',  ( 44.97237157117559292, 9.999999999999980460, -3.164074568774566387 ) ) ;
#13227=( LENGTH_UNIT ( ) NAMED_UNIT ( * ) SI_UNIT ( .MILLI., .METRE. ) );
#13245=EDGE_CURVE ( 'NONE', #68902, #28179, #12557, .T. ) ;
#13246=CARTESIAN_POINT ( 'NONE',  ( 8.102448949553181734, 148.5049999999999955, 5.886773742842750679 ) ) ;
#13249=CARTESIAN_POINT ( 'NONE',  ( 74.50000000000000000, -2.135340797662720349E-14, -10.00000000000000000 ) ) ;
#13250=CARTESIAN_POINT ( 'NONE',  ( -19.98288066869250201, 115.0281754944747235, -9.999999999997170264 ) ) ;
#13251=EDGE_CURVE ( 'NONE', #67765, #68848, #23767, .T. ) ;
#13252=DIRECTION ( 'NONE',  ( 1.000000000000000000, 0.000000000000000000, 0.000000000000000000 ) ) ;
#13255=LINE ( 'NONE', #39345, #21422 ) ;
#13256=LINE ( 'NONE', #22802, #48751 ) ;
#13258=CYLINDRICAL_SURFACE ( 'NONE', #55297, 0.5000000000000004441 ) ;
#13262=CARTESIAN_POINT ( 'NONE',  ( 71.18918918918917882, 14.09971791521133433, -7.500000000000000000 ) ) ;
#13264=SURFACE_STYLE_FILL_AREA ( #39696 ) ;
#13266=ORIENTED_EDGE ( 'NONE', *, *, #53170, .T. ) ;
#13267=ORIENTED_EDGE ( 'NONE', *, *, #66134, .T. ) ;
#13269=LINE ( 'NONE', #19942, #60064 ) ;
#13271=CARTESIAN_POINT ( 'NONE',  ( -5.598654528085806881, 110.8549999999999756, -7.705886871421374629 ) ) ;
#13273=ORIENTED_EDGE ( 'NONE', *, *, #3137, .T. ) ;
#13280=CARTESIAN_POINT ( 'NONE',  ( -0.4422543624570795529, 110.4999999999999716, -9.524999999999996803 ) ) ;
#13282=CARTESIAN_POINT ( 'NONE',  ( -44.99999999999977263, 147.4999999999999716, 10.00000000000000000 ) ) ;
#13284=CARTESIAN_POINT ( 'NONE',  ( 2.607480562269076430, 143.7929263765338135, -8.025000000000000355 ) ) ;
#13286=DIRECTION ( 'NONE',  ( 0.000000000000000000, 0.000000000000000000, -1.000000000000000000 ) ) ;
#13287=VECTOR ( 'NONE', #33239, 1000.000000000000000 ) ;
#13288=SURFACE_SIDE_STYLE ('',( #18905 ) ) ;
#13291=LINE ( 'NONE', #35470, #67836 ) ;
#13293=CARTESIAN_POINT ( 'NONE',  ( -4.716976649647098618, 140.2570736234661410, 6.492361379858953008 ) ) ;
#13294=CARTESIAN_POINT ( 'NONE',  ( -19.89974874213239886, 114.9999999999999574, 10.49999999999999645 ) ) ;
#13301=EDGE_CURVE ( 'NONE', #10952, #55126, #29435, .T. ) ;
#13304=FACE_OUTER_BOUND ( 'NONE', #22653, .T. ) ;
#13305=ORIENTED_EDGE ( 'NONE', *, *, #50526, .T. ) ;
#13307=EDGE_LOOP ( 'NONE', ( #55244, #8023, #8783, #33447 ) ) ;
#13309=DIRECTION ( 'NONE',  ( -7.080503983578803083E-17, -1.000000000000000000, 0.000000000000000000 ) ) ;
#13314=DIRECTION ( 'NONE',  ( 1.000000000000000000, 0.000000000000000000, 0.000000000000000000 ) ) ;
#13318=SURFACE_SIDE_STYLE ('',( #55190 ) ) ;
#13320=CARTESIAN_POINT ( 'NONE',  ( -74.59575606080316845, 36.31161697799826271, -9.993293536547614764 ) ) ;
#13321=EDGE_CURVE ( 'NONE', #30278, #60536, #11621, .T. ) ;
#13322=( NAMED_UNIT ( * ) PLANE_ANGLE_UNIT ( ) SI_UNIT ( $, .RADIAN. ) );
#13328=SURFACE_SIDE_STYLE ('',( #61502 ) ) ;
#13330=EDGE_CURVE ( 'NONE', #37089, #4040, #14858, .T. ) ;
#13333=CARTESIAN_POINT ( 'NONE',  ( -8.102448949553181734, 117.6049999999999898, 5.886773742842747126 ) ) ;
#13335=DIRECTION ( 'NONE',  ( 0.000000000000000000, 0.000000000000000000, 1.000000000000000000 ) ) ;
#13338=PRESENTATION_STYLE_ASSIGNMENT (( #4150 ) ) ;
#13339=DIRECTION ( 'NONE',  ( -1.000000000000000000, 0.000000000000000000, 0.000000000000000000 ) ) ;
#13340=ORIENTED_EDGE ( 'NONE', *, *, #63383, .T. ) ;
#13353=LINE ( 'NONE', #4077, #31022 ) ;
#13359=ORIENTED_EDGE ( 'NONE', *, *, #53344, .T. ) ;
#13361=EDGE_LOOP ( 'NONE', ( #57401, #26762, #40766, #18488 ) ) ;
#13370=CARTESIAN_POINT ( 'NONE',  ( 10.01517768586949231, 144.6949999999999932, 1.839758294383810543E-15 ) ) ;
#13373=CARTESIAN_POINT ( 'NONE',  ( -3.094860106618432471, 140.7049999999999557, -9.525000000000000355 ) ) ;
#13374=FILL_AREA_STYLE ('',( #9169 ) ) ;
#13378=CARTESIAN_POINT ( 'NONE',  ( 7.632228543268608334, 116.3429263765338106, -2.479861379858951942 ) ) ;
#13379=( NAMED_UNIT ( * ) SI_UNIT ( $, .STERADIAN. ) SOLID_ANGLE_UNIT ( ) );
#13384=MECHANICAL_DESIGN_GEOMETRIC_PRESENTATION_REPRESENTATION('',(#65050),#62888);
#13385=CARTESIAN_POINT ( 'NONE',  ( 41.45361433042954502, 107.0152407614178856, 3.499999999999999556 ) ) ;
#13387=CARTESIAN_POINT ( 'NONE',  ( 15.98999599679679839, 117.9999999999999716, 9.500000000000000000 ) ) ;
#13389=CARTESIAN_POINT ( 'NONE',  ( 20.46001754528041161, 114.7916627990982192, 10.31416700829639588 ) ) ;
#13392=ORIENTED_EDGE ( 'NONE', *, *, #38801, .F. ) ;
#13394=( NAMED_UNIT ( * ) SI_UNIT ( $, .STERADIAN. ) SOLID_ANGLE_UNIT ( ) );
#13395=CIRCLE ( 'NONE', #17924, 0.4999999999999993339 ) ;
#13396=CARTESIAN_POINT ( 'NONE',  ( -75.50000000000000000, 64.49137674618943095, -41.30495168499704306 ) ) ;
#13397=CARTESIAN_POINT ( 'NONE',  ( 45.54151037965925752, 9.791825115386158629, -6.500000000000000888 ) ) ;
#13398=DIRECTION ( 'NONE',  ( 1.000000000000000000, 0.000000000000000000, 0.000000000000000000 ) ) ;
#13403=CARTESIAN_POINT ( 'NONE',  ( 0.000000000000000000, 152.9429263765338192, -8.025000000000000355 ) ) ;
#13409=CYLINDRICAL_SURFACE ( 'NONE', #58919, 8.025000000000000355 ) ;
#13411=CARTESIAN_POINT ( 'NONE',  ( -75.00000000000000000, 9.581381838473308932, -6.370847823861820025 ) ) ;
#13412=ORIENTED_EDGE ( 'NONE', *, *, #24456, .F. ) ;
#13417=CARTESIAN_POINT ( 'NONE',  ( 10.01517768586949231, 141.6949999999999363, 1.839758294383810543E-15 ) ) ;
#13420=( BOUNDED_CURVE ( )  B_SPLINE_CURVE ( 2, ( #10185, #25995, #20744, #4535, #48547, #52760, #32312, #36950, #58360, #47523, #5229 ),
 .UNSPECIFIED., .F., .F. ) 
 B_SPLINE_CURVE_WITH_KNOTS ( ( 3, 2, 2, 2, 2, 3 ),
 ( 0.3823529411764706176, 0.3882352941176471228, 0.3941176470588235725, 0.4000000000000001332, 0.4058823529411765829, 0.4117647058823530326 ),
 .UNSPECIFIED. ) 
 CURVE ( )  GEOMETRIC_REPRESENTATION_ITEM ( )  RATIONAL_B_SPLINE_CURVE ( ( 0.9999999999999995559, 0.9510565162951539753, 1.000000000000000000, 0.9510565162951535312, 1.000000000000000000, 0.9510565162951535312, 1.000000000000000000, 0.9510565162951535312, 1.000000000000000000, 0.9510565162951526430, 1.000000000000000888 ) ) 
 REPRESENTATION_ITEM ( '' )  );
#13422=PRESENTATION_STYLE_ASSIGNMENT (( #22962 ) ) ;
#13423=( GEOMETRIC_REPRESENTATION_CONTEXT ( 3 ) GLOBAL_UNCERTAINTY_ASSIGNED_CONTEXT ( ( #17101 ) ) GLOBAL_UNIT_ASSIGNED_CONTEXT ( ( #62400, #46259, #57468 ) ) REPRESENTATION_CONTEXT ( 'NONE', 'WORKASPACE' ) );
#13430=STYLED_ITEM ( 'NONE', ( #17743 ), #10848 ) ;
#13433=CARTESIAN_POINT ( 'NONE',  ( -4.716976649647098618, 130.1429263765338362, 6.492361379858953008 ) ) ;
#13436=( GEOMETRIC_REPRESENTATION_CONTEXT ( 3 ) GLOBAL_UNCERTAINTY_ASSIGNED_CONTEXT ( ( #60212 ) ) GLOBAL_UNIT_ASSIGNED_CONTEXT ( ( #63756, #58840, #43061 ) ) REPRESENTATION_CONTEXT ( 'NONE', 'WORKASPACE' ) );
#13437=CIRCLE ( 'NONE', #62839, 8.025000000000000355 ) ;
#13438=CYLINDRICAL_SURFACE ( 'NONE', #15896, 0.5000000000000004441 ) ;
#13439=CARTESIAN_POINT ( 'NONE',  ( -45.00000000000000711, 7.768687147774683943, 6.500000000000007105 ) ) ;
#13442=DIRECTION ( 'NONE',  ( 0.000000000000000000, 1.000000000000000000, 0.000000000000000000 ) ) ;
#13446=CARTESIAN_POINT ( 'NONE',  ( -20.86636340060661610, 115.0297054428233707, -10.00000000000000000 ) ) ;
#13447=SURFACE_STYLE_USAGE ( .BOTH. , #61620 ) ;
#13448=ORIENTED_EDGE ( 'NONE', *, *, #61239, .T. ) ;
#13451=FILL_AREA_STYLE_COLOUR ( '', #67994 ) ;
#13452=CARTESIAN_POINT ( 'NONE',  ( -5.598654528085808657, 113.6449999999999818, 7.705886871421373741 ) ) ;
#13455=DIRECTION ( 'NONE',  ( 1.000000000000000000, 0.000000000000000000, 0.000000000000000000 ) ) ;
#13457=LINE ( 'NONE', #29989, #67785 ) ;
#13458=CARTESIAN_POINT ( 'NONE',  ( -9.058813317711338797, 141.4549999999999841, 2.943386871421373563 ) ) ;
#13459=AXIS2_PLACEMENT_3D ( 'NONE', #62554, #46078, #58009 ) ;
#13460=SURFACE_STYLE_FILL_AREA ( #18750 ) ;
#13461=SURFACE_STYLE_USAGE ( .BOTH. , #45180 ) ;
#13464=( NAMED_UNIT ( * ) SI_UNIT ( $, .STERADIAN. ) SOLID_ANGLE_UNIT ( ) );
#13465=AXIS2_PLACEMENT_3D ( 'NONE', #25500, #10040, #65564 ) ;
#13471=CARTESIAN_POINT ( 'NONE',  ( -45.00000000000000000, 7.966012280117821476, -7.000000003579909702 ) ) ;
#13472=CARTESIAN_POINT ( 'NONE',  ( 72.50000000000000000, 14.49137674618942562, -9.500000000000000000 ) ) ;
#13473=ORIENTED_EDGE ( 'NONE', *, *, #16945, .T. ) ;
#13474=DIRECTION ( 'NONE',  ( 0.000000000000000000, 0.000000000000000000, 1.000000000000000000 ) ) ;
#13476=DIRECTION ( 'NONE',  ( 1.000000000000000000, 0.000000000000000000, 0.000000000000000000 ) ) ;
#13483=AXIS2_PLACEMENT_3D ( 'NONE', #47573, #37350, #5607 ) ;
#13486=DIRECTION ( 'NONE',  ( -0.000000000000000000, 1.000000000000000000, -0.000000000000000000 ) ) ;
#13487=CARTESIAN_POINT ( 'NONE',  ( 3.094860106618435136, 139.2949999999999875, -9.525000000000000355 ) ) ;
#13489=AXIS2_PLACEMENT_3D ( 'NONE', #54611, #19041, #20088 ) ;
#13492=DIRECTION ( 'NONE',  ( -0.000000000000000000, 1.000000000000000000, -0.000000000000000000 ) ) ;
#13493=CARTESIAN_POINT ( 'NONE',  ( 4.716976649647099507, 120.7570736234661553, -6.492361379858953008 ) ) ;
#13502=VERTEX_POINT ( 'NONE', #23902 ) ;
#13503=STYLED_ITEM ( 'NONE', ( #16508 ), #16648 ) ;
#13507=DIRECTION ( 'NONE',  ( -0.000000000000000000, 1.000000000000000000, -0.000000000000000000 ) ) ;
#13509=VECTOR ( 'NONE', #67410, 1000.000000000000000 ) ;
#13513=CARTESIAN_POINT ( 'NONE',  ( 71.18918918918917882, 14.09971791521133255, 7.000000000000000000 ) ) ;
#13515=CARTESIAN_POINT ( 'NONE',  ( -9.827790563157511022E-16, 136.4429263765338192, 8.025000000000000355 ) ) ;
#13516=ORIENTED_EDGE ( 'NONE', *, *, #67271, .F. ) ;
#13522=CARTESIAN_POINT ( 'NONE',  ( -60.00000000000000000, -2.024042244987997205E-14, 11.50000000000000000 ) ) ;
#13523=( GEOMETRIC_REPRESENTATION_CONTEXT ( 3 ) GLOBAL_UNCERTAINTY_ASSIGNED_CONTEXT ( ( #27596 ) ) GLOBAL_UNIT_ASSIGNED_CONTEXT ( ( #6669, #28108, #1349 ) ) REPRESENTATION_CONTEXT ( 'NONE', 'WORKASPACE' ) );
#13525=DIRECTION ( 'NONE',  ( 0.000000000000000000, 0.000000000000000000, 1.000000000000000000 ) ) ;
#13526=CARTESIAN_POINT ( 'NONE',  ( -41.03152803655121517, 107.9804733858014032, 3.206774974534162048 ) ) ;
#13530=CARTESIAN_POINT ( 'NONE',  ( -15.48999599679679662, 146.4999999999999716, -9.500000000000000000 ) ) ;
#13531=FILL_AREA_STYLE_COLOUR ( '', #38585 ) ;
#13534=DIRECTION ( 'NONE',  ( 0.000000000000000000, 0.000000000000000000, -1.000000000000000000 ) ) ;
#13536=CARTESIAN_POINT ( 'NONE',  ( -9.827790563157511022E-16, 137.5570736234661808, 8.025000000000000355 ) ) ;
#13537=DIRECTION ( 'NONE',  ( -0.000000000000000000, 1.000000000000000000, -0.000000000000000000 ) ) ;
#13538=( GEOMETRIC_REPRESENTATION_CONTEXT ( 3 ) GLOBAL_UNCERTAINTY_ASSIGNED_CONTEXT ( ( #40501 ) ) GLOBAL_UNIT_ASSIGNED_CONTEXT ( ( #1882, #60666, #18482 ) ) REPRESENTATION_CONTEXT ( 'NONE', 'WORKASPACE' ) );
#13541=PRESENTATION_STYLE_ASSIGNMENT (( #55773 ) ) ;
#13543=DIRECTION ( 'NONE',  ( 1.000000000000000000, 1.156482317317866302E-16, 0.000000000000000000 ) ) ;
#13549=( GEOMETRIC_REPRESENTATION_CONTEXT ( 3 ) GLOBAL_UNCERTAINTY_ASSIGNED_CONTEXT ( ( #9502 ) ) GLOBAL_UNIT_ASSIGNED_CONTEXT ( ( #1539, #44560, #33941 ) ) REPRESENTATION_CONTEXT ( 'NONE', 'WORKASPACE' ) );
#13551=LINE ( 'NONE', #31730, #65939 ) ;
#13553=UNCERTAINTY_MEASURE_WITH_UNIT (LENGTH_MEASURE( 1.000000000000000082E-05 ), #25679, 'distance_accuracy_value', 'NONE');
#13560=ORIENTED_EDGE ( 'NONE', *, *, #57741, .T. ) ;
#13561=CARTESIAN_POINT ( 'NONE',  ( -60.00000000000000000, -2.024042244987997205E-14, 9.500000000000000000 ) ) ;
#13562=( NAMED_UNIT ( * ) SI_UNIT ( $, .STERADIAN. ) SOLID_ANGLE_UNIT ( ) );
#13563=( NAMED_UNIT ( * ) PLANE_ANGLE_UNIT ( ) SI_UNIT ( $, .RADIAN. ) );
#13567=CARTESIAN_POINT ( 'NONE',  ( 5.598654528085809545, 112.1449999999999818, -7.705886871421373741 ) ) ;
#13574=LINE ( 'NONE', #56492, #32905 ) ;
#13580=DIRECTION ( 'NONE',  ( 0.000000000000000000, 1.000000000000000000, 0.000000000000000000 ) ) ;
#13581=CARTESIAN_POINT ( 'NONE',  ( -1.601699666116353837, 110.6836774114466664, -9.211824715481125025 ) ) ;
#13582=STYLED_ITEM ( 'NONE', ( #67527 ), #21929 ) ;
#13586=VERTEX_POINT ( 'NONE', #61871 ) ;
#13592=AXIS2_PLACEMENT_3D ( 'NONE', #57945, #46738, #57580 ) ;
#13595=CARTESIAN_POINT ( 'NONE',  ( 3.094860106618431583, 145.2049999999999272, 9.525000000000000355 ) ) ;
#13596=DIRECTION ( 'NONE',  ( 0.000000000000000000, 0.000000000000000000, 1.000000000000000000 ) ) ;
#13600=AXIS2_PLACEMENT_3D ( 'NONE', #32460, #27528, #7135 ) ;
#13601=ADVANCED_FACE ( 'NONE', ( #21651 ), #64578, .T. ) ;
#13608=DIRECTION ( 'NONE',  ( 0.000000000000000000, 0.000000000000000000, 1.000000000000000000 ) ) ;
#13612=ORIENTED_EDGE ( 'NONE', *, *, #32613, .F. ) ;
#13613=TOROIDAL_SURFACE ( 'NONE', #21506, 27.49999999999999645, 0.5000000000000000000 ) ;
#13617=AXIS2_PLACEMENT_3D ( 'NONE', #62476, #18184, #67770 ) ;
#13618=CARTESIAN_POINT ( 'NONE',  ( -44.99999999999999289, 9.708372675170620525, 6.100541755698618118 ) ) ;
#13619=ORIENTED_EDGE ( 'NONE', *, *, #56619, .T. ) ;
#13622=PRESENTATION_STYLE_ASSIGNMENT (( #24507 ) ) ;
#13624=ORIENTED_EDGE ( 'NONE', *, *, #56809, .T. ) ;
#13625=CARTESIAN_POINT ( 'NONE',  ( 3.094860106618431583, 112.2049999999999841, 9.525000000000000355 ) ) ;
#13627=ORIENTED_EDGE ( 'NONE', *, *, #22043, .F. ) ;
#13629=SURFACE_STYLE_FILL_AREA ( #24515 ) ;
#13631=DIRECTION ( 'NONE',  ( -1.000000000000000000, 0.000000000000000000, 0.000000000000000000 ) ) ;
#13635=CARTESIAN_POINT ( 'NONE',  ( -2.185379354980680588, 110.5000000000000000, -9.281319716557792532 ) ) ;
#13636=DIRECTION ( 'NONE',  ( 0.000000000000000000, 0.000000000000000000, -1.000000000000000000 ) ) ;
#13638=DIRECTION ( 'NONE',  ( 1.000000000000000000, 0.000000000000000000, 0.000000000000000000 ) ) ;
#13640=CARTESIAN_POINT ( 'NONE',  ( 0.000000000000000000, 143.9429263765338192, -8.025000000000000355 ) ) ;
#13643=( GEOMETRIC_REPRESENTATION_CONTEXT ( 3 ) GLOBAL_UNCERTAINTY_ASSIGNED_CONTEXT ( ( #53166 ) ) GLOBAL_UNIT_ASSIGNED_CONTEXT ( ( #69092, #32454, #42739 ) ) REPRESENTATION_CONTEXT ( 'NONE', 'WORKASPACE' ) );
#13645=SURFACE_STYLE_USAGE ( .BOTH. , #51637 ) ;
#13648=COLOUR_RGB ( '', 0.09019608, 0.27058824, 0.51372549) ;
#13652=FILL_AREA_STYLE ('',( #1988 ) ) ;
#13655=FILL_AREA_STYLE ('',( #14347 ) ) ;
#13656=LINE ( 'NONE', #9441, #26004 ) ;
#13657=ORIENTED_EDGE ( 'NONE', *, *, #35751, .F. ) ;
#13658=EDGE_CURVE ( 'NONE', #67222, #62684, #61881, .T. ) ;
#13660=CARTESIAN_POINT ( 'NONE',  ( -74.91375090774572243, 36.08647711726809604, 9.790149245326144722 ) ) ;
#13661=CARTESIAN_POINT ( 'NONE',  ( 15.98999599679679839, 118.4999999999999716, 7.000000000000000000 ) ) ;
#13665=EDGE_LOOP ( 'NONE', ( #23643, #52885, #63972, #19718 ) ) ;
#13666=CARTESIAN_POINT ( 'NONE',  ( -44.99154893926771592, 9.591540375271078389, 3.113444503357928994 ) ) ;
#13667=CARTESIAN_POINT ( 'NONE',  ( 45.50000000000000000, 9.639620389971920389, 6.500000000000000000 ) ) ;
#13670=VERTEX_POINT ( 'NONE', #37975 ) ;
#13679=VERTEX_POINT ( 'NONE', #53741 ) ;
#13681=AXIS2_PLACEMENT_3D ( 'NONE', #14562, #69668, #57473 ) ;
#13683=EDGE_CURVE ( 'NONE', #35027, #60834, #37235, .T. ) ;
#13686=CARTESIAN_POINT ( 'NONE',  ( 0.4393420241418015126, 154.5000000000000853, -9.524999999999996803 ) ) ;
#13691=CARTESIAN_POINT ( 'NONE',  ( -1.166476076187854022E-15, 121.0549999999999784, 9.525000000000000355 ) ) ;
#13693=AXIS2_PLACEMENT_3D ( 'NONE', #23078, #22727, #54370 ) ;
#13697=STYLED_ITEM ( 'NONE', ( #3475 ), #54393 ) ;
#13699=ORIENTED_EDGE ( 'NONE', *, *, #34707, .F. ) ;
#13702=STYLED_ITEM ( 'NONE', ( #4241 ), #53599 ) ;
#13703=VECTOR ( 'NONE', #2546, 1000.000000000000000 ) ;
#13704=DIRECTION ( 'NONE',  ( 0.000000000000000000, 0.000000000000000000, 1.000000000000000000 ) ) ;
#13705=AXIS2_PLACEMENT_3D ( 'NONE', #62197, #66804, #23520 ) ;
#13709=VERTEX_POINT ( 'NONE', #68561 ) ;
#13714=CARTESIAN_POINT ( 'NONE',  ( 34.99999999999999289, 99.99999999999997158, 9.500000000000000000 ) ) ;
#13722=VERTEX_POINT ( 'NONE', #36924 ) ;
#13724=DIRECTION ( 'NONE',  ( 1.000000000000000000, 0.000000000000000000, -0.000000000000000000 ) ) ;
#13726=LINE ( 'NONE', #46479, #21993 ) ;
#13727=CARTESIAN_POINT ( 'NONE',  ( -10.01517768586949231, 140.1949999999999932, -6.132527647946036459E-16 ) ) ;
#13730=( GEOMETRIC_REPRESENTATION_CONTEXT ( 3 ) GLOBAL_UNCERTAINTY_ASSIGNED_CONTEXT ( ( #64208 ) ) GLOBAL_UNIT_ASSIGNED_CONTEXT ( ( #68007, #67640, #29995 ) ) REPRESENTATION_CONTEXT ( 'NONE', 'WORKASPACE' ) );
#13731=EDGE_CURVE ( 'NONE', #22750, #51627, #43555, .T. ) ;
#13732=CARTESIAN_POINT ( 'NONE',  ( -5.598654528085808657, 135.7549999999999955, 7.705886871421373741 ) ) ;
#13736=CARTESIAN_POINT ( 'NONE',  ( -6.826472737025120807, 117.3929263765338078, -4.959722759717907437 ) ) ;
#13737=SURFACE_STYLE_USAGE ( .BOTH. , #40500 ) ;
#13738=UNCERTAINTY_MEASURE_WITH_UNIT (LENGTH_MEASURE( 1.000000000000000082E-05 ), #66394, 'distance_accuracy_value', 'NONE');
#13742=( NAMED_UNIT ( * ) SI_UNIT ( $, .STERADIAN. ) SOLID_ANGLE_UNIT ( ) );
#13745=CARTESIAN_POINT ( 'NONE',  ( 41.49999999999998579, 106.9282032302754999, 3.500000000000000000 ) ) ;
#13752=EDGE_LOOP ( 'NONE', ( #39643, #37908, #57667, #7036 ) ) ;
#13753=DIRECTION ( 'NONE',  ( 1.000000000000000000, 0.000000000000000000, 0.000000000000000000 ) ) ;
#13755=CIRCLE ( 'NONE', #63166, 0.4999999999999994449 ) ;
#13757=( NAMED_UNIT ( * ) PLANE_ANGLE_UNIT ( ) SI_UNIT ( $, .RADIAN. ) );
#13759=SURFACE_STYLE_USAGE ( .BOTH. , #7777 ) ;
#13761=ORIENTED_EDGE ( 'NONE', *, *, #801, .T. ) ;
#13767=ORIENTED_EDGE ( 'NONE', *, *, #2739, .F. ) ;
#13768=CARTESIAN_POINT ( 'NONE',  ( 23.21231517720797655, 117.4999999999999716, 9.500000000000000000 ) ) ;
#13769=CIRCLE ( 'NONE', #225, 0.5000000000000004441 ) ;
#13771=SURFACE_STYLE_FILL_AREA ( #54243 ) ;
#13773=CARTESIAN_POINT ( 'NONE',  ( -74.08452722063037754, 9.430195807687219656, -6.000000000000000000 ) ) ;
#13775=LINE ( 'NONE', #25019, #51768 ) ;
#13779=CARTESIAN_POINT ( 'NONE',  ( -5.598654528085806881, 139.7449999999999761, -7.705886871421374629 ) ) ;
#13784=CARTESIAN_POINT ( 'NONE',  ( 74.50000000000000000, -2.220952357103124925E-14, 9.500000000000000000 ) ) ;
#13788=( GEOMETRIC_REPRESENTATION_CONTEXT ( 3 ) GLOBAL_UNCERTAINTY_ASSIGNED_CONTEXT ( ( #68461 ) ) GLOBAL_UNIT_ASSIGNED_CONTEXT ( ( #55868, #35468, #56200 ) ) REPRESENTATION_CONTEXT ( 'NONE', 'WORKASPACE' ) );
#13792=SURFACE_STYLE_FILL_AREA ( #67252 ) ;
#13794=FILL_AREA_STYLE ('',( #61966 ) ) ;
#13795=VERTEX_POINT ( 'NONE', #7306 ) ;
#13798=( GEOMETRIC_REPRESENTATION_CONTEXT ( 3 ) GLOBAL_UNCERTAINTY_ASSIGNED_CONTEXT ( ( #50305 ) ) GLOBAL_UNIT_ASSIGNED_CONTEXT ( ( #9617, #4273, #43043 ) ) REPRESENTATION_CONTEXT ( 'NONE', 'WORKASPACE' ) );
#13799=( NAMED_UNIT ( * ) SI_UNIT ( $, .STERADIAN. ) SOLID_ANGLE_UNIT ( ) );
#13800=CARTESIAN_POINT ( 'NONE',  ( -45.54132543224191210, 7.945093266342319716, 6.500000000000000888 ) ) ;
#13801=CARTESIAN_POINT ( 'NONE',  ( 44.28021770739998431, 9.999999999999980460, 3.500000000000000000 ) ) ;
#13802=CIRCLE ( 'NONE', #34030, 0.5000000000000004441 ) ;
#13806=EDGE_LOOP ( 'NONE', ( #50700, #4875, #15046, #512 ) ) ;
#13809=CARTESIAN_POINT ( 'NONE',  ( -12.34222745343792127, 114.9999999999999574, -10.18181818181818166 ) ) ;
#13812=CARTESIAN_POINT ( 'NONE',  ( -60.00000000000000000, -2.024042244987997205E-14, -12.00000000000000000 ) ) ;
#13813=CARTESIAN_POINT ( 'NONE',  ( -8.102448949553181734, 115.8949999999999960, -5.886773742842749790 ) ) ;
#13815=EDGE_CURVE ( 'NONE', #25507, #67841, #27338, .T. ) ;
#13816=CYLINDRICAL_SURFACE ( 'NONE', #11701, 13.99999999999999822 ) ;
#13817=CARTESIAN_POINT ( 'NONE',  ( -8.102448949553179958, 114.0049999999999670, -5.886773742842749790 ) ) ;
#13819=DIRECTION ( 'NONE',  ( -1.000000000000000000, 0.000000000000000000, 0.000000000000000000 ) ) ;
#13822=CARTESIAN_POINT ( 'NONE',  ( -10.01517768586949231, 135.3049999999999784, -6.132527647946036459E-16 ) ) ;
#13823=UNCERTAINTY_MEASURE_WITH_UNIT (LENGTH_MEASURE( 1.000000000000000082E-05 ), #52497, 'distance_accuracy_value', 'NONE');
#13824=CARTESIAN_POINT ( 'NONE',  ( -41.49999999999997868, 10.49999999999998046, 3.000000000000000000 ) ) ;
#13827=CARTESIAN_POINT ( 'NONE',  ( -41.25908726609139876, 107.3516760703038102, 3.442203282073898141 ) ) ;
#13831=MECHANICAL_DESIGN_GEOMETRIC_PRESENTATION_REPRESENTATION('',(#17226),#50935);
#13834=ORIENTED_EDGE ( 'NONE', *, *, #64901, .T. ) ;
#13836=DIRECTION ( 'NONE',  ( 0.000000000000000000, 0.7071067811865469066, 0.7071067811865482389 ) ) ;
#13837=CARTESIAN_POINT ( 'NONE',  ( 72.50000000000000000, 14.49137674618942562, 10.00000000000000000 ) ) ;
#13844=ORIENTED_EDGE ( 'NONE', *, *, #25812, .F. ) ;
#13846=CIRCLE ( 'NONE', #49655, 0.5000000000000004441 ) ;
#13849=STYLED_ITEM ( 'NONE', ( #42599 ), #36174 ) ;
#13851=CARTESIAN_POINT ( 'NONE',  ( -8.102448949553179958, 140.4949999999999761, 5.886773742842747126 ) ) ;
#13854=MECHANICAL_DESIGN_GEOMETRIC_PRESENTATION_REPRESENTATION('',(#17257),#33095);
#13859=AXIS2_PLACEMENT_3D ( 'NONE', #41506, #52744, #25298 ) ;
#13864=SURFACE_STYLE_FILL_AREA ( #41673 ) ;
#13866=ORIENTED_EDGE ( 'NONE', *, *, #52172, .F. ) ;
#13869=DIRECTION ( 'NONE',  ( -0.000000000000000000, -0.000000000000000000, 1.000000000000000000 ) ) ;
#13874=MECHANICAL_DESIGN_GEOMETRIC_PRESENTATION_REPRESENTATION('',(#39708),#67763);
#13881=DIRECTION ( 'NONE',  ( -0.000000000000000000, -0.000000000000000000, -1.000000000000000000 ) ) ;
#13882=LINE ( 'NONE', #40287, #24793 ) ;
#13884=COLOUR_RGB ( '', 0.09019608, 0.27058824, 0.51372549) ;
#13886=CARTESIAN_POINT ( 'NONE',  ( 6.826472737025119919, 123.0070736234661553, 4.959722759717908325 ) ) ;
#13889=CIRCLE ( 'NONE', #21723, 0.5000000000000004441 ) ;
#13896=FACE_OUTER_BOUND ( 'NONE', #14501, .T. ) ;
#13897=CARTESIAN_POINT ( 'NONE',  ( 2.607480562269071989, 134.7070736234661297, 8.025000000000002132 ) ) ;
#13899=ORIENTED_EDGE ( 'NONE', *, *, #44074, .F. ) ;
#13905=VECTOR ( 'NONE', #57604, 1000.000000000000000 ) ;
#13909=( NAMED_UNIT ( * ) PLANE_ANGLE_UNIT ( ) SI_UNIT ( $, .RADIAN. ) );
#13912=CARTESIAN_POINT ( 'NONE',  ( -74.49999999999998579, 1.735173206890467813E-14, -10.00000000000000000 ) ) ;
#13914=ORIENTED_EDGE ( 'NONE', *, *, #68679, .T. ) ;
#13915=AXIS2_PLACEMENT_3D ( 'NONE', #24040, #45546, #45867 ) ;
#13916=EDGE_CURVE ( 'NONE', #10860, #27560, #34293, .T. ) ;
#13919=DIRECTION ( 'NONE',  ( 1.000000000000000000, 0.000000000000000000, 0.000000000000000000 ) ) ;
#13920=EDGE_CURVE ( 'NONE', #34398, #55502, #21101, .T. ) ;
#13922=ORIENTED_EDGE ( 'NONE', *, *, #39926, .T. ) ;
#13926=( GEOMETRIC_REPRESENTATION_CONTEXT ( 3 ) GLOBAL_UNCERTAINTY_ASSIGNED_CONTEXT ( ( #57197 ) ) GLOBAL_UNIT_ASSIGNED_CONTEXT ( ( #62497, #57220, #13973 ) ) REPRESENTATION_CONTEXT ( 'NONE', 'WORKASPACE' ) );
#13927=AXIS2_PLACEMENT_3D ( 'NONE', #6515, #47789, #42488 ) ;
#13930=CARTESIAN_POINT ( 'NONE',  ( -10.01517768586949408, 116.1949999999999932, -6.132527647946036459E-16 ) ) ;
#13935=CARTESIAN_POINT ( 'NONE',  ( -44.50000000000000000, 9.999999999999980460, -3.000000000000000444 ) ) ;
#13937=CARTESIAN_POINT ( 'NONE',  ( -60.00000000000000000, -2.024042244987997205E-14, 12.00000000000000000 ) ) ;
#13938=LINE ( 'NONE', #36820, #49332 ) ;
#13939=SURFACE_SIDE_STYLE ('',( #62114 ) ) ;
#13942=( NAMED_UNIT ( * ) PLANE_ANGLE_UNIT ( ) SI_UNIT ( $, .RADIAN. ) );
#13947=( BOUNDED_CURVE ( )  B_SPLINE_CURVE ( 3, ( #5938, #53460, #68602, #69296 ),
 .UNSPECIFIED., .F., .F. ) 
 B_SPLINE_CURVE_WITH_KNOTS ( ( 4, 4 ),
 ( 5.144579788448437441, 6.283185307179586232 ),
 .UNSPECIFIED. ) 
 CURVE ( )  GEOMETRIC_REPRESENTATION_ITEM ( )  RATIONAL_B_SPLINE_CURVE ( ( 1.000000000000000000, 0.8948513492540277614, 0.8948513492540277614, 1.000000000000000000 ) ) 
 REPRESENTATION_ITEM ( '' )  );
#13950=CARTESIAN_POINT ( 'NONE',  ( 20.57648123223228254, 110.4999999999999858, 10.27659574468085069 ) ) ;
#13955=COLOUR_RGB ( '', 0.72549020, 0.75294118, 0.79215686) ;
#13957=CARTESIAN_POINT ( 'NONE',  ( 8.102448949553183510, 152.1049999999999613, -5.886773742842746238 ) ) ;
#13958=DIRECTION ( 'NONE',  ( 1.000000000000000000, 0.000000000000000000, 0.000000000000000000 ) ) ;
#13962=( GEOMETRIC_REPRESENTATION_CONTEXT ( 3 ) GLOBAL_UNCERTAINTY_ASSIGNED_CONTEXT ( ( #55965 ) ) GLOBAL_UNIT_ASSIGNED_CONTEXT ( ( #6629, #44344, #39390 ) ) REPRESENTATION_CONTEXT ( 'NONE', 'WORKASPACE' ) );
#13963=( NAMED_UNIT ( * ) PLANE_ANGLE_UNIT ( ) SI_UNIT ( $, .RADIAN. ) );
#13964=COLOUR_RGB ( '', 0.72549020, 0.75294118, 0.79215686) ;
#13969=ORIENTED_EDGE ( 'NONE', *, *, #55922, .F. ) ;
#13970=CIRCLE ( 'NONE', #6085, 0.5000000000000004441 ) ;
#13972=VECTOR ( 'NONE', #8976, 1000.000000000000000 ) ;
#13973=( NAMED_UNIT ( * ) SI_UNIT ( $, .STERADIAN. ) SOLID_ANGLE_UNIT ( ) );
#13976=EDGE_CURVE ( 'NONE', #30278, #6517, #6470, .T. ) ;
#13977=FILL_AREA_STYLE_COLOUR ( '', #1172 ) ;
#13982=( LENGTH_UNIT ( ) NAMED_UNIT ( * ) SI_UNIT ( .MILLI., .METRE. ) );
#13986=VERTEX_POINT ( 'NONE', #15033 ) ;
#13988=CARTESIAN_POINT ( 'NONE',  ( -71.62068965517239860, 36.41396814395972115, 7.000000000000000000 ) ) ;
#13989=ORIENTED_EDGE ( 'NONE', *, *, #10355, .T. ) ;
#13993=EDGE_CURVE ( 'NONE', #28559, #10224, #61540, .T. ) ;
#13996=ORIENTED_EDGE ( 'NONE', *, *, #39135, .T. ) ;
#13998=CARTESIAN_POINT ( 'NONE',  ( -7.647808743681030030, 110.5000000000002984, 5.677732506914710875 ) ) ;
#13999=ADVANCED_FACE ( 'NONE', ( #26237 ), #15709, .F. ) ;
#14000=DIRECTION ( 'NONE',  ( -1.156482317317873451E-16, -1.000000000000000000, 0.000000000000000000 ) ) ;
#14003=CARTESIAN_POINT ( 'NONE',  ( 2.607480562269071989, 148.5929263765338249, 8.025000000000002132 ) ) ;
#14006=ORIENTED_EDGE ( 'NONE', *, *, #1527, .T. ) ;
#14008=DIRECTION ( 'NONE',  ( 1.000000000000000000, 0.000000000000000000, 0.000000000000000000 ) ) ;
#14009=CARTESIAN_POINT ( 'NONE',  ( -45.91547277936962956, 9.430195807687221432, 3.508932040081435222 ) ) ;
#14015=FILL_AREA_STYLE ('',( #24896 ) ) ;
#14016=CIRCLE ( 'NONE', #53346, 0.5000000000000004441 ) ;
#14026=CARTESIAN_POINT ( 'NONE',  ( 40.99999999999997868, 9.999999999999978684, 3.500000000000000000 ) ) ;
#14033=STYLED_ITEM ( 'NONE', ( #61635 ), #62492 ) ;
#14036=CARTESIAN_POINT ( 'NONE',  ( 41.26944598842810308, 107.7917661767790776, 3.849001801206918927 ) ) ;
#14038=EDGE_CURVE ( 'NONE', #5042, #48671, #47052, .T. ) ;
#14040=CARTESIAN_POINT ( 'NONE',  ( 12.34222745343792127, 149.9999999999999716, -10.18181818181818166 ) ) ;
#14045=MECHANICAL_DESIGN_GEOMETRIC_PRESENTATION_REPRESENTATION('',(#38788),#45521);
#14047=CARTESIAN_POINT ( 'NONE',  ( 3.094860106618435136, 122.4049999999999727, -9.525000000000000355 ) ) ;
#14057=AXIS2_PLACEMENT_3D ( 'NONE', #63531, #4781, #19913 ) ;
#14060=ADVANCED_FACE ( 'NONE', ( #69501 ), #36853, .T. ) ;
#14062=CARTESIAN_POINT ( 'NONE',  ( 6.826472737025119919, 135.0070736234661126, 4.959722759717908325 ) ) ;
#14068=EDGE_CURVE ( 'NONE', #30995, #50360, #45830, .T. ) ;
#14082=CARTESIAN_POINT ( 'NONE',  ( 60.00000000000000000, 1.797044900979284448E-15, -10.00000000000000000 ) ) ;
#14088=CARTESIAN_POINT ( 'NONE',  ( -5.598654528085806881, 136.7449999999999761, -7.705886871421374629 ) ) ;
#14091=DIRECTION ( 'NONE',  ( -0.000000000000000000, -0.000000000000000000, -1.000000000000000000 ) ) ;
#14092=CARTESIAN_POINT ( 'NONE',  ( 8.102448949553179958, 139.5049999999999955, 5.886773742842750679 ) ) ;
#14095=( NAMED_UNIT ( * ) SI_UNIT ( $, .STERADIAN. ) SOLID_ANGLE_UNIT ( ) );
#14097=CARTESIAN_POINT ( 'NONE',  ( -6.826472737025120807, 111.9929263765338021, 4.959722759717906548 ) ) ;
#14098=FILL_AREA_STYLE_COLOUR ( '', #32253 ) ;
#14099=FILL_AREA_STYLE ('',( #18418 ) ) ;
#14100=DIRECTION ( 'NONE',  ( 1.000000000000000000, 0.000000000000000000, -0.000000000000000000 ) ) ;
#14101=( LENGTH_UNIT ( ) NAMED_UNIT ( * ) SI_UNIT ( .MILLI., .METRE. ) );
#14107=EDGE_LOOP ( 'NONE', ( #69203, #55235, #43617 ) ) ;
#14112=DIRECTION ( 'NONE',  ( 1.000000000000000000, -0.000000000000000000, -0.000000000000000000 ) ) ;
#14113=( GEOMETRIC_REPRESENTATION_CONTEXT ( 3 ) GLOBAL_UNCERTAINTY_ASSIGNED_CONTEXT ( ( #62227 ) ) GLOBAL_UNIT_ASSIGNED_CONTEXT ( ( #49297, #40148, #7068 ) ) REPRESENTATION_CONTEXT ( 'NONE', 'WORKASPACE' ) );
#14116=LINE ( 'NONE', #35574, #66243 ) ;
#14121=CARTESIAN_POINT ( 'NONE',  ( -74.99999999999998579, 50.00000000000000000, 7.500000000000000000 ) ) ;
#14123=ORIENTED_EDGE ( 'NONE', *, *, #56962, .F. ) ;
#14128=EDGE_CURVE ( 'NONE', #22128, #16768, #11447, .T. ) ;
#14130=STYLED_ITEM ( 'NONE', ( #10487 ), #8375 ) ;
#14131=CARTESIAN_POINT ( 'NONE',  ( -74.17525885966198018, 9.083251256839373511, -6.320036396439323134 ) ) ;
#14134=LINE ( 'NONE', #62636, #39101 ) ;
#14135=CARTESIAN_POINT ( 'NONE',  ( -1.166476076187854022E-15, 134.9449999999999932, 9.525000000000000355 ) ) ;
#14139=AXIS2_PLACEMENT_3D ( 'NONE', #12891, #50882, #34354 ) ;
#14141=CARTESIAN_POINT ( 'NONE',  ( -23.21231517720798010, 117.4999999999999716, -9.500000000000000000 ) ) ;
#14145=EDGE_CURVE ( 'NONE', #40918, #29858, #37897, .T. ) ;
#14154=CARTESIAN_POINT ( 'NONE',  ( 60.00000000000000000, 1.797044900979284448E-15, -7.000000000000017764 ) ) ;
#14157=DIRECTION ( 'NONE',  ( 0.000000000000000000, 0.000000000000000000, 1.000000000000000000 ) ) ;
#14158=CARTESIAN_POINT ( 'NONE',  ( -45.00000000000000000, 8.456227461324044015, 6.943431694471519755 ) ) ;
#14160=ADVANCED_FACE ( 'NONE', ( #64906 ), #16756, .F. ) ;
#14166=DIRECTION ( 'NONE',  ( 0.000000000000000000, 0.000000000000000000, 1.000000000000000000 ) ) ;
#14167=ORIENTED_EDGE ( 'NONE', *, *, #53279, .T. ) ;
#14168=EDGE_CURVE ( 'NONE', #46059, #25577, #23058, .T. ) ;
#14171=CARTESIAN_POINT ( 'NONE',  ( -9.058813317711338797, 110.3449999999999847, 2.943386871421373563 ) ) ;
#14175=CARTESIAN_POINT ( 'NONE',  ( -74.99999999999998579, 50.00000000000000000, 10.50000000000000000 ) ) ;
#14177=ADVANCED_FACE ( 'NONE', ( #2204 ), #51176, .F. ) ;
#14178=CARTESIAN_POINT ( 'NONE',  ( -40.78947368421051323, 108.1536491499103505, -3.000000000000005773 ) ) ;
#14180=CARTESIAN_POINT ( 'NONE',  ( -8.102448949553181734, 141.0049999999999386, -5.886773742842749790 ) ) ;
#14181=DIRECTION ( 'NONE',  ( 0.000000000000000000, 0.000000000000000000, 1.000000000000000000 ) ) ;
#14183=( NAMED_UNIT ( * ) SI_UNIT ( $, .STERADIAN. ) SOLID_ANGLE_UNIT ( ) );
#14184=CIRCLE ( 'NONE', #5214, 1.000000000000000888 ) ;
#14186=SURFACE_STYLE_FILL_AREA ( #8567 ) ;
#14187=LINE ( 'NONE', #63412, #42949 ) ;
#14189=ORIENTED_EDGE ( 'NONE', *, *, #50517, .T. ) ;
#14190=CARTESIAN_POINT ( 'NONE',  ( 6.240333192270946405, 111.1483426130140515, 6.318785644388214884 ) ) ;
#14192=DIRECTION ( 'NONE',  ( 1.156482317317873451E-16, -1.000000000000000000, -0.000000000000000000 ) ) ;
#14195=FILL_AREA_STYLE ('',( #34948 ) ) ;
#14201=AXIS2_PLACEMENT_3D ( 'NONE', #67305, #19092, #7182 ) ;
#14203=CARTESIAN_POINT ( 'NONE',  ( 9.058813317711338797, 144.8449999999999989, -2.943386871421372675 ) ) ;
#14208=DIRECTION ( 'NONE',  ( 0.000000000000000000, 0.000000000000000000, -1.000000000000000000 ) ) ;
#14211=CARTESIAN_POINT ( 'NONE',  ( 2.607480562269107072, 120.9070736234661609, -8.024999999999979039 ) ) ;
#14213=SURFACE_STYLE_USAGE ( .BOTH. , #62032 ) ;
#14214=CARTESIAN_POINT ( 'NONE',  ( -8.102448949553181734, 112.8949999999999818, -5.886773742842749790 ) ) ;
#14217=CARTESIAN_POINT ( 'NONE',  ( 48.50000000000000000, 14.49137674618942562, -9.500000000000000000 ) ) ;
#14218=ORIENTED_EDGE ( 'NONE', *, *, #6667, .T. ) ;
#14219=( LENGTH_UNIT ( ) NAMED_UNIT ( * ) SI_UNIT ( .MILLI., .METRE. ) );
#14220=EDGE_CURVE ( 'NONE', #13679, #50952, #67007, .T. ) ;
#14223=EDGE_CURVE ( 'NONE', #18076, #62248, #66076, .T. ) ;
#14224=MECHANICAL_DESIGN_GEOMETRIC_PRESENTATION_REPRESENTATION('',(#9766),#32197);
#14231=ORIENTED_EDGE ( 'NONE', *, *, #64564, .T. ) ;
#14234=DIRECTION ( 'NONE',  ( -0.000000000000000000, -1.000000000000000000, -0.000000000000000000 ) ) ;
#14236=( BOUNDED_CURVE ( )  B_SPLINE_CURVE ( 2, ( #44025, #38747, #60154, #65782, #39084, #44716, #17936, #18291, #50641, #8073, #58555 ),
 .UNSPECIFIED., .F., .F. ) 
 B_SPLINE_CURVE_WITH_KNOTS ( ( 3, 2, 2, 2, 2, 3 ),
 ( 0.5882352941176473005, 0.5941176470588237502, 0.6000000000000001998, 0.6058823529411767606, 0.6117647058823533213, 0.6176470588235297710 ),
 .UNSPECIFIED. ) 
 CURVE ( )  GEOMETRIC_REPRESENTATION_ITEM ( )  RATIONAL_B_SPLINE_CURVE ( ( 0.9999999999999981126, 0.9510565162951554186, 1.000000000000000000, 0.9510565162951535312, 1.000000000000000000, 0.9510565162951535312, 1.000000000000000000, 0.9510565162951535312, 1.000000000000000000, 0.9510565162951507556, 1.000000000000002665 ) ) 
 REPRESENTATION_ITEM ( '' )  );
#14237=FACE_OUTER_BOUND ( 'NONE', #5427, .T. ) ;
#14240=ORIENTED_EDGE ( 'NONE', *, *, #20051, .T. ) ;
#14242=FACE_OUTER_BOUND ( 'NONE', #43470, .T. ) ;
#14244=DIRECTION ( 'NONE',  ( 0.000000000000000000, 0.000000000000000000, 1.000000000000000000 ) ) ;
#14245=CARTESIAN_POINT ( 'NONE',  ( -6.826472737025120807, 136.5070736234661410, -4.959722759717907437 ) ) ;
#14247=EDGE_LOOP ( 'NONE', ( #69529, #11152, #30136, #11030, #65413, #16880, #22777 ) ) ;
#14250=CIRCLE ( 'NONE', #44627, 17.50000000000000000 ) ;
#14254=CARTESIAN_POINT ( 'NONE',  ( 0.000000000000000000, 151.0570736234661524, -8.025000000000000355 ) ) ;
#14259=ORIENTED_EDGE ( 'NONE', *, *, #21567, .T. ) ;
#14263=EDGE_LOOP ( 'NONE', ( #63314, #60583, #16993, #57720 ) ) ;
#14265=AXIS2_PLACEMENT_3D ( 'NONE', #39226, #40523, #61936 ) ;
#14266=DIRECTION ( 'NONE',  ( 0.000000000000000000, 0.000000000000000000, 1.000000000000000000 ) ) ;
#14270=SURFACE_STYLE_USAGE ( .BOTH. , #24454 ) ;
#14271=VERTEX_POINT ( 'NONE', #44887 ) ;
#14276=CARTESIAN_POINT ( 'NONE',  ( -8.102448949553179958, 115.8949999999999818, -5.886773742842749790 ) ) ;
#14284=FILL_AREA_STYLE ('',( #31138 ) ) ;
#14288=EDGE_CURVE ( 'NONE', #30516, #31691, #55991, .T. ) ;
#14292=LINE ( 'NONE', #42128, #12268 ) ;
#14294=EDGE_CURVE ( 'NONE', #4798, #21468, #36910, .T. ) ;
#14298=CARTESIAN_POINT ( 'NONE',  ( -34.99999999999999289, 99.99999999999998579, -3.500000000000000000 ) ) ;
#14299=EDGE_CURVE ( 'NONE', #34430, #5028, #9972, .T. ) ;
#14301=CARTESIAN_POINT ( 'NONE',  ( -8.102448949553181734, 156.6049999999999329, 5.886773742842747126 ) ) ;
#14306=DIRECTION ( 'NONE',  ( 0.000000000000000000, -1.000000000000000000, 0.000000000000000000 ) ) ;
#14314=CARTESIAN_POINT ( 'NONE',  ( 0.000000000000000000, 154.9999999999999716, 0.000000000000000000 ) ) ;
#14315=LINE ( 'NONE', #20279, #8166 ) ;
#14316=ORIENTED_EDGE ( 'NONE', *, *, #6491, .F. ) ;
#14319=CARTESIAN_POINT ( 'NONE',  ( -4.716976649647097730, 109.3570736234661496, -6.492361379858953896 ) ) ;
#14320=DIRECTION ( 'NONE',  ( 1.000000000000000000, 0.000000000000000000, 0.000000000000000000 ) ) ;
#14323=CIRCLE ( 'NONE', #54727, 0.5000000000000004441 ) ;
#14326=DIRECTION ( 'NONE',  ( -0.000000000000000000, -0.000000000000000000, -1.000000000000000000 ) ) ;
#14329=DIRECTION ( 'NONE',  ( 0.000000000000000000, 0.000000000000000000, 1.000000000000000000 ) ) ;
#14333=DIRECTION ( 'NONE',  ( 1.000000000000000000, 0.000000000000000000, 0.000000000000000000 ) ) ;
#14335=CARTESIAN_POINT ( 'NONE',  ( 0.000000000000000000, 149.9429263765338476, -8.025000000000000355 ) ) ;
#14336=PRESENTATION_STYLE_ASSIGNMENT (( #3032 ) ) ;
#14341=FILL_AREA_STYLE ('',( #25246 ) ) ;
#14344=( NAMED_UNIT ( * ) SI_UNIT ( $, .STERADIAN. ) SOLID_ANGLE_UNIT ( ) );
#14347=FILL_AREA_STYLE_COLOUR ( '', #69069 ) ;
#14348=DIRECTION ( 'NONE',  ( 1.000000000000000000, 0.000000000000000000, 0.000000000000000000 ) ) ;
#14360=( LENGTH_UNIT ( ) NAMED_UNIT ( * ) SI_UNIT ( .MILLI., .METRE. ) );
#14362=EDGE_CURVE ( 'NONE', #31626, #31846, #18913, .T. ) ;
#14364=AXIS2_PLACEMENT_3D ( 'NONE', #64215, #33262, #5809 ) ;
#14366=DIRECTION ( 'NONE',  ( -0.7071067811865549002, 8.659560562355022838E-17, 0.7071067811865401342 ) ) ;
#14367=ORIENTED_EDGE ( 'NONE', *, *, #32546, .T. ) ;
#14371=CARTESIAN_POINT ( 'NONE',  ( 7.647808743684392674, 154.4999999999999432, 5.677732506910178500 ) ) ;
#14372=LINE ( 'NONE', #3794, #20234 ) ;
#14376=CARTESIAN_POINT ( 'NONE',  ( -8.102448949553181734, 126.0049999999999812, -5.886773742842749790 ) ) ;
#14382=UNCERTAINTY_MEASURE_WITH_UNIT (LENGTH_MEASURE( 1.000000000000000082E-05 ), #20916, 'distance_accuracy_value', 'NONE');
#14383=FILL_AREA_STYLE_COLOUR ( '', #37179 ) ;
#14385=EDGE_CURVE ( 'NONE', #51271, #51980, #26150, .T. ) ;
#14388=DIRECTION ( 'NONE',  ( -1.000000000000000000, 0.000000000000000000, 0.000000000000000000 ) ) ;
#14389=( NAMED_UNIT ( * ) SI_UNIT ( $, .STERADIAN. ) SOLID_ANGLE_UNIT ( ) );
#14391=STYLED_ITEM ( 'NONE', ( #19060 ), #9712 ) ;
#14394=UNCERTAINTY_MEASURE_WITH_UNIT (LENGTH_MEASURE( 1.000000000000000082E-05 ), #25620, 'distance_accuracy_value', 'NONE');
#14395=DIRECTION ( 'NONE',  ( 0.000000000000000000, 0.000000000000000000, 1.000000000000000000 ) ) ;
#14397=TOROIDAL_SURFACE ( 'NONE', #22292, 1.000000000000000000, 0.5000000000000000000 ) ;
#14398=SURFACE_SIDE_STYLE ('',( #19684 ) ) ;
#14400=CARTESIAN_POINT ( 'NONE',  ( -14.98999599679679662, 146.4999999999999716, 10.00000000000000000 ) ) ;
#14401=ORIENTED_EDGE ( 'NONE', *, *, #28329, .T. ) ;
#14403=VERTEX_POINT ( 'NONE', #46636 ) ;
#14407=EDGE_LOOP ( 'NONE', ( #42689, #55624, #25481, #67073 ) ) ;
#14408=AXIS2_PLACEMENT_3D ( 'NONE', #51872, #13168, #34627 ) ;
#14410=CARTESIAN_POINT ( 'NONE',  ( 8.102448949553181734, 141.3949999999999818, 5.886773742842750679 ) ) ;
#14412=ORIENTED_EDGE ( 'NONE', *, *, #42787, .F. ) ;
#14413=FILL_AREA_STYLE_COLOUR ( '', #30767 ) ;
#14414=CARTESIAN_POINT ( 'NONE',  ( 5.598654528085805993, 145.3549999999999898, 7.705886871421374629 ) ) ;
#14415=LINE ( 'NONE', #46126, #56366 ) ;
#14418=CARTESIAN_POINT ( 'NONE',  ( -6.826472737025120807, 120.9929263765338021, 4.959722759717906548 ) ) ;
#14419=( LENGTH_UNIT ( ) NAMED_UNIT ( * ) SI_UNIT ( .MILLI., .METRE. ) );
#14421=CYLINDRICAL_SURFACE ( 'NONE', #12105, 30.00000000000000000 ) ;
#14423=CARTESIAN_POINT ( 'NONE',  ( -15.48999599679679662, 146.4999999999999716, -7.500000000000000000 ) ) ;
#14424=DIRECTION ( 'NONE',  ( -0.7833176619561891263, -0.6216216216216174928, -0.000000000000000000 ) ) ;
#14427=EDGE_LOOP ( 'NONE', ( #19653, #25852 ) ) ;
#14432=SURFACE_STYLE_USAGE ( .BOTH. , #31295 ) ;
#14433=UNCERTAINTY_MEASURE_WITH_UNIT (LENGTH_MEASURE( 1.000000000000000082E-05 ), #48150, 'distance_accuracy_value', 'NONE');
#14435=SURFACE_SIDE_STYLE ('',( #57010 ) ) ;
#14436=CARTESIAN_POINT ( 'NONE',  ( -2.607480562269032021, 151.2070736234661581, -8.025000000000032330 ) ) ;
#14437=FACE_OUTER_BOUND ( 'NONE', #35391, .T. ) ;
#14438=CARTESIAN_POINT ( 'NONE',  ( -9.827790563157511022E-16, 145.4429263765338192, 8.025000000000000355 ) ) ;
#14441=ORIENTED_EDGE ( 'NONE', *, *, #22431, .T. ) ;
#14444=DIRECTION ( 'NONE',  ( 1.000000000000000000, 0.000000000000000000, 0.000000000000000000 ) ) ;
#14448=ADVANCED_BREP_SHAPE_REPRESENTATION ( '', ( #3964, #42840 ), #2244 ) ;
#14454=ORIENTED_EDGE ( 'NONE', *, *, #48019, .F. ) ;
#14456=CARTESIAN_POINT ( 'NONE',  ( -75.00000000000000000, 9.609776836748626039, -6.329322064279367943 ) ) ;
#14461=CARTESIAN_POINT ( 'NONE',  ( 9.058813317711338797, 144.8449999999999989, -2.943386871421372675 ) ) ;
#14464=DIRECTION ( 'NONE',  ( 0.000000000000000000, 0.000000000000000000, 1.000000000000000000 ) ) ;
#14465=VECTOR ( 'NONE', #25865, 1000.000000000000000 ) ;
#14467=UNCERTAINTY_MEASURE_WITH_UNIT (LENGTH_MEASURE( 1.000000000000000082E-05 ), #11371, 'distance_accuracy_value', 'NONE');
#14472=( NAMED_UNIT ( * ) PLANE_ANGLE_UNIT ( ) SI_UNIT ( $, .RADIAN. ) );
#14475=FACE_OUTER_BOUND ( 'NONE', #37484, .T. ) ;
#14476=DIRECTION ( 'NONE',  ( 0.000000000000000000, 1.000000000000000000, 0.000000000000000000 ) ) ;
#14477=DIRECTION ( 'NONE',  ( 0.000000000000000000, 0.000000000000000000, 1.000000000000000000 ) ) ;
#14483=SURFACE_SIDE_STYLE ('',( #51794 ) ) ;
#14484=FACE_OUTER_BOUND ( 'NONE', #49891, .T. ) ;
#14487=VECTOR ( 'NONE', #58932, 1000.000000000000000 ) ;
#14488=ORIENTED_EDGE ( 'NONE', *, *, #64613, .F. ) ;
#14491=DIRECTION ( 'NONE',  ( 0.000000000000000000, 0.000000000000000000, 1.000000000000000000 ) ) ;
#14493=ORIENTED_EDGE ( 'NONE', *, *, #48720, .T. ) ;
#14494=STYLED_ITEM ( 'NONE', ( #10498 ), #19930 ) ;
#14497=CARTESIAN_POINT ( 'NONE',  ( -23.21231517720797655, 113.4999999999999858, 9.500000000000000000 ) ) ;
#14498=CARTESIAN_POINT ( 'NONE',  ( -1.166476076187854022E-15, 113.9449999999999932, 9.525000000000000355 ) ) ;
#14499=VECTOR ( 'NONE', #59593, 1000.000000000000000 ) ;
#14501=EDGE_LOOP ( 'NONE', ( #45522, #40831, #23448, #64003 ) ) ;
#14503=CARTESIAN_POINT ( 'NONE',  ( -5.598654528085806881, 122.8549999999999898, -7.705886871421374629 ) ) ;
#14507=CARTESIAN_POINT ( 'NONE',  ( 8.102448949553183510, 137.1049999999999898, -5.886773742842746238 ) ) ;
#14508=UNCERTAINTY_MEASURE_WITH_UNIT (LENGTH_MEASURE( 1.000000000000000082E-05 ), #22104, 'distance_accuracy_value', 'NONE');
#14513=CARTESIAN_POINT ( 'NONE',  ( 51.49999999999998579, 2.837994680254535968E-15, 10.00000000000000000 ) ) ;
#14514=CARTESIAN_POINT ( 'NONE',  ( 60.00000000000000000, 1.797044900979284448E-15, -12.00000000000000000 ) ) ;
#14517=CARTESIAN_POINT ( 'NONE',  ( 8.325601791849228661, 111.5275746901607619, -1.721597945495230819 ) ) ;
#14518=SURFACE_STYLE_USAGE ( .BOTH. , #4283 ) ;
#14521=CARTESIAN_POINT ( 'NONE',  ( -69.49999999999997158, 50.00000000000000000, -6.500000000000000000 ) ) ;
#14524=AXIS2_PLACEMENT_3D ( 'NONE', #51490, #46623, #2559 ) ;
#14526=ADVANCED_FACE ( 'NONE', ( #52235 ), #43689, .T. ) ;
#14534=CIRCLE ( 'NONE', #25778, 0.5000000000000004441 ) ;
#14536=CARTESIAN_POINT ( 'NONE',  ( -1.166476076187854022E-15, 152.9449999999999932, 9.525000000000000355 ) ) ;
#14545=DIRECTION ( 'NONE',  ( 0.000000000000000000, 0.000000000000000000, -1.000000000000000000 ) ) ;
#14546=FILL_AREA_STYLE ('',( #62716 ) ) ;
#14550=CARTESIAN_POINT ( 'NONE',  ( 3.094860106618435136, 124.2949999999999733, -9.525000000000000355 ) ) ;
#14553=EDGE_CURVE ( 'NONE', #29454, #10808, #34690, .T. ) ;
#14557=VECTOR ( 'NONE', #59165, 1000.000000000000000 ) ;
#14560=SURFACE_STYLE_USAGE ( .BOTH. , #26489 ) ;
#14562=CARTESIAN_POINT ( 'NONE',  ( 60.00000000000000000, 1.797044900979284448E-15, 12.00000000000000000 ) ) ;
#14568=B_SPLINE_CURVE_WITH_KNOTS ( 'NONE', 3,
 ( #1678, #23872, #28076, #17259, #12969, #7364, #2351, #38721, #33395, #34429, #7008, #54824, #49590, #1321 ),
 .UNSPECIFIED., .F., .F.,
 ( 4, 2, 2, 2, 2, 2, 4 ),
 ( 0.000000000000000000, 0.0005917671672764528764, 0.001183534334552905753, 0.001479417918191132733, 0.001775301501829359713, 0.002071185085467586694, 0.002367068669105813674 ),
 .UNSPECIFIED. ) ;
#14569=CARTESIAN_POINT ( 'NONE',  ( -6.826472737025120807, 125.1070736234661496, 4.959722759717906548 ) ) ;
#14578=SURFACE_STYLE_FILL_AREA ( #57128 ) ;
#14580=CARTESIAN_POINT ( 'NONE',  ( 7.632228543268607446, 123.1570736234661609, 2.479861379858954606 ) ) ;
#14583=FACE_OUTER_BOUND ( 'NONE', #31004, .T. ) ;
#14587=SURFACE_STYLE_USAGE ( .BOTH. , #67710 ) ;
#14589=DIRECTION ( 'NONE',  ( -1.000000000000000000, 0.000000000000000000, 0.000000000000000000 ) ) ;
#14592=CARTESIAN_POINT ( 'NONE',  ( -8.437984349512095861, 130.8070736234661524, -5.166775262442723748E-16 ) ) ;
#14593=EDGE_CURVE ( 'NONE', #34471, #40156, #39205, .T. ) ;
#14598=LINE ( 'NONE', #4017, #45510 ) ;
#14599=ORIENTED_EDGE ( 'NONE', *, *, #26752, .T. ) ;
#14603=PRESENTATION_STYLE_ASSIGNMENT (( #25153 ) ) ;
#14604=AXIS2_PLACEMENT_3D ( 'NONE', #46097, #18304, #61201 ) ;
#14606=ORIENTED_EDGE ( 'NONE', *, *, #61684, .T. ) ;
#14607=SURFACE_STYLE_USAGE ( .BOTH. , #63139 ) ;
#14609=CIRCLE ( 'NONE', #21313, 0.5000000000000004441 ) ;
#14611=FACE_OUTER_BOUND ( 'NONE', #65876, .T. ) ;
#14615=AXIS2_PLACEMENT_3D ( 'NONE', #67973, #18720, #68307 ) ;
#14617=DIRECTION ( 'NONE',  ( 0.000000000000000000, -1.000000000000000000, 0.000000000000000000 ) ) ;
#14621=( NAMED_UNIT ( * ) PLANE_ANGLE_UNIT ( ) SI_UNIT ( $, .RADIAN. ) );
#14623=EDGE_CURVE ( 'NONE', #62586, #67110, #66124, .T. ) ;
#14626=ORIENTED_EDGE ( 'NONE', *, *, #61683, .T. ) ;
#14627=CARTESIAN_POINT ( 'NONE',  ( 15.48999599679679662, 146.4999999999999716, -7.000000000000000000 ) ) ;
#14629=( NAMED_UNIT ( * ) SI_UNIT ( $, .STERADIAN. ) SOLID_ANGLE_UNIT ( ) );
#14632=MECHANICAL_DESIGN_GEOMETRIC_PRESENTATION_REPRESENTATION('',(#12346),#32576);
#14633=CARTESIAN_POINT ( 'NONE',  ( -3.094860106618434248, 125.7949999999999591, 9.525000000000000355 ) ) ;
#14638=VERTEX_POINT ( 'NONE', #68115 ) ;
#14639=CIRCLE ( 'NONE', #25863, 13.49999999999999822 ) ;
#14643=LINE ( 'NONE', #41392, #69498 ) ;
#14644=FACE_OUTER_BOUND ( 'NONE', #54566, .T. ) ;
#14651=CARTESIAN_POINT ( 'NONE',  ( -75.00000000000000000, 33.00000000000000000, 6.500000000000000000 ) ) ;
#14652=SURFACE_SIDE_STYLE ('',( #68126 ) ) ;
#14653=AXIS2_PLACEMENT_3D ( 'NONE', #19991, #67872, #30194 ) ;
#14654=DIRECTION ( 'NONE',  ( 0.000000000000000000, 0.000000000000000000, 1.000000000000000000 ) ) ;
#14658=CARTESIAN_POINT ( 'NONE',  ( -1.166476076187854022E-15, 160.0550000000000068, 9.525000000000000355 ) ) ;
#14663=EDGE_CURVE ( 'NONE', #39204, #43611, #41393, .T. ) ;
#14669=( GEOMETRIC_REPRESENTATION_CONTEXT ( 3 ) GLOBAL_UNCERTAINTY_ASSIGNED_CONTEXT ( ( #21482 ) ) GLOBAL_UNIT_ASSIGNED_CONTEXT ( ( #26503, #64503, #26158 ) ) REPRESENTATION_CONTEXT ( 'NONE', 'WORKASPACE' ) );
#14671=CIRCLE ( 'NONE', #11254, 0.5000000000000004441 ) ;
#14672=DIRECTION ( 'NONE',  ( -0.000000000000000000, 1.000000000000000000, -0.000000000000000000 ) ) ;
#14674=SURFACE_STYLE_USAGE ( .BOTH. , #15044 ) ;
#14677=VERTEX_POINT ( 'NONE', #35749 ) ;
#14681=CARTESIAN_POINT ( 'NONE',  ( -20.71462254620879762, 114.5909367637873402, 9.999999999998797406 ) ) ;
#14682=DIRECTION ( 'NONE',  ( 0.000000000000000000, 1.000000000000000000, -0.000000000000000000 ) ) ;
#14685=ORIENTED_EDGE ( 'NONE', *, *, #28671, .T. ) ;
#14687=DIRECTION ( 'NONE',  ( 0.000000000000000000, 0.000000000000000000, 1.000000000000000000 ) ) ;
#14688=FILL_AREA_STYLE ('',( #51026 ) ) ;
#14690=CARTESIAN_POINT ( 'NONE',  ( -9.058813317711337021, 117.1549999999999869, -2.943386871421374895 ) ) ;
#14692=EDGE_CURVE ( 'NONE', #49243, #41309, #13938, .T. ) ;
#14700=ADVANCED_FACE ( 'NONE', ( #14644 ), #19555, .F. ) ;
#14702=ORIENTED_EDGE ( 'NONE', *, *, #32467, .F. ) ;
#14703=CARTESIAN_POINT ( 'NONE',  ( -6.826472737025120807, 153.3929263765338078, -4.959722759717907437 ) ) ;
#14704=CARTESIAN_POINT ( 'NONE',  ( 54.99999999999999289, 2.409368300552961372E-15, 11.50000000000003730 ) ) ;
#14705=DIRECTION ( 'NONE',  ( -1.274184670190250597E-16, 1.000000000000000000, 2.430666987507993885E-16 ) ) ;
#14706=EDGE_CURVE ( 'NONE', #62143, #39909, #15608, .T. ) ;
#14707=CARTESIAN_POINT ( 'NONE',  ( 60.00000000000000000, 1.797044900979284448E-15, 10.50000000000000000 ) ) ;
#14708=VERTEX_POINT ( 'NONE', #4054 ) ;
#14710=( NAMED_UNIT ( * ) SI_UNIT ( $, .STERADIAN. ) SOLID_ANGLE_UNIT ( ) );
#14712=SURFACE_STYLE_FILL_AREA ( #41459 ) ;
#14713=FILL_AREA_STYLE ('',( #42873 ) ) ;
#14716=CARTESIAN_POINT ( 'NONE',  ( -9.827790563157511022E-16, 140.5570736234661524, 8.025000000000000355 ) ) ;
#14717=( NAMED_UNIT ( * ) PLANE_ANGLE_UNIT ( ) SI_UNIT ( $, .RADIAN. ) );
#14718=AXIS2_PLACEMENT_3D ( 'NONE', #54444, #32298, #64990 ) ;
#14719=CARTESIAN_POINT ( 'NONE',  ( -74.35421852510367557, 8.378235220106981629, 6.482771786488847887 ) ) ;
#14723=ORIENTED_EDGE ( 'NONE', *, *, #62566, .F. ) ;
#14724=AXIS2_PLACEMENT_3D ( 'NONE', #9592, #52502, #4245 ) ;
#14725=ORIENTED_EDGE ( 'NONE', *, *, #55183, .F. ) ;
#14727=FACE_BOUND ( 'NONE', #67648, .T. ) ;
#14729=DIRECTION ( 'NONE',  ( 1.000000000000000000, 0.000000000000000000, 0.000000000000000000 ) ) ;
#14731=CARTESIAN_POINT ( 'NONE',  ( 15.48999599679679662, 117.9999999999999716, -7.000000000000000000 ) ) ;
#14734=DIRECTION ( 'NONE',  ( 1.000000000000000000, 0.000000000000000000, 0.000000000000000000 ) ) ;
#14740=CARTESIAN_POINT ( 'NONE',  ( 34.99999999999992895, 112.4999999999999858, 9.500000000000000000 ) ) ;
#14741=LINE ( 'NONE', #46800, #50449 ) ;
#14742=CYLINDRICAL_SURFACE ( 'NONE', #48524, 16.00000000000000000 ) ;
#14744=CARTESIAN_POINT ( 'NONE',  ( 8.876997378076488587, 154.5000000000000284, -3.480709456473927599 ) ) ;
#14745=SURFACE_STYLE_USAGE ( .BOTH. , #62900 ) ;
#14746=FILL_AREA_STYLE_COLOUR ( '', #17988 ) ;
#14748=CARTESIAN_POINT ( 'NONE',  ( 8.102448949553181734, 124.5049999999999812, 5.886773742842750679 ) ) ;
#14750=CARTESIAN_POINT ( 'NONE',  ( -75.00000000000001421, 9.585601099689363025, -6.373959028214384759 ) ) ;
#14754=DIRECTION ( 'NONE',  ( -1.000000000000000000, 0.000000000000000000, 0.000000000000000000 ) ) ;
#14758=AXIS2_PLACEMENT_3D ( 'NONE', #42129, #31149, #52644 ) ;
#14761=( LENGTH_UNIT ( ) NAMED_UNIT ( * ) SI_UNIT ( .MILLI., .METRE. ) );
#14762=AXIS2_PLACEMENT_3D ( 'NONE', #11979, #33438, #49631 ) ;
#14763=CARTESIAN_POINT ( 'NONE',  ( 6.826472737025121695, 135.6070736234661638, -4.959722759717905660 ) ) ;
#14765=DIRECTION ( 'NONE',  ( 0.2413793103448194644, -0.9704308468600220117, 0.000000000000000000 ) ) ;
#14768=FACE_OUTER_BOUND ( 'NONE', #29749, .T. ) ;
#14773=AXIS2_PLACEMENT_3D ( 'NONE', #50147, #66294, #17783 ) ;
#14777=ORIENTED_EDGE ( 'NONE', *, *, #69029, .T. ) ;
#14780=EDGE_LOOP ( 'NONE', ( #5959, #50891, #429, #28490 ) ) ;
#14786=CARTESIAN_POINT ( 'NONE',  ( -74.99999999999998579, 50.00000000000000000, -12.00000000000000000 ) ) ;
#14787=CARTESIAN_POINT ( 'NONE',  ( -9.058813317711337021, 152.0449999999999875, -2.943386871421374895 ) ) ;
#14789=ORIENTED_EDGE ( 'NONE', *, *, #26039, .F. ) ;
#14790=CIRCLE ( 'NONE', #47585, 0.5000000000000004441 ) ;
#14791=( NAMED_UNIT ( * ) PLANE_ANGLE_UNIT ( ) SI_UNIT ( $, .RADIAN. ) );
#14792=CARTESIAN_POINT ( 'NONE',  ( 5.598654528085805993, 154.3549999999999898, 7.705886871421374629 ) ) ;
#14794=( LENGTH_UNIT ( ) NAMED_UNIT ( * ) SI_UNIT ( .MILLI., .METRE. ) );
#14796=CARTESIAN_POINT ( 'NONE',  ( 6.826472737025119919, 112.8929263765338078, 4.959722759717908325 ) ) ;
#14797=SURFACE_STYLE_USAGE ( .BOTH. , #30233 ) ;
#14799=CARTESIAN_POINT ( 'NONE',  ( 45.65811388300840434, 10.21937129433612057, -6.292893218813452982 ) ) ;
#14800=ORIENTED_EDGE ( 'NONE', *, *, #53837, .T. ) ;
#14802=ORIENTED_EDGE ( 'NONE', *, *, #30032, .F. ) ;
#14804=CARTESIAN_POINT ( 'NONE',  ( 34.99999999999999289, 99.99999999999998579, -7.000000000000000000 ) ) ;
#14805=( NAMED_UNIT ( * ) SI_UNIT ( $, .STERADIAN. ) SOLID_ANGLE_UNIT ( ) );
#14806=COLOUR_RGB ( '', 0.31764706, 0.68627451, 0.89019608) ;
#14809=ORIENTED_EDGE ( 'NONE', *, *, #55673, .F. ) ;
#14810=( NAMED_UNIT ( * ) SI_UNIT ( $, .STERADIAN. ) SOLID_ANGLE_UNIT ( ) );
#14811=( GEOMETRIC_REPRESENTATION_CONTEXT ( 3 ) GLOBAL_UNCERTAINTY_ASSIGNED_CONTEXT ( ( #37548 ) ) GLOBAL_UNIT_ASSIGNED_CONTEXT ( ( #59572, #32857, #759 ) ) REPRESENTATION_CONTEXT ( 'NONE', 'WORKASPACE' ) );
#14812=ADVANCED_FACE ( 'NONE', ( #26877 ), #28631, .F. ) ;
#14817=DIRECTION ( 'NONE',  ( -0.000000000000000000, -0.000000000000000000, -1.000000000000000000 ) ) ;
#14818=ORIENTED_EDGE ( 'NONE', *, *, #62637, .T. ) ;
#14819=VERTEX_POINT ( 'NONE', #11069 ) ;
#14826=DIRECTION ( 'NONE',  ( 1.000000000000000000, 0.000000000000000000, 0.000000000000000000 ) ) ;
#14827=CIRCLE ( 'NONE', #12561, 0.5000000000000004441 ) ;
#14828=MECHANICAL_DESIGN_GEOMETRIC_PRESENTATION_REPRESENTATION('',(#57483),#27130);
#14832=MECHANICAL_DESIGN_GEOMETRIC_PRESENTATION_REPRESENTATION('',(#11435),#48536);
#14835=AXIS2_PLACEMENT_3D ( 'NONE', #33845, #65875, #27855 ) ;
#14838=CARTESIAN_POINT ( 'NONE',  ( -9.058813317711337021, 152.0449999999999875, -2.943386871421374895 ) ) ;
#14845=ORIENTED_EDGE ( 'NONE', *, *, #22172, .T. ) ;
#14849=( GEOMETRIC_REPRESENTATION_CONTEXT ( 3 ) GLOBAL_UNCERTAINTY_ASSIGNED_CONTEXT ( ( #26522 ) ) GLOBAL_UNIT_ASSIGNED_CONTEXT ( ( #42779, #22657, #33553 ) ) REPRESENTATION_CONTEXT ( 'NONE', 'WORKASPACE' ) );
#14850=CARTESIAN_POINT ( 'NONE',  ( 71.99999999999998579, 119.9999999999997868, 9.500000000000000000 ) ) ;
#14852=DIRECTION ( 'NONE',  ( 0.000000000000000000, -1.000000000000000000, 0.000000000000000000 ) ) ;
#14855=MECHANICAL_DESIGN_GEOMETRIC_PRESENTATION_REPRESENTATION('',(#26019),#1258);
#14857=AXIS2_PLACEMENT_3D ( 'NONE', #5332, #33805, #27122 ) ;
#14858=CIRCLE ( 'NONE', #32820, 0.5000000000000004441 ) ;
#14859=CARTESIAN_POINT ( 'NONE',  ( -24.21231517720798010, 113.4999999999999858, 7.500000000000000000 ) ) ;
#14860=CARTESIAN_POINT ( 'NONE',  ( 0.000000000000000000, 119.9429263765338050, -8.025000000000000355 ) ) ;
#14863=( NAMED_UNIT ( * ) SI_UNIT ( $, .STERADIAN. ) SOLID_ANGLE_UNIT ( ) );
#14867=DIRECTION ( 'NONE',  ( 0.000000000000000000, 1.000000000000000000, -0.000000000000000000 ) ) ;
#14870=EDGE_CURVE ( 'NONE', #46789, #55490, #51523, .T. ) ;
#14874=CARTESIAN_POINT ( 'NONE',  ( -9.058813317711338797, 125.3449999999999847, 2.943386871421373563 ) ) ;
#14875=ADVANCED_FACE ( 'NONE', ( #29326 ), #33596, .T. ) ;
#14876=AXIS2_PLACEMENT_3D ( 'NONE', #9428, #69455, #58905 ) ;
#14880=CARTESIAN_POINT ( 'NONE',  ( -3.094860106618434248, 120.9049999999999869, 9.525000000000000355 ) ) ;
#14884=CARTESIAN_POINT ( 'NONE',  ( 9.058813317711337021, 142.6549999999999727, 2.943386871421375783 ) ) ;
#14889=CARTESIAN_POINT ( 'NONE',  ( -41.16151714082912605, 107.5071857241661348, 3.372843186988513597 ) ) ;
#14890=AXIS2_PLACEMENT_3D ( 'NONE', #35921, #48231, #30613 ) ;
#14892=FACE_OUTER_BOUND ( 'NONE', #66873, .T. ) ;
#14895=FILL_AREA_STYLE_COLOUR ( '', #19414 ) ;
#14898=ORIENTED_EDGE ( 'NONE', *, *, #43266, .T. ) ;
#14901=PRESENTATION_STYLE_ASSIGNMENT (( #14518 ) ) ;
#14903=DIRECTION ( 'NONE',  ( 1.000000000000000000, 0.000000000000000000, 0.000000000000000000 ) ) ;
#14913=AXIS2_PLACEMENT_3D ( 'NONE', #7641, #2295, #29442 ) ;
#14914=CARTESIAN_POINT ( 'NONE',  ( 10.01517768586949408, 153.6949999999999932, 1.839758294383810543E-15 ) ) ;
#14918=SURFACE_STYLE_USAGE ( .BOTH. , #24731 ) ;
#14919=AXIS2_PLACEMENT_3D ( 'NONE', #6523, #16787, #22380 ) ;
#14921=SURFACE_STYLE_USAGE ( .BOTH. , #42033 ) ;
#14925=CARTESIAN_POINT ( 'NONE',  ( -5.598654528085806881, 121.7449999999999903, -7.705886871421374629 ) ) ;
#14926=MECHANICAL_DESIGN_GEOMETRIC_PRESENTATION_REPRESENTATION('',(#38551),#22735);
#14931=AXIS2_PLACEMENT_3D ( 'NONE', #8214, #68340, #3214 ) ;
#14932=FILL_AREA_STYLE_COLOUR ( '', #59469 ) ;
#14935=DIRECTION ( 'NONE',  ( -0.000000000000000000, -0.000000000000000000, -1.000000000000000000 ) ) ;
#14939=AXIS2_PLACEMENT_3D ( 'NONE', #40673, #52273, #3666 ) ;
#14941=DIRECTION ( 'NONE',  ( 0.000000000000000000, 0.000000000000000000, -1.000000000000000000 ) ) ;
#14945=VERTEX_POINT ( 'NONE', #4305 ) ;
#14957=ORIENTED_EDGE ( 'NONE', *, *, #51549, .F. ) ;
#14962=CARTESIAN_POINT ( 'NONE',  ( 7.632228543268608334, 135.4570736234661581, -2.479861379858951942 ) ) ;
#14963=SURFACE_STYLE_FILL_AREA ( #27448 ) ;
#14964=ADVANCED_FACE ( 'NONE', ( #51855 ), #57821, .F. ) ;
#14972=CARTESIAN_POINT ( 'NONE',  ( 7.632228543268607446, 143.0429263765338135, 2.479861379858954606 ) ) ;
#14973=DIRECTION ( 'NONE',  ( 1.000000000000000000, 0.000000000000000000, 0.000000000000000000 ) ) ;
#14979=( LENGTH_UNIT ( ) NAMED_UNIT ( * ) SI_UNIT ( .MILLI., .METRE. ) );
#14985=ADVANCED_FACE ( 'NONE', ( #26483 ), #719, .F. ) ;
#14987=UNCERTAINTY_MEASURE_WITH_UNIT (LENGTH_MEASURE( 1.000000000000000082E-05 ), #62540, 'distance_accuracy_value', 'NONE');
#14988=ORIENTED_EDGE ( 'NONE', *, *, #30509, .F. ) ;
#14991=FILL_AREA_STYLE ('',( #48395 ) ) ;
#14992=CARTESIAN_POINT ( 'NONE',  ( 71.50000000000000000, 14.49137674618942562, 7.500000000000000000 ) ) ;
#14993=ORIENTED_EDGE ( 'NONE', *, *, #13658, .T. ) ;
#14997=FACE_OUTER_BOUND ( 'NONE', #28350, .T. ) ;
#14999=B_SPLINE_CURVE_WITH_KNOTS ( 'NONE', 3,
 ( #9479, #53075, #63947, #57653, #8770, #30543, #47129, #26311 ),
 .UNSPECIFIED., .F., .F.,
 ( 4, 2, 2, 4 ),
 ( 0.000000000000000000, 0.0004792974172913012877, 0.0007189461259369623941, 0.0009585948345826236089 ),
 .UNSPECIFIED. ) ;
#15000=CARTESIAN_POINT ( 'NONE',  ( -8.102448949553179958, 127.8949999999999534, -5.886773742842749790 ) ) ;
#15005=DIRECTION ( 'NONE',  ( 1.000000000000000000, 0.000000000000000000, 0.000000000000000000 ) ) ;
#15006=ORIENTED_EDGE ( 'NONE', *, *, #49184, .F. ) ;
#15014=( GEOMETRIC_REPRESENTATION_CONTEXT ( 3 ) GLOBAL_UNCERTAINTY_ASSIGNED_CONTEXT ( ( #43259 ) ) GLOBAL_UNIT_ASSIGNED_CONTEXT ( ( #62247, #40139, #50325 ) ) REPRESENTATION_CONTEXT ( 'NONE', 'WORKASPACE' ) );
#15019=CARTESIAN_POINT ( 'NONE',  ( -44.50000000000000000, 10.49999999999998224, -3.500000000000000000 ) ) ;
#15021=( NAMED_UNIT ( * ) PLANE_ANGLE_UNIT ( ) SI_UNIT ( $, .RADIAN. ) );
#15023=UNCERTAINTY_MEASURE_WITH_UNIT (LENGTH_MEASURE( 1.000000000000000082E-05 ), #594, 'distance_accuracy_value', 'NONE');
#15026=DIRECTION ( 'NONE',  ( 1.000000000000000000, 0.000000000000000000, 0.000000000000000000 ) ) ;
#15029=CARTESIAN_POINT ( 'NONE',  ( 8.102448949553181734, 157.5050000000000239, 5.886773742842750679 ) ) ;
#15030=SURFACE_STYLE_FILL_AREA ( #48436 ) ;
#15032=TOROIDAL_SURFACE ( 'NONE', #45373, 26.49999999999999645, 0.5000000000000000000 ) ;
#15033=CARTESIAN_POINT ( 'NONE',  ( -69.49999999999997158, 50.00000000000000000, 6.500000000000000000 ) ) ;
#15034=UNCERTAINTY_MEASURE_WITH_UNIT (LENGTH_MEASURE( 1.000000000000000082E-05 ), #28009, 'distance_accuracy_value', 'NONE');
#15037=( LENGTH_UNIT ( ) NAMED_UNIT ( * ) SI_UNIT ( .MILLI., .METRE. ) );
#15038=ADVANCED_FACE ( 'NONE', ( #53900 ), #59174, .T. ) ;
#15042=COLOUR_RGB ( '', 0.09019608, 0.27058824, 0.51372549) ;
#15044=SURFACE_SIDE_STYLE ('',( #67789 ) ) ;
#15045=EDGE_LOOP ( 'NONE', ( #19642, #5183, #55729, #18262 ) ) ;
#15046=ORIENTED_EDGE ( 'NONE', *, *, #24077, .T. ) ;
#15048=MECHANICAL_DESIGN_GEOMETRIC_PRESENTATION_REPRESENTATION('',(#8301),#9460);
#15050=B_SPLINE_CURVE_WITH_KNOTS ( 'NONE', 3,
 ( #39632, #6527, #65295, #17811, #1568, #29017, #44240, #66329 ),
 .UNSPECIFIED., .F., .F.,
 ( 4, 2, 2, 4 ),
 ( 0.000000000000000000, 0.0004782788118992547534, 0.0007174182178488821031, 0.0009565576237985095069 ),
 .UNSPECIFIED. ) ;
#15054=DIRECTION ( 'NONE',  ( 0.000000000000000000, 0.000000000000000000, 1.000000000000000000 ) ) ;
#15055=DIRECTION ( 'NONE',  ( 1.000000000000000000, 1.156482317317866302E-16, 0.000000000000000000 ) ) ;
#15058=ORIENTED_EDGE ( 'NONE', *, *, #46532, .F. ) ;
#15063=CARTESIAN_POINT ( 'NONE',  ( -8.102448949553181734, 117.6049999999999898, 5.886773742842747126 ) ) ;
#15065=ORIENTED_EDGE ( 'NONE', *, *, #7692, .T. ) ;
#15073=SURFACE_STYLE_FILL_AREA ( #25238 ) ;
#15076=CARTESIAN_POINT ( 'NONE',  ( -2.607480562269073765, 156.0929263765337964, -8.025000000000000355 ) ) ;
#15078=CARTESIAN_POINT ( 'NONE',  ( 0.000000000000000000, 128.9429263765338192, -8.025000000000000355 ) ) ;
#15083=CARTESIAN_POINT ( 'NONE',  ( 4.716976649647096842, 127.7429263765338163, 6.492361379858953896 ) ) ;
#15086=VECTOR ( 'NONE', #11141, 1000.000000000000000 ) ;
#15087=SURFACE_STYLE_USAGE ( .BOTH. , #20319 ) ;
#15088=CARTESIAN_POINT ( 'NONE',  ( 6.826472737025121695, 141.6070736234661354, -4.959722759717905660 ) ) ;
#15090=TOROIDAL_SURFACE ( 'NONE', #8337, 8.499999999999994671, 0.5000000000000000000 ) ;
#15093=DIRECTION ( 'NONE',  ( 0.000000000000000000, 0.000000000000000000, -1.000000000000000000 ) ) ;
#15100=SURFACE_STYLE_FILL_AREA ( #19641 ) ;
#15104=CARTESIAN_POINT ( 'NONE',  ( 45.65811388300841855, 10.21937129433612235, 6.000000000000000888 ) ) ;
#15105=CARTESIAN_POINT ( 'NONE',  ( 47.50000000000000000, 99.99999999999992895, 9.500000000000000000 ) ) ;
#15108=ORIENTED_EDGE ( 'NONE', *, *, #63256, .T. ) ;
#15110=FILL_AREA_STYLE ('',( #53414 ) ) ;
#15111=CIRCLE ( 'NONE', #53256, 0.5000000000000004441 ) ;
#15115=( LENGTH_UNIT ( ) NAMED_UNIT ( * ) SI_UNIT ( .MILLI., .METRE. ) );
#15116=( GEOMETRIC_REPRESENTATION_CONTEXT ( 3 ) GLOBAL_UNCERTAINTY_ASSIGNED_CONTEXT ( ( #53080 ) ) GLOBAL_UNIT_ASSIGNED_CONTEXT ( ( #16989, #21909, #49688 ) ) REPRESENTATION_CONTEXT ( 'NONE', 'WORKASPACE' ) );
#15118=CARTESIAN_POINT ( 'NONE',  ( 9.058813317711337021, 124.6549999999999869, 2.943386871421375783 ) ) ;
#15120=DIRECTION ( 'NONE',  ( -0.000000000000000000, -0.000000000000000000, 1.000000000000000000 ) ) ;
#15122=TOROIDAL_SURFACE ( 'NONE', #8319, 13.50000000000000178, 0.5000000000000000000 ) ;
#15123=CARTESIAN_POINT ( 'NONE',  ( -20.57648123223228254, 114.4999999999999574, 10.27659574468085069 ) ) ;
#15127=ORIENTED_EDGE ( 'NONE', *, *, #32272, .F. ) ;
#15128=EDGE_CURVE ( 'NONE', #43530, #44582, #28033, .T. ) ;
#15130=CARTESIAN_POINT ( 'NONE',  ( -8.437984349512095861, 145.8070736234661808, -5.166775262442723748E-16 ) ) ;
#15131=EDGE_CURVE ( 'NONE', #34861, #60166, #61737, .T. ) ;
#15135=CARTESIAN_POINT ( 'NONE',  ( -23.21231517720797655, 117.4999999999999716, -7.500000000000000000 ) ) ;
#15138=VECTOR ( 'NONE', #43140, 1000.000000000000000 ) ;
#15143=CARTESIAN_POINT ( 'NONE',  ( 24.21231517720798010, 112.4999999999999858, 10.00000000000000000 ) ) ;
#15149=DIRECTION ( 'NONE',  ( -0.7071067811865345831, 0.000000000000000000, -0.7071067811865603403 ) ) ;
#15151=VERTEX_POINT ( 'NONE', #7465 ) ;
#15155=CARTESIAN_POINT ( 'NONE',  ( -74.99999999999998579, 50.00000000000000000, -10.49999999999999822 ) ) ;
#15156=CARTESIAN_POINT ( 'NONE',  ( 0.000000000000000000, 145.4449999999999932, -9.525000000000000355 ) ) ;
#15159=VERTEX_POINT ( 'NONE', #17691 ) ;
#15162=CARTESIAN_POINT ( 'NONE',  ( 10.01517768586949408, 145.8050000000000068, 1.839758294383810543E-15 ) ) ;
#15163=PRESENTATION_STYLE_ASSIGNMENT (( #31276 ) ) ;
#15164=ORIENTED_EDGE ( 'NONE', *, *, #45859, .T. ) ;
#15165=CARTESIAN_POINT ( 'NONE',  ( -7.632228543268607446, 126.5429263765337993, -2.479861379858953718 ) ) ;
#15166=CARTESIAN_POINT ( 'NONE',  ( 0.000000000000000000, 114.9999999999999574, -10.50000000000000000 ) ) ;
#15167=UNCERTAINTY_MEASURE_WITH_UNIT (LENGTH_MEASURE( 1.000000000000000082E-05 ), #34951, 'distance_accuracy_value', 'NONE');
#15169=( LENGTH_UNIT ( ) NAMED_UNIT ( * ) SI_UNIT ( .MILLI., .METRE. ) );
#15170=( GEOMETRIC_REPRESENTATION_CONTEXT ( 3 ) GLOBAL_UNCERTAINTY_ASSIGNED_CONTEXT ( ( #5897 ) ) GLOBAL_UNIT_ASSIGNED_CONTEXT ( ( #23210, #7700, #24229 ) ) REPRESENTATION_CONTEXT ( 'NONE', 'WORKASPACE' ) );
#15171=( NAMED_UNIT ( * ) SI_UNIT ( $, .STERADIAN. ) SOLID_ANGLE_UNIT ( ) );
#15172=SURFACE_STYLE_FILL_AREA ( #52449 ) ;
#15174=ORIENTED_EDGE ( 'NONE', *, *, #59374, .F. ) ;
#15177=MECHANICAL_DESIGN_GEOMETRIC_PRESENTATION_REPRESENTATION('',(#41021),#18501);
#15179=SURFACE_SIDE_STYLE ('',( #39831 ) ) ;
#15180=FILL_AREA_STYLE_COLOUR ( '', #2545 ) ;
#15182=ORIENTED_EDGE ( 'NONE', *, *, #38171, .T. ) ;
#15184=UNCERTAINTY_MEASURE_WITH_UNIT (LENGTH_MEASURE( 1.000000000000000082E-05 ), #8547, 'distance_accuracy_value', 'NONE');
#15187=CARTESIAN_POINT ( 'NONE',  ( 75.00000000000000000, 19.62820054891024668, 6.498343828034905734 ) ) ;
#15188=EDGE_LOOP ( 'NONE', ( #18733, #3157, #16944, #30400 ) ) ;
#15189=AXIS2_PLACEMENT_3D ( 'NONE', #64369, #32008, #49497 ) ;
#15192=CARTESIAN_POINT ( 'NONE',  ( 45.00000000000000000, 10.69371294336137979, -4.000000000000000000 ) ) ;
#15200=AXIS2_PLACEMENT_3D ( 'NONE', #10955, #59132, #64429 ) ;
#15201=ORIENTED_EDGE ( 'NONE', *, *, #1733, .F. ) ;
#15205=CARTESIAN_POINT ( 'NONE',  ( 65.49999999999997158, 2.470600640510325396E-15, -12.00000000000000000 ) ) ;
#15206=( NAMED_UNIT ( * ) SI_UNIT ( $, .STERADIAN. ) SOLID_ANGLE_UNIT ( ) );
#15207=CARTESIAN_POINT ( 'NONE',  ( -8.102448949553181734, 146.4950000000000045, 5.886773742842747126 ) ) ;
#15212=UNCERTAINTY_MEASURE_WITH_UNIT (LENGTH_MEASURE( 1.000000000000000082E-05 ), #29633, 'distance_accuracy_value', 'NONE');
#15214=CARTESIAN_POINT ( 'NONE',  ( -41.05151532188900632, 107.6719357445258680, -3.224518739502661990 ) ) ;
#15223=LINE ( 'NONE', #21139, #64415 ) ;
#15224=LINE ( 'NONE', #3534, #32702 ) ;
#15235=VECTOR ( 'NONE', #19061, 1000.000000000000000 ) ;
#15238=ORIENTED_EDGE ( 'NONE', *, *, #53837, .F. ) ;
#15241=CARTESIAN_POINT ( 'NONE',  ( -3.094860106618434248, 122.7949999999999875, 9.525000000000000355 ) ) ;
#15243=VERTEX_POINT ( 'NONE', #3516 ) ;
#15245=CARTESIAN_POINT ( 'NONE',  ( -8.102448949553179958, 117.0049999999999670, -5.886773742842749790 ) ) ;
#15250=CARTESIAN_POINT ( 'NONE',  ( -3.094860106618434248, 147.9049999999999727, 9.525000000000000355 ) ) ;
#15260=CARTESIAN_POINT ( 'NONE',  ( 3.607123150363803710, 111.8710042735134209, -7.332553890433502808 ) ) ;
#15261=MECHANICAL_DESIGN_GEOMETRIC_PRESENTATION_REPRESENTATION('',(#53391),#19680);
#15263=DIRECTION ( 'NONE',  ( 0.000000000000000000, 0.000000000000000000, 1.000000000000000000 ) ) ;
#15266=SURFACE_STYLE_FILL_AREA ( #63421 ) ;
#15270=SURFACE_STYLE_FILL_AREA ( #47996 ) ;
#15278=CARTESIAN_POINT ( 'NONE',  ( 3.094860106618435136, 154.2949999999999875, -9.525000000000000355 ) ) ;
#15284=CARTESIAN_POINT ( 'NONE',  ( -44.99999999999998579, 119.9999999999999716, -7.500000000000000000 ) ) ;
#15285=SURFACE_STYLE_FILL_AREA ( #43073 ) ;
#15289=CARTESIAN_POINT ( 'NONE',  ( -8.102448949553181734, 115.8949999999999960, -5.886773742842749790 ) ) ;
#15291=AXIS2_PLACEMENT_3D ( 'NONE', #20403, #14424, #46495 ) ;
#15292=EDGE_CURVE ( 'NONE', #10407, #6631, #46531, .T. ) ;
#15293=FILL_AREA_STYLE_COLOUR ( '', #35888 ) ;
#15294=COLOUR_RGB ( '', 0.40784314, 0.44705882, 0.49803922) ;
#15296=CARTESIAN_POINT ( 'NONE',  ( 23.71231517720798010, 117.4999999999999716, 9.500000000000000000 ) ) ;
#15297=VERTEX_POINT ( 'NONE', #61951 ) ;
#15298=COLOUR_RGB ( '', 0.09019608, 0.27058824, 0.51372549) ;
#15306=CARTESIAN_POINT ( 'NONE',  ( -21.02379605245189964, 114.6413612702713465, -10.00000000000000000 ) ) ;
#15309=EDGE_CURVE ( 'NONE', #6894, #46319, #56568, .T. ) ;
#15313=MECHANICAL_DESIGN_GEOMETRIC_PRESENTATION_REPRESENTATION('',(#27594),#22007);
#15314=ADVANCED_FACE ( 'NONE', ( #4591 ), #10923, .T. ) ;
#15315=( NAMED_UNIT ( * ) PLANE_ANGLE_UNIT ( ) SI_UNIT ( $, .RADIAN. ) );
#15317=STYLED_ITEM ( 'NONE', ( #67129 ), #64439 ) ;
#15319=ORIENTED_EDGE ( 'NONE', *, *, #60488, .F. ) ;
#15320=CARTESIAN_POINT ( 'NONE',  ( 71.50000000000000000, 35.92875272052971525, -9.500000000000000000 ) ) ;
#15321=VERTEX_POINT ( 'NONE', #58419 ) ;
#15323=AXIS2_PLACEMENT_3D ( 'NONE', #49854, #7608, #1592 ) ;
#15324=( BOUNDED_CURVE ( )  B_SPLINE_CURVE ( 2, ( #42526, #68893, #19970, #9805, #24907, #51659, #9104, #47111, #52020, #69232, #25595 ),
 .UNSPECIFIED., .F., .F. ) 
 B_SPLINE_CURVE_WITH_KNOTS ( ( 3, 2, 2, 2, 2, 3 ),
 ( 0.08823529411764713393, 0.09411764705882361137, 0.1000000000000000888, 0.1058823529411765663, 0.1117647058823530437, 0.1176470588235295212 ),
 .UNSPECIFIED. ) 
 CURVE ( )  GEOMETRIC_REPRESENTATION_ITEM ( )  RATIONAL_B_SPLINE_CURVE ( ( 0.9999999999999994449, 0.9510565162951540863, 1.000000000000000000, 0.9510565162951535312, 1.000000000000000000, 0.9510565162951535312, 1.000000000000000000, 0.9510565162951535312, 1.000000000000000000, 0.9510565162951526430, 1.000000000000000888 ) ) 
 REPRESENTATION_ITEM ( '' )  );
#15325=CARTESIAN_POINT ( 'NONE',  ( -74.99999999999998579, 50.00000000000000000, -12.00000000000000000 ) ) ;
#15326=CARTESIAN_POINT ( 'NONE',  ( 4.716976649647096842, 146.8570736234661638, 6.492361379858953896 ) ) ;
#15328=DIRECTION ( 'NONE',  ( -0.000000000000000000, -0.000000000000000000, -1.000000000000000000 ) ) ;
#15330=UNCERTAINTY_MEASURE_WITH_UNIT (LENGTH_MEASURE( 1.000000000000000082E-05 ), #37642, 'distance_accuracy_value', 'NONE');
#15339=DIRECTION ( 'NONE',  ( -0.000000000000000000, -0.000000000000000000, -1.000000000000000000 ) ) ;
#15341=EDGE_LOOP ( 'NONE', ( #39744, #12932, #42164 ) ) ;
#15342=MECHANICAL_DESIGN_GEOMETRIC_PRESENTATION_REPRESENTATION('',(#42326),#66984);
#15344=DIRECTION ( 'NONE',  ( -0.000000000000000000, -1.000000000000000000, 0.000000000000000000 ) ) ;
#15346=ORIENTED_EDGE ( 'NONE', *, *, #19128, .T. ) ;
#15349=CARTESIAN_POINT ( 'NONE',  ( -44.99999999999998579, 119.9999999999999716, 9.500000000000000000 ) ) ;
#15350=PRESENTATION_STYLE_ASSIGNMENT (( #30779 ) ) ;
#15351=ORIENTED_EDGE ( 'NONE', *, *, #53071, .T. ) ;
#15353=EDGE_LOOP ( 'NONE', ( #32679, #21026, #58909, #11892 ) ) ;
#15356=CARTESIAN_POINT ( 'NONE',  ( -48.50000000000000000, 50.00000000000000000, 7.500000000000000000 ) ) ;
#15358=CARTESIAN_POINT ( 'NONE',  ( 10.01517768586949408, 120.6949999999999790, 1.839758294383810543E-15 ) ) ;
#15363=DIRECTION ( 'NONE',  ( 0.000000000000000000, 0.000000000000000000, -1.000000000000000000 ) ) ;
#15365=DIRECTION ( 'NONE',  ( -0.000000000000000000, -1.000000000000000000, -0.000000000000000000 ) ) ;
#15376=ORIENTED_EDGE ( 'NONE', *, *, #67393, .F. ) ;
#15380=CARTESIAN_POINT ( 'NONE',  ( 20.94636006565341191, 149.9999999999999716, -9.500000000000000000 ) ) ;
#15382=CARTESIAN_POINT ( 'NONE',  ( 10.01517768586949231, 151.8049999999999784, 1.839758294383810543E-15 ) ) ;
#15386=FILL_AREA_STYLE_COLOUR ( '', #53675 ) ;
#15393=ORIENTED_EDGE ( 'NONE', *, *, #5096, .T. ) ;
#15394=VERTEX_POINT ( 'NONE', #11957 ) ;
#15396=CARTESIAN_POINT ( 'NONE',  ( 4.716976649647096842, 116.8570736234661638, 6.492361379858953896 ) ) ;
#15397=SURFACE_STYLE_FILL_AREA ( #16088 ) ;
#15400=ORIENTED_EDGE ( 'NONE', *, *, #43665, .T. ) ;
#15404=CARTESIAN_POINT ( 'NONE',  ( -20.71231517720797655, 149.4999999999999716, 10.00000000000000000 ) ) ;
#15406=CARTESIAN_POINT ( 'NONE',  ( 9.058813317711338797, 121.9549999999999841, -2.943386871421372675 ) ) ;
#15407=SURFACE_SIDE_STYLE ('',( #26597 ) ) ;
#15410=CARTESIAN_POINT ( 'NONE',  ( -34.99999999999992895, 112.9999999999999858, 7.500000000000000000 ) ) ;
#15415=CARTESIAN_POINT ( 'NONE',  ( 8.468573276252547188, 153.4411133142860137, -0.3466697492072565168 ) ) ;
#15416=( NAMED_UNIT ( * ) PLANE_ANGLE_UNIT ( ) SI_UNIT ( $, .RADIAN. ) );
#15417=VERTEX_POINT ( 'NONE', #44018 ) ;
#15418=CARTESIAN_POINT ( 'NONE',  ( 7.632228543268607446, 155.0429263765338419, 2.479861379858954606 ) ) ;
#15420=DIRECTION ( 'NONE',  ( -1.000000000000000000, 0.000000000000000000, 0.000000000000000000 ) ) ;
#15421=AXIS2_PLACEMENT_3D ( 'NONE', #17325, #16965, #65474 ) ;
#15422=DIRECTION ( 'NONE',  ( -0.000000000000000000, -1.000000000000000000, -0.000000000000000000 ) ) ;
#15424=DIRECTION ( 'NONE',  ( -0.000000000000000000, -0.000000000000000000, 1.000000000000000000 ) ) ;
#15426=PRESENTATION_STYLE_ASSIGNMENT (( #19959 ) ) ;
#15432=FACE_OUTER_BOUND ( 'NONE', #36727, .T. ) ;
#15434=EDGE_LOOP ( 'NONE', ( #65022, #55958, #5638 ) ) ;
#15452=PRESENTATION_STYLE_ASSIGNMENT (( #56946 ) ) ;
#15454=CARTESIAN_POINT ( 'NONE',  ( -74.99999999976296294, 35.99166914554462693, -9.502300335055899438 ) ) ;
#15456=ADVANCED_FACE ( 'NONE', ( #7025 ), #6661, .T. ) ;
#15458=CARTESIAN_POINT ( 'NONE',  ( -3.094860106618432471, 125.7049999999999841, -9.525000000000000355 ) ) ;
#15460=CARTESIAN_POINT ( 'NONE',  ( -75.00000000000000000, 8.747703778475438341, -6.883446876413754190 ) ) ;
#15465=FACE_OUTER_BOUND ( 'NONE', #59171, .T. ) ;
#15467=EDGE_CURVE ( 'NONE', #7095, #35876, #43669, .T. ) ;
#15469=VECTOR ( 'NONE', #33709, 1000.000000000000000 ) ;
#15472=CARTESIAN_POINT ( 'NONE',  ( 48.50000000000000000, 14.49137674618942562, -7.500000000000000000 ) ) ;
#15474=EDGE_LOOP ( 'NONE', ( #31815, #52664, #14167, #10881, #7750 ) ) ;
#15475=LINE ( 'NONE', #20011, #64394 ) ;
#15484=DIRECTION ( 'NONE',  ( 1.000000000000000000, 1.453863484628180989E-14, 0.000000000000000000 ) ) ;
#15486=ORIENTED_EDGE ( 'NONE', *, *, #14299, .T. ) ;
#15487=SURFACE_STYLE_FILL_AREA ( #63305 ) ;
#15490=CARTESIAN_POINT ( 'NONE',  ( -9.058813317711338797, 152.3449999999999704, 2.943386871421373563 ) ) ;
#15492=EDGE_CURVE ( 'NONE', #29106, #12316, #4501, .T. ) ;
#15495=CARTESIAN_POINT ( 'NONE',  ( -3.094860106618432471, 152.7049999999999841, -9.525000000000000355 ) ) ;
#15497=VECTOR ( 'NONE', #45984, 1000.000000000000000 ) ;
#15500=CARTESIAN_POINT ( 'NONE',  ( -7.632228543268608334, 126.8429263765338249, 2.479861379858952830 ) ) ;
#15502=VECTOR ( 'NONE', #69556, 1000.000000000000000 ) ;
#15504=( NAMED_UNIT ( * ) PLANE_ANGLE_UNIT ( ) SI_UNIT ( $, .RADIAN. ) );
#15505=ORIENTED_EDGE ( 'NONE', *, *, #32174, .F. ) ;
#15506=CARTESIAN_POINT ( 'NONE',  ( -41.26944598842810308, 107.7917661767790776, -3.849001801206922480 ) ) ;
#15511=STYLED_ITEM ( 'NONE', ( #43848 ), #14160 ) ;
#15514=EDGE_CURVE ( 'NONE', #65971, #40883, #1697, .T. ) ;
#15517=LINE ( 'NONE', #57718, #50013 ) ;
#15520=VERTEX_POINT ( 'NONE', #2015 ) ;
#15535=DIRECTION ( 'NONE',  ( -0.000000000000000000, -0.000000000000000000, 1.000000000000000000 ) ) ;
#15536=DIRECTION ( 'NONE',  ( 0.000000000000000000, 1.000000000000000000, 0.000000000000000000 ) ) ;
#15537=( NAMED_UNIT ( * ) SI_UNIT ( $, .STERADIAN. ) SOLID_ANGLE_UNIT ( ) );
#15538=EDGE_CURVE ( 'NONE', #2689, #29106, #29518, .T. ) ;
#15540=CARTESIAN_POINT ( 'NONE',  ( 9.058813317711337021, 150.5449999999999875, 2.943386871421375783 ) ) ;
#15544=PRESENTATION_STYLE_ASSIGNMENT (( #22183 ) ) ;
#15545=ORIENTED_EDGE ( 'NONE', *, *, #67762, .T. ) ;
#15550=COLOUR_RGB ( '', 0.08235294, 0.09019608, 0.10196078) ;
#15551=VECTOR ( 'NONE', #36482, 1000.000000000000000 ) ;
#15552=EDGE_CURVE ( 'NONE', #24087, #57942, #24927, .T. ) ;
#15553=DIRECTION ( 'NONE',  ( -0.000000000000000000, -0.000000000000000000, 1.000000000000000000 ) ) ;
#15554=( NAMED_UNIT ( * ) PLANE_ANGLE_UNIT ( ) SI_UNIT ( $, .RADIAN. ) );
#15556=( GEOMETRIC_REPRESENTATION_CONTEXT ( 3 ) GLOBAL_UNCERTAINTY_ASSIGNED_CONTEXT ( ( #32005 ) ) GLOBAL_UNIT_ASSIGNED_CONTEXT ( ( #11715, #43765, #59897 ) ) REPRESENTATION_CONTEXT ( 'NONE', 'WORKASPACE' ) );
#15560=CARTESIAN_POINT ( 'NONE',  ( 72.50000000000000000, 13.41640786499872284, 10.00000000000000000 ) ) ;
#15561=CARTESIAN_POINT ( 'NONE',  ( -45.00000000000000000, 9.708372671849131663, 6.049000248776977173 ) ) ;
#15564=FILL_AREA_STYLE_COLOUR ( '', #13955 ) ;
#15568=DIRECTION ( 'NONE',  ( -0.000000000000000000, -0.000000000000000000, -1.000000000000000000 ) ) ;
#15569=( NAMED_UNIT ( * ) SI_UNIT ( $, .STERADIAN. ) SOLID_ANGLE_UNIT ( ) );
#15571=CARTESIAN_POINT ( 'NONE',  ( 10.01517768586949231, 120.6949999999999790, 1.839758294383810543E-15 ) ) ;
#15572=SURFACE_SIDE_STYLE ('',( #42669 ) ) ;
#15574=CARTESIAN_POINT ( 'NONE',  ( 9.058813317711338797, 118.9549999999999983, -2.943386871421372675 ) ) ;
#15576=STYLED_ITEM ( 'NONE', ( #63689 ), #43323 ) ;
#15578=ORIENTED_EDGE ( 'NONE', *, *, #18202, .F. ) ;
#15579=CARTESIAN_POINT ( 'NONE',  ( 10.01517768586949231, 151.8049999999999784, 1.839758294383810543E-15 ) ) ;
#15582=CARTESIAN_POINT ( 'NONE',  ( 24.21231517720798010, 113.4999999999999858, -9.500000000000000000 ) ) ;
#15585=ORIENTED_EDGE ( 'NONE', *, *, #52304, .F. ) ;
#15586=COLOUR_RGB ( '', 0.40784314, 0.44705882, 0.49803922) ;
#15590=EDGE_LOOP ( 'NONE', ( #33807, #53507, #22157, #25982 ) ) ;
#15593=DIRECTION ( 'NONE',  ( -0.7292845505553197105, 0.6842105263157864936, -0.000000000000000000 ) ) ;
#15594=EDGE_CURVE ( 'NONE', #65484, #5088, #14372, .T. ) ;
#15595=( LENGTH_UNIT ( ) NAMED_UNIT ( * ) SI_UNIT ( .MILLI., .METRE. ) );
#15596=ORIENTED_EDGE ( 'NONE', *, *, #16246, .T. ) ;
#15598=ORIENTED_EDGE ( 'NONE', *, *, #62081, .T. ) ;
#15599=COLOUR_RGB ( '', 0.40784314, 0.44705882, 0.49803922) ;
#15602=( LENGTH_UNIT ( ) NAMED_UNIT ( * ) SI_UNIT ( .MILLI., .METRE. ) );
#15603=ADVANCED_FACE ( 'NONE', ( #45404 ), #63758, .F. ) ;
#15608=CIRCLE ( 'NONE', #23446, 16.00000000000000000 ) ;
#15611=CARTESIAN_POINT ( 'NONE',  ( 8.102448949553179958, 147.3950000000000102, 5.886773742842750679 ) ) ;
#15619=ADVANCED_FACE ( 'NONE', ( #52725 ), #53736, .F. ) ;
#15621=CARTESIAN_POINT ( 'NONE',  ( 8.102448949553181734, 120.3949999999999960, 5.886773742842750679 ) ) ;
#15626=STYLED_ITEM ( 'NONE', ( #30533 ), #43534 ) ;
#15629=COLOUR_RGB ( '', 0.40784314, 0.44705882, 0.49803922) ;
#15631=CARTESIAN_POINT ( 'NONE',  ( -20.86663389611626229, 115.0293260623345475, -10.00000000000000000 ) ) ;
#15633=FACE_OUTER_BOUND ( 'NONE', #50494, .T. ) ;
#15634=VERTEX_POINT ( 'NONE', #60058 ) ;
#15640=SURFACE_STYLE_USAGE ( .BOTH. , #26504 ) ;
#15642=MECHANICAL_DESIGN_GEOMETRIC_PRESENTATION_REPRESENTATION('',(#35804),#6595);
#15643=AXIS2_PLACEMENT_3D ( 'NONE', #24, #21559, #32809 ) ;
#15648=( LENGTH_UNIT ( ) NAMED_UNIT ( * ) SI_UNIT ( .MILLI., .METRE. ) );
#15649=STYLED_ITEM ( 'NONE', ( #42720 ), #14985 ) ;
#15650=CARTESIAN_POINT ( 'NONE',  ( 6.826472737025121695, 147.6070736234661638, -4.959722759717905660 ) ) ;
#15660=VERTEX_POINT ( 'NONE', #55476 ) ;
#15664=CARTESIAN_POINT ( 'NONE',  ( -23.21231517720798010, 117.4999999999999716, -10.00000000000000000 ) ) ;
#15665=( NAMED_UNIT ( * ) SI_UNIT ( $, .STERADIAN. ) SOLID_ANGLE_UNIT ( ) );
#15666=VERTEX_POINT ( 'NONE', #1937 ) ;
#15667=FACE_OUTER_BOUND ( 'NONE', #1655, .T. ) ;
#15669=( GEOMETRIC_REPRESENTATION_CONTEXT ( 3 ) GLOBAL_UNCERTAINTY_ASSIGNED_CONTEXT ( ( #36968 ) ) GLOBAL_UNIT_ASSIGNED_CONTEXT ( ( #43826, #64555, #38559 ) ) REPRESENTATION_CONTEXT ( 'NONE', 'WORKASPACE' ) );
#15670=LINE ( 'NONE', #58920, #16672 ) ;
#15672=ORIENTED_EDGE ( 'NONE', *, *, #13731, .T. ) ;
#15673=SURFACE_STYLE_FILL_AREA ( #52621 ) ;
#15675=ORIENTED_EDGE ( 'NONE', *, *, #46595, .T. ) ;
#15676=COLOUR_RGB ( '', 0.31764706, 0.68627451, 0.89019608) ;
#15677=SURFACE_STYLE_FILL_AREA ( #63832 ) ;
#15678=CARTESIAN_POINT ( 'NONE',  ( -40.78947368421051323, 108.1536491499103505, 3.000000000000000000 ) ) ;
#15682=CARTESIAN_POINT ( 'NONE',  ( -1.166476076187854022E-15, 119.9449999999999790, 9.525000000000000355 ) ) ;
#15685=EDGE_CURVE ( 'NONE', #61874, #14945, #17851, .T. ) ;
#15688=SURFACE_STYLE_USAGE ( .BOTH. , #65234 ) ;
#15690=DIRECTION ( 'NONE',  ( 0.000000000000000000, -1.000000000000000000, 0.000000000000000000 ) ) ;
#15693=PLANE ( 'NONE',  #18447 ) ;
#15697=ORIENTED_EDGE ( 'NONE', *, *, #7213, .T. ) ;
#15701=FILL_AREA_STYLE_COLOUR ( '', #2301 ) ;
#15702=UNCERTAINTY_MEASURE_WITH_UNIT (LENGTH_MEASURE( 1.000000000000000082E-05 ), #60862, 'distance_accuracy_value', 'NONE');
#15704=( NAMED_UNIT ( * ) SI_UNIT ( $, .STERADIAN. ) SOLID_ANGLE_UNIT ( ) );
#15705=CIRCLE ( 'NONE', #7793, 0.5000000000000004441 ) ;
#15706=DIRECTION ( 'NONE',  ( 0.000000000000000000, 0.000000000000000000, 1.000000000000000000 ) ) ;
#15708=CARTESIAN_POINT ( 'NONE',  ( -49.12162162162162105, 13.70805908423323594, 9.500000000000000000 ) ) ;
#15709=PLANE ( 'NONE',  #3065 ) ;
#15711=CIRCLE ( 'NONE', #54979, 30.00000000000000000 ) ;
#15717=LINE ( 'NONE', #4415, #56075 ) ;
#15718=TOROIDAL_SURFACE ( 'NONE', #68477, 12.50000000000000000, 0.5000000000000000000 ) ;
#15722=DIRECTION ( 'NONE',  ( 1.000000000000000000, 0.000000000000000000, 0.000000000000000000 ) ) ;
#15724=VERTEX_POINT ( 'NONE', #7298 ) ;
#15725=CIRCLE ( 'NONE', #30288, 9.500000000000005329 ) ;
#15726=CARTESIAN_POINT ( 'NONE',  ( -4.716976649647098618, 116.2570736234661553, 6.492361379858953008 ) ) ;
#15730=FILL_AREA_STYLE_COLOUR ( '', #43207 ) ;
#15732=ORIENTED_EDGE ( 'NONE', *, *, #14553, .F. ) ;
#15737=CARTESIAN_POINT ( 'NONE',  ( 9.058813317711338797, 115.9549999999999841, -2.943386871421372675 ) ) ;
#15738=CARTESIAN_POINT ( 'NONE',  ( -71.62068965517238439, 63.58603185604027885, -7.500000000000000000 ) ) ;
#15740=MECHANICAL_DESIGN_GEOMETRIC_PRESENTATION_REPRESENTATION('',(#67388),#39304);
#15741=CARTESIAN_POINT ( 'NONE',  ( -44.99999999999977973, 149.4999999999999716, -9.500000000000000000 ) ) ;
#15743=ORIENTED_EDGE ( 'NONE', *, *, #35707, .F. ) ;
#15744=MECHANICAL_DESIGN_GEOMETRIC_PRESENTATION_REPRESENTATION('',(#31420),#3321);
#15748=( NAMED_UNIT ( * ) SI_UNIT ( $, .STERADIAN. ) SOLID_ANGLE_UNIT ( ) );
#15749=CARTESIAN_POINT ( 'NONE',  ( 15.48999599679679662, 146.4999999999999716, -7.500000000000000000 ) ) ;
#15751=CARTESIAN_POINT ( 'NONE',  ( -7.632228543268608334, 156.8429263765338249, 2.479861379858952830 ) ) ;
#15752=FACE_OUTER_BOUND ( 'NONE', #47030, .T. ) ;
#15753=AXIS2_PLACEMENT_3D ( 'NONE', #65776, #39077, #7024 ) ;
#15761=LINE ( 'NONE', #5168, #53760 ) ;
#15762=DIRECTION ( 'NONE',  ( 1.000000000000000000, 0.000000000000000000, 0.000000000000000000 ) ) ;
#15769=LINE ( 'NONE', #43228, #9209 ) ;
#15770=CARTESIAN_POINT ( 'NONE',  ( -9.827790563157511022E-16, 115.4429263765338192, 8.025000000000000355 ) ) ;
#15771=FACE_OUTER_BOUND ( 'NONE', #44586, .T. ) ;
#15772=ORIENTED_EDGE ( 'NONE', *, *, #43959, .T. ) ;
#15773=ORIENTED_EDGE ( 'NONE', *, *, #8836, .T. ) ;
#15775=PRESENTATION_STYLE_ASSIGNMENT (( #19639 ) ) ;
#15778=CARTESIAN_POINT ( 'NONE',  ( -48.50000000000000000, 14.49137674618942562, 7.000000000000000000 ) ) ;
#15785=DIRECTION ( 'NONE',  ( 0.000000000000000000, 0.000000000000000000, 1.000000000000000000 ) ) ;
#15790=FACE_OUTER_BOUND ( 'NONE', #57231, .T. ) ;
#15791=CARTESIAN_POINT ( 'NONE',  ( -74.61313452252784373, 36.44950204765962809, -10.00000000000000000 ) ) ;
#15793=CARTESIAN_POINT ( 'NONE',  ( 8.102448949553183510, 134.1049999999999329, -5.886773742842746238 ) ) ;
#15794=CARTESIAN_POINT ( 'NONE',  ( -2.607480562269073321, 126.0929263765338249, -8.025000000000000355 ) ) ;
#15798=UNCERTAINTY_MEASURE_WITH_UNIT (LENGTH_MEASURE( 1.000000000000000082E-05 ), #28420, 'distance_accuracy_value', 'NONE');
#15799=MECHANICAL_DESIGN_GEOMETRIC_PRESENTATION_REPRESENTATION('',(#45044),#41674);
#15802=DIRECTION ( 'NONE',  ( -0.000000000000000000, -0.000000000000000000, -1.000000000000000000 ) ) ;
#15804=CARTESIAN_POINT ( 'NONE',  ( -34.99999999999999289, 99.99999999999998579, 7.000000000000000000 ) ) ;
#15808=EDGE_LOOP ( 'NONE', ( #3387, #41785, #36162, #1480 ) ) ;
#15809=ORIENTED_EDGE ( 'NONE', *, *, #3438, .F. ) ;
#15810=FILL_AREA_STYLE ('',( #31248 ) ) ;
#15812=CARTESIAN_POINT ( 'NONE',  ( 6.826472737025119919, 130.8929263765338362, 4.959722759717908325 ) ) ;
#15818=CYLINDRICAL_SURFACE ( 'NONE', #8290, 0.5000000000000004441 ) ;
#15825=FILL_AREA_STYLE ('',( #42256 ) ) ;
#15827=ORIENTED_EDGE ( 'NONE', *, *, #12447, .F. ) ;
#15829=FACE_OUTER_BOUND ( 'NONE', #6460, .T. ) ;
#15830=VERTEX_POINT ( 'NONE', #8683 ) ;
#15833=STYLED_ITEM ( 'NONE', ( #25144 ), #34693 ) ;
#15834=CARTESIAN_POINT ( 'NONE',  ( -3.094860106618434248, 146.7950000000000159, 9.525000000000000355 ) ) ;
#15835=EDGE_CURVE ( 'NONE', #10952, #35366, #8344, .T. ) ;
#15838=CARTESIAN_POINT ( 'NONE',  ( -8.102448949553179958, 147.6049999999999898, 5.886773742842747126 ) ) ;
#15840=CARTESIAN_POINT ( 'NONE',  ( -48.00000000000000000, 14.49137674618942562, 7.500000000000000000 ) ) ;
#15842=CARTESIAN_POINT ( 'NONE',  ( -4.716976649647097730, 126.2429263765338163, -6.492361379858953896 ) ) ;
#15844=COLOUR_RGB ( '', 0.40784314, 0.44705882, 0.49803922) ;
#15847=ORIENTED_EDGE ( 'NONE', *, *, #21849, .F. ) ;
#15849=CARTESIAN_POINT ( 'NONE',  ( -41.38221592241692548, 107.7000202725880911, -3.906946855746217473 ) ) ;
#15851=EDGE_LOOP ( 'NONE', ( #13899, #18181, #23243, #1679 ) ) ;
#15853=DIRECTION ( 'NONE',  ( 0.000000000000000000, -0.000000000000000000, 1.000000000000000000 ) ) ;
#15861=FACE_OUTER_BOUND ( 'NONE', #56170, .T. ) ;
#15862=ORIENTED_EDGE ( 'NONE', *, *, #50069, .F. ) ;
#15863=( GEOMETRIC_REPRESENTATION_CONTEXT ( 3 ) GLOBAL_UNCERTAINTY_ASSIGNED_CONTEXT ( ( #8689 ) ) GLOBAL_UNIT_ASSIGNED_CONTEXT ( ( #38219, #42132, #52983 ) ) REPRESENTATION_CONTEXT ( 'NONE', 'WORKASPACE' ) );
#15866=CARTESIAN_POINT ( 'NONE',  ( -69.99999999999998579, 50.00000000000000000, 6.999999999999988454 ) ) ;
#15872=DIRECTION ( 'NONE',  ( -0.000000000000000000, -1.000000000000000000, -0.000000000000000000 ) ) ;
#15874=ORIENTED_EDGE ( 'NONE', *, *, #11192, .T. ) ;
#15876=LINE ( 'NONE', #32357, #4313 ) ;
#15881=CARTESIAN_POINT ( 'NONE',  ( -1.166476076187854022E-15, 152.9449999999999932, 9.525000000000000355 ) ) ;
#15891=VERTEX_POINT ( 'NONE', #27513 ) ;
#15896=AXIS2_PLACEMENT_3D ( 'NONE', #13092, #45156, #61286 ) ;
#15902=STYLED_ITEM ( 'NONE', ( #33187 ), #17314 ) ;
#15909=DIRECTION ( 'NONE',  ( -0.9704308468600219006, 0.2413793103448194366, 0.000000000000000000 ) ) ;
#15913=ORIENTED_EDGE ( 'NONE', *, *, #66134, .F. ) ;
#15916=EDGE_CURVE ( 'NONE', #16524, #25661, #727, .T. ) ;
#15919=FACE_OUTER_BOUND ( 'NONE', #33359, .T. ) ;
#15923=CARTESIAN_POINT ( 'NONE',  ( 8.102448949553181734, 117.3949999999999818, 5.886773742842750679 ) ) ;
#15927=CARTESIAN_POINT ( 'NONE',  ( 8.102448949553181734, 119.1049999999999756, -5.886773742842746238 ) ) ;
#15932=CARTESIAN_POINT ( 'NONE',  ( -41.84210526315789025, 107.2928455055531600, -4.000000000000000888 ) ) ;
#15934=CARTESIAN_POINT ( 'NONE',  ( 0.000000000000000000, 143.5549999999999784, -9.525000000000000355 ) ) ;
#15935=UNCERTAINTY_MEASURE_WITH_UNIT (LENGTH_MEASURE( 1.000000000000000082E-05 ), #41590, 'distance_accuracy_value', 'NONE');
#15941=CARTESIAN_POINT ( 'NONE',  ( 40.78947368421051323, 108.1536491499103363, -3.000000000000000444 ) ) ;
#15943=DIRECTION ( 'NONE',  ( 1.000000000000000000, 1.027984282060330356E-15, 0.000000000000000000 ) ) ;
#15944=( LENGTH_UNIT ( ) NAMED_UNIT ( * ) SI_UNIT ( .MILLI., .METRE. ) );
#15947=ORIENTED_EDGE ( 'NONE', *, *, #3531, .F. ) ;
#15951=DIRECTION ( 'NONE',  ( -0.000000000000000000, 1.000000000000000000, -0.000000000000000000 ) ) ;
#15952=( NAMED_UNIT ( * ) PLANE_ANGLE_UNIT ( ) SI_UNIT ( $, .RADIAN. ) );
#15953=CARTESIAN_POINT ( 'NONE',  ( -24.21231517720798010, 113.4999999999999858, -9.500000000000000000 ) ) ;
#15959=ORIENTED_EDGE ( 'NONE', *, *, #60564, .T. ) ;
#15962=DIRECTION ( 'NONE',  ( -1.000000000000000000, 0.000000000000000000, 0.000000000000000000 ) ) ;
#15965=CARTESIAN_POINT ( 'NONE',  ( -3.094860106618432471, 148.5949999999999136, -9.525000000000000355 ) ) ;
#15967=VECTOR ( 'NONE', #12095, 1000.000000000000000 ) ;
#15969=ORIENTED_EDGE ( 'NONE', *, *, #49668, .F. ) ;
#15971=CARTESIAN_POINT ( 'NONE',  ( -60.00000000000000000, -2.024042244987997205E-14, 10.00000000000000000 ) ) ;
#15972=DIRECTION ( 'NONE',  ( 1.000000000000000000, 0.000000000000000000, 0.000000000000000000 ) ) ;
#15974=CARTESIAN_POINT ( 'NONE',  ( 3.094860106618431583, 123.0949999999999704, 9.525000000000000355 ) ) ;
#15986=VECTOR ( 'NONE', #44785, 1000.000000000000000 ) ;
#15989=CARTESIAN_POINT ( 'NONE',  ( -20.57648123434812959, 114.5706806360227290, -10.27659574044459667 ) ) ;
#15991=ORIENTED_EDGE ( 'NONE', *, *, #26062, .F. ) ;
#15995=AXIS2_PLACEMENT_3D ( 'NONE', #34061, #27378, #1296 ) ;
#15997=( NAMED_UNIT ( * ) PLANE_ANGLE_UNIT ( ) SI_UNIT ( $, .RADIAN. ) );
#15998=DIRECTION ( 'NONE',  ( -3.552713678800500929E-15, 0.000000000000000000, 1.000000000000000000 ) ) ;
#16001=ADVANCED_FACE ( 'NONE', ( #64487 ), #33646, .T. ) ;
#16007=LINE ( 'NONE', #47702, #64395 ) ;
#16008=CARTESIAN_POINT ( 'NONE',  ( -44.50000000000000000, 99.99999999999992895, -4.000000000000000000 ) ) ;
#16009=CARTESIAN_POINT ( 'NONE',  ( -7.632228543268608334, 139.9570736234661581, 2.479861379858952830 ) ) ;
#16014=UNCERTAINTY_MEASURE_WITH_UNIT (LENGTH_MEASURE( 1.000000000000000082E-05 ), #7411, 'distance_accuracy_value', 'NONE');
#16015=VECTOR ( 'NONE', #43800, 1000.000000000000000 ) ;
#16017=ORIENTED_EDGE ( 'NONE', *, *, #26958, .T. ) ;
#16020=CARTESIAN_POINT ( 'NONE',  ( -44.99154893936433552, 9.591540374752316467, -3.000000000000000444 ) ) ;
#16023=EDGE_LOOP ( 'NONE', ( #9989, #38321, #33772, #67051 ) ) ;
#16025=SURFACE_STYLE_FILL_AREA ( #64167 ) ;
#16028=DIRECTION ( 'NONE',  ( 0.000000000000000000, 0.000000000000000000, 1.000000000000000000 ) ) ;
#16034=FILL_AREA_STYLE_COLOUR ( '', #54772 ) ;
#16039=ORIENTED_EDGE ( 'NONE', *, *, #39333, .F. ) ;
#16045=CARTESIAN_POINT ( 'NONE',  ( -5.598654528085808657, 119.6449999999999818, 7.705886871421373741 ) ) ;
#16047=STYLED_ITEM ( 'NONE', ( #27886 ), #54765 ) ;
#16048=AXIS2_PLACEMENT_3D ( 'NONE', #3029, #8719, #13638 ) ;
#16049=ORIENTED_EDGE ( 'NONE', *, *, #57961, .F. ) ;
#16052=DIRECTION ( 'NONE',  ( 0.000000000000000000, 0.000000000000000000, -1.000000000000000000 ) ) ;
#16056=VECTOR ( 'NONE', #16129, 1000.000000000000000 ) ;
#16061=PRESENTATION_STYLE_ASSIGNMENT (( #479 ) ) ;
#16062=AXIS2_PLACEMENT_3D ( 'NONE', #13768, #7459, #29940 ) ;
#16063=CARTESIAN_POINT ( 'NONE',  ( 60.00000000000000000, 1.797044900979284448E-15, 12.00000000000000000 ) ) ;
#16064=SURFACE_STYLE_USAGE ( .BOTH. , #19906 ) ;
#16069=EDGE_CURVE ( 'NONE', #27439, #67575, #813, .T. ) ;
#16071=AXIS2_PLACEMENT_3D ( 'NONE', #26909, #59641, #11460 ) ;
#16078=EDGE_CURVE ( 'NONE', #2723, #36960, #66805, .T. ) ;
#16084=FILL_AREA_STYLE_COLOUR ( '', #31843 ) ;
#16086=CARTESIAN_POINT ( 'NONE',  ( -7.632228543268607446, 115.6570736234661467, -2.479861379858953718 ) ) ;
#16088=FILL_AREA_STYLE ('',( #63552 ) ) ;
#16090=PRESENTATION_STYLE_ASSIGNMENT (( #42841 ) ) ;
#16091=ORIENTED_EDGE ( 'NONE', *, *, #23310, .T. ) ;
#16092=EDGE_LOOP ( 'NONE', ( #3100, #52839, #11590, #45759 ) ) ;
#16093=( GEOMETRIC_REPRESENTATION_CONTEXT ( 3 ) GLOBAL_UNCERTAINTY_ASSIGNED_CONTEXT ( ( #368 ) ) GLOBAL_UNIT_ASSIGNED_CONTEXT ( ( #47808, #21007, #48827 ) ) REPRESENTATION_CONTEXT ( 'NONE', 'WORKASPACE' ) );
#16100=CARTESIAN_POINT ( 'NONE',  ( -8.102448949553181734, 129.6049999999999613, 5.886773742842747126 ) ) ;
#16101=( NAMED_UNIT ( * ) SI_UNIT ( $, .STERADIAN. ) SOLID_ANGLE_UNIT ( ) );
#16103=PRESENTATION_STYLE_ASSIGNMENT (( #26928 ) ) ;
#16106=STYLED_ITEM ( 'NONE', ( #45038 ), #26271 ) ;
#16109=EDGE_LOOP ( 'NONE', ( #29270, #8383, #21698, #46672 ) ) ;
#16110=CARTESIAN_POINT ( 'NONE',  ( -9.827790563157511022E-16, 151.4429263765338192, 8.025000000000000355 ) ) ;
#16111=( BOUNDED_CURVE ( )  B_SPLINE_CURVE ( 2, ( #39083, #5283, #10928, #54848, #69665, #21479, #38042, #11617, #42990, #6668, #650 ),
 .UNSPECIFIED., .F., .F. ) 
 B_SPLINE_CURVE_WITH_KNOTS ( ( 3, 2, 2, 2, 2, 3 ),
 ( 0.05882352941176476058, 0.06470588235294123802, 0.07058823529411770159, 0.07647058823529419291, 0.08235294117647065648, 0.08823529411764713393 ),
 .UNSPECIFIED. ) 
 CURVE ( )  GEOMETRIC_REPRESENTATION_ITEM ( )  RATIONAL_B_SPLINE_CURVE ( ( 0.9999999999999995559, 0.9510565162951539753, 1.000000000000000000, 0.9510565162951535312, 1.000000000000000000, 0.9510565162951535312, 1.000000000000000000, 0.9510565162951535312, 1.000000000000000000, 0.9510565162951529761, 1.000000000000000666 ) ) 
 REPRESENTATION_ITEM ( '' )  );
#16117=SURFACE_SIDE_STYLE ('',( #855 ) ) ;
#16118=SURFACE_STYLE_USAGE ( .BOTH. , #30868 ) ;
#16120=TOROIDAL_SURFACE ( 'NONE', #34054, 8.500000000000012434, 0.5000000000000000000 ) ;
#16123=AXIS2_PLACEMENT_3D ( 'NONE', #40404, #12599, #34068 ) ;
#16126=CARTESIAN_POINT ( 'NONE',  ( 2.128399401614408669E-13, 154.1464374838464266, 9.171437483846471395 ) ) ;
#16129=DIRECTION ( 'NONE',  ( -0.000000000000000000, -0.000000000000000000, 1.000000000000000000 ) ) ;
#16133=LINE ( 'NONE', #69559, #68590 ) ;
#16134=VECTOR ( 'NONE', #10688, 1000.000000000000000 ) ;
#16137=DIRECTION ( 'NONE',  ( -0.000000000000000000, -0.000000000000000000, -1.000000000000000000 ) ) ;
#16141=ORIENTED_EDGE ( 'NONE', *, *, #27780, .T. ) ;
#16147=VECTOR ( 'NONE', #43393, 1000.000000000000000 ) ;
#16150=CARTESIAN_POINT ( 'NONE',  ( -10.01517768586949231, 135.3049999999999784, -6.132527647946036459E-16 ) ) ;
#16154=FACE_OUTER_BOUND ( 'NONE', #56297, .T. ) ;
#16155=FILL_AREA_STYLE ('',( #37978 ) ) ;
#16160=( GEOMETRIC_REPRESENTATION_CONTEXT ( 3 ) GLOBAL_UNCERTAINTY_ASSIGNED_CONTEXT ( ( #63619 ) ) GLOBAL_UNIT_ASSIGNED_CONTEXT ( ( #57073, #56374, #35984 ) ) REPRESENTATION_CONTEXT ( 'NONE', 'WORKASPACE' ) );
#16161=FACE_OUTER_BOUND ( 'NONE', #23338, .T. ) ;
#16163=EDGE_CURVE ( 'NONE', #34861, #24214, #40395, .T. ) ;
#16164=FILL_AREA_STYLE ('',( #64992 ) ) ;
#16170=CARTESIAN_POINT ( 'NONE',  ( 60.00000000000000000, -2.024042244987997205E-14, -7.500000000000000000 ) ) ;
#16172=CARTESIAN_POINT ( 'NONE',  ( 4.716976649647096842, 130.7429263765338021, 6.492361379858953896 ) ) ;
#16175=EDGE_CURVE ( 'NONE', #61539, #8709, #59441, .T. ) ;
#16178=CARTESIAN_POINT ( 'NONE',  ( 8.437984349512095861, 140.1929263765337907, 1.550032578732816828E-15 ) ) ;
#16181=EDGE_LOOP ( 'NONE', ( #31648, #49518 ) ) ;
#16182=VERTEX_POINT ( 'NONE', #42995 ) ;
#16187=CARTESIAN_POINT ( 'NONE',  ( 9.058813317711337021, 147.5449999999999875, 2.943386871421375783 ) ) ;
#16188=CARTESIAN_POINT ( 'NONE',  ( 14.98999599679679662, 118.4999999999999716, 9.500000000000000000 ) ) ;
#16191=FACE_OUTER_BOUND ( 'NONE', #35, .T. ) ;
#16195=ORIENTED_EDGE ( 'NONE', *, *, #48261, .F. ) ;
#16196=CARTESIAN_POINT ( 'NONE',  ( 4.716976649647096842, 130.7429263765338021, 6.492361379858953896 ) ) ;
#16197=CARTESIAN_POINT ( 'NONE',  ( -9.827790563157511022E-16, 115.4429263765338192, 8.025000000000000355 ) ) ;
#16198=DIRECTION ( 'NONE',  ( -0.000000000000000000, -0.000000000000000000, 1.000000000000000000 ) ) ;
#16199=AXIS2_PLACEMENT_3D ( 'NONE', #8480, #52441, #35194 ) ;
#16200=STYLED_ITEM ( 'NONE', ( #61437 ), #29799 ) ;
#16201=CARTESIAN_POINT ( 'NONE',  ( 0.000000000000000000, 125.9429263765338192, -8.025000000000000355 ) ) ;
#16205=ORIENTED_EDGE ( 'NONE', *, *, #9491, .T. ) ;
#16209=CIRCLE ( 'NONE', #46553, 0.5000000000000004441 ) ;
#16214=VECTOR ( 'NONE', #11426, 1000.000000000000000 ) ;
#16217=CARTESIAN_POINT ( 'NONE',  ( 41.13967244528110712, 107.8968002066633574, 3.376844662569574940 ) ) ;
#16218=DIRECTION ( 'NONE',  ( 0.000000000000000000, 0.000000000000000000, 1.000000000000000000 ) ) ;
#16223=MECHANICAL_DESIGN_GEOMETRIC_PRESENTATION_REPRESENTATION('',(#65586),#3796);
#16228=CARTESIAN_POINT ( 'NONE',  ( 14.98999599679679662, 146.4999999999999716, 9.500000000000000000 ) ) ;
#16233=LINE ( 'NONE', #54165, #51498 ) ;
#16239=CARTESIAN_POINT ( 'NONE',  ( -10.01517768586949231, 111.3049999999999784, -6.132527647946036459E-16 ) ) ;
#16246=EDGE_CURVE ( 'NONE', #8395, #67546, #43680, .T. ) ;
#16255=FILL_AREA_STYLE_COLOUR ( '', #24635 ) ;
#16259=SURFACE_STYLE_USAGE ( .BOTH. , #65077 ) ;
#16262=SURFACE_STYLE_FILL_AREA ( #47953 ) ;
#16263=AXIS2_PLACEMENT_3D ( 'NONE', #49582, #61475, #28071 ) ;
#16264=ADVANCED_FACE ( 'NONE', ( #53167 ), #58428, .T. ) ;
#16266=CARTESIAN_POINT ( 'NONE',  ( -45.90836907650464127, 9.403269179647979925, 6.097839204891423392 ) ) ;
#16270=ORIENTED_EDGE ( 'NONE', *, *, #44751, .T. ) ;
#16273=ORIENTED_EDGE ( 'NONE', *, *, #63058, .F. ) ;
#16274=SURFACE_SIDE_STYLE ('',( #64425 ) ) ;
#16277=VECTOR ( 'NONE', #43791, 1000.000000000000000 ) ;
#16280=CARTESIAN_POINT ( 'NONE',  ( 9.058813317711338797, 117.8449999999999847, -2.943386871421372675 ) ) ;
#16282=ORIENTED_EDGE ( 'NONE', *, *, #58239, .F. ) ;
#16283=CARTESIAN_POINT ( 'NONE',  ( -71.50000000000000000, 35.92875272052971525, 7.000000000000000000 ) ) ;
#16284=CARTESIAN_POINT ( 'NONE',  ( -1.166476076187854022E-15, 130.0549999999999784, 9.525000000000000355 ) ) ;
#16288=ORIENTED_EDGE ( 'NONE', *, *, #19128, .F. ) ;
#16289=CARTESIAN_POINT ( 'NONE',  ( 8.102448949553181734, 151.5049999999999955, 5.886773742842750679 ) ) ;
#16291=AXIS2_PLACEMENT_3D ( 'NONE', #35739, #51923, #51561 ) ;
#16294=CARTESIAN_POINT ( 'NONE',  ( -49.12162162162162105, 13.70805908423323238, -9.500000000000000000 ) ) ;
#16295=PRESENTATION_STYLE_ASSIGNMENT (( #9949 ) ) ;
#16297=DIRECTION ( 'NONE',  ( 0.000000000000000000, 0.000000000000000000, 1.000000000000000000 ) ) ;
#16298=AXIS2_PLACEMENT_3D ( 'NONE', #61329, #28617, #66259 ) ;
#16299=PRESENTATION_STYLE_ASSIGNMENT (( #63052 ) ) ;
#16304=EDGE_CURVE ( 'NONE', #33822, #68848, #16910, .T. ) ;
#16305=MECHANICAL_DESIGN_GEOMETRIC_PRESENTATION_REPRESENTATION('',(#48888),#25239);
#16307=ORIENTED_EDGE ( 'NONE', *, *, #58494, .T. ) ;
#16312=FACE_OUTER_BOUND ( 'NONE', #16109, .T. ) ;
#16313=DIRECTION ( 'NONE',  ( -0.000000000000000000, -0.000000000000000000, -1.000000000000000000 ) ) ;
#16315=AXIS2_PLACEMENT_3D ( 'NONE', #55198, #7023, #49960 ) ;
#16316=( NAMED_UNIT ( * ) PLANE_ANGLE_UNIT ( ) SI_UNIT ( $, .RADIAN. ) );
#16317=ORIENTED_EDGE ( 'NONE', *, *, #49262, .F. ) ;
#16320=PRESENTATION_STYLE_ASSIGNMENT (( #64477 ) ) ;
#16321=DIRECTION ( 'NONE',  ( 1.000000000000000000, 0.000000000000000000, 0.000000000000000000 ) ) ;
#16325=CARTESIAN_POINT ( 'NONE',  ( -5.598654528085808657, 131.6449999999999818, 7.705886871421373741 ) ) ;
#16330=LINE ( 'NONE', #60555, #52617 ) ;
#16335=ADVANCED_FACE ( 'NONE', ( #47940 ), #21132, .F. ) ;
#16339=ADVANCED_FACE ( 'NONE', ( #7393 ), #17993, .F. ) ;
#16342=DIRECTION ( 'NONE',  ( -1.000000000000000000, 0.000000000000000000, 0.000000000000000000 ) ) ;
#16345=AXIS2_PLACEMENT_3D ( 'NONE', #14497, #20476, #62347 ) ;
#16346=DIRECTION ( 'NONE',  ( -0.000000000000000000, -0.000000000000000000, -1.000000000000000000 ) ) ;
#16348=MECHANICAL_DESIGN_GEOMETRIC_PRESENTATION_REPRESENTATION('',(#28687),#7380);
#16350=DIRECTION ( 'NONE',  ( 0.000000000000000000, 0.000000000000000000, -1.000000000000000000 ) ) ;
#16357=CARTESIAN_POINT ( 'NONE',  ( 4.716976649647099507, 138.7570736234661695, -6.492361379858953008 ) ) ;
#16359=AXIS2_PLACEMENT_3D ( 'NONE', #68192, #20332, #30174 ) ;
#16366=VECTOR ( 'NONE', #49448, 1000.000000000000000 ) ;
#16377=EDGE_CURVE ( 'NONE', #27439, #16813, #22529, .T. ) ;
#16380=VERTEX_POINT ( 'NONE', #33424 ) ;
#16381=PRESENTATION_STYLE_ASSIGNMENT (( #43129 ) ) ;
#16383=CARTESIAN_POINT ( 'NONE',  ( 45.50000000000000000, 9.639620389971918613, -6.500000000000000888 ) ) ;
#16384=STYLED_ITEM ( 'NONE', ( #30577 ), #39347 ) ;
#16390=VERTEX_POINT ( 'NONE', #54855 ) ;
#16394=CARTESIAN_POINT ( 'NONE',  ( -8.102448949553179958, 130.8949999999999818, -5.886773742842749790 ) ) ;
#16398=MECHANICAL_DESIGN_GEOMETRIC_PRESENTATION_REPRESENTATION('',(#5140),#45626);
#16399=DIRECTION ( 'NONE',  ( 0.000000000000000000, 0.000000000000000000, 1.000000000000000000 ) ) ;
#16400=ORIENTED_EDGE ( 'NONE', *, *, #69634, .F. ) ;
#16401=FILL_AREA_STYLE_COLOUR ( '', #34033 ) ;
#16405=CARTESIAN_POINT ( 'NONE',  ( -4.716976649647098618, 131.2570736234661695, 6.492361379858953008 ) ) ;
#16409=EDGE_CURVE ( 'NONE', #44595, #10638, #4446, .T. ) ;
#16410=CARTESIAN_POINT ( 'NONE',  ( 75.00000000000000000, 20.36037961002804053, 6.000000000000000888 ) ) ;
#16416=CIRCLE ( 'NONE', #49007, 0.5000000000000004441 ) ;
#16422=ADVANCED_FACE ( 'NONE', ( #57657 ), #40122, .F. ) ;
#16423=STYLED_ITEM ( 'NONE', ( #35604 ), #64234 ) ;
#16426=CARTESIAN_POINT ( 'NONE',  ( 6.422934014168398598, 153.0000000000000000, 4.811085495980990778 ) ) ;
#16427=CIRCLE ( 'NONE', #54593, 0.5000000000000004441 ) ;
#16429=( GEOMETRIC_REPRESENTATION_CONTEXT ( 3 ) GLOBAL_UNCERTAINTY_ASSIGNED_CONTEXT ( ( #19169 ) ) GLOBAL_UNIT_ASSIGNED_CONTEXT ( ( #18171, #50541, #56493 ) ) REPRESENTATION_CONTEXT ( 'NONE', 'WORKASPACE' ) );
#16430=DIRECTION ( 'NONE',  ( 0.000000000000000000, 0.000000000000000000, 1.000000000000000000 ) ) ;
#16431=PRODUCT_DEFINITION_CONTEXT ( 'detailed design', #5990, 'design' ) ;
#16434=DIRECTION ( 'NONE',  ( 1.000000000000000000, 0.000000000000000000, 0.000000000000000000 ) ) ;
#16436=CARTESIAN_POINT ( 'NONE',  ( -14.98999599679678951, 146.4999999999999716, -9.500000000000000000 ) ) ;
#16437=TOROIDAL_SURFACE ( 'NONE', #47947, 7.499999999999998224, 0.5000000000000000000 ) ;
#16439=ORIENTED_EDGE ( 'NONE', *, *, #27135, .T. ) ;
#16440=DIRECTION ( 'NONE',  ( -0.000000000000000000, -0.000000000000000000, 1.000000000000000000 ) ) ;
#16442=ORIENTED_EDGE ( 'NONE', *, *, #27454, .F. ) ;
#16445=COLOUR_RGB ( '', 0.72549020, 0.75294118, 0.79215686) ;
#16446=CARTESIAN_POINT ( 'NONE',  ( -6.826472737025120807, 118.5070736234661695, -4.959722759717907437 ) ) ;
#16447=SPHERICAL_SURFACE ( 'NONE', #7973, 0.5000000000000000000 ) ;
#16448=CARTESIAN_POINT ( 'NONE',  ( 75.00000000000000000, 20.14920990499773268, -6.614546734589650256 ) ) ;
#16449=( NAMED_UNIT ( * ) PLANE_ANGLE_UNIT ( ) SI_UNIT ( $, .RADIAN. ) );
#16450=VERTEX_POINT ( 'NONE', #24576 ) ;
#16451=VERTEX_POINT ( 'NONE', #50994 ) ;
#16455=CARTESIAN_POINT ( 'NONE',  ( 5.598654528085805993, 124.3549999999999898, 7.705886871421374629 ) ) ;
#16459=ORIENTED_EDGE ( 'NONE', *, *, #58106, .F. ) ;
#16460=VECTOR ( 'NONE', #14672, 1000.000000000000000 ) ;
#16461=CARTESIAN_POINT ( 'NONE',  ( 8.425467196792491009, 153.5331836710477660, -1.554025292114362022 ) ) ;
#16463=VERTEX_POINT ( 'NONE', #66837 ) ;
#16466=CARTESIAN_POINT ( 'NONE',  ( 0.000000000000000000, 87.30187232391182306, 0.000000000000000000 ) ) ;
#16467=ORIENTED_EDGE ( 'NONE', *, *, #9870, .F. ) ;
#16480=LINE ( 'NONE', #54059, #12404 ) ;
#16483=ORIENTED_EDGE ( 'NONE', *, *, #41702, .T. ) ;
#16488=ORIENTED_EDGE ( 'NONE', *, *, #51175, .T. ) ;
#16496=VERTEX_POINT ( 'NONE', #18952 ) ;
#16504=CARTESIAN_POINT ( 'NONE',  ( -3.094860106618432471, 137.7049999999999841, -9.525000000000000355 ) ) ;
#16506=CARTESIAN_POINT ( 'NONE',  ( 72.50000000000000000, 35.92875272052971525, 9.500000000000000000 ) ) ;
#16507=UNCERTAINTY_MEASURE_WITH_UNIT (LENGTH_MEASURE( 1.000000000000000082E-05 ), #48435, 'distance_accuracy_value', 'NONE');
#16508=PRESENTATION_STYLE_ASSIGNMENT (( #43261 ) ) ;
#16512=( LENGTH_UNIT ( ) NAMED_UNIT ( * ) SI_UNIT ( .MILLI., .METRE. ) );
#16513=DIRECTION ( 'NONE',  ( 0.000000000000000000, 0.000000000000000000, -1.000000000000000000 ) ) ;
#16514=( NAMED_UNIT ( * ) SI_UNIT ( $, .STERADIAN. ) SOLID_ANGLE_UNIT ( ) );
#16518=EDGE_LOOP ( 'NONE', ( #3126, #26674, #62930, #30471 ) ) ;
#16519=CARTESIAN_POINT ( 'NONE',  ( -7.632228543268608334, 135.8429263765337964, 2.479861379858952830 ) ) ;
#16520=( NAMED_UNIT ( * ) PLANE_ANGLE_UNIT ( ) SI_UNIT ( $, .RADIAN. ) );
#16521=SURFACE_STYLE_FILL_AREA ( #32649 ) ;
#16522=CARTESIAN_POINT ( 'NONE',  ( -34.99999999999999289, 99.99999999999998579, 9.500000000000000000 ) ) ;
#16524=VERTEX_POINT ( 'NONE', #56611 ) ;
#16529=PRESENTATION_STYLE_ASSIGNMENT (( #31261 ) ) ;
#16531=DIRECTION ( 'NONE',  ( 1.000000000000000000, 0.000000000000000000, 0.000000000000000000 ) ) ;
#16535=CARTESIAN_POINT ( 'NONE',  ( 9.058813317711337021, 156.5449999999999875, 2.943386871421375783 ) ) ;
#16536=SURFACE_SIDE_STYLE ('',( #21784 ) ) ;
#16540=DIRECTION ( 'NONE',  ( -0.000000000000000000, 1.000000000000000000, -0.000000000000000000 ) ) ;
#16543=CARTESIAN_POINT ( 'NONE',  ( 8.437984349512095861, 122.1929263765337907, 1.550032578732817026E-15 ) ) ;
#16544=DIRECTION ( 'NONE',  ( -1.000000000000000000, 0.000000000000000000, 0.000000000000000000 ) ) ;
#16546=DIRECTION ( 'NONE',  ( 0.000000000000000000, 0.000000000000000000, 1.000000000000000000 ) ) ;
#16548=EDGE_LOOP ( 'NONE', ( #50583, #3653, #4727, #58723 ) ) ;
#16553=LINE ( 'NONE', #54135, #21672 ) ;
#16557=DIRECTION ( 'NONE',  ( -0.000000000000000000, -0.000000000000000000, -1.000000000000000000 ) ) ;
#16560=SURFACE_STYLE_USAGE ( .BOTH. , #48580 ) ;
#16561=VERTEX_POINT ( 'NONE', #25290 ) ;
#16562=EDGE_CURVE ( 'NONE', #14271, #12616, #33740, .T. ) ;
#16566=CARTESIAN_POINT ( 'NONE',  ( 74.99999999999998579, 50.00000000000000000, -9.500000000000000000 ) ) ;
#16568=ORIENTED_EDGE ( 'NONE', *, *, #18955, .T. ) ;
#16570=EDGE_CURVE ( 'NONE', #22515, #5568, #10163, .T. ) ;
#16577=ORIENTED_EDGE ( 'NONE', *, *, #11434, .T. ) ;
#16578=ADVANCED_FACE ( 'NONE', ( #16154 ), #19119, .T. ) ;
#16580=PRESENTATION_STYLE_ASSIGNMENT (( #58092 ) ) ;
#16585=CARTESIAN_POINT ( 'NONE',  ( 10.01517768586949231, 112.8049999999999784, 1.839758294383810543E-15 ) ) ;
#16587=DIRECTION ( 'NONE',  ( 0.000000000000000000, 0.000000000000000000, 1.000000000000000000 ) ) ;
#16588=CARTESIAN_POINT ( 'NONE',  ( -23.71231517720798010, 113.4999999999999858, 9.500000000000000000 ) ) ;
#16590=UNCERTAINTY_MEASURE_WITH_UNIT (LENGTH_MEASURE( 1.000000000000000082E-05 ), #4741, 'distance_accuracy_value', 'NONE');
#16595=PLANE ( 'NONE',  #63088 ) ;
#16596=ORIENTED_EDGE ( 'NONE', *, *, #66733, .F. ) ;
#16599=CARTESIAN_POINT ( 'NONE',  ( -20.71231517720798010, 149.9999999999999716, 10.00000000000000000 ) ) ;
#16606=ORIENTED_EDGE ( 'NONE', *, *, #1303, .T. ) ;
#16608=EDGE_LOOP ( 'NONE', ( #65834, #43788, #51742, #31210 ) ) ;
#16609=STYLED_ITEM ( 'NONE', ( #269 ), #3945 ) ;
#16614=CARTESIAN_POINT ( 'NONE',  ( -1.166476076187854022E-15, 131.9449999999999932, 9.525000000000000355 ) ) ;
#16617=CARTESIAN_POINT ( 'NONE',  ( -67.99999999999998579, -2.024042244987997205E-14, 12.00000000000000000 ) ) ;
#16618=CARTESIAN_POINT ( 'NONE',  ( -5.598654528085806881, 128.8549999999999898, -7.705886871421374629 ) ) ;
#16623=CARTESIAN_POINT ( 'NONE',  ( -9.058813317711337021, 147.1549999999999727, -2.943386871421374895 ) ) ;
#16624=FILL_AREA_STYLE ('',( #27119 ) ) ;
#16625=UNCERTAINTY_MEASURE_WITH_UNIT (LENGTH_MEASURE( 1.000000000000000082E-05 ), #3002, 'distance_accuracy_value', 'NONE');
#16627=VECTOR ( 'NONE', #24614, 1000.000000000000000 ) ;
#16630=EDGE_CURVE ( 'NONE', #36960, #9072, #47137, .T. ) ;
#16633=PRESENTATION_STYLE_ASSIGNMENT (( #49665 ) ) ;
#16636=CARTESIAN_POINT ( 'NONE',  ( 3.105708046185522875, 111.8963703285356104, -7.531667776144067794 ) ) ;
#16637=UNCERTAINTY_MEASURE_WITH_UNIT (LENGTH_MEASURE( 1.000000000000000082E-05 ), #42793, 'distance_accuracy_value', 'NONE');
#16638=EDGE_CURVE ( 'NONE', #57494, #25423, #46146, .T. ) ;
#16639=FILL_AREA_STYLE_COLOUR ( '', #59321 ) ;
#16640=DIRECTION ( 'NONE',  ( 0.000000000000000000, 0.000000000000000000, 1.000000000000000000 ) ) ;
#16641=LINE ( 'NONE', #10988, #17535 ) ;
#16643=( NAMED_UNIT ( * ) SI_UNIT ( $, .STERADIAN. ) SOLID_ANGLE_UNIT ( ) );
#16648=ADVANCED_FACE ( 'NONE', ( #42551 ), #3365, .F. ) ;
#16650=DIRECTION ( 'NONE',  ( -0.000000000000000000, -0.000000000000000000, 1.000000000000000000 ) ) ;
#16654=VECTOR ( 'NONE', #63351, 1000.000000000000000 ) ;
#16660=( NAMED_UNIT ( * ) PLANE_ANGLE_UNIT ( ) SI_UNIT ( $, .RADIAN. ) );
#16661=DIRECTION ( 'NONE',  ( 0.000000000000000000, 1.000000000000000000, 0.000000000000000000 ) ) ;
#16664=CARTESIAN_POINT ( 'NONE',  ( -3.094860106618432471, 133.5949999999999989, -9.525000000000000355 ) ) ;
#16672=VECTOR ( 'NONE', #27569, 1000.000000000000000 ) ;
#16673=CARTESIAN_POINT ( 'NONE',  ( -9.827790563157511022E-16, 149.5570736234661524, 8.025000000000000355 ) ) ;
#16683=SURFACE_STYLE_USAGE ( .BOTH. , #23311 ) ;
#16686=ORIENTED_EDGE ( 'NONE', *, *, #33349, .F. ) ;
#16690=CARTESIAN_POINT ( 'NONE',  ( -12.34222745343792127, 149.9999999999999716, -10.18181818181818166 ) ) ;
#16692=FILL_AREA_STYLE ('',( #59203 ) ) ;
#16694=CARTESIAN_POINT ( 'NONE',  ( -7.632228543268607446, 142.6570736234661751, -2.479861379858953718 ) ) ;
#16698=UNCERTAINTY_MEASURE_WITH_UNIT (LENGTH_MEASURE( 1.000000000000000082E-05 ), #940, 'distance_accuracy_value', 'NONE');
#16702=COLOUR_RGB ( '', 0.72549020, 0.75294118, 0.79215686) ;
#16704=EDGE_CURVE ( 'NONE', #33108, #25004, #37163, .T. ) ;
#16712=EDGE_LOOP ( 'NONE', ( #58834, #9700, #18080, #67954 ) ) ;
#16713=CARTESIAN_POINT ( 'NONE',  ( 20.12916642283592950, 110.4999999999999858, -10.05319148936170137 ) ) ;
#16716=CARTESIAN_POINT ( 'NONE',  ( -45.00000000000000711, 8.092690183932669257, -5.807220890438251182 ) ) ;
#16718=SURFACE_STYLE_FILL_AREA ( #59585 ) ;
#16723=CARTESIAN_POINT ( 'NONE',  ( -75.00000000000000000, 8.062885781073912739, 6.000000000000000888 ) ) ;
#16727=EDGE_CURVE ( 'NONE', #16804, #20191, #23707, .T. ) ;
#16728=CARTESIAN_POINT ( 'NONE',  ( -72.50000000000001421, 1.797044900979284448E-15, -9.500000000000000000 ) ) ;
#16729=FACE_OUTER_BOUND ( 'NONE', #22908, .T. ) ;
#16731=CARTESIAN_POINT ( 'NONE',  ( -3.094860106618434248, 134.7949999999999875, 9.525000000000000355 ) ) ;
#16737=AXIS2_PLACEMENT_3D ( 'NONE', #5345, #42017, #10991 ) ;
#16739=FILL_AREA_STYLE_COLOUR ( '', #28500 ) ;
#16746=VERTEX_POINT ( 'NONE', #8690 ) ;
#16747=CARTESIAN_POINT ( 'NONE',  ( 44.82807636874883173, 9.942692122916261255, -2.999113325960748533 ) ) ;
#16748=FACE_OUTER_BOUND ( 'NONE', #15434, .T. ) ;
#16750=PLANE ( 'NONE',  #41683 ) ;
#16752=CIRCLE ( 'NONE', #48245, 1.000000000000000888 ) ;
#16756=CYLINDRICAL_SURFACE ( 'NONE', #8799, 0.5000000000000004441 ) ;
#16760=CARTESIAN_POINT ( 'NONE',  ( 0.000000000000000000, 87.30187232391182306, 8.025000000000000355 ) ) ;
#16765=ORIENTED_EDGE ( 'NONE', *, *, #9897, .F. ) ;
#16766=CARTESIAN_POINT ( 'NONE',  ( -6.826472737025120807, 138.9929263765338305, 4.959722759717906548 ) ) ;
#16768=VERTEX_POINT ( 'NONE', #24487 ) ;
#16769=LINE ( 'NONE', #44220, #52170 ) ;
#16770=CARTESIAN_POINT ( 'NONE',  ( -2.607480562269073765, 115.2070736234661723, -8.025000000000000355 ) ) ;
#16772=COLOUR_RGB ( '', 0.08235294, 0.09019608, 0.10196078) ;
#16774=FILL_AREA_STYLE_COLOUR ( '', #20714 ) ;
#16776=AXIS2_PLACEMENT_3D ( 'NONE', #69476, #53977, #27911 ) ;
#16780=EDGE_CURVE ( 'NONE', #47468, #9347, #67488, .T. ) ;
#16782=VERTEX_POINT ( 'NONE', #51594 ) ;
#16783=EDGE_CURVE ( 'NONE', #44684, #30484, #65274, .T. ) ;
#16784=FILL_AREA_STYLE_COLOUR ( '', #23231 ) ;
#16787=DIRECTION ( 'NONE',  ( 0.000000000000000000, 0.000000000000000000, 1.000000000000000000 ) ) ;
#16789=AXIS2_PLACEMENT_3D ( 'NONE', #34029, #28738, #18562 ) ;
#16790=ORIENTED_EDGE ( 'NONE', *, *, #40458, .F. ) ;
#16792=CARTESIAN_POINT ( 'NONE',  ( 8.301136498571505484, 153.5927615316110746, -2.349027669732494772 ) ) ;
#16796=ORIENTED_EDGE ( 'NONE', *, *, #15594, .T. ) ;
#16800=EDGE_CURVE ( 'NONE', #62320, #2411, #5712, .T. ) ;
#16801=CYLINDRICAL_SURFACE ( 'NONE', #45353, 0.5000000000000004441 ) ;
#16802=ORIENTED_EDGE ( 'NONE', *, *, #38950, .T. ) ;
#16804=VERTEX_POINT ( 'NONE', #13249 ) ;
#16806=DIRECTION ( 'NONE',  ( 0.000000000000000000, 0.000000000000000000, 1.000000000000000000 ) ) ;
#16812=CARTESIAN_POINT ( 'NONE',  ( -6.257356667978481113, 153.2770626485485650, -5.482883996731844789 ) ) ;
#16813=VERTEX_POINT ( 'NONE', #57209 ) ;
#16815=FILL_AREA_STYLE_COLOUR ( '', #59806 ) ;
#16817=FILL_AREA_STYLE_COLOUR ( '', #33495 ) ;
#16821=DIRECTION ( 'NONE',  ( -0.000000000000000000, 1.000000000000000000, -0.000000000000000000 ) ) ;
#16827=CARTESIAN_POINT ( 'NONE',  ( 45.00000000000000000, 10.69371294334680300, 3.912397846414697788 ) ) ;
#16829=FACE_OUTER_BOUND ( 'NONE', #52591, .T. ) ;
#16830=( NAMED_UNIT ( * ) PLANE_ANGLE_UNIT ( ) SI_UNIT ( $, .RADIAN. ) );
#16833=DIRECTION ( 'NONE',  ( -0.000000000000000000, -0.000000000000000000, -1.000000000000000000 ) ) ;
#16836=CARTESIAN_POINT ( 'NONE',  ( 8.102448949553181734, 139.5049999999999955, 5.886773742842750679 ) ) ;
#16848=( NAMED_UNIT ( * ) PLANE_ANGLE_UNIT ( ) SI_UNIT ( $, .RADIAN. ) );
#16850=CARTESIAN_POINT ( 'NONE',  ( -72.49999999999998579, 64.07124727947029896, -10.00000000000000000 ) ) ;
#16851=EDGE_LOOP ( 'NONE', ( #63894, #58110, #66405, #62977 ) ) ;
#16855=ADVANCED_FACE ( 'NONE', ( #61429 ), #9751, .F. ) ;
#16859=CARTESIAN_POINT ( 'NONE',  ( 44.99999999999998579, 119.9999999999999716, -7.000000000000000000 ) ) ;
#16860=ORIENTED_EDGE ( 'NONE', *, *, #49886, .F. ) ;
#16862=EDGE_LOOP ( 'NONE', ( #42937, #63709, #64249, #38723 ) ) ;
#16863=SURFACE_STYLE_USAGE ( .BOTH. , #29085 ) ;
#16865=ORIENTED_EDGE ( 'NONE', *, *, #23420, .T. ) ;
#16869=STYLED_ITEM ( 'NONE', ( #53304 ), #1334 ) ;
#16870=MECHANICAL_DESIGN_GEOMETRIC_PRESENTATION_REPRESENTATION('',(#41581),#48369);
#16872=CARTESIAN_POINT ( 'NONE',  ( -5.598654528085808657, 155.6449999999999818, 7.705886871421373741 ) ) ;
#16873=DIRECTION ( 'NONE',  ( -0.000000000000000000, -0.000000000000000000, -1.000000000000000000 ) ) ;
#16874=ORIENTED_EDGE ( 'NONE', *, *, #49595, .F. ) ;
#16880=ORIENTED_EDGE ( 'NONE', *, *, #60648, .T. ) ;
#16881=CARTESIAN_POINT ( 'NONE',  ( -4.716976649647098618, 133.1429263765338362, 6.492361379858953008 ) ) ;
#16882=CARTESIAN_POINT ( 'NONE',  ( -74.99999999999998579, 50.00000000000000000, 10.50000000000000000 ) ) ;
#16886=CARTESIAN_POINT ( 'NONE',  ( -23.71231517720798010, 113.4999999999999858, -9.500000000000000000 ) ) ;
#16894=FILL_AREA_STYLE_COLOUR ( '', #30625 ) ;
#16897=MECHANICAL_DESIGN_GEOMETRIC_PRESENTATION_REPRESENTATION('',(#29196),#30290);
#16898=SURFACE_STYLE_USAGE ( .BOTH. , #69637 ) ;
#16900=AXIS2_PLACEMENT_3D ( 'NONE', #59634, #61021, #43857 ) ;
#16902=LINE ( 'NONE', #60458, #55284 ) ;
#16907=COLOUR_RGB ( '', 0.72549020, 0.75294118, 0.79215686) ;
#16909=CARTESIAN_POINT ( 'NONE',  ( -75.50000000000000000, 35.50862325381056905, -9.500000000000000000 ) ) ;
#16910=CIRCLE ( 'NONE', #38262, 0.5000000000000004441 ) ;
#16915=DIRECTION ( 'NONE',  ( 1.000000000000000000, 0.000000000000000000, 0.000000000000000000 ) ) ;
#16918=CARTESIAN_POINT ( 'NONE',  ( -8.102448949553181734, 155.4950000000000045, 5.886773742842747126 ) ) ;
#16926=ORIENTED_EDGE ( 'NONE', *, *, #53690, .F. ) ;
#16933=MECHANICAL_DESIGN_GEOMETRIC_PRESENTATION_REPRESENTATION('',(#25885),#5784);
#16935=EDGE_LOOP ( 'NONE', ( #7974, #17306, #54878, #44650, #34654 ) ) ;
#16937=CYLINDRICAL_SURFACE ( 'NONE', #62301, 8.025000000000000355 ) ;
#16942=VERTEX_POINT ( 'NONE', #66299 ) ;
#16944=ORIENTED_EDGE ( 'NONE', *, *, #2647, .T. ) ;
#16945=EDGE_CURVE ( 'NONE', #46101, #30840, #39462, .T. ) ;
#16951=ADVANCED_FACE ( 'NONE', ( #49127 ), #58509, .F. ) ;
#16953=CARTESIAN_POINT ( 'NONE',  ( -3.094860106618434248, 131.7950000000000159, 9.525000000000000355 ) ) ;
#16957=DIRECTION ( 'NONE',  ( 0.000000000000000000, 0.000000000000000000, -1.000000000000000000 ) ) ;
#16958=CARTESIAN_POINT ( 'NONE',  ( -5.598654528085808657, 132.7549999999999955, 7.705886871421373741 ) ) ;
#16962=CARTESIAN_POINT ( 'NONE',  ( -41.36494435661896318, 107.7173713599242717, -3.929015280517311748 ) ) ;
#16964=CARTESIAN_POINT ( 'NONE',  ( -1.166476076187854022E-15, 157.0550000000000068, 9.525000000000000355 ) ) ;
#16965=DIRECTION ( 'NONE',  ( 0.000000000000000000, 0.000000000000000000, 1.000000000000000000 ) ) ;
#16966=PRESENTATION_STYLE_ASSIGNMENT (( #59853 ) ) ;
#16967=EDGE_CURVE ( 'NONE', #67575, #41256, #17460, .T. ) ;
#16970=CARTESIAN_POINT ( 'NONE',  ( -71.49999999999998579, 119.9999999999997868, 7.000000000000000000 ) ) ;
#16971=AXIS2_PLACEMENT_3D ( 'NONE', #38139, #48351, #33180 ) ;
#16975=SURFACE_STYLE_USAGE ( .BOTH. , #6734 ) ;
#16976=VECTOR ( 'NONE', #53859, 1000.000000000000000 ) ;
#16977=CARTESIAN_POINT ( 'NONE',  ( 44.50000000000000000, 99.99999999999992895, 4.000000000000000000 ) ) ;
#16979=ORIENTED_EDGE ( 'NONE', *, *, #23147, .T. ) ;
#16980=CARTESIAN_POINT ( 'NONE',  ( -9.827790563157511022E-16, 152.5570736234661524, 8.025000000000000355 ) ) ;
#16984=EDGE_LOOP ( 'NONE', ( #34396, #63384, #61896, #50595, #30668 ) ) ;
#16985=UNCERTAINTY_MEASURE_WITH_UNIT (LENGTH_MEASURE( 1.000000000000000082E-05 ), #41478, 'distance_accuracy_value', 'NONE');
#16988=FILL_AREA_STYLE ('',( #22243 ) ) ;
#16989=( LENGTH_UNIT ( ) NAMED_UNIT ( * ) SI_UNIT ( .MILLI., .METRE. ) );
#16992=SURFACE_STYLE_FILL_AREA ( #53239 ) ;
#16993=ORIENTED_EDGE ( 'NONE', *, *, #51484, .T. ) ;
#16997=CARTESIAN_POINT ( 'NONE',  ( 5.598654528085805993, 132.2450000000000045, 7.705886871421374629 ) ) ;
#16999=( GEOMETRIC_REPRESENTATION_CONTEXT ( 3 ) GLOBAL_UNCERTAINTY_ASSIGNED_CONTEXT ( ( #21495 ) ) GLOBAL_UNIT_ASSIGNED_CONTEXT ( ( #20676, #36187, #52001 ) ) REPRESENTATION_CONTEXT ( 'NONE', 'WORKASPACE' ) );
#17000=( NAMED_UNIT ( * ) SI_UNIT ( $, .STERADIAN. ) SOLID_ANGLE_UNIT ( ) );
#17004=DIRECTION ( 'NONE',  ( 1.000000000000000000, 4.336808689941999001E-16, 0.000000000000000000 ) ) ;
#17009=B_SPLINE_CURVE_WITH_KNOTS ( 'NONE', 3,
 ( #30223, #51716, #24273, #29905 ),
 .UNSPECIFIED., .F., .F.,
 ( 4, 4 ),
 ( -4.944132332486997984E-06, 0.0004171697701591836637 ),
 .UNSPECIFIED. ) ;
#17010=CARTESIAN_POINT ( 'NONE',  ( -60.00000000000000000, -2.024042244987997205E-14, 6.500000000000000000 ) ) ;
#17011=EDGE_CURVE ( 'NONE', #69035, #54309, #17117, .T. ) ;
#17016=ORIENTED_EDGE ( 'NONE', *, *, #25959, .F. ) ;
#17019=CARTESIAN_POINT ( 'NONE',  ( 71.50000000000000000, 35.92875272052971525, 7.500000000000000000 ) ) ;
#17021=SURFACE_SIDE_STYLE ('',( #21943 ) ) ;
#17022=EDGE_CURVE ( 'NONE', #37089, #48904, #63016, .T. ) ;
#17023=( GEOMETRIC_REPRESENTATION_CONTEXT ( 3 ) GLOBAL_UNCERTAINTY_ASSIGNED_CONTEXT ( ( #15702 ) ) GLOBAL_UNIT_ASSIGNED_CONTEXT ( ( #60862, #4089, #40489 ) ) REPRESENTATION_CONTEXT ( 'NONE', 'WORKASPACE' ) );
#17024=( GEOMETRIC_REPRESENTATION_CONTEXT ( 3 ) GLOBAL_UNCERTAINTY_ASSIGNED_CONTEXT ( ( #51750 ) ) GLOBAL_UNIT_ASSIGNED_CONTEXT ( ( #28277, #21649, #23050 ) ) REPRESENTATION_CONTEXT ( 'NONE', 'WORKASPACE' ) );
#17025=DIRECTION ( 'NONE',  ( 0.000000000000000000, 0.000000000000000000, 1.000000000000000000 ) ) ;
#17027=DIRECTION ( 'NONE',  ( 1.000000000000000000, -1.387778780781444256E-14, 0.000000000000000000 ) ) ;
#17031=ORIENTED_EDGE ( 'NONE', *, *, #39057, .T. ) ;
#17033=ADVANCED_FACE ( 'NONE', ( #6177 ), #1176, .F. ) ;
#17036=STYLED_ITEM ( 'NONE', ( #54453 ), #22097 ) ;
#17037=EDGE_CURVE ( 'NONE', #28244, #66508, #12443, .T. ) ;
#17041=DIRECTION ( 'NONE',  ( 0.000000000000000000, 0.000000000000000000, 1.000000000000000000 ) ) ;
#17042=CARTESIAN_POINT ( 'NONE',  ( -2.607480562269075097, 152.4070736234661751, 8.025000000000000355 ) ) ;
#17043=( GEOMETRIC_REPRESENTATION_CONTEXT ( 3 ) GLOBAL_UNCERTAINTY_ASSIGNED_CONTEXT ( ( #56700 ) ) GLOBAL_UNIT_ASSIGNED_CONTEXT ( ( #65621, #60332, #65267 ) ) REPRESENTATION_CONTEXT ( 'NONE', 'WORKASPACE' ) );
#17045=FILL_AREA_STYLE ('',( #55331 ) ) ;
#17046=EDGE_CURVE ( 'NONE', #26176, #60543, #13882, .T. ) ;
#17051=DIRECTION ( 'NONE',  ( -0.000000000000000000, 1.000000000000000000, -0.000000000000000000 ) ) ;
#17052=DIRECTION ( 'NONE',  ( 1.000000000000000000, 0.000000000000000000, 0.000000000000000000 ) ) ;
#17059=MECHANICAL_DESIGN_GEOMETRIC_PRESENTATION_REPRESENTATION('',(#38422),#37265);
#17060=( NAMED_UNIT ( * ) SI_UNIT ( $, .STERADIAN. ) SOLID_ANGLE_UNIT ( ) );
#17062=CARTESIAN_POINT ( 'NONE',  ( -45.76717108624533381, 8.859195963244948402, -6.389740745940694744 ) ) ;
#17063=VERTEX_POINT ( 'NONE', #3272 ) ;
#17065=EDGE_LOOP ( 'NONE', ( #55593, #8742, #51272 ) ) ;
#17068=LINE ( 'NONE', #53963, #67376 ) ;
#17070=ORIENTED_EDGE ( 'NONE', *, *, #33222, .F. ) ;
#17073=CYLINDRICAL_SURFACE ( 'NONE', #57175, 0.5000000000000004441 ) ;
#17074=SURFACE_SIDE_STYLE ('',( #59946 ) ) ;
#17077=AXIS2_PLACEMENT_3D ( 'NONE', #15472, #20727, #25299 ) ;
#17078=CARTESIAN_POINT ( 'NONE',  ( 5.598654528085805993, 132.2450000000000045, 7.705886871421374629 ) ) ;
#17080=EDGE_CURVE ( 'NONE', #7834, #65093, #40557, .T. ) ;
#17082=DIRECTION ( 'NONE',  ( -1.000000000000000000, 0.000000000000000000, 0.000000000000000000 ) ) ;
#17085=CIRCLE ( 'NONE', #56351, 0.5000000000000004441 ) ;
#17088=( GEOMETRIC_REPRESENTATION_CONTEXT ( 3 ) GLOBAL_UNCERTAINTY_ASSIGNED_CONTEXT ( ( #13057 ) ) GLOBAL_UNIT_ASSIGNED_CONTEXT ( ( #23975, #3514, #51074 ) ) REPRESENTATION_CONTEXT ( 'NONE', 'WORKASPACE' ) );
#17089=CARTESIAN_POINT ( 'NONE',  ( -15.98999599679679839, 147.4999999999999716, 10.00000000000000000 ) ) ;
#17095=COLOUR_RGB ( '', 0.72549020, 0.75294118, 0.79215686) ;
#17096=EDGE_LOOP ( 'NONE', ( #9023, #54994, #67940, #43626 ) ) ;
#17101=UNCERTAINTY_MEASURE_WITH_UNIT (LENGTH_MEASURE( 1.000000000000000082E-05 ), #62400, 'distance_accuracy_value', 'NONE');
#17108=DIRECTION ( 'NONE',  ( 0.000000000000000000, 0.000000000000000000, 1.000000000000000000 ) ) ;
#17111=CARTESIAN_POINT ( 'NONE',  ( 34.99999999999999289, 99.99999999999997158, -9.500000000000000000 ) ) ;
#17117=LINE ( 'NONE', #54010, #52901 ) ;
#17123=EDGE_CURVE ( 'NONE', #24951, #12385, #30457, .T. ) ;
#17124=CARTESIAN_POINT ( 'NONE',  ( -74.99999999999998579, 50.00000000000000000, 11.50000000000003730 ) ) ;
#17127=STYLED_ITEM ( 'NONE', ( #56885 ), #60819 ) ;
#17128=CARTESIAN_POINT ( 'NONE',  ( 7.632228543268607446, 123.1570736234661609, 2.479861379858954606 ) ) ;
#17130=DIRECTION ( 'NONE',  ( 0.000000000000000000, 1.000000000000000000, 0.000000000000000000 ) ) ;
#17136=VERTEX_POINT ( 'NONE', #40640 ) ;
#17138=STYLED_ITEM ( 'NONE', ( #47806 ), #35600 ) ;
#17139=CARTESIAN_POINT ( 'NONE',  ( 4.716976649647099507, 134.6429263765338362, -6.492361379858953008 ) ) ;
#17143=CARTESIAN_POINT ( 'NONE',  ( -2.607480562269095969, 124.2929263765338135, 8.024999999999986144 ) ) ;
#17148=( GEOMETRIC_REPRESENTATION_CONTEXT ( 3 ) GLOBAL_UNCERTAINTY_ASSIGNED_CONTEXT ( ( #45535 ) ) GLOBAL_UNIT_ASSIGNED_CONTEXT ( ( #64110, #44100, #54917 ) ) REPRESENTATION_CONTEXT ( 'NONE', 'WORKASPACE' ) );
#17150=ORIENTED_EDGE ( 'NONE', *, *, #20745, .F. ) ;
#17156=DIRECTION ( 'NONE',  ( -1.000000000000000000, 0.000000000000000000, -0.000000000000000000 ) ) ;
#17159=DIRECTION ( 'NONE',  ( 1.000000000000000000, 0.000000000000000000, 0.000000000000000000 ) ) ;
#17160=ADVANCED_FACE ( 'NONE', ( #13174, #45236 ), #18804, .T. ) ;
#17164=ORIENTED_EDGE ( 'NONE', *, *, #24946, .T. ) ;
#17172=CARTESIAN_POINT ( 'NONE',  ( -74.99999999999998579, 50.00000000000000000, 11.50000000000000000 ) ) ;
#17174=( GEOMETRIC_REPRESENTATION_CONTEXT ( 3 ) GLOBAL_UNCERTAINTY_ASSIGNED_CONTEXT ( ( #36835 ) ) GLOBAL_UNIT_ASSIGNED_CONTEXT ( ( #38466, #28527, #65842 ) ) REPRESENTATION_CONTEXT ( 'NONE', 'WORKASPACE' ) );
#17175=TOROIDAL_SURFACE ( 'NONE', #44159, 1.000000000000000000, 0.5000000000000000000 ) ;
#17181=CARTESIAN_POINT ( 'NONE',  ( 45.43546989188912022, 10.14515663062970496, 3.347022959407293996 ) ) ;
#17184=AXIS2_PLACEMENT_3D ( 'NONE', #51131, #24368, #45862 ) ;
#17185=CARTESIAN_POINT ( 'NONE',  ( -83.99999999999997158, 50.00000000000000000, 12.00000000000000000 ) ) ;
#17186=ADVANCED_FACE ( 'NONE', ( #19495 ), #56092, .T. ) ;
#17190=CARTESIAN_POINT ( 'NONE',  ( -3.094860106618432471, 140.7049999999999557, -9.525000000000000355 ) ) ;
#17195=UNCERTAINTY_MEASURE_WITH_UNIT (LENGTH_MEASURE( 1.000000000000000082E-05 ), #35580, 'distance_accuracy_value', 'NONE');
#17196=COLOUR_RGB ( '', 0.72549020, 0.75294118, 0.79215686) ;
#17197=DIRECTION ( 'NONE',  ( 0.000000000000000000, 0.000000000000000000, -1.000000000000000000 ) ) ;
#17199=ORIENTED_EDGE ( 'NONE', *, *, #50209, .F. ) ;
#17202=CARTESIAN_POINT ( 'NONE',  ( -74.99999999999998579, 64.49137674618943095, -6.500000000000000888 ) ) ;
#17204=( GEOMETRIC_REPRESENTATION_CONTEXT ( 3 ) GLOBAL_UNCERTAINTY_ASSIGNED_CONTEXT ( ( #24119 ) ) GLOBAL_UNIT_ASSIGNED_CONTEXT ( ( #20669, #15416, #58986 ) ) REPRESENTATION_CONTEXT ( 'NONE', 'WORKASPACE' ) );
#17205=AXIS2_PLACEMENT_3D ( 'NONE', #69653, #6317, #38391 ) ;
#17207=CONICAL_SURFACE ( 'NONE', #62093, 5.000000000000004441, 0.7853981633974587151 ) ;
#17208=SURFACE_STYLE_USAGE ( .BOTH. , #53432 ) ;
#17211=EDGE_LOOP ( 'NONE', ( #46151, #57627, #32751, #20659, #23873, #17640, #13996, #53141, #42657, #53293 ) ) ;
#17212=DIRECTION ( 'NONE',  ( 0.000000000000000000, 0.000000000000000000, 1.000000000000000000 ) ) ;
#17214=EDGE_CURVE ( 'NONE', #49204, #33857, #31579, .T. ) ;
#17216=DIRECTION ( 'NONE',  ( -0.000000000000000000, -1.000000000000000000, -0.000000000000000000 ) ) ;
#17218=ORIENTED_EDGE ( 'NONE', *, *, #17037, .F. ) ;
#17220=VERTEX_POINT ( 'NONE', #53270 ) ;
#17223=DIRECTION ( 'NONE',  ( -0.000000000000000000, 1.000000000000000000, -0.000000000000000000 ) ) ;
#17225=AXIS2_PLACEMENT_3D ( 'NONE', #36563, #36891, #30512 ) ;
#17226=STYLED_ITEM ( 'NONE', ( #68069 ), #61247 ) ;
#17227=( NAMED_UNIT ( * ) SI_UNIT ( $, .STERADIAN. ) SOLID_ANGLE_UNIT ( ) );
#17228=CARTESIAN_POINT ( 'NONE',  ( -1.166476076187854022E-15, 158.9449999999999932, 9.525000000000000355 ) ) ;
#17231=ORIENTED_EDGE ( 'NONE', *, *, #11988, .F. ) ;
#17234=( NAMED_UNIT ( * ) SI_UNIT ( $, .STERADIAN. ) SOLID_ANGLE_UNIT ( ) );
#17235=FILL_AREA_STYLE_COLOUR ( '', #46282 ) ;
#17237=CARTESIAN_POINT ( 'NONE',  ( 8.437984349512095861, 137.1929263765338192, 1.550032578732817026E-15 ) ) ;
#17240=CARTESIAN_POINT ( 'NONE',  ( 4.716976649647099507, 125.6429263765338220, -6.492361379858953008 ) ) ;
#17249=SURFACE_STYLE_USAGE ( .BOTH. , #49580 ) ;
#17253=SURFACE_STYLE_FILL_AREA ( #1673 ) ;
#17254=UNCERTAINTY_MEASURE_WITH_UNIT (LENGTH_MEASURE( 1.000000000000000082E-05 ), #58853, 'distance_accuracy_value', 'NONE');
#17256=VECTOR ( 'NONE', #46497, 1000.000000000000000 ) ;
#17257=STYLED_ITEM ( 'NONE', ( #33779 ), #30480 ) ;
#17259=CARTESIAN_POINT ( 'NONE',  ( -45.00000000000000000, 8.554728201919928665, -6.928664365919924073 ) ) ;
#17261=ORIENTED_EDGE ( 'NONE', *, *, #25892, .F. ) ;
#17262=CARTESIAN_POINT ( 'NONE',  ( -45.13107125746175541, 8.257302774158723935, 3.517169940558448893 ) ) ;
#17263=SURFACE_STYLE_FILL_AREA ( #22155 ) ;
#17269=CARTESIAN_POINT ( 'NONE',  ( 0.000000000000000000, 87.30187232391182306, 0.000000000000000000 ) ) ;
#17271=CIRCLE ( 'NONE', #7136, 8.500000000000007105 ) ;
#17277=EDGE_CURVE ( 'NONE', #29444, #65459, #66435, .T. ) ;
#17278=EDGE_CURVE ( 'NONE', #35366, #68002, #11397, .T. ) ;
#17280=CARTESIAN_POINT ( 'NONE',  ( -9.058813317711337021, 155.0449999999999875, -2.943386871421374895 ) ) ;
#17282=CARTESIAN_POINT ( 'NONE',  ( -60.00000000000000000, -2.024042244987997205E-14, -7.500000000000000000 ) ) ;
#17285=UNCERTAINTY_MEASURE_WITH_UNIT (LENGTH_MEASURE( 1.000000000000000082E-05 ), #37060, 'distance_accuracy_value', 'NONE');
#17286=SURFACE_STYLE_FILL_AREA ( #49618 ) ;
#17288=STYLED_ITEM ( 'NONE', ( #23667 ), #2427 ) ;
#17292=CIRCLE ( 'NONE', #32979, 0.5000000000000004441 ) ;
#17296=AXIS2_PLACEMENT_3D ( 'NONE', #57615, #31558, #15762 ) ;
#17298=( NAMED_UNIT ( * ) PLANE_ANGLE_UNIT ( ) SI_UNIT ( $, .RADIAN. ) );
#17299=AXIS2_PLACEMENT_3D ( 'NONE', #11137, #27296, #528 ) ;
#17306=ORIENTED_EDGE ( 'NONE', *, *, #30377, .T. ) ;
#17314=ADVANCED_FACE ( 'NONE', ( #48 ), #64171, .F. ) ;
#17315=CARTESIAN_POINT ( 'NONE',  ( -3.094860106618434248, 128.7949999999999875, 9.525000000000000355 ) ) ;
#17319=CARTESIAN_POINT ( 'NONE',  ( -48.50000000000000000, 13.41640786499872284, -7.000000000000000000 ) ) ;
#17320=CARTESIAN_POINT ( 'NONE',  ( -9.058813317711337021, 135.1550000000000011, -2.943386871421374895 ) ) ;
#17322=CARTESIAN_POINT ( 'NONE',  ( 40.99999999999998579, 107.7459666924148252, -3.000000000000000444 ) ) ;
#17324=CARTESIAN_POINT ( 'NONE',  ( 8.102448949553183510, 158.1049999999999898, -5.886773742842746238 ) ) ;
#17325=CARTESIAN_POINT ( 'NONE',  ( 44.99999999999998579, 119.9999999999999716, -10.00000000000000000 ) ) ;
#17327=VECTOR ( 'NONE', #22065, 1000.000000000000000 ) ;
#17328=DIRECTION ( 'NONE',  ( 0.000000000000000000, 0.000000000000000000, 1.000000000000000000 ) ) ;
#17329=LINE ( 'NONE', #55258, #24167 ) ;
#17331=CYLINDRICAL_SURFACE ( 'NONE', #21674, 0.5000000000000004441 ) ;
#17334=DIRECTION ( 'NONE',  ( 0.000000000000000000, 0.000000000000000000, 1.000000000000000000 ) ) ;
#17339=STYLED_ITEM ( 'NONE', ( #40517 ), #47220 ) ;
#17341=SURFACE_STYLE_USAGE ( .BOTH. , #10309 ) ;
#17344=ORIENTED_EDGE ( 'NONE', *, *, #42146, .F. ) ;
#17345=PRESENTATION_STYLE_ASSIGNMENT (( #50033 ) ) ;
#17350=STYLED_ITEM ( 'NONE', ( #22321 ), #37076 ) ;
#17353=COLOUR_RGB ( '', 0.09019608, 0.27058824, 0.51372549) ;
#17356=AXIS2_PLACEMENT_3D ( 'NONE', #45838, #19055, #67262 ) ;
#17358=CARTESIAN_POINT ( 'NONE',  ( -8.102448949553181734, 128.4950000000000045, 5.886773742842747126 ) ) ;
#17360=VECTOR ( 'NONE', #69371, 1000.000000000000000 ) ;
#17369=VECTOR ( 'NONE', #30978, 1000.000000000000000 ) ;
#17374=ORIENTED_EDGE ( 'NONE', *, *, #36763, .T. ) ;
#17383=EDGE_LOOP ( 'NONE', ( #24577, #31072, #6908, #18534 ) ) ;
#17386=CARTESIAN_POINT ( 'NONE',  ( -45.00000000000000000, 10.49999999999998579, 4.000000000000000000 ) ) ;
#17389=PRESENTATION_STYLE_ASSIGNMENT (( #53604 ) ) ;
#17391=FACE_OUTER_BOUND ( 'NONE', #52522, .T. ) ;
#17392=CARTESIAN_POINT ( 'NONE',  ( 2.607480562269076430, 150.9070736234661183, -8.025000000000000355 ) ) ;
#17394=ORIENTED_EDGE ( 'NONE', *, *, #62987, .T. ) ;
#17398=UNCERTAINTY_MEASURE_WITH_UNIT (LENGTH_MEASURE( 1.000000000000000082E-05 ), #61940, 'distance_accuracy_value', 'NONE');
#17401=CARTESIAN_POINT ( 'NONE',  ( -74.50000000000000000, 64.00000000000000000, 10.00000000000000000 ) ) ;
#17402=DIRECTION ( 'NONE',  ( 0.000000000000000000, 0.000000000000000000, 1.000000000000000000 ) ) ;
#17405=ORIENTED_EDGE ( 'NONE', *, *, #48098, .T. ) ;
#17408=ORIENTED_EDGE ( 'NONE', *, *, #12, .F. ) ;
#17409=PRESENTATION_STYLE_ASSIGNMENT (( #1121 ) ) ;
#17410=AXIS2_PLACEMENT_3D ( 'NONE', #2558, #25020, #67957 ) ;
#17412=PRESENTATION_STYLE_ASSIGNMENT (( #22659 ) ) ;
#17413=CARTESIAN_POINT ( 'NONE',  ( -44.99999999999999289, 8.589831058620415405, -5.576814063796836862 ) ) ;
#17417=CARTESIAN_POINT ( 'NONE',  ( -75.00000000000000000, 9.289150624329691297, 6.641434857031756955 ) ) ;
#17419=VERTEX_POINT ( 'NONE', #54949 ) ;
#17420=DIRECTION ( 'NONE',  ( -0.000000000000000000, -1.000000000000000000, -0.000000000000000000 ) ) ;
#17421=CARTESIAN_POINT ( 'NONE',  ( -74.99999999999998579, 50.00000000000000000, -9.500000000000000000 ) ) ;
#17423=( NAMED_UNIT ( * ) PLANE_ANGLE_UNIT ( ) SI_UNIT ( $, .RADIAN. ) );
#17425=AXIS2_PLACEMENT_3D ( 'NONE', #5739, #5389, #38855 ) ;
#17428=CARTESIAN_POINT ( 'NONE',  ( -9.058813317711337021, 134.0449999999999875, -2.943386871421374895 ) ) ;
#17433=AXIS2_PLACEMENT_3D ( 'NONE', #12523, #21108, #12882 ) ;
#17435=CARTESIAN_POINT ( 'NONE',  ( 12.72792206135785698, 115.4999999999999574, -10.50000000000000000 ) ) ;
#17436=FACE_OUTER_BOUND ( 'NONE', #66044, .T. ) ;
#17439=EDGE_CURVE ( 'NONE', #49204, #53532, #24586, .T. ) ;
#17440=CARTESIAN_POINT ( 'NONE',  ( -44.99999999999998579, 119.9999999999999716, -7.500000000000000000 ) ) ;
#17446=EDGE_CURVE ( 'NONE', #35727, #42295, #46099, .T. ) ;
#17447=ORIENTED_EDGE ( 'NONE', *, *, #52039, .F. ) ;
#17449=EDGE_CURVE ( 'NONE', #58089, #38966, #23601, .T. ) ;
#17453=( NAMED_UNIT ( * ) SI_UNIT ( $, .STERADIAN. ) SOLID_ANGLE_UNIT ( ) );
#17454=DIRECTION ( 'NONE',  ( 0.000000000000000000, 0.000000000000000000, 1.000000000000000000 ) ) ;
#17460=LINE ( 'NONE', #16760, #57405 ) ;
#17465=CIRCLE ( 'NONE', #38823, 0.4999999999999991118 ) ;
#17468=DIRECTION ( 'NONE',  ( 0.000000000000000000, 1.000000000000000000, -0.000000000000000000 ) ) ;
#17470=CIRCLE ( 'NONE', #18607, 5.000000000000004441 ) ;
#17471=CARTESIAN_POINT ( 'NONE',  ( 4.716976649647096842, 122.8570736234661638, 6.492361379858953896 ) ) ;
#17472=FILL_AREA_STYLE_COLOUR ( '', #34938 ) ;
#17473=PLANE ( 'NONE',  #45217 ) ;
#17476=CIRCLE ( 'NONE', #21930, 1.000000000000000888 ) ;
#17480=SURFACE_STYLE_USAGE ( .BOTH. , #49821 ) ;
#17481=CARTESIAN_POINT ( 'NONE',  ( 0.000000000000000000, 87.30187232391182306, 8.025000000000000355 ) ) ;
#17482=AXIS2_PLACEMENT_3D ( 'NONE', #68691, #69041, #4647 ) ;
#17486=STYLED_ITEM ( 'NONE', ( #11994 ), #56833 ) ;
#17487=DIRECTION ( 'NONE',  ( 0.000000000000000000, 1.000000000000000000, 0.000000000000000000 ) ) ;
#17489=( GEOMETRIC_REPRESENTATION_CONTEXT ( 3 ) GLOBAL_UNCERTAINTY_ASSIGNED_CONTEXT ( ( #47630 ) ) GLOBAL_UNIT_ASSIGNED_CONTEXT ( ( #7221, #66291, #35339 ) ) REPRESENTATION_CONTEXT ( 'NONE', 'WORKASPACE' ) );
#17490=ORIENTED_EDGE ( 'NONE', *, *, #60742, .T. ) ;
#17492=CARTESIAN_POINT ( 'NONE',  ( 40.99999999999998579, 108.0000000000000000, 3.500000000000000000 ) ) ;
#17497=ORIENTED_EDGE ( 'NONE', *, *, #20051, .F. ) ;
#17499=SURFACE_STYLE_USAGE ( .BOTH. , #50531 ) ;
#17507=CARTESIAN_POINT ( 'NONE',  ( -2.056319983864984824, 153.0517686201319805, -7.829595205988884032 ) ) ;
#17512=CIRCLE ( 'NONE', #56810, 10.02499999999997904 ) ;
#17513=ORIENTED_EDGE ( 'NONE', *, *, #16945, .F. ) ;
#17520=TOROIDAL_SURFACE ( 'NONE', #40028, 1.000000000000000000, 0.5000000000000000000 ) ;
#17523=DIRECTION ( 'NONE',  ( 0.000000000000000000, 0.000000000000000000, 1.000000000000000000 ) ) ;
#17524=CARTESIAN_POINT ( 'NONE',  ( 44.34845674352007450, 9.782818914506686170, 3.509226550553890878 ) ) ;
#17526=PLANE ( 'NONE',  #19229 ) ;
#17530=( GEOMETRIC_REPRESENTATION_CONTEXT ( 3 ) GLOBAL_UNCERTAINTY_ASSIGNED_CONTEXT ( ( #41901 ) ) GLOBAL_UNIT_ASSIGNED_CONTEXT ( ( #38436, #44409, #12673 ) ) REPRESENTATION_CONTEXT ( 'NONE', 'WORKASPACE' ) );
#17532=CARTESIAN_POINT ( 'NONE',  ( 10.01517768586949231, 145.8050000000000068, 1.839758294383810543E-15 ) ) ;
#17534=COLOUR_RGB ( '', 0.09019608, 0.27058824, 0.51372549) ;
#17535=VECTOR ( 'NONE', #59865, 1000.000000000000000 ) ;
#17537=CIRCLE ( 'NONE', #38895, 9.499999999999998224 ) ;
#17538=DIRECTION ( 'NONE',  ( 1.000000000000000000, 0.000000000000000000, 0.000000000000000000 ) ) ;
#17542=SURFACE_SIDE_STYLE ('',( #44634 ) ) ;
#17544=FILL_AREA_STYLE ('',( #21396 ) ) ;
#17547=CARTESIAN_POINT ( 'NONE',  ( -15.98999599679679839, 147.4999999999999716, -10.00000000000000000 ) ) ;
#17550=( NAMED_UNIT ( * ) PLANE_ANGLE_UNIT ( ) SI_UNIT ( $, .RADIAN. ) );
#17555=CIRCLE ( 'NONE', #4055, 0.5000000000000004441 ) ;
#17561=AXIS2_PLACEMENT_3D ( 'NONE', #5401, #43471, #33542 ) ;
#17562=AXIS2_PLACEMENT_3D ( 'NONE', #21430, #16198, #21090 ) ;
#17569=CARTESIAN_POINT ( 'NONE',  ( -7.593134170275801509, 110.5000000000000000, -5.767355889360383792 ) ) ;
#17570=FILL_AREA_STYLE_COLOUR ( '', #55209 ) ;
#17572=CARTESIAN_POINT ( 'NONE',  ( 44.50000000000000000, 10.36037961002804408, 3.500000000000000000 ) ) ;
#17574=CARTESIAN_POINT ( 'NONE',  ( -7.632228543268608334, 138.8429263765337964, 2.479861379858952830 ) ) ;
#17575=CARTESIAN_POINT ( 'NONE',  ( -75.00000000000000000, -2.215169945516535778E-14, 6.999999999999999112 ) ) ;
#17576=ADVANCED_FACE ( 'NONE', ( #19675 ), #2190, .F. ) ;
#17578=COLOUR_RGB ( '', 0.31764706, 0.68627451, 0.89019608) ;
#17579=CARTESIAN_POINT ( 'NONE',  ( -2.607480562269094637, 114.0929263765338106, -8.024999999999986144 ) ) ;
#17580=EDGE_CURVE ( 'NONE', #68346, #37399, #14671, .T. ) ;
#17581=EDGE_LOOP ( 'NONE', ( #22814, #63303, #15006, #12651 ) ) ;
#17585=DIRECTION ( 'NONE',  ( 0.000000000000000000, 0.000000000000000000, 1.000000000000000000 ) ) ;
#17587=DIRECTION ( 'NONE',  ( 1.000000000000000000, 0.000000000000000000, 0.000000000000000000 ) ) ;
#17588=DIRECTION ( 'NONE',  ( 0.000000000000000000, 0.000000000000000000, 1.000000000000000000 ) ) ;
#17594=DIRECTION ( 'NONE',  ( -0.000000000000000000, -0.000000000000000000, 1.000000000000000000 ) ) ;
#17597=CARTESIAN_POINT ( 'NONE',  ( -45.90821247049333920, 9.419343807758844278, 3.356427483424777147 ) ) ;
#17600=ORIENTED_EDGE ( 'NONE', *, *, #62709, .T. ) ;
#17604=FACE_OUTER_BOUND ( 'NONE', #30487, .T. ) ;
#17605=ORIENTED_EDGE ( 'NONE', *, *, #68811, .T. ) ;
#17606=CARTESIAN_POINT ( 'NONE',  ( -45.50000000000000000, 9.708372675170618749, -3.611004237778681514 ) ) ;
#17613=( GEOMETRIC_REPRESENTATION_CONTEXT ( 3 ) GLOBAL_UNCERTAINTY_ASSIGNED_CONTEXT ( ( #11530 ) ) GLOBAL_UNIT_ASSIGNED_CONTEXT ( ( #69140, #64185, #14629 ) ) REPRESENTATION_CONTEXT ( 'NONE', 'WORKASPACE' ) );
#17615=CARTESIAN_POINT ( 'NONE',  ( -3.094860106618434248, 155.7950000000000159, 9.525000000000000355 ) ) ;
#17622=DIRECTION ( 'NONE',  ( 0.000000000000000000, 0.000000000000000000, -1.000000000000000000 ) ) ;
#17627=CYLINDRICAL_SURFACE ( 'NONE', #60537, 0.5000000000000004441 ) ;
#17631=ORIENTED_EDGE ( 'NONE', *, *, #37100, .T. ) ;
#17633=CARTESIAN_POINT ( 'NONE',  ( 15.48999599679679662, 118.4999999999999716, -10.00000000000000000 ) ) ;
#17634=( NAMED_UNIT ( * ) SI_UNIT ( $, .STERADIAN. ) SOLID_ANGLE_UNIT ( ) );
#17635=EDGE_CURVE ( 'NONE', #47666, #23836, #52745, .T. ) ;
#17638=COLOUR_RGB ( '', 0.66274510, 0.83137255, 0.94901961) ;
#17640=ORIENTED_EDGE ( 'NONE', *, *, #58684, .T. ) ;
#17642=VERTEX_POINT ( 'NONE', #20726 ) ;
#17644=CARTESIAN_POINT ( 'NONE',  ( -60.00000000000000000, -2.024042244987997205E-14, 6.500000000000000000 ) ) ;
#17648=DIRECTION ( 'NONE',  ( 1.000000000000000000, 0.000000000000000000, 0.000000000000000000 ) ) ;
#17649=CARTESIAN_POINT ( 'NONE',  ( -8.102448949553181734, 130.8949999999999818, -5.886773742842749790 ) ) ;
#17654=CARTESIAN_POINT ( 'NONE',  ( -3.094860106618434248, 129.9050000000000011, 9.525000000000000355 ) ) ;
#17656=LINE ( 'NONE', #23938, #57647 ) ;
#17658=CARTESIAN_POINT ( 'NONE',  ( -5.598654528085806881, 152.8549999999999898, -7.705886871421374629 ) ) ;
#17661=CIRCLE ( 'NONE', #35619, 1.000000000000000888 ) ;
#17666=DIRECTION ( 'NONE',  ( 0.000000000000000000, 0.000000000000000000, 1.000000000000000000 ) ) ;
#17667=ORIENTED_EDGE ( 'NONE', *, *, #53672, .F. ) ;
#17669=CARTESIAN_POINT ( 'NONE',  ( 0.9728900412908074724, 111.9999999999999858, -7.965808808122197604 ) ) ;
#17675=CYLINDRICAL_SURFACE ( 'NONE', #29486, 0.5000000000000004441 ) ;
#17678=ORIENTED_EDGE ( 'NONE', *, *, #46951, .F. ) ;
#17681=FACE_OUTER_BOUND ( 'NONE', #28042, .T. ) ;
#17685=ORIENTED_EDGE ( 'NONE', *, *, #59289, .T. ) ;
#17688=CARTESIAN_POINT ( 'NONE',  ( -74.29315614335106943, 8.620779964796561501, -6.438673729883925390 ) ) ;
#17690=SURFACE_STYLE_FILL_AREA ( #12724 ) ;
#17691=CARTESIAN_POINT ( 'NONE',  ( -75.00000000000000000, -2.215169945516535778E-14, -9.500000000000000000 ) ) ;
#17693=CARTESIAN_POINT ( 'NONE',  ( -9.058813317711337021, 134.0449999999999875, -2.943386871421374895 ) ) ;
#17703=AXIS2_PLACEMENT_3D ( 'NONE', #14804, #15853, #10214 ) ;
#17705=DIRECTION ( 'NONE',  ( 0.000000000000000000, 0.000000000000000000, 1.000000000000000000 ) ) ;
#17706=ORIENTED_EDGE ( 'NONE', *, *, #40356, .T. ) ;
#17718=CARTESIAN_POINT ( 'NONE',  ( 60.00000000000000000, 147.4999999999999716, -9.500000000000000000 ) ) ;
#17719=ADVANCED_FACE ( 'NONE', ( #39068 ), #29505, .T. ) ;
#17720=( NAMED_UNIT ( * ) PLANE_ANGLE_UNIT ( ) SI_UNIT ( $, .RADIAN. ) );
#17721=CARTESIAN_POINT ( 'NONE',  ( -40.99999999999997868, 10.49999999999998046, -3.000000000000000444 ) ) ;
#17722=CARTESIAN_POINT ( 'NONE',  ( 2.607480562269071989, 149.7070736234661581, 8.025000000000002132 ) ) ;
#17728=CARTESIAN_POINT ( 'NONE',  ( 8.102448949553181734, 130.5049999999999670, 5.886773742842750679 ) ) ;
#17736=CARTESIAN_POINT ( 'NONE',  ( 23.71231517720798010, 117.4999999999999716, 7.000000000000000000 ) ) ;
#17742=ORIENTED_EDGE ( 'NONE', *, *, #21060, .F. ) ;
#17743=PRESENTATION_STYLE_ASSIGNMENT (( #38879 ) ) ;
#17745=FILL_AREA_STYLE_COLOUR ( '', #10128 ) ;
#17749=CARTESIAN_POINT ( 'NONE',  ( -74.23282891375464487, 8.859195963244939520, 6.389740745940710731 ) ) ;
#17751=ORIENTED_EDGE ( 'NONE', *, *, #57620, .T. ) ;
#17752=SURFACE_SIDE_STYLE ('',( #28616 ) ) ;
#17754=( LENGTH_UNIT ( ) NAMED_UNIT ( * ) SI_UNIT ( .MILLI., .METRE. ) );
#17758=CARTESIAN_POINT ( 'NONE',  ( -9.058813317711338797, 137.3449999999999989, 2.943386871421373563 ) ) ;
#17763=AXIS2_PLACEMENT_3D ( 'NONE', #59887, #64821, #32817 ) ;
#17764=SURFACE_STYLE_USAGE ( .BOTH. , #44532 ) ;
#17765=( NAMED_UNIT ( * ) SI_UNIT ( $, .STERADIAN. ) SOLID_ANGLE_UNIT ( ) );
#17766=( GEOMETRIC_REPRESENTATION_CONTEXT ( 3 ) GLOBAL_UNCERTAINTY_ASSIGNED_CONTEXT ( ( #42590 ) ) GLOBAL_UNIT_ASSIGNED_CONTEXT ( ( #7668, #34741, #8025 ) ) REPRESENTATION_CONTEXT ( 'NONE', 'WORKASPACE' ) );
#17769=DIRECTION ( 'NONE',  ( -0.000000000000000000, -1.000000000000000000, 0.000000000000000000 ) ) ;
#17776=( LENGTH_UNIT ( ) NAMED_UNIT ( * ) SI_UNIT ( .MILLI., .METRE. ) );
#17780=FACE_OUTER_BOUND ( 'NONE', #46278, .T. ) ;
#17782=SURFACE_STYLE_USAGE ( .BOTH. , #44886 ) ;
#17783=DIRECTION ( 'NONE',  ( 1.000000000000000000, 0.000000000000000000, 0.000000000000000000 ) ) ;
#17787=SURFACE_SIDE_STYLE ('',( #60661 ) ) ;
#17789=CYLINDRICAL_SURFACE ( 'NONE', #23630, 0.5000000000000004441 ) ;
#17792=CARTESIAN_POINT ( 'NONE',  ( -74.99999999999998579, 50.00000000000000000, 10.00000000000000000 ) ) ;
#17798=CARTESIAN_POINT ( 'NONE',  ( 0.000000000000000000, 121.0570736234661524, -8.025000000000000355 ) ) ;
#17802=EDGE_LOOP ( 'NONE', ( #17875, #18652, #19881, #40822 ) ) ;
#17803=EDGE_CURVE ( 'NONE', #66756, #24087, #2233, .T. ) ;
#17805=CARTESIAN_POINT ( 'NONE',  ( 34.99999999999992895, 109.9999999999999858, -9.500000000000000000 ) ) ;
#17806=EDGE_CURVE ( 'NONE', #13013, #11552, #68608, .T. ) ;
#17811=CARTESIAN_POINT ( 'NONE',  ( -20.40110905463057023, 114.8435661791816358, -10.33328836125512851 ) ) ;
#17812=CARTESIAN_POINT ( 'NONE',  ( 45.58253334211660501, 9.942242644401712681, 6.446113437190048145 ) ) ;
#17813=ADVANCED_FACE ( 'NONE', ( #2340 ), #29829, .T. ) ;
#17823=SURFACE_STYLE_USAGE ( .BOTH. , #13214 ) ;
#17830=DIRECTION ( 'NONE',  ( 1.156482317317873451E-16, 1.000000000000000000, -0.000000000000000000 ) ) ;
#17831=CARTESIAN_POINT ( 'NONE',  ( -48.00000000000000000, 13.41640786499872284, -9.500000000000000000 ) ) ;
#17832=ORIENTED_EDGE ( 'NONE', *, *, #62690, .F. ) ;
#17834=DIRECTION ( 'NONE',  ( -0.000000000000000000, -0.000000000000000000, -1.000000000000000000 ) ) ;
#17835=DIRECTION ( 'NONE',  ( 1.000000000000000000, 0.000000000000000000, 0.000000000000000000 ) ) ;
#17838=ORIENTED_EDGE ( 'NONE', *, *, #51315, .T. ) ;
#17842=AXIS2_PLACEMENT_3D ( 'NONE', #17435, #56061, #22684 ) ;
#17846=CARTESIAN_POINT ( 'NONE',  ( 44.58498124287052633, 10.41703377194163949, 3.499556662980364496 ) ) ;
#17847=SURFACE_STYLE_USAGE ( .BOTH. , #37963 ) ;
#17851=LINE ( 'NONE', #17185, #32626 ) ;
#17853=CARTESIAN_POINT ( 'NONE',  ( -10.01517768586949231, 144.3049999999999784, -6.132527647946036459E-16 ) ) ;
#17854=FACE_OUTER_BOUND ( 'NONE', #16548, .T. ) ;
#17856=UNCERTAINTY_MEASURE_WITH_UNIT (LENGTH_MEASURE( 1.000000000000000082E-05 ), #56252, 'distance_accuracy_value', 'NONE');
#17857=( NAMED_UNIT ( * ) PLANE_ANGLE_UNIT ( ) SI_UNIT ( $, .RADIAN. ) );
#17859=VECTOR ( 'NONE', #18105, 1000.000000000000000 ) ;
#17863=AXIS2_PLACEMENT_3D ( 'NONE', #14740, #41846, #52390 ) ;
#17864=CARTESIAN_POINT ( 'NONE',  ( -44.99999999999977973, 146.4999999999999716, -7.000000000000000000 ) ) ;
#17867=CARTESIAN_POINT ( 'NONE',  ( 48.00000000000000000, 13.41640786499872462, 9.500000000000000000 ) ) ;
#17871=CARTESIAN_POINT ( 'NONE',  ( 14.98999599679679662, 118.4999999999999716, 10.00000000000000000 ) ) ;
#17874=FILL_AREA_STYLE ('',( #29452 ) ) ;
#17875=ORIENTED_EDGE ( 'NONE', *, *, #32399, .T. ) ;
#17879=ORIENTED_EDGE ( 'NONE', *, *, #1122, .F. ) ;
#17883=ADVANCED_FACE ( 'NONE', ( #31198 ), #68517, .F. ) ;
#17885=DIRECTION ( 'NONE',  ( -1.000000000000000000, -0.000000000000000000, 0.000000000000000000 ) ) ;
#17888=CIRCLE ( 'NONE', #68407, 0.5000000000000004441 ) ;
#17893=EDGE_CURVE ( 'NONE', #11547, #45027, #62147, .T. ) ;
#17896=CARTESIAN_POINT ( 'NONE',  ( -7.632228543268607446, 135.5429263765338135, -2.479861379858953718 ) ) ;
#17897=DIRECTION ( 'NONE',  ( 0.000000000000000000, 0.000000000000000000, 1.000000000000000000 ) ) ;
#17898=CIRCLE ( 'NONE', #46042, 26.99999999999999645 ) ;
#17900=EDGE_LOOP ( 'NONE', ( #68862, #18044, #66549, #8829 ) ) ;
#17901=ORIENTED_EDGE ( 'NONE', *, *, #47156, .F. ) ;
#17902=PRESENTATION_STYLE_ASSIGNMENT (( #66426 ) ) ;
#17903=LINE ( 'NONE', #39388, #46820 ) ;
#17905=SURFACE_SIDE_STYLE ('',( #1672 ) ) ;
#17910=( NAMED_UNIT ( * ) PLANE_ANGLE_UNIT ( ) SI_UNIT ( $, .RADIAN. ) );
#17913=FILL_AREA_STYLE_COLOUR ( '', #62000 ) ;
#17915=DIRECTION ( 'NONE',  ( -0.000000000000000000, 1.000000000000000000, -0.000000000000000000 ) ) ;
#17917=CARTESIAN_POINT ( 'NONE',  ( -44.99154893936433552, 9.591540374752312914, 3.500000000000000000 ) ) ;
#17919=DIRECTION ( 'NONE',  ( 0.000000000000000000, 0.000000000000000000, 1.000000000000000000 ) ) ;
#17920=COLOUR_RGB ( '', 0.08235294, 0.09019608, 0.10196078) ;
#17923=ADVANCED_FACE ( 'NONE', ( #62527 ), #36882, .T. ) ;
#17924=AXIS2_PLACEMENT_3D ( 'NONE', #18811, #34998, #29725 ) ;
#17925=PRESENTATION_STYLE_ASSIGNMENT (( #60810 ) ) ;
#17926=DIRECTION ( 'NONE',  ( -0.000000000000000000, -0.000000000000000000, 1.000000000000000000 ) ) ;
#17927=CARTESIAN_POINT ( 'NONE',  ( 4.716976649647096842, 116.8570736234661638, 6.492361379858953896 ) ) ;
#17928=CARTESIAN_POINT ( 'NONE',  ( 5.728833613173035744, 154.5000000000000568, -7.622147220416790603 ) ) ;
#17930=DIRECTION ( 'NONE',  ( 1.000000000000000000, 0.000000000000000000, 0.000000000000000000 ) ) ;
#17932=CARTESIAN_POINT ( 'NONE',  ( 3.094860106618435136, 116.4049999999999869, -9.525000000000000355 ) ) ;
#17934=DIRECTION ( 'NONE',  ( 0.000000000000000000, 0.000000000000000000, -1.000000000000000000 ) ) ;
#17936=CARTESIAN_POINT ( 'NONE',  ( -7.632228543268608334, 141.8429263765338249, 2.479861379858952830 ) ) ;
#17939=UNCERTAINTY_MEASURE_WITH_UNIT (LENGTH_MEASURE( 1.000000000000000082E-05 ), #33564, 'distance_accuracy_value', 'NONE');
#17941=LINE ( 'NONE', #8080, #61054 ) ;
#17948=EDGE_CURVE ( 'NONE', #37046, #46653, #65188, .T. ) ;
#17950=PLANE ( 'NONE',  #29570 ) ;
#17952=ORIENTED_EDGE ( 'NONE', *, *, #18692, .F. ) ;
#17955=( BOUNDED_SURFACE ( )  B_SPLINE_SURFACE ( 1, 2, ( 
 ( #7332, #8710, #13271, #30134, #61453, #1964, #61795, #24511, #3376, #55852, #7651, #13625, #56183, #51276, #29087, #46383, #66403, #39705, #24869, #12937, #34399, #8009, #35086, #56536, #8378, #29811, #20293, #47434, #52343, #57594, #35790, #57232, #25228, #9770, #36866, #68502, #15737, #4811, #37218, #30845, #31180, #4091, #30485, #68856, #14690, #5151, #51981, #15063, #9422, #42848, #46747, #52672, #36535, #25559, #42169, #4439, #64242, #20998, #9065, #69197, #63220, #58631, #47074, #3736, #20657, #26263, #53018, #36164, #41799, #25910, #57955, #31537, #63561, #26596, #58279, #68157, #15406, #69522, #53366, #10107, #47799, #42496, #10454, #19944, #21326, #63888, #41437, #31887, #48119, #62849, #13116, #39898, #16455, #60593, #18414, #2517, #5836, #29287, #59293, #39197, #7838, #27275, #23330, #32240, #43205, #513, #44495, #56022, #37582, #21686, #50768, #66595, #18058, #48462, #65898, #24026, #23000, #34569, #28590, #61305, #45534, #11119, #32569, #60948, #33872, #54031, #48815, #16100, #58979, #50087, #12766, #2141, #7160, #17728, #12411, #55335, #10792, #1815, #44828, #66232, #64609, #39543, #53688, #50416, #37918, #34238, #155, #55692, #23672, #7500, #28929, #45176, #5474, #26925, #3205, #68336, #62680, #56372, #19438, #8209, #66950, #46216, #35636, #51818, #57787, #13822, #31029, #68003, #45854, #57072, #4268, #61994, #40228, #40580, #25749, #52181, #29991, #14507, #29656, #34926, #35283, #30314, #56746, #52523, #8889, #2870, #35983, #57428, #40935, #18747, #3940, #25411, #67636, #3567, #46926, #9257, #24698, #9612, #62357, #30673, #8558, #20116, #25069, #14180, #51455, #61633, #13458, #41624, #51123, #63042, #46578, #19791, #41283, #24359, #14884, #67285, #36367, #19074, #32770, #48296, #15934, #36718, #58817, #43395, #37765, #10967, #21168, #9943, #59141, #37053, #54219, #27118, #32405, #6035, #26769, #28187, #21520, #31366, #10293, #53208, #4993, #64786, #31724, #43037, #16623, #26446, #4642, #59487, #58133, #15250, #68688, #53872, #350, #38089, #37416, #47266, #42680, #11313, #10632, #26097, #20486, #32083, #64442, #41993, #52864, #21885, #47629, #63403, #69036, #47978, #20847, #42347, #63731, #16289, #64081, #15579, #58468, #69377, #53540, #5326, #5669, #48651, #17658, #28144, #49652, #22567, #61233, #44424, #44069, #1397, #54567, #60197, #28859, #60872, #688, #13044, #45104, #39468, #6375, #39818, #65110, #50341, #22220, #17981, #12004, #39126, #65473, #49309, #27472, #48999, #16964, #22925, #28509, #33465, #7437, #66151, #2065, #17324, #65826, #38784, #43715, #60516, #27803, #66516, #38451, #6717, #1020, #34498, #59851, #12328, #33801, #54890, #55252, #7078, #55950, #12685, #11660, #34156, #50011, #23593, #1749 ),
 ( #18338, #23259, #33130, #44756, #55614, #25329, #18990, #14097, #67916, #30587, #29199, #41534, #8482, #14796, #2795, #19708, #3844, #46850, #52094, #8123, #51375, #9171, #62950, #67201, #20035, #51036, #29916, #68255, #40499, #35557, #23941, #34839, #61916, #35196, #36273, #50687, #13378, #7756, #57337, #8807, #40157, #56655, #2430, #13736, #45454, #19349, #66874, #18679, #24284, #61551, #56291, #24613, #3118, #45781, #56994, #46130, #29566, #62604, #67552, #41203, #40853, #62270, #30232, #51730, #3478, #46490, #24979, #14418, #35891, #47896, #20761, #53459, #58054, #48562, #58730, #16543, #53119, #21793, #5581, #68952, #63993, #48211, #10887, #9527, #43306, #58378, #64705, #52778, #69619, #53779, #27028, #32328, #9861, #31640, #59068, #57698, #47538, #258, #31279, #10203, #30946, #42269, #15842, #4187, #15165, #63657, #15500, #52443, #25662, #63315, #47181, #37672, #10549, #20397, #36966, #68601, #4907, #41899, #69295, #36636, #4552, #26009, #26358, #31988, #21089, #42588, #37323, #5243, #26687, #21428, #42947, #64349, #16196, #38703, #60103, #33040, #1975, #54805, #54476, #11920, #65023, #926, #39376, #1661, #11223, #23497, #55521, #49922, #16881, #50256, #5937, #60775, #32672, #28410, #22477, #49567, #6290, #59758, #38003, #59390, #27382, #33380, #39039, #43975, #17896, #6989, #12595, #27721, #6615, #49219, #54126, #1299, #38356, #7345, #48913, #17237, #11568, #65390, #28056, #34065, #28772, #22832, #33708, #23179, #44332, #65729, #17574, #60436, #45011, #12243, #55157, #44669, #66062, #66419, #610, #22133, #43627, #51995, #35801, #30150, #66778, #30496, #55865, #41113, #12949, #8721, #2703, #29822, #34740, #40078, #18236, #39720, #7667, #61810, #19251, #50944, #67817, #56908, #19615, #13284, #13640, #56196, #34411, #51288, #18593, #57246, #29099, #67116, #61466, #25241, #50596, #35103, #18900, #8024, #24523, #56552, #46759, #3388, #61143, #51631, #45701, #62519, #29474, #2331, #3031, #24883, #35466, #24195, #40401, #8390, #46039, #14003, #67454, #9079, #40755, #23852, #62172, #3749, #45359, #46395, #14335, #58641, #21338, #19951, #32249, #68870, #5485, #63230, #10467, #64255, #16110, #42862, #68512, #42182, #69535, #53697, #57964, #10802, #41813, #20671, #58989, #9780, #4820, #14703, #21009, #26273, #63572, #4451, #26936, #20306, #25920, #37591, #63899, #57606, #15418, #9431, #68172, #47447, #36875, #53030, #41449, #15076, #62858, #69208, #47085, #37232, #15751, #36548, #31190, #58291, #52686, #31898, #10121, #36177, #42503, #30858, #31548, #52353, #4103, #47810, #53379, #5162, #25572, #26608, #48129, #49151, #55438, #43554, #38960, #44587, #65987, #1572, #48829, #22389, #49832, #33978, #38270, #60698, #22051, #848, #39294 ) ),
 .UNSPECIFIED., .F., .F., .F. ) 
 B_SPLINE_SURFACE_WITH_KNOTS ( ( 2, 2 ),
 ( 3, 2, 2, 2, 2, 2, 2, 2, 2, 2, 2, 2, 2, 2, 2, 2, 2, 2, 2, 2, 2, 2, 2, 2, 2, 2, 2, 2, 2, 2, 2, 2, 2, 2, 2, 2, 2, 2, 2, 2, 2, 2, 2, 2, 2, 2, 2, 2, 2, 2, 2, 2, 2, 2, 2, 2, 2, 2, 2, 2, 2, 2, 2, 2, 2, 2, 2, 2, 2, 2, 2, 2, 2, 2, 2, 2, 2, 2, 2, 2, 2, 2, 2, 2, 2, 2, 2, 2, 2, 2, 2, 2, 2, 2, 2, 2, 2, 2, 2, 2, 2, 2, 2, 2, 2, 2, 2, 2, 2, 2, 2, 2, 2, 2, 2, 2, 2, 2, 2, 2, 2, 2, 2, 2, 2, 2, 2, 2, 2, 2, 2, 2, 2, 2, 2, 2, 2, 2, 2, 2, 2, 2, 2, 2, 2, 2, 2, 2, 2, 2, 2, 2, 2, 2, 2, 2, 2, 2, 2, 2, 2, 2, 2, 2, 2, 2, 2, 2, 2, 2, 3 ),
 ( 0.000000000000000000, 1.000000000000000000 ),
 ( 0.000000000000000000, 0.005882352941176470507, 0.01176470588235294101, 0.01764705882352941152, 0.02352941176470588203, 0.02941176470588235253, 0.03529411764705882304, 0.04117647058823529355, 0.04705882352941176405, 0.05294117647058823456, 0.05882352941176470507, 0.06470588235294118251, 0.07058823529411764608, 0.07647058823529412352, 0.08235294117647058709, 0.08823529411764706454, 0.09411764705882352811, 0.1000000000000000056, 0.1058823529411764691, 0.1117647058823529466, 0.1176470588235294101, 0.1235294117647058876, 0.1294117647058823650, 0.1352941176470588147, 0.1411764705882352922, 0.1470588235294117696, 0.1529411764705882470, 0.1588235294117646967, 0.1647058823529411742, 0.1705882352941176516, 0.1764705882352941291, 0.1823529411764705788, 0.1882352941176470562, 0.1941176470588235337, 0.2000000000000000111, 0.2058823529411764608, 0.2117647058823529382, 0.2176470588235294157, 0.2235294117647058931, 0.2294117647058823428, 0.2352941176470588203, 0.2411764705882352977, 0.2470588235294117752, 0.2529411764705882248, 0.2588235294117647300, 0.2647058823529411797, 0.2705882352941176294, 0.2764705882352941346, 0.2823529411764705843, 0.2882352941176470340, 0.2941176470588235392, 0.2999999999999999889, 0.3058823529411764941, 0.3117647058823529438, 0.3176470588235293935, 0.3235294117647058987, 0.3294117647058823484, 0.3352941176470587981, 0.3411764705882353033, 0.3470588235294117530, 0.3529411764705882582, 0.3588235294117647078, 0.3647058823529411575, 0.3705882352941176627, 0.3764705882352941124, 0.3823529411764705621, 0.3882352941176470673, 0.3941176470588235170, 0.4000000000000000222, 0.4058823529411764719, 0.4117647058823529216, 0.4176470588235294268, 0.4235294117647058765, 0.4294117647058823262, 0.4352941176470588314, 0.4411764705882352811, 0.4470588235294117863, 0.4529411764705882359, 0.4588235294117646856, 0.4647058823529411908, 0.4705882352941176405, 0.4764705882352940902, 0.4823529411764705954, 0.4882352941176470451, 0.4941176470588235503, 0.5000000000000000000, 0.5058823529411764497, 0.5117647058823528994, 0.5176470588235294601, 0.5235294117647059098, 0.5294117647058823595, 0.5352941176470588092, 0.5411764705882352589, 0.5470588235294118196, 0.5529411764705882693, 0.5588235294117647189, 0.5647058823529411686, 0.5705882352941176183, 0.5764705882352940680, 0.5823529411764706287, 0.5882352941176470784, 0.5941176470588235281, 0.5999999999999999778, 0.6058823529411764275, 0.6117647058823529882, 0.6176470588235294379, 0.6235294117647058876, 0.6294117647058823373, 0.6352941176470587870, 0.6411764705882353477, 0.6470588235294117974, 0.6529411764705882470, 0.6588235294117646967, 0.6647058823529411464, 0.6705882352941175961, 0.6764705882352941568, 0.6823529411764706065, 0.6882352941176470562, 0.6941176470588235059, 0.6999999999999999556, 0.7058823529411765163, 0.7117647058823529660, 0.7176470588235294157, 0.7235294117647058654, 0.7294117647058823151, 0.7352941176470588758, 0.7411764705882353255, 0.7470588235294117752, 0.7529411764705882248, 0.7588235294117646745, 0.7647058823529411242, 0.7705882352941176849, 0.7764705882352941346, 0.7823529411764705843, 0.7882352941176470340, 0.7941176470588234837, 0.8000000000000000444, 0.8058823529411764941, 0.8117647058823529438, 0.8176470588235293935, 0.8235294117647058432, 0.8294117647058824039, 0.8352941176470588536, 0.8411764705882353033, 0.8470588235294117530, 0.8529411764705882026, 0.8588235294117646523, 0.8647058823529412130, 0.8705882352941176627, 0.8764705882352941124, 0.8823529411764705621, 0.8882352941176470118, 0.8941176470588235725, 0.9000000000000000222, 0.9058823529411764719, 0.9117647058823529216, 0.9176470588235293713, 0.9235294117647059320, 0.9294117647058823817, 0.9352941176470588314, 0.9411764705882352811, 0.9470588235294117307, 0.9529411764705881804, 0.9588235294117647411, 0.9647058823529411908, 0.9705882352941176405, 0.9764705882352940902, 0.9823529411764705399, 0.9882352941176471006, 0.9941176470588235503, 1.000000000000000000 ),
 .UNSPECIFIED. ) 
 GEOMETRIC_REPRESENTATION_ITEM ( )  RATIONAL_B_SPLINE_SURFACE ( (
 ( 1.000000000000000000, 0.9510565162951535312, 1.000000000000000000, 0.9510565162951535312, 1.000000000000000000, 0.9510565162951535312, 1.000000000000000000, 0.9510565162951535312, 1.000000000000000000, 0.9510565162951535312, 1.000000000000000000, 0.9510565162951535312, 1.000000000000000000, 0.9510565162951535312, 1.000000000000000000, 0.9510565162951535312, 1.000000000000000000, 0.9510565162951535312, 1.000000000000000000, 0.9510565162951535312, 1.000000000000000000, 0.9510565162951535312, 1.000000000000000000, 0.9510565162951535312, 1.000000000000000000, 0.9510565162951535312, 1.000000000000000000, 0.9510565162951535312, 1.000000000000000000, 0.9510565162951535312, 1.000000000000000000, 0.9510565162951535312, 1.000000000000000000, 0.9510565162951535312, 1.000000000000000000, 0.9510565162951535312, 1.000000000000000000, 0.9510565162951535312, 1.000000000000000000, 0.9510565162951535312, 1.000000000000000000, 0.9510565162951535312, 1.000000000000000000, 0.9510565162951535312, 1.000000000000000000, 0.9510565162951535312, 1.000000000000000000, 0.9510565162951535312, 1.000000000000000000, 0.9510565162951535312, 1.000000000000000000, 0.9510565162951535312, 1.000000000000000000, 0.9510565162951535312, 1.000000000000000000, 0.9510565162951535312, 1.000000000000000000, 0.9510565162951535312, 1.000000000000000000, 0.9510565162951535312, 1.000000000000000000, 0.9510565162951535312, 1.000000000000000000, 0.9510565162951535312, 1.000000000000000000, 0.9510565162951535312, 1.000000000000000000, 0.9510565162951535312, 1.000000000000000000, 0.9510565162951535312, 1.000000000000000000, 0.9510565162951535312, 1.000000000000000000, 0.9510565162951535312, 1.000000000000000000, 0.9510565162951535312, 1.000000000000000000, 0.9510565162951535312, 1.000000000000000000, 0.9510565162951535312, 1.000000000000000000, 0.9510565162951535312, 1.000000000000000000, 0.9510565162951535312, 1.000000000000000000, 0.9510565162951535312, 1.000000000000000000, 0.9510565162951535312, 1.000000000000000000, 0.9510565162951535312, 1.000000000000000000, 0.9510565162951535312, 1.000000000000000000, 0.9510565162951535312, 1.000000000000000000, 0.9510565162951535312, 1.000000000000000000, 0.9510565162951535312, 1.000000000000000000, 0.9510565162951535312, 1.000000000000000000, 0.9510565162951535312, 1.000000000000000000, 0.9510565162951535312, 1.000000000000000000, 0.9510565162951535312, 1.000000000000000000, 0.9510565162951535312, 1.000000000000000000, 0.9510565162951535312, 1.000000000000000000, 0.9510565162951535312, 1.000000000000000000, 0.9510565162951535312, 1.000000000000000000, 0.9510565162951535312, 1.000000000000000000, 0.9510565162951535312, 1.000000000000000000, 0.9510565162951535312, 1.000000000000000000, 0.9510565162951535312, 1.000000000000000000, 0.9510565162951535312, 1.000000000000000000, 0.9510565162951535312, 1.000000000000000000, 0.9510565162951535312, 1.000000000000000000, 0.9510565162951535312, 1.000000000000000000, 0.9510565162951535312, 1.000000000000000000, 0.9510565162951535312, 1.000000000000000000, 0.9510565162951535312, 1.000000000000000000, 0.9510565162951535312, 1.000000000000000000, 0.9510565162951535312, 1.000000000000000000, 0.9510565162951535312, 1.000000000000000000, 0.9510565162951535312, 1.000000000000000000, 0.9510565162951535312, 1.000000000000000000, 0.9510565162951535312, 1.000000000000000000, 0.9510565162951535312, 1.000000000000000000, 0.9510565162951535312, 1.000000000000000000, 0.9510565162951535312, 1.000000000000000000, 0.9510565162951535312, 1.000000000000000000, 0.9510565162951535312, 1.000000000000000000, 0.9510565162951535312, 1.000000000000000000, 0.9510565162951535312, 1.000000000000000000, 0.9510565162951535312, 1.000000000000000000, 0.9510565162951535312, 1.000000000000000000, 0.9510565162951535312, 1.000000000000000000, 0.9510565162951535312, 1.000000000000000000, 0.9510565162951535312, 1.000000000000000000, 0.9510565162951535312, 1.000000000000000000, 0.9510565162951535312, 1.000000000000000000, 0.9510565162951535312, 1.000000000000000000, 0.9510565162951535312, 1.000000000000000000, 0.9510565162951535312, 1.000000000000000000, 0.9510565162951535312, 1.000000000000000000, 0.9510565162951535312, 1.000000000000000000, 0.9510565162951535312, 1.000000000000000000, 0.9510565162951535312, 1.000000000000000000, 0.9510565162951535312, 1.000000000000000000, 0.9510565162951535312, 1.000000000000000000, 0.9510565162951535312, 1.000000000000000000, 0.9510565162951535312, 1.000000000000000000, 0.9510565162951535312, 1.000000000000000000, 0.9510565162951535312, 1.000000000000000000, 0.9510565162951535312, 1.000000000000000000, 0.9510565162951535312, 1.000000000000000000, 0.9510565162951535312, 1.000000000000000000, 0.9510565162951535312, 1.000000000000000000, 0.9510565162951535312, 1.000000000000000000, 0.9510565162951535312, 1.000000000000000000, 0.9510565162951535312, 1.000000000000000000, 0.9510565162951535312, 1.000000000000000000, 0.9510565162951535312, 1.000000000000000000, 0.9510565162951535312, 1.000000000000000000, 0.9510565162951535312, 1.000000000000000000, 0.9510565162951535312, 1.000000000000000000, 0.9510565162951535312, 1.000000000000000000, 0.9510565162951535312, 1.000000000000000000, 0.9510565162951535312, 1.000000000000000000, 0.9510565162951535312, 1.000000000000000000, 0.9510565162951535312, 1.000000000000000000, 0.9510565162951535312, 1.000000000000000000, 0.9510565162951535312, 1.000000000000000000, 0.9510565162951535312, 1.000000000000000000, 0.9510565162951535312, 1.000000000000000000, 0.9510565162951535312, 1.000000000000000000, 0.9510565162951535312, 1.000000000000000000, 0.9510565162951535312, 1.000000000000000000, 0.9510565162951535312, 1.000000000000000000, 0.9510565162951535312, 1.000000000000000000, 0.9510565162951535312, 1.000000000000000000, 0.9510565162951535312, 1.000000000000000000, 0.9510565162951535312, 1.000000000000000000, 0.9510565162951535312, 1.000000000000000000, 0.9510565162951535312, 1.000000000000000000, 0.9510565162951535312, 1.000000000000000000, 0.9510565162951535312, 1.000000000000000000, 0.9510565162951535312, 1.000000000000000000, 0.9510565162951535312, 1.000000000000000000, 0.9510565162951535312, 1.000000000000000000, 0.9510565162951535312, 1.000000000000000000, 0.9510565162951535312, 1.000000000000000000, 0.9510565162951535312, 1.000000000000000000, 0.9510565162951535312, 1.000000000000000000, 0.9510565162951535312, 1.000000000000000000, 0.9510565162951535312, 1.000000000000000000, 0.9510565162951535312, 1.000000000000000000, 0.9510565162951535312, 1.000000000000000000, 0.9510565162951535312, 1.000000000000000000, 0.9510565162951535312, 1.000000000000000000, 0.9510565162951535312, 1.000000000000000000, 0.9510565162951535312, 1.000000000000000000, 0.9510565162951535312, 1.000000000000000000, 0.9510565162951535312, 1.000000000000000000, 0.9510565162951535312, 1.000000000000000000, 0.9510565162951535312, 1.000000000000000000, 0.9510565162951535312, 1.000000000000000000, 0.9510565162951535312, 1.000000000000000000, 0.9510565162951535312, 1.000000000000000000, 0.9510565162951535312, 1.000000000000000000, 0.9510565162951535312, 1.000000000000000000, 0.9510565162951535312, 1.000000000000000000, 0.9510565162951535312, 1.000000000000000000, 0.9510565162951535312, 1.000000000000000000, 0.9510565162951535312, 1.000000000000000000, 0.9510565162951535312, 1.000000000000000000, 0.9510565162951535312, 1.000000000000000000, 0.9510565162951535312, 1.000000000000000000, 0.9510565162951535312, 1.000000000000000000, 0.9510565162951535312, 1.000000000000000000, 0.9510565162951535312, 1.000000000000000000, 0.9510565162951535312, 1.000000000000000000, 0.9510565162951535312, 1.000000000000000000),
 ( 1.000000000000000000, 0.9510565162951535312, 1.000000000000000000, 0.9510565162951535312, 1.000000000000000000, 0.9510565162951535312, 1.000000000000000000, 0.9510565162951535312, 1.000000000000000000, 0.9510565162951535312, 1.000000000000000000, 0.9510565162951535312, 1.000000000000000000, 0.9510565162951535312, 1.000000000000000000, 0.9510565162951535312, 1.000000000000000000, 0.9510565162951535312, 1.000000000000000000, 0.9510565162951535312, 1.000000000000000000, 0.9510565162951535312, 1.000000000000000000, 0.9510565162951535312, 1.000000000000000000, 0.9510565162951535312, 1.000000000000000000, 0.9510565162951535312, 1.000000000000000000, 0.9510565162951535312, 1.000000000000000000, 0.9510565162951535312, 1.000000000000000000, 0.9510565162951535312, 1.000000000000000000, 0.9510565162951535312, 1.000000000000000000, 0.9510565162951535312, 1.000000000000000000, 0.9510565162951535312, 1.000000000000000000, 0.9510565162951535312, 1.000000000000000000, 0.9510565162951535312, 1.000000000000000000, 0.9510565162951535312, 1.000000000000000000, 0.9510565162951535312, 1.000000000000000000, 0.9510565162951535312, 1.000000000000000000, 0.9510565162951535312, 1.000000000000000000, 0.9510565162951535312, 1.000000000000000000, 0.9510565162951535312, 1.000000000000000000, 0.9510565162951535312, 1.000000000000000000, 0.9510565162951535312, 1.000000000000000000, 0.9510565162951535312, 1.000000000000000000, 0.9510565162951535312, 1.000000000000000000, 0.9510565162951535312, 1.000000000000000000, 0.9510565162951535312, 1.000000000000000000, 0.9510565162951535312, 1.000000000000000000, 0.9510565162951535312, 1.000000000000000000, 0.9510565162951535312, 1.000000000000000000, 0.9510565162951535312, 1.000000000000000000, 0.9510565162951535312, 1.000000000000000000, 0.9510565162951535312, 1.000000000000000000, 0.9510565162951535312, 1.000000000000000000, 0.9510565162951535312, 1.000000000000000000, 0.9510565162951535312, 1.000000000000000000, 0.9510565162951535312, 1.000000000000000000, 0.9510565162951535312, 1.000000000000000000, 0.9510565162951535312, 1.000000000000000000, 0.9510565162951535312, 1.000000000000000000, 0.9510565162951535312, 1.000000000000000000, 0.9510565162951535312, 1.000000000000000000, 0.9510565162951535312, 1.000000000000000000, 0.9510565162951535312, 1.000000000000000000, 0.9510565162951535312, 1.000000000000000000, 0.9510565162951535312, 1.000000000000000000, 0.9510565162951535312, 1.000000000000000000, 0.9510565162951535312, 1.000000000000000000, 0.9510565162951535312, 1.000000000000000000, 0.9510565162951535312, 1.000000000000000000, 0.9510565162951535312, 1.000000000000000000, 0.9510565162951535312, 1.000000000000000000, 0.9510565162951535312, 1.000000000000000000, 0.9510565162951535312, 1.000000000000000000, 0.9510565162951535312, 1.000000000000000000, 0.9510565162951535312, 1.000000000000000000, 0.9510565162951535312, 1.000000000000000000, 0.9510565162951535312, 1.000000000000000000, 0.9510565162951535312, 1.000000000000000000, 0.9510565162951535312, 1.000000000000000000, 0.9510565162951535312, 1.000000000000000000, 0.9510565162951535312, 1.000000000000000000, 0.9510565162951535312, 1.000000000000000000, 0.9510565162951535312, 1.000000000000000000, 0.9510565162951535312, 1.000000000000000000, 0.9510565162951535312, 1.000000000000000000, 0.9510565162951535312, 1.000000000000000000, 0.9510565162951535312, 1.000000000000000000, 0.9510565162951535312, 1.000000000000000000, 0.9510565162951535312, 1.000000000000000000, 0.9510565162951535312, 1.000000000000000000, 0.9510565162951535312, 1.000000000000000000, 0.9510565162951535312, 1.000000000000000000, 0.9510565162951535312, 1.000000000000000000, 0.9510565162951535312, 1.000000000000000000, 0.9510565162951535312, 1.000000000000000000, 0.9510565162951535312, 1.000000000000000000, 0.9510565162951535312, 1.000000000000000000, 0.9510565162951535312, 1.000000000000000000, 0.9510565162951535312, 1.000000000000000000, 0.9510565162951535312, 1.000000000000000000, 0.9510565162951535312, 1.000000000000000000, 0.9510565162951535312, 1.000000000000000000, 0.9510565162951535312, 1.000000000000000000, 0.9510565162951535312, 1.000000000000000000, 0.9510565162951535312, 1.000000000000000000, 0.9510565162951535312, 1.000000000000000000, 0.9510565162951535312, 1.000000000000000000, 0.9510565162951535312, 1.000000000000000000, 0.9510565162951535312, 1.000000000000000000, 0.9510565162951535312, 1.000000000000000000, 0.9510565162951535312, 1.000000000000000000, 0.9510565162951535312, 1.000000000000000000, 0.9510565162951535312, 1.000000000000000000, 0.9510565162951535312, 1.000000000000000000, 0.9510565162951535312, 1.000000000000000000, 0.9510565162951535312, 1.000000000000000000, 0.9510565162951535312, 1.000000000000000000, 0.9510565162951535312, 1.000000000000000000, 0.9510565162951535312, 1.000000000000000000, 0.9510565162951535312, 1.000000000000000000, 0.9510565162951535312, 1.000000000000000000, 0.9510565162951535312, 1.000000000000000000, 0.9510565162951535312, 1.000000000000000000, 0.9510565162951535312, 1.000000000000000000, 0.9510565162951535312, 1.000000000000000000, 0.9510565162951535312, 1.000000000000000000, 0.9510565162951535312, 1.000000000000000000, 0.9510565162951535312, 1.000000000000000000, 0.9510565162951535312, 1.000000000000000000, 0.9510565162951535312, 1.000000000000000000, 0.9510565162951535312, 1.000000000000000000, 0.9510565162951535312, 1.000000000000000000, 0.9510565162951535312, 1.000000000000000000, 0.9510565162951535312, 1.000000000000000000, 0.9510565162951535312, 1.000000000000000000, 0.9510565162951535312, 1.000000000000000000, 0.9510565162951535312, 1.000000000000000000, 0.9510565162951535312, 1.000000000000000000, 0.9510565162951535312, 1.000000000000000000, 0.9510565162951535312, 1.000000000000000000, 0.9510565162951535312, 1.000000000000000000, 0.9510565162951535312, 1.000000000000000000, 0.9510565162951535312, 1.000000000000000000, 0.9510565162951535312, 1.000000000000000000, 0.9510565162951535312, 1.000000000000000000, 0.9510565162951535312, 1.000000000000000000, 0.9510565162951535312, 1.000000000000000000, 0.9510565162951535312, 1.000000000000000000, 0.9510565162951535312, 1.000000000000000000, 0.9510565162951535312, 1.000000000000000000, 0.9510565162951535312, 1.000000000000000000, 0.9510565162951535312, 1.000000000000000000, 0.9510565162951535312, 1.000000000000000000, 0.9510565162951535312, 1.000000000000000000, 0.9510565162951535312, 1.000000000000000000, 0.9510565162951535312, 1.000000000000000000, 0.9510565162951535312, 1.000000000000000000, 0.9510565162951535312, 1.000000000000000000, 0.9510565162951535312, 1.000000000000000000, 0.9510565162951535312, 1.000000000000000000, 0.9510565162951535312, 1.000000000000000000, 0.9510565162951535312, 1.000000000000000000, 0.9510565162951535312, 1.000000000000000000, 0.9510565162951535312, 1.000000000000000000, 0.9510565162951535312, 1.000000000000000000, 0.9510565162951535312, 1.000000000000000000, 0.9510565162951535312, 1.000000000000000000, 0.9510565162951535312, 1.000000000000000000, 0.9510565162951535312, 1.000000000000000000, 0.9510565162951535312, 1.000000000000000000, 0.9510565162951535312, 1.000000000000000000, 0.9510565162951535312, 1.000000000000000000, 0.9510565162951535312, 1.000000000000000000, 0.9510565162951535312, 1.000000000000000000, 0.9510565162951535312, 1.000000000000000000, 0.9510565162951535312, 1.000000000000000000, 0.9510565162951535312, 1.000000000000000000, 0.9510565162951535312, 1.000000000000000000, 0.9510565162951535312, 1.000000000000000000, 0.9510565162951535312, 1.000000000000000000, 0.9510565162951535312, 1.000000000000000000, 0.9510565162951535312, 1.000000000000000000) ) ) 
 REPRESENTATION_ITEM ( '' )  SURFACE ( )  );
#17956=SURFACE_SIDE_STYLE ('',( #34127 ) ) ;
#17960=CARTESIAN_POINT ( 'NONE',  ( 34.99999999999999289, 99.99999999999997158, 3.500000000000000000 ) ) ;
#17963=ORIENTED_EDGE ( 'NONE', *, *, #2041, .T. ) ;
#17966=ORIENTED_EDGE ( 'NONE', *, *, #7716, .F. ) ;
#17970=CIRCLE ( 'NONE', #57279, 5.500000000000005329 ) ;
#17971=CARTESIAN_POINT ( 'NONE',  ( -45.00000000000000000, 10.49999999999998224, -3.000000000000000444 ) ) ;
#17972=CARTESIAN_POINT ( 'NONE',  ( -3.094860106618432471, 133.5949999999999989, -9.525000000000000355 ) ) ;
#17974=ORIENTED_EDGE ( 'NONE', *, *, #28739, .F. ) ;
#17976=CARTESIAN_POINT ( 'NONE',  ( 8.102448949553181734, 140.1049999999999898, -5.886773742842746238 ) ) ;
#17979=CARTESIAN_POINT ( 'NONE',  ( 41.27272961514506022, 107.3325180337009073, -3.464233254637873571 ) ) ;
#17980=ORIENTED_EDGE ( 'NONE', *, *, #22088, .T. ) ;
#17981=CARTESIAN_POINT ( 'NONE',  ( -8.102448949553181734, 156.0050000000000239, -5.886773742842749790 ) ) ;
#17982=DIRECTION ( 'NONE',  ( 0.000000000000000000, 0.000000000000000000, -1.000000000000000000 ) ) ;
#17983=UNCERTAINTY_MEASURE_WITH_UNIT (LENGTH_MEASURE( 1.000000000000000082E-05 ), #57353, 'distance_accuracy_value', 'NONE');
#17988=COLOUR_RGB ( '', 0.72549020, 0.75294118, 0.79215686) ;
#17992=UNCERTAINTY_MEASURE_WITH_UNIT (LENGTH_MEASURE( 1.000000000000000082E-05 ), #45566, 'distance_accuracy_value', 'NONE');
#17993=CONICAL_SURFACE ( 'NONE', #35975, 5.499999999999976907, 0.7853981633974309595 ) ;
#17994=SURFACE_STYLE_FILL_AREA ( #66168 ) ;
#17996=MECHANICAL_DESIGN_GEOMETRIC_PRESENTATION_REPRESENTATION('',(#1090),#32582);
#17997=ORIENTED_EDGE ( 'NONE', *, *, #4330, .T. ) ;
#17998=DIRECTION ( 'NONE',  ( 1.000000000000000000, 0.000000000000000000, -0.000000000000000000 ) ) ;
#18002=SURFACE_STYLE_USAGE ( .BOTH. , #18365 ) ;
#18005=LINE ( 'NONE', #60901, #57822 ) ;
#18009=ORIENTED_EDGE ( 'NONE', *, *, #45689, .T. ) ;
#18012=CARTESIAN_POINT ( 'NONE',  ( -10.01517768586949231, 140.1949999999999932, -6.132527647946036459E-16 ) ) ;
#18015=CARTESIAN_POINT ( 'NONE',  ( 15.98999599679679839, 117.4999999999999716, 9.500000000000000000 ) ) ;
#18016=COLOUR_RGB ( '', 0.08235294, 0.09019608, 0.10196078) ;
#18018=DIRECTION ( 'NONE',  ( -1.000000000000000000, 0.000000000000000000, 6.938893903907221278E-15 ) ) ;
#18019=EDGE_CURVE ( 'NONE', #63831, #6631, #32964, .T. ) ;
#18036=EDGE_CURVE ( 'NONE', #54975, #6724, #2337, .T. ) ;
#18037=CARTESIAN_POINT ( 'NONE',  ( 71.50000000000000000, 35.92875272052971525, 9.500000000000000000 ) ) ;
#18038=DIRECTION ( 'NONE',  ( 0.6363636363636357984, 0.000000000000000000, -0.7713892158398705234 ) ) ;
#18039=SURFACE_STYLE_USAGE ( .BOTH. , #39883 ) ;
#18044=ORIENTED_EDGE ( 'NONE', *, *, #68395, .F. ) ;
#18046=DIRECTION ( 'NONE',  ( 1.000000000000000000, 0.000000000000000000, 0.000000000000000000 ) ) ;
#18047=CARTESIAN_POINT ( 'NONE',  ( 0.000000000000000000, 110.4999999999999858, 0.000000000000000000 ) ) ;
#18049=FILL_AREA_STYLE ('',( #60267 ) ) ;
#18050=CARTESIAN_POINT ( 'NONE',  ( -7.632228543268608334, 154.9570736234661581, 2.479861379858952830 ) ) ;
#18054=CARTESIAN_POINT ( 'NONE',  ( -71.74137931034481142, 36.89918356738973415, 9.500000000000000000 ) ) ;
#18057=SURFACE_STYLE_FILL_AREA ( #45852 ) ;
#18058=CARTESIAN_POINT ( 'NONE',  ( 5.598654528085805993, 127.3549999999999898, 7.705886871421374629 ) ) ;
#18059=UNCERTAINTY_MEASURE_WITH_UNIT (LENGTH_MEASURE( 1.000000000000000082E-05 ), #40868, 'distance_accuracy_value', 'NONE');
#18060=CARTESIAN_POINT ( 'NONE',  ( -71.49999999999998579, 119.9999999999997868, -7.500000000000000000 ) ) ;
#18063=CARTESIAN_POINT ( 'NONE',  ( 48.81081081081080697, 14.09971791521132900, -9.500000000000000000 ) ) ;
#18065=( NAMED_UNIT ( * ) PLANE_ANGLE_UNIT ( ) SI_UNIT ( $, .RADIAN. ) );
#18074=CARTESIAN_POINT ( 'NONE',  ( -45.86631659065714928, 9.243037840626161739, -6.242508038240250912 ) ) ;
#18076=VERTEX_POINT ( 'NONE', #853 ) ;
#18080=ORIENTED_EDGE ( 'NONE', *, *, #32634, .T. ) ;
#18081=CARTESIAN_POINT ( 'NONE',  ( -75.00000000000000000, 9.482577857128569931, 6.485016072424482303 ) ) ;
#18086=CARTESIAN_POINT ( 'NONE',  ( -12.34222745343792127, 149.9999999999999716, 10.18181818181818166 ) ) ;
#18087=CARTESIAN_POINT ( 'NONE',  ( -12.72792206135785698, 114.9999999999999574, -10.50000000000000000 ) ) ;
#18089=DIRECTION ( 'NONE',  ( 0.000000000000000000, 0.000000000000000000, 1.000000000000000000 ) ) ;
#18091=CARTESIAN_POINT ( 'NONE',  ( -9.058813317711338797, 143.3449999999999989, 2.943386871421373563 ) ) ;
#18097=FILL_AREA_STYLE ('',( #46251 ) ) ;
#18105=DIRECTION ( 'NONE',  ( 0.000000000000000000, 0.000000000000000000, -1.000000000000000000 ) ) ;
#18108=SURFACE_STYLE_FILL_AREA ( #1867 ) ;
#18109=EDGE_CURVE ( 'NONE', #49901, #37663, #29313, .T. ) ;
#18110=CARTESIAN_POINT ( 'NONE',  ( 68.50000000000000000, 1.797044900979284448E-15, 10.00000000000000000 ) ) ;
#18117=SURFACE_STYLE_USAGE ( .BOTH. , #22703 ) ;
#18119=CARTESIAN_POINT ( 'NONE',  ( 72.49999999999998579, 119.9999999999997868, -10.00000000000000000 ) ) ;
#18124=DIRECTION ( 'NONE',  ( 0.000000000000000000, 0.000000000000000000, 1.000000000000000000 ) ) ;
#18128=SURFACE_STYLE_USAGE ( .BOTH. , #39964 ) ;
#18132=ORIENTED_EDGE ( 'NONE', *, *, #55288, .F. ) ;
#18134=SURFACE_STYLE_FILL_AREA ( #61025 ) ;
#18136=ORIENTED_EDGE ( 'NONE', *, *, #495, .T. ) ;
#18137=FILL_AREA_STYLE_COLOUR ( '', #40981 ) ;
#18138=CARTESIAN_POINT ( 'NONE',  ( 2.607480562269071989, 122.7070736234661439, 8.025000000000002132 ) ) ;
#18140=PRESENTATION_STYLE_ASSIGNMENT (( #7576 ) ) ;
#18142=DIRECTION ( 'NONE',  ( -1.000000000000000000, 0.000000000000000000, 0.000000000000000000 ) ) ;
#18143=EDGE_LOOP ( 'NONE', ( #62337, #26028, #6206, #22856 ) ) ;
#18145=DIRECTION ( 'NONE',  ( 0.000000000000000000, 0.000000000000000000, 1.000000000000000000 ) ) ;
#18147=CYLINDRICAL_SURFACE ( 'NONE', #55517, 26.99999999999999645 ) ;
#18151=ORIENTED_EDGE ( 'NONE', *, *, #25892, .T. ) ;
#18153=LINE ( 'NONE', #65297, #52473 ) ;
#18156=CIRCLE ( 'NONE', #48527, 0.5000000000000004441 ) ;
#18157=DIRECTION ( 'NONE',  ( 0.6363636363636357984, 0.000000000000000000, -0.7713892158398705234 ) ) ;
#18160=DIRECTION ( 'NONE',  ( -0.000000000000000000, -0.000000000000000000, -1.000000000000000000 ) ) ;
#18164=CARTESIAN_POINT ( 'NONE',  ( 24.21231517720798010, 112.9999999999999858, -7.000000000000000000 ) ) ;
#18166=CIRCLE ( 'NONE', #33866, 0.5000000000000004441 ) ;
#18168=ORIENTED_EDGE ( 'NONE', *, *, #66895, .T. ) ;
#18169=( GEOMETRIC_REPRESENTATION_CONTEXT ( 3 ) GLOBAL_UNCERTAINTY_ASSIGNED_CONTEXT ( ( #34888 ) ) GLOBAL_UNIT_ASSIGNED_CONTEXT ( ( #21575, #31081, #63102 ) ) REPRESENTATION_CONTEXT ( 'NONE', 'WORKASPACE' ) );
#18171=( LENGTH_UNIT ( ) NAMED_UNIT ( * ) SI_UNIT ( .MILLI., .METRE. ) );
#18173=DIRECTION ( 'NONE',  ( 0.000000000000000000, 0.000000000000000000, 1.000000000000000000 ) ) ;
#18181=ORIENTED_EDGE ( 'NONE', *, *, #2008, .F. ) ;
#18183=CARTESIAN_POINT ( 'NONE',  ( 45.50000000000000000, 10.69371294336137801, 10.00000000000000000 ) ) ;
#18184=DIRECTION ( 'NONE',  ( 0.000000000000000000, 0.000000000000000000, 1.000000000000000000 ) ) ;
#18191=CARTESIAN_POINT ( 'NONE',  ( 5.598654528085805993, 142.3549999999999898, 7.705886871421374629 ) ) ;
#18193=AXIS2_PLACEMENT_3D ( 'NONE', #23560, #49982, #29888 ) ;
#18196=( LENGTH_UNIT ( ) NAMED_UNIT ( * ) SI_UNIT ( .MILLI., .METRE. ) );
#18197=( LENGTH_UNIT ( ) NAMED_UNIT ( * ) SI_UNIT ( .MILLI., .METRE. ) );
#18198=CIRCLE ( 'NONE', #29382, 0.5000000000000004441 ) ;
#18201=VECTOR ( 'NONE', #3023, 1000.000000000000000 ) ;
#18202=EDGE_CURVE ( 'NONE', #9347, #47468, #40649, .T. ) ;
#18203=DIRECTION ( 'NONE',  ( 0.000000000000000000, 1.000000000000000000, -0.000000000000000000 ) ) ;
#18204=MECHANICAL_DESIGN_GEOMETRIC_PRESENTATION_REPRESENTATION('',(#9241),#53020);
#18211=AXIS2_PLACEMENT_3D ( 'NONE', #32860, #27554, #49075 ) ;
#18213=PLANE ( 'NONE',  #22539 ) ;
#18215=DIRECTION ( 'NONE',  ( 0.000000000000000000, 0.000000000000000000, 1.000000000000000000 ) ) ;
#18219=SURFACE_STYLE_USAGE ( .BOTH. , #12227 ) ;
#18220=CARTESIAN_POINT ( 'NONE',  ( -74.99999999999998579, 113.4999999999999858, 7.500000000000000000 ) ) ;
#18224=CARTESIAN_POINT ( 'NONE',  ( 72.49999999999998579, 119.9999999999997868, 9.500000000000000000 ) ) ;
#18225=ORIENTED_EDGE ( 'NONE', *, *, #62709, .F. ) ;
#18226=( GEOMETRIC_REPRESENTATION_CONTEXT ( 3 ) GLOBAL_UNCERTAINTY_ASSIGNED_CONTEXT ( ( #68663 ) ) GLOBAL_UNIT_ASSIGNED_CONTEXT ( ( #12972, #7689, #29499 ) ) REPRESENTATION_CONTEXT ( 'NONE', 'WORKASPACE' ) );
#18234=FILL_AREA_STYLE ('',( #12241 ) ) ;
#18236=CARTESIAN_POINT ( 'NONE',  ( -9.827790563157511022E-16, 142.4429263765338192, 8.025000000000000355 ) ) ;
#18239=FILL_AREA_STYLE_COLOUR ( '', #2479 ) ;
#18240=CARTESIAN_POINT ( 'NONE',  ( -6.826472737025120807, 114.3929263765337936, -4.959722759717907437 ) ) ;
#18243=ORIENTED_EDGE ( 'NONE', *, *, #31429, .F. ) ;
#18244=CARTESIAN_POINT ( 'NONE',  ( -34.99999999999999289, 99.99999999999998579, -9.500000000000000000 ) ) ;
#18249=PRESENTATION_STYLE_ASSIGNMENT (( #55878 ) ) ;
#18250=CARTESIAN_POINT ( 'NONE',  ( -45.00000000000000000, 9.708372675170618749, -6.000000000000000000 ) ) ;
#18258=ORIENTED_EDGE ( 'NONE', *, *, #10660, .F. ) ;
#18262=ORIENTED_EDGE ( 'NONE', *, *, #11228, .T. ) ;
#18269=AXIS2_PLACEMENT_3D ( 'NONE', #698, #65122, #59860 ) ;
#18271=ORIENTED_EDGE ( 'NONE', *, *, #48419, .T. ) ;
#18273=CIRCLE ( 'NONE', #1389, 26.99999999999999645 ) ;
#18274=CARTESIAN_POINT ( 'NONE',  ( -45.91547277936962956, 9.430195807687216103, -6.000000000000000000 ) ) ;
#18279=CARTESIAN_POINT ( 'NONE',  ( 1.754102292061050283, 154.4999999999999716, -9.372469107644919362 ) ) ;
#18283=CIRCLE ( 'NONE', #7082, 0.5000000000000004441 ) ;
#18287=CARTESIAN_POINT ( 'NONE',  ( 5.598654528085805993, 121.3549999999999898, 7.705886871421374629 ) ) ;
#18290=DIRECTION ( 'NONE',  ( -0.000000000000000000, 1.000000000000000000, -0.000000000000000000 ) ) ;
#18291=CARTESIAN_POINT ( 'NONE',  ( -6.826472737025120807, 141.9929263765338305, 4.959722759717906548 ) ) ;
#18294=VECTOR ( 'NONE', #32108, 1000.000000000000000 ) ;
#18303=COLOUR_RGB ( '', 0.31764706, 0.68627451, 0.89019608) ;
#18304=DIRECTION ( 'NONE',  ( -0.000000000000000000, -1.000000000000000000, 0.000000000000000000 ) ) ;
#18305=CARTESIAN_POINT ( 'NONE',  ( -44.99999999999977973, 146.9999999999999716, 9.500000000000000000 ) ) ;
#18306=SURFACE_SIDE_STYLE ('',( #60843 ) ) ;
#18310=VECTOR ( 'NONE', #62061, 1000.000000000000000 ) ;
#18311=FACE_OUTER_BOUND ( 'NONE', #10570, .T. ) ;
#18312=CIRCLE ( 'NONE', #60963, 5.499999999999976907 ) ;
#18313=DIRECTION ( 'NONE',  ( -0.000000000000000000, -0.000000000000000000, -1.000000000000000000 ) ) ;
#18319=ORIENTED_EDGE ( 'NONE', *, *, #13330, .T. ) ;
#18320=ORIENTED_EDGE ( 'NONE', *, *, #47663, .F. ) ;
#18324=VERTEX_POINT ( 'NONE', #63066 ) ;
#18328=CARTESIAN_POINT ( 'NONE',  ( 5.598654528085805993, 141.2449999999999761, 7.705886871421374629 ) ) ;
#18333=DIRECTION ( 'NONE',  ( 1.156482317317873451E-16, 1.000000000000000000, -0.000000000000000000 ) ) ;
#18334=CARTESIAN_POINT ( 'NONE',  ( -9.058813317711338797, 144.4550000000000125, 2.943386871421373563 ) ) ;
#18338=CARTESIAN_POINT ( 'NONE',  ( 0.000000000000000000, 110.9429263765338192, -8.025000000000000355 ) ) ;
#18342=STYLED_ITEM ( 'NONE', ( #50655 ), #29531 ) ;
#18343=DIRECTION ( 'NONE',  ( 1.000000000000000000, 0.000000000000000000, 0.000000000000000000 ) ) ;
#18344=DIRECTION ( 'NONE',  ( -0.000000000000000000, 0.000000000000000000, 1.000000000000000000 ) ) ;
#18345=ORIENTED_EDGE ( 'NONE', *, *, #6557, .T. ) ;
#18349=FACE_OUTER_BOUND ( 'NONE', #26850, .T. ) ;
#18352=ORIENTED_EDGE ( 'NONE', *, *, #24389, .F. ) ;
#18355=CARTESIAN_POINT ( 'NONE',  ( 0.000000000000000000, 114.4999999999999574, 0.000000000000000000 ) ) ;
#18357=PRESENTATION_STYLE_ASSIGNMENT (( #61930 ) ) ;
#18359=ORIENTED_EDGE ( 'NONE', *, *, #50683, .T. ) ;
#18360=VERTEX_POINT ( 'NONE', #16980 ) ;
#18365=SURFACE_SIDE_STYLE ('',( #19018 ) ) ;
#18366=CIRCLE ( 'NONE', #57668, 0.5000000000000004441 ) ;
#18367=MECHANICAL_DESIGN_GEOMETRIC_PRESENTATION_REPRESENTATION('',(#52065),#15014);
#18368=MECHANICAL_DESIGN_GEOMETRIC_PRESENTATION_REPRESENTATION('',(#42003),#69418);
#18369=ADVANCED_FACE ( 'NONE', ( #17681 ), #44093, .T. ) ;
#18374=SURFACE_SIDE_STYLE ('',( #45135 ) ) ;
#18375=CARTESIAN_POINT ( 'NONE',  ( -23.21231517720797655, 117.4999999999999716, -9.500000000000000000 ) ) ;
#18376=AXIS2_PLACEMENT_3D ( 'NONE', #69096, #58184, #42404 ) ;
#18377=CARTESIAN_POINT ( 'NONE',  ( -5.598654528085806881, 142.7449999999999761, -7.705886871421374629 ) ) ;
#18380=COLOUR_RGB ( '', 0.09019608, 0.27058824, 0.51372549) ;
#18384=ADVANCED_FACE ( 'NONE', ( #11679 ), #62923, .T. ) ;
#18388=AXIS2_PLACEMENT_3D ( 'NONE', #64313, #16513, #27348 ) ;
#18390=PRESENTATION_STYLE_ASSIGNMENT (( #28904 ) ) ;
#18392=CARTESIAN_POINT ( 'NONE',  ( -6.826472737025120807, 128.1070736234661638, 4.959722759717906548 ) ) ;
#18394=AXIS2_PLACEMENT_3D ( 'NONE', #23880, #49950, #17919 ) ;
#18400=ORIENTED_EDGE ( 'NONE', *, *, #30301, .F. ) ;
#18405=CARTESIAN_POINT ( 'NONE',  ( -74.99999999999998579, 50.00000000000000000, -9.500000000000000000 ) ) ;
#18406=CARTESIAN_POINT ( 'NONE',  ( 9.058813317711337021, 111.5449999999999875, 2.943386871421375783 ) ) ;
#18407=EDGE_CURVE ( 'NONE', #38702, #28358, #11445, .T. ) ;
#18408=STYLED_ITEM ( 'NONE', ( #30250 ), #47148 ) ;
#18411=CARTESIAN_POINT ( 'NONE',  ( 8.102448949553181734, 116.1049999999999756, -5.886773742842746238 ) ) ;
#18414=CARTESIAN_POINT ( 'NONE',  ( 9.058813317711337021, 124.6549999999999869, 2.943386871421375783 ) ) ;
#18415=CARTESIAN_POINT ( 'NONE',  ( 20.30121256018846765, 114.9093931177592509, 10.36597400192487939 ) ) ;
#18416=VECTOR ( 'NONE', #68662, 1000.000000000000000 ) ;
#18418=FILL_AREA_STYLE_COLOUR ( '', #51482 ) ;
#18422=CARTESIAN_POINT ( 'NONE',  ( 74.50000000000000000, 19.30628705663858113, -6.500000000000000000 ) ) ;
#18430=EDGE_LOOP ( 'NONE', ( #23006, #62549, #44403, #57093 ) ) ;
#18433=DIRECTION ( 'NONE',  ( 0.000000000000000000, 1.000000000000000000, 0.000000000000000000 ) ) ;
#18434=ORIENTED_EDGE ( 'NONE', *, *, #23598, .F. ) ;
#18437=CARTESIAN_POINT ( 'NONE',  ( -74.10613849977178802, 9.348154474468920228, 6.165151716360274925 ) ) ;
#18439=ORIENTED_EDGE ( 'NONE', *, *, #57041, .T. ) ;
#18441=DIRECTION ( 'NONE',  ( -0.000000000000000000, -0.000000000000000000, -1.000000000000000000 ) ) ;
#18444=FILL_AREA_STYLE_COLOUR ( '', #41865 ) ;
#18445=CARTESIAN_POINT ( 'NONE',  ( 5.598654528085805993, 144.2449999999999761, 7.705886871421374629 ) ) ;
#18447=AXIS2_PLACEMENT_3D ( 'NONE', #26217, #10064, #31488 ) ;
#18448=AXIS2_PLACEMENT_3D ( 'NONE', #40594, #35300, #41295 ) ;
#18453=CIRCLE ( 'NONE', #63338, 8.499999999999992895 ) ;
#18457=CARTESIAN_POINT ( 'NONE',  ( -9.058813317711337021, 113.0449999999999875, -2.943386871421374895 ) ) ;
#18463=ORIENTED_EDGE ( 'NONE', *, *, #48019, .T. ) ;
#18470=( NAMED_UNIT ( * ) SI_UNIT ( $, .STERADIAN. ) SOLID_ANGLE_UNIT ( ) );
#18471=CARTESIAN_POINT ( 'NONE',  ( 60.00000000000000000, 1.797044900979284448E-15, 11.50000000000000000 ) ) ;
#18472=VECTOR ( 'NONE', #1138, 1000.000000000000000 ) ;
#18481=DIRECTION ( 'NONE',  ( -1.000000000000000000, 0.000000000000000000, 0.000000000000000000 ) ) ;
#18482=( NAMED_UNIT ( * ) SI_UNIT ( $, .STERADIAN. ) SOLID_ANGLE_UNIT ( ) );
#18486=DIRECTION ( 'NONE',  ( 1.000000000000000000, 0.000000000000000000, -0.000000000000000000 ) ) ;
#18487=DIRECTION ( 'NONE',  ( 8.659560562354722084E-17, -0.7071067811865647812, 0.7071067811865302533 ) ) ;
#18488=ORIENTED_EDGE ( 'NONE', *, *, #43516, .F. ) ;
#18490=CARTESIAN_POINT ( 'NONE',  ( 4.716976649647096842, 125.8570736234661496, 6.492361379858953896 ) ) ;
#18492=TOROIDAL_SURFACE ( 'NONE', #53297, 12.50000000000000000, 0.5000000000000000000 ) ;
#18495=CARTESIAN_POINT ( 'NONE',  ( 15.98999599679679839, 146.4999999999999716, -9.500000000000000000 ) ) ;
#18500=FILL_AREA_STYLE_COLOUR ( '', #3634 ) ;
#18501=( GEOMETRIC_REPRESENTATION_CONTEXT ( 3 ) GLOBAL_UNCERTAINTY_ASSIGNED_CONTEXT ( ( #5801 ) ) GLOBAL_UNIT_ASSIGNED_CONTEXT ( ( #32473, #54286, #60585 ) ) REPRESENTATION_CONTEXT ( 'NONE', 'WORKASPACE' ) );
#18509=MECHANICAL_DESIGN_GEOMETRIC_PRESENTATION_REPRESENTATION('',(#30837),#9551);
#18512=VERTEX_POINT ( 'NONE', #19730 ) ;
#18514=SURFACE_STYLE_USAGE ( .BOTH. , #67383 ) ;
#18517=( LENGTH_UNIT ( ) NAMED_UNIT ( * ) SI_UNIT ( .MILLI., .METRE. ) );
#18518=CYLINDRICAL_SURFACE ( 'NONE', #45741, 0.5000000000000004441 ) ;
#18522=CARTESIAN_POINT ( 'NONE',  ( 9.058813317711338797, 114.8449999999999847, -2.943386871421372675 ) ) ;
#18530=CARTESIAN_POINT ( 'NONE',  ( -34.99999999999999289, 99.99999999999998579, -9.500000000000000000 ) ) ;
#18534=ORIENTED_EDGE ( 'NONE', *, *, #53199, .F. ) ;
#18549=VECTOR ( 'NONE', #45043, 1000.000000000000000 ) ;
#18551=CARTESIAN_POINT ( 'NONE',  ( -3.094860106618432471, 146.7049999999999841, -9.525000000000000355 ) ) ;
#18557=EDGE_CURVE ( 'NONE', #47468, #58906, #19318, .T. ) ;
#18558=UNCERTAINTY_MEASURE_WITH_UNIT (LENGTH_MEASURE( 1.000000000000000082E-05 ), #33255, 'distance_accuracy_value', 'NONE');
#18560=CARTESIAN_POINT ( 'NONE',  ( -19.89974874213239886, 114.9999999999999574, -10.50000000000000000 ) ) ;
#18561=SURFACE_STYLE_USAGE ( .BOTH. , #17542 ) ;
#18562=DIRECTION ( 'NONE',  ( -3.552713678800500929E-15, 0.000000000000000000, 1.000000000000000000 ) ) ;
#18566=ORIENTED_EDGE ( 'NONE', *, *, #31777, .F. ) ;
#18568=VECTOR ( 'NONE', #59646, 1000.000000000000000 ) ;
#18576=DIRECTION ( 'NONE',  ( -1.000000000000000000, 0.000000000000000000, 0.000000000000000000 ) ) ;
#18580=EDGE_LOOP ( 'NONE', ( #68713, #150, #67267, #64712 ) ) ;
#18581=EDGE_CURVE ( 'NONE', #62518, #64181, #58644, .T. ) ;
#18584=COLOUR_RGB ( '', 0.31764706, 0.68627451, 0.89019608) ;
#18586=AXIS2_PLACEMENT_3D ( 'NONE', #12534, #50543, #2265 ) ;
#18587=CARTESIAN_POINT ( 'NONE',  ( -74.09989551642895833, 9.371898184802235576, -6.142471281331790323 ) ) ;
#18591=SURFACE_STYLE_FILL_AREA ( #18234 ) ;
#18593=CARTESIAN_POINT ( 'NONE',  ( -7.632228543268607446, 144.5429263765338135, -2.479861379858953718 ) ) ;
#18599=ORIENTED_EDGE ( 'NONE', *, *, #64407, .T. ) ;
#18603=CIRCLE ( 'NONE', #57928, 0.5000000000000004441 ) ;
#18605=SURFACE_STYLE_FILL_AREA ( #13652 ) ;
#18606=FACE_OUTER_BOUND ( 'NONE', #44775, .T. ) ;
#18607=AXIS2_PLACEMENT_3D ( 'NONE', #11504, #59685, #1235 ) ;
#18609=DIRECTION ( 'NONE',  ( 0.000000000000000000, 0.000000000000000000, 1.000000000000000000 ) ) ;
#18615=ORIENTED_EDGE ( 'NONE', *, *, #5086, .T. ) ;
#18617=( NAMED_UNIT ( * ) PLANE_ANGLE_UNIT ( ) SI_UNIT ( $, .RADIAN. ) );
#18621=AXIS2_PLACEMENT_3D ( 'NONE', #59057, #27014, #48550 ) ;
#18624=DIRECTION ( 'NONE',  ( -0.000000000000000000, 1.000000000000000000, -0.000000000000000000 ) ) ;
#18627=CYLINDRICAL_SURFACE ( 'NONE', #45507, 13.99999999999999822 ) ;
#18629=ORIENTED_EDGE ( 'NONE', *, *, #37126, .F. ) ;
#18631=CIRCLE ( 'NONE', #57946, 5.500000000000005329 ) ;
#18634=CARTESIAN_POINT ( 'NONE',  ( -74.99999999999998579, 50.00000000000000000, 11.50000000000003730 ) ) ;
#18635=FILL_AREA_STYLE_COLOUR ( '', #16907 ) ;
#18637=CARTESIAN_POINT ( 'NONE',  ( -8.102448949553181734, 114.0049999999999812, -5.886773742842749790 ) ) ;
#18641=UNCERTAINTY_MEASURE_WITH_UNIT (LENGTH_MEASURE( 1.000000000000000082E-05 ), #2813, 'distance_accuracy_value', 'NONE');
#18642=FILL_AREA_STYLE ('',( #19995 ) ) ;
#18644=EDGE_LOOP ( 'NONE', ( #39989, #53640, #12264, #33143 ) ) ;
#18649=CARTESIAN_POINT ( 'NONE',  ( 15.98999599679679839, 146.9999999999999716, -9.500000000000000000 ) ) ;
#18652=ORIENTED_EDGE ( 'NONE', *, *, #42966, .T. ) ;
#18654=CIRCLE ( 'NONE', #15323, 0.5000000000000004441 ) ;
#18659=SURFACE_STYLE_USAGE ( .BOTH. , #750 ) ;
#18662=ORIENTED_EDGE ( 'NONE', *, *, #4119, .F. ) ;
#18667=ORIENTED_EDGE ( 'NONE', *, *, #41571, .F. ) ;
#18669=MECHANICAL_DESIGN_GEOMETRIC_PRESENTATION_REPRESENTATION('',(#44522),#53469);
#18671=CARTESIAN_POINT ( 'NONE',  ( 9.058813317711337021, 144.5449999999999875, 2.943386871421375783 ) ) ;
#18675=CARTESIAN_POINT ( 'NONE',  ( -3.094860106618434248, 138.9049999999999727, 9.525000000000000355 ) ) ;
#18677=CARTESIAN_POINT ( 'NONE',  ( 41.84210526315787604, 107.2928455055531600, -3.500000000000000888 ) ) ;
#18679=CARTESIAN_POINT ( 'NONE',  ( -6.826472737025120807, 117.9929263765338021, 4.959722759717906548 ) ) ;
#18681=CARTESIAN_POINT ( 'NONE',  ( -60.00000000000000000, -2.024042244987997205E-14, 11.50000000000000000 ) ) ;
#18684=ORIENTED_EDGE ( 'NONE', *, *, #42869, .F. ) ;
#18686=CARTESIAN_POINT ( 'NONE',  ( 41.40606286463611241, 107.1009606408074006, 3.493716402184701586 ) ) ;
#18687=ORIENTED_EDGE ( 'NONE', *, *, #61385, .T. ) ;
#18689=CARTESIAN_POINT ( 'NONE',  ( 20.40110905463057023, 114.8435661791816358, 10.33328836125512851 ) ) ;
#18692=EDGE_CURVE ( 'NONE', #41694, #62679, #43651, .T. ) ;
#18693=ORIENTED_EDGE ( 'NONE', *, *, #21567, .F. ) ;
#18694=UNCERTAINTY_MEASURE_WITH_UNIT (LENGTH_MEASURE( 1.000000000000000082E-05 ), #60906, 'distance_accuracy_value', 'NONE');
#18695=EDGE_CURVE ( 'NONE', #1012, #33055, #59412, .T. ) ;
#18696=CARTESIAN_POINT ( 'NONE',  ( 45.00000000000000000, 9.999999999999992895, -5.999999999999999112 ) ) ;
#18697=( LENGTH_UNIT ( ) NAMED_UNIT ( * ) SI_UNIT ( .MILLI., .METRE. ) );
#18699=ORIENTED_EDGE ( 'NONE', *, *, #40697, .T. ) ;
#18706=CIRCLE ( 'NONE', #1807, 0.5000000000000004441 ) ;
#18707=DIRECTION ( 'NONE',  ( 0.000000000000000000, 0.000000000000000000, 1.000000000000000000 ) ) ;
#18708=DIRECTION ( 'NONE',  ( 0.000000000000000000, 0.000000000000000000, 1.000000000000000000 ) ) ;
#18713=CARTESIAN_POINT ( 'NONE',  ( -5.598654528085806881, 136.7449999999999761, -7.705886871421374629 ) ) ;
#18720=DIRECTION ( 'NONE',  ( -7.080503983578803083E-17, -1.000000000000000000, 0.000000000000000000 ) ) ;
#18724=ORIENTED_EDGE ( 'NONE', *, *, #44771, .T. ) ;
#18725=PLANE ( 'NONE',  #67528 ) ;
#18726=LINE ( 'NONE', #29266, #24769 ) ;
#18728=CARTESIAN_POINT ( 'NONE',  ( -7.632228543268608334, 142.9570736234661581, 2.479861379858952830 ) ) ;
#18733=ORIENTED_EDGE ( 'NONE', *, *, #66192, .F. ) ;
#18734=SURFACE_STYLE_FILL_AREA ( #52511 ) ;
#18737=AXIS2_PLACEMENT_3D ( 'NONE', #67731, #30073, #2954 ) ;
#18738=FACE_OUTER_BOUND ( 'NONE', #43448, .T. ) ;
#18739=DIRECTION ( 'NONE',  ( 1.000000000000000000, 0.000000000000000000, -0.000000000000000000 ) ) ;
#18740=CARTESIAN_POINT ( 'NONE',  ( 6.826472737025121695, 159.6070736234661069, -4.959722759717905660 ) ) ;
#18743=DIRECTION ( 'NONE',  ( -0.000000000000000000, -0.000000000000000000, 1.000000000000000000 ) ) ;
#18744=DIRECTION ( 'NONE',  ( 1.000000000000000000, 0.000000000000000000, 0.000000000000000000 ) ) ;
#18747=CARTESIAN_POINT ( 'NONE',  ( -3.094860106618434248, 138.9049999999999727, 9.525000000000000355 ) ) ;
#18750=FILL_AREA_STYLE ('',( #55694 ) ) ;
#18752=CARTESIAN_POINT ( 'NONE',  ( 20.68758241885016247, 114.6823486699484107, 10.00000000000000178 ) ) ;
#18755=ORIENTED_EDGE ( 'NONE', *, *, #35808, .F. ) ;
#18756=SURFACE_STYLE_FILL_AREA ( #25079 ) ;
#18758=ORIENTED_EDGE ( 'NONE', *, *, #40448, .F. ) ;
#18769=SURFACE_SIDE_STYLE ('',( #4289 ) ) ;
#18775=DIRECTION ( 'NONE',  ( 1.000000000000000000, 0.000000000000000000, 0.000000000000000000 ) ) ;
#18776=CARTESIAN_POINT ( 'NONE',  ( -3.094860106618432471, 139.5949999999999420, -9.525000000000000355 ) ) ;
#18778=( NAMED_UNIT ( * ) SI_UNIT ( $, .STERADIAN. ) SOLID_ANGLE_UNIT ( ) );
#18779=FACE_OUTER_BOUND ( 'NONE', #21484, .T. ) ;
#18780=FILL_AREA_STYLE_COLOUR ( '', #51581 ) ;
#18783=MECHANICAL_DESIGN_GEOMETRIC_PRESENTATION_REPRESENTATION('',(#8695),#68261);
#18785=LINE ( 'NONE', #19111, #52314 ) ;
#18791=CARTESIAN_POINT ( 'NONE',  ( -45.50000000000000000, 7.893193270153692431, -6.500000000000000000 ) ) ;
#18797=LINE ( 'NONE', #13513, #62404 ) ;
#18798=DIRECTION ( 'NONE',  ( 0.000000000000000000, -0.000000000000000000, 1.000000000000000000 ) ) ;
#18804=PLANE ( 'NONE',  #68719 ) ;
#18808=EDGE_CURVE ( 'NONE', #68902, #64181, #48933, .T. ) ;
#18809=EDGE_CURVE ( 'NONE', #20280, #25670, #16902, .T. ) ;
#18811=CARTESIAN_POINT ( 'NONE',  ( -75.46551724137930250, 63.49197145334878201, -9.500000000000000000 ) ) ;
#18812=( NAMED_UNIT ( * ) SI_UNIT ( $, .STERADIAN. ) SOLID_ANGLE_UNIT ( ) );
#18814=CARTESIAN_POINT ( 'NONE',  ( -7.632228543268607446, 133.6570736234661467, -2.479861379858953718 ) ) ;
#18815=CARTESIAN_POINT ( 'NONE',  ( 2.607480562269071989, 131.7070736234661865, 8.025000000000002132 ) ) ;
#18816=EDGE_CURVE ( 'NONE', #1577, #2723, #28080, .T. ) ;
#18818=COLOUR_RGB ( '', 0.40784314, 0.44705882, 0.49803922) ;
#18820=CARTESIAN_POINT ( 'NONE',  ( 74.54138597727603610, 19.45803563998442343, -6.486986334521338549 ) ) ;
#18825=DIRECTION ( 'NONE',  ( 0.000000000000000000, 0.000000000000000000, 1.000000000000000000 ) ) ;
#18826=ADVANCED_FACE ( 'NONE', ( #32347 ), #427, .T. ) ;
#18831=ADVANCED_FACE ( 'NONE', ( #29125 ), #2000, .F. ) ;
#18833=( NAMED_UNIT ( * ) SI_UNIT ( $, .STERADIAN. ) SOLID_ANGLE_UNIT ( ) );
#18834=SURFACE_STYLE_USAGE ( .BOTH. , #62088 ) ;
#18835=( NAMED_UNIT ( * ) SI_UNIT ( $, .STERADIAN. ) SOLID_ANGLE_UNIT ( ) );
#18836=EDGE_LOOP ( 'NONE', ( #32960, #41112, #10940, #47069 ) ) ;
#18837=DIRECTION ( 'NONE',  ( 1.000000000000000000, 0.000000000000000000, 0.000000000000000000 ) ) ;
#18840=CARTESIAN_POINT ( 'NONE',  ( -5.598654528085808657, 110.6449999999999960, 7.705886871421373741 ) ) ;
#18844=CARTESIAN_POINT ( 'NONE',  ( 4.716976649647099507, 122.6429263765338220, -6.492361379858953008 ) ) ;
#18845=DIRECTION ( 'NONE',  ( -0.000000000000000000, -1.000000000000000000, 0.000000000000000000 ) ) ;
#18852=( BOUNDED_CURVE ( )  B_SPLINE_CURVE ( 3, ( #68696, #31731, #20495, #63411 ),
 .UNSPECIFIED., .F., .F. ) 
 B_SPLINE_CURVE_WITH_KNOTS ( ( 4, 4 ),
 ( 1.570796326794891007, 3.141592653589793116 ),
 .UNSPECIFIED. ) 
 CURVE ( )  GEOMETRIC_REPRESENTATION_ITEM ( )  RATIONAL_B_SPLINE_CURVE ( ( 1.000000000000000000, 0.8047378541243637162, 0.8047378541243637162, 1.000000000000000000 ) ) 
 REPRESENTATION_ITEM ( '' )  );
#18863=CARTESIAN_POINT ( 'NONE',  ( -3.094860106618434248, 144.9050000000000011, 9.525000000000000355 ) ) ;
#18865=STYLED_ITEM ( 'NONE', ( #31155 ), #14060 ) ;
#18870=CARTESIAN_POINT ( 'NONE',  ( -3.569376287081467591, 110.7040900683961411, 8.618005638702442184 ) ) ;
#18871=( NAMED_UNIT ( * ) SI_UNIT ( $, .STERADIAN. ) SOLID_ANGLE_UNIT ( ) );
#18872=EDGE_CURVE ( 'NONE', #9835, #46789, #34432, .T. ) ;
#18875=DIRECTION ( 'NONE',  ( -0.000000000000000000, 1.000000000000000000, -0.000000000000000000 ) ) ;
#18876=ORIENTED_EDGE ( 'NONE', *, *, #50141, .T. ) ;
#18880=ADVANCED_FACE ( 'NONE', ( #61837 ), #45722, .T. ) ;
#18882=FACE_OUTER_BOUND ( 'NONE', #49069, .T. ) ;
#18884=ORIENTED_EDGE ( 'NONE', *, *, #19298, .T. ) ;
#18886=CYLINDRICAL_SURFACE ( 'NONE', #53410, 0.5000000000000004441 ) ;
#18889=( LENGTH_UNIT ( ) NAMED_UNIT ( * ) SI_UNIT ( .MILLI., .METRE. ) );
#18892=VECTOR ( 'NONE', #67268, 1000.000000000000000 ) ;
#18900=CARTESIAN_POINT ( 'NONE',  ( 4.716976649647096842, 145.7429263765338305, 6.492361379858953896 ) ) ;
#18901=FILL_AREA_STYLE_COLOUR ( '', #67101 ) ;
#18902=SURFACE_STYLE_FILL_AREA ( #7669 ) ;
#18905=SURFACE_STYLE_FILL_AREA ( #50946 ) ;
#18913=CIRCLE ( 'NONE', #25651, 0.5000000000000006661 ) ;
#18915=DIRECTION ( 'NONE',  ( 1.000000000000000000, 0.000000000000000000, 0.000000000000000000 ) ) ;
#18916=EDGE_CURVE ( 'NONE', #53591, #31626, #57549, .T. ) ;
#18920=CYLINDRICAL_SURFACE ( 'NONE', #6274, 0.5000000000000004441 ) ;
#18926=CARTESIAN_POINT ( 'NONE',  ( -20.17806131642189271, 115.4772719928210876, 10.00000000000000178 ) ) ;
#18927=LINE ( 'NONE', #56581, #15502 ) ;
#18929=VERTEX_POINT ( 'NONE', #36201 ) ;
#18932=FACE_OUTER_BOUND ( 'NONE', #52756, .T. ) ;
#18936=DIRECTION ( 'NONE',  ( 0.000000000000000000, 1.000000000000000000, 0.000000000000000000 ) ) ;
#18937=EDGE_LOOP ( 'NONE', ( #44741, #2687, #54664, #29933 ) ) ;
#18939=CARTESIAN_POINT ( 'NONE',  ( -74.99999999999998579, 50.00000000000000000, 12.00000000000000000 ) ) ;
#18942=DIRECTION ( 'NONE',  ( 0.000000000000000000, 1.000000000000000000, 0.000000000000000000 ) ) ;
#18946=CARTESIAN_POINT ( 'NONE',  ( -1.166476076187854022E-15, 118.0549999999999926, 9.525000000000000355 ) ) ;
#18951=COLOUR_RGB ( '', 0.31764706, 0.68627451, 0.89019608) ;
#18952=CARTESIAN_POINT ( 'NONE',  ( 71.99999999999998579, 119.9999999999997868, 9.500000000000000000 ) ) ;
#18954=ORIENTED_EDGE ( 'NONE', *, *, #38156, .F. ) ;
#18955=EDGE_CURVE ( 'NONE', #54121, #44684, #12645, .T. ) ;
#18958=SURFACE_STYLE_USAGE ( .BOTH. , #41864 ) ;
#18963=VERTEX_POINT ( 'NONE', #68190 ) ;
#18965=EDGE_LOOP ( 'NONE', ( #45425, #44569, #17742, #33221 ) ) ;
#18968=DIRECTION ( 'NONE',  ( -1.000000000000000000, -0.000000000000000000, 0.000000000000000000 ) ) ;
#18969=FILL_AREA_STYLE ('',( #66497 ) ) ;
#18973=ORIENTED_EDGE ( 'NONE', *, *, #3789, .T. ) ;
#18976=ORIENTED_EDGE ( 'NONE', *, *, #33222, .T. ) ;
#18980=CARTESIAN_POINT ( 'NONE',  ( 71.50000000000000000, 35.92875272052971525, -7.000000000000000000 ) ) ;
#18982=CARTESIAN_POINT ( 'NONE',  ( 3.094860106618431583, 141.0949999999999989, 9.525000000000000355 ) ) ;
#18986=CARTESIAN_POINT ( 'NONE',  ( -9.058813317711337021, 141.1549999999999727, -2.943386871421374895 ) ) ;
#18989=ORIENTED_EDGE ( 'NONE', *, *, #21152, .T. ) ;
#18990=CARTESIAN_POINT ( 'NONE',  ( -7.632228543268608334, 111.8429263765338106, 2.479861379858952830 ) ) ;
#18992=CARTESIAN_POINT ( 'NONE',  ( -45.50000000000000000, 9.708372675170618749, -6.000000000000000000 ) ) ;
#18994=DIRECTION ( 'NONE',  ( 0.000000000000000000, 1.000000000000000000, 0.000000000000000000 ) ) ;
#18996=AXIS2_PLACEMENT_3D ( 'NONE', #69159, #30808, #19904 ) ;
#18997=CARTESIAN_POINT ( 'NONE',  ( 41.30869453359411381, 107.2693964154586155, 3.464738947915712686 ) ) ;
#18998=VERTEX_POINT ( 'NONE', #4125 ) ;
#19000=CIRCLE ( 'NONE', #26866, 15.00000000000000000 ) ;
#19002=CARTESIAN_POINT ( 'NONE',  ( 48.00000000000000000, 14.49137674618942562, 9.500000000000000000 ) ) ;
#19004=ORIENTED_EDGE ( 'NONE', *, *, #40105, .T. ) ;
#19009=( NAMED_UNIT ( * ) PLANE_ANGLE_UNIT ( ) SI_UNIT ( $, .RADIAN. ) );
#19011=FACE_OUTER_BOUND ( 'NONE', #47572, .T. ) ;
#19014=CYLINDRICAL_SURFACE ( 'NONE', #14265, 0.5000000000000004441 ) ;
#19018=SURFACE_STYLE_FILL_AREA ( #40179 ) ;
#19019=( GEOMETRIC_REPRESENTATION_CONTEXT ( 3 ) GLOBAL_UNCERTAINTY_ASSIGNED_CONTEXT ( ( #5257 ) ) GLOBAL_UNIT_ASSIGNED_CONTEXT ( ( #33574, #55732, #55011 ) ) REPRESENTATION_CONTEXT ( 'NONE', 'WORKASPACE' ) );
#19022=CARTESIAN_POINT ( 'NONE',  ( -75.00000000000000000, 8.706976341191499102, -5.725845108612586998 ) ) ;
#19023=EDGE_LOOP ( 'NONE', ( #65383, #63571, #24588, #65047 ) ) ;
#19027=CARTESIAN_POINT ( 'NONE',  ( 0.000000000000000000, 139.4449999999999932, -9.525000000000000355 ) ) ;
#19033=CIRCLE ( 'NONE', #57206, 0.5000000000000003331 ) ;
#19034=FACE_BOUND ( 'NONE', #14427, .T. ) ;
#19035=DIRECTION ( 'NONE',  ( -0.000000000000000000, -1.000000000000000000, -0.000000000000000000 ) ) ;
#19039=COLOUR_RGB ( '', 0.40784314, 0.44705882, 0.49803922) ;
#19041=DIRECTION ( 'NONE',  ( -0.000000000000000000, 1.000000000000000000, -0.000000000000000000 ) ) ;
#19050=ADVANCED_FACE ( 'NONE', ( #63249 ), #57597, .F. ) ;
#19051=CIRCLE ( 'NONE', #34785, 14.49999999999999822 ) ;
#19052=CARTESIAN_POINT ( 'NONE',  ( -9.827790563157511022E-16, 118.4429263765338192, 8.025000000000000355 ) ) ;
#19054=AXIS2_PLACEMENT_3D ( 'NONE', #15804, #47501, #63623 ) ;
#19055=DIRECTION ( 'NONE',  ( 0.000000000000000000, 0.000000000000000000, -1.000000000000000000 ) ) ;
#19056=EDGE_CURVE ( 'NONE', #13795, #10407, #22751, .T. ) ;
#19057=EDGE_LOOP ( 'NONE', ( #25761, #14412, #104, #38411 ) ) ;
#19060=PRESENTATION_STYLE_ASSIGNMENT (( #45523 ) ) ;
#19061=DIRECTION ( 'NONE',  ( -0.000000000000000000, 1.000000000000000000, -0.000000000000000000 ) ) ;
#19066=CARTESIAN_POINT ( 'NONE',  ( 7.632228543268608334, 159.4570736234661581, -2.479861379858951942 ) ) ;
#19070=CARTESIAN_POINT ( 'NONE',  ( -10.01517768586949408, 114.3049999999999926, -6.132527647946036459E-16 ) ) ;
#19074=CARTESIAN_POINT ( 'NONE',  ( 8.102448949553183510, 143.1049999999999329, -5.886773742842746238 ) ) ;
#19076=PLANE ( 'NONE',  #8563 ) ;
#19077=PRESENTATION_STYLE_ASSIGNMENT (( #13461 ) ) ;
#19078=CARTESIAN_POINT ( 'NONE',  ( -41.49999999999997868, 10.49999999999998046, -3.000000000000000000 ) ) ;
#19080=ORIENTED_EDGE ( 'NONE', *, *, #30641, .T. ) ;
#19081=DIRECTION ( 'NONE',  ( -0.000000000000000000, -0.000000000000000000, -1.000000000000000000 ) ) ;
#19082=CARTESIAN_POINT ( 'NONE',  ( 60.00000000000000000, 1.797044900979284448E-15, -10.00000000000000000 ) ) ;
#19083=STYLED_ITEM ( 'NONE', ( #28792 ), #59292 ) ;
#19087=CARTESIAN_POINT ( 'NONE',  ( -44.99999999999999289, 7.768687147774684831, -6.500000000000010658 ) ) ;
#19090=VERTEX_POINT ( 'NONE', #67843 ) ;
#19092=DIRECTION ( 'NONE',  ( -1.000000000000000000, 0.000000000000000000, 0.000000000000000000 ) ) ;
#19094=PLANE ( 'NONE',  #51611 ) ;
#19096=ORIENTED_EDGE ( 'NONE', *, *, #13683, .T. ) ;
#19097=FACE_OUTER_BOUND ( 'NONE', #40957, .T. ) ;
#19100=CIRCLE ( 'NONE', #58435, 0.5000000000000004441 ) ;
#19102=CARTESIAN_POINT ( 'NONE',  ( 5.598654528085809545, 142.1449999999999818, -7.705886871421373741 ) ) ;
#19106=( LENGTH_UNIT ( ) NAMED_UNIT ( * ) SI_UNIT ( .MILLI., .METRE. ) );
#19108=LINE ( 'NONE', #7876, #28997 ) ;
#19111=CARTESIAN_POINT ( 'NONE',  ( 20.71231517720798010, 146.9999999999999716, -7.500000000000000000 ) ) ;
#19115=STYLED_ITEM ( 'NONE', ( #58010 ), #15619 ) ;
#19117=CARTESIAN_POINT ( 'NONE',  ( -45.50000000000000000, 9.708372675170618749, -6.500000000000000000 ) ) ;
#19119=TOROIDAL_SURFACE ( 'NONE', #59597, 22.50000000000000000, 0.5000000000000000000 ) ;
#19120=ADVANCED_FACE ( 'NONE', ( #30517, #62879 ), #53716, .F. ) ;
#19121=DIRECTION ( 'NONE',  ( 0.000000000000000000, -0.000000000000000000, -1.000000000000000000 ) ) ;
#19128=EDGE_CURVE ( 'NONE', #25427, #2048, #5506, .T. ) ;
#19139=DIRECTION ( 'NONE',  ( -0.000000000000000000, -0.000000000000000000, -1.000000000000000000 ) ) ;
#19141=CIRCLE ( 'NONE', #58483, 4.999999999999997335 ) ;
#19143=FILL_AREA_STYLE_COLOUR ( '', #12417 ) ;
#19148=DIRECTION ( 'NONE',  ( -0.000000000000000000, -0.000000000000000000, -1.000000000000000000 ) ) ;
#19149=DIRECTION ( 'NONE',  ( 0.000000000000000000, 0.000000000000000000, -1.000000000000000000 ) ) ;
#19150=COLOUR_RGB ( '', 0.09019608, 0.27058824, 0.51372549) ;
#19153=COLOUR_RGB ( '', 0.09019608, 0.27058824, 0.51372549) ;
#19154=CARTESIAN_POINT ( 'NONE',  ( 4.716976649647096842, 137.8570736234661638, 6.492361379858953896 ) ) ;
#19156=ORIENTED_EDGE ( 'NONE', *, *, #59554, .F. ) ;
#19159=TOROIDAL_SURFACE ( 'NONE', #7924, 1.000000000000000000, 0.5000000000000000000 ) ;
#19164=STYLED_ITEM ( 'NONE', ( #54833 ), #17719 ) ;
#19166=VERTEX_POINT ( 'NONE', #33318 ) ;
#19167=EDGE_CURVE ( 'NONE', #40156, #18929, #51984, .T. ) ;
#19169=UNCERTAINTY_MEASURE_WITH_UNIT (LENGTH_MEASURE( 1.000000000000000082E-05 ), #18171, 'distance_accuracy_value', 'NONE');
#19173=( LENGTH_UNIT ( ) NAMED_UNIT ( * ) SI_UNIT ( .MILLI., .METRE. ) );
#19174=CARTESIAN_POINT ( 'NONE',  ( -23.21231517720797655, 118.4999999999999716, -7.000000000000000000 ) ) ;
#19177=CARTESIAN_POINT ( 'NONE',  ( -68.49999999999998579, -1.919947267060472329E-14, 10.50000000000000000 ) ) ;
#19178=SURFACE_STYLE_USAGE ( .BOTH. , #51221 ) ;
#19183=CARTESIAN_POINT ( 'NONE',  ( 0.000000000000000000, 112.4449999999999932, -9.525000000000000355 ) ) ;
#19186=COLOUR_RGB ( '', 0.66274510, 0.83137255, 0.94901961) ;
#19195=FACE_OUTER_BOUND ( 'NONE', #5385, .T. ) ;
#19196=CARTESIAN_POINT ( 'NONE',  ( -7.398177350229779847, 111.8698371976141743, 3.525222019987722000 ) ) ;
#19200=ORIENTED_EDGE ( 'NONE', *, *, #3539, .T. ) ;
#19202=COLOUR_RGB ( '', 0.31764706, 0.68627451, 0.89019608) ;
#19203=DIRECTION ( 'NONE',  ( 0.000000000000000000, 0.000000000000000000, -1.000000000000000000 ) ) ;
#19207=CIRCLE ( 'NONE', #14724, 0.5000000000000004441 ) ;
#19210=CARTESIAN_POINT ( 'NONE',  ( 5.598654528085805993, 154.3549999999999898, 7.705886871421374629 ) ) ;
#19211=( NAMED_UNIT ( * ) SI_UNIT ( $, .STERADIAN. ) SOLID_ANGLE_UNIT ( ) );
#19213=EDGE_CURVE ( 'NONE', #10613, #7095, #36490, .T. ) ;
#19215=COLOUR_RGB ( '', 0.08235294, 0.09019608, 0.10196078) ;
#19220=CYLINDRICAL_SURFACE ( 'NONE', #37247, 0.5000000000000004441 ) ;
#19221=DIRECTION ( 'NONE',  ( -0.000000000000000000, -1.000000000000000000, -0.000000000000000000 ) ) ;
#19223=ORIENTED_EDGE ( 'NONE', *, *, #43529, .T. ) ;
#19229=AXIS2_PLACEMENT_3D ( 'NONE', #64652, #22423, #38655 ) ;
#19232=ORIENTED_EDGE ( 'NONE', *, *, #19290, .T. ) ;
#19233=VERTEX_POINT ( 'NONE', #13935 ) ;
#19239=VERTEX_POINT ( 'NONE', #24466 ) ;
#19240=FILL_AREA_STYLE_COLOUR ( '', #16445 ) ;
#19241=AXIS2_PLACEMENT_3D ( 'NONE', #49464, #6881, #28306 ) ;
#19246=AXIS2_PLACEMENT_3D ( 'NONE', #12484, #38933, #49801 ) ;
#19248=FILL_AREA_STYLE ('',( #29095 ) ) ;
#19250=VERTEX_POINT ( 'NONE', #39655 ) ;
#19251=CARTESIAN_POINT ( 'NONE',  ( 7.632228543268607446, 143.0429263765338135, 2.479861379858954606 ) ) ;
#19254=COLOUR_RGB ( '', 0.31764706, 0.68627451, 0.89019608) ;
#19260=DIRECTION ( 'NONE',  ( 1.000000000000000000, 0.000000000000000000, 0.000000000000000000 ) ) ;
#19261=CARTESIAN_POINT ( 'NONE',  ( -60.00000000000000000, -2.024042244987997205E-14, -9.500000000000000000 ) ) ;
#19262=CARTESIAN_POINT ( 'NONE',  ( 41.49999999999998579, 106.9282032302754999, -3.500000000000000000 ) ) ;
#19265=FACE_OUTER_BOUND ( 'NONE', #69061, .T. ) ;
#19267=CARTESIAN_POINT ( 'NONE',  ( 0.000000000000000000, 110.4999999999999858, -23.00000000000000000 ) ) ;
#19268=CARTESIAN_POINT ( 'NONE',  ( -8.437984349512095861, 120.6929263765338050, -5.166775262442723748E-16 ) ) ;
#19270=STYLED_ITEM ( 'NONE', ( #17409 ), #24302 ) ;
#19272=FILL_AREA_STYLE_COLOUR ( '', #44098 ) ;
#19273=CARTESIAN_POINT ( 'NONE',  ( 45.65811388300841855, 10.21937129433612057, 6.292893218813452982 ) ) ;
#19274=DIRECTION ( 'NONE',  ( -1.000000000000000000, 0.000000000000000000, 0.000000000000000000 ) ) ;
#19284=COLOUR_RGB ( '', 0.66274510, 0.83137255, 0.94901961) ;
#19287=ORIENTED_EDGE ( 'NONE', *, *, #44776, .F. ) ;
#19289=AXIS2_PLACEMENT_3D ( 'NONE', #4352, #5402, #36791 ) ;
#19290=EDGE_CURVE ( 'NONE', #13063, #10616, #23898, .T. ) ;
#19292=LINE ( 'NONE', #24562, #66148 ) ;
#19293=DIRECTION ( 'NONE',  ( -0.000000000000000000, -0.000000000000000000, -1.000000000000000000 ) ) ;
#19295=DIRECTION ( 'NONE',  ( 1.000000000000000000, 0.000000000000000000, 0.000000000000000000 ) ) ;
#19298=EDGE_CURVE ( 'NONE', #49707, #7942, #13769, .T. ) ;
#19299=AXIS2_PLACEMENT_3D ( 'NONE', #49029, #55291, #13073 ) ;
#19301=CARTESIAN_POINT ( 'NONE',  ( -8.102448949553181734, 120.6049999999999756, 5.886773742842747126 ) ) ;
#19306=CARTESIAN_POINT ( 'NONE',  ( -15.98999599679679839, 118.4999999999999716, -7.500000000000000000 ) ) ;
#19308=UNCERTAINTY_MEASURE_WITH_UNIT (LENGTH_MEASURE( 1.000000000000000082E-05 ), #44689, 'distance_accuracy_value', 'NONE');
#19310=ORIENTED_EDGE ( 'NONE', *, *, #33012, .T. ) ;
#19315=SURFACE_STYLE_FILL_AREA ( #52739 ) ;
#19316=AXIS2_PLACEMENT_3D ( 'NONE', #10816, #26619, #10479 ) ;
#19317=DIRECTION ( 'NONE',  ( 0.000000000000000000, -1.000000000000000000, -0.000000000000000000 ) ) ;
#19318=CIRCLE ( 'NONE', #50774, 0.5000000000000004441 ) ;
#19321=FILL_AREA_STYLE ('',( #30917 ) ) ;
#19322=ORIENTED_EDGE ( 'NONE', *, *, #12447, .T. ) ;
#19323=ORIENTED_EDGE ( 'NONE', *, *, #2493, .F. ) ;
#19324=CARTESIAN_POINT ( 'NONE',  ( 15.98999599679679839, 117.9999999999999716, -9.500000000000000000 ) ) ;
#19325=AXIS2_PLACEMENT_3D ( 'NONE', #65222, #17420, #38886 ) ;
#19326=DIRECTION ( 'NONE',  ( 1.000000000000000000, 0.000000000000000000, -0.000000000000000000 ) ) ;
#19331=ORIENTED_EDGE ( 'NONE', *, *, #65591, .T. ) ;
#19338=LINE ( 'NONE', #46839, #50109 ) ;
#19339=ORIENTED_EDGE ( 'NONE', *, *, #9728, .F. ) ;
#19341=CARTESIAN_POINT ( 'NONE',  ( -9.058813317711338797, 143.3449999999999989, 2.943386871421373563 ) ) ;
#19345=CARTESIAN_POINT ( 'NONE',  ( 9.058813317711338797, 136.9549999999999841, -2.943386871421372675 ) ) ;
#19348=ORIENTED_EDGE ( 'NONE', *, *, #34801, .F. ) ;
#19349=CARTESIAN_POINT ( 'NONE',  ( -8.437984349512095861, 117.6929263765338050, -5.166775262442723748E-16 ) ) ;
#19350=FACE_OUTER_BOUND ( 'NONE', #30285, .T. ) ;
#19351=UNCERTAINTY_MEASURE_WITH_UNIT (LENGTH_MEASURE( 1.000000000000000082E-05 ), #59201, 'distance_accuracy_value', 'NONE');
#19352=CIRCLE ( 'NONE', #5890, 0.5000000000000004441 ) ;
#19354=( NAMED_UNIT ( * ) PLANE_ANGLE_UNIT ( ) SI_UNIT ( $, .RADIAN. ) );
#19355=ORIENTED_EDGE ( 'NONE', *, *, #501, .F. ) ;
#19357=DIRECTION ( 'NONE',  ( 0.000000000000000000, 0.000000000000000000, 1.000000000000000000 ) ) ;
#19360=PLANE ( 'NONE',  #61436 ) ;
#19363=ORIENTED_EDGE ( 'NONE', *, *, #8606, .T. ) ;
#19364=DIRECTION ( 'NONE',  ( 1.000000000000000000, 0.000000000000000000, 0.000000000000000000 ) ) ;
#19368=TOROIDAL_SURFACE ( 'NONE', #9452, 14.49999999999999822, 0.5000000000000000000 ) ;
#19369=( NAMED_UNIT ( * ) SI_UNIT ( $, .STERADIAN. ) SOLID_ANGLE_UNIT ( ) );
#19373=CYLINDRICAL_SURFACE ( 'NONE', #66770, 8.025000000000000355 ) ;
#19374=EDGE_CURVE ( 'NONE', #60681, #52169, #13574, .T. ) ;
#19375=ORIENTED_EDGE ( 'NONE', *, *, #63780, .T. ) ;
#19377=DIRECTION ( 'NONE',  ( 1.000000000000000000, -5.204170427930416550E-15, 0.000000000000000000 ) ) ;
#19382=DIRECTION ( 'NONE',  ( -0.000000000000000000, -0.000000000000000000, -1.000000000000000000 ) ) ;
#19386=MECHANICAL_DESIGN_GEOMETRIC_PRESENTATION_REPRESENTATION('',(#55332),#1357);
#19388=( NAMED_UNIT ( * ) PLANE_ANGLE_UNIT ( ) SI_UNIT ( $, .RADIAN. ) );
#19391=DIRECTION ( 'NONE',  ( -0.000000000000000000, -0.000000000000000000, -1.000000000000000000 ) ) ;
#19394=CARTESIAN_POINT ( 'NONE',  ( 5.598654528085809545, 136.1449999999999818, -7.705886871421373741 ) ) ;
#19398=( GEOMETRIC_REPRESENTATION_CONTEXT ( 3 ) GLOBAL_UNCERTAINTY_ASSIGNED_CONTEXT ( ( #33340 ) ) GLOBAL_UNIT_ASSIGNED_CONTEXT ( ( #4079, #30469, #19587 ) ) REPRESENTATION_CONTEXT ( 'NONE', 'WORKASPACE' ) );
#19400=UNCERTAINTY_MEASURE_WITH_UNIT (LENGTH_MEASURE( 1.000000000000000082E-05 ), #68396, 'distance_accuracy_value', 'NONE');
#19405=DIRECTION ( 'NONE',  ( 1.000000000000000000, 0.000000000000000000, 0.000000000000000000 ) ) ;
#19407=VECTOR ( 'NONE', #68697, 1000.000000000000000 ) ;
#19408=ADVANCED_FACE ( 'NONE', ( #25181 ), #10060, .T. ) ;
#19413=ORIENTED_EDGE ( 'NONE', *, *, #51616, .F. ) ;
#19414=COLOUR_RGB ( '', 0.66274510, 0.83137255, 0.94901961) ;
#19417=FILL_AREA_STYLE_COLOUR ( '', #31567 ) ;
#19418=CARTESIAN_POINT ( 'NONE',  ( 6.826472737025121695, 119.4929263765338163, -4.959722759717905660 ) ) ;
#19420=MECHANICAL_DESIGN_GEOMETRIC_PRESENTATION_REPRESENTATION('',(#63213),#17204);
#19423=CIRCLE ( 'NONE', #25053, 0.5000000000000004441 ) ;
#19425=FACE_OUTER_BOUND ( 'NONE', #68057, .T. ) ;
#19426=DIRECTION ( 'NONE',  ( -0.000000000000000000, -1.000000000000000000, -6.938893903907234689E-15 ) ) ;
#19430=CARTESIAN_POINT ( 'NONE',  ( 2.607480562269071989, 158.7070736234661865, 8.025000000000002132 ) ) ;
#19433=CARTESIAN_POINT ( 'NONE',  ( -52.00000000000000000, -1.926070501056209087E-14, -11.50000000000000000 ) ) ;
#19436=( NAMED_UNIT ( * ) SI_UNIT ( $, .STERADIAN. ) SOLID_ANGLE_UNIT ( ) );
#19437=ORIENTED_EDGE ( 'NONE', *, *, #57297, .F. ) ;
#19438=CARTESIAN_POINT ( 'NONE',  ( 5.598654528085809545, 134.2549999999999955, -7.705886871421373741 ) ) ;
#19439=UNCERTAINTY_MEASURE_WITH_UNIT (LENGTH_MEASURE( 1.000000000000000082E-05 ), #37249, 'distance_accuracy_value', 'NONE');
#19440=FACE_OUTER_BOUND ( 'NONE', #62542, .T. ) ;
#19442=EDGE_CURVE ( 'NONE', #21468, #38966, #62797, .T. ) ;
#19443=LINE ( 'NONE', #56380, #60889 ) ;
#19449=VECTOR ( 'NONE', #64621, 1000.000000000000000 ) ;
#19451=CARTESIAN_POINT ( 'NONE',  ( -45.50000000000000000, -2.024042244987997205E-14, -10.00000000000000000 ) ) ;
#19455=CARTESIAN_POINT ( 'NONE',  ( 71.50000000000000000, 14.49137674618942562, -7.500000000000000000 ) ) ;
#19463=( GEOMETRIC_REPRESENTATION_CONTEXT ( 3 ) GLOBAL_UNCERTAINTY_ASSIGNED_CONTEXT ( ( #17983 ) ) GLOBAL_UNIT_ASSIGNED_CONTEXT ( ( #57353, #5253, #14805 ) ) REPRESENTATION_CONTEXT ( 'NONE', 'WORKASPACE' ) );
#19464=DIRECTION ( 'NONE',  ( 0.000000000000000000, 0.000000000000000000, 1.000000000000000000 ) ) ;
#19465=CARTESIAN_POINT ( 'NONE',  ( 8.102448949553181734, 144.9949999999999761, -5.886773742842746238 ) ) ;
#19473=ADVANCED_FACE ( 'NONE', ( #26212 ), #52295, .F. ) ;
#19480=SPHERICAL_SURFACE ( 'NONE', #2169, 0.5000000000000000000 ) ;
#19488=STYLED_ITEM ( 'NONE', ( #55499 ), #61844 ) ;
#19489=FILL_AREA_STYLE ('',( #40279 ) ) ;
#19491=VERTEX_POINT ( 'NONE', #53322 ) ;
#19495=FACE_OUTER_BOUND ( 'NONE', #29503, .T. ) ;
#19504=DIRECTION ( 'NONE',  ( -0.000000000000000000, 0.000000000000000000, -1.000000000000000000 ) ) ;
#19505=LINE ( 'NONE', #36441, #27252 ) ;
#19507=CARTESIAN_POINT ( 'NONE',  ( -45.91547277936962246, 9.430195807687219656, 3.611004237778671744 ) ) ;
#19508=MECHANICAL_DESIGN_GEOMETRIC_PRESENTATION_REPRESENTATION('',(#44273),#6002);
#19510=CARTESIAN_POINT ( 'NONE',  ( -7.632228543268607446, 133.6570736234661467, -2.479861379858953718 ) ) ;
#19512=VECTOR ( 'NONE', #23859, 1000.000000000000000 ) ;
#19517=COLOUR_RGB ( '', 0.08235294, 0.09019608, 0.10196078) ;
#19519=CARTESIAN_POINT ( 'NONE',  ( 4.716976649647096842, 149.8570736234661638, 6.492361379858953896 ) ) ;
#19520=CARTESIAN_POINT ( 'NONE',  ( 0.000000000000000000, 114.9999999999999574, 0.000000000000000000 ) ) ;
#19526=VECTOR ( 'NONE', #14192, 1000.000000000000000 ) ;
#19529=ORIENTED_EDGE ( 'NONE', *, *, #59394, .T. ) ;
#19531=ADVANCED_FACE ( 'NONE', ( #37875 ), #5782, .T. ) ;
#19533=DIRECTION ( 'NONE',  ( -1.000000000000000000, 0.000000000000000000, 0.000000000000000000 ) ) ;
#19535=ADVANCED_FACE ( 'NONE', ( #48766 ), #17207, .F. ) ;
#19537=FILL_AREA_STYLE_COLOUR ( '', #65560 ) ;
#19540=CARTESIAN_POINT ( 'NONE',  ( -60.00000000000000000, -2.024042244987997205E-14, -7.000000000000000888 ) ) ;
#19547=CARTESIAN_POINT ( 'NONE',  ( 10.01517768586949408, 117.6949999999999790, 1.839758294383810543E-15 ) ) ;
#19550=( NAMED_UNIT ( * ) SI_UNIT ( $, .STERADIAN. ) SOLID_ANGLE_UNIT ( ) );
#19555=CYLINDRICAL_SURFACE ( 'NONE', #63867, 0.5000000000000004441 ) ;
#19557=STYLED_ITEM ( 'NONE', ( #39792 ), #38514 ) ;
#19559=CARTESIAN_POINT ( 'NONE',  ( -74.99999999999998579, 9.027015924850166684, 6.778771685250380763 ) ) ;
#19560=CARTESIAN_POINT ( 'NONE',  ( -5.201328222576680815, 110.9678030318073496, -7.425688344617400460 ) ) ;
#19562=STYLED_ITEM ( 'NONE', ( #40006 ), #36824 ) ;
#19564=ORIENTED_EDGE ( 'NONE', *, *, #8206, .F. ) ;
#19565=STYLED_ITEM ( 'NONE', ( #51553 ), #55902 ) ;
#19568=CARTESIAN_POINT ( 'NONE',  ( 34.99999999999999289, 113.4999999999999858, -7.000000000000000000 ) ) ;
#19571=CARTESIAN_POINT ( 'NONE',  ( 48.50000000000000000, 14.49137674618942562, 10.00000000000000000 ) ) ;
#19575=CARTESIAN_POINT ( 'NONE',  ( -9.058813317711337021, 159.1550000000000011, -2.943386871421374895 ) ) ;
#19576=DIRECTION ( 'NONE',  ( 1.000000000000000000, 0.000000000000000000, 0.000000000000000000 ) ) ;
#19580=VECTOR ( 'NONE', #12115, 1000.000000000000000 ) ;
#19582=TOROIDAL_SURFACE ( 'NONE', #3840, 14.49999999999999822, 0.5000000000000000000 ) ;
#19584=DIRECTION ( 'NONE',  ( 1.000000000000000000, 0.000000000000000000, 0.000000000000000000 ) ) ;
#19585=AXIS2_PLACEMENT_3D ( 'NONE', #5351, #16313, #53566 ) ;
#19586=DIRECTION ( 'NONE',  ( 0.2413793103448194644, 0.9704308468600220117, 0.000000000000000000 ) ) ;
#19587=( NAMED_UNIT ( * ) SI_UNIT ( $, .STERADIAN. ) SOLID_ANGLE_UNIT ( ) );
#19588=ORIENTED_EDGE ( 'NONE', *, *, #40363, .F. ) ;
#19589=VECTOR ( 'NONE', #46113, 1000.000000000000000 ) ;
#19593=( NAMED_UNIT ( * ) PLANE_ANGLE_UNIT ( ) SI_UNIT ( $, .RADIAN. ) );
#19594=CARTESIAN_POINT ( 'NONE',  ( -45.00000000000000000, 8.553246373267509028, 6.928940927505456315 ) ) ;
#19597=VERTEX_POINT ( 'NONE', #61660 ) ;
#19601=( NAMED_UNIT ( * ) SI_UNIT ( $, .STERADIAN. ) SOLID_ANGLE_UNIT ( ) );
#19605=MECHANICAL_DESIGN_GEOMETRIC_PRESENTATION_REPRESENTATION('',(#38748),#46473);
#19609=AXIS2_PLACEMENT_3D ( 'NONE', #22284, #60, #58537 ) ;
#19610=EDGE_CURVE ( 'NONE', #63887, #13795, #60304, .T. ) ;
#19615=CARTESIAN_POINT ( 'NONE',  ( 4.716976649647099507, 143.6429263765338078, -6.492361379858953008 ) ) ;
#19616=CARTESIAN_POINT ( 'NONE',  ( 0.000000000000000000, 149.9999999999999716, -23.00000000000000355 ) ) ;
#19617=SURFACE_SIDE_STYLE ('',( #18902 ) ) ;
#19620=DIRECTION ( 'NONE',  ( 1.000000000000000000, -0.000000000000000000, 0.000000000000000000 ) ) ;
#19622=EDGE_LOOP ( 'NONE', ( #19943, #30581, #4107, #53944 ) ) ;
#19625=SURFACE_STYLE_FILL_AREA ( #30867 ) ;
#19629=CARTESIAN_POINT ( 'NONE',  ( 0.000000000000000000, 142.0570736234661524, -8.025000000000000355 ) ) ;
#19630=SURFACE_STYLE_USAGE ( .BOTH. , #67835 ) ;
#19631=VECTOR ( 'NONE', #59341, 1000.000000000000000 ) ;
#19635=CARTESIAN_POINT ( 'NONE',  ( -74.72379611408101141, 36.27863051838266983, 9.964730096445045149 ) ) ;
#19639=SURFACE_STYLE_USAGE ( .BOTH. , #46785 ) ;
#19640=AXIS2_PLACEMENT_3D ( 'NONE', #2365, #40106, #56592 ) ;
#19641=FILL_AREA_STYLE ('',( #67846 ) ) ;
#19642=ORIENTED_EDGE ( 'NONE', *, *, #11825, .T. ) ;
#19645=LINE ( 'NONE', #52713, #29582 ) ;
#19652=PRESENTATION_STYLE_ASSIGNMENT (( #67856 ) ) ;
#19653=ORIENTED_EDGE ( 'NONE', *, *, #4793, .T. ) ;
#19657=CARTESIAN_POINT ( 'NONE',  ( 9.385348596157497170, 154.4999999999999432, 1.684017021904244737 ) ) ;
#19661=CARTESIAN_POINT ( 'NONE',  ( -5.598654528085806881, 131.8549999999999898, -7.705886871421374629 ) ) ;
#19663=CARTESIAN_POINT ( 'NONE',  ( -75.00000000000000000, 9.298035018096992843, -6.651463925736444516 ) ) ;
#19667=COLOUR_RGB ( '', 0.40784314, 0.44705882, 0.49803922) ;
#19668=ADVANCED_FACE ( 'NONE', ( #56412 ), #50124, .F. ) ;
#19669=DIRECTION ( 'NONE',  ( 1.000000000000000000, 0.000000000000000000, 0.000000000000000000 ) ) ;
#19673=DIRECTION ( 'NONE',  ( 0.000000000000000000, 0.000000000000000000, -1.000000000000000000 ) ) ;
#19675=FACE_OUTER_BOUND ( 'NONE', #41938, .T. ) ;
#19676=( NAMED_UNIT ( * ) SI_UNIT ( $, .STERADIAN. ) SOLID_ANGLE_UNIT ( ) );
#19677=ORIENTED_EDGE ( 'NONE', *, *, #58239, .T. ) ;
#19678=ORIENTED_EDGE ( 'NONE', *, *, #27629, .T. ) ;
#19679=FILL_AREA_STYLE_COLOUR ( '', #46581 ) ;
#19680=( GEOMETRIC_REPRESENTATION_CONTEXT ( 3 ) GLOBAL_UNCERTAINTY_ASSIGNED_CONTEXT ( ( #56747 ) ) GLOBAL_UNIT_ASSIGNED_CONTEXT ( ( #30334, #46599, #68705 ) ) REPRESENTATION_CONTEXT ( 'NONE', 'WORKASPACE' ) );
#19681=AXIS2_PLACEMENT_3D ( 'NONE', #5181, #11156, #64640 ) ;
#19682=DIRECTION ( 'NONE',  ( 0.000000000000000000, 0.000000000000000000, -1.000000000000000000 ) ) ;
#19683=DIRECTION ( 'NONE',  ( 1.000000000000000000, 0.000000000000000000, 0.000000000000000000 ) ) ;
#19684=SURFACE_STYLE_FILL_AREA ( #24956 ) ;
#19685=DIRECTION ( 'NONE',  ( 0.000000000000000000, 0.000000000000000000, -1.000000000000000000 ) ) ;
#19686=ORIENTED_EDGE ( 'NONE', *, *, #1954, .T. ) ;
#19693=EDGE_LOOP ( 'NONE', ( #14599, #20063, #49852, #26184 ) ) ;
#19695=DIRECTION ( 'NONE',  ( 1.000000000000000000, 0.000000000000000000, 0.000000000000000000 ) ) ;
#19697=AXIS2_PLACEMENT_3D ( 'NONE', #542, #43234, #27658 ) ;
#19699=CARTESIAN_POINT ( 'NONE',  ( -3.094860106618434248, 137.7950000000000159, 9.525000000000000355 ) ) ;
#19703=CARTESIAN_POINT ( 'NONE',  ( -5.598654528085808657, 150.7549999999999955, 7.705886871421373741 ) ) ;
#19705=DIRECTION ( 'NONE',  ( -1.000000000000000000, 0.000000000000000000, 0.000000000000000000 ) ) ;
#19706=SURFACE_STYLE_FILL_AREA ( #41897 ) ;
#19708=CARTESIAN_POINT ( 'NONE',  ( 8.437984349512095861, 113.1929263765338050, 1.550032578732817026E-15 ) ) ;
#19709=CARTESIAN_POINT ( 'NONE',  ( 15.48999599679679662, 146.4999999999999716, 10.00000000000000000 ) ) ;
#19710=FILL_AREA_STYLE_COLOUR ( '', #695 ) ;
#19712=MECHANICAL_DESIGN_GEOMETRIC_PRESENTATION_REPRESENTATION('',(#10727),#48936);
#19713=DIRECTION ( 'NONE',  ( -0.000000000000000000, 0.000000000000000000, -1.000000000000000000 ) ) ;
#19715=AXIS2_PLACEMENT_3D ( 'NONE', #16294, #32776, #43718 ) ;
#19718=ORIENTED_EDGE ( 'NONE', *, *, #46184, .T. ) ;
#19720=( LENGTH_UNIT ( ) NAMED_UNIT ( * ) SI_UNIT ( .MILLI., .METRE. ) );
#19725=EDGE_CURVE ( 'NONE', #39381, #12255, #31327, .T. ) ;
#19727=CARTESIAN_POINT ( 'NONE',  ( -71.50000000000000000, 14.49137674618942562, 7.500000000000000000 ) ) ;
#19730=CARTESIAN_POINT ( 'NONE',  ( -70.87837837837835764, 13.70805908423323949, 10.00000000000000000 ) ) ;
#19734=CARTESIAN_POINT ( 'NONE',  ( -80.49999999999995737, 50.00000000000000000, 12.00000000000000000 ) ) ;
#19737=ORIENTED_EDGE ( 'NONE', *, *, #58859, .T. ) ;
#19739=CARTESIAN_POINT ( 'NONE',  ( -75.00000000000000000, 9.118333594695574362, -6.737587966311150645 ) ) ;
#19741=DIRECTION ( 'NONE',  ( -1.000000000000000000, -0.000000000000000000, -0.000000000000000000 ) ) ;
#19743=( GEOMETRIC_REPRESENTATION_CONTEXT ( 3 ) GLOBAL_UNCERTAINTY_ASSIGNED_CONTEXT ( ( #69253 ) ) GLOBAL_UNIT_ASSIGNED_CONTEXT ( ( #40089, #62534, #50959 ) ) REPRESENTATION_CONTEXT ( 'NONE', 'WORKASPACE' ) );
#19744=CARTESIAN_POINT ( 'NONE',  ( -3.094860106618432471, 145.5949999999999136, -9.525000000000000355 ) ) ;
#19749=EDGE_CURVE ( 'NONE', #54396, #1660, #17888, .T. ) ;
#19750=CARTESIAN_POINT ( 'NONE',  ( -2.607480562269157254, 144.0929263765338249, -8.024999999999939959 ) ) ;
#19751=EDGE_LOOP ( 'NONE', ( #29295, #46514, #44518, #2652 ) ) ;
#19754=AXIS2_PLACEMENT_3D ( 'NONE', #55237, #33114, #7061 ) ;
#19755=CARTESIAN_POINT ( 'NONE',  ( 49.12162162162162105, 13.70805908423323238, 9.500000000000000000 ) ) ;
#19757=COLOUR_RGB ( '', 0.09019608, 0.27058824, 0.51372549) ;
#19759=DIRECTION ( 'NONE',  ( -0.000000000000000000, 1.000000000000000000, -0.000000000000000000 ) ) ;
#19760=ORIENTED_EDGE ( 'NONE', *, *, #14128, .T. ) ;
#19761=CARTESIAN_POINT ( 'NONE',  ( -2.607480562269073321, 129.0929263765338249, -8.025000000000000355 ) ) ;
#19764=DIRECTION ( 'NONE',  ( -0.000000000000000000, -0.000000000000000000, 1.000000000000000000 ) ) ;
#19766=CARTESIAN_POINT ( 'NONE',  ( 60.00000000000000000, 115.4999999999999574, -10.50000000000000000 ) ) ;
#19767=CARTESIAN_POINT ( 'NONE',  ( -45.00000000000000000, 7.768687147774683943, 7.000000000000000888 ) ) ;
#19772=ADVANCED_FACE ( 'NONE', ( #37453 ), #34099, .F. ) ;
#19774=EDGE_LOOP ( 'NONE', ( #63790, #386, #52717 ) ) ;
#19775=CARTESIAN_POINT ( 'NONE',  ( 9.827790563157511022E-16, 87.30187232391182306, -8.025000000000000355 ) ) ;
#19777=VERTEX_POINT ( 'NONE', #26797 ) ;
#19780=CARTESIAN_POINT ( 'NONE',  ( -8.102448949553181734, 109.8949999999999818, -5.886773742842749790 ) ) ;
#19784=CARTESIAN_POINT ( 'NONE',  ( -1.166476076187854022E-15, 118.0549999999999926, 9.525000000000000355 ) ) ;
#19791=CARTESIAN_POINT ( 'NONE',  ( 3.094860106618431583, 142.2050000000000125, 9.525000000000000355 ) ) ;
#19795=CARTESIAN_POINT ( 'NONE',  ( 20.26325459587049238, 115.0245731144845394, 10.00000000000000000 ) ) ;
#19797=EDGE_LOOP ( 'NONE', ( #20194, #45525, #25456, #18629 ) ) ;
#19798=( NAMED_UNIT ( * ) PLANE_ANGLE_UNIT ( ) SI_UNIT ( $, .RADIAN. ) );
#19799=CARTESIAN_POINT ( 'NONE',  ( -69.50000000000000000, 50.00000000000000000, 12.00000000000000000 ) ) ;
#19803=CARTESIAN_POINT ( 'NONE',  ( 8.601545703395382603, 111.4306875064348503, 0.4166762051479315221 ) ) ;
#19806=ORIENTED_EDGE ( 'NONE', *, *, #31873, .T. ) ;
#19808=ORIENTED_EDGE ( 'NONE', *, *, #60737, .F. ) ;
#19809=DIRECTION ( 'NONE',  ( 1.000000000000000000, 0.000000000000000000, 0.000000000000000000 ) ) ;
#19811=FILL_AREA_STYLE_COLOUR ( '', #33680 ) ;
#19814=EDGE_CURVE ( 'NONE', #52933, #47797, #53829, .T. ) ;
#19818=CARTESIAN_POINT ( 'NONE',  ( -8.102448949553179958, 148.8950000000000102, -5.886773742842749790 ) ) ;
#19822=CARTESIAN_POINT ( 'NONE',  ( -83.99999999999997158, 50.00000000000000000, 11.50000000000000000 ) ) ;
#19824=DIRECTION ( 'NONE',  ( -1.000000000000000000, 0.000000000000000000, 0.000000000000000000 ) ) ;
#19828=CARTESIAN_POINT ( 'NONE',  ( 5.598654528085805993, 114.2449999999999903, 7.705886871421374629 ) ) ;
#19832=SURFACE_SIDE_STYLE ('',( #25454 ) ) ;
#19834=DIRECTION ( 'NONE',  ( -0.000000000000000000, -0.000000000000000000, -1.000000000000000000 ) ) ;
#19841=DIRECTION ( 'NONE',  ( 6.938893903907222067E-15, 0.000000000000000000, 1.000000000000000000 ) ) ;
#19848=CARTESIAN_POINT ( 'NONE',  ( 2.607480562269075985, 123.9070736234661467, -8.025000000000000355 ) ) ;
#19849=LINE ( 'NONE', #52920, #31409 ) ;
#19855=EDGE_LOOP ( 'NONE', ( #65090, #37079, #48128, #18225 ) ) ;
#19858=CARTESIAN_POINT ( 'NONE',  ( 2.607480562269076430, 135.9070736234661467, -8.025000000000000355 ) ) ;
#19859=FILL_AREA_STYLE_COLOUR ( '', #32661 ) ;
#19860=VERTEX_POINT ( 'NONE', #28806 ) ;
#19864=CARTESIAN_POINT ( 'NONE',  ( 75.00000000000000000, 20.36037961002804053, -6.000000000000000000 ) ) ;
#19865=EDGE_CURVE ( 'NONE', #49361, #61387, #45255, .T. ) ;
#19868=ORIENTED_EDGE ( 'NONE', *, *, #53472, .F. ) ;
#19872=DIRECTION ( 'NONE',  ( 0.6216216216216311485, 0.7833176619561784682, 0.000000000000000000 ) ) ;
#19873=DIRECTION ( 'NONE',  ( 1.000000000000000000, 0.000000000000000000, 0.000000000000000000 ) ) ;
#19874=UNCERTAINTY_MEASURE_WITH_UNIT (LENGTH_MEASURE( 1.000000000000000082E-05 ), #37048, 'distance_accuracy_value', 'NONE');
#19879=VERTEX_POINT ( 'NONE', #18274 ) ;
#19880=SURFACE_SIDE_STYLE ('',( #15673 ) ) ;
#19881=ORIENTED_EDGE ( 'NONE', *, *, #69082, .T. ) ;
#19889=CARTESIAN_POINT ( 'NONE',  ( 4.716976649647099507, 113.6429263765338078, -6.492361379858953008 ) ) ;
#19890=PRESENTATION_STYLE_ASSIGNMENT (( #57902 ) ) ;
#19894=CARTESIAN_POINT ( 'NONE',  ( 44.28021770739998431, 9.999999999999980460, 3.500000000000000000 ) ) ;
#19897=AXIS2_PLACEMENT_3D ( 'NONE', #57338, #29567, #51731 ) ;
#19899=DIRECTION ( 'NONE',  ( 1.000000000000000000, 0.000000000000000000, 0.000000000000000000 ) ) ;
#19904=DIRECTION ( 'NONE',  ( 0.6216216216216311485, 0.7833176619561784682, 0.000000000000000000 ) ) ;
#19905=CARTESIAN_POINT ( 'NONE',  ( 40.99999999999997868, 9.999999999999978684, 3.500000000000000000 ) ) ;
#19906=SURFACE_SIDE_STYLE ('',( #31850 ) ) ;
#19912=CARTESIAN_POINT ( 'NONE',  ( 3.094860106618435136, 158.4049999999999727, -9.525000000000000355 ) ) ;
#19913=DIRECTION ( 'NONE',  ( -1.000000000000000000, 4.336808689941999001E-16, 0.000000000000000000 ) ) ;
#19916=UNCERTAINTY_MEASURE_WITH_UNIT (LENGTH_MEASURE( 1.000000000000000082E-05 ), #35677, 'distance_accuracy_value', 'NONE');
#19923=DIRECTION ( 'NONE',  ( -0.000000000000000000, -0.000000000000000000, -1.000000000000000000 ) ) ;
#19925=DIRECTION ( 'NONE',  ( -1.000000000000000000, -0.000000000000000000, -0.000000000000000000 ) ) ;
#19930=ADVANCED_FACE ( 'NONE', ( #8758 ), #26302, .T. ) ;
#19933=CARTESIAN_POINT ( 'NONE',  ( -20.57648123223228254, 114.4999999999999574, 10.27659574468085069 ) ) ;
#19936=DIRECTION ( 'NONE',  ( 1.156482317317873451E-16, -1.000000000000000000, 0.000000000000000000 ) ) ;
#19939=DIRECTION ( 'NONE',  ( -0.000000000000000000, 1.000000000000000000, 0.000000000000000000 ) ) ;
#19942=CARTESIAN_POINT ( 'NONE',  ( 48.00000000000000000, 13.41640786499872284, -7.500000000000000000 ) ) ;
#19943=ORIENTED_EDGE ( 'NONE', *, *, #57839, .T. ) ;
#19944=CARTESIAN_POINT ( 'NONE',  ( -8.102448949553181734, 123.0049999999999955, -5.886773742842749790 ) ) ;
#19945=FACE_OUTER_BOUND ( 'NONE', #29699, .T. ) ;
#19947=ORIENTED_EDGE ( 'NONE', *, *, #3300, .T. ) ;
#19949=PRESENTATION_STYLE_ASSIGNMENT (( #30148 ) ) ;
#19950=ORIENTED_EDGE ( 'NONE', *, *, #53672, .T. ) ;
#19951=CARTESIAN_POINT ( 'NONE',  ( -6.826472737025120807, 150.3929263765338078, -4.959722759717907437 ) ) ;
#19953=DIRECTION ( 'NONE',  ( -0.000000000000000000, -0.000000000000000000, -1.000000000000000000 ) ) ;
#19954=CARTESIAN_POINT ( 'NONE',  ( 54.99999999999999289, 2.409368300552961372E-15, 6.999999999999988454 ) ) ;
#19957=ORIENTED_EDGE ( 'NONE', *, *, #22172, .F. ) ;
#19958=CARTESIAN_POINT ( 'NONE',  ( 21.02379604162863558, 114.6409683457797115, 9.999999999999998224 ) ) ;
#19959=SURFACE_STYLE_USAGE ( .BOTH. , #68181 ) ;
#19963=MECHANICAL_DESIGN_GEOMETRIC_PRESENTATION_REPRESENTATION('',(#6459),#33437);
#19964=CARTESIAN_POINT ( 'NONE',  ( -74.14894044101720283, 9.184648417642964802, 6.276141209865989445 ) ) ;
#19965=CARTESIAN_POINT ( 'NONE',  ( 24.21231517720798010, 112.9999999999999858, 7.500000000000000000 ) ) ;
#19966=EDGE_LOOP ( 'NONE', ( #67790, #19375, #35539, #26008 ) ) ;
#19968=ORIENTED_EDGE ( 'NONE', *, *, #48720, .F. ) ;
#19970=CARTESIAN_POINT ( 'NONE',  ( 4.716976649647096842, 113.8570736234661638, 6.492361379858953896 ) ) ;
#19972=SURFACE_STYLE_USAGE ( .BOTH. , #68194 ) ;
#19976=MECHANICAL_DESIGN_GEOMETRIC_PRESENTATION_REPRESENTATION('',(#50332),#68311);
#19978=DIRECTION ( 'NONE',  ( 0.000000000000000000, 1.000000000000000000, 0.000000000000000000 ) ) ;
#19979=ORIENTED_EDGE ( 'NONE', *, *, #66213, .T. ) ;
#19983=CARTESIAN_POINT ( 'NONE',  ( 72.00000000000000000, 35.92875272052971525, 7.000000000000000000 ) ) ;
#19984=DIRECTION ( 'NONE',  ( -0.000000000000000000, 1.000000000000000000, 0.000000000000000000 ) ) ;
#19985=MECHANICAL_DESIGN_GEOMETRIC_PRESENTATION_REPRESENTATION('',(#64927),#60404);
#19987=CARTESIAN_POINT ( 'NONE',  ( 3.094860106618435136, 125.4050000000000011, -9.525000000000000355 ) ) ;
#19989=CARTESIAN_POINT ( 'NONE',  ( -74.99999999999998579, 50.00000000000000000, 9.500000000000000000 ) ) ;
#19991=CARTESIAN_POINT ( 'NONE',  ( 15.98999599679679839, 118.4999999999999716, -10.00000000000000000 ) ) ;
#19993=UNCERTAINTY_MEASURE_WITH_UNIT (LENGTH_MEASURE( 1.000000000000000082E-05 ), #3942, 'distance_accuracy_value', 'NONE');
#19995=FILL_AREA_STYLE_COLOUR ( '', #52812 ) ;
#19997=VERTEX_POINT ( 'NONE', #25605 ) ;
#20000=CARTESIAN_POINT ( 'NONE',  ( -2.607480562269158586, 146.4070736234661751, 8.024999999999939959 ) ) ;
#20001=EDGE_CURVE ( 'NONE', #41724, #26112, #60523, .T. ) ;
#20002=ADVANCED_FACE ( 'NONE', ( #11168 ), #43922, .F. ) ;
#20005=LINE ( 'NONE', #25978, #64479 ) ;
#20011=CARTESIAN_POINT ( 'NONE',  ( -80.49999999999998579, 50.00000000000000000, 6.499999999999999112 ) ) ;
#20017=STYLED_ITEM ( 'NONE', ( #12020 ), #50999 ) ;
#20018=CARTESIAN_POINT ( 'NONE',  ( -47.50000000000000000, 99.99999999999992895, -9.500000000000000000 ) ) ;
#20021=ORIENTED_EDGE ( 'NONE', *, *, #6491, .T. ) ;
#20024=ORIENTED_EDGE ( 'NONE', *, *, #41194, .T. ) ;
#20029=CARTESIAN_POINT ( 'NONE',  ( -8.102448949553181734, 151.8950000000000102, -5.886773742842749790 ) ) ;
#20033=CARTESIAN_POINT ( 'NONE',  ( -3.094860106618434248, 153.9049999999999727, 9.525000000000000355 ) ) ;
#20034=ORIENTED_EDGE ( 'NONE', *, *, #48539, .T. ) ;
#20035=CARTESIAN_POINT ( 'NONE',  ( -7.632228543268607446, 114.5429263765338277, -2.479861379858953718 ) ) ;
#20036=PRESENTATION_STYLE_ASSIGNMENT (( #61552 ) ) ;
#20037=UNCERTAINTY_MEASURE_WITH_UNIT (LENGTH_MEASURE( 1.000000000000000082E-05 ), #52264, 'distance_accuracy_value', 'NONE');
#20040=CARTESIAN_POINT ( 'NONE',  ( -23.71231517720798010, 117.4999999999999716, 7.500000000000000000 ) ) ;
#20042=EDGE_LOOP ( 'NONE', ( #64355, #20839, #46260, #66445 ) ) ;
#20046=SURFACE_STYLE_USAGE ( .BOTH. , #30242 ) ;
#20049=CYLINDRICAL_SURFACE ( 'NONE', #63232, 17.00000000000000000 ) ;
#20051=EDGE_CURVE ( 'NONE', #66072, #39399, #27922, .T. ) ;
#20052=( GEOMETRIC_REPRESENTATION_CONTEXT ( 3 ) GLOBAL_UNCERTAINTY_ASSIGNED_CONTEXT ( ( #4554 ) ) GLOBAL_UNIT_ASSIGNED_CONTEXT ( ( #42301, #69328, #26722 ) ) REPRESENTATION_CONTEXT ( 'NONE', 'WORKASPACE' ) );
#20056=CARTESIAN_POINT ( 'NONE',  ( 0.000000000000000000, 146.9429263765338192, -8.025000000000000355 ) ) ;
#20057=ORIENTED_EDGE ( 'NONE', *, *, #66120, .T. ) ;
#20058=EDGE_LOOP ( 'NONE', ( #56042, #65324, #66114, #55127 ) ) ;
#20060=VECTOR ( 'NONE', #56134, 1000.000000000000000 ) ;
#20061=FILL_AREA_STYLE ('',( #29589 ) ) ;
#20063=ORIENTED_EDGE ( 'NONE', *, *, #45689, .F. ) ;
#20066=AXIS2_PLACEMENT_3D ( 'NONE', #37267, #58667, #62895 ) ;
#20070=MECHANICAL_DESIGN_GEOMETRIC_PRESENTATION_REPRESENTATION('',(#50410),#47080);
#20072=CARTESIAN_POINT ( 'NONE',  ( -74.99999999999998579, 8.681192140609642394, -5.652915417256433983 ) ) ;
#20074=TOROIDAL_SURFACE ( 'NONE', #29040, 1.000000000000000000, 0.5000000000000000000 ) ;
#20075=ADVANCED_FACE ( 'NONE', ( #54751 ), #11867, .T. ) ;
#20076=CARTESIAN_POINT ( 'NONE',  ( -5.598654528085808657, 149.6450000000000102, 7.705886871421373741 ) ) ;
#20088=DIRECTION ( 'NONE',  ( 0.000000000000000000, 0.000000000000000000, -1.000000000000000000 ) ) ;
#20089=ADVANCED_FACE ( 'NONE', ( #28008 ), #43720, .T. ) ;
#20094=CARTESIAN_POINT ( 'NONE',  ( -2.607480562269032909, 118.2929263765338135, 8.025000000000032330 ) ) ;
#20097=AXIS2_PLACEMENT_3D ( 'NONE', #46697, #63168, #15005 ) ;
#20100=ORIENTED_EDGE ( 'NONE', *, *, #53682, .T. ) ;
#20103=ORIENTED_EDGE ( 'NONE', *, *, #48985, .T. ) ;
#20104=AXIS2_PLACEMENT_3D ( 'NONE', #2914, #65946, #61348 ) ;
#20109=CARTESIAN_POINT ( 'NONE',  ( -3.094860106618434248, 119.7949999999999733, 9.525000000000000355 ) ) ;
#20112=CARTESIAN_POINT ( 'NONE',  ( -10.01517768586949408, 117.3049999999999784, -6.132527647946036459E-16 ) ) ;
#20116=CARTESIAN_POINT ( 'NONE',  ( -3.094860106618432471, 140.7049999999999557, -9.525000000000000355 ) ) ;
#20117=UNCERTAINTY_MEASURE_WITH_UNIT (LENGTH_MEASURE( 1.000000000000000082E-05 ), #9395, 'distance_accuracy_value', 'NONE');
#20118=FILL_AREA_STYLE_COLOUR ( '', #46668 ) ;
#20120=CARTESIAN_POINT ( 'NONE',  ( -34.99999999999999289, 99.99999999999998579, 7.500000000000000000 ) ) ;
#20123=AXIS2_PLACEMENT_3D ( 'NONE', #63438, #16661, #16321 ) ;
#20125=DIRECTION ( 'NONE',  ( 0.000000000000000000, 0.000000000000000000, 1.000000000000000000 ) ) ;
#20126=LINE ( 'NONE', #25421, #62071 ) ;
#20129=CARTESIAN_POINT ( 'NONE',  ( 6.780819373525680760, 111.6853910234447369, -4.862369566202438875 ) ) ;
#20133=ORIENTED_EDGE ( 'NONE', *, *, #55015, .F. ) ;
#20134=CARTESIAN_POINT ( 'NONE',  ( 60.00000000000000000, 1.797044900979284448E-15, 11.50000000000000000 ) ) ;
#20135=PRESENTATION_STYLE_ASSIGNMENT (( #69393 ) ) ;
#20137=STYLED_ITEM ( 'NONE', ( #41317 ), #68959 ) ;
#20143=CARTESIAN_POINT ( 'NONE',  ( -74.50000000000000000, 7.768687147774688384, -6.500000000000000000 ) ) ;
#20147=CARTESIAN_POINT ( 'NONE',  ( -1.166476076187854022E-15, 149.9449999999999932, 9.525000000000000355 ) ) ;
#20151=VECTOR ( 'NONE', #40984, 1000.000000000000000 ) ;
#20152=DIRECTION ( 'NONE',  ( -1.000000000000000000, 0.000000000000000000, 0.000000000000000000 ) ) ;
#20157=MECHANICAL_DESIGN_GEOMETRIC_PRESENTATION_REPRESENTATION('',(#43807),#49405);
#20162=CARTESIAN_POINT ( 'NONE',  ( 9.058813317711338797, 123.8449999999999847, -2.943386871421372675 ) ) ;
#20166=MECHANICAL_DESIGN_GEOMETRIC_PRESENTATION_REPRESENTATION('',(#25794),#20216);
#20167=CIRCLE ( 'NONE', #27973, 1.000000000000000888 ) ;
#20169=VECTOR ( 'NONE', #7146, 1000.000000000000114 ) ;
#20170=PRESENTATION_STYLE_ASSIGNMENT (( #14560 ) ) ;
#20171=EDGE_CURVE ( 'NONE', #17220, #26318, #10046, .T. ) ;
#20172=VERTEX_POINT ( 'NONE', #67407 ) ;
#20176=EDGE_CURVE ( 'NONE', #17419, #55126, #38138, .T. ) ;
#20179=CARTESIAN_POINT ( 'NONE',  ( -20.99077900071323199, 114.7777241159145518, -10.00000000000000000 ) ) ;
#20181=ORIENTED_EDGE ( 'NONE', *, *, #52972, .T. ) ;
#20184=CARTESIAN_POINT ( 'NONE',  ( -71.50000000000000000, 14.49137674618942562, -7.000000000000000000 ) ) ;
#20185=DIRECTION ( 'NONE',  ( 0.000000000000000000, -1.000000000000000000, 0.000000000000000000 ) ) ;
#20186=EDGE_CURVE ( 'NONE', #44405, #13586, #66199, .T. ) ;
#20189=CYLINDRICAL_SURFACE ( 'NONE', #68487, 8.025000000000000355 ) ;
#20191=VERTEX_POINT ( 'NONE', #50892 ) ;
#20194=ORIENTED_EDGE ( 'NONE', *, *, #68767, .T. ) ;
#20195=( NAMED_UNIT ( * ) SI_UNIT ( $, .STERADIAN. ) SOLID_ANGLE_UNIT ( ) );
#20196=STYLED_ITEM ( 'NONE', ( #16381 ), #1450 ) ;
#20200=CARTESIAN_POINT ( 'NONE',  ( 4.716976649647096842, 134.8570736234661638, 6.492361379858953896 ) ) ;
#20202=ORIENTED_EDGE ( 'NONE', *, *, #58785, .F. ) ;
#20205=UNCERTAINTY_MEASURE_WITH_UNIT (LENGTH_MEASURE( 1.000000000000000082E-05 ), #22211, 'distance_accuracy_value', 'NONE');
#20211=( GEOMETRIC_REPRESENTATION_CONTEXT ( 3 ) GLOBAL_UNCERTAINTY_ASSIGNED_CONTEXT ( ( #53942 ) ) GLOBAL_UNIT_ASSIGNED_CONTEXT ( ( #29352, #61366, #7908 ) ) REPRESENTATION_CONTEXT ( 'NONE', 'WORKASPACE' ) );
#20212=CIRCLE ( 'NONE', #1066, 5.000000000000004441 ) ;
#20214=CARTESIAN_POINT ( 'NONE',  ( 44.99999999999977973, 149.4999999999999716, -10.00000000000000000 ) ) ;
#20216=( GEOMETRIC_REPRESENTATION_CONTEXT ( 3 ) GLOBAL_UNCERTAINTY_ASSIGNED_CONTEXT ( ( #37767 ) ) GLOBAL_UNIT_ASSIGNED_CONTEXT ( ( #39524, #49713, #65884 ) ) REPRESENTATION_CONTEXT ( 'NONE', 'WORKASPACE' ) );
#20219=CARTESIAN_POINT ( 'NONE',  ( 23.21231517720797655, 117.9999999999999716, 10.00000000000000000 ) ) ;
#20226=DIRECTION ( 'NONE',  ( 0.000000000000000000, 1.000000000000000000, 0.000000000000000000 ) ) ;
#20227=DIRECTION ( 'NONE',  ( 1.000000000000000000, 0.000000000000000000, 0.000000000000000000 ) ) ;
#20231=ORIENTED_EDGE ( 'NONE', *, *, #45843, .F. ) ;
#20234=VECTOR ( 'NONE', #19984, 1000.000000000000000 ) ;
#20237=CARTESIAN_POINT ( 'NONE',  ( -5.598654528085806881, 124.7449999999999903, -7.705886871421374629 ) ) ;
#20240=FILL_AREA_STYLE_COLOUR ( '', #62158 ) ;
#20241=SURFACE_SIDE_STYLE ('',( #30093 ) ) ;
#20243=CIRCLE ( 'NONE', #52865, 15.00000000000000000 ) ;
#20244=PRESENTATION_STYLE_ASSIGNMENT (( #68447 ) ) ;
#20245=LINE ( 'NONE', #53643, #15551 ) ;
#20246=DIRECTION ( 'NONE',  ( 1.000000000000000000, 0.000000000000000000, 0.000000000000000000 ) ) ;
#20250=CARTESIAN_POINT ( 'NONE',  ( 23.21231517720797655, 117.4999999999999716, 7.000000000000000000 ) ) ;
#20254=ORIENTED_EDGE ( 'NONE', *, *, #25372, .T. ) ;
#20256=CARTESIAN_POINT ( 'NONE',  ( -71.49999999999998579, 50.00000000000000000, 7.000000000000000000 ) ) ;
#20262=CARTESIAN_POINT ( 'NONE',  ( 5.598654528085805993, 157.3549999999999898, 7.705886871421374629 ) ) ;
#20266=CIRCLE ( 'NONE', #38241, 0.5000000000000004441 ) ;
#20267=FILL_AREA_STYLE ('',( #68469 ) ) ;
#20269=PRESENTATION_STYLE_ASSIGNMENT (( #4073 ) ) ;
#20273=MECHANICAL_DESIGN_GEOMETRIC_PRESENTATION_REPRESENTATION('',(#67477),#65216);
#20275=EDGE_CURVE ( 'NONE', #16380, #26318, #42663, .T. ) ;
#20277=DIRECTION ( 'NONE',  ( 0.000000000000000000, 0.000000000000000000, 1.000000000000000000 ) ) ;
#20279=CARTESIAN_POINT ( 'NONE',  ( -15.48999599679678951, 146.9999999999999716, -9.500000000000000000 ) ) ;
#20280=VERTEX_POINT ( 'NONE', #14651 ) ;
#20284=AXIS2_PLACEMENT_3D ( 'NONE', #42910, #41860, #25969 ) ;
#20288=ORIENTED_EDGE ( 'NONE', *, *, #37950, .F. ) ;
#20291=SURFACE_STYLE_USAGE ( .BOTH. , #39458 ) ;
#20293=CARTESIAN_POINT ( 'NONE',  ( -9.058813317711338797, 114.4549999999999841, 2.943386871421373563 ) ) ;
#20294=CARTESIAN_POINT ( 'NONE',  ( 45.00000000000000000, 10.69371294336137801, 6.000000000000000888 ) ) ;
#20296=( NAMED_UNIT ( * ) PLANE_ANGLE_UNIT ( ) SI_UNIT ( $, .RADIAN. ) );
#20301=SURFACE_STYLE_FILL_AREA ( #46391 ) ;
#20303=AXIS2_PLACEMENT_3D ( 'NONE', #27753, #66456, #28098 ) ;
#20306=CARTESIAN_POINT ( 'NONE',  ( -2.607480562269075097, 154.2929263765338135, 8.025000000000000355 ) ) ;
#20316=( NAMED_UNIT ( * ) PLANE_ANGLE_UNIT ( ) SI_UNIT ( $, .RADIAN. ) );
#20319=SURFACE_SIDE_STYLE ('',( #57977 ) ) ;
#20320=MECHANICAL_DESIGN_GEOMETRIC_PRESENTATION_REPRESENTATION('',(#68645),#40590);
#20321=DIRECTION ( 'NONE',  ( -0.000000000000000000, -0.000000000000000000, -1.000000000000000000 ) ) ;
#20322=CARTESIAN_POINT ( 'NONE',  ( 72.00000000000000000, 35.92875272052971525, 9.500000000000000000 ) ) ;
#20332=DIRECTION ( 'NONE',  ( 0.000000000000000000, 0.000000000000000000, 1.000000000000000000 ) ) ;
#20334=( LENGTH_UNIT ( ) NAMED_UNIT ( * ) SI_UNIT ( .MILLI., .METRE. ) );
#20337=FACE_OUTER_BOUND ( 'NONE', #32091, .T. ) ;
#20342=ORIENTED_EDGE ( 'NONE', *, *, #31523, .F. ) ;
#20343=DIRECTION ( 'NONE',  ( -0.000000000000000000, -0.000000000000000000, -1.000000000000000000 ) ) ;
#20350=CARTESIAN_POINT ( 'NONE',  ( 5.598654528085809545, 131.2549999999999955, -7.705886871421373741 ) ) ;
#20355=FILL_AREA_STYLE_COLOUR ( '', #42799 ) ;
#20361=CARTESIAN_POINT ( 'NONE',  ( 0.000000000000000000, 145.0570736234661524, -8.025000000000000355 ) ) ;
#20368=VERTEX_POINT ( 'NONE', #15019 ) ;
#20369=( NAMED_UNIT ( * ) SI_UNIT ( $, .STERADIAN. ) SOLID_ANGLE_UNIT ( ) );
#20384=DIRECTION ( 'NONE',  ( 1.000000000000000000, 0.000000000000000000, 0.000000000000000000 ) ) ;
#20385=PRESENTATION_STYLE_ASSIGNMENT (( #69283 ) ) ;
#20388=CARTESIAN_POINT ( 'NONE',  ( 10.01517768586949231, 147.6949999999999932, 1.839758294383810543E-15 ) ) ;
#20389=CYLINDRICAL_SURFACE ( 'NONE', #12674, 0.5000000000000004441 ) ;
#20392=MECHANICAL_DESIGN_GEOMETRIC_PRESENTATION_REPRESENTATION('',(#37316),#42941);
#20393=SURFACE_STYLE_USAGE ( .BOTH. , #10197 ) ;
#20394=CARTESIAN_POINT ( 'NONE',  ( 3.094860106618435136, 152.4049999999999443, -9.525000000000000355 ) ) ;
#20397=CARTESIAN_POINT ( 'NONE',  ( 6.826472737025119919, 127.8929263765338220, 4.959722759717908325 ) ) ;
#20401=SURFACE_STYLE_USAGE ( .BOTH. , #9530 ) ;
#20403=CARTESIAN_POINT ( 'NONE',  ( 48.50000000000000000, 14.49137674618942562, 7.500000000000000000 ) ) ;
#20411=VERTEX_POINT ( 'NONE', #31494 ) ;
#20412=PRESENTATION_STYLE_ASSIGNMENT (( #14432 ) ) ;
#20413=EDGE_CURVE ( 'NONE', #55502, #13013, #14292, .T. ) ;
#20415=AXIS2_PLACEMENT_3D ( 'NONE', #68414, #40307, #35009 ) ;
#20416=CIRCLE ( 'NONE', #46311, 0.4999999999999991118 ) ;
#20419=CARTESIAN_POINT ( 'NONE',  ( 75.00000000000000000, 19.44429231213349141, 6.999999999972111198 ) ) ;
#20420=CARTESIAN_POINT ( 'NONE',  ( 7.632228543268607446, 146.0429263765338135, 2.479861379858954606 ) ) ;
#20423=ADVANCED_FACE ( 'NONE', ( #41405 ), #69101, .T. ) ;
#20424=ORIENTED_EDGE ( 'NONE', *, *, #28901, .T. ) ;
#20426=AXIS2_PLACEMENT_3D ( 'NONE', #50451, #37611, #36404 ) ;
#20433=AXIS2_PLACEMENT_3D ( 'NONE', #25065, #67280, #29283 ) ;
#20438=STYLED_ITEM ( 'NONE', ( #25134 ), #54315 ) ;
#20444=CARTESIAN_POINT ( 'NONE',  ( -8.102448949553181734, 145.8949999999999534, -5.886773742842749790 ) ) ;
#20449=CARTESIAN_POINT ( 'NONE',  ( -40.99999999999998579, 107.7459666924148252, -3.050022167383943383 ) ) ;
#20455=MECHANICAL_DESIGN_GEOMETRIC_PRESENTATION_REPRESENTATION('',(#50787),#46352);
#20459=ORIENTED_EDGE ( 'NONE', *, *, #49668, .T. ) ;
#20461=LINE ( 'NONE', #53180, #55462 ) ;
#20465=CARTESIAN_POINT ( 'NONE',  ( -45.91547277787986303, 9.430195805462179948, 6.024500123752370762 ) ) ;
#20468=ORIENTED_EDGE ( 'NONE', *, *, #24503, .F. ) ;
#20470=VERTEX_POINT ( 'NONE', #48776 ) ;
#20474=ORIENTED_EDGE ( 'NONE', *, *, #49043, .F. ) ;
#20476=DIRECTION ( 'NONE',  ( -0.000000000000000000, 1.000000000000000000, -0.000000000000000000 ) ) ;
#20477=CARTESIAN_POINT ( 'NONE',  ( -5.598654528085808657, 125.6449999999999818, 7.705886871421373741 ) ) ;
#20480=VERTEX_POINT ( 'NONE', #22345 ) ;
#20481=FILL_AREA_STYLE ('',( #26441 ) ) ;
#20482=CARTESIAN_POINT ( 'NONE',  ( -8.102448949553179958, 120.6049999999999756, 5.886773742842747126 ) ) ;
#20484=FILL_AREA_STYLE_COLOUR ( '', #65519 ) ;
#20485=EDGE_LOOP ( 'NONE', ( #7088, #58479, #40835, #2336 ) ) ;
#20486=CARTESIAN_POINT ( 'NONE',  ( 0.000000000000000000, 149.5550000000000068, -9.525000000000000355 ) ) ;
#20487=CARTESIAN_POINT ( 'NONE',  ( 0.000000000000000000, 149.9999999999999716, 0.000000000000000000 ) ) ;
#20490=ADVANCED_FACE ( 'NONE', ( #59973 ), #43839, .T. ) ;
#20495=CARTESIAN_POINT ( 'NONE',  ( 74.65811388300841145, 19.88603796100278487, -6.292893218813454759 ) ) ;
#20499=CARTESIAN_POINT ( 'NONE',  ( 4.325530127497533073, 111.8337402250126900, -6.961252418569971567 ) ) ;
#20502=FILL_AREA_STYLE ('',( #58481 ) ) ;
#20503=ORIENTED_EDGE ( 'NONE', *, *, #40052, .T. ) ;
#20510=ORIENTED_EDGE ( 'NONE', *, *, #35122, .T. ) ;
#20513=FILL_AREA_STYLE_COLOUR ( '', #25795 ) ;
#20516=CONICAL_SURFACE ( 'NONE', #37445, 5.500000000000005329, 0.7853981633974309595 ) ;
#20517=CARTESIAN_POINT ( 'NONE',  ( -1.113559396844004956, 154.5000000000000000, -9.459683423334018570 ) ) ;
#20524=( LENGTH_UNIT ( ) NAMED_UNIT ( * ) SI_UNIT ( .MILLI., .METRE. ) );
#20528=CARTESIAN_POINT ( 'NONE',  ( -8.102448949553181734, 119.4949999999999903, 5.886773742842747126 ) ) ;
#20531=LINE ( 'NONE', #31408, #20151 ) ;
#20533=ORIENTED_EDGE ( 'NONE', *, *, #23124, .F. ) ;
#20537=AXIS2_PLACEMENT_3D ( 'NONE', #52475, #51408, #46881 ) ;
#20540=DIRECTION ( 'NONE',  ( 0.000000000000000000, 0.000000000000000000, 1.000000000000000000 ) ) ;
#20541=ORIENTED_EDGE ( 'NONE', *, *, #32354, .T. ) ;
#20544=DIRECTION ( 'NONE',  ( -1.000000000000000000, -3.469446951953611033E-15, 0.000000000000000000 ) ) ;
#20546=CARTESIAN_POINT ( 'NONE',  ( 8.437984349512095861, 152.1929263765338192, 1.550032578732816828E-15 ) ) ;
#20547=CARTESIAN_POINT ( 'NONE',  ( 6.826472737025119919, 147.0070736234661695, 4.959722759717908325 ) ) ;
#20549=VERTEX_POINT ( 'NONE', #12820 ) ;
#20550=CARTESIAN_POINT ( 'NONE',  ( -83.49999999999997158, 50.00000000000000000, -12.00000000000000000 ) ) ;
#20551=FILL_AREA_STYLE_COLOUR ( '', #61013 ) ;
#20552=VERTEX_POINT ( 'NONE', #40268 ) ;
#20555=STYLED_ITEM ( 'NONE', ( #57135 ), #61294 ) ;
#20557=CARTESIAN_POINT ( 'NONE',  ( 48.81081081081080697, 14.09971791521132900, -7.500000000000000000 ) ) ;
#20558=CARTESIAN_POINT ( 'NONE',  ( -9.827790563157511022E-16, 146.5570736234661524, 8.025000000000000355 ) ) ;
#20560=MECHANICAL_DESIGN_GEOMETRIC_PRESENTATION_REPRESENTATION('',(#23919),#58830);
#20564=LINE ( 'NONE', #42081, #13972 ) ;
#20568=CARTESIAN_POINT ( 'NONE',  ( 4.716976649647099507, 143.6429263765338078, -6.492361379858953008 ) ) ;
#20569=EDGE_CURVE ( 'NONE', #40909, #19597, #55741, .T. ) ;
#20570=CARTESIAN_POINT ( 'NONE',  ( -45.50000000000000000, -2.024042244987997205E-14, -6.999999999999999112 ) ) ;
#20572=EDGE_LOOP ( 'NONE', ( #8011, #18667, #62196, #62975 ) ) ;
#20576=ORIENTED_EDGE ( 'NONE', *, *, #58882, .T. ) ;
#20577=CYLINDRICAL_SURFACE ( 'NONE', #36199, 5.000000000000004441 ) ;
#20579=SURFACE_STYLE_USAGE ( .BOTH. , #52948 ) ;
#20581=DIRECTION ( 'NONE',  ( 0.000000000000000000, 0.000000000000000000, -1.000000000000000000 ) ) ;
#20583=ORIENTED_EDGE ( 'NONE', *, *, #57927, .F. ) ;
#20587=MECHANICAL_DESIGN_GEOMETRIC_PRESENTATION_REPRESENTATION('',(#34086),#1437);
#20589=( LENGTH_UNIT ( ) NAMED_UNIT ( * ) SI_UNIT ( .MILLI., .METRE. ) );
#20592=LINE ( 'NONE', #30783, #22948 ) ;
#20595=CARTESIAN_POINT ( 'NONE',  ( 0.000000000000000000, 118.4449999999999932, -9.525000000000000355 ) ) ;
#20597=MECHANICAL_DESIGN_GEOMETRIC_PRESENTATION_REPRESENTATION('',(#25062),#65486);
#20598=SURFACE_STYLE_FILL_AREA ( #57540 ) ;
#20599=EDGE_CURVE ( 'NONE', #5467, #11645, #50462, .T. ) ;
#20601=VERTEX_POINT ( 'NONE', #7214 ) ;
#20602=( BOUNDED_CURVE ( )  B_SPLINE_CURVE ( 2, ( #12257, #5597, #27045, #43993, #43324, #6633, #59778, #48579, #33724, #54493, #11240 ),
 .UNSPECIFIED., .F., .F. ) 
 B_SPLINE_CURVE_WITH_KNOTS ( ( 3, 2, 2, 2, 2, 3 ),
 ( 0.1176470588235295212, 0.1235294117647059986, 0.1294117647058824760, 0.1352941176470589257, 0.1411764705882354032, 0.1470588235294118806 ),
 .UNSPECIFIED. ) 
 CURVE ( )  GEOMETRIC_REPRESENTATION_ITEM ( )  RATIONAL_B_SPLINE_CURVE ( ( 0.9999999999999991118, 0.9510565162951544194, 1.000000000000000000, 0.9510565162951535312, 1.000000000000000000, 0.9510565162951535312, 1.000000000000000000, 0.9510565162951535312, 1.000000000000000000, 0.9510565162951526430, 1.000000000000000888 ) ) 
 REPRESENTATION_ITEM ( '' )  );
#20604=CARTESIAN_POINT ( 'NONE',  ( 48.50000000000000000, 14.49137674618942562, 7.000000000000000000 ) ) ;
#20605=( NAMED_UNIT ( * ) PLANE_ANGLE_UNIT ( ) SI_UNIT ( $, .RADIAN. ) );
#20607=LINE ( 'NONE', #25867, #16214 ) ;
#20608=LINE ( 'NONE', #473, #25770 ) ;
#20611=AXIS2_PLACEMENT_3D ( 'NONE', #63971, #68933, #31256 ) ;
#20613=VERTEX_POINT ( 'NONE', #50136 ) ;
#20615=STYLED_ITEM ( 'NONE', ( #32100 ), #47057 ) ;
#20616=DIRECTION ( 'NONE',  ( -0.000000000000000000, -0.000000000000000000, -1.000000000000000000 ) ) ;
#20618=UNCERTAINTY_MEASURE_WITH_UNIT (LENGTH_MEASURE( 1.000000000000000082E-05 ), #47102, 'distance_accuracy_value', 'NONE');
#20621=CARTESIAN_POINT ( 'NONE',  ( 10.01517768586949231, 157.8050000000000068, 1.839758294383810543E-15 ) ) ;
#20623=CARTESIAN_POINT ( 'NONE',  ( 41.49999999999998579, 106.9282032302754999, 4.000000000000000000 ) ) ;
#20625=( BOUNDED_CURVE ( )  B_SPLINE_CURVE ( 2, ( #26215, #20958, #10750, #27586, #11778, #5109, #69481, #58581, #16405, #59608, #42808 ),
 .UNSPECIFIED., .F., .F. ) 
 B_SPLINE_CURVE_WITH_KNOTS ( ( 3, 2, 2, 2, 2, 3 ),
 ( 0.4117647058823530326, 0.4176470588235295378, 0.4235294117647059875, 0.4294117647058824372, 0.4352941176470589424, 0.4411764705882353921 ),
 .UNSPECIFIED. ) 
 CURVE ( )  GEOMETRIC_REPRESENTATION_ITEM ( )  RATIONAL_B_SPLINE_CURVE ( ( 0.9999999999999991118, 0.9510565162951544194, 1.000000000000000000, 0.9510565162951535312, 1.000000000000000000, 0.9510565162951535312, 1.000000000000000000, 0.9510565162951535312, 1.000000000000000000, 0.9510565162951526430, 1.000000000000000888 ) ) 
 REPRESENTATION_ITEM ( '' )  );
#20630=STYLED_ITEM ( 'NONE', ( #68235 ), #30860 ) ;
#20634=VECTOR ( 'NONE', #36930, 1000.000000000000000 ) ;
#20635=FILL_AREA_STYLE_COLOUR ( '', #46231 ) ;
#20636=SURFACE_STYLE_FILL_AREA ( #25212 ) ;
#20642=VECTOR ( 'NONE', #6029, 1000.000000000000000 ) ;
#20643=CARTESIAN_POINT ( 'NONE',  ( 6.826472737025121695, 114.6070736234661496, -4.959722759717905660 ) ) ;
#20646=ADVANCED_FACE ( 'NONE', ( #45900 ), #32553, .T. ) ;
#20651=CARTESIAN_POINT ( 'NONE',  ( -75.00000000000000000, 35.50862325381056905, -9.500000000000000000 ) ) ;
#20653=COLOUR_RGB ( '', 0.09019608, 0.27058824, 0.51372549) ;
#20654=CARTESIAN_POINT ( 'NONE',  ( -20.71938756518089875, 149.6378529145318907, 9.985383568374002650 ) ) ;
#20656=ADVANCED_FACE ( 'NONE', ( #52567 ), #19480, .F. ) ;
#20657=CARTESIAN_POINT ( 'NONE',  ( -9.058813317711337021, 120.1549999999999869, -2.943386871421374895 ) ) ;
#20659=ORIENTED_EDGE ( 'NONE', *, *, #40632, .F. ) ;
#20662=CARTESIAN_POINT ( 'NONE',  ( 51.99999999999998579, 1.797044900979284448E-15, 11.50000000000000000 ) ) ;
#20669=( LENGTH_UNIT ( ) NAMED_UNIT ( * ) SI_UNIT ( .MILLI., .METRE. ) );
#20671=CARTESIAN_POINT ( 'NONE',  ( 2.607480562269076430, 152.7929263765338135, -8.025000000000000355 ) ) ;
#20675=ORIENTED_EDGE ( 'NONE', *, *, #50651, .F. ) ;
#20676=( LENGTH_UNIT ( ) NAMED_UNIT ( * ) SI_UNIT ( .MILLI., .METRE. ) );
#20677=CARTESIAN_POINT ( 'NONE',  ( -45.89905495956738690, 9.405628579031729330, 3.000000000000000000 ) ) ;
#20682=CARTESIAN_POINT ( 'NONE',  ( -45.89905495956738690, 9.405628579031731107, -3.000000000000000444 ) ) ;
#20684=CARTESIAN_POINT ( 'NONE',  ( -74.24147510199526323, 8.825811131586496217, 6.400570753484256414 ) ) ;
#20685=CIRCLE ( 'NONE', #69003, 22.49999999999999645 ) ;
#20687=CARTESIAN_POINT ( 'NONE',  ( 74.50000000000000000, 19.99999999999997868, -6.500000000000000000 ) ) ;
#20691=CARTESIAN_POINT ( 'NONE',  ( 72.00000000000000000, 14.49137674618942562, 9.500000000000000000 ) ) ;
#20703=VERTEX_POINT ( 'NONE', #62281 ) ;
#20708=CYLINDRICAL_SURFACE ( 'NONE', #49986, 0.5000000000000004441 ) ;
#20709=CIRCLE ( 'NONE', #63382, 0.5000000000000004441 ) ;
#20711=CARTESIAN_POINT ( 'NONE',  ( -9.058813317711338797, 129.4549999999999841, 2.943386871421373563 ) ) ;
#20712=CARTESIAN_POINT ( 'NONE',  ( -75.00000000000000000, 7.967158085982124049, -7.000000000000000888 ) ) ;
#20714=COLOUR_RGB ( '', 0.31764706, 0.68627451, 0.89019608) ;
#20716=DIRECTION ( 'NONE',  ( 0.000000000000000000, 0.000000000000000000, 1.000000000000000000 ) ) ;
#20721=CARTESIAN_POINT ( 'NONE',  ( -8.437984349512095861, 132.6929263765338192, -5.166775262442723748E-16 ) ) ;
#20724=EDGE_CURVE ( 'NONE', #38702, #36309, #50507, .T. ) ;
#20726=CARTESIAN_POINT ( 'NONE',  ( -48.00000000000000000, 99.99999999999992895, 7.500000000000000000 ) ) ;
#20727=DIRECTION ( 'NONE',  ( 0.7833176619561891263, 0.6216216216216174928, -0.000000000000000000 ) ) ;
#20732=( NAMED_UNIT ( * ) SI_UNIT ( $, .STERADIAN. ) SOLID_ANGLE_UNIT ( ) );
#20733=MECHANICAL_DESIGN_GEOMETRIC_PRESENTATION_REPRESENTATION('',(#69049),#57798);
#20734=( BOUNDED_SURFACE ( )  B_SPLINE_SURFACE ( 3, 2, ( 
 ( #8894, #3570, #40938 ),
 ( #51458, #30319, #25073 ),
 ( #62362, #46580, #29658 ),
 ( #50773, #19795, #50421 ),
 ( #34572, #2145, #18415 ),
 ( #39902, #13119, #56025 ),
 ( #7841, #24027, #45536 ),
 ( #66952, #18752, #61998 ),
 ( #51127, #9947, #41628 ),
 ( #4646, #58472, #48301 ) ),
 .UNSPECIFIED., .F., .F., .F. ) 
 B_SPLINE_SURFACE_WITH_KNOTS ( ( 4, 2, 2, 2, 4 ),
 ( 3, 3 ),
 ( 0.0004231141141892710367, 0.0008386083364002310404, 0.001254102558611191152, 0.001669596780822151265, 0.002085091003033111377 ),
 ( 0.000000000000000000, 1.000000000000000000 ),
 .UNSPECIFIED. ) 
 GEOMETRIC_REPRESENTATION_ITEM ( )  RATIONAL_B_SPLINE_SURFACE ( (
 ( 1.000000000000000000, 0.7071067811865573427, 1.000000000000000000),
 ( 1.000000000000000000, 0.7275888720224806816, 1.000000000000000000),
 ( 1.000000000000000000, 0.7463828630404263365, 1.000000000000000000),
 ( 1.000000000000000000, 0.7812714640742435268, 1.000000000000000000),
 ( 1.000000000000000000, 0.7963642535525788935, 1.000000000000000000),
 ( 1.000000000000000000, 0.8224433532025096083, 1.000000000000000000),
 ( 1.000000000000000000, 0.8326146287104877475, 1.000000000000000000),
 ( 1.000000000000000000, 0.8468497872537316118, 1.000000000000000000),
 ( 1.000000000000000000, 0.8504932968929420634, 1.000000000000000000),
 ( 1.000000000000000000, 0.8505317485662416965, 1.000000000000000000) ) ) 
 REPRESENTATION_ITEM ( '' )  SURFACE ( )  );
#20736=AXIS2_PLACEMENT_3D ( 'NONE', #19989, #51684, #31235 ) ;
#20744=CARTESIAN_POINT ( 'NONE',  ( 4.716976649647096842, 128.8570736234661638, 6.492361379858953896 ) ) ;
#20745=EDGE_CURVE ( 'NONE', #53126, #38818, #23951, .T. ) ;
#20747=( LENGTH_UNIT ( ) NAMED_UNIT ( * ) SI_UNIT ( .MILLI., .METRE. ) );
#20749=ORIENTED_EDGE ( 'NONE', *, *, #60564, .F. ) ;
#20751=CARTESIAN_POINT ( 'NONE',  ( 9.058813317711338797, 153.8449999999999704, -2.943386871421372675 ) ) ;
#20754=ORIENTED_EDGE ( 'NONE', *, *, #50683, .F. ) ;
#20757=CARTESIAN_POINT ( 'NONE',  ( -5.598654528085806881, 152.8549999999999898, -7.705886871421374629 ) ) ;
#20760=ORIENTED_EDGE ( 'NONE', *, *, #60080, .T. ) ;
#20761=CARTESIAN_POINT ( 'NONE',  ( -9.827790563157511022E-16, 121.4429263765338050, 8.025000000000000355 ) ) ;
#20763=UNCERTAINTY_MEASURE_WITH_UNIT (LENGTH_MEASURE( 1.000000000000000082E-05 ), #3119, 'distance_accuracy_value', 'NONE');
#20764=( NAMED_UNIT ( * ) SI_UNIT ( $, .STERADIAN. ) SOLID_ANGLE_UNIT ( ) );
#20765=CARTESIAN_POINT ( 'NONE',  ( 44.99999999999999289, 10.00436330937146145, 6.147562757269795952 ) ) ;
#20769=EDGE_LOOP ( 'NONE', ( #15732, #13267, #2354 ) ) ;
#20772=AXIS2_PLACEMENT_3D ( 'NONE', #18495, #39624, #49816 ) ;
#20775=ORIENTED_EDGE ( 'NONE', *, *, #16800, .F. ) ;
#20777=UNCERTAINTY_MEASURE_WITH_UNIT (LENGTH_MEASURE( 1.000000000000000082E-05 ), #1128, 'distance_accuracy_value', 'NONE');
#20779=CARTESIAN_POINT ( 'NONE',  ( -48.50000000000000000, 14.49137674618942384, -7.500000000000000000 ) ) ;
#20780=CARTESIAN_POINT ( 'NONE',  ( 4.716976649647096842, 145.7429263765338305, 6.492361379858953896 ) ) ;
#20782=CIRCLE ( 'NONE', #3869, 8.999999999999994671 ) ;
#20790=CARTESIAN_POINT ( 'NONE',  ( 54.50000000000002132, 2.470600640510325790E-15, 12.00000000000000000 ) ) ;
#20794=ORIENTED_EDGE ( 'NONE', *, *, #32984, .T. ) ;
#20796=AXIS2_PLACEMENT_3D ( 'NONE', #20623, #62483, #42136 ) ;
#20799=SURFACE_STYLE_FILL_AREA ( #68993 ) ;
#20801=CARTESIAN_POINT ( 'NONE',  ( -3.094860106618432471, 148.5949999999999704, -9.525000000000000355 ) ) ;
#20803=( LENGTH_UNIT ( ) NAMED_UNIT ( * ) SI_UNIT ( .MILLI., .METRE. ) );
#20805=UNCERTAINTY_MEASURE_WITH_UNIT (LENGTH_MEASURE( 1.000000000000000082E-05 ), #34571, 'distance_accuracy_value', 'NONE');
#20807=AXIS2_PLACEMENT_3D ( 'NONE', #14026, #62882, #52377 ) ;
#20808=VERTEX_POINT ( 'NONE', #13387 ) ;
#20814=( GEOMETRIC_REPRESENTATION_CONTEXT ( 3 ) GLOBAL_UNCERTAINTY_ASSIGNED_CONTEXT ( ( #16507 ) ) GLOBAL_UNIT_ASSIGNED_CONTEXT ( ( #48435, #59262, #31855 ) ) REPRESENTATION_CONTEXT ( 'NONE', 'WORKASPACE' ) );
#20817=COLOUR_RGB ( '', 0.72549020, 0.75294118, 0.79215686) ;
#20818=SURFACE_SIDE_STYLE ('',( #69007 ) ) ;
#20821=LINE ( 'NONE', #4243, #18416 ) ;
#20823=CARTESIAN_POINT ( 'NONE',  ( -45.00000000000000000, 9.609776836748578077, 6.329322064279326199 ) ) ;
#20824=CARTESIAN_POINT ( 'NONE',  ( 34.99999999999992895, 109.9999999999999858, -9.500000000000000000 ) ) ;
#20825=ORIENTED_EDGE ( 'NONE', *, *, #52921, .F. ) ;
#20828=ORIENTED_EDGE ( 'NONE', *, *, #50526, .F. ) ;
#20834=EDGE_CURVE ( 'NONE', #23161, #21193, #22433, .T. ) ;
#20836=CARTESIAN_POINT ( 'NONE',  ( 10.01517768586949231, 117.6949999999999790, 1.839758294383810543E-15 ) ) ;
#20837=DIRECTION ( 'NONE',  ( 0.000000000000000000, -0.7071067811865469066, -0.7071067811865482389 ) ) ;
#20838=CIRCLE ( 'NONE', #10740, 0.5000000000000004441 ) ;
#20839=ORIENTED_EDGE ( 'NONE', *, *, #39057, .F. ) ;
#20841=CARTESIAN_POINT ( 'NONE',  ( 9.058813317711338797, 121.9549999999999841, -2.943386871421372675 ) ) ;
#20847=CARTESIAN_POINT ( 'NONE',  ( -1.166476076187854022E-15, 151.0550000000000068, 9.525000000000000355 ) ) ;
#20850=EDGE_CURVE ( 'NONE', #9272, #61826, #68481, .T. ) ;
#20852=DIRECTION ( 'NONE',  ( 1.000000000000000000, 0.000000000000000000, 0.000000000000000000 ) ) ;
#20853=VERTEX_POINT ( 'NONE', #18649 ) ;
#20859=CARTESIAN_POINT ( 'NONE',  ( 0.000000000000000000, 111.9999999999999858, 0.000000000000000000 ) ) ;
#20862=FACE_OUTER_BOUND ( 'NONE', #42694, .T. ) ;
#20863=ORIENTED_EDGE ( 'NONE', *, *, #1631, .T. ) ;
#20865=FILL_AREA_STYLE_COLOUR ( '', #50519 ) ;
#20871=CIRCLE ( 'NONE', #53451, 0.5000000000000004441 ) ;
#20872=CARTESIAN_POINT ( 'NONE',  ( 5.598654528085805993, 150.2449999999999761, 7.705886871421374629 ) ) ;
#20879=CARTESIAN_POINT ( 'NONE',  ( -9.058813317711337021, 116.0449999999999875, -2.943386871421374895 ) ) ;
#20884=AXIS2_PLACEMENT_3D ( 'NONE', #6978, #17885, #23170 ) ;
#20885=FILL_AREA_STYLE_COLOUR ( '', #27849 ) ;
#20886=ORIENTED_EDGE ( 'NONE', *, *, #30898, .F. ) ;
#20890=EDGE_CURVE ( 'NONE', #28212, #12977, #60622, .T. ) ;
#20898=EDGE_CURVE ( 'NONE', #55490, #41057, #39334, .T. ) ;
#20900=SURFACE_STYLE_USAGE ( .BOTH. , #32462 ) ;
#20906=ORIENTED_EDGE ( 'NONE', *, *, #41645, .T. ) ;
#20908=( NAMED_UNIT ( * ) PLANE_ANGLE_UNIT ( ) SI_UNIT ( $, .RADIAN. ) );
#20909=EDGE_CURVE ( 'NONE', #27901, #54497, #66845, .T. ) ;
#20911=MECHANICAL_DESIGN_GEOMETRIC_PRESENTATION_REPRESENTATION('',(#5166),#44553);
#20915=AXIS2_PLACEMENT_3D ( 'NONE', #65006, #12934, #28044 ) ;
#20916=( LENGTH_UNIT ( ) NAMED_UNIT ( * ) SI_UNIT ( .MILLI., .METRE. ) );
#20917=CARTESIAN_POINT ( 'NONE',  ( -4.716976649647097730, 139.3570736234661638, -6.492361379858953896 ) ) ;
#20922=UNCERTAINTY_MEASURE_WITH_UNIT (LENGTH_MEASURE( 1.000000000000000082E-05 ), #37755, 'distance_accuracy_value', 'NONE');
#20924=VERTEX_POINT ( 'NONE', #51000 ) ;
#20926=( GEOMETRIC_REPRESENTATION_CONTEXT ( 3 ) GLOBAL_UNCERTAINTY_ASSIGNED_CONTEXT ( ( #41205 ) ) GLOBAL_UNIT_ASSIGNED_CONTEXT ( ( #36626, #4896, #31264 ) ) REPRESENTATION_CONTEXT ( 'NONE', 'WORKASPACE' ) );
#20930=STYLED_ITEM ( 'NONE', ( #56393 ), #1457 ) ;
#20933=EDGE_LOOP ( 'NONE', ( #54475, #60231, #68976, #32346 ) ) ;
#20937=ORIENTED_EDGE ( 'NONE', *, *, #24599, .F. ) ;
#20941=CARTESIAN_POINT ( 'NONE',  ( -74.99999999999998579, 8.062885929673678120, 5.900610682603717017 ) ) ;
#20944=ORIENTED_EDGE ( 'NONE', *, *, #12714, .T. ) ;
#20945=LINE ( 'NONE', #37865, #14499 ) ;
#20948=CARTESIAN_POINT ( 'NONE',  ( -8.102448949553179958, 119.4949999999999903, 5.886773742842747126 ) ) ;
#20951=CARTESIAN_POINT ( 'NONE',  ( -1.113559396844004956, 154.5000000000000000, -9.459683423334018570 ) ) ;
#20954=FILL_AREA_STYLE_COLOUR ( '', #33984 ) ;
#20955=DIRECTION ( 'NONE',  ( 0.000000000000000000, -1.000000000000000000, 0.000000000000000000 ) ) ;
#20958=CARTESIAN_POINT ( 'NONE',  ( -2.607480562269115509, 130.2070736234661865, -8.024999999999970157 ) ) ;
#20965=ORIENTED_EDGE ( 'NONE', *, *, #57927, .T. ) ;
#20967=CARTESIAN_POINT ( 'NONE',  ( 20.71231517720797655, 149.4999999999999716, -10.00000000000000000 ) ) ;
#20969=DIRECTION ( 'NONE',  ( -1.000000000000000000, 0.000000000000000000, 0.000000000000000000 ) ) ;
#20973=CARTESIAN_POINT ( 'NONE',  ( 0.000000000000000000, 87.30187232391182306, 0.000000000000000000 ) ) ;
#20974=DIRECTION ( 'NONE',  ( -1.000000000000000000, 0.000000000000000000, 0.000000000000000000 ) ) ;
#20975=( NAMED_UNIT ( * ) SI_UNIT ( $, .STERADIAN. ) SOLID_ANGLE_UNIT ( ) );
#20980=DIRECTION ( 'NONE',  ( -1.156482317317873451E-16, 1.000000000000000000, 0.000000000000000000 ) ) ;
#20981=CARTESIAN_POINT ( 'NONE',  ( -4.716976649647098618, 139.1429263765338078, 6.492361379858953008 ) ) ;
#20986=CARTESIAN_POINT ( 'NONE',  ( 4.716976649647099507, 117.7570736234661553, -6.492361379858953008 ) ) ;
#20988=EDGE_CURVE ( 'NONE', #65204, #29181, #2217, .T. ) ;
#20993=COLOUR_RGB ( '', 0.09019608, 0.27058824, 0.51372549) ;
#20998=CARTESIAN_POINT ( 'NONE',  ( 8.102448949553183510, 119.1049999999999756, -5.886773742842746238 ) ) ;
#20999=PRESENTATION_STYLE_ASSIGNMENT (( #69523 ) ) ;
#21001=AXIS2_PLACEMENT_3D ( 'NONE', #49148, #17487, #23413 ) ;
#21006=DIRECTION ( 'NONE',  ( 0.000000000000000000, 1.000000000000000000, 0.000000000000000000 ) ) ;
#21007=( NAMED_UNIT ( * ) PLANE_ANGLE_UNIT ( ) SI_UNIT ( $, .RADIAN. ) );
#21008=EDGE_LOOP ( 'NONE', ( #15697, #64650 ) ) ;
#21009=CARTESIAN_POINT ( 'NONE',  ( -7.632228543268607446, 153.5429263765338419, -2.479861379858953718 ) ) ;
#21010=( BOUNDED_CURVE ( )  B_SPLINE_CURVE ( 2, ( #58844, #714, #12031, #54242, #43065, #6744, #5696, #48679, #11335, #59514, #65498 ),
 .UNSPECIFIED., .F., .F. ) 
 B_SPLINE_CURVE_WITH_KNOTS ( ( 3, 2, 2, 2, 2, 3 ),
 ( 0.6764705882352939348, 0.6823529411764703845, 0.6882352941176468342, 0.6941176470588232839, 0.6999999999999997335, 0.7058823529411762943 ),
 .UNSPECIFIED. ) 
 CURVE ( )  GEOMETRIC_REPRESENTATION_ITEM ( )  RATIONAL_B_SPLINE_CURVE ( ( 1.000000000000001776, 0.9510565162951516438, 1.000000000000000000, 0.9510565162951535312, 1.000000000000000000, 0.9510565162951535312, 1.000000000000000000, 0.9510565162951535312, 1.000000000000000000, 0.9510565162951554186, 0.9999999999999981126 ) ) 
 REPRESENTATION_ITEM ( '' )  );
#21012=VECTOR ( 'NONE', #49653, 1000.000000000000000 ) ;
#21013=CARTESIAN_POINT ( 'NONE',  ( -20.83091330386927353, 149.9514755777528023, -9.751095921151032186 ) ) ;
#21014=CARTESIAN_POINT ( 'NONE',  ( 21.02379601146600763, 114.6388938931947763, -10.00000000000000000 ) ) ;
#21016=CARTESIAN_POINT ( 'NONE',  ( 6.826472737025121695, 128.4929263765338021, -4.959722759717905660 ) ) ;
#21018=FILL_AREA_STYLE_COLOUR ( '', #11633 ) ;
#21019=CARTESIAN_POINT ( 'NONE',  ( -60.00000000000000000, -2.024042244987997205E-14, 12.00000000000000000 ) ) ;
#21020=FACE_OUTER_BOUND ( 'NONE', #48040, .T. ) ;
#21021=LINE ( 'NONE', #53390, #21816 ) ;
#21023=CARTESIAN_POINT ( 'NONE',  ( 6.826472737025119919, 115.8929263765338220, 4.959722759717908325 ) ) ;
#21026=ORIENTED_EDGE ( 'NONE', *, *, #8594, .F. ) ;
#21030=( NAMED_UNIT ( * ) PLANE_ANGLE_UNIT ( ) SI_UNIT ( $, .RADIAN. ) );
#21032=FILL_AREA_STYLE ('',( #47838 ) ) ;
#21037=( NAMED_UNIT ( * ) PLANE_ANGLE_UNIT ( ) SI_UNIT ( $, .RADIAN. ) );
#21039=DIRECTION ( 'NONE',  ( -0.000000000000000000, -0.000000000000000000, -1.000000000000000000 ) ) ;
#21043=LINE ( 'NONE', #11173, #19631 ) ;
#21045=CARTESIAN_POINT ( 'NONE',  ( -74.49999999999998579, 36.50926243676796190, -10.00000000000000000 ) ) ;
#21047=EDGE_CURVE ( 'NONE', #34213, #52924, #29186, .T. ) ;
#21050=CARTESIAN_POINT ( 'NONE',  ( -8.102448949553181734, 129.0049999999999670, -5.886773742842749790 ) ) ;
#21052=CARTESIAN_POINT ( 'NONE',  ( -15.98999599679679839, 146.4999999999999716, -7.500000000000000000 ) ) ;
#21055=DIRECTION ( 'NONE',  ( 7.080503983578803083E-17, -1.000000000000000000, -0.000000000000000000 ) ) ;
#21056=ORIENTED_EDGE ( 'NONE', *, *, #1051, .F. ) ;
#21057=ADVANCED_FACE ( 'NONE', ( #1542 ), #17789, .F. ) ;
#21059=STYLED_ITEM ( 'NONE', ( #12462 ), #67433 ) ;
#21060=EDGE_CURVE ( 'NONE', #24259, #51230, #60665, .T. ) ;
#21061=DIRECTION ( 'NONE',  ( -0.000000000000000000, -0.000000000000000000, -1.000000000000000000 ) ) ;
#21062=SURFACE_STYLE_USAGE ( .BOTH. , #21757 ) ;
#21063=CARTESIAN_POINT ( 'NONE',  ( -4.716976649647098618, 137.2570736234661695, 6.492361379858953008 ) ) ;
#21066=CARTESIAN_POINT ( 'NONE',  ( 74.50000000000000000, 20.36037961002804053, -6.500000000000000000 ) ) ;
#21071=VERTEX_POINT ( 'NONE', #13176 ) ;
#21073=ORIENTED_EDGE ( 'NONE', *, *, #20599, .F. ) ;
#21076=EDGE_LOOP ( 'NONE', ( #26789, #40669 ) ) ;
#21078=ORIENTED_EDGE ( 'NONE', *, *, #41194, .F. ) ;
#21080=CARTESIAN_POINT ( 'NONE',  ( 34.99999999999992895, 112.9999999999999858, 9.500000000000000000 ) ) ;
#21081=CARTESIAN_POINT ( 'NONE',  ( -8.102448949553181734, 152.4949999999999477, 5.886773742842747126 ) ) ;
#21084=CARTESIAN_POINT ( 'NONE',  ( 3.094860106618431583, 151.2049999999999841, 9.525000000000000355 ) ) ;
#21089=CARTESIAN_POINT ( 'NONE',  ( -7.632228543268607446, 129.5429263765338135, -2.479861379858953718 ) ) ;
#21090=DIRECTION ( 'NONE',  ( 1.000000000000000000, 0.000000000000000000, 0.000000000000000000 ) ) ;
#21092=STYLED_ITEM ( 'NONE', ( #50966 ), #65643 ) ;
#21094=FILL_AREA_STYLE ('',( #32675 ) ) ;
#21101=CIRCLE ( 'NONE', #35720, 9.999999999999998224 ) ;
#21104=LINE ( 'NONE', #33054, #21652 ) ;
#21108=DIRECTION ( 'NONE',  ( 0.000000000000000000, 1.000000000000000000, -0.000000000000000000 ) ) ;
#21110=ORIENTED_EDGE ( 'NONE', *, *, #64809, .F. ) ;
#21112=STYLED_ITEM ( 'NONE', ( #4370 ), #41361 ) ;
#21122=ADVANCED_FACE ( 'NONE', ( #27945 ), #23741, .F. ) ;
#21123=CARTESIAN_POINT ( 'NONE',  ( -15.98999599679679839, 118.4999999999999716, 7.500000000000000000 ) ) ;
#21128=CARTESIAN_POINT ( 'NONE',  ( -5.598654528085808657, 152.6449999999999818, 7.705886871421373741 ) ) ;
#21131=( BOUNDED_SURFACE ( )  B_SPLINE_SURFACE ( 3, 2, ( 
 ( #31467, #16723, #52954 ),
 ( #69135, #20941, #23348 ),
 ( #55715, #44852, #50788 ),
 ( #66253, #61325, #2538 ),
 ( #13136, #50110, #59939 ),
 ( #18437, #39922, #66619 ),
 ( #12433, #45554, #12792 ),
 ( #60293, #24048, #22667 ),
 ( #60972, #56044, #18081 ),
 ( #2165, #28242, #1838 ),
 ( #39569, #34258, #17417 ),
 ( #49408, #34589, #23697 ),
 ( #17749, #7522, #7857 ),
 ( #44170, #50437, #33224 ),
 ( #6817, #29310, #45198 ),
 ( #28948, #66974, #38547 ),
 ( #11756, #49753, #54662 ),
 ( #6465, #27899, #38882 ) ),
 .UNSPECIFIED., .F., .F., .T. ) 
 B_SPLINE_SURFACE_WITH_KNOTS ( ( 4, 2, 2, 2, 2, 2, 2, 2, 4 ),
 ( 3, 3 ),
 ( 0.0008275086428995133761, 0.0009765612317269614347, 0.001125613820554409493, 0.001274666409381857660, 0.001423718998209305611, 0.001721824175864201728, 0.002019929353519097845, 0.002616139708828890513, 0.003212350064138682747 ),
 ( 0.000000000000000000, 1.000000000000000000 ),
 .UNSPECIFIED. ) 
 GEOMETRIC_REPRESENTATION_ITEM ( )  RATIONAL_B_SPLINE_SURFACE ( (
 ( 1.000000000000000000, 0.2907356542125049681, 1.000000000000000000),
 ( 1.000000000000000000, 0.2907339171233887520, 1.000000000000000000),
 ( 1.000000000000000000, 0.2933218126492017630, 1.000000000000000000),
 ( 1.000000000000000000, 0.3027174795993979872, 1.000000000000000000),
 ( 1.000000000000000000, 0.3096405143333775256, 1.000000000000000000),
 ( 1.000000000000000000, 0.3258903432231474162, 1.000000000000000000),
 ( 1.000000000000000000, 0.3352112554374609976, 1.000000000000000000),
 ( 1.000000000000000000, 0.3552330613601621945, 1.000000000000000000),
 ( 1.000000000000000000, 0.3657822831407469000, 1.000000000000000000),
 ( 1.000000000000000000, 0.3977110304216009973, 1.000000000000000000),
 ( 1.000000000000000000, 0.4197187326556824361, 1.000000000000000000),
 ( 1.000000000000000000, 0.4623670587024229506, 1.000000000000000000),
 ( 1.000000000000000000, 0.4829316641227751616, 1.000000000000000000),
 ( 1.000000000000000000, 0.5424860661042288923, 1.000000000000000000),
 ( 1.000000000000000000, 0.5795047887218846006, 1.000000000000000000),
 ( 1.000000000000000000, 0.6470713767466169664, 1.000000000000000000),
 ( 1.000000000000000000, 0.6780453138456912221, 1.000000000000000000),
 ( 1.000000000000000000, 0.7071067811865469066, 1.000000000000000000) ) ) 
 REPRESENTATION_ITEM ( '' )  SURFACE ( )  );
#21132=CYLINDRICAL_SURFACE ( 'NONE', #60644, 0.5000000000000004441 ) ;
#21135=DIRECTION ( 'NONE',  ( 0.000000000000000000, 0.000000000000000000, 1.000000000000000000 ) ) ;
#21139=CARTESIAN_POINT ( 'NONE',  ( 48.00000000000000000, 99.99999999999992895, 7.000000000000000000 ) ) ;
#21146=CARTESIAN_POINT ( 'NONE',  ( -45.78727775085652496, 8.937790484662075485, 6.368793980437917668 ) ) ;
#21150=ORIENTED_EDGE ( 'NONE', *, *, #38950, .F. ) ;
#21152=EDGE_CURVE ( 'NONE', #37052, #35876, #33151, .T. ) ;
#21154=FACE_OUTER_BOUND ( 'NONE', #68511, .T. ) ;
#21155=VERTEX_POINT ( 'NONE', #62746 ) ;
#21156=DIRECTION ( 'NONE',  ( 0.000000000000000000, 0.000000000000000000, -1.000000000000000000 ) ) ;
#21158=CARTESIAN_POINT ( 'NONE',  ( -3.094860106618432471, 118.5949999999999847, -9.525000000000000355 ) ) ;
#21159=DIRECTION ( 'NONE',  ( -0.000000000000000000, -0.000000000000000000, -1.000000000000000000 ) ) ;
#21161=SURFACE_SIDE_STYLE ('',( #41988 ) ) ;
#21162=CARTESIAN_POINT ( 'NONE',  ( -3.094860106618432471, 125.7049999999999841, -9.525000000000000355 ) ) ;
#21166=CARTESIAN_POINT ( 'NONE',  ( -41.01803665359474138, 107.7206116573237722, -3.151333386623310862 ) ) ;
#21168=CARTESIAN_POINT ( 'NONE',  ( -9.058813317711338797, 144.4550000000000125, 2.943386871421373563 ) ) ;
#21171=LINE ( 'NONE', #57789, #51909 ) ;
#21172=CARTESIAN_POINT ( 'NONE',  ( -35.00000000000003553, 10.49999999999998224, -3.500000000000000000 ) ) ;
#21175=SURFACE_STYLE_USAGE ( .BOTH. , #64452 ) ;
#21177=VERTEX_POINT ( 'NONE', #41342 ) ;
#21180=FACE_OUTER_BOUND ( 'NONE', #5416, .T. ) ;
#21184=DIRECTION ( 'NONE',  ( -1.000000000000000000, 0.000000000000000000, 0.000000000000000000 ) ) ;
#21189=AXIS2_PLACEMENT_3D ( 'NONE', #2184, #7877, #28262 ) ;
#21191=FACE_OUTER_BOUND ( 'NONE', #25312, .T. ) ;
#21193=VERTEX_POINT ( 'NONE', #40289 ) ;
#21194=DIRECTION ( 'NONE',  ( -0.000000000000000000, -1.000000000000000000, -0.000000000000000000 ) ) ;
#21198=SURFACE_SIDE_STYLE ('',( #15285 ) ) ;
#21200=EDGE_CURVE ( 'NONE', #54121, #30484, #64106, .T. ) ;
#21201=CARTESIAN_POINT ( 'NONE',  ( -5.598654528085808657, 122.6449999999999960, 7.705886871421373741 ) ) ;
#21208=VECTOR ( 'NONE', #48859, 1000.000000000000000 ) ;
#21212=ADVANCED_FACE ( 'NONE', ( #14237 ), #7914, .F. ) ;
#21213=( NAMED_UNIT ( * ) SI_UNIT ( $, .STERADIAN. ) SOLID_ANGLE_UNIT ( ) );
#21216=CARTESIAN_POINT ( 'NONE',  ( -20.44241585271047867, 115.3856657692246444, -10.00000000000000000 ) ) ;
#21220=CARTESIAN_POINT ( 'NONE',  ( 54.99999999999999289, 2.409368300552961372E-15, -11.50000000000001066 ) ) ;
#21221=CARTESIAN_POINT ( 'NONE',  ( 0.000000000000000000, 139.0570736234661808, -8.025000000000000355 ) ) ;
#21222=DIRECTION ( 'NONE',  ( -0.000000000000000000, -1.000000000000000000, 0.000000000000000000 ) ) ;
#21227=DIRECTION ( 'NONE',  ( -0.000000000000000000, -0.000000000000000000, -1.000000000000000000 ) ) ;
#21228=SURFACE_STYLE_USAGE ( .BOTH. , #37829 ) ;
#21230=( GEOMETRIC_REPRESENTATION_CONTEXT ( 3 ) GLOBAL_UNCERTAINTY_ASSIGNED_CONTEXT ( ( #42602 ) ) GLOBAL_UNIT_ASSIGNED_CONTEXT ( ( #5705, #11342, #47668 ) ) REPRESENTATION_CONTEXT ( 'NONE', 'WORKASPACE' ) );
#21231=CARTESIAN_POINT ( 'NONE',  ( 4.716976649647099507, 141.7570736234661410, -6.492361379858953008 ) ) ;
#21232=STYLED_ITEM ( 'NONE', ( #12108 ), #19668 ) ;
#21236=MECHANICAL_DESIGN_GEOMETRIC_PRESENTATION_REPRESENTATION('',(#20137),#69552);
#21238=CARTESIAN_POINT ( 'NONE',  ( -71.74137931034481142, 36.89918356738973415, -9.500000000000000000 ) ) ;
#21239=DIRECTION ( 'NONE',  ( 0.7833176619561811327, -0.6216216216216277068, -4.313366480807242114E-15 ) ) ;
#21243=VERTEX_POINT ( 'NONE', #51879 ) ;
#21244=FACE_OUTER_BOUND ( 'NONE', #42672, .T. ) ;
#21246=VERTEX_POINT ( 'NONE', #21221 ) ;
#21247=FILL_AREA_STYLE ('',( #49396 ) ) ;
#21251=DIRECTION ( 'NONE',  ( 0.000000000000000000, -0.000000000000000000, 1.000000000000000000 ) ) ;
#21252=FILL_AREA_STYLE ('',( #16034 ) ) ;
#21253=VERTEX_POINT ( 'NONE', #4710 ) ;
#21259=LINE ( 'NONE', #30784, #7487 ) ;
#21260=( GEOMETRIC_REPRESENTATION_CONTEXT ( 3 ) GLOBAL_UNCERTAINTY_ASSIGNED_CONTEXT ( ( #4567 ) ) GLOBAL_UNIT_ASSIGNED_CONTEXT ( ( #18889, #61125, #19601 ) ) REPRESENTATION_CONTEXT ( 'NONE', 'WORKASPACE' ) );
#21263=CARTESIAN_POINT ( 'NONE',  ( -9.058813317711337021, 125.0449999999999875, -2.943386871421374895 ) ) ;
#21269=CARTESIAN_POINT ( 'NONE',  ( -0.7418830492402813670, 154.4749711138048838, -9.478234102103829883 ) ) ;
#21272=DIRECTION ( 'NONE',  ( -1.000000000000000000, 0.000000000000000000, 0.000000000000000000 ) ) ;
#21274=CARTESIAN_POINT ( 'NONE',  ( 0.000000000000000000, 148.0570736234661524, -8.025000000000000355 ) ) ;
#21278=ADVANCED_FACE ( 'NONE', ( #10692 ), #21947, .F. ) ;
#21280=CARTESIAN_POINT ( 'NONE',  ( 75.00000000000000000, 20.36037961002804408, 6.585786437626904188 ) ) ;
#21284=EDGE_CURVE ( 'NONE', #41256, #66255, #26334, .T. ) ;
#21285=ORIENTED_EDGE ( 'NONE', *, *, #4425, .F. ) ;
#21286=AXIS2_PLACEMENT_3D ( 'NONE', #45141, #55657, #61273 ) ;
#21290=EDGE_CURVE ( 'NONE', #7249, #37399, #47288, .T. ) ;
#21291=SURFACE_STYLE_USAGE ( .BOTH. , #69493 ) ;
#21294=SURFACE_STYLE_USAGE ( .BOTH. , #54349 ) ;
#21296=DIRECTION ( 'NONE',  ( 0.000000000000000000, 0.000000000000000000, -1.000000000000000000 ) ) ;
#21297=SURFACE_SIDE_STYLE ('',( #15030 ) ) ;
#21298=FILL_AREA_STYLE ('',( #26571 ) ) ;
#21302=UNCERTAINTY_MEASURE_WITH_UNIT (LENGTH_MEASURE( 1.000000000000000082E-05 ), #23714, 'distance_accuracy_value', 'NONE');
#21307=CIRCLE ( 'NONE', #846, 1.000000000000000888 ) ;
#21313=AXIS2_PLACEMENT_3D ( 'NONE', #1726, #11980, #33439 ) ;
#21314=CARTESIAN_POINT ( 'NONE',  ( -7.632228543268607446, 118.6570736234661609, -2.479861379858953718 ) ) ;
#21317=CARTESIAN_POINT ( 'NONE',  ( -19.98431065987488608, 114.9999999999999574, 10.47133983857574613 ) ) ;
#21326=CARTESIAN_POINT ( 'NONE',  ( -9.058813317711337021, 123.1549999999999869, -2.943386871421374895 ) ) ;
#21327=( LENGTH_UNIT ( ) NAMED_UNIT ( * ) SI_UNIT ( .MILLI., .METRE. ) );
#21329=VECTOR ( 'NONE', #56242, 1000.000000000000000 ) ;
#21333=COLOUR_RGB ( '', 0.08235294, 0.09019608, 0.10196078) ;
#21335=DIRECTION ( 'NONE',  ( -0.000000000000000000, -0.000000000000000000, -1.000000000000000000 ) ) ;
#21336=SURFACE_SIDE_STYLE ('',( #64939 ) ) ;
#21337=ORIENTED_EDGE ( 'NONE', *, *, #44771, .F. ) ;
#21338=CARTESIAN_POINT ( 'NONE',  ( -4.716976649647097730, 150.2429263765338021, -6.492361379858953896 ) ) ;
#21340=SURFACE_SIDE_STYLE ('',( #45191 ) ) ;
#21343=CARTESIAN_POINT ( 'NONE',  ( 20.17763807713225432, 115.4773716707933460, -10.00000000000000000 ) ) ;
#21350=( GEOMETRIC_REPRESENTATION_CONTEXT ( 3 ) GLOBAL_UNCERTAINTY_ASSIGNED_CONTEXT ( ( #19308 ) ) GLOBAL_UNIT_ASSIGNED_CONTEXT ( ( #44689, #17910, #41464 ) ) REPRESENTATION_CONTEXT ( 'NONE', 'WORKASPACE' ) );
#21352=EDGE_CURVE ( 'NONE', #25927, #6724, #25884, .T. ) ;
#21354=CARTESIAN_POINT ( 'NONE',  ( -6.766228288048926842, 153.8165025765505334, 5.697616492254880427 ) ) ;
#21356=ORIENTED_EDGE ( 'NONE', *, *, #53552, .F. ) ;
#21360=DIRECTION ( 'NONE',  ( 1.000000000000000000, 0.000000000000000000, 0.000000000000000000 ) ) ;
#21361=ORIENTED_EDGE ( 'NONE', *, *, #67206, .T. ) ;
#21362=DIRECTION ( 'NONE',  ( -0.000000000000000000, -0.000000000000000000, 1.000000000000000000 ) ) ;
#21370=MECHANICAL_DESIGN_GEOMETRIC_PRESENTATION_REPRESENTATION('',(#47290),#58439);
#21371=ORIENTED_EDGE ( 'NONE', *, *, #65130, .F. ) ;
#21373=AXIS2_PLACEMENT_3D ( 'NONE', #41777, #41421, #19584 ) ;
#21374=EDGE_CURVE ( 'NONE', #59919, #58485, #34217, .T. ) ;
#21378=CARTESIAN_POINT ( 'NONE',  ( 65.00000000000000000, 1.797044900979284448E-15, 11.50000000000003730 ) ) ;
#21380=CARTESIAN_POINT ( 'NONE',  ( -74.99999999999998579, 35.99166914535020823, -9.500000000000000000 ) ) ;
#21382=CARTESIAN_POINT ( 'NONE',  ( 9.058813317711338797, 136.9549999999999841, -2.943386871421372675 ) ) ;
#21383=( GEOMETRIC_REPRESENTATION_CONTEXT ( 3 ) GLOBAL_UNCERTAINTY_ASSIGNED_CONTEXT ( ( #4524 ) ) GLOBAL_UNIT_ASSIGNED_CONTEXT ( ( #59042, #5213, #16514 ) ) REPRESENTATION_CONTEXT ( 'NONE', 'WORKASPACE' ) );
#21391=SURFACE_STYLE_FILL_AREA ( #37282 ) ;
#21393=CARTESIAN_POINT ( 'NONE',  ( -66.49999999999998579, 50.00000000000000000, 12.00000000000000000 ) ) ;
#21394=CIRCLE ( 'NONE', #30364, 1.000000000000000888 ) ;
#21396=FILL_AREA_STYLE_COLOUR ( '', #15042 ) ;
#21401=CARTESIAN_POINT ( 'NONE',  ( -45.50000000000000000, 7.768687147774684831, -6.500000000000000000 ) ) ;
#21406=( BOUNDED_CURVE ( )  B_SPLINE_CURVE ( 2, ( #62576, #3447, #67883, #14062, #41867, #35525, #62917, #14763, #30915, #52414, #4158 ),
 .UNSPECIFIED., .F., .F. ) 
 B_SPLINE_CURVE_WITH_KNOTS ( ( 3, 2, 2, 2, 2, 3 ),
 ( 0.5000000000000002220, 0.5058823529411766717, 0.5117647058823531214, 0.5176470588235296821, 0.5235294117647061318, 0.5294117647058825815 ),
 .UNSPECIFIED. ) 
 CURVE ( )  GEOMETRIC_REPRESENTATION_ITEM ( )  RATIONAL_B_SPLINE_CURVE ( ( 0.9999999999999981126, 0.9510565162951554186, 1.000000000000000000, 0.9510565162951535312, 1.000000000000000000, 0.9510565162951535312, 1.000000000000000000, 0.9510565162951535312, 1.000000000000000000, 0.9510565162951516438, 1.000000000000001776 ) ) 
 REPRESENTATION_ITEM ( '' )  );
#21412=ORIENTED_EDGE ( 'NONE', *, *, #25346, .T. ) ;
#21416=LINE ( 'NONE', #49908, #62480 ) ;
#21417=ORIENTED_EDGE ( 'NONE', *, *, #34655, .T. ) ;
#21419=VECTOR ( 'NONE', #41010, 1000.000000000000000 ) ;
#21420=CARTESIAN_POINT ( 'NONE',  ( 9.058813317711338797, 150.8449999999999989, -2.943386871421372675 ) ) ;
#21422=VECTOR ( 'NONE', #55831, 1000.000000000000000 ) ;
#21424=DIRECTION ( 'NONE',  ( 0.7713892158398690801, 0.000000000000000000, -0.6363636363636374638 ) ) ;
#21425=FACE_OUTER_BOUND ( 'NONE', #33450, .T. ) ;
#21426=( LENGTH_UNIT ( ) NAMED_UNIT ( * ) SI_UNIT ( .MILLI., .METRE. ) );
#21428=CARTESIAN_POINT ( 'NONE',  ( -2.607480562269075097, 130.2929263765337851, 8.025000000000000355 ) ) ;
#21430=CARTESIAN_POINT ( 'NONE',  ( -71.50000000000000000, 14.49137674618942562, 7.000000000000000000 ) ) ;
#21433=CARTESIAN_POINT ( 'NONE',  ( 7.632228543268608334, 125.3429263765338249, -2.479861379858951942 ) ) ;
#21436=VERTEX_POINT ( 'NONE', #46906 ) ;
#21437=CARTESIAN_POINT ( 'NONE',  ( -41.61274205743404053, 107.5029750606318544, -3.982828305957058390 ) ) ;
#21438=ORIENTED_EDGE ( 'NONE', *, *, #10262, .T. ) ;
#21444=LINE ( 'NONE', #43321, #63077 ) ;
#21449=DIRECTION ( 'NONE',  ( -0.7071067811865549002, 8.659560562355021605E-17, 0.7071067811865402453 ) ) ;
#21450=CARTESIAN_POINT ( 'NONE',  ( -34.99999999999999289, 99.99999999999998579, 7.000000000000000000 ) ) ;
#21455=EDGE_CURVE ( 'NONE', #41477, #21177, #18726, .T. ) ;
#21463=( NAMED_UNIT ( * ) PLANE_ANGLE_UNIT ( ) SI_UNIT ( $, .RADIAN. ) );
#21468=VERTEX_POINT ( 'NONE', #2849 ) ;
#21469=AXIS2_PLACEMENT_3D ( 'NONE', #17971, #67191, #55602 ) ;
#21477=CARTESIAN_POINT ( 'NONE',  ( 10.01517768586949231, 159.6949999999999648, 1.839758294383810543E-15 ) ) ;
#21479=CARTESIAN_POINT ( 'NONE',  ( -8.437984349512095861, 112.8070736234661382, -5.166775262442723748E-16 ) ) ;
#21482=UNCERTAINTY_MEASURE_WITH_UNIT (LENGTH_MEASURE( 1.000000000000000082E-05 ), #26503, 'distance_accuracy_value', 'NONE');
#21484=EDGE_LOOP ( 'NONE', ( #18973, #4510, #4312, #57026 ) ) ;
#21495=UNCERTAINTY_MEASURE_WITH_UNIT (LENGTH_MEASURE( 1.000000000000000082E-05 ), #20676, 'distance_accuracy_value', 'NONE');
#21496=EDGE_CURVE ( 'NONE', #59291, #57062, #57382, .T. ) ;
#21497=PRESENTATION_STYLE_ASSIGNMENT (( #3543 ) ) ;
#21503=( NAMED_UNIT ( * ) PLANE_ANGLE_UNIT ( ) SI_UNIT ( $, .RADIAN. ) );
#21504=DIRECTION ( 'NONE',  ( 0.000000000000000000, 0.000000000000000000, 1.000000000000000000 ) ) ;
#21506=AXIS2_PLACEMENT_3D ( 'NONE', #29258, #31698, #63370 ) ;
#21509=CARTESIAN_POINT ( 'NONE',  ( -3.094860106618432471, 124.5949999999999704, -9.525000000000000355 ) ) ;
#21510=ORIENTED_EDGE ( 'NONE', *, *, #28489, .F. ) ;
#21512=CARTESIAN_POINT ( 'NONE',  ( -55.00000000000000000, -2.024042244987997205E-14, 6.999999999999995559 ) ) ;
#21513=CARTESIAN_POINT ( 'NONE',  ( -5.598654528085806881, 131.8549999999999898, -7.705886871421374629 ) ) ;
#21514=CIRCLE ( 'NONE', #36099, 0.5000000000000004441 ) ;
#21517=CARTESIAN_POINT ( 'NONE',  ( -41.05143861928701199, 107.9622656938500000, -3.673005875159361278 ) ) ;
#21519=ORIENTED_EDGE ( 'NONE', *, *, #24861, .F. ) ;
#21520=CARTESIAN_POINT ( 'NONE',  ( 9.058813317711338797, 145.9550000000000125, -2.943386871421372675 ) ) ;
#21521=CARTESIAN_POINT ( 'NONE',  ( 15.98999599679679839, 118.4999999999999716, 10.00000000000000000 ) ) ;
#21522=UNCERTAINTY_MEASURE_WITH_UNIT (LENGTH_MEASURE( 1.000000000000000082E-05 ), #33376, 'distance_accuracy_value', 'NONE');
#21524=DIRECTION ( 'NONE',  ( 0.000000000000000000, 0.000000000000000000, 1.000000000000000000 ) ) ;
#21526=ADVANCED_FACE ( 'NONE', ( #14484 ), #32712, .T. ) ;
#21528=DIRECTION ( 'NONE',  ( 0.000000000000000000, 0.000000000000000000, 1.000000000000000000 ) ) ;
#21530=SURFACE_SIDE_STYLE ('',( #43400 ) ) ;
#21533=CARTESIAN_POINT ( 'NONE',  ( 41.49999999999998579, 108.0000000000000000, -3.000000000000000444 ) ) ;
#21536=CARTESIAN_POINT ( 'NONE',  ( 72.00000000000000000, 36.32520566882265456, 9.500000000000000000 ) ) ;
#21538=( GEOMETRIC_REPRESENTATION_CONTEXT ( 3 ) GLOBAL_UNCERTAINTY_ASSIGNED_CONTEXT ( ( #30633 ) ) GLOBAL_UNIT_ASSIGNED_CONTEXT ( ( #2426, #67198, #51033 ) ) REPRESENTATION_CONTEXT ( 'NONE', 'WORKASPACE' ) );
#21539=SURFACE_SIDE_STYLE ('',( #38105 ) ) ;
#21540=SURFACE_SIDE_STYLE ('',( #53222 ) ) ;
#21541=FACE_OUTER_BOUND ( 'NONE', #29840, .T. ) ;
#21542=AXIS2_PLACEMENT_3D ( 'NONE', #2923, #50824, #2579 ) ;
#21549=LINE ( 'NONE', #43418, #63226 ) ;
#21552=DIRECTION ( 'NONE',  ( 0.000000000000000000, 0.000000000000000000, 1.000000000000000000 ) ) ;
#21555=EDGE_LOOP ( 'NONE', ( #53580, #49169, #13473, #58028 ) ) ;
#21558=AXIS2_PLACEMENT_3D ( 'NONE', #6128, #16028, #59221 ) ;
#21559=DIRECTION ( 'NONE',  ( -1.000000000000000000, 0.000000000000000000, 0.000000000000000000 ) ) ;
#21560=CARTESIAN_POINT ( 'NONE',  ( -23.71231517720798010, 117.4999999999999716, 9.500000000000000000 ) ) ;
#21562=EDGE_CURVE ( 'NONE', #37680, #5084, #4597, .T. ) ;
#21563=CARTESIAN_POINT ( 'NONE',  ( -10.01517768586949231, 116.1949999999999932, -6.132527647946036459E-16 ) ) ;
#21567=EDGE_CURVE ( 'NONE', #17642, #36186, #31553, .T. ) ;
#21573=DIRECTION ( 'NONE',  ( 0.000000000000000000, 0.000000000000000000, 1.000000000000000000 ) ) ;
#21575=( LENGTH_UNIT ( ) NAMED_UNIT ( * ) SI_UNIT ( .MILLI., .METRE. ) );
#21577=VECTOR ( 'NONE', #39206, 1000.000000000000000 ) ;
#21581=SURFACE_STYLE_USAGE ( .BOTH. , #17021 ) ;
#21582=AXIS2_PLACEMENT_3D ( 'NONE', #7844, #44500, #23680 ) ;
#21585=DIRECTION ( 'NONE',  ( 1.387778780781444413E-14, 1.000000000000000000, 0.000000000000000000 ) ) ;
#21592=CARTESIAN_POINT ( 'NONE',  ( 41.49999999999997868, 9.999999999999978684, 3.500000000000000000 ) ) ;
#21594=CARTESIAN_POINT ( 'NONE',  ( -8.437984349512095861, 145.8070736234661808, -5.166775262442723748E-16 ) ) ;
#21600=ORIENTED_EDGE ( 'NONE', *, *, #23574, .F. ) ;
#21604=FILL_AREA_STYLE_COLOUR ( '', #59796 ) ;
#21605=ORIENTED_EDGE ( 'NONE', *, *, #35427, .F. ) ;
#21610=SURFACE_SIDE_STYLE ('',( #79 ) ) ;
#21611=FILL_AREA_STYLE ('',( #26188 ) ) ;
#21613=SURFACE_SIDE_STYLE ('',( #48394 ) ) ;
#21615=STYLED_ITEM ( 'NONE', ( #3660 ), #23634 ) ;
#21620=VECTOR ( 'NONE', #21159, 1000.000000000000000 ) ;
#21624=CARTESIAN_POINT ( 'NONE',  ( 0.000000000000000000, 87.30187232391182306, 8.025000000000000355 ) ) ;
#21627=MECHANICAL_DESIGN_GEOMETRIC_PRESENTATION_REPRESENTATION('',(#8183),#44178);
#21628=CARTESIAN_POINT ( 'NONE',  ( -5.598654528085808657, 131.6449999999999818, 7.705886871421373741 ) ) ;
#21631=DIRECTION ( 'NONE',  ( -0.000000000000000000, -0.000000000000000000, 1.000000000000000000 ) ) ;
#21632=ORIENTED_EDGE ( 'NONE', *, *, #65724, .T. ) ;
#21640=( LENGTH_UNIT ( ) NAMED_UNIT ( * ) SI_UNIT ( .MILLI., .METRE. ) );
#21641=AXIS2_PLACEMENT_3D ( 'NONE', #6548, #27997, #49505 ) ;
#21646=CARTESIAN_POINT ( 'NONE',  ( 44.94709371290443300, 9.982364570967856565, -3.713690726390495911 ) ) ;
#21648=VECTOR ( 'NONE', #50852, 1000.000000000000000 ) ;
#21649=( NAMED_UNIT ( * ) PLANE_ANGLE_UNIT ( ) SI_UNIT ( $, .RADIAN. ) );
#21651=FACE_OUTER_BOUND ( 'NONE', #49177, .T. ) ;
#21652=VECTOR ( 'NONE', #4921, 1000.000000000000000 ) ;
#21656=AXIS2_PLACEMENT_3D ( 'NONE', #17124, #7572, #7235 ) ;
#21662=DIRECTION ( 'NONE',  ( 0.000000000000000000, 0.000000000000000000, 1.000000000000000000 ) ) ;
#21664=AXIS2_PLACEMENT_3D ( 'NONE', #29664, #7510, #23683 ) ;
#21670=ORIENTED_EDGE ( 'NONE', *, *, #17948, .T. ) ;
#21672=VECTOR ( 'NONE', #65741, 1000.000000000000000 ) ;
#21673=CARTESIAN_POINT ( 'NONE',  ( 6.826472737025119919, 117.0070736234661410, 4.959722759717908325 ) ) ;
#21674=AXIS2_PLACEMENT_3D ( 'NONE', #45462, #29922, #19357 ) ;
#21675=CARTESIAN_POINT ( 'NONE',  ( -20.58979310427664444, 114.8389001175783051, 9.999999999999879208 ) ) ;
#21676=CARTESIAN_POINT ( 'NONE',  ( 75.00000000000000000, 20.33294439365979756, -6.261747904192522363 ) ) ;
#21677=( LENGTH_UNIT ( ) NAMED_UNIT ( * ) SI_UNIT ( .MILLI., .METRE. ) );
#21686=CARTESIAN_POINT ( 'NONE',  ( -3.094860106618434248, 126.9049999999999869, 9.525000000000000355 ) ) ;
#21691=ADVANCED_FACE ( 'NONE', ( #59457 ), #2042, .F. ) ;
#21692=CARTESIAN_POINT ( 'NONE',  ( 71.50000000000000000, 35.92875272052971525, 9.500000000000000000 ) ) ;
#21695=AXIS2_PLACEMENT_3D ( 'NONE', #3879, #19382, #31670 ) ;
#21698=ORIENTED_EDGE ( 'NONE', *, *, #32010, .F. ) ;
#21700=DIRECTION ( 'NONE',  ( 0.000000000000000000, 0.000000000000000000, 1.000000000000000000 ) ) ;
#21701=FILL_AREA_STYLE ('',( #48476 ) ) ;
#21702=CARTESIAN_POINT ( 'NONE',  ( 20.55652580482692926, 114.6393193824117844, -10.28299520148690682 ) ) ;
#21703=VERTEX_POINT ( 'NONE', #7051 ) ;
#21707=STYLED_ITEM ( 'NONE', ( #36936 ), #48104 ) ;
#21708=COLOUR_RGB ( '', 0.72549020, 0.75294118, 0.79215686) ;
#21710=CARTESIAN_POINT ( 'NONE',  ( -71.99999999999998579, 64.07124727947029896, 7.500000000000000000 ) ) ;
#21712=SURFACE_STYLE_FILL_AREA ( #27654 ) ;
#21714=CARTESIAN_POINT ( 'NONE',  ( 4.716976649647096842, 115.7429263765338163, 6.492361379858953896 ) ) ;
#21717=ORIENTED_EDGE ( 'NONE', *, *, #40052, .F. ) ;
#21718=FACE_OUTER_BOUND ( 'NONE', #27480, .T. ) ;
#21720=DIRECTION ( 'NONE',  ( 0.000000000000000000, 0.000000000000000000, 1.000000000000000000 ) ) ;
#21722=FACE_OUTER_BOUND ( 'NONE', #27583, .T. ) ;
#21723=AXIS2_PLACEMENT_3D ( 'NONE', #30048, #62743, #62050 ) ;
#21728=AXIS2_PLACEMENT_3D ( 'NONE', #50265, #66428, #23507 ) ;
#21730=ORIENTED_EDGE ( 'NONE', *, *, #69191, .T. ) ;
#21732=FILL_AREA_STYLE ('',( #205 ) ) ;
#21734=PRESENTATION_STYLE_ASSIGNMENT (( #17847 ) ) ;
#21739=CARTESIAN_POINT ( 'NONE',  ( -75.48275862205373699, 36.00832590027795987, -9.539713814030060135 ) ) ;
#21743=CARTESIAN_POINT ( 'NONE',  ( 5.598654528085809545, 134.2549999999999955, -7.705886871421373741 ) ) ;
#21755=EDGE_CURVE ( 'NONE', #38501, #40909, #68641, .T. ) ;
#21757=SURFACE_SIDE_STYLE ('',( #42240 ) ) ;
#21758=CARTESIAN_POINT ( 'NONE',  ( 0.000000000000000000, 146.9429263765338192, -8.025000000000000355 ) ) ;
#21765=EDGE_CURVE ( 'NONE', #51230, #58139, #1725, .T. ) ;
#21766=VECTOR ( 'NONE', #41219, 999.9999999999998863 ) ;
#21767=CIRCLE ( 'NONE', #12761, 13.00000000000000178 ) ;
#21768=FACE_OUTER_BOUND ( 'NONE', #60044, .T. ) ;
#21769=DIRECTION ( 'NONE',  ( 0.000000000000000000, 0.000000000000000000, 1.000000000000000000 ) ) ;
#21770=( NAMED_UNIT ( * ) PLANE_ANGLE_UNIT ( ) SI_UNIT ( $, .RADIAN. ) );
#21771=ORIENTED_EDGE ( 'NONE', *, *, #17893, .F. ) ;
#21774=LINE ( 'NONE', #43289, #44411 ) ;
#21775=CARTESIAN_POINT ( 'NONE',  ( 21.02379604162863558, 114.6405644170961153, -10.00000000000000000 ) ) ;
#21776=MECHANICAL_DESIGN_GEOMETRIC_PRESENTATION_REPRESENTATION('',(#61079),#7164);
#21782=COLOUR_RGB ( '', 0.09019608, 0.27058824, 0.51372549) ;
#21783=CARTESIAN_POINT ( 'NONE',  ( -5.598654528085808657, 158.6449999999999818, 7.705886871421373741 ) ) ;
#21784=SURFACE_STYLE_FILL_AREA ( #53773 ) ;
#21788=LINE ( 'NONE', #43303, #8142 ) ;
#21789=ADVANCED_FACE ( 'NONE', ( #23240 ), #44734, .F. ) ;
#21791=AXIS2_PLACEMENT_3D ( 'NONE', #42322, #51786, #35607 ) ;
#21793=CARTESIAN_POINT ( 'NONE',  ( 6.826472737025121695, 122.4929263765338021, -4.959722759717905660 ) ) ;
#21797=CIRCLE ( 'NONE', #34199, 5.000000000000004441 ) ;
#21798=DIRECTION ( 'NONE',  ( 1.000000000000000000, 0.000000000000000000, 0.000000000000000000 ) ) ;
#21811=DIRECTION ( 'NONE',  ( -0.6216216216216311485, 0.7833176619561784682, 0.000000000000000000 ) ) ;
#21816=VECTOR ( 'NONE', #47821, 1000.000000000000000 ) ;
#21819=CARTESIAN_POINT ( 'NONE',  ( 60.99999999999998579, 50.00000000000000000, 7.500000000000000000 ) ) ;
#21822=PLANE ( 'NONE',  #35771 ) ;
#21824=MECHANICAL_DESIGN_GEOMETRIC_PRESENTATION_REPRESENTATION('',(#39830),#34171);
#21825=( NAMED_UNIT ( * ) SI_UNIT ( $, .STERADIAN. ) SOLID_ANGLE_UNIT ( ) );
#21832=CARTESIAN_POINT ( 'NONE',  ( 0.000000000000000000, 127.0570736234661666, -8.025000000000000355 ) ) ;
#21835=CARTESIAN_POINT ( 'NONE',  ( -8.102448949553181734, 154.8949999999999534, -5.886773742842749790 ) ) ;
#21838=FILL_AREA_STYLE ('',( #42635 ) ) ;
#21840=AXIS2_PLACEMENT_3D ( 'NONE', #7597, #29024, #50528 ) ;
#21842=( GEOMETRIC_REPRESENTATION_CONTEXT ( 3 ) GLOBAL_UNCERTAINTY_ASSIGNED_CONTEXT ( ( #2241 ) ) GLOBAL_UNIT_ASSIGNED_CONTEXT ( ( #47721, #36071, #63486 ) ) REPRESENTATION_CONTEXT ( 'NONE', 'WORKASPACE' ) );
#21845=CIRCLE ( 'NONE', #61141, 0.5000000000000004441 ) ;
#21848=FILL_AREA_STYLE ('',( #16255 ) ) ;
#21849=EDGE_CURVE ( 'NONE', #44684, #46060, #3095, .T. ) ;
#21851=EDGE_CURVE ( 'NONE', #2677, #42412, #57, .T. ) ;
#21852=SURFACE_STYLE_FILL_AREA ( #663 ) ;
#21858=EDGE_CURVE ( 'NONE', #64972, #42340, #25925, .T. ) ;
#21860=CARTESIAN_POINT ( 'NONE',  ( -45.00000000000036238, 8.675277573170289358, 5.941086794573004148 ) ) ;
#21863=DIRECTION ( 'NONE',  ( 1.000000000000000000, -1.776356839400250465E-15, 0.000000000000000000 ) ) ;
#21868=DIRECTION ( 'NONE',  ( 1.000000000000000000, -1.776356839400250465E-15, 0.000000000000000000 ) ) ;
#21873=CIRCLE ( 'NONE', #20772, 0.5000000000000004441 ) ;
#21875=CARTESIAN_POINT ( 'NONE',  ( 8.102448949553183510, 126.9950000000000045, -5.886773742842746238 ) ) ;
#21876=LINE ( 'NONE', #69028, #8178 ) ;
#21877=ORIENTED_EDGE ( 'NONE', *, *, #62985, .F. ) ;
#21878=CARTESIAN_POINT ( 'NONE',  ( 44.91886116991580735, 10.49999999999998224, -6.500000000000000000 ) ) ;
#21879=CARTESIAN_POINT ( 'NONE',  ( 3.094860106618435136, 134.4049999999999727, -9.525000000000000355 ) ) ;
#21883=DIRECTION ( 'NONE',  ( 1.000000000000000000, 0.000000000000000000, 0.000000000000000000 ) ) ;
#21885=CARTESIAN_POINT ( 'NONE',  ( -10.01517768586949231, 150.3050000000000068, -6.132527647946036459E-16 ) ) ;
#21887=CARTESIAN_POINT ( 'NONE',  ( 44.99999999999998579, 119.9999999999999716, -9.500000000000000000 ) ) ;
#21888=CARTESIAN_POINT ( 'NONE',  ( -44.99999999999977973, 146.9999999999999716, -7.500000000000000000 ) ) ;
#21891=EDGE_LOOP ( 'NONE', ( #4677, #45475, #18662, #49374 ) ) ;
#21893=( GEOMETRIC_REPRESENTATION_CONTEXT ( 3 ) GLOBAL_UNCERTAINTY_ASSIGNED_CONTEXT ( ( #55254 ) ) GLOBAL_UNIT_ASSIGNED_CONTEXT ( ( #37519, #64549, #32506 ) ) REPRESENTATION_CONTEXT ( 'NONE', 'WORKASPACE' ) );
#21899=DIRECTION ( 'NONE',  ( 0.000000000000000000, -1.000000000000000000, 0.000000000000000000 ) ) ;
#21901=EDGE_LOOP ( 'NONE', ( #42969, #37407, #67558, #596 ) ) ;
#21902=DIRECTION ( 'NONE',  ( -0.000000000000000000, 0.000000000000000000, -1.000000000000000000 ) ) ;
#21903=PRESENTATION_STYLE_ASSIGNMENT (( #38114 ) ) ;
#21907=CARTESIAN_POINT ( 'NONE',  ( -5.696827471326999515, 112.0732520954904032, 5.780458086807509943 ) ) ;
#21908=CARTESIAN_POINT ( 'NONE',  ( -60.00000000000000000, -2.024042244987997205E-14, -12.00000000000000000 ) ) ;
#21909=( NAMED_UNIT ( * ) PLANE_ANGLE_UNIT ( ) SI_UNIT ( $, .RADIAN. ) );
#21911=CIRCLE ( 'NONE', #30872, 0.9999999999999991118 ) ;
#21913=MECHANICAL_DESIGN_GEOMETRIC_PRESENTATION_REPRESENTATION('',(#43300),#42194);
#21915=ORIENTED_EDGE ( 'NONE', *, *, #22327, .T. ) ;
#21917=DIRECTION ( 'NONE',  ( 1.000000000000000000, 0.000000000000000000, 0.000000000000000000 ) ) ;
#21922=CARTESIAN_POINT ( 'NONE',  ( -9.058813317711338797, 128.3449999999999989, 2.943386871421373563 ) ) ;
#21924=CARTESIAN_POINT ( 'NONE',  ( 21.02379604162863913, 110.4999999999999858, -9.500000000000000000 ) ) ;
#21929=ADVANCED_FACE ( 'NONE', ( #8458 ), #34815, .F. ) ;
#21930=AXIS2_PLACEMENT_3D ( 'NONE', #7147, #50756, #18046 ) ;
#21932=FACE_OUTER_BOUND ( 'NONE', #22546, .T. ) ;
#21933=MECHANICAL_DESIGN_GEOMETRIC_PRESENTATION_REPRESENTATION('',(#38835),#65767);
#21936=DIRECTION ( 'NONE',  ( 0.000000000000000000, 0.000000000000000000, 1.000000000000000000 ) ) ;
#21937=CARTESIAN_POINT ( 'NONE',  ( -15.98999599679679839, 146.4999999999999716, -9.500000000000000000 ) ) ;
#21943=SURFACE_STYLE_FILL_AREA ( #22978 ) ;
#21946=FILL_AREA_STYLE_COLOUR ( '', #66315 ) ;
#21947=PLANE ( 'NONE',  #55102 ) ;
#21948=CARTESIAN_POINT ( 'NONE',  ( 0.000000000000000000, 109.9999999999999858, 0.000000000000000000 ) ) ;
#21949=EDGE_CURVE ( 'NONE', #60632, #67825, #39952, .T. ) ;
#21956=FACE_OUTER_BOUND ( 'NONE', #26755, .T. ) ;
#21958=CARTESIAN_POINT ( 'NONE',  ( -6.826472737025120807, 143.1070736234661638, 4.959722759717906548 ) ) ;
#21971=CIRCLE ( 'NONE', #11808, 26.99999999999999645 ) ;
#21976=CARTESIAN_POINT ( 'NONE',  ( 44.99999999999977973, 149.9999999999999716, -9.500000000000000000 ) ) ;
#21977=( NAMED_UNIT ( * ) PLANE_ANGLE_UNIT ( ) SI_UNIT ( $, .RADIAN. ) );
#21982=CARTESIAN_POINT ( 'NONE',  ( 45.00000000000000000, 10.18984267075341066, -6.892226874380344093 ) ) ;
#21989=DIRECTION ( 'NONE',  ( -0.000000000000000000, -0.000000000000000000, -1.000000000000000000 ) ) ;
#21992=CARTESIAN_POINT ( 'NONE',  ( -9.058813317711338797, 134.3449999999999989, 2.943386871421373563 ) ) ;
#21993=VECTOR ( 'NONE', #35186, 1000.000000000000000 ) ;
#21995=AXIS2_PLACEMENT_3D ( 'NONE', #54264, #59184, #42736 ) ;
#22000=SURFACE_STYLE_USAGE ( .BOTH. , #49104 ) ;
#22007=( GEOMETRIC_REPRESENTATION_CONTEXT ( 3 ) GLOBAL_UNCERTAINTY_ASSIGNED_CONTEXT ( ( #9545 ) ) GLOBAL_UNIT_ASSIGNED_CONTEXT ( ( #47755, #27230, #10409 ) ) REPRESENTATION_CONTEXT ( 'NONE', 'WORKASPACE' ) );
#22008=CYLINDRICAL_SURFACE ( 'NONE', #44709, 18.00000000000000355 ) ;
#22012=PRESENTATION_STYLE_ASSIGNMENT (( #26232 ) ) ;
#22014=AXIS2_PLACEMENT_3D ( 'NONE', #50142, #55033, #19405 ) ;
#22017=( NAMED_UNIT ( * ) PLANE_ANGLE_UNIT ( ) SI_UNIT ( $, .RADIAN. ) );
#22021=DIRECTION ( 'NONE',  ( -0.000000000000000000, 1.000000000000000000, -0.000000000000000000 ) ) ;
#22022=CARTESIAN_POINT ( 'NONE',  ( -71.99999999999998579, 119.9999999999997868, -9.500000000000000000 ) ) ;
#22024=CIRCLE ( 'NONE', #38932, 0.5000000000000004441 ) ;
#22030=DIRECTION ( 'NONE',  ( -0.000000000000000000, 0.000000000000000000, 1.000000000000000000 ) ) ;
#22031=AXIS2_PLACEMENT_3D ( 'NONE', #27711, #22468, #65013 ) ;
#22032=CARTESIAN_POINT ( 'NONE',  ( -7.632228543268608334, 115.9570736234661581, 2.479861379858952830 ) ) ;
#22033=( NAMED_UNIT ( * ) PLANE_ANGLE_UNIT ( ) SI_UNIT ( $, .RADIAN. ) );
#22040=ORIENTED_EDGE ( 'NONE', *, *, #186, .T. ) ;
#22042=CARTESIAN_POINT ( 'NONE',  ( 4.716976649647096842, 133.7429263765338021, 6.492361379858953896 ) ) ;
#22043=EDGE_CURVE ( 'NONE', #19239, #50261, #12515, .T. ) ;
#22049=PRESENTATION_STYLE_ASSIGNMENT (( #25918 ) ) ;
#22050=EDGE_LOOP ( 'NONE', ( #67729, #45935, #40477, #7059 ) ) ;
#22051=CARTESIAN_POINT ( 'NONE',  ( 4.716976649647099507, 161.6429263765338362, -6.492361379858953008 ) ) ;
#22054=ORIENTED_EDGE ( 'NONE', *, *, #32010, .T. ) ;
#22058=DIRECTION ( 'NONE',  ( 0.000000000000000000, 1.000000000000000000, -0.000000000000000000 ) ) ;
#22061=CARTESIAN_POINT ( 'NONE',  ( 44.91886116991580735, 9.999999999999980460, 3.201362207699192997 ) ) ;
#22065=DIRECTION ( 'NONE',  ( -0.000000000000000000, -0.000000000000000000, 1.000000000000000000 ) ) ;
#22067=CARTESIAN_POINT ( 'NONE',  ( -4.325530127497521526, 153.1662597749872816, -6.961252418570021305 ) ) ;
#22069=FILL_AREA_STYLE ('',( #16815 ) ) ;
#22071=( LENGTH_UNIT ( ) NAMED_UNIT ( * ) SI_UNIT ( .MILLI., .METRE. ) );
#22073=SURFACE_STYLE_USAGE ( .BOTH. , #198 ) ;
#22076=CYLINDRICAL_SURFACE ( 'NONE', #33604, 8.025000000000000355 ) ;
#22077=ADVANCED_FACE ( 'NONE', ( #27700 ), #46274, .T. ) ;
#22080=ORIENTED_EDGE ( 'NONE', *, *, #14362, .T. ) ;
#22081=( LENGTH_UNIT ( ) NAMED_UNIT ( * ) SI_UNIT ( .MILLI., .METRE. ) );
#22083=CARTESIAN_POINT ( 'NONE',  ( -2.607480562269240298, 150.0929263765338817, -8.024999999999879563 ) ) ;
#22088=EDGE_CURVE ( 'NONE', #47153, #43960, #49201, .T. ) ;
#22090=CARTESIAN_POINT ( 'NONE',  ( 3.094860106618431583, 139.2050000000000125, 9.525000000000000355 ) ) ;
#22094=UNCERTAINTY_MEASURE_WITH_UNIT (LENGTH_MEASURE( 1.000000000000000082E-05 ), #13215, 'distance_accuracy_value', 'NONE');
#22097=ADVANCED_FACE ( 'NONE', ( #21768 ), #34984, .T. ) ;
#22099=CARTESIAN_POINT ( 'NONE',  ( 24.21231517720798010, 117.4999999999999716, 7.500000000000000000 ) ) ;
#22100=COLOUR_RGB ( '', 0.08235294, 0.09019608, 0.10196078) ;
#22101=EDGE_CURVE ( 'NONE', #2048, #52429, #44023, .T. ) ;
#22102=DIRECTION ( 'NONE',  ( 1.000000000000000000, 0.000000000000000000, 0.000000000000000000 ) ) ;
#22104=( LENGTH_UNIT ( ) NAMED_UNIT ( * ) SI_UNIT ( .MILLI., .METRE. ) );
#22105=COLOUR_RGB ( '', 0.72549020, 0.75294118, 0.79215686) ;
#22109=DIRECTION ( 'NONE',  ( 1.000000000000000000, 0.000000000000000000, 0.000000000000000000 ) ) ;
#22111=( NAMED_UNIT ( * ) PLANE_ANGLE_UNIT ( ) SI_UNIT ( $, .RADIAN. ) );
#22112=CARTESIAN_POINT ( 'NONE',  ( -23.71231517720798010, 117.9999999999999716, 7.000000000000000000 ) ) ;
#22113=DIRECTION ( 'NONE',  ( 0.000000000000000000, -1.000000000000000000, -0.000000000000000000 ) ) ;
#22116=ORIENTED_EDGE ( 'NONE', *, *, #22716, .T. ) ;
#22118=CARTESIAN_POINT ( 'NONE',  ( 20.44164625062140317, 115.3859073845563756, -10.00000000000000000 ) ) ;
#22120=B_SPLINE_CURVE_WITH_KNOTS ( 'NONE', 3,
 ( #64139, #1083, #22977, #55311, #60572, #65880, #59900, #7134, #12389, #38507, #33849, #54273 ),
 .UNSPECIFIED., .F., .F.,
 ( 4, 2, 2, 2, 2, 4 ),
 ( 0.000000000000000000, 0.0001173275976309089770, 0.0002346551952618179540, 0.0004693103905236373718, 0.0009386207810472817908, 0.001877241562094575291 ),
 .UNSPECIFIED. ) ;
#22123=ORIENTED_EDGE ( 'NONE', *, *, #28580, .F. ) ;
#22125=CARTESIAN_POINT ( 'NONE',  ( -3.094860106618434248, 155.7950000000000159, 9.525000000000000355 ) ) ;
#22128=VERTEX_POINT ( 'NONE', #45679 ) ;
#22129=CARTESIAN_POINT ( 'NONE',  ( -12.72792206135785520, 115.4999999999999574, 10.50000000000000000 ) ) ;
#22130=SURFACE_SIDE_STYLE ('',( #65020 ) ) ;
#22133=CARTESIAN_POINT ( 'NONE',  ( 8.437984349512095861, 140.1929263765337907, 1.550032578732817026E-15 ) ) ;
#22134=LINE ( 'NONE', #49220, #15469 ) ;
#22138=ORIENTED_EDGE ( 'NONE', *, *, #14038, .T. ) ;
#22145=SURFACE_STYLE_FILL_AREA ( #27397 ) ;
#22146=UNCERTAINTY_MEASURE_WITH_UNIT (LENGTH_MEASURE( 1.000000000000000082E-05 ), #24735, 'distance_accuracy_value', 'NONE');
#22149=CYLINDRICAL_SURFACE ( 'NONE', #38427, 23.00000000000000000 ) ;
#22150=CARTESIAN_POINT ( 'NONE',  ( 40.99999999999998579, 107.7459666690181450, 3.075798416731059692 ) ) ;
#22152=ORIENTED_EDGE ( 'NONE', *, *, #13301, .F. ) ;
#22154=AXIS2_PLACEMENT_3D ( 'NONE', #51062, #33902, #57370 ) ;
#22155=FILL_AREA_STYLE ('',( #633 ) ) ;
#22157=ORIENTED_EDGE ( 'NONE', *, *, #51926, .T. ) ;
#22158=DIRECTION ( 'NONE',  ( -0.000000000000000000, -0.000000000000000000, -1.000000000000000000 ) ) ;
#22160=CARTESIAN_POINT ( 'NONE',  ( 68.50000000000000000, 1.797044900979284448E-15, -9.999999999999998224 ) ) ;
#22161=EDGE_CURVE ( 'NONE', #11645, #30516, #28749, .T. ) ;
#22162=CARTESIAN_POINT ( 'NONE',  ( -74.99999999999998579, 50.00000000000000000, -11.50000000000000000 ) ) ;
#22165=ADVANCED_FACE ( 'NONE', ( #18882 ), #23833, .T. ) ;
#22167=EDGE_CURVE ( 'NONE', #320, #21193, #63524, .T. ) ;
#22168=CARTESIAN_POINT ( 'NONE',  ( -15.98999599679679839, 146.4999999999999716, -10.00000000000000000 ) ) ;
#22172=EDGE_CURVE ( 'NONE', #9835, #15666, #14827, .T. ) ;
#22176=CARTESIAN_POINT ( 'NONE',  ( -8.102448949553181734, 111.6049999999999613, 5.886773742842747126 ) ) ;
#22183=SURFACE_STYLE_USAGE ( .BOTH. , #69340 ) ;
#22184=ORIENTED_EDGE ( 'NONE', *, *, #28329, .F. ) ;
#22188=SURFACE_SIDE_STYLE ('',( #21852 ) ) ;
#22190=ORIENTED_EDGE ( 'NONE', *, *, #47280, .F. ) ;
#22193=( LENGTH_UNIT ( ) NAMED_UNIT ( * ) SI_UNIT ( .MILLI., .METRE. ) );
#22196=COLOUR_RGB ( '', 0.72549020, 0.75294118, 0.79215686) ;
#22200=ORIENTED_EDGE ( 'NONE', *, *, #25977, .F. ) ;
#22203=( GEOMETRIC_REPRESENTATION_CONTEXT ( 3 ) GLOBAL_UNCERTAINTY_ASSIGNED_CONTEXT ( ( #45951 ) ) GLOBAL_UNIT_ASSIGNED_CONTEXT ( ( #61472, #44679, #66789 ) ) REPRESENTATION_CONTEXT ( 'NONE', 'WORKASPACE' ) );
#22205=CARTESIAN_POINT ( 'NONE',  ( -0.9728900412908211282, 153.0000000000000000, -7.965808808122195828 ) ) ;
#22206=DIRECTION ( 'NONE',  ( 1.000000000000000000, 0.000000000000000000, 0.000000000000000000 ) ) ;
#22207=ORIENTED_EDGE ( 'NONE', *, *, #26448, .F. ) ;
#22210=CARTESIAN_POINT ( 'NONE',  ( -9.058813317711338797, 128.3449999999999989, 2.943386871421373563 ) ) ;
#22211=( LENGTH_UNIT ( ) NAMED_UNIT ( * ) SI_UNIT ( .MILLI., .METRE. ) );
#22215=CARTESIAN_POINT ( 'NONE',  ( -9.058813317711338797, 132.4549999999999841, 2.943386871421373563 ) ) ;
#22219=ORIENTED_EDGE ( 'NONE', *, *, #9946, .T. ) ;
#22220=CARTESIAN_POINT ( 'NONE',  ( -5.598654528085806881, 155.8549999999999898, -7.705886871421374629 ) ) ;
#22221=DIRECTION ( 'NONE',  ( 0.000000000000000000, 0.000000000000000000, 1.000000000000000000 ) ) ;
#22222=UNCERTAINTY_MEASURE_WITH_UNIT (LENGTH_MEASURE( 1.000000000000000082E-05 ), #65194, 'distance_accuracy_value', 'NONE');
#22225=DIRECTION ( 'NONE',  ( 1.000000000000000000, 0.000000000000000000, 0.000000000000000000 ) ) ;
#22226=( NAMED_UNIT ( * ) SI_UNIT ( $, .STERADIAN. ) SOLID_ANGLE_UNIT ( ) );
#22229=ORIENTED_EDGE ( 'NONE', *, *, #67935, .T. ) ;
#22234=FILL_AREA_STYLE ('',( #49009 ) ) ;
#22235=( NAMED_UNIT ( * ) SI_UNIT ( $, .STERADIAN. ) SOLID_ANGLE_UNIT ( ) );
#22237=CARTESIAN_POINT ( 'NONE',  ( -45.89905495956738690, 9.405628579031734660, -3.000000000000000444 ) ) ;
#22242=CARTESIAN_POINT ( 'NONE',  ( 23.21231517720797655, 117.4999999999999716, -7.000000000000000000 ) ) ;
#22243=FILL_AREA_STYLE_COLOUR ( '', #63173 ) ;
#22250=SURFACE_STYLE_USAGE ( .BOTH. , #7792 ) ;
#22251=AXIS2_PLACEMENT_3D ( 'NONE', #56470, #29380, #19873 ) ;
#22255=CARTESIAN_POINT ( 'NONE',  ( -8.102448949553181734, 131.4950000000000045, 5.886773742842747126 ) ) ;
#22257=ADVANCED_FACE ( 'NONE', ( #37209 ), #64232, .T. ) ;
#22259=( NAMED_UNIT ( * ) SI_UNIT ( $, .STERADIAN. ) SOLID_ANGLE_UNIT ( ) );
#22261=EDGE_CURVE ( 'NONE', #13670, #31668, #33919, .T. ) ;
#22265=CARTESIAN_POINT ( 'NONE',  ( -7.632228543268607446, 148.6570736234661751, -2.479861379858953718 ) ) ;
#22272=( NAMED_UNIT ( * ) SI_UNIT ( $, .STERADIAN. ) SOLID_ANGLE_UNIT ( ) );
#22273=CARTESIAN_POINT ( 'NONE',  ( 4.716976649647099507, 147.7570736234661695, -6.492361379858953008 ) ) ;
#22274=DIRECTION ( 'NONE',  ( -0.000000000000000000, -0.000000000000000000, -1.000000000000000000 ) ) ;
#22275=CARTESIAN_POINT ( 'NONE',  ( -71.18918918918917882, 14.09971791521133255, 7.500000000000000000 ) ) ;
#22280=PRESENTATION_STYLE_ASSIGNMENT (( #21228 ) ) ;
#22283=VECTOR ( 'NONE', #54552, 1000.000000000000000 ) ;
#22284=CARTESIAN_POINT ( 'NONE',  ( -44.99999999999998579, 119.9999999999999716, -9.500000000000000000 ) ) ;
#22285=CARTESIAN_POINT ( 'NONE',  ( -6.826472737025120807, 148.5070736234661126, -4.959722759717907437 ) ) ;
#22288=ORIENTED_EDGE ( 'NONE', *, *, #41979, .F. ) ;
#22290=UNCERTAINTY_MEASURE_WITH_UNIT (LENGTH_MEASURE( 1.000000000000000082E-05 ), #43950, 'distance_accuracy_value', 'NONE');
#22292=AXIS2_PLACEMENT_3D ( 'NONE', #10646, #15263, #36729 ) ;
#22293=TOROIDAL_SURFACE ( 'NONE', #45921, 26.49999999999999645, 0.5000000000000000000 ) ;
#22296=ORIENTED_EDGE ( 'NONE', *, *, #22559, .F. ) ;
#22302=PLANE ( 'NONE',  #54184 ) ;
#22306=CARTESIAN_POINT ( 'NONE',  ( -45.00000000000000711, 8.707403661853012622, -5.727618941854548673 ) ) ;
#22311=AXIS2_PLACEMENT_3D ( 'NONE', #16228, #26718, #27058 ) ;
#22313=LINE ( 'NONE', #40519, #22418 ) ;
#22319=( LENGTH_UNIT ( ) NAMED_UNIT ( * ) SI_UNIT ( .MILLI., .METRE. ) );
#22320=FILL_AREA_STYLE_COLOUR ( '', #34676 ) ;
#22321=PRESENTATION_STYLE_ASSIGNMENT (( #63833 ) ) ;
#22325=CARTESIAN_POINT ( 'NONE',  ( 8.102448949553179958, 135.3949999999999534, 5.886773742842750679 ) ) ;
#22327=EDGE_CURVE ( 'NONE', #48570, #6729, #8130, .T. ) ;
#22330=EDGE_LOOP ( 'NONE', ( #42573, #20034, #27694, #17879 ) ) ;
#22334=CIRCLE ( 'NONE', #41433, 15.00000000000000000 ) ;
#22335=DIRECTION ( 'NONE',  ( -0.000000000000000000, 1.000000000000000000, -0.000000000000000000 ) ) ;
#22340=ADVANCED_FACE ( 'NONE', ( #64922, #49815 ), #17473, .T. ) ;
#22345=CARTESIAN_POINT ( 'NONE',  ( 15.48999599679679662, 146.4999999999999716, 9.500000000000000000 ) ) ;
#22347=EDGE_CURVE ( 'NONE', #38818, #21246, #43053, .T. ) ;
#22352=FILL_AREA_STYLE ('',( #808 ) ) ;
#22353=CARTESIAN_POINT ( 'NONE',  ( 24.21231517720798010, 117.4999999999999716, -7.500000000000000000 ) ) ;
#22354=CARTESIAN_POINT ( 'NONE',  ( 0.000000000000000000, 87.30187232391182306, 8.025000000000000355 ) ) ;
#22366=( LENGTH_UNIT ( ) NAMED_UNIT ( * ) SI_UNIT ( .MILLI., .METRE. ) );
#22368=CARTESIAN_POINT ( 'NONE',  ( 8.437984349512095861, 123.3070736234661666, 1.550032578732817026E-15 ) ) ;
#22369=CARTESIAN_POINT ( 'NONE',  ( 20.71231517720797299, 149.6390813561872619, 10.00000000000000000 ) ) ;
#22370=SURFACE_STYLE_USAGE ( .BOTH. , #32561 ) ;
#22371=SURFACE_SIDE_STYLE ('',( #49136 ) ) ;
#22374=ORIENTED_EDGE ( 'NONE', *, *, #14385, .F. ) ;
#22377=PRESENTATION_STYLE_ASSIGNMENT (( #17480 ) ) ;
#22380=DIRECTION ( 'NONE',  ( 1.000000000000000000, 0.000000000000000000, 0.000000000000000000 ) ) ;
#22384=CARTESIAN_POINT ( 'NONE',  ( 7.683128691873284843, 153.7401750098334503, -4.275384889837861024 ) ) ;
#22385=ADVANCED_FACE ( 'NONE', ( #54025 ), #1641, .T. ) ;
#22389=CARTESIAN_POINT ( 'NONE',  ( 6.826472737025119919, 160.8929263765338078, 4.959722759717908325 ) ) ;
#22396=CARTESIAN_POINT ( 'NONE',  ( 48.00000000000000000, 99.99999999999992895, -9.500000000000000000 ) ) ;
#22397=CARTESIAN_POINT ( 'NONE',  ( 55.65811388300842566, 13.02565835097472657, -6.000000000000000000 ) ) ;
#22399=MECHANICAL_DESIGN_GEOMETRIC_PRESENTATION_REPRESENTATION('',(#15649),#58348);
#22403=( LENGTH_UNIT ( ) NAMED_UNIT ( * ) SI_UNIT ( .MILLI., .METRE. ) );
#22404=CARTESIAN_POINT ( 'NONE',  ( -0.5396081309076679045, 154.1248569342653809, 9.149856934265343966 ) ) ;
#22406=MECHANICAL_DESIGN_GEOMETRIC_PRESENTATION_REPRESENTATION('',(#47159),#60594);
#22408=EDGE_CURVE ( 'NONE', #27227, #59919, #63156, .T. ) ;
#22409=CYLINDRICAL_SURFACE ( 'NONE', #25592, 7.999999999999992895 ) ;
#22418=VECTOR ( 'NONE', #54314, 1000.000000000000000 ) ;
#22419=VERTEX_POINT ( 'NONE', #33957 ) ;
#22421=CARTESIAN_POINT ( 'NONE',  ( 44.56131952741601765, 9.853773175805232043, 3.472780323909878675 ) ) ;
#22423=DIRECTION ( 'NONE',  ( 1.000000000000000000, 0.000000000000000000, 0.000000000000000000 ) ) ;
#22429=CARTESIAN_POINT ( 'NONE',  ( 9.058813317711337021, 139.6550000000000011, 2.943386871421375783 ) ) ;
#22431=EDGE_CURVE ( 'NONE', #11358, #8903, #39978, .T. ) ;
#22433=CIRCLE ( 'NONE', #7808, 0.5000000000000004441 ) ;
#22434=CARTESIAN_POINT ( 'NONE',  ( 1.447422522084233387, 154.2051516657656691, 9.145303841767301378 ) ) ;
#22436=B_SPLINE_CURVE_WITH_KNOTS ( 'NONE', 3,
 ( #56796, #36422, #3991, #57479, #25120, #8949 ),
 .UNSPECIFIED., .F., .F.,
 ( 4, 2, 4 ),
 ( 0.000000000000000000, 0.0003110060432796291855, 0.0006220120865592583710 ),
 .UNSPECIFIED. ) ;
#22437=AXIS2_PLACEMENT_3D ( 'NONE', #10655, #64107, #15962 ) ;
#22440=ORIENTED_EDGE ( 'NONE', *, *, #63078, .T. ) ;
#22442=FILL_AREA_STYLE ('',( #49884 ) ) ;
#22444=CIRCLE ( 'NONE', #19054, 13.50000000000000178 ) ;
#22446=SURFACE_STYLE_FILL_AREA ( #16164 ) ;
#22450=DIRECTION ( 'NONE',  ( -0.000000000000000000, -0.000000000000000000, 1.000000000000000000 ) ) ;
#22451=DIRECTION ( 'NONE',  ( -1.000000000000000000, 0.000000000000000000, 0.000000000000000000 ) ) ;
#22454=FILL_AREA_STYLE ('',( #28036 ) ) ;
#22457=CARTESIAN_POINT ( 'NONE',  ( 0.000000000000000000, 140.9429263765338192, -8.025000000000000355 ) ) ;
#22465=ORIENTED_EDGE ( 'NONE', *, *, #3539, .F. ) ;
#22468=DIRECTION ( 'NONE',  ( -0.000000000000000000, 1.000000000000000000, -0.000000000000000000 ) ) ;
#22470=CARTESIAN_POINT ( 'NONE',  ( 5.598654528085809545, 157.1449999999999818, -7.705886871421373741 ) ) ;
#22472=VERTEX_POINT ( 'NONE', #7923 ) ;
#22473=ORIENTED_EDGE ( 'NONE', *, *, #57270, .F. ) ;
#22475=CARTESIAN_POINT ( 'NONE',  ( 21.02379604162863913, 154.9999999999999716, -10.50000000000000000 ) ) ;
#22477=CARTESIAN_POINT ( 'NONE',  ( 7.632228543268607446, 134.0429263765338135, 2.479861379858954606 ) ) ;
#22481=ADVANCED_FACE ( 'NONE', ( #24106 ), #24431, .T. ) ;
#22483=ORIENTED_EDGE ( 'NONE', *, *, #38670, .T. ) ;
#22489=DIRECTION ( 'NONE',  ( 1.000000000000000000, 0.000000000000000000, 0.000000000000000000 ) ) ;
#22490=CARTESIAN_POINT ( 'NONE',  ( 71.50000000000000000, 14.49137674618942562, 7.500000000000000000 ) ) ;
#22493=DIRECTION ( 'NONE',  ( -0.000000000000000000, -0.000000000000000000, 1.000000000000000000 ) ) ;
#22497=COLOUR_RGB ( '', 0.31764706, 0.68627451, 0.89019608) ;
#22500=CIRCLE ( 'NONE', #31465, 0.5000000000000004441 ) ;
#22501=ORIENTED_EDGE ( 'NONE', *, *, #10722, .T. ) ;
#22502=CARTESIAN_POINT ( 'NONE',  ( -45.03910207541591859, 8.121286912818771242, 3.616120970039215621 ) ) ;
#22507=LINE ( 'NONE', #48590, #59527 ) ;
#22508=DIRECTION ( 'NONE',  ( 0.000000000000000000, 0.000000000000000000, -1.000000000000000000 ) ) ;
#22510=CARTESIAN_POINT ( 'NONE',  ( 23.71231517720798010, 113.4999999999999858, 9.500000000000000000 ) ) ;
#22511=STYLED_ITEM ( 'NONE', ( #9833 ), #17576 ) ;
#22515=VERTEX_POINT ( 'NONE', #31717 ) ;
#22517=CARTESIAN_POINT ( 'NONE',  ( -60.00000000000000000, -2.024042244987997205E-14, -6.500000000000000000 ) ) ;
#22523=CARTESIAN_POINT ( 'NONE',  ( 8.102448949553181734, 159.3949999999999534, 5.886773742842750679 ) ) ;
#22529=LINE ( 'NONE', #65437, #59545 ) ;
#22536=FILL_AREA_STYLE_COLOUR ( '', #24913 ) ;
#22538=ORIENTED_EDGE ( 'NONE', *, *, #53279, .F. ) ;
#22539=AXIS2_PLACEMENT_3D ( 'NONE', #22112, #1640, #64998 ) ;
#22546=EDGE_LOOP ( 'NONE', ( #11306, #18687, #10264, #50099 ) ) ;
#22556=CARTESIAN_POINT ( 'NONE',  ( -10.01517768586949231, 134.1949999999999932, -6.132527647946036459E-16 ) ) ;
#22557=CARTESIAN_POINT ( 'NONE',  ( 71.62068965517239860, 36.41396814395972115, -9.500000000000000000 ) ) ;
#22558=AXIS2_PLACEMENT_3D ( 'NONE', #43854, #37901, #11096 ) ;
#22559=EDGE_CURVE ( 'NONE', #49424, #2072, #48285, .T. ) ;
#22561=EDGE_LOOP ( 'NONE', ( #49076, #33705 ) ) ;
#22562=CARTESIAN_POINT ( 'NONE',  ( -5.598654528085806881, 125.8549999999999898, -7.705886871421374629 ) ) ;
#22565=CARTESIAN_POINT ( 'NONE',  ( -0.9728900412908211282, 153.0000000000000000, -7.965808808122195828 ) ) ;
#22567=CARTESIAN_POINT ( 'NONE',  ( -10.01517768586949231, 153.3050000000000068, -6.132527647946036459E-16 ) ) ;
#22569=COLOUR_RGB ( '', 0.72549020, 0.75294118, 0.79215686) ;
#22570=EDGE_CURVE ( 'NONE', #47273, #61027, #21876, .T. ) ;
#22571=DIRECTION ( 'NONE',  ( 0.000000000000000000, -1.000000000000000000, 0.000000000000000000 ) ) ;
#22572=LINE ( 'NONE', #21888, #66509 ) ;
#22574=EDGE_CURVE ( 'NONE', #26003, #7688, #35073, .T. ) ;
#22576=CARTESIAN_POINT ( 'NONE',  ( -15.98999599679679839, 50.00000000000000000, 7.000000000000000000 ) ) ;
#22582=( NAMED_UNIT ( * ) PLANE_ANGLE_UNIT ( ) SI_UNIT ( $, .RADIAN. ) );
#22584=EDGE_CURVE ( 'NONE', #30995, #53241, #5317, .T. ) ;
#22587=( NAMED_UNIT ( * ) PLANE_ANGLE_UNIT ( ) SI_UNIT ( $, .RADIAN. ) );
#22589=ORIENTED_EDGE ( 'NONE', *, *, #63854, .T. ) ;
#22596=MECHANICAL_DESIGN_GEOMETRIC_PRESENTATION_REPRESENTATION('',(#4600),#36115);
#22597=SURFACE_STYLE_USAGE ( .BOTH. , #27147 ) ;
#22598=( LENGTH_UNIT ( ) NAMED_UNIT ( * ) SI_UNIT ( .MILLI., .METRE. ) );
#22603=B_SPLINE_CURVE_WITH_KNOTS ( 'NONE', 3,
 ( #39489, #12710, #34186, #55639, #45123, #49014 ),
 .UNSPECIFIED., .F., .F.,
 ( 4, 2, 4 ),
 ( 0.000000000000000000, 0.0003058591473678601161, 0.0006117182947357202322 ),
 .UNSPECIFIED. ) ;
#22604=VECTOR ( 'NONE', #4974, 1000.000000000000000 ) ;
#22607=CARTESIAN_POINT ( 'NONE',  ( 9.058813317711337021, 126.5449999999999875, 2.943386871421375783 ) ) ;
#22614=VECTOR ( 'NONE', #61568, 1000.000000000000000 ) ;
#22615=DIRECTION ( 'NONE',  ( 0.000000000000000000, 1.000000000000000000, -0.000000000000000000 ) ) ;
#22617=ORIENTED_EDGE ( 'NONE', *, *, #8349, .T. ) ;
#22622=B_SPLINE_CURVE_WITH_KNOTS ( 'NONE', 3,
 ( #50910, #47054, #25537, #51259, #52322, #62137, #61777, #24163, #18870, #9042, #30462, #62826, #35770, #3719 ),
 .UNSPECIFIED., .F., .F.,
 ( 4, 2, 2, 2, 2, 2, 4 ),
 ( 5.830426119014177358E-15, 0.002172676916780083827, 0.003259015375167209454, 0.004345353833554335514, 0.005431692291941461574, 0.006518030750328586767, 0.008690707667102838888 ),
 .UNSPECIFIED. ) ;
#22624=( LENGTH_UNIT ( ) NAMED_UNIT ( * ) SI_UNIT ( .MILLI., .METRE. ) );
#22626=COLOUR_RGB ( '', 0.40784314, 0.44705882, 0.49803922) ;
#22629=CARTESIAN_POINT ( 'NONE',  ( 44.28021770739999852, 9.999999999999980460, -3.500000000000000000 ) ) ;
#22632=ORIENTED_EDGE ( 'NONE', *, *, #13245, .T. ) ;
#22634=ORIENTED_EDGE ( 'NONE', *, *, #55032, .F. ) ;
#22635=CARTESIAN_POINT ( 'NONE',  ( -55.00000000000000000, -2.024042244987997205E-14, 11.50000000000003020 ) ) ;
#22636=COLOUR_RGB ( '', 0.40784314, 0.44705882, 0.49803922) ;
#22638=ADVANCED_FACE ( 'NONE', ( #52858, #36710 ), #9936, .T. ) ;
#22641=CARTESIAN_POINT ( 'NONE',  ( -4.716976649647098618, 152.2570736234661695, 6.492361379858953008 ) ) ;
#22645=AXIS2_PLACEMENT_3D ( 'NONE', #6173, #11448, #44555 ) ;
#22646=CARTESIAN_POINT ( 'NONE',  ( 7.632228543268608334, 132.4570736234661581, -2.479861379858951942 ) ) ;
#22647=LINE ( 'NONE', #17401, #67613 ) ;
#22648=CARTESIAN_POINT ( 'NONE',  ( 60.00000000000000000, 1.797044900979284448E-15, -11.50000000000000000 ) ) ;
#22649=CARTESIAN_POINT ( 'NONE',  ( 71.50000000000000000, 35.92875272052971525, 7.000000000000000000 ) ) ;
#22652=( LENGTH_UNIT ( ) NAMED_UNIT ( * ) SI_UNIT ( .MILLI., .METRE. ) );
#22653=EDGE_LOOP ( 'NONE', ( #25154, #17605, #65305, #26165 ) ) ;
#22654=DIRECTION ( 'NONE',  ( 0.000000000000000000, 0.000000000000000000, 1.000000000000000000 ) ) ;
#22657=( NAMED_UNIT ( * ) PLANE_ANGLE_UNIT ( ) SI_UNIT ( $, .RADIAN. ) );
#22659=SURFACE_STYLE_USAGE ( .BOTH. , #64862 ) ;
#22660=CARTESIAN_POINT ( 'NONE',  ( -45.00000000000000000, 8.443649368548083345, -5.542175914092441147 ) ) ;
#22661=ADVANCED_FACE ( 'NONE', ( #680 ), #49645, .T. ) ;
#22662=ORIENTED_EDGE ( 'NONE', *, *, #63219, .T. ) ;
#22664=ORIENTED_EDGE ( 'NONE', *, *, #51566, .F. ) ;
#22665=CIRCLE ( 'NONE', #47467, 0.5000000000000006661 ) ;
#22667=CARTESIAN_POINT ( 'NONE',  ( -75.00000000000000000, 9.517485987480760912, 6.449082597785469773 ) ) ;
#22671=SURFACE_STYLE_USAGE ( .BOTH. , #65924 ) ;
#22672=( NAMED_UNIT ( * ) PLANE_ANGLE_UNIT ( ) SI_UNIT ( $, .RADIAN. ) );
#22673=FILL_AREA_STYLE_COLOUR ( '', #35341 ) ;
#22674=DIRECTION ( 'NONE',  ( 0.000000000000000000, 1.000000000000000000, 0.000000000000000000 ) ) ;
#22676=CARTESIAN_POINT ( 'NONE',  ( 8.102448949553179958, 132.3949999999999534, 5.886773742842750679 ) ) ;
#22678=CIRCLE ( 'NONE', #4688, 4.999999999999997335 ) ;
#22681=ORIENTED_EDGE ( 'NONE', *, *, #22408, .F. ) ;
#22682=DIRECTION ( 'NONE',  ( 0.000000000000000000, 0.000000000000000000, -1.000000000000000000 ) ) ;
#22684=DIRECTION ( 'NONE',  ( 0.000000000000000000, 0.000000000000000000, 1.000000000000000000 ) ) ;
#22693=VERTEX_POINT ( 'NONE', #22557 ) ;
#22694=CARTESIAN_POINT ( 'NONE',  ( -44.50000000000000000, 99.99999999999992895, -3.500000000000000000 ) ) ;
#22700=SURFACE_STYLE_USAGE ( .BOTH. , #49445 ) ;
#22703=SURFACE_SIDE_STYLE ('',( #39252 ) ) ;
#22704=CARTESIAN_POINT ( 'NONE',  ( -15.98999599679679839, 50.00000000000000000, 7.500000000000000000 ) ) ;
#22706=MECHANICAL_DESIGN_GEOMETRIC_PRESENTATION_REPRESENTATION('',(#54175),#67642);
#22707=CARTESIAN_POINT ( 'NONE',  ( -45.00000000000000000, 9.708372675170618749, -3.611004237778681514 ) ) ;
#22716=EDGE_CURVE ( 'NONE', #22912, #56203, #10398, .T. ) ;
#22718=ORIENTED_EDGE ( 'NONE', *, *, #4682, .T. ) ;
#22723=CARTESIAN_POINT ( 'NONE',  ( -8.437984349512095861, 127.8070736234661666, -5.166775262442723748E-16 ) ) ;
#22724=STYLED_ITEM ( 'NONE', ( #1403 ), #46191 ) ;
#22726=DIRECTION ( 'NONE',  ( 0.000000000000000000, 0.000000000000000000, -1.000000000000000000 ) ) ;
#22727=DIRECTION ( 'NONE',  ( -8.673617379884027583E-15, 1.295453483465570108E-14, 1.000000000000000000 ) ) ;
#22728=VECTOR ( 'NONE', #33624, 1000.000000000000000 ) ;
#22735=( GEOMETRIC_REPRESENTATION_CONTEXT ( 3 ) GLOBAL_UNCERTAINTY_ASSIGNED_CONTEXT ( ( #20205 ) ) GLOBAL_UNIT_ASSIGNED_CONTEXT ( ( #22211, #34490, #60864 ) ) REPRESENTATION_CONTEXT ( 'NONE', 'WORKASPACE' ) );
#22747=FACE_OUTER_BOUND ( 'NONE', #50544, .T. ) ;
#22750=VERTEX_POINT ( 'NONE', #61544 ) ;
#22751=CIRCLE ( 'NONE', #59856, 0.5000000000000004441 ) ;
#22758=CARTESIAN_POINT ( 'NONE',  ( 60.00000000000000000, 1.797044900979284448E-15, 11.50000000000003730 ) ) ;
#22760=COLOUR_RGB ( '', 0.40784314, 0.44705882, 0.49803922) ;
#22762=CARTESIAN_POINT ( 'NONE',  ( -5.871527698221338909, 153.2522028323956533, -5.859198738425243747 ) ) ;
#22765=DIRECTION ( 'NONE',  ( 0.000000000000000000, 0.000000000000000000, 1.000000000000000000 ) ) ;
#22766=DIRECTION ( 'NONE',  ( 0.000000000000000000, 0.000000000000000000, -1.000000000000000000 ) ) ;
#22769=EDGE_LOOP ( 'NONE', ( #34497, #55309, #54630, #46034 ) ) ;
#22774=VECTOR ( 'NONE', #62874, 1000.000000000000000 ) ;
#22775=AXIS2_PLACEMENT_3D ( 'NONE', #65624, #17468, #38936 ) ;
#22777=ORIENTED_EDGE ( 'NONE', *, *, #3952, .T. ) ;
#22779=SURFACE_STYLE_USAGE ( .BOTH. , #49520 ) ;
#22780=CARTESIAN_POINT ( 'NONE',  ( 45.65811388296465623, 10.21937129432154556, 3.824795692829482174 ) ) ;
#22783=DIRECTION ( 'NONE',  ( 1.000000000000000000, 0.000000000000000000, 0.000000000000000000 ) ) ;
#22787=CARTESIAN_POINT ( 'NONE',  ( -10.01517768586949231, 141.3050000000000068, -6.132527647946036459E-16 ) ) ;
#22792=AXIS2_PLACEMENT_3D ( 'NONE', #10637, #47635, #20852 ) ;
#22802=CARTESIAN_POINT ( 'NONE',  ( 72.49999999999998579, 119.9999999999997868, -10.00000000000000000 ) ) ;
#22807=VECTOR ( 'NONE', #5969, 1000.000000000000000 ) ;
#22809=PRESENTATION_STYLE_ASSIGNMENT (( #1275 ) ) ;
#22810=DIRECTION ( 'NONE',  ( 0.000000000000000000, 0.000000000000000000, -1.000000000000000000 ) ) ;
#22814=ORIENTED_EDGE ( 'NONE', *, *, #32910, .T. ) ;
#22816=ORIENTED_EDGE ( 'NONE', *, *, #55015, .T. ) ;
#22819=EDGE_LOOP ( 'NONE', ( #58029, #6132, #31803, #44096 ) ) ;
#22820=FACE_BOUND ( 'NONE', #64205, .T. ) ;
#22825=CARTESIAN_POINT ( 'NONE',  ( -3.094860106618432471, 157.5949999999999989, -9.525000000000000355 ) ) ;
#22830=SURFACE_STYLE_FILL_AREA ( #33036 ) ;
#22832=CARTESIAN_POINT ( 'NONE',  ( -2.607480562269073765, 138.0929263765337964, -8.025000000000000355 ) ) ;
#22836=CARTESIAN_POINT ( 'NONE',  ( -7.632228543268607446, 114.5429263765338277, -2.479861379858953718 ) ) ;
#22837=ADVANCED_FACE ( 'NONE', ( #31632 ), #20389, .F. ) ;
#22843=SURFACE_STYLE_USAGE ( .BOTH. , #38367 ) ;
#22844=DIRECTION ( 'NONE',  ( 0.000000000000000000, 0.000000000000000000, 1.000000000000000000 ) ) ;
#22848=UNCERTAINTY_MEASURE_WITH_UNIT (LENGTH_MEASURE( 1.000000000000000082E-05 ), #12733, 'distance_accuracy_value', 'NONE');
#22849=VERTEX_POINT ( 'NONE', #42581 ) ;
#22854=CARTESIAN_POINT ( 'NONE',  ( -9.827790563157511022E-16, 118.4429263765338192, 8.025000000000000355 ) ) ;
#22855=ORIENTED_EDGE ( 'NONE', *, *, #28812, .T. ) ;
#22856=ORIENTED_EDGE ( 'NONE', *, *, #19610, .F. ) ;
#22857=CARTESIAN_POINT ( 'NONE',  ( -45.20196116979489176, 8.361269815420033780, 3.290768940563960854 ) ) ;
#22862=SURFACE_STYLE_FILL_AREA ( #28438 ) ;
#22863=SURFACE_SIDE_STYLE ('',( #40431 ) ) ;
#22864=DIRECTION ( 'NONE',  ( -1.000000000000000000, 0.000000000000000000, 0.000000000000000000 ) ) ;
#22867=ORIENTED_EDGE ( 'NONE', *, *, #42993, .T. ) ;
#22869=VECTOR ( 'NONE', #10439, 1000.000000000000000 ) ;
#22870=LINE ( 'NONE', #50292, #12466 ) ;
#22874=CARTESIAN_POINT ( 'NONE',  ( 3.094860106618435136, 157.2949999999999591, -9.525000000000000355 ) ) ;
#22878=COLOUR_RGB ( '', 0.08235294, 0.09019608, 0.10196078) ;
#22881=FILL_AREA_STYLE_COLOUR ( '', #67408 ) ;
#22882=CARTESIAN_POINT ( 'NONE',  ( 23.71231517720798010, 113.4999999999999858, -10.00000000000000000 ) ) ;
#22883=UNCERTAINTY_MEASURE_WITH_UNIT (LENGTH_MEASURE( 1.000000000000000082E-05 ), #50936, 'distance_accuracy_value', 'NONE');
#22884=SURFACE_SIDE_STYLE ('',( #17286 ) ) ;
#22888=EDGE_CURVE ( 'NONE', #19090, #34565, #36329, .T. ) ;
#22892=CARTESIAN_POINT ( 'NONE',  ( -75.00000000000000000, 9.708372675170620525, 6.000000000000000888 ) ) ;
#22894=CIRCLE ( 'NONE', #35236, 29.50000000000000000 ) ;
#22900=( BOUNDED_CURVE ( )  B_SPLINE_CURVE ( 2, ( #48797, #26579, #11102, #48448, #64594, #27616, #69179, #16766, #20981, #31517, #42478 ),
 .UNSPECIFIED., .F., .F. ) 
 B_SPLINE_CURVE_WITH_KNOTS ( ( 3, 2, 2, 2, 2, 3 ),
 ( 0.5294117647058825815, 0.5352941176470590312, 0.5411764705882354809, 0.5470588235294120416, 0.5529411764705884913, 0.5588235294117649410 ),
 .UNSPECIFIED. ) 
 CURVE ( )  GEOMETRIC_REPRESENTATION_ITEM ( )  RATIONAL_B_SPLINE_CURVE ( ( 0.9999999999999981126, 0.9510565162951554186, 1.000000000000000000, 0.9510565162951535312, 1.000000000000000000, 0.9510565162951535312, 1.000000000000000000, 0.9510565162951535312, 1.000000000000000000, 0.9510565162951516438, 1.000000000000001776 ) ) 
 REPRESENTATION_ITEM ( '' )  );
#22901=CARTESIAN_POINT ( 'NONE',  ( 24.21231517720798010, 112.9999999999999858, 7.500000000000000000 ) ) ;
#22902=( NAMED_UNIT ( * ) PLANE_ANGLE_UNIT ( ) SI_UNIT ( $, .RADIAN. ) );
#22908=EDGE_LOOP ( 'NONE', ( #19004, #4826, #54228, #60748, #22718, #6957, #25398, #45036 ) ) ;
#22910=ORIENTED_EDGE ( 'NONE', *, *, #8592, .F. ) ;
#22912=VERTEX_POINT ( 'NONE', #48903 ) ;
#22913=CARTESIAN_POINT ( 'NONE',  ( -12.72792206135785698, 115.4999999999999574, -10.50000000000000000 ) ) ;
#22916=CARTESIAN_POINT ( 'NONE',  ( 3.094860106618431583, 126.0949999999999847, 9.525000000000000355 ) ) ;
#22919=STYLED_ITEM ( 'NONE', ( #53793 ), #7618 ) ;
#22920=DIRECTION ( 'NONE',  ( 0.000000000000000000, -1.000000000000000000, -0.000000000000000000 ) ) ;
#22921=CARTESIAN_POINT ( 'NONE',  ( 8.102448949553179958, 127.5049999999999812, 5.886773742842750679 ) ) ;
#22923=PRESENTATION_STYLE_ASSIGNMENT (( #23591 ) ) ;
#22925=CARTESIAN_POINT ( 'NONE',  ( 3.094860106618431583, 157.2050000000000125, 9.525000000000000355 ) ) ;
#22927=UNCERTAINTY_MEASURE_WITH_UNIT (LENGTH_MEASURE( 1.000000000000000082E-05 ), #39450, 'distance_accuracy_value', 'NONE');
#22929=SURFACE_STYLE_USAGE ( .BOTH. , #60878 ) ;
#22930=ORIENTED_EDGE ( 'NONE', *, *, #9603, .F. ) ;
#22931=SURFACE_SIDE_STYLE ('',( #65118 ) ) ;
#22933=AXIS2_PLACEMENT_3D ( 'NONE', #50233, #55839, #46370 ) ;
#22934=COLOUR_RGB ( '', 0.66274510, 0.83137255, 0.94901961) ;
#22935=CARTESIAN_POINT ( 'NONE',  ( -67.49999999999998579, -1.932193735051945844E-14, 11.50000000000000000 ) ) ;
#22937=ORIENTED_EDGE ( 'NONE', *, *, #51175, .F. ) ;
#22939=UNCERTAINTY_MEASURE_WITH_UNIT (LENGTH_MEASURE( 1.000000000000000082E-05 ), #36645, 'distance_accuracy_value', 'NONE');
#22943=EDGE_LOOP ( 'NONE', ( #62109, #52704, #42093 ) ) ;
#22948=VECTOR ( 'NONE', #42107, 1000.000000000000000 ) ;
#22952=EDGE_LOOP ( 'NONE', ( #11157, #45045, #32069, #55675 ) ) ;
#22954=SURFACE_STYLE_FILL_AREA ( #48332 ) ;
#22956=AXIS2_PLACEMENT_3D ( 'NONE', #69356, #46908, #58795 ) ;
#22957=CARTESIAN_POINT ( 'NONE',  ( -10.01517768586949231, 128.1950000000000216, -6.132527647946036459E-16 ) ) ;
#22962=SURFACE_STYLE_USAGE ( .BOTH. , #2109 ) ;
#22968=EDGE_CURVE ( 'NONE', #45132, #43730, #54253, .T. ) ;
#22972=ORIENTED_EDGE ( 'NONE', *, *, #31106, .F. ) ;
#22977=CARTESIAN_POINT ( 'NONE',  ( -45.91158085204516226, 9.415459729490459395, 6.077763577362913949 ) ) ;
#22978=FILL_AREA_STYLE ('',( #1448 ) ) ;
#22987=B_SPLINE_CURVE_WITH_KNOTS ( 'NONE', 3,
 ( #51110, #68324, #35624, #13446, #24681, #41608, #29642, #7827, #8195, #34560 ),
 .UNSPECIFIED., .F., .F.,
 ( 4, 2, 2, 2, 4 ),
 ( 0.000000000000000000, 0.0004222318702814410588, 0.0008444637405628821177, 0.001266695610844323231, 0.001688927481125764235 ),
 .UNSPECIFIED. ) ;
#22988=MECHANICAL_DESIGN_GEOMETRIC_PRESENTATION_REPRESENTATION('',(#42119),#35338);
#22990=( LENGTH_UNIT ( ) NAMED_UNIT ( * ) SI_UNIT ( .MILLI., .METRE. ) );
#22994=( NAMED_UNIT ( * ) PLANE_ANGLE_UNIT ( ) SI_UNIT ( $, .RADIAN. ) );
#22995=CARTESIAN_POINT ( 'NONE',  ( -8.437984349512095861, 151.8070736234661524, -5.166775262442723748E-16 ) ) ;
#22996=( GEOMETRIC_REPRESENTATION_CONTEXT ( 3 ) GLOBAL_UNCERTAINTY_ASSIGNED_CONTEXT ( ( #14382 ) ) GLOBAL_UNIT_ASSIGNED_CONTEXT ( ( #20916, #63803, #48370 ) ) REPRESENTATION_CONTEXT ( 'NONE', 'WORKASPACE' ) );
#22998=EDGE_LOOP ( 'NONE', ( #3725, #10488, #24868, #26042 ) ) ;
#23000=CARTESIAN_POINT ( 'NONE',  ( 9.058813317711338797, 127.9549999999999841, -2.943386871421372675 ) ) ;
#23001=UNCERTAINTY_MEASURE_WITH_UNIT (LENGTH_MEASURE( 1.000000000000000082E-05 ), #60531, 'distance_accuracy_value', 'NONE');
#23004=FACE_OUTER_BOUND ( 'NONE', #43747, .T. ) ;
#23006=ORIENTED_EDGE ( 'NONE', *, *, #46837, .T. ) ;
#23007=DIRECTION ( 'NONE',  ( 0.000000000000000000, 0.000000000000000000, 1.000000000000000000 ) ) ;
#23010=ORIENTED_EDGE ( 'NONE', *, *, #63780, .F. ) ;
#23011=STYLED_ITEM ( 'NONE', ( #15452 ), #27490 ) ;
#23013=CARTESIAN_POINT ( 'NONE',  ( -45.66531550846541876, 8.455116999143502454, -6.464599779185706829 ) ) ;
#23014=ORIENTED_EDGE ( 'NONE', *, *, #47577, .T. ) ;
#23018=ORIENTED_EDGE ( 'NONE', *, *, #64732, .T. ) ;
#23020=LINE ( 'NONE', #55360, #40440 ) ;
#23024=PRESENTATION_STYLE_ASSIGNMENT (( #49415 ) ) ;
#23025=DIRECTION ( 'NONE',  ( 1.000000000000000000, -1.156482317317873451E-16, 0.000000000000000000 ) ) ;
#23028=STYLED_ITEM ( 'NONE', ( #40059 ), #5800 ) ;
#23029=( NAMED_UNIT ( * ) SI_UNIT ( $, .STERADIAN. ) SOLID_ANGLE_UNIT ( ) );
#23030=CARTESIAN_POINT ( 'NONE',  ( -10.01517768586949408, 134.1949999999999932, -6.132527647946036459E-16 ) ) ;
#23034=CIRCLE ( 'NONE', #17433, 0.9999999999999991118 ) ;
#23035=SURFACE_STYLE_FILL_AREA ( #53981 ) ;
#23038=AXIS2_PLACEMENT_3D ( 'NONE', #32305, #5555, #22451 ) ;
#23040=FILL_AREA_STYLE_COLOUR ( '', #39266 ) ;
#23041=CARTESIAN_POINT ( 'NONE',  ( -20.71231517720798010, 146.9999999999999716, 7.000000000000000000 ) ) ;
#23049=SURFACE_STYLE_USAGE ( .BOTH. , #5799 ) ;
#23050=( NAMED_UNIT ( * ) SI_UNIT ( $, .STERADIAN. ) SOLID_ANGLE_UNIT ( ) );
#23058=LINE ( 'NONE', #66293, #24485 ) ;
#23059=SURFACE_STYLE_USAGE ( .BOTH. , #44888 ) ;
#23062=FILL_AREA_STYLE ('',( #28290 ) ) ;
#23063=AXIS2_PLACEMENT_3D ( 'NONE', #20134, #25767, #42014 ) ;
#23064=DIRECTION ( 'NONE',  ( -0.000000000000000000, -0.000000000000000000, 1.000000000000000000 ) ) ;
#23065=VECTOR ( 'NONE', #36761, 1000.000000000000000 ) ;
#23068=CARTESIAN_POINT ( 'NONE',  ( -40.78947368421051323, 108.1536491499103505, 3.000000000000000444 ) ) ;
#23069=EDGE_LOOP ( 'NONE', ( #52423, #27036, #55456, #28119 ) ) ;
#23073=ORIENTED_EDGE ( 'NONE', *, *, #11167, .F. ) ;
#23076=CARTESIAN_POINT ( 'NONE',  ( 4.716976649647099507, 123.7570736234661695, -6.492361379858953008 ) ) ;
#23077=CARTESIAN_POINT ( 'NONE',  ( 20.88905466131707200, 149.9999999999999432, 9.626351540309148191 ) ) ;
#23078=CARTESIAN_POINT ( 'NONE',  ( -45.50000000000000000, 9.708372675170618749, 3.611004237778671744 ) ) ;
#23080=ORIENTED_EDGE ( 'NONE', *, *, #47236, .T. ) ;
#23085=CARTESIAN_POINT ( 'NONE',  ( -40.99999999999997868, 10.49999999999998224, 3.000000000000000000 ) ) ;
#23087=( GEOMETRIC_REPRESENTATION_CONTEXT ( 3 ) GLOBAL_UNCERTAINTY_ASSIGNED_CONTEXT ( ( #12290 ) ) GLOBAL_UNIT_ASSIGNED_CONTEXT ( ( #56295, #60203, #6721 ) ) REPRESENTATION_CONTEXT ( 'NONE', 'WORKASPACE' ) );
#23090=ORIENTED_EDGE ( 'NONE', *, *, #5163, .F. ) ;
#23093=CARTESIAN_POINT ( 'NONE',  ( -74.99999999999998579, 50.00000000000000000, 10.00000000000000000 ) ) ;
#23094=FILL_AREA_STYLE_COLOUR ( '', #22105 ) ;
#23095=DIRECTION ( 'NONE',  ( 0.000000000000000000, 0.000000000000000000, -1.000000000000000000 ) ) ;
#23097=EDGE_LOOP ( 'NONE', ( #36243, #68586, #65373, #257 ) ) ;
#23099=CARTESIAN_POINT ( 'NONE',  ( -24.21231517720798010, 117.4999999999999716, -7.500000000000000000 ) ) ;
#23105=CARTESIAN_POINT ( 'NONE',  ( 71.18918918918917882, 14.09971791521133255, -7.000000000000000000 ) ) ;
#23106=SURFACE_STYLE_USAGE ( .BOTH. , #67386 ) ;
#23109=FILL_AREA_STYLE ('',( #44602 ) ) ;
#23114=LINE ( 'NONE', #44608, #54893 ) ;
#23116=CARTESIAN_POINT ( 'NONE',  ( 7.632228543268608334, 122.3429263765338249, -2.479861379858951942 ) ) ;
#23118=SURFACE_STYLE_USAGE ( .BOTH. , #543 ) ;
#23121=SURFACE_STYLE_FILL_AREA ( #29411 ) ;
#23124=EDGE_CURVE ( 'NONE', #23699, #34665, #17085, .T. ) ;
#23125=DIRECTION ( 'NONE',  ( 0.000000000000000000, 0.000000000000000000, 1.000000000000000000 ) ) ;
#23129=VECTOR ( 'NONE', #32654, 1000.000000000000000 ) ;
#23132=EDGE_CURVE ( 'NONE', #61898, #24543, #57237, .T. ) ;
#23133=DIRECTION ( 'NONE',  ( 1.000000000000000000, 0.000000000000000000, 0.000000000000000000 ) ) ;
#23134=( NAMED_UNIT ( * ) PLANE_ANGLE_UNIT ( ) SI_UNIT ( $, .RADIAN. ) );
#23139=CARTESIAN_POINT ( 'NONE',  ( 0.000000000000000000, 149.5550000000000068, -9.525000000000000355 ) ) ;
#23142=EDGE_CURVE ( 'NONE', #16451, #56993, #44214, .T. ) ;
#23143=AXIS2_PLACEMENT_3D ( 'NONE', #67221, #3142, #35219 ) ;
#23147=EDGE_CURVE ( 'NONE', #34665, #36214, #8015, .T. ) ;
#23148=CARTESIAN_POINT ( 'NONE',  ( -60.00000000000000000, -2.024042244987997205E-14, 10.00000000000000000 ) ) ;
#23149=CARTESIAN_POINT ( 'NONE',  ( -75.00000000000000000, 35.50862325381056905, -6.500000000000000888 ) ) ;
#23150=DIRECTION ( 'NONE',  ( 0.000000000000000000, 1.000000000000000000, 0.000000000000000000 ) ) ;
#23151=LINE ( 'NONE', #55836, #24968 ) ;
#23153=ORIENTED_EDGE ( 'NONE', *, *, #50141, .F. ) ;
#23154=( NAMED_UNIT ( * ) PLANE_ANGLE_UNIT ( ) SI_UNIT ( $, .RADIAN. ) );
#23155=LINE ( 'NONE', #53847, #66 ) ;
#23156=AXIS2_PLACEMENT_3D ( 'NONE', #53983, #64196, #65236 ) ;
#23157=CARTESIAN_POINT ( 'NONE',  ( 75.00000000000000000, -2.215169945516535778E-14, -7.000000000000000888 ) ) ;
#23158=SURFACE_STYLE_FILL_AREA ( #17874 ) ;
#23161=VERTEX_POINT ( 'NONE', #61457 ) ;
#23162=AXIS2_PLACEMENT_3D ( 'NONE', #29832, #9437, #26281 ) ;
#23170=DIRECTION ( 'NONE',  ( 0.000000000000000000, 0.000000000000000000, -1.000000000000000000 ) ) ;
#23171=CARTESIAN_POINT ( 'NONE',  ( -48.50000000000000000, 14.49137674618942562, 10.00000000000000000 ) ) ;
#23174=EDGE_LOOP ( 'NONE', ( #6925, #62428, #34310, #42346 ) ) ;
#23177=( LENGTH_UNIT ( ) NAMED_UNIT ( * ) SI_UNIT ( .MILLI., .METRE. ) );
#23179=CARTESIAN_POINT ( 'NONE',  ( -6.826472737025120807, 138.3929263765337794, -4.959722759717907437 ) ) ;
#23182=FACE_OUTER_BOUND ( 'NONE', #13138, .T. ) ;
#23184=CARTESIAN_POINT ( 'NONE',  ( -8.437984349512095861, 114.6929263765338050, -5.166775262442723748E-16 ) ) ;
#23185=VERTEX_POINT ( 'NONE', #40749 ) ;
#23189=( NAMED_UNIT ( * ) PLANE_ANGLE_UNIT ( ) SI_UNIT ( $, .RADIAN. ) );
#23194=EDGE_CURVE ( 'NONE', #23416, #54956, #13846, .T. ) ;
#23201=CARTESIAN_POINT ( 'NONE',  ( -75.46551724137930250, 63.49197145334878201, 10.00000000000000000 ) ) ;
#23203=PLANE ( 'NONE',  #20807 ) ;
#23204=VERTEX_POINT ( 'NONE', #20662 ) ;
#23210=( LENGTH_UNIT ( ) NAMED_UNIT ( * ) SI_UNIT ( .MILLI., .METRE. ) );
#23213=CARTESIAN_POINT ( 'NONE',  ( -9.827790563157511022E-16, 116.5570736234661666, 8.025000000000000355 ) ) ;
#23214=CARTESIAN_POINT ( 'NONE',  ( 5.374308355190992259, 154.5000000000000853, -7.876141323669411776 ) ) ;
#23215=LINE ( 'NONE', #44708, #38220 ) ;
#23219=CARTESIAN_POINT ( 'NONE',  ( 0.000000000000000000, 116.5549999999999926, -9.525000000000000355 ) ) ;
#23224=DIRECTION ( 'NONE',  ( 1.000000000000000000, 0.000000000000000000, 0.000000000000000000 ) ) ;
#23227=DIRECTION ( 'NONE',  ( -0.000000000000000000, -0.000000000000000000, -1.000000000000000000 ) ) ;
#23231=COLOUR_RGB ( '', 0.08235294, 0.09019608, 0.10196078) ;
#23234=ORIENTED_EDGE ( 'NONE', *, *, #4942, .T. ) ;
#23239=MECHANICAL_DESIGN_GEOMETRIC_PRESENTATION_REPRESENTATION('',(#5238),#60285);
#23240=FACE_OUTER_BOUND ( 'NONE', #24280, .T. ) ;
#23242=SURFACE_STYLE_FILL_AREA ( #55231 ) ;
#23243=ORIENTED_EDGE ( 'NONE', *, *, #24338, .F. ) ;
#23245=ORIENTED_EDGE ( 'NONE', *, *, #18557, .F. ) ;
#23246=EDGE_LOOP ( 'NONE', ( #30056, #56312, #66769, #48932 ) ) ;
#23248=SURFACE_STYLE_FILL_AREA ( #55598 ) ;
#23249=EDGE_LOOP ( 'NONE', ( #58729, #50686, #35837, #49628 ) ) ;
#23251=CARTESIAN_POINT ( 'NONE',  ( 3.094860106618431583, 129.0949999999999704, 9.525000000000000355 ) ) ;
#23255=CARTESIAN_POINT ( 'NONE',  ( -9.058813317711338797, 141.4549999999999841, 2.943386871421373563 ) ) ;
#23258=ORIENTED_EDGE ( 'NONE', *, *, #52854, .T. ) ;
#23259=CARTESIAN_POINT ( 'NONE',  ( -2.607480562269073765, 111.0929263765337964, -8.025000000000000355 ) ) ;
#23261=AXIS2_PLACEMENT_3D ( 'NONE', #16566, #37696, #52804 ) ;
#23262=FACE_OUTER_BOUND ( 'NONE', #61292, .T. ) ;
#23269=FILL_AREA_STYLE_COLOUR ( '', #60348 ) ;
#23274=ADVANCED_FACE ( 'NONE', ( #57958 ), #30849, .T. ) ;
#23276=CARTESIAN_POINT ( 'NONE',  ( -74.99999999999998579, 50.00000000000000000, -9.500000000000000000 ) ) ;
#23278=ORIENTED_EDGE ( 'NONE', *, *, #58442, .F. ) ;
#23279=VERTEX_POINT ( 'NONE', #15410 ) ;
#23281=AXIS2_PLACEMENT_3D ( 'NONE', #57149, #47005, #14973 ) ;
#23285=FACE_OUTER_BOUND ( 'NONE', #59651, .T. ) ;
#23287=CARTESIAN_POINT ( 'NONE',  ( -54.50000000000002132, -1.956686671034893189E-14, -12.00000000000000000 ) ) ;
#23294=CARTESIAN_POINT ( 'NONE',  ( 8.102448949553181734, 129.3949999999999818, 5.886773742842750679 ) ) ;
#23302=CIRCLE ( 'NONE', #62606, 16.50000000000000000 ) ;
#23304=EDGE_CURVE ( 'NONE', #49636, #64569, #59721, .T. ) ;
#23306=VERTEX_POINT ( 'NONE', #69201 ) ;
#23310=EDGE_CURVE ( 'NONE', #21071, #38290, #37343, .T. ) ;
#23311=SURFACE_SIDE_STYLE ('',( #50070 ) ) ;
#23316=AXIS2_PLACEMENT_3D ( 'NONE', #46851, #67202, #66875 ) ;
#23319=ORIENTED_EDGE ( 'NONE', *, *, #16562, .F. ) ;
#23320=CARTESIAN_POINT ( 'NONE',  ( 48.00000000000000000, 14.49137674618942562, -7.500000000000000000 ) ) ;
#23321=CARTESIAN_POINT ( 'NONE',  ( -15.98999599679679839, 146.4999999999999716, 9.500000000000000000 ) ) ;
#23322=B_SPLINE_CURVE_WITH_KNOTS ( 'NONE', 3,
 ( #15678, #41383, #57534, #31474, #25510, #57895, #63504, #51921, #52960, #4749 ),
 .UNSPECIFIED., .F., .F.,
 ( 4, 2, 2, 2, 4 ),
 ( 0.000000000000000000, 0.0004706383985570308597, 0.0009412767971140617194, 0.001411915195671093392, 0.001882553594228125174 ),
 .UNSPECIFIED. ) ;
#23323=DIRECTION ( 'NONE',  ( 0.000000000000000000, 0.000000000000000000, 1.000000000000000000 ) ) ;
#23324=CARTESIAN_POINT ( 'NONE',  ( 7.632228543268607446, 156.1570736234661467, 2.479861379858954606 ) ) ;
#23325=ORIENTED_EDGE ( 'NONE', *, *, #11988, .T. ) ;
#23326=( NAMED_UNIT ( * ) SI_UNIT ( $, .STERADIAN. ) SOLID_ANGLE_UNIT ( ) );
#23330=CARTESIAN_POINT ( 'NONE',  ( -5.598654528085806881, 125.8549999999999898, -7.705886871421374629 ) ) ;
#23332=CARTESIAN_POINT ( 'NONE',  ( 41.49999999999998579, 106.9282032302754999, -3.500000000000000000 ) ) ;
#23334=CARTESIAN_POINT ( 'NONE',  ( -74.99999999999998579, 113.4999999999999858, 7.000000000000000000 ) ) ;
#23335=ORIENTED_EDGE ( 'NONE', *, *, #15292, .F. ) ;
#23336=( LENGTH_UNIT ( ) NAMED_UNIT ( * ) SI_UNIT ( .MILLI., .METRE. ) );
#23338=EDGE_LOOP ( 'NONE', ( #10173, #20886, #22937, #9961 ) ) ;
#23339=CARTESIAN_POINT ( 'NONE',  ( -75.00000000000000000, -2.215169945516535778E-14, -9.500000000000000000 ) ) ;
#23340=CARTESIAN_POINT ( 'NONE',  ( -45.91547276418385337, 9.430195785006416642, -6.025268399887218074 ) ) ;
#23341=AXIS2_PLACEMENT_3D ( 'NONE', #41944, #15536, #57737 ) ;
#23342=DIRECTION ( 'NONE',  ( 8.881784197001252323E-16, 0.000000000000000000, 1.000000000000000000 ) ) ;
#23343=ORIENTED_EDGE ( 'NONE', *, *, #67271, .T. ) ;
#23345=EDGE_LOOP ( 'NONE', ( #13340, #52077, #24353, #40554 ) ) ;
#23346=VECTOR ( 'NONE', #65561, 1000.000000000000000 ) ;
#23347=AXIS2_PLACEMENT_3D ( 'NONE', #50542, #61076, #25184 ) ;
#23348=CARTESIAN_POINT ( 'NONE',  ( -75.00000000000000000, 9.708372641349372500, 6.050536800209464161 ) ) ;
#23351=ORIENTED_EDGE ( 'NONE', *, *, #54620, .T. ) ;
#23352=CARTESIAN_POINT ( 'NONE',  ( -4.716976649647098618, 119.2570736234661553, 6.492361379858953008 ) ) ;
#23354=VECTOR ( 'NONE', #28287, 1000.000000000000000 ) ;
#23358=CARTESIAN_POINT ( 'NONE',  ( 8.102448949553179958, 144.3949999999999818, 5.886773742842750679 ) ) ;
#23360=EDGE_CURVE ( 'NONE', #43611, #11506, #40676, .T. ) ;
#23362=AXIS2_PLACEMENT_3D ( 'NONE', #34204, #18018, #12732 ) ;
#23364=CARTESIAN_POINT ( 'NONE',  ( -44.99999999999998579, 119.9999999999999716, -9.500000000000000000 ) ) ;
#23370=( NAMED_UNIT ( * ) SI_UNIT ( $, .STERADIAN. ) SOLID_ANGLE_UNIT ( ) );
#23373=DIRECTION ( 'NONE',  ( 0.000000000000000000, 1.000000000000000000, 0.000000000000000000 ) ) ;
#23374=ORIENTED_EDGE ( 'NONE', *, *, #35683, .T. ) ;
#23376=FILL_AREA_STYLE_COLOUR ( '', #26653 ) ;
#23377=CARTESIAN_POINT ( 'NONE',  ( -74.99999999999998579, 64.49137674618943095, 10.00000000000000000 ) ) ;
#23381=CARTESIAN_POINT ( 'NONE',  ( -60.00000000000000000, -2.024042244987997205E-14, -10.00000000000000000 ) ) ;
#23390=DIRECTION ( 'NONE',  ( -0.000000000000000000, -0.000000000000000000, -1.000000000000000000 ) ) ;
#23391=SURFACE_STYLE_USAGE ( .BOTH. , #34304 ) ;
#23395=DIRECTION ( 'NONE',  ( 1.000000000000000000, 0.000000000000000000, -0.000000000000000000 ) ) ;
#23396=AXIS2_PLACEMENT_3D ( 'NONE', #61014, #12830, #7558 ) ;
#23397=CARTESIAN_POINT ( 'NONE',  ( -6.826472737025120807, 119.1070736234661496, 4.959722759717906548 ) ) ;
#23398=( GEOMETRIC_REPRESENTATION_CONTEXT ( 3 ) GLOBAL_UNCERTAINTY_ASSIGNED_CONTEXT ( ( #45273 ) ) GLOBAL_UNIT_ASSIGNED_CONTEXT ( ( #26609, #42863, #53380 ) ) REPRESENTATION_CONTEXT ( 'NONE', 'WORKASPACE' ) );
#23402=( NAMED_UNIT ( * ) SI_UNIT ( $, .STERADIAN. ) SOLID_ANGLE_UNIT ( ) );
#23403=ORIENTED_EDGE ( 'NONE', *, *, #35040, .T. ) ;
#23405=CARTESIAN_POINT ( 'NONE',  ( 0.000000000000000000, 152.9999999999999716, 0.000000000000000000 ) ) ;
#23406=EDGE_CURVE ( 'NONE', #67825, #7755, #8887, .T. ) ;
#23411=DIRECTION ( 'NONE',  ( 0.000000000000000000, 0.000000000000000000, 1.000000000000000000 ) ) ;
#23412=EDGE_CURVE ( 'NONE', #58654, #62684, #24926, .T. ) ;
#23413=DIRECTION ( 'NONE',  ( 0.000000000000000000, 0.000000000000000000, 1.000000000000000000 ) ) ;
#23414=CARTESIAN_POINT ( 'NONE',  ( -44.50000000000000000, 99.99999999999998579, 4.000000000000000000 ) ) ;
#23415=AXIS2_PLACEMENT_3D ( 'NONE', #21123, #4587, #68989 ) ;
#23416=VERTEX_POINT ( 'NONE', #44580 ) ;
#23417=( LENGTH_UNIT ( ) NAMED_UNIT ( * ) SI_UNIT ( .MILLI., .METRE. ) );
#23418=EDGE_CURVE ( 'NONE', #12977, #41202, #159, .T. ) ;
#23420=EDGE_CURVE ( 'NONE', #26152, #52352, #37391, .T. ) ;
#23423=EDGE_CURVE ( 'NONE', #13722, #34864, #60921, .T. ) ;
#23429=CYLINDRICAL_SURFACE ( 'NONE', #15189, 0.5000000000000004441 ) ;
#23431=CIRCLE ( 'NONE', #57127, 18.00000000000000355 ) ;
#23435=CARTESIAN_POINT ( 'NONE',  ( -23.21231517720797655, 118.4999999999999716, 7.000000000000000000 ) ) ;
#23436=ORIENTED_EDGE ( 'NONE', *, *, #61615, .F. ) ;
#23437=CARTESIAN_POINT ( 'NONE',  ( -74.99999999999998579, 50.00000000000000000, -6.499999999999999112 ) ) ;
#23438=AXIS2_PLACEMENT_3D ( 'NONE', #50045, #2829, #40184 ) ;
#23439=SURFACE_STYLE_FILL_AREA ( #55094 ) ;
#23440=DIRECTION ( 'NONE',  ( 1.000000000000000000, 0.000000000000000000, 0.000000000000000000 ) ) ;
#23441=SURFACE_SIDE_STYLE ('',( #23121 ) ) ;
#23444=DIRECTION ( 'NONE',  ( 1.000000000000000000, -4.336808689941999001E-16, 0.000000000000000000 ) ) ;
#23446=AXIS2_PLACEMENT_3D ( 'NONE', #51573, #15365, #56857 ) ;
#23448=ORIENTED_EDGE ( 'NONE', *, *, #24389, .T. ) ;
#23450=FILL_AREA_STYLE_COLOUR ( '', #64909 ) ;
#23453=CARTESIAN_POINT ( 'NONE',  ( -24.21231517720798010, 113.4999999999999858, -10.00000000000000000 ) ) ;
#23454=CIRCLE ( 'NONE', #30169, 0.5000000000000004441 ) ;
#23455=( NAMED_UNIT ( * ) SI_UNIT ( $, .STERADIAN. ) SOLID_ANGLE_UNIT ( ) );
#23457=CARTESIAN_POINT ( 'NONE',  ( 0.000000000000000000, 143.5549999999999784, -9.525000000000000355 ) ) ;
#23459=CARTESIAN_POINT ( 'NONE',  ( 3.906371588341139400, 154.3107745167562825, 8.486918976161017980 ) ) ;
#23461=EDGE_CURVE ( 'NONE', #42583, #12229, #61878, .T. ) ;
#23465=CARTESIAN_POINT ( 'NONE',  ( 60.00000000000000000, -2.024042244987997205E-14, 9.500000000000000000 ) ) ;
#23470=ORIENTED_EDGE ( 'NONE', *, *, #46764, .F. ) ;
#23472=ORIENTED_EDGE ( 'NONE', *, *, #27364, .F. ) ;
#23477=SURFACE_SIDE_STYLE ('',( #6963 ) ) ;
#23478=MECHANICAL_DESIGN_GEOMETRIC_PRESENTATION_REPRESENTATION('',(#57181),#30203);
#23481=ORIENTED_EDGE ( 'NONE', *, *, #43890, .F. ) ;
#23483=ORIENTED_EDGE ( 'NONE', *, *, #43529, .F. ) ;
#23484=LINE ( 'NONE', #33362, #28665 ) ;
#23487=ORIENTED_EDGE ( 'NONE', *, *, #6431, .F. ) ;
#23490=AXIS2_PLACEMENT_3D ( 'NONE', #9287, #30705, #68368 ) ;
#23495=DIRECTION ( 'NONE',  ( 1.000000000000000000, 0.000000000000000000, 0.000000000000000000 ) ) ;
#23497=CARTESIAN_POINT ( 'NONE',  ( -8.437984349512095861, 132.6929263765338192, -5.166775262442723748E-16 ) ) ;
#23499=AXIS2_PLACEMENT_3D ( 'NONE', #69154, #31489, #64891 ) ;
#23500=DIRECTION ( 'NONE',  ( -0.000000000000000000, -0.000000000000000000, -1.000000000000000000 ) ) ;
#23502=ORIENTED_EDGE ( 'NONE', *, *, #15835, .F. ) ;
#23503=CARTESIAN_POINT ( 'NONE',  ( -45.00000000000000000, 99.99999999999992895, -4.000000000000000000 ) ) ;
#23507=DIRECTION ( 'NONE',  ( 0.000000000000000000, 0.000000000000000000, 1.000000000000000000 ) ) ;
#23508=DIRECTION ( 'NONE',  ( 0.000000000000000000, 0.000000000000000000, 1.000000000000000000 ) ) ;
#23511=SURFACE_STYLE_USAGE ( .BOTH. , #1991 ) ;
#23512=ORIENTED_EDGE ( 'NONE', *, *, #34461, .T. ) ;
#23518=EDGE_LOOP ( 'NONE', ( #10723, #32492, #15827, #16483, #36281, #20576, #52260, #3373, #61523, #4562, #11596, #7458, #63321, #19678 ) ) ;
#23520=DIRECTION ( 'NONE',  ( 1.000000000000000000, 0.000000000000000000, 0.000000000000000000 ) ) ;
#23522=DIRECTION ( 'NONE',  ( 0.000000000000000000, 0.000000000000000000, -1.000000000000000000 ) ) ;
#23525=ORIENTED_EDGE ( 'NONE', *, *, #62985, .T. ) ;
#23529=AXIS2_PLACEMENT_3D ( 'NONE', #45628, #62450, #46313 ) ;
#23533=ORIENTED_EDGE ( 'NONE', *, *, #5425, .F. ) ;
#23534=CARTESIAN_POINT ( 'NONE',  ( -74.94185258274741557, 35.62135875951527453, -9.737060520187748480 ) ) ;
#23539=DIRECTION ( 'NONE',  ( 0.000000000000000000, 0.000000000000000000, 1.000000000000000000 ) ) ;
#23543=CARTESIAN_POINT ( 'NONE',  ( 5.598654528085809545, 113.2549999999999812, -7.705886871421373741 ) ) ;
#23546=CARTESIAN_POINT ( 'NONE',  ( -60.00000000000000000, -2.024042244987997205E-14, -11.50000000000000000 ) ) ;
#23549=UNCERTAINTY_MEASURE_WITH_UNIT (LENGTH_MEASURE( 1.000000000000000082E-05 ), #10636, 'distance_accuracy_value', 'NONE');
#23551=EDGE_CURVE ( 'NONE', #48746, #61898, #26077, .T. ) ;
#23559=CARTESIAN_POINT ( 'NONE',  ( -60.00000000000000000, -2.024042244987997205E-14, 10.00000000000000000 ) ) ;
#23560=CARTESIAN_POINT ( 'NONE',  ( 0.000000000000000000, 110.4999999999999858, 0.000000000000000000 ) ) ;
#23562=ORIENTED_EDGE ( 'NONE', *, *, #5219, .T. ) ;
#23563=COLOUR_RGB ( '', 0.09019608, 0.27058824, 0.51372549) ;
#23566=SURFACE_STYLE_USAGE ( .BOTH. , #2040 ) ;
#23574=EDGE_CURVE ( 'NONE', #65204, #23886, #44918, .T. ) ;
#23575=EDGE_CURVE ( 'NONE', #41309, #52342, #19352, .T. ) ;
#23581=DIRECTION ( 'NONE',  ( 0.000000000000000000, 0.000000000000000000, 1.000000000000000000 ) ) ;
#23582=AXIS2_PLACEMENT_3D ( 'NONE', #35962, #67260, #29973 ) ;
#23583=CARTESIAN_POINT ( 'NONE',  ( -8.102448949553181734, 140.4949999999999761, 5.886773742842747126 ) ) ;
#23587=CARTESIAN_POINT ( 'NONE',  ( 0.000000000000000000, 143.5549999999999784, -9.525000000000000355 ) ) ;
#23590=MECHANICAL_DESIGN_GEOMETRIC_PRESENTATION_REPRESENTATION('',(#37148),#11241);
#23591=SURFACE_STYLE_USAGE ( .BOTH. , #8121 ) ;
#23593=CARTESIAN_POINT ( 'NONE',  ( 3.094860106618435136, 161.4050000000000296, -9.525000000000000355 ) ) ;
#23596=AXIS2_PLACEMENT_3D ( 'NONE', #57211, #46363, #30119 ) ;
#23598=EDGE_CURVE ( 'NONE', #24181, #11645, #30069, .T. ) ;
#23601=CIRCLE ( 'NONE', #56166, 0.5000000000000004441 ) ;
#23602=FACE_OUTER_BOUND ( 'NONE', #22952, .T. ) ;
#23603=EDGE_CURVE ( 'NONE', #27627, #31846, #65412, .T. ) ;
#23604=VERTEX_POINT ( 'NONE', #20214 ) ;
#23612=FILL_AREA_STYLE_COLOUR ( '', #8324 ) ;
#23613=EDGE_CURVE ( 'NONE', #27683, #14403, #50804, .T. ) ;
#23614=FACE_OUTER_BOUND ( 'NONE', #18143, .T. ) ;
#23621=COLOUR_RGB ( '', 0.31764706, 0.68627451, 0.89019608) ;
#23623=DIRECTION ( 'NONE',  ( -0.000000000000000000, -0.000000000000000000, 1.000000000000000000 ) ) ;
#23624=AXIS2_PLACEMENT_3D ( 'NONE', #50303, #34110, #23224 ) ;
#23628=CARTESIAN_POINT ( 'NONE',  ( 0.000000000000000000, 142.4449999999999932, -9.525000000000000355 ) ) ;
#23630=AXIS2_PLACEMENT_3D ( 'NONE', #2587, #6869, #28294 ) ;
#23634=ADVANCED_FACE ( 'NONE', ( #21244 ), #58672, .T. ) ;
#23637=COLOUR_RGB ( '', 0.66274510, 0.83137255, 0.94901961) ;
#23642=CARTESIAN_POINT ( 'NONE',  ( 24.21231517720798010, 113.4999999999999858, 7.500000000000000000 ) ) ;
#23643=ORIENTED_EDGE ( 'NONE', *, *, #66218, .T. ) ;
#23660=ORIENTED_EDGE ( 'NONE', *, *, #24969, .F. ) ;
#23661=SURFACE_STYLE_USAGE ( .BOTH. , #49720 ) ;
#23664=CARTESIAN_POINT ( 'NONE',  ( 8.437984349512095861, 153.3070736234660956, 1.550032578732817026E-15 ) ) ;
#23667=PRESENTATION_STYLE_ASSIGNMENT (( #13112 ) ) ;
#23669=EDGE_CURVE ( 'NONE', #12588, #59936, #29438, .T. ) ;
#23672=CARTESIAN_POINT ( 'NONE',  ( -5.598654528085808657, 132.7549999999999955, 7.705886871421373741 ) ) ;
#23675=LINE ( 'NONE', #45857, #35527 ) ;
#23676=EDGE_CURVE ( 'NONE', #14403, #27683, #53070, .T. ) ;
#23678=DIRECTION ( 'NONE',  ( -0.000000000000000000, -0.000000000000000000, -1.000000000000000000 ) ) ;
#23680=DIRECTION ( 'NONE',  ( 1.000000000000000000, 0.000000000000000000, 0.000000000000000000 ) ) ;
#23683=DIRECTION ( 'NONE',  ( -1.000000000000000000, -1.156482317317866302E-16, 0.000000000000000000 ) ) ;
#23686=ORIENTED_EDGE ( 'NONE', *, *, #52057, .F. ) ;
#23687=LINE ( 'NONE', #34579, #51948 ) ;
#23690=CARTESIAN_POINT ( 'NONE',  ( 65.50000000000000000, 2.470600640510328946E-15, 6.500000000000000000 ) ) ;
#23691=FILL_AREA_STYLE ('',( #28606 ) ) ;
#23697=CARTESIAN_POINT ( 'NONE',  ( -75.00000000000000000, 9.115532208874117970, 6.738970650128760731 ) ) ;
#23699=VERTEX_POINT ( 'NONE', #31455 ) ;
#23707=CIRCLE ( 'NONE', #50679, 14.49999999999999822 ) ;
#23708=CARTESIAN_POINT ( 'NONE',  ( -5.598654528085806881, 139.7449999999999761, -7.705886871421374629 ) ) ;
#23710=DIRECTION ( 'NONE',  ( 0.000000000000000000, 0.000000000000000000, -1.000000000000000000 ) ) ;
#23711=CARTESIAN_POINT ( 'NONE',  ( 20.71231517720798010, 149.9999999999999716, 10.00000000000000000 ) ) ;
#23714=( LENGTH_UNIT ( ) NAMED_UNIT ( * ) SI_UNIT ( .MILLI., .METRE. ) );
#23718=CARTESIAN_POINT ( 'NONE',  ( 3.094860106618431583, 114.0949999999999704, 9.525000000000000355 ) ) ;
#23722=LINE ( 'NONE', #62037, #17859 ) ;
#23725=CIRCLE ( 'NONE', #27064, 0.5000000000000004441 ) ;
#23726=VECTOR ( 'NONE', #63521, 1000.000000000000000 ) ;
#23729=AXIS2_PLACEMENT_3D ( 'NONE', #26986, #64665, #52402 ) ;
#23731=EDGE_CURVE ( 'NONE', #50952, #53532, #12617, .T. ) ;
#23732=( NAMED_UNIT ( * ) SI_UNIT ( $, .STERADIAN. ) SOLID_ANGLE_UNIT ( ) );
#23733=DIRECTION ( 'NONE',  ( 6.938893903907222067E-15, 0.000000000000000000, 1.000000000000000000 ) ) ;
#23741=CYLINDRICAL_SURFACE ( 'NONE', #33713, 26.99999999999999645 ) ;
#23742=CARTESIAN_POINT ( 'NONE',  ( -41.36364127011528069, 107.7184400395438644, 3.928466540244182958 ) ) ;
#23743=MECHANICAL_DESIGN_GEOMETRIC_PRESENTATION_REPRESENTATION('',(#9206),#13643);
#23746=ORIENTED_EDGE ( 'NONE', *, *, #46439, .F. ) ;
#23747=COLOUR_RGB ( '', 0.31764706, 0.68627451, 0.89019608) ;
#23752=AXIS2_PLACEMENT_3D ( 'NONE', #32833, #39177, #12052 ) ;
#23753=CARTESIAN_POINT ( 'NONE',  ( 2.607480562269076430, 120.9070736234661609, -8.025000000000000355 ) ) ;
#23754=MECHANICAL_DESIGN_GEOMETRIC_PRESENTATION_REPRESENTATION('',(#62055),#64323);
#23757=VECTOR ( 'NONE', #54144, 1000.000000000000000 ) ;
#23759=ORIENTED_EDGE ( 'NONE', *, *, #4171, .F. ) ;
#23762=CARTESIAN_POINT ( 'NONE',  ( 4.716976649647099507, 150.7570736234661695, -6.492361379858953008 ) ) ;
#23765=CIRCLE ( 'NONE', #45153, 0.5000000000000004441 ) ;
#23767=CIRCLE ( 'NONE', #38446, 0.5000000000000004441 ) ;
#23768=PRESENTATION_STYLE_ASSIGNMENT (( #12508 ) ) ;
#23770=SURFACE_STYLE_FILL_AREA ( #30076 ) ;
#23772=COLOUR_RGB ( '', 0.40784314, 0.44705882, 0.49803922) ;
#23776=( NAMED_UNIT ( * ) SI_UNIT ( $, .STERADIAN. ) SOLID_ANGLE_UNIT ( ) );
#23779=PRESENTATION_STYLE_ASSIGNMENT (( #19178 ) ) ;
#23784=CARTESIAN_POINT ( 'NONE',  ( -8.102448949553179958, 112.8949999999999818, -5.886773742842749790 ) ) ;
#23787=FACE_OUTER_BOUND ( 'NONE', #7746, .T. ) ;
#23790=STYLED_ITEM ( 'NONE', ( #63456 ), #53305 ) ;
#23792=FACE_OUTER_BOUND ( 'NONE', #47628, .T. ) ;
#23794=CARTESIAN_POINT ( 'NONE',  ( 44.50000000000000000, 99.99999999999992895, -3.500000000000000000 ) ) ;
#23796=CIRCLE ( 'NONE', #11441, 13.99999999999999822 ) ;
#23798=DIRECTION ( 'NONE',  ( 1.000000000000000000, 0.000000000000000000, -0.000000000000000000 ) ) ;
#23800=B_SPLINE_CURVE_WITH_KNOTS ( 'NONE', 3,
 ( #33326, #29776, #19196, #46706, #57189, #9376, #24824, #25524, #57548, #2983, #2646, #7969, #45651, #35411, #41054, #40343, #67070, #9019, #51238, #41397, #19560, #52302, #47036, #68451, #62805, #13581, #30436, #51938, #3693 ),
 .UNSPECIFIED., .F., .F.,
 ( 4, 2, 2, 2, 2, 2, 2, 1, 2, 2, 2, 2, 2, 2, 4 ),
 ( 5.102712030719938591E-17, 0.002418039429563660549, 0.003627059144345467188, 0.004836078859127274261, 0.006045098573909080467, 0.007254118288690887539, 0.008463138003472692877, 0.009672157718254499950, 0.01088117743303630876, 0.01209019714781811757, 0.01329921686259992637, 0.01450823657738173518, 0.01692627600694535453, 0.01813529572172715987, 0.01934431543650896868 ),
 .UNSPECIFIED. ) ;
#23805=DIRECTION ( 'NONE',  ( 1.224646799147353207E-16, 1.000000000000000000, -0.000000000000000000 ) ) ;
#23806=VECTOR ( 'NONE', #40087, 1000.000000000000114 ) ;
#23809=COLOUR_RGB ( '', 0.09019608, 0.27058824, 0.51372549) ;
#23812=CARTESIAN_POINT ( 'NONE',  ( -8.102448949553181734, 147.6049999999999329, 5.886773742842747126 ) ) ;
#23814=ADVANCED_FACE ( 'NONE', ( #24705 ), #7171, .T. ) ;
#23815=CIRCLE ( 'NONE', #68735, 0.4999999999999994449 ) ;
#23817=DIRECTION ( 'NONE',  ( -0.000000000000000000, -0.000000000000000000, -1.000000000000000000 ) ) ;
#23818=CARTESIAN_POINT ( 'NONE',  ( -19.89974874213239886, 115.4999999999999574, -10.00000000000000000 ) ) ;
#23821=ADVANCED_FACE ( 'NONE', ( #34575 ), #56383, .F. ) ;
#23822=CARTESIAN_POINT ( 'NONE',  ( 60.00000000000000000, 1.797044900979284448E-15, 12.00000000000000000 ) ) ;
#23823=EDGE_CURVE ( 'NONE', #68013, #2160, #35126, .T. ) ;
#23830=EDGE_CURVE ( 'NONE', #53774, #54731, #20126, .T. ) ;
#23832=EDGE_CURVE ( 'NONE', #43960, #54714, #31039, .T. ) ;
#23833=PLANE ( 'NONE',  #45164 ) ;
#23834=( NAMED_UNIT ( * ) PLANE_ANGLE_UNIT ( ) SI_UNIT ( $, .RADIAN. ) );
#23836=VERTEX_POINT ( 'NONE', #19799 ) ;
#23837=CARTESIAN_POINT ( 'NONE',  ( -74.99999999999998579, 50.00000000000000000, 12.00000000000000000 ) ) ;
#23838=( LENGTH_UNIT ( ) NAMED_UNIT ( * ) SI_UNIT ( .MILLI., .METRE. ) );
#23839=ORIENTED_EDGE ( 'NONE', *, *, #9897, .T. ) ;
#23840=DIRECTION ( 'NONE',  ( 1.000000000000000000, 0.000000000000000000, -0.000000000000000000 ) ) ;
#23843=DIRECTION ( 'NONE',  ( 0.000000000000000000, 0.000000000000000000, 1.000000000000000000 ) ) ;
#23847=ORIENTED_EDGE ( 'NONE', *, *, #42275, .T. ) ;
#23852=CARTESIAN_POINT ( 'NONE',  ( 8.437984349512095861, 149.1929263765337623, 1.550032578732817026E-15 ) ) ;
#23855=AXIS2_PLACEMENT_3D ( 'NONE', #7513, #39910, #50779 ) ;
#23857=CARTESIAN_POINT ( 'NONE',  ( 0.000000000000000000, 113.9429263765338192, -8.025000000000000355 ) ) ;
#23858=ORIENTED_EDGE ( 'NONE', *, *, #26374, .T. ) ;
#23859=DIRECTION ( 'NONE',  ( -0.000000000000000000, -0.000000000000000000, 1.000000000000000000 ) ) ;
#23860=ORIENTED_EDGE ( 'NONE', *, *, #10823, .T. ) ;
#23861=( NAMED_UNIT ( * ) SI_UNIT ( $, .STERADIAN. ) SOLID_ANGLE_UNIT ( ) );
#23862=FACE_OUTER_BOUND ( 'NONE', #3868, .T. ) ;
#23864=COLOUR_RGB ( '', 0.72549020, 0.75294118, 0.79215686) ;
#23866=CARTESIAN_POINT ( 'NONE',  ( 0.000000000000000000, 149.9429263765338476, -8.025000000000000355 ) ) ;
#23867=ORIENTED_EDGE ( 'NONE', *, *, #34317, .F. ) ;
#23868=DIRECTION ( 'NONE',  ( 0.000000000000000000, 1.000000000000000000, 0.000000000000000000 ) ) ;
#23872=CARTESIAN_POINT ( 'NONE',  ( -45.00000000000000711, 7.967268226264182296, -7.000000000000000000 ) ) ;
#23873=ORIENTED_EDGE ( 'NONE', *, *, #62228, .F. ) ;
#23878=CARTESIAN_POINT ( 'NONE',  ( 34.99999999999992895, 112.9999999999999858, -7.500000000000000000 ) ) ;
#23880=CARTESIAN_POINT ( 'NONE',  ( 0.000000000000000000, 115.4999999999999574, 0.000000000000000000 ) ) ;
#23884=AXIS2_PLACEMENT_3D ( 'NONE', #35643, #30324, #8900 ) ;
#23886=VERTEX_POINT ( 'NONE', #47638 ) ;
#23887=MECHANICAL_DESIGN_GEOMETRIC_PRESENTATION_REPRESENTATION('',(#44182),#45270);
#23894=AXIS2_PLACEMENT_3D ( 'NONE', #49954, #50627, #12982 ) ;
#23896=CARTESIAN_POINT ( 'NONE',  ( -1.166476076187854022E-15, 115.0549999999999926, 9.525000000000000355 ) ) ;
#23898=CIRCLE ( 'NONE', #30619, 13.99999999999999822 ) ;
#23900=ADVANCED_FACE ( 'NONE', ( #57440 ), #26104, .F. ) ;
#23902=CARTESIAN_POINT ( 'NONE',  ( -71.62068965517239860, 36.41396814395972115, -7.500000000000000000 ) ) ;
#23906=CARTESIAN_POINT ( 'NONE',  ( 41.38256758237926647, 107.6997254016901451, -3.907089461173330225 ) ) ;
#23912=EDGE_CURVE ( 'NONE', #6337, #40506, #31373, .T. ) ;
#23913=CARTESIAN_POINT ( 'NONE',  ( 48.00000000000000000, 13.41640786499872284, 7.000000000000000000 ) ) ;
#23915=AXIS2_PLACEMENT_3D ( 'NONE', #28791, #50272, #66436 ) ;
#23916=ORIENTED_EDGE ( 'NONE', *, *, #20569, .F. ) ;
#23917=CIRCLE ( 'NONE', #22775, 0.5000000000000004441 ) ;
#23918=PRESENTATION_STYLE_ASSIGNMENT (( #7734 ) ) ;
#23919=STYLED_ITEM ( 'NONE', ( #66614 ), #46858 ) ;
#23922=ORIENTED_EDGE ( 'NONE', *, *, #1211, .T. ) ;
#23932=CARTESIAN_POINT ( 'NONE',  ( 5.598654528085809545, 136.1449999999999818, -7.705886871421373741 ) ) ;
#23935=EDGE_LOOP ( 'NONE', ( #3854, #16596, #37993, #11735 ) ) ;
#23936=CARTESIAN_POINT ( 'NONE',  ( -1.166476076187854022E-15, 139.0549999999999784, 9.525000000000000355 ) ) ;
#23938=CARTESIAN_POINT ( 'NONE',  ( 71.62068965517238439, 63.58603185604027885, -7.000000000000000000 ) ) ;
#23941=CARTESIAN_POINT ( 'NONE',  ( -9.827790563157511022E-16, 115.4429263765338192, 8.025000000000000355 ) ) ;
#23944=VECTOR ( 'NONE', #64079, 1000.000000000000000 ) ;
#23946=SURFACE_STYLE_USAGE ( .BOTH. , #51737 ) ;
#23947=CARTESIAN_POINT ( 'NONE',  ( -74.99999999999998579, 50.00000000000000000, -10.49999999999999822 ) ) ;
#23951=LINE ( 'NONE', #50350, #37098 ) ;
#23952=CARTESIAN_POINT ( 'NONE',  ( 20.57648123223228964, 114.5812418126072174, 10.27659574468084891 ) ) ;
#23955=EDGE_LOOP ( 'NONE', ( #46877, #54028, #36459, #59614 ) ) ;
#23956=DIRECTION ( 'NONE',  ( 0.000000000000000000, 0.000000000000000000, -1.000000000000000000 ) ) ;
#23959=CARTESIAN_POINT ( 'NONE',  ( 15.98999599679679839, 118.4999999999999716, -7.000000000000000000 ) ) ;
#23961=CARTESIAN_POINT ( 'NONE',  ( 45.58253334211749319, 9.942242644401853013, -6.446113437190194695 ) ) ;
#23967=ORIENTED_EDGE ( 'NONE', *, *, #52660, .F. ) ;
#23970=CIRCLE ( 'NONE', #8266, 0.5000000000000004441 ) ;
#23973=CARTESIAN_POINT ( 'NONE',  ( -74.45867456775532389, 7.945093266341785920, -6.500000000000000888 ) ) ;
#23975=( LENGTH_UNIT ( ) NAMED_UNIT ( * ) SI_UNIT ( .MILLI., .METRE. ) );
#23976=FACE_OUTER_BOUND ( 'NONE', #8115, .T. ) ;
#23978=EDGE_CURVE ( 'NONE', #44039, #32321, #57794, .T. ) ;
#23980=EDGE_CURVE ( 'NONE', #6580, #3957, #14187, .T. ) ;
#23981=CARTESIAN_POINT ( 'NONE',  ( -8.102448949553181734, 143.4949999999999477, 5.886773742842747126 ) ) ;
#23984=AXIS2_PLACEMENT_3D ( 'NONE', #61820, #67465, #29831 ) ;
#23986=COLOUR_RGB ( '', 0.31764706, 0.68627451, 0.89019608) ;
#23987=PRESENTATION_STYLE_ASSIGNMENT (( #2477 ) ) ;
#23994=CIRCLE ( 'NONE', #35249, 22.50000000000000000 ) ;
#24006=( NAMED_UNIT ( * ) SI_UNIT ( $, .STERADIAN. ) SOLID_ANGLE_UNIT ( ) );
#24009=LINE ( 'NONE', #3547, #51018 ) ;
#24014=FILL_AREA_STYLE_COLOUR ( '', #15586 ) ;
#24015=DIRECTION ( 'NONE',  ( 1.000000000000000000, 0.000000000000000000, 0.000000000000000000 ) ) ;
#24018=FACE_OUTER_BOUND ( 'NONE', #35787, .T. ) ;
#24019=CARTESIAN_POINT ( 'NONE',  ( 5.598654528085805993, 111.2449999999999761, 7.705886871421374629 ) ) ;
#24022=SURFACE_STYLE_FILL_AREA ( #40574 ) ;
#24023=CARTESIAN_POINT ( 'NONE',  ( -3.094860106618432471, 110.7049999999999983, -9.525000000000000355 ) ) ;
#24025=FILL_AREA_STYLE_COLOUR ( '', #34266 ) ;
#24026=CARTESIAN_POINT ( 'NONE',  ( 10.01517768586949231, 127.8050000000000068, 1.839758294383810543E-15 ) ) ;
#24027=CARTESIAN_POINT ( 'NONE',  ( 20.58910881788679603, 114.8399099445016276, 10.00000000000000355 ) ) ;
#24030=( NAMED_UNIT ( * ) SI_UNIT ( $, .STERADIAN. ) SOLID_ANGLE_UNIT ( ) );
#24032=TOROIDAL_SURFACE ( 'NONE', #63355, 1.000000000000000000, 0.5000000000000000000 ) ;
#24033=PRESENTATION_STYLE_ASSIGNMENT (( #56030 ) ) ;
#24035=ORIENTED_EDGE ( 'NONE', *, *, #25255, .F. ) ;
#24037=COLOUR_RGB ( '', 0.66274510, 0.83137255, 0.94901961) ;
#24040=CARTESIAN_POINT ( 'NONE',  ( -67.49999999999998579, -1.932193735051945844E-14, -11.50000000000000000 ) ) ;
#24048=CARTESIAN_POINT ( 'NONE',  ( -75.00000000000000000, 8.547452476118923670, 5.556748833514874697 ) ) ;
#24051=DIRECTION ( 'NONE',  ( 1.000000000000000000, 0.000000000000000000, 0.000000000000000000 ) ) ;
#24055=CARTESIAN_POINT ( 'NONE',  ( 0.000000000000000000, 154.4999999999999432, -23.00000000000000000 ) ) ;
#24056=CARTESIAN_POINT ( 'NONE',  ( -3.094860106618434248, 137.7949999999999875, 9.525000000000000355 ) ) ;
#24059=EDGE_CURVE ( 'NONE', #35967, #12421, #33537, .T. ) ;
#24060=DIRECTION ( 'NONE',  ( 0.000000000000000000, 0.000000000000000000, 1.000000000000000000 ) ) ;
#24061=( NAMED_UNIT ( * ) SI_UNIT ( $, .STERADIAN. ) SOLID_ANGLE_UNIT ( ) );
#24063=CARTESIAN_POINT ( 'NONE',  ( 6.826472737025119919, 120.0070736234661410, 4.959722759717908325 ) ) ;
#24077=EDGE_CURVE ( 'NONE', #2411, #16463, #8097, .T. ) ;
#24083=DIRECTION ( 'NONE',  ( -0.000000000000000000, -0.000000000000000000, -1.000000000000000000 ) ) ;
#24084=VECTOR ( 'NONE', #60298, 1000.000000000000000 ) ;
#24085=( LENGTH_UNIT ( ) NAMED_UNIT ( * ) SI_UNIT ( .MILLI., .METRE. ) );
#24087=VERTEX_POINT ( 'NONE', #44378 ) ;
#24092=CARTESIAN_POINT ( 'NONE',  ( 44.99999999999977973, 149.9999999999999716, 10.00000000000000000 ) ) ;
#24102=CARTESIAN_POINT ( 'NONE',  ( 0.000000000000000000, 136.0570736234661808, -8.025000000000000355 ) ) ;
#24106=FACE_OUTER_BOUND ( 'NONE', #33707, .T. ) ;
#24110=VECTOR ( 'NONE', #14366, 1000.000000000000000 ) ;
#24113=TOROIDAL_SURFACE ( 'NONE', #30830, 16.50000000000000000, 0.5000000000000000000 ) ;
#24119=UNCERTAINTY_MEASURE_WITH_UNIT (LENGTH_MEASURE( 1.000000000000000082E-05 ), #20669, 'distance_accuracy_value', 'NONE');
#24121=PRESENTATION_STYLE_ASSIGNMENT (( #61393 ) ) ;
#24123=FACE_OUTER_BOUND ( 'NONE', #14107, .T. ) ;
#24126=EDGE_CURVE ( 'NONE', #42981, #46203, #14236, .T. ) ;
#24127=CYLINDRICAL_SURFACE ( 'NONE', #21840, 0.5000000000000004441 ) ;
#24128=ORIENTED_EDGE ( 'NONE', *, *, #33659, .F. ) ;
#24131=CARTESIAN_POINT ( 'NONE',  ( 3.094860106618431583, 117.0949999999999847, 9.525000000000000355 ) ) ;
#24134=EDGE_CURVE ( 'NONE', #36214, #62297, #52995, .T. ) ;
#24136=CIRCLE ( 'NONE', #30856, 5.500000000000005329 ) ;
#24140=PRESENTATION_STYLE_ASSIGNMENT (( #7282 ) ) ;
#24146=ORIENTED_EDGE ( 'NONE', *, *, #45391, .T. ) ;
#24154=EDGE_CURVE ( 'NONE', #10212, #49424, #63142, .T. ) ;
#24157=CARTESIAN_POINT ( 'NONE',  ( 10.01517768586949231, 148.8050000000000068, 1.839758294383810543E-15 ) ) ;
#24159=STYLED_ITEM ( 'NONE', ( #49207 ), #49121 ) ;
#24160=CARTESIAN_POINT ( 'NONE',  ( 0.000000000000000000, 154.5000000000000000, -9.524999999999998579 ) ) ;
#24162=CARTESIAN_POINT ( 'NONE',  ( -20.07516809221520404, 115.0406803144924766, -9.999999999999998224 ) ) ;
#24163=CARTESIAN_POINT ( 'NONE',  ( -3.906371588338814149, 110.6892254832438311, 8.486918976161996753 ) ) ;
#24165=AXIS2_PLACEMENT_3D ( 'NONE', #44816, #55325, #65890 ) ;
#24166=CARTESIAN_POINT ( 'NONE',  ( 60.00000000000000000, 1.797044900979284448E-15, 11.50000000000003730 ) ) ;
#24167=VECTOR ( 'NONE', #34502, 1000.000000000000000 ) ;
#24171=ORIENTED_EDGE ( 'NONE', *, *, #68633, .T. ) ;
#24173=ADVANCED_FACE ( 'NONE', ( #14611 ), #20577, .F. ) ;
#24176=COLOUR_RGB ( '', 0.08235294, 0.09019608, 0.10196078) ;
#24181=VERTEX_POINT ( 'NONE', #42094 ) ;
#24185=DIRECTION ( 'NONE',  ( -1.000000000000000000, 0.000000000000000000, 0.000000000000000000 ) ) ;
#24187=ORIENTED_EDGE ( 'NONE', *, *, #38101, .T. ) ;
#24189=CIRCLE ( 'NONE', #25305, 8.500000000000000000 ) ;
#24190=CARTESIAN_POINT ( 'NONE',  ( -6.724421053716080898, 110.4999999999999574, -6.760127308664230839 ) ) ;
#24194=ORIENTED_EDGE ( 'NONE', *, *, #42809, .F. ) ;
#24195=CARTESIAN_POINT ( 'NONE',  ( -6.826472737025120807, 147.9929263765338305, 4.959722759717906548 ) ) ;
#24200=EDGE_CURVE ( 'NONE', #19239, #4086, #22665, .T. ) ;
#24201=DIRECTION ( 'NONE',  ( 0.7071067811865549002, 0.000000000000000000, 0.7071067811865401342 ) ) ;
#24202=ORIENTED_EDGE ( 'NONE', *, *, #24313, .T. ) ;
#24204=LINE ( 'NONE', #45022, #8286 ) ;
#24205=DIRECTION ( 'NONE',  ( 0.000000000000000000, -0.000000000000000000, 1.000000000000000000 ) ) ;
#24208=DIRECTION ( 'NONE',  ( 0.000000000000000000, 0.000000000000000000, 1.000000000000000000 ) ) ;
#24210=ORIENTED_EDGE ( 'NONE', *, *, #60737, .T. ) ;
#24212=FILL_AREA_STYLE ('',( #50961 ) ) ;
#24213=FILL_AREA_STYLE ('',( #39059 ) ) ;
#24214=VERTEX_POINT ( 'NONE', #15664 ) ;
#24216=FILL_AREA_STYLE ('',( #19272 ) ) ;
#24217=CARTESIAN_POINT ( 'NONE',  ( -21.02379604162863558, 114.6405644170961153, 10.00000000000000000 ) ) ;
#24220=STYLED_ITEM ( 'NONE', ( #58123 ), #39202 ) ;
#24226=AXIS2_PLACEMENT_3D ( 'NONE', #39380, #45014, #66068 ) ;
#24229=( NAMED_UNIT ( * ) SI_UNIT ( $, .STERADIAN. ) SOLID_ANGLE_UNIT ( ) );
#24231=ORIENTED_EDGE ( 'NONE', *, *, #5247, .T. ) ;
#24236=CARTESIAN_POINT ( 'NONE',  ( 2.607480562269128388, 117.9070736234661609, -8.024999999999963052 ) ) ;
#24242=CARTESIAN_POINT ( 'NONE',  ( -9.058813317711337021, 120.1549999999999869, -2.943386871421374895 ) ) ;
#24249=DIRECTION ( 'NONE',  ( -0.000000000000000000, -1.000000000000000000, 0.000000000000000000 ) ) ;
#24256=CARTESIAN_POINT ( 'NONE',  ( 19.89974874213240597, 115.4999999999999574, -10.50000000000000000 ) ) ;
#24259=VERTEX_POINT ( 'NONE', #52612 ) ;
#24262=FILL_AREA_STYLE_COLOUR ( '', #34933 ) ;
#24263=CARTESIAN_POINT ( 'NONE',  ( 23.21231517720797655, 117.9999999999999716, -7.000000000000000000 ) ) ;
#24268=EDGE_LOOP ( 'NONE', ( #8910, #24128, #29360, #26295 ) ) ;
#24270=CIRCLE ( 'NONE', #1782, 0.5000000000000004441 ) ;
#24273=CARTESIAN_POINT ( 'NONE',  ( 44.36184162591897717, 10.11502268137275351, -3.500000000000000000 ) ) ;
#24277=CARTESIAN_POINT ( 'NONE',  ( 8.102448949553181734, 144.3950000000000102, 5.886773742842750679 ) ) ;
#24280=EDGE_LOOP ( 'NONE', ( #11567, #15585, #69043, #67442, #34726 ) ) ;
#24282=CARTESIAN_POINT ( 'NONE',  ( 3.094860106618431583, 139.2050000000000125, 9.525000000000000355 ) ) ;
#24283=ORIENTED_EDGE ( 'NONE', *, *, #68539, .F. ) ;
#24284=CARTESIAN_POINT ( 'NONE',  ( -4.716976649647098618, 118.1429263765338078, 6.492361379858953008 ) ) ;
#24285=CARTESIAN_POINT ( 'NONE',  ( -74.99999999999998579, 50.00000000000000000, 7.000000000000000000 ) ) ;
#24286=UNCERTAINTY_MEASURE_WITH_UNIT (LENGTH_MEASURE( 1.000000000000000082E-05 ), #62426, 'distance_accuracy_value', 'NONE');
#24292=CARTESIAN_POINT ( 'NONE',  ( 71.99999999999998579, 64.07124727947029896, -7.000000000000000000 ) ) ;
#24293=ORIENTED_EDGE ( 'NONE', *, *, #9491, .F. ) ;
#24302=ADVANCED_FACE ( 'NONE', ( #9703, #36798 ), #38875, .T. ) ;
#24303=CARTESIAN_POINT ( 'NONE',  ( 71.50000000000000000, 14.49137674618942562, 7.000000000000000000 ) ) ;
#24304=CARTESIAN_POINT ( 'NONE',  ( 45.65811388300841855, 10.21937129433612235, -5.999999999999999112 ) ) ;
#24305=( NAMED_UNIT ( * ) SI_UNIT ( $, .STERADIAN. ) SOLID_ANGLE_UNIT ( ) );
#24306=ORIENTED_EDGE ( 'NONE', *, *, #47317, .T. ) ;
#24312=ORIENTED_EDGE ( 'NONE', *, *, #43869, .T. ) ;
#24313=EDGE_CURVE ( 'NONE', #67765, #38434, #58910, .T. ) ;
#24314=CARTESIAN_POINT ( 'NONE',  ( -44.50000000000000000, 10.49999999999998579, 4.000000000000000000 ) ) ;
#24315=ADVANCED_FACE ( 'NONE', ( #54982 ), #22302, .T. ) ;
#24318=EDGE_CURVE ( 'NONE', #60144, #49636, #53954, .T. ) ;
#24319=CARTESIAN_POINT ( 'NONE',  ( -75.00000000000000000, 9.675769070491714530, -6.195678411461598145 ) ) ;
#24325=CARTESIAN_POINT ( 'NONE',  ( -10.01517768586949231, 137.1949999999999363, -6.132527647946036459E-16 ) ) ;
#24328=UNCERTAINTY_MEASURE_WITH_UNIT (LENGTH_MEASURE( 1.000000000000000082E-05 ), #16512, 'distance_accuracy_value', 'NONE');
#24329=DIRECTION ( 'NONE',  ( 1.000000000000000000, -0.000000000000000000, -0.000000000000000000 ) ) ;
#24330=CARTESIAN_POINT ( 'NONE',  ( -6.826472737025120807, 144.9929263765338021, 4.959722759717906548 ) ) ;
#24334=DIRECTION ( 'NONE',  ( -1.000000000000000000, -0.000000000000000000, -0.000000000000000000 ) ) ;
#24338=EDGE_CURVE ( 'NONE', #54731, #25443, #50832, .T. ) ;
#24339=CARTESIAN_POINT ( 'NONE',  ( 2.607480562269128388, 119.7929263765338277, -8.024999999999963052 ) ) ;
#24340=CARTESIAN_POINT ( 'NONE',  ( 44.86933527532148247, 9.999999999999984013, 3.235873323885559039 ) ) ;
#24345=CIRCLE ( 'NONE', #693, 26.99999999999999645 ) ;
#24346=ORIENTED_EDGE ( 'NONE', *, *, #67754, .F. ) ;
#24347=CARTESIAN_POINT ( 'NONE',  ( 48.50000000000000000, 14.49137674618942562, -7.500000000000000000 ) ) ;
#24349=AXIS2_PLACEMENT_3D ( 'NONE', #62273, #14100, #47184 ) ;
#24350=DIRECTION ( 'NONE',  ( -1.000000000000000000, 0.000000000000000000, 0.000000000000000000 ) ) ;
#24352=CARTESIAN_POINT ( 'NONE',  ( -5.598654528085806881, 115.7449999999999903, -7.705886871421374629 ) ) ;
#24353=ORIENTED_EDGE ( 'NONE', *, *, #35845, .F. ) ;
#24355=CARTESIAN_POINT ( 'NONE',  ( 5.598654528085805993, 112.3549999999999898, 7.705886871421374629 ) ) ;
#24357=DIRECTION ( 'NONE',  ( 1.000000000000000000, 0.000000000000000000, 0.000000000000000000 ) ) ;
#24358=ORIENTED_EDGE ( 'NONE', *, *, #69191, .F. ) ;
#24359=CARTESIAN_POINT ( 'NONE',  ( 8.102448949553181734, 142.5049999999999955, 5.886773742842750679 ) ) ;
#24360=UNCERTAINTY_MEASURE_WITH_UNIT (LENGTH_MEASURE( 1.000000000000000082E-05 ), #62928, 'distance_accuracy_value', 'NONE');
#24361=FACE_OUTER_BOUND ( 'NONE', #657, .T. ) ;
#24366=ORIENTED_EDGE ( 'NONE', *, *, #48261, .T. ) ;
#24367=DIRECTION ( 'NONE',  ( -0.000000000000000000, 1.000000000000000000, -0.000000000000000000 ) ) ;
#24368=DIRECTION ( 'NONE',  ( 0.000000000000000000, 1.000000000000000000, 0.000000000000000000 ) ) ;
#24370=EDGE_LOOP ( 'NONE', ( #62156, #26954, #51802, #38765 ) ) ;
#24371=DIRECTION ( 'NONE',  ( -1.000000000000000000, 1.387778780781444256E-14, 0.000000000000000000 ) ) ;
#24379=ORIENTED_EDGE ( 'NONE', *, *, #39843, .F. ) ;
#24381=ORIENTED_EDGE ( 'NONE', *, *, #61606, .T. ) ;
#24382=CARTESIAN_POINT ( 'NONE',  ( 45.00000000000000000, 99.99999999999992895, 10.00000000000000000 ) ) ;
#24384=CARTESIAN_POINT ( 'NONE',  ( -74.99999999999998579, 50.00000000000000000, 12.00000000000000000 ) ) ;
#24387=CARTESIAN_POINT ( 'NONE',  ( 10.01517768586949408, 141.6949999999999648, 1.839758294383810543E-15 ) ) ;
#24389=EDGE_CURVE ( 'NONE', #21071, #52175, #23687, .T. ) ;
#24393=( LENGTH_UNIT ( ) NAMED_UNIT ( * ) SI_UNIT ( .MILLI., .METRE. ) );
#24394=( NAMED_UNIT ( * ) PLANE_ANGLE_UNIT ( ) SI_UNIT ( $, .RADIAN. ) );
#24396=MECHANICAL_DESIGN_GEOMETRIC_PRESENTATION_REPRESENTATION('',(#69317),#8650);
#24398=COLOUR_RGB ( '', 0.09019608, 0.27058824, 0.51372549) ;
#24400=CARTESIAN_POINT ( 'NONE',  ( -9.058813317711338797, 113.3449999999999847, 2.943386871421373563 ) ) ;
#24411=CARTESIAN_POINT ( 'NONE',  ( -6.826472737025120807, 124.5070736234661553, -4.959722759717907437 ) ) ;
#24419=DIRECTION ( 'NONE',  ( 0.000000000000000000, 0.000000000000000000, -1.000000000000000000 ) ) ;
#24420=CARTESIAN_POINT ( 'NONE',  ( -23.21231517720797655, 117.4999999999999716, 9.500000000000000000 ) ) ;
#24421=CARTESIAN_POINT ( 'NONE',  ( -41.00000000735875716, 108.0041655766031568, 3.104053578549263115 ) ) ;
#24422=SURFACE_SIDE_STYLE ('',( #2590 ) ) ;
#24423=VERTEX_POINT ( 'NONE', #29300 ) ;
#24427=CARTESIAN_POINT ( 'NONE',  ( 6.826472737025119919, 129.0070736234661695, 4.959722759717908325 ) ) ;
#24430=DIRECTION ( 'NONE',  ( 0.000000000000000000, 0.000000000000000000, -1.000000000000000000 ) ) ;
#24431=CYLINDRICAL_SURFACE ( 'NONE', #66566, 13.99999999999999822 ) ;
#24436=FACE_OUTER_BOUND ( 'NONE', #28327, .T. ) ;
#24439=PRESENTATION_STYLE_ASSIGNMENT (( #40665 ) ) ;
#24440=AXIS2_PLACEMENT_3D ( 'NONE', #35430, #8688, #3350 ) ;
#24446=ORIENTED_EDGE ( 'NONE', *, *, #57493, .T. ) ;
#24451=COLOUR_RGB ( '', 0.08235294, 0.09019608, 0.10196078) ;
#24452=DIRECTION ( 'NONE',  ( 0.000000000000000000, 1.000000000000000000, 0.000000000000000000 ) ) ;
#24454=SURFACE_SIDE_STYLE ('',( #41038 ) ) ;
#24456=EDGE_CURVE ( 'NONE', #13502, #35776, #37378, .T. ) ;
#24457=DIRECTION ( 'NONE',  ( 1.000000000000000000, 0.000000000000000000, 0.000000000000000000 ) ) ;
#24460=CARTESIAN_POINT ( 'NONE',  ( 3.094860106618435136, 115.2949999999999733, -9.525000000000000355 ) ) ;
#24465=ORIENTED_EDGE ( 'NONE', *, *, #35751, .T. ) ;
#24466=CARTESIAN_POINT ( 'NONE',  ( 71.18918918918917882, 14.09971791521133433, -9.500000000000000000 ) ) ;
#24467=( NAMED_UNIT ( * ) PLANE_ANGLE_UNIT ( ) SI_UNIT ( $, .RADIAN. ) );
#24468=DIRECTION ( 'NONE',  ( 0.000000000000000000, 0.000000000000000000, 1.000000000000000000 ) ) ;
#24469=DIRECTION ( 'NONE',  ( 0.000000000000000000, 0.000000000000000000, -1.000000000000000000 ) ) ;
#24472=( LENGTH_UNIT ( ) NAMED_UNIT ( * ) SI_UNIT ( .MILLI., .METRE. ) );
#24477=DIRECTION ( 'NONE',  ( 1.000000000000000000, 0.000000000000000000, 0.000000000000000000 ) ) ;
#24480=( GEOMETRIC_REPRESENTATION_CONTEXT ( 3 ) GLOBAL_UNCERTAINTY_ASSIGNED_CONTEXT ( ( #63700 ) ) GLOBAL_UNIT_ASSIGNED_CONTEXT ( ( #58831, #42697, #53555 ) ) REPRESENTATION_CONTEXT ( 'NONE', 'WORKASPACE' ) );
#24481=( GEOMETRIC_REPRESENTATION_CONTEXT ( 3 ) GLOBAL_UNCERTAINTY_ASSIGNED_CONTEXT ( ( #39681 ) ) GLOBAL_UNIT_ASSIGNED_CONTEXT ( ( #28709, #27659, #6231 ) ) REPRESENTATION_CONTEXT ( 'NONE', 'WORKASPACE' ) );
#24483=CARTESIAN_POINT ( 'NONE',  ( -3.094860106618434248, 150.9050000000000011, 9.525000000000000355 ) ) ;
#24485=VECTOR ( 'NONE', #7899, 1000.000000000000000 ) ;
#24486=MECHANICAL_DESIGN_GEOMETRIC_PRESENTATION_REPRESENTATION('',(#39164),#67124);
#24487=CARTESIAN_POINT ( 'NONE',  ( 45.50000000000000000, -1.469576158976824618E-14, -6.500000000000000000 ) ) ;
#24491=VECTOR ( 'NONE', #45821, 1000.000000000000000 ) ;
#24492=DIRECTION ( 'NONE',  ( 0.000000000000000000, 1.000000000000000000, 0.000000000000000000 ) ) ;
#24494=FACE_OUTER_BOUND ( 'NONE', #59697, .T. ) ;
#24495=ORIENTED_EDGE ( 'NONE', *, *, #3610, .T. ) ;
#24496=EDGE_LOOP ( 'NONE', ( #39858, #56533, #28485, #42490 ) ) ;
#24501=CARTESIAN_POINT ( 'NONE',  ( -45.00000000000000711, 9.298035018096991067, 6.651463925736444516 ) ) ;
#24503=EDGE_CURVE ( 'NONE', #60196, #58400, #27191, .T. ) ;
#24506=EDGE_LOOP ( 'NONE', ( #68188, #48471, #67255, #51906 ) ) ;
#24507=SURFACE_STYLE_USAGE ( .BOTH. , #30131 ) ;
#24511=CARTESIAN_POINT ( 'NONE',  ( -8.102448949553181734, 111.6049999999999613, 5.886773742842747126 ) ) ;
#24514=STYLED_ITEM ( 'NONE', ( #63719 ), #9738 ) ;
#24515=FILL_AREA_STYLE ('',( #19240 ) ) ;
#24518=AXIS2_PLACEMENT_3D ( 'NONE', #57973, #26280, #41123 ) ;
#24520=( NAMED_UNIT ( * ) SI_UNIT ( $, .STERADIAN. ) SOLID_ANGLE_UNIT ( ) );
#24522=ORIENTED_EDGE ( 'NONE', *, *, #50987, .F. ) ;
#24523=CARTESIAN_POINT ( 'NONE',  ( 7.632228543268607446, 146.0429263765338135, 2.479861379858954606 ) ) ;
#24532=DIRECTION ( 'NONE',  ( 0.000000000000000000, 0.000000000000000000, 1.000000000000000000 ) ) ;
#24541=DIRECTION ( 'NONE',  ( -1.000000000000000000, -0.000000000000000000, -0.000000000000000000 ) ) ;
#24543=VERTEX_POINT ( 'NONE', #4655 ) ;
#24547=CARTESIAN_POINT ( 'NONE',  ( 45.59262096826685706, 9.979230606950402205, 6.500000000000000000 ) ) ;
#24554=CARTESIAN_POINT ( 'NONE',  ( -45.48309787872866394, 9.683080749504643592, -6.499999999999997335 ) ) ;
#24562=CARTESIAN_POINT ( 'NONE',  ( -24.21231517720798365, 50.00000000000000000, 7.000000000000000000 ) ) ;
#24567=AXIS2_PLACEMENT_3D ( 'NONE', #30791, #9012, #57179 ) ;
#24569=CARTESIAN_POINT ( 'NONE',  ( 8.102448949553181734, 121.5049999999999670, 5.886773742842750679 ) ) ;
#24573=CIRCLE ( 'NONE', #63891, 0.5000000000000004441 ) ;
#24575=MECHANICAL_DESIGN_GEOMETRIC_PRESENTATION_REPRESENTATION('',(#37002),#30196);
#24576=CARTESIAN_POINT ( 'NONE',  ( -71.50000000000000000, 14.49137674618942206, -7.000000000000000000 ) ) ;
#24577=ORIENTED_EDGE ( 'NONE', *, *, #2888, .T. ) ;
#24580=DIRECTION ( 'NONE',  ( -1.000000000000000000, 0.000000000000000000, 0.000000000000000000 ) ) ;
#24582=STYLED_ITEM ( 'NONE', ( #38820 ), #66751 ) ;
#24585=DIRECTION ( 'NONE',  ( 0.000000000000000000, 0.000000000000000000, -1.000000000000000000 ) ) ;
#24586=LINE ( 'NONE', #63286, #55064 ) ;
#24588=ORIENTED_EDGE ( 'NONE', *, *, #13167, .T. ) ;
#24590=( GEOMETRIC_REPRESENTATION_CONTEXT ( 3 ) GLOBAL_UNCERTAINTY_ASSIGNED_CONTEXT ( ( #9362 ) ) GLOBAL_UNIT_ASSIGNED_CONTEXT ( ( #24393, #60987, #33573 ) ) REPRESENTATION_CONTEXT ( 'NONE', 'WORKASPACE' ) );
#24592=CARTESIAN_POINT ( 'NONE',  ( -20.71231517720798010, 149.9999999999999716, -10.00000000000000000 ) ) ;
#24596=ORIENTED_EDGE ( 'NONE', *, *, #64734, .T. ) ;
#24599=EDGE_CURVE ( 'NONE', #5542, #35967, #27958, .T. ) ;
#24600=ORIENTED_EDGE ( 'NONE', *, *, #56238, .F. ) ;
#24603=ORIENTED_EDGE ( 'NONE', *, *, #4149, .F. ) ;
#24605=CARTESIAN_POINT ( 'NONE',  ( -3.094860106618432471, 142.5950000000000273, -9.525000000000000355 ) ) ;
#24608=CARTESIAN_POINT ( 'NONE',  ( -3.094860106618434248, 135.9050000000000011, 9.525000000000000355 ) ) ;
#24609=CARTESIAN_POINT ( 'NONE',  ( 24.21231517720798010, 112.9999999999999858, -9.500000000000000000 ) ) ;
#24611=SURFACE_STYLE_FILL_AREA ( #30944 ) ;
#24612=ORIENTED_EDGE ( 'NONE', *, *, #60125, .F. ) ;
#24613=CARTESIAN_POINT ( 'NONE',  ( 2.607480562269071989, 118.5929263765338106, 8.025000000000002132 ) ) ;
#24614=DIRECTION ( 'NONE',  ( -0.000000000000000000, -0.000000000000000000, -1.000000000000000000 ) ) ;
#24615=EDGE_CURVE ( 'NONE', #65906, #62684, #54229, .T. ) ;
#24616=FACE_OUTER_BOUND ( 'NONE', #635, .T. ) ;
#24617=SURFACE_SIDE_STYLE ('',( #15172 ) ) ;
#24622=DIRECTION ( 'NONE',  ( 1.000000000000000000, 0.000000000000000000, 0.000000000000000000 ) ) ;
#24625=FACE_OUTER_BOUND ( 'NONE', #496, .T. ) ;
#24629=CARTESIAN_POINT ( 'NONE',  ( 71.50000000000000000, 35.92875272052971525, -7.500000000000000000 ) ) ;
#24631=CARTESIAN_POINT ( 'NONE',  ( 9.827790563157511022E-16, 111.9999999999999858, 8.025000000000000355 ) ) ;
#24632=CARTESIAN_POINT ( 'NONE',  ( 74.65399860055322279, 19.87094859200032815, 6.130873952096200341 ) ) ;
#24635=COLOUR_RGB ( '', 0.08235294, 0.09019608, 0.10196078) ;
#24636=ORIENTED_EDGE ( 'NONE', *, *, #58361, .T. ) ;
#24638=DIRECTION ( 'NONE',  ( 0.000000000000000000, -1.000000000000000000, 0.000000000000000000 ) ) ;
#24641=DIRECTION ( 'NONE',  ( -0.000000000000000000, -0.000000000000000000, 1.000000000000000000 ) ) ;
#24644=DIRECTION ( 'NONE',  ( -0.000000000000000000, -0.000000000000000000, 1.000000000000000000 ) ) ;
#24646=CARTESIAN_POINT ( 'NONE',  ( -75.00000000000000000, 9.484039020261590736, -6.483595844450460888 ) ) ;
#24650=COLOUR_RGB ( '', 0.08235294, 0.09019608, 0.10196078) ;
#24652=CARTESIAN_POINT ( 'NONE',  ( -9.058813317711338797, 140.3449999999999989, 2.943386871421373563 ) ) ;
#24655=CIRCLE ( 'NONE', #26847, 0.5000000000000004441 ) ;
#24661=SURFACE_STYLE_USAGE ( .BOTH. , #3171 ) ;
#24666=AXIS2_PLACEMENT_3D ( 'NONE', #24744, #9659, #31070 ) ;
#24669=CARTESIAN_POINT ( 'NONE',  ( -9.827790563157511022E-16, 128.5570736234661524, 8.025000000000000355 ) ) ;
#24671=AXIS2_PLACEMENT_3D ( 'NONE', #7412, #54873, #6693 ) ;
#24673=SURFACE_SIDE_STYLE ('',( #40205 ) ) ;
#24674=CARTESIAN_POINT ( 'NONE',  ( -45.64493973069768629, 8.371839367610334648, 6.471715848474669741 ) ) ;
#24675=CARTESIAN_POINT ( 'NONE',  ( 44.81375845693835203, 9.999999999999982236, 3.255894049711700600 ) ) ;
#24681=CARTESIAN_POINT ( 'NONE',  ( -20.77867704735745136, 115.1383905251040716, -10.00000000000000000 ) ) ;
#24683=ORIENTED_EDGE ( 'NONE', *, *, #28489, .T. ) ;
#24687=DIRECTION ( 'NONE',  ( 1.000000000000000000, 0.000000000000000000, 0.000000000000000000 ) ) ;
#24688=CARTESIAN_POINT ( 'NONE',  ( -6.826472737025120807, 158.1070736234661922, 4.959722759717906548 ) ) ;
#24691=ORIENTED_EDGE ( 'NONE', *, *, #23360, .F. ) ;
#24693=CARTESIAN_POINT ( 'NONE',  ( -8.102448949553179958, 111.6049999999999613, 5.886773742842747126 ) ) ;
#24694=EDGE_CURVE ( 'NONE', #58540, #1721, #59863, .T. ) ;
#24698=CARTESIAN_POINT ( 'NONE',  ( 9.058813317711338797, 139.9549999999999841, -2.943386871421372675 ) ) ;
#24700=SURFACE_STYLE_FILL_AREA ( #45855 ) ;
#24701=DIRECTION ( 'NONE',  ( 0.000000000000000000, 0.000000000000000000, -1.000000000000000000 ) ) ;
#24702=SURFACE_STYLE_FILL_AREA ( #41286 ) ;
#24703=FACE_OUTER_BOUND ( 'NONE', #11641, .T. ) ;
#24705=FACE_OUTER_BOUND ( 'NONE', #16862, .T. ) ;
#24710=CARTESIAN_POINT ( 'NONE',  ( 7.863253753129176182, 111.2778445948750203, 3.841316429231172780 ) ) ;
#24711=CARTESIAN_POINT ( 'NONE',  ( 0.000000000000000000, 115.0570736234661666, -8.025000000000000355 ) ) ;
#24712=CARTESIAN_POINT ( 'NONE',  ( -45.54107139885136490, 7.944008872641631136, -6.500000000000004441 ) ) ;
#24722=STYLED_ITEM ( 'NONE', ( #33944 ), #21122 ) ;
#24726=DIRECTION ( 'NONE',  ( 0.000000000000000000, 0.000000000000000000, -1.000000000000000000 ) ) ;
#24727=CARTESIAN_POINT ( 'NONE',  ( -9.058813317711338797, 140.3449999999999989, 2.943386871421373563 ) ) ;
#24731=SURFACE_SIDE_STYLE ('',( #4301 ) ) ;
#24735=( LENGTH_UNIT ( ) NAMED_UNIT ( * ) SI_UNIT ( .MILLI., .METRE. ) );
#24738=CARTESIAN_POINT ( 'NONE',  ( 8.102448949553183510, 111.9949999999999761, -5.886773742842746238 ) ) ;
#24744=CARTESIAN_POINT ( 'NONE',  ( 0.000000000000000000, 114.4999999999999574, 0.000000000000000000 ) ) ;
#24746=CARTESIAN_POINT ( 'NONE',  ( 44.99999999999977973, 146.9999999999999716, 7.500000000000000000 ) ) ;
#24753=CARTESIAN_POINT ( 'NONE',  ( -21.02379604162863913, 110.4999999999999858, 10.50000000000000000 ) ) ;
#24757=SURFACE_STYLE_USAGE ( .BOTH. , #8271 ) ;
#24761=CIRCLE ( 'NONE', #38455, 12.50000000000000000 ) ;
#24766=EDGE_LOOP ( 'NONE', ( #58488, #46638, #4336, #33481 ) ) ;
#24767=CARTESIAN_POINT ( 'NONE',  ( -45.00000000000000000, 99.99999999999992895, 4.000000000000000000 ) ) ;
#24769=VECTOR ( 'NONE', #25391, 1000.000000000000000 ) ;
#24773=CARTESIAN_POINT ( 'NONE',  ( -6.826472737025120807, 134.1070736234661638, 4.959722759717906548 ) ) ;
#24775=CARTESIAN_POINT ( 'NONE',  ( -6.826472737025120807, 130.5070736234661695, -4.959722759717907437 ) ) ;
#24776=AXIS2_PLACEMENT_3D ( 'NONE', #23822, #39011, #7639 ) ;
#24777=ORIENTED_EDGE ( 'NONE', *, *, #7241, .F. ) ;
#24782=AXIS2_PLACEMENT_3D ( 'NONE', #742, #17025, #6432 ) ;
#24787=LINE ( 'NONE', #2232, #40081 ) ;
#24788=CARTESIAN_POINT ( 'NONE',  ( 71.49999999999998579, 64.07124727947029896, 9.500000000000000000 ) ) ;
#24789=MECHANICAL_DESIGN_GEOMETRIC_PRESENTATION_REPRESENTATION('',(#56229),#51784);
#24790=CARTESIAN_POINT ( 'NONE',  ( 71.50000000000000000, 14.49137674618942562, 7.500000000000000000 ) ) ;
#24792=ORIENTED_EDGE ( 'NONE', *, *, #61221, .F. ) ;
#24793=VECTOR ( 'NONE', #28993, 1000.000000000000000 ) ;
#24796=EDGE_LOOP ( 'NONE', ( #66672, #44184, #29757, #7917 ) ) ;
#24800=EDGE_LOOP ( 'NONE', ( #52493, #27131, #25245, #66337 ) ) ;
#24801=( LENGTH_UNIT ( ) NAMED_UNIT ( * ) SI_UNIT ( .MILLI., .METRE. ) );
#24802=ORIENTED_EDGE ( 'NONE', *, *, #60732, .F. ) ;
#24803=SURFACE_STYLE_FILL_AREA ( #9358 ) ;
#24808=CARTESIAN_POINT ( 'NONE',  ( -1.166476076187854022E-15, 116.9449999999999932, 9.525000000000000355 ) ) ;
#24809=( BOUNDED_CURVE ( )  B_SPLINE_CURVE ( 3, ( #10707, #37496, #63484, #19864 ),
 .UNSPECIFIED., .F., .F. ) 
 B_SPLINE_CURVE_WITH_KNOTS ( ( 4, 4 ),
 ( 1.570796326794893227, 3.141592653589793116 ),
 .UNSPECIFIED. ) 
 CURVE ( )  GEOMETRIC_REPRESENTATION_ITEM ( )  RATIONAL_B_SPLINE_CURVE ( ( 1.000000000000000000, 0.8047378541243641603, 0.8047378541243641603, 1.000000000000000000 ) ) 
 REPRESENTATION_ITEM ( '' )  );
#24812=( NAMED_UNIT ( * ) PLANE_ANGLE_UNIT ( ) SI_UNIT ( $, .RADIAN. ) );
#24816=DIRECTION ( 'NONE',  ( -0.000000000000000000, -1.000000000000000000, 0.000000000000000000 ) ) ;
#24817=CARTESIAN_POINT ( 'NONE',  ( 23.21231517720797655, 113.4999999999999858, 9.500000000000000000 ) ) ;
#24819=( LENGTH_UNIT ( ) NAMED_UNIT ( * ) SI_UNIT ( .MILLI., .METRE. ) );
#24823=CARTESIAN_POINT ( 'NONE',  ( -75.00000000000000000, 9.708372675170620525, 6.100915009778867137 ) ) ;
#24824=CARTESIAN_POINT ( 'NONE',  ( -8.337051230037234362, 111.6531430745036886, 0.8624690973152070450 ) ) ;
#24829=AXIS2_PLACEMENT_3D ( 'NONE', #43185, #48103, #5131 ) ;
#24831=( NAMED_UNIT ( * ) SI_UNIT ( $, .STERADIAN. ) SOLID_ANGLE_UNIT ( ) );
#24832=UNCERTAINTY_MEASURE_WITH_UNIT (LENGTH_MEASURE( 1.000000000000000082E-05 ), #9868, 'distance_accuracy_value', 'NONE');
#24835=CIRCLE ( 'NONE', #64158, 0.5000000000000004441 ) ;
#24837=ADVANCED_FACE ( 'NONE', ( #42695 ), #37428, .T. ) ;
#24840=CARTESIAN_POINT ( 'NONE',  ( 0.000000000000000000, 158.5550000000000068, -9.525000000000000355 ) ) ;
#24841=FACE_OUTER_BOUND ( 'NONE', #58798, .T. ) ;
#24843=CARTESIAN_POINT ( 'NONE',  ( -0.7423632831649431552, 154.4999999999999716, -9.503379274660218812 ) ) ;
#24845=DIRECTION ( 'NONE',  ( 1.000000000000000000, 0.000000000000000000, 0.000000000000000000 ) ) ;
#24846=ADVANCED_FACE ( 'NONE', ( #67217 ), #55964, .T. ) ;
#24847=FACE_OUTER_BOUND ( 'NONE', #19057, .T. ) ;
#24853=DIRECTION ( 'NONE',  ( -0.000000000000000000, -0.000000000000000000, 1.000000000000000000 ) ) ;
#24858=CARTESIAN_POINT ( 'NONE',  ( -2.607480562269073765, 109.2070736234661439, -8.025000000000000355 ) ) ;
#24861=EDGE_CURVE ( 'NONE', #34471, #18929, #14790, .T. ) ;
#24862=SURFACE_STYLE_USAGE ( .BOTH. , #56890 ) ;
#24864=AXIS2_PLACEMENT_3D ( 'NONE', #59013, #56057, #37954 ) ;
#24866=CARTESIAN_POINT ( 'NONE',  ( -71.49999999999998579, 64.07124727947029896, 7.000000000000000000 ) ) ;
#24867=( NAMED_UNIT ( * ) PLANE_ANGLE_UNIT ( ) SI_UNIT ( $, .RADIAN. ) );
#24868=ORIENTED_EDGE ( 'NONE', *, *, #40105, .F. ) ;
#24869=CARTESIAN_POINT ( 'NONE',  ( 5.598654528085809545, 113.2549999999999812, -7.705886871421373741 ) ) ;
#24877=( GEOMETRIC_REPRESENTATION_CONTEXT ( 3 ) GLOBAL_UNCERTAINTY_ASSIGNED_CONTEXT ( ( #19400 ) ) GLOBAL_UNIT_ASSIGNED_CONTEXT ( ( #68396, #45601, #8279 ) ) REPRESENTATION_CONTEXT ( 'NONE', 'WORKASPACE' ) );
#24881=DIRECTION ( 'NONE',  ( -0.7071067811865352493, 0.000000000000000000, -0.7071067811865597852 ) ) ;
#24883=CARTESIAN_POINT ( 'NONE',  ( -8.437984349512095861, 147.6929263765338192, -5.166775262442723748E-16 ) ) ;
#24884=CARTESIAN_POINT ( 'NONE',  ( -9.827790563157511022E-16, 146.5570736234661524, 8.025000000000000355 ) ) ;
#24893=CARTESIAN_POINT ( 'NONE',  ( 41.03154609328242941, 107.7014457728230354, -3.191672614837956612 ) ) ;
#24895=DIRECTION ( 'NONE',  ( 0.000000000000000000, 1.000000000000000000, 0.000000000000000000 ) ) ;
#24896=FILL_AREA_STYLE_COLOUR ( '', #40019 ) ;
#24905=DIRECTION ( 'NONE',  ( 0.000000000000000000, 0.000000000000000000, -1.000000000000000000 ) ) ;
#24907=CARTESIAN_POINT ( 'NONE',  ( 7.632228543268607446, 114.1570736234661609, 2.479861379858954606 ) ) ;
#24913=COLOUR_RGB ( '', 0.09019608, 0.27058824, 0.51372549) ;
#24915=SURFACE_SIDE_STYLE ('',( #3421 ) ) ;
#24918=AXIS2_PLACEMENT_3D ( 'NONE', #32410, #38091, #60202 ) ;
#24919=ADVANCED_FACE ( 'NONE', ( #68270 ), #20049, .F. ) ;
#24921=( NAMED_UNIT ( * ) SI_UNIT ( $, .STERADIAN. ) SOLID_ANGLE_UNIT ( ) );
#24924=( NAMED_UNIT ( * ) PLANE_ANGLE_UNIT ( ) SI_UNIT ( $, .RADIAN. ) );
#24926=CIRCLE ( 'NONE', #64233, 0.5000000000000004441 ) ;
#24927=LINE ( 'NONE', #68208, #29212 ) ;
#24928=EDGE_CURVE ( 'NONE', #53321, #38434, #49732, .T. ) ;
#24930=ADVANCED_FACE ( 'NONE', ( #41217 ), #51749, .F. ) ;
#24931=CARTESIAN_POINT ( 'NONE',  ( 8.102448949553183510, 128.1049999999999898, -5.886773742842746238 ) ) ;
#24938=VECTOR ( 'NONE', #39905, 1000.000000000000000 ) ;
#24941=EDGE_CURVE ( 'NONE', #29891, #67533, #53098, .T. ) ;
#24945=PRESENTATION_STYLE_ASSIGNMENT (( #46819 ) ) ;
#24946=EDGE_CURVE ( 'NONE', #56993, #19879, #1360, .T. ) ;
#24948=DIRECTION ( 'NONE',  ( 0.000000000000000000, 0.000000000000000000, 1.000000000000000000 ) ) ;
#24951=VERTEX_POINT ( 'NONE', #46865 ) ;
#24952=ORIENTED_EDGE ( 'NONE', *, *, #3124, .F. ) ;
#24954=CARTESIAN_POINT ( 'NONE',  ( -6.826472737025120807, 147.3929263765337794, -4.959722759717907437 ) ) ;
#24955=SURFACE_SIDE_STYLE ('',( #56632 ) ) ;
#24956=FILL_AREA_STYLE ('',( #51708 ) ) ;
#24966=DIRECTION ( 'NONE',  ( 1.000000000000000000, 0.000000000000000000, 0.000000000000000000 ) ) ;
#24967=VERTEX_POINT ( 'NONE', #11581 ) ;
#24968=VECTOR ( 'NONE', #56167, 1000.000000000000000 ) ;
#24969=EDGE_CURVE ( 'NONE', #10638, #29261, #21104, .T. ) ;
#24971=CARTESIAN_POINT ( 'NONE',  ( -3.094860106618434248, 143.7949999999999875, 9.525000000000000355 ) ) ;
#24973=ORIENTED_EDGE ( 'NONE', *, *, #6200, .T. ) ;
#24975=CARTESIAN_POINT ( 'NONE',  ( 8.102448949553181734, 149.1049999999999898, -5.886773742842746238 ) ) ;
#24976=CARTESIAN_POINT ( 'NONE',  ( 34.99999999999999289, 99.99999999999998579, -7.000000000000000000 ) ) ;
#24977=SURFACE_SIDE_STYLE ('',( #24611 ) ) ;
#24979=CARTESIAN_POINT ( 'NONE',  ( -7.632228543268608334, 120.8429263765338249, 2.479861379858952830 ) ) ;
#24980=CARTESIAN_POINT ( 'NONE',  ( -71.50000000000000000, 50.00000000000000000, 7.000000000000000000 ) ) ;
#24982=( NAMED_UNIT ( * ) SI_UNIT ( $, .STERADIAN. ) SOLID_ANGLE_UNIT ( ) );
#24994=( GEOMETRIC_REPRESENTATION_CONTEXT ( 3 ) GLOBAL_UNCERTAINTY_ASSIGNED_CONTEXT ( ( #53874 ) ) GLOBAL_UNIT_ASSIGNED_CONTEXT ( ( #15944, #36376, #42356 ) ) REPRESENTATION_CONTEXT ( 'NONE', 'WORKASPACE' ) );
#24996=DIRECTION ( 'NONE',  ( 1.000000000000000000, -8.881784197001254296E-16, 0.000000000000000000 ) ) ;
#24997=UNCERTAINTY_MEASURE_WITH_UNIT (LENGTH_MEASURE( 1.000000000000000082E-05 ), #64629, 'distance_accuracy_value', 'NONE');
#24998=AXIS2_PLACEMENT_3D ( 'NONE', #51286, #35464, #4101 ) ;
#25000=CARTESIAN_POINT ( 'NONE',  ( 75.00000000000000000, 20.36037960999351881, 6.130923279862163788 ) ) ;
#25001=CARTESIAN_POINT ( 'NONE',  ( -74.99999999999998579, 50.00000000000000000, 11.50000000000000000 ) ) ;
#25002=ORIENTED_EDGE ( 'NONE', *, *, #27682, .F. ) ;
#25003=SURFACE_STYLE_FILL_AREA ( #3500 ) ;
#25004=VERTEX_POINT ( 'NONE', #64716 ) ;
#25006=PRESENTATION_STYLE_ASSIGNMENT (( #3504 ) ) ;
#25007=AXIS2_PLACEMENT_3D ( 'NONE', #30017, #8240, #56771 ) ;
#25009=ORIENTED_EDGE ( 'NONE', *, *, #40958, .T. ) ;
#25012=EDGE_CURVE ( 'NONE', #20601, #373, #60950, .T. ) ;
#25017=ADVANCED_FACE ( 'NONE', ( #54490 ), #58747, .F. ) ;
#25019=CARTESIAN_POINT ( 'NONE',  ( -45.91547277936962246, 9.430195807687219656, -6.500000000000000000 ) ) ;
#25020=DIRECTION ( 'NONE',  ( -0.000000000000000000, -0.000000000000000000, -1.000000000000000000 ) ) ;
#25024=CARTESIAN_POINT ( 'NONE',  ( 9.058813317711337021, 153.5449999999999875, 2.943386871421375783 ) ) ;
#25029=UNCERTAINTY_MEASURE_WITH_UNIT (LENGTH_MEASURE( 1.000000000000000082E-05 ), #51102, 'distance_accuracy_value', 'NONE');
#25035=CARTESIAN_POINT ( 'NONE',  ( 9.827790563157511022E-16, 87.30187232391182306, -8.025000000000000355 ) ) ;
#25040=SURFACE_STYLE_FILL_AREA ( #25715 ) ;
#25044=EDGE_LOOP ( 'NONE', ( #23562, #41448, #16459 ) ) ;
#25045=STYLED_ITEM ( 'NONE', ( #39907 ), #35828 ) ;
#25047=UNCERTAINTY_MEASURE_WITH_UNIT (LENGTH_MEASURE( 1.000000000000000082E-05 ), #12026, 'distance_accuracy_value', 'NONE');
#25050=COLOUR_RGB ( '', 0.31764706, 0.68627451, 0.89019608) ;
#25053=AXIS2_PLACEMENT_3D ( 'NONE', #9898, #4583, #46523 ) ;
#25057=DIRECTION ( 'NONE',  ( 0.000000000000000000, -6.938893903907222067E-15, 1.000000000000000000 ) ) ;
#25061=CARTESIAN_POINT ( 'NONE',  ( -9.058813317711337021, 113.0449999999999875, -2.943386871421374895 ) ) ;
#25062=STYLED_ITEM ( 'NONE', ( #60803 ), #26314 ) ;
#25063=EDGE_LOOP ( 'NONE', ( #62771, #61576, #57761, #40779 ) ) ;
#25064=DIRECTION ( 'NONE',  ( 0.000000000000000000, -0.000000000000000000, -1.000000000000000000 ) ) ;
#25065=CARTESIAN_POINT ( 'NONE',  ( -71.50000000000000000, 35.92875272052971525, 10.00000000000000000 ) ) ;
#25068=EDGE_LOOP ( 'NONE', ( #68506, #32317, #53923, #65981 ) ) ;
#25069=CARTESIAN_POINT ( 'NONE',  ( -5.598654528085806881, 140.8549999999999898, -7.705886871421374629 ) ) ;
#25073=CARTESIAN_POINT ( 'NONE',  ( 19.98523465219084017, 114.9999999999999574, 10.47102667436386625 ) ) ;
#25074=DIRECTION ( 'NONE',  ( 1.000000000000000000, 0.000000000000000000, 0.000000000000000000 ) ) ;
#25075=SURFACE_STYLE_USAGE ( .BOTH. , #29660 ) ;
#25079=FILL_AREA_STYLE ('',( #40944 ) ) ;
#25083=CARTESIAN_POINT ( 'NONE',  ( 8.440061761865212731, 111.3586140163384215, 2.039925464057781745 ) ) ;
#25086=DIRECTION ( 'NONE',  ( 0.000000000000000000, 0.000000000000000000, -1.000000000000000000 ) ) ;
#25090=SURFACE_STYLE_USAGE ( .BOTH. , #18769 ) ;
#25092=CIRCLE ( 'NONE', #65604, 0.4999999999999991118 ) ;
#25095=EDGE_CURVE ( 'NONE', #17136, #64475, #21444, .T. ) ;
#25108=CARTESIAN_POINT ( 'NONE',  ( 10.01517768586949231, 111.6949999999999932, 1.839758294383810543E-15 ) ) ;
#25113=DIRECTION ( 'NONE',  ( -0.000000000000000000, -0.000000000000000000, -1.000000000000000000 ) ) ;
#25118=ADVANCED_FACE ( 'NONE', ( #28788 ), #8039, .F. ) ;
#25119=AXIS2_PLACEMENT_3D ( 'NONE', #30675, #3207, #8559 ) ;
#25120=CARTESIAN_POINT ( 'NONE',  ( -45.00000000000463984, 9.678589032125119118, -3.510839860134217005 ) ) ;
#25130=CIRCLE ( 'NONE', #2585, 0.5000000000000004441 ) ;
#25132=CARTESIAN_POINT ( 'NONE',  ( 4.716976649647096842, 122.8570736234661638, 6.492361379858953896 ) ) ;
#25134=PRESENTATION_STYLE_ASSIGNMENT (( #57131 ) ) ;
#25137=( NAMED_UNIT ( * ) PLANE_ANGLE_UNIT ( ) SI_UNIT ( $, .RADIAN. ) );
#25140=STYLED_ITEM ( 'NONE', ( #42511 ), #36609 ) ;
#25143=CARTESIAN_POINT ( 'NONE',  ( 6.826472737025119919, 132.0070736234661695, 4.959722759717908325 ) ) ;
#25144=PRESENTATION_STYLE_ASSIGNMENT (( #30752 ) ) ;
#25149=ORIENTED_EDGE ( 'NONE', *, *, #33983, .F. ) ;
#25152=( NAMED_UNIT ( * ) PLANE_ANGLE_UNIT ( ) SI_UNIT ( $, .RADIAN. ) );
#25153=SURFACE_STYLE_USAGE ( .BOTH. , #30398 ) ;
#25154=ORIENTED_EDGE ( 'NONE', *, *, #35524, .F. ) ;
#25156=( NAMED_UNIT ( * ) PLANE_ANGLE_UNIT ( ) SI_UNIT ( $, .RADIAN. ) );
#25162=ORIENTED_EDGE ( 'NONE', *, *, #22584, .T. ) ;
#25164=SURFACE_STYLE_FILL_AREA ( #56839 ) ;
#25167=ORIENTED_EDGE ( 'NONE', *, *, #40354, .F. ) ;
#25171=DIRECTION ( 'NONE',  ( 1.000000000000000000, 0.000000000000000000, 0.000000000000000000 ) ) ;
#25172=DIRECTION ( 'NONE',  ( 0.000000000000000000, 0.000000000000000000, 1.000000000000000000 ) ) ;
#25173=FACE_OUTER_BOUND ( 'NONE', #19797, .T. ) ;
#25176=CARTESIAN_POINT ( 'NONE',  ( -1.166476076187854022E-15, 110.9449999999999932, 9.525000000000000355 ) ) ;
#25177=EDGE_CURVE ( 'NONE', #28083, #58801, #43989, .T. ) ;
#25180=VERTEX_POINT ( 'NONE', #18250 ) ;
#25181=FACE_OUTER_BOUND ( 'NONE', #23069, .T. ) ;
#25184=DIRECTION ( 'NONE',  ( 1.000000000000000000, 0.000000000000000000, 0.000000000000000000 ) ) ;
#25186=( GEOMETRIC_REPRESENTATION_CONTEXT ( 3 ) GLOBAL_UNCERTAINTY_ASSIGNED_CONTEXT ( ( #29201 ) ) GLOBAL_UNIT_ASSIGNED_CONTEXT ( ( #10176, #47871, #20732 ) ) REPRESENTATION_CONTEXT ( 'NONE', 'WORKASPACE' ) );
#25190=ADVANCED_FACE ( 'NONE', ( #65404 ), #28072, .T. ) ;
#25196=FILL_AREA_STYLE_COLOUR ( '', #32325 ) ;
#25203=CARTESIAN_POINT ( 'NONE',  ( -5.598654528085806881, 158.8549999999999898, -7.705886871421374629 ) ) ;
#25210=AXIS2_PLACEMENT_3D ( 'NONE', #26793, #65499, #28175 ) ;
#25211=CARTESIAN_POINT ( 'NONE',  ( 45.00000000000000000, -1.469576158976824618E-14, 10.00000000000000000 ) ) ;
#25212=FILL_AREA_STYLE ('',( #68838 ) ) ;
#25216=EDGE_LOOP ( 'NONE', ( #27960, #17513, #57610, #34914 ) ) ;
#25218=FACE_OUTER_BOUND ( 'NONE', #68017, .T. ) ;
#25225=CARTESIAN_POINT ( 'NONE',  ( -21.02379604162863913, 154.9999999999999716, 10.50000000000000000 ) ) ;
#25228=CARTESIAN_POINT ( 'NONE',  ( 5.598654528085805993, 115.3549999999999898, 7.705886871421374629 ) ) ;
#25230=DIRECTION ( 'NONE',  ( 0.000000000000000000, -1.000000000000000000, 0.000000000000000000 ) ) ;
#25237=DIRECTION ( 'NONE',  ( 0.000000000000000000, 0.000000000000000000, 1.000000000000000000 ) ) ;
#25238=FILL_AREA_STYLE ('',( #8387 ) ) ;
#25239=( GEOMETRIC_REPRESENTATION_CONTEXT ( 3 ) GLOBAL_UNCERTAINTY_ASSIGNED_CONTEXT ( ( #20117 ) ) GLOBAL_UNIT_ASSIGNED_CONTEXT ( ( #9395, #58253, #19211 ) ) REPRESENTATION_CONTEXT ( 'NONE', 'WORKASPACE' ) );
#25241=CARTESIAN_POINT ( 'NONE',  ( -2.607480562269075097, 145.2929263765338135, 8.025000000000000355 ) ) ;
#25244=EDGE_CURVE ( 'NONE', #60543, #44642, #3525, .T. ) ;
#25245=ORIENTED_EDGE ( 'NONE', *, *, #8981, .T. ) ;
#25246=FILL_AREA_STYLE_COLOUR ( '', #23986 ) ;
#25247=EDGE_LOOP ( 'NONE', ( #59833, #15959, #50614 ) ) ;
#25250=PLANE ( 'NONE',  #64467 ) ;
#25254=FILL_AREA_STYLE ('',( #35120 ) ) ;
#25255=EDGE_CURVE ( 'NONE', #28559, #10363, #47099, .T. ) ;
#25260=CARTESIAN_POINT ( 'NONE',  ( -60.00000000000000000, -2.024042244987997205E-14, -7.000000000000000000 ) ) ;
#25263=CYLINDRICAL_SURFACE ( 'NONE', #5081, 0.5000000000000004441 ) ;
#25264=CARTESIAN_POINT ( 'NONE',  ( -54.50000000000002132, -2.024042244987997205E-14, 12.00000000000000000 ) ) ;
#25272=CIRCLE ( 'NONE', #41070, 0.5000000000000004441 ) ;
#25273=( GEOMETRIC_REPRESENTATION_CONTEXT ( 3 ) GLOBAL_UNCERTAINTY_ASSIGNED_CONTEXT ( ( #1036 ) ) GLOBAL_UNIT_ASSIGNED_CONTEXT ( ( #23838, #24867, #66759 ) ) REPRESENTATION_CONTEXT ( 'NONE', 'WORKASPACE' ) );
#25275=CARTESIAN_POINT ( 'NONE',  ( 40.96599324808799025, 108.0258340745533161, 3.573232801688252636 ) ) ;
#25278=EDGE_CURVE ( 'NONE', #34471, #55705, #13656, .T. ) ;
#25281=CARTESIAN_POINT ( 'NONE',  ( 9.527321842919894479, 154.4999999999999716, 0.3821556790526681180 ) ) ;
#25282=CARTESIAN_POINT ( 'NONE',  ( -60.00000000000000000, -2.024042244987997205E-14, 6.999999999999999112 ) ) ;
#25284=CARTESIAN_POINT ( 'NONE',  ( -10.01517768586949231, 126.3049999999999784, -6.132527647946036459E-16 ) ) ;
#25290=CARTESIAN_POINT ( 'NONE',  ( -40.99999999999998579, 107.7459666924148394, 3.000000000000000000 ) ) ;
#25298=DIRECTION ( 'NONE',  ( 0.000000000000000000, 0.000000000000000000, 1.000000000000000000 ) ) ;
#25299=DIRECTION ( 'NONE',  ( -0.6216216216216174928, 0.7833176619561892373, 0.000000000000000000 ) ) ;
#25305=AXIS2_PLACEMENT_3D ( 'NONE', #60043, #21720, #21360 ) ;
#25306=DIRECTION ( 'NONE',  ( 1.000000000000000000, 0.000000000000000000, -0.000000000000000000 ) ) ;
#25307=DIRECTION ( 'NONE',  ( 0.000000000000000000, 0.000000000000000000, 1.000000000000000000 ) ) ;
#25308=( LENGTH_UNIT ( ) NAMED_UNIT ( * ) SI_UNIT ( .MILLI., .METRE. ) );
#25312=EDGE_LOOP ( 'NONE', ( #1322, #15486, #23967 ) ) ;
#25313=CARTESIAN_POINT ( 'NONE',  ( 0.000000000000000000, 115.4999999999999574, 0.000000000000000000 ) ) ;
#25316=ORIENTED_EDGE ( 'NONE', *, *, #24694, .F. ) ;
#25317=AXIS2_PLACEMENT_3D ( 'NONE', #8295, #68775, #57510 ) ;
#25320=CARTESIAN_POINT ( 'NONE',  ( -3.094860106618432471, 151.5949999999999989, -9.525000000000000355 ) ) ;
#25324=CARTESIAN_POINT ( 'NONE',  ( 8.102448949553179958, 148.5049999999999955, 5.886773742842750679 ) ) ;
#25329=CARTESIAN_POINT ( 'NONE',  ( -8.437984349512095861, 111.6929263765338192, -5.166775262442723748E-16 ) ) ;
#25330=FILL_AREA_STYLE_COLOUR ( '', #38629 ) ;
#25331=FACE_OUTER_BOUND ( 'NONE', #18836, .T. ) ;
#25343=EDGE_LOOP ( 'NONE', ( #35296, #41352, #62628, #55307 ) ) ;
#25344=DIRECTION ( 'NONE',  ( -0.000000000000000000, -0.000000000000000000, 1.000000000000000000 ) ) ;
#25346=EDGE_CURVE ( 'NONE', #47500, #11929, #47584, .T. ) ;
#25347=AXIS2_PLACEMENT_3D ( 'NONE', #48349, #39, #21573 ) ;
#25348=DIRECTION ( 'NONE',  ( 0.000000000000000000, 0.000000000000000000, -1.000000000000000000 ) ) ;
#25350=CARTESIAN_POINT ( 'NONE',  ( 74.63815776008151204, 19.81286551027082155, 6.251809480268890162 ) ) ;
#25352=ORIENTED_EDGE ( 'NONE', *, *, #22101, .T. ) ;
#25353=EDGE_CURVE ( 'NONE', #58654, #35727, #32741, .T. ) ;
#25356=ORIENTED_EDGE ( 'NONE', *, *, #8239, .F. ) ;
#25359=DIRECTION ( 'NONE',  ( 0.000000000000000000, -1.000000000000000000, 3.469446951953613794E-15 ) ) ;
#25361=AXIS2_PLACEMENT_3D ( 'NONE', #38563, #22335, #16052 ) ;
#25364=FACE_OUTER_BOUND ( 'NONE', #66079, .T. ) ;
#25367=CARTESIAN_POINT ( 'NONE',  ( 8.102448949553183510, 150.9950000000000045, -5.886773742842746238 ) ) ;
#25370=MECHANICAL_DESIGN_GEOMETRIC_PRESENTATION_REPRESENTATION('',(#68073),#13015);
#25371=CARTESIAN_POINT ( 'NONE',  ( -52.50000000000000000, -2.024042244987997205E-14, 11.50000000000000000 ) ) ;
#25372=EDGE_CURVE ( 'NONE', #12385, #11851, #54666, .T. ) ;
#25374=ORIENTED_EDGE ( 'NONE', *, *, #43825, .F. ) ;
#25382=CIRCLE ( 'NONE', #6297, 12.50000000000000000 ) ;
#25385=EDGE_LOOP ( 'NONE', ( #6182, #66858, #65825, #46201 ) ) ;
#25386=SURFACE_STYLE_USAGE ( .BOTH. , #59724 ) ;
#25390=CARTESIAN_POINT ( 'NONE',  ( -2.607480562269115509, 117.0929263765338249, -8.024999999999970157 ) ) ;
#25391=DIRECTION ( 'NONE',  ( -0.000000000000000000, -0.000000000000000000, -1.000000000000000000 ) ) ;
#25398=ORIENTED_EDGE ( 'NONE', *, *, #13048, .T. ) ;
#25401=CARTESIAN_POINT ( 'NONE',  ( 8.102448949553183510, 111.9949999999999761, -5.886773742842746238 ) ) ;
#25403=ORIENTED_EDGE ( 'NONE', *, *, #63528, .T. ) ;
#25406=CARTESIAN_POINT ( 'NONE',  ( 8.102448949553181734, 125.1049999999999613, -5.886773742842746238 ) ) ;
#25411=CARTESIAN_POINT ( 'NONE',  ( 3.094860106618431583, 139.2050000000000125, 9.525000000000000355 ) ) ;
#25412=CARTESIAN_POINT ( 'NONE',  ( 65.00000000000000000, 1.797044900979284448E-15, 6.999999999999988454 ) ) ;
#25413=DIRECTION ( 'NONE',  ( -0.000000000000000000, -0.000000000000000000, -1.000000000000000000 ) ) ;
#25414=AXIS2_PLACEMENT_3D ( 'NONE', #37243, #36558, #9792 ) ;
#25417=CIRCLE ( 'NONE', #2920, 0.4999999999999990563 ) ;
#25419=ORIENTED_EDGE ( 'NONE', *, *, #35122, .F. ) ;
#25420=PLANE ( 'NONE',  #46430 ) ;
#25421=CARTESIAN_POINT ( 'NONE',  ( 20.57648123223228254, 154.9999999999999716, -10.27659574468085069 ) ) ;
#25423=VERTEX_POINT ( 'NONE', #68881 ) ;
#25424=CARTESIAN_POINT ( 'NONE',  ( 7.255760115451125536, 111.6477319965992763, -4.196031671614247394 ) ) ;
#25427=VERTEX_POINT ( 'NONE', #20682 ) ;
#25428=SURFACE_STYLE_FILL_AREA ( #41641 ) ;
#25431=EDGE_CURVE ( 'NONE', #39125, #28212, #456, .T. ) ;
#25433=AXIS2_PLACEMENT_3D ( 'NONE', #63889, #57595, #10455 ) ;
#25434=CARTESIAN_POINT ( 'NONE',  ( 60.00000000000000000, 1.797044900979284448E-15, 10.00000000000000000 ) ) ;
#25440=( LENGTH_UNIT ( ) NAMED_UNIT ( * ) SI_UNIT ( .MILLI., .METRE. ) );
#25441=SURFACE_STYLE_FILL_AREA ( #37446 ) ;
#25443=VERTEX_POINT ( 'NONE', #39222 ) ;
#25450=CARTESIAN_POINT ( 'NONE',  ( -10.01517768586949231, 119.1949999999999932, -6.132527647946036459E-16 ) ) ;
#25452=SURFACE_STYLE_FILL_AREA ( #8599 ) ;
#25454=SURFACE_STYLE_FILL_AREA ( #68049 ) ;
#25455=CYLINDRICAL_SURFACE ( 'NONE', #39129, 0.5000000000000004441 ) ;
#25456=ORIENTED_EDGE ( 'NONE', *, *, #67206, .F. ) ;
#25461=VECTOR ( 'NONE', #44080, 1000.000000000000000 ) ;
#25462=AXIS2_PLACEMENT_3D ( 'NONE', #9175, #3848, #26012 ) ;
#25464=SURFACE_SIDE_STYLE ('',( #26497 ) ) ;
#25469=CARTESIAN_POINT ( 'NONE',  ( 6.826472737025121695, 152.4929263765338305, -4.959722759717905660 ) ) ;
#25474=DIRECTION ( 'NONE',  ( -1.000000000000000000, 0.000000000000000000, 0.000000000000000000 ) ) ;
#25479=CARTESIAN_POINT ( 'NONE',  ( 2.607480562269076430, 129.9070736234661467, -8.025000000000000355 ) ) ;
#25480=( LENGTH_UNIT ( ) NAMED_UNIT ( * ) SI_UNIT ( .MILLI., .METRE. ) );
#25481=ORIENTED_EDGE ( 'NONE', *, *, #34479, .F. ) ;
#25484=DIRECTION ( 'NONE',  ( 0.9486832980505138790, 0.3162277660168378857, -0.000000000000000000 ) ) ;
#25485=ORIENTED_EDGE ( 'NONE', *, *, #25557, .F. ) ;
#25489=DIRECTION ( 'NONE',  ( 0.000000000000000000, 0.000000000000000000, 1.000000000000000000 ) ) ;
#25497=UNCERTAINTY_MEASURE_WITH_UNIT (LENGTH_MEASURE( 1.000000000000000082E-05 ), #41734, 'distance_accuracy_value', 'NONE');
#25500=CARTESIAN_POINT ( 'NONE',  ( -74.99999999999998579, 50.00000000000000000, -11.50000000000000000 ) ) ;
#25502=EDGE_CURVE ( 'NONE', #41266, #44352, #59753, .T. ) ;
#25503=( NAMED_UNIT ( * ) SI_UNIT ( $, .STERADIAN. ) SOLID_ANGLE_UNIT ( ) );
#25504=SPHERICAL_SURFACE ( 'NONE', #66034, 0.5000000000000000000 ) ;
#25507=VERTEX_POINT ( 'NONE', #60296 ) ;
#25508=( NAMED_UNIT ( * ) PLANE_ANGLE_UNIT ( ) SI_UNIT ( $, .RADIAN. ) );
#25509=FACE_OUTER_BOUND ( 'NONE', #30775, .T. ) ;
#25510=CARTESIAN_POINT ( 'NONE',  ( -41.06080360525773187, 107.9551383427286737, 3.682527553402528131 ) ) ;
#25512=CARTESIAN_POINT ( 'NONE',  ( 8.102448949553181734, 126.9949999999999903, -5.886773742842746238 ) ) ;
#25514=CARTESIAN_POINT ( 'NONE',  ( 2.607480562269055113, 113.7929263765338277, -8.025000000000016342 ) ) ;
#25518=SURFACE_STYLE_FILL_AREA ( #57182 ) ;
#25520=( NAMED_UNIT ( * ) PLANE_ANGLE_UNIT ( ) SI_UNIT ( $, .RADIAN. ) );
#25524=CARTESIAN_POINT ( 'NONE',  ( -8.443929654699774190, 111.5904618153164449, 0.06143411491520953116 ) ) ;
#25527=ORIENTED_EDGE ( 'NONE', *, *, #24861, .T. ) ;
#25529=( LENGTH_UNIT ( ) NAMED_UNIT ( * ) SI_UNIT ( .MILLI., .METRE. ) );
#25530=UNCERTAINTY_MEASURE_WITH_UNIT (LENGTH_MEASURE( 1.000000000000000082E-05 ), #48368, 'distance_accuracy_value', 'NONE');
#25533=CARTESIAN_POINT ( 'NONE',  ( -8.102448949553181734, 153.6049999999999898, 5.886773742842747126 ) ) ;
#25534=DIRECTION ( 'NONE',  ( -0.000000000000000000, -0.000000000000000000, -1.000000000000000000 ) ) ;
#25536=UNCERTAINTY_MEASURE_WITH_UNIT (LENGTH_MEASURE( 1.000000000000000082E-05 ), #21640, 'distance_accuracy_value', 'NONE');
#25537=CARTESIAN_POINT ( 'NONE',  ( -6.669484432086554726, 110.5589211602357267, 6.756431230639685204 ) ) ;
#25538=LINE ( 'NONE', #47055, #4549 ) ;
#25539=AXIS2_PLACEMENT_3D ( 'NONE', #16466, #31552, #9784 ) ;
#25549=ADVANCED_FACE ( 'NONE', ( #19097 ), #3234, .F. ) ;
#25550=CARTESIAN_POINT ( 'NONE',  ( -20.86748625714523087, 115.0277251398784273, 10.00000000000000000 ) ) ;
#25557=EDGE_CURVE ( 'NONE', #43604, #52539, #45293, .T. ) ;
#25559=CARTESIAN_POINT ( 'NONE',  ( 8.102448949553181734, 118.5049999999999955, 5.886773742842750679 ) ) ;
#25560=LINE ( 'NONE', #5152, #49032 ) ;
#25566=ORIENTED_EDGE ( 'NONE', *, *, #13916, .T. ) ;
#25567=LINE ( 'NONE', #51628, #58025 ) ;
#25572=CARTESIAN_POINT ( 'NONE',  ( -4.716976649647097730, 159.2429263765338021, -6.492361379858953896 ) ) ;
#25577=VERTEX_POINT ( 'NONE', #2894 ) ;
#25578=( LENGTH_UNIT ( ) NAMED_UNIT ( * ) SI_UNIT ( .MILLI., .METRE. ) );
#25579=( NAMED_UNIT ( * ) SI_UNIT ( $, .STERADIAN. ) SOLID_ANGLE_UNIT ( ) );
#25582=CARTESIAN_POINT ( 'NONE',  ( 6.826472737025119919, 141.0070736234661410, 4.959722759717908325 ) ) ;
#25585=SURFACE_STYLE_FILL_AREA ( #26285 ) ;
#25586=CARTESIAN_POINT ( 'NONE',  ( -74.99999999999998579, 36.00000000000000711, 9.500000000000001776 ) ) ;
#25589=ORIENTED_EDGE ( 'NONE', *, *, #46548, .F. ) ;
#25590=AXIS2_PLACEMENT_3D ( 'NONE', #58914, #41721, #10390 ) ;
#25592=AXIS2_PLACEMENT_3D ( 'NONE', #13937, #45648, #67399 ) ;
#25593=DIRECTION ( 'NONE',  ( 1.000000000000000000, 0.000000000000000000, 0.000000000000000000 ) ) ;
#25595=CARTESIAN_POINT ( 'NONE',  ( 0.000000000000000000, 115.0570736234661666, -8.025000000000000355 ) ) ;
#25597=FACE_OUTER_BOUND ( 'NONE', #66802, .T. ) ;
#25600=LINE ( 'NONE', #35135, #54923 ) ;
#25603=CARTESIAN_POINT ( 'NONE',  ( 48.00000000000000000, 14.49137674618942562, -9.500000000000000000 ) ) ;
#25605=CARTESIAN_POINT ( 'NONE',  ( 71.62068965517239860, 36.41396814395972115, -7.500000000000000000 ) ) ;
#25606=CARTESIAN_POINT ( 'NONE',  ( 0.000000000000000000, 118.0570736234661524, -8.025000000000000355 ) ) ;
#25611=CARTESIAN_POINT ( 'NONE',  ( -75.31874094084331261, 36.08947156080473206, -9.789663200461481196 ) ) ;
#25612=MECHANICAL_DESIGN_GEOMETRIC_PRESENTATION_REPRESENTATION('',(#6437),#17766);
#25614=CARTESIAN_POINT ( 'NONE',  ( -9.058813317711338797, 126.4549999999999841, 2.943386871421373563 ) ) ;
#25616=CARTESIAN_POINT ( 'NONE',  ( -15.48999599679679662, 118.4999999999999716, -7.500000000000000000 ) ) ;
#25620=( LENGTH_UNIT ( ) NAMED_UNIT ( * ) SI_UNIT ( .MILLI., .METRE. ) );
#25625=CARTESIAN_POINT ( 'NONE',  ( -9.827790563157511022E-16, 146.5570736234661524, 8.025000000000000355 ) ) ;
#25626=EDGE_CURVE ( 'NONE', #5088, #52924, #67660, .T. ) ;
#25627=ADVANCED_FACE ( 'NONE', ( #50441 ), #51147, .T. ) ;
#25630=ORIENTED_EDGE ( 'NONE', *, *, #52972, .F. ) ;
#25637=CARTESIAN_POINT ( 'NONE',  ( -71.99999999999998579, 64.07124727947029896, -7.500000000000000000 ) ) ;
#25639=SURFACE_STYLE_FILL_AREA ( #56974 ) ;
#25640=MECHANICAL_DESIGN_GEOMETRIC_PRESENTATION_REPRESENTATION('',(#49277),#35762);
#25651=AXIS2_PLACEMENT_3D ( 'NONE', #42399, #68387, #36426 ) ;
#25653=CARTESIAN_POINT ( 'NONE',  ( -8.102448949553181734, 149.4949999999999761, 5.886773742842747126 ) ) ;
#25654=( LENGTH_UNIT ( ) NAMED_UNIT ( * ) SI_UNIT ( .MILLI., .METRE. ) );
#25655=COLOUR_RGB ( '', 0.72549020, 0.75294118, 0.79215686) ;
#25657=PRESENTATION_STYLE_ASSIGNMENT (( #20393 ) ) ;
#25658=CARTESIAN_POINT ( 'NONE',  ( 3.094860106618431583, 145.2049999999999557, 9.525000000000000355 ) ) ;
#25660=DIRECTION ( 'NONE',  ( -0.000000000000000000, -0.000000000000000000, 1.000000000000000000 ) ) ;
#25661=VERTEX_POINT ( 'NONE', #51842 ) ;
#25662=CARTESIAN_POINT ( 'NONE',  ( -4.716976649647098618, 127.1429263765338220, 6.492361379858953008 ) ) ;
#25664=UNCERTAINTY_MEASURE_WITH_UNIT (LENGTH_MEASURE( 1.000000000000000082E-05 ), #46318, 'distance_accuracy_value', 'NONE');
#25667=CARTESIAN_POINT ( 'NONE',  ( 45.64107345563336793, 10.15688972729204487, 6.260993343996500649 ) ) ;
#25670=VERTEX_POINT ( 'NONE', #25774 ) ;
#25674=VERTEX_POINT ( 'NONE', #58157 ) ;
#25679=( LENGTH_UNIT ( ) NAMED_UNIT ( * ) SI_UNIT ( .MILLI., .METRE. ) );
#25681=EDGE_LOOP ( 'NONE', ( #28666, #39370, #65975, #68071, #37750, #6303, #16039 ) ) ;
#25686=SURFACE_SIDE_STYLE ('',( #57022 ) ) ;
#25691=AXIS2_PLACEMENT_3D ( 'NONE', #44934, #33640, #45283 ) ;
#25694=CARTESIAN_POINT ( 'NONE',  ( -75.00000000000000000, 8.092291901769643303, -5.807866024088082391 ) ) ;
#25698=CARTESIAN_POINT ( 'NONE',  ( 44.99999999999999289, 10.00000000000000533, 4.000000000000000000 ) ) ;
#25699=CARTESIAN_POINT ( 'NONE',  ( -9.827790563157511022E-16, 125.5570736234661524, 8.025000000000000355 ) ) ;
#25700=CARTESIAN_POINT ( 'NONE',  ( 5.598654528085805993, 144.2449999999999761, 7.705886871421374629 ) ) ;
#25702=FILL_AREA_STYLE_COLOUR ( '', #3766 ) ;
#25709=LINE ( 'NONE', #47944, #62421 ) ;
#25711=CIRCLE ( 'NONE', #48214, 0.5000000000000004441 ) ;
#25714=DIRECTION ( 'NONE',  ( 0.000000000000000000, 1.000000000000000000, -0.000000000000000000 ) ) ;
#25715=FILL_AREA_STYLE ('',( #69006 ) ) ;
#25717=ORIENTED_EDGE ( 'NONE', *, *, #13993, .F. ) ;
#25722=AXIS2_PLACEMENT_3D ( 'NONE', #68904, #15785, #47120 ) ;
#25724=CARTESIAN_POINT ( 'NONE',  ( -45.90428468476780210, 9.387774908331767421, 6.120769290545535313 ) ) ;
#25728=AXIS2_PLACEMENT_3D ( 'NONE', #28346, #61406, #13222 ) ;
#25733=DIRECTION ( 'NONE',  ( 0.000000000000000000, 1.000000000000000000, 0.000000000000000000 ) ) ;
#25734=ORIENTED_EDGE ( 'NONE', *, *, #1933, .T. ) ;
#25737=AXIS2_PLACEMENT_3D ( 'NONE', #48057, #25848, #30411 ) ;
#25740=CARTESIAN_POINT ( 'NONE',  ( -5.598654528085808657, 119.6449999999999818, 7.705886871421373741 ) ) ;
#25741=( GEOMETRIC_REPRESENTATION_CONTEXT ( 3 ) GLOBAL_UNCERTAINTY_ASSIGNED_CONTEXT ( ( #54581 ) ) GLOBAL_UNIT_ASSIGNED_CONTEXT ( ( #12438, #17423, #1843 ) ) REPRESENTATION_CONTEXT ( 'NONE', 'WORKASPACE' ) );
#25744=CARTESIAN_POINT ( 'NONE',  ( 3.094860106618435136, 122.4049999999999727, -9.525000000000000355 ) ) ;
#25749=CARTESIAN_POINT ( 'NONE',  ( 9.058813317711337021, 136.6550000000000011, 2.943386871421375783 ) ) ;
#25750=UNCERTAINTY_MEASURE_WITH_UNIT (LENGTH_MEASURE( 1.000000000000000082E-05 ), #56227, 'distance_accuracy_value', 'NONE');
#25754=CARTESIAN_POINT ( 'NONE',  ( -41.11302593432306196, 107.5810679765800444, 3.326249178529583350 ) ) ;
#25758=CARTESIAN_POINT ( 'NONE',  ( -51.50000000000000000, -2.024042244987997205E-14, 10.00000000000000000 ) ) ;
#25759=DIRECTION ( 'NONE',  ( 1.156482317317873451E-16, 1.000000000000000000, -0.000000000000000000 ) ) ;
#25761=ORIENTED_EDGE ( 'NONE', *, *, #68873, .T. ) ;
#25762=CARTESIAN_POINT ( 'NONE',  ( 7.398101581744993993, 111.6353782664878764, -3.965660541892887636 ) ) ;
#25764=SURFACE_STYLE_FILL_AREA ( #20502 ) ;
#25765=FACE_OUTER_BOUND ( 'NONE', #35642, .T. ) ;
#25767=DIRECTION ( 'NONE',  ( 0.000000000000000000, 0.000000000000000000, 1.000000000000000000 ) ) ;
#25770=VECTOR ( 'NONE', #42121, 1000.000000000000000 ) ;
#25773=ORIENTED_EDGE ( 'NONE', *, *, #16727, .F. ) ;
#25774=CARTESIAN_POINT ( 'NONE',  ( -75.00000000000000000, 33.00000000000000000, -6.500000000000000000 ) ) ;
#25775=( NAMED_UNIT ( * ) SI_UNIT ( $, .STERADIAN. ) SOLID_ANGLE_UNIT ( ) );
#25778=AXIS2_PLACEMENT_3D ( 'NONE', #34338, #55786, #7595 ) ;
#25780=CARTESIAN_POINT ( 'NONE',  ( 10.01517768586949408, 147.6949999999999932, 1.839758294383810543E-15 ) ) ;
#25785=ORIENTED_EDGE ( 'NONE', *, *, #11098, .F. ) ;
#25786=CARTESIAN_POINT ( 'NONE',  ( -34.99999999999992895, 109.9999999999999858, -9.500000000000000000 ) ) ;
#25791=CARTESIAN_POINT ( 'NONE',  ( 3.094860106618431583, 117.0949999999999989, 9.525000000000000355 ) ) ;
#25794=STYLED_ITEM ( 'NONE', ( #50398 ), #33954 ) ;
#25795=COLOUR_RGB ( '', 0.66274510, 0.83137255, 0.94901961) ;
#25797=FILL_AREA_STYLE_COLOUR ( '', #7637 ) ;
#25804=EDGE_CURVE ( 'NONE', #40233, #6517, #50829, .T. ) ;
#25812=EDGE_CURVE ( 'NONE', #20191, #13722, #58839, .T. ) ;
#25816=EDGE_CURVE ( 'NONE', #43736, #53241, #47513, .T. ) ;
#25821=ORIENTED_EDGE ( 'NONE', *, *, #16246, .F. ) ;
#25823=MECHANICAL_DESIGN_GEOMETRIC_PRESENTATION_REPRESENTATION('',(#46103),#55038);
#25824=DIRECTION ( 'NONE',  ( -0.000000000000000000, -0.000000000000000000, 1.000000000000000000 ) ) ;
#25825=CARTESIAN_POINT ( 'NONE',  ( -4.716976649647097730, 145.3570736234661638, -6.492361379858953896 ) ) ;
#25826=ORIENTED_EDGE ( 'NONE', *, *, #30630, .T. ) ;
#25830=UNCERTAINTY_MEASURE_WITH_UNIT (LENGTH_MEASURE( 1.000000000000000082E-05 ), #3612, 'distance_accuracy_value', 'NONE');
#25834=DIRECTION ( 'NONE',  ( -0.6216216216216311485, -0.7833176619561784682, 0.000000000000000000 ) ) ;
#25841=EDGE_CURVE ( 'NONE', #25004, #29393, #21549, .T. ) ;
#25846=VECTOR ( 'NONE', #25714, 1000.000000000000000 ) ;
#25848=DIRECTION ( 'NONE',  ( -0.000000000000000000, -1.000000000000000000, -0.000000000000000000 ) ) ;
#25850=DIRECTION ( 'NONE',  ( 1.000000000000000000, 9.251858538542971828E-16, 0.000000000000000000 ) ) ;
#25851=CARTESIAN_POINT ( 'NONE',  ( -15.98999599679679839, 118.4999999999999716, -7.500000000000000000 ) ) ;
#25852=ORIENTED_EDGE ( 'NONE', *, *, #46548, .T. ) ;
#25859=( GEOMETRIC_REPRESENTATION_CONTEXT ( 3 ) GLOBAL_UNCERTAINTY_ASSIGNED_CONTEXT ( ( #62925 ) ) GLOBAL_UNIT_ASSIGNED_CONTEXT ( ( #18196, #17857, #33341 ) ) REPRESENTATION_CONTEXT ( 'NONE', 'WORKASPACE' ) );
#25860=CARTESIAN_POINT ( 'NONE',  ( -9.058813317711338797, 119.3449999999999989, 2.943386871421373563 ) ) ;
#25862=ORIENTED_EDGE ( 'NONE', *, *, #29960, .F. ) ;
#25863=AXIS2_PLACEMENT_3D ( 'NONE', #68129, #40351, #41409 ) ;
#25864=CARTESIAN_POINT ( 'NONE',  ( -12.34222745343792127, 114.9999999999999574, 10.18181818181818166 ) ) ;
#25865=DIRECTION ( 'NONE',  ( -0.000000000000000000, -1.000000000000000000, -0.000000000000000000 ) ) ;
#25867=CARTESIAN_POINT ( 'NONE',  ( 15.48999599679679662, 117.9999999999999716, -7.500000000000000000 ) ) ;
#25872=CIRCLE ( 'NONE', #38282, 18.50000000000000355 ) ;
#25875=AXIS2_PLACEMENT_3D ( 'NONE', #37279, #215, #47858 ) ;
#25876=EDGE_CURVE ( 'NONE', #12107, #9513, #60941, .T. ) ;
#25877=DIRECTION ( 'NONE',  ( 1.000000000000000000, 0.000000000000000000, 0.000000000000000000 ) ) ;
#25878=CIRCLE ( 'NONE', #61980, 23.00000000000000000 ) ;
#25880=LINE ( 'NONE', #67773, #13509 ) ;
#25881=ADVANCED_FACE ( 'NONE', ( #23285 ), #45810, .F. ) ;
#25882=CARTESIAN_POINT ( 'NONE',  ( 9.058813317711337021, 151.6549999999999727, 2.943386871421375783 ) ) ;
#25884=CIRCLE ( 'NONE', #65201, 8.000000000000000000 ) ;
#25885=STYLED_ITEM ( 'NONE', ( #4848 ), #11468 ) ;
#25892=EDGE_CURVE ( 'NONE', #44595, #43189, #33992, .T. ) ;
#25895=CARTESIAN_POINT ( 'NONE',  ( 0.000000000000000000, 114.9999999999999574, 0.000000000000000000 ) ) ;
#25901=PRODUCT_DEFINITION_FORMATION_WITH_SPECIFIED_SOURCE ( 'ANY', '', #47375, .NOT_KNOWN. ) ;
#25910=CARTESIAN_POINT ( 'NONE',  ( -3.094860106618434248, 120.9049999999999869, 9.525000000000000355 ) ) ;
#25918=SURFACE_STYLE_USAGE ( .BOTH. , #37927 ) ;
#25919=ORIENTED_EDGE ( 'NONE', *, *, #53695, .T. ) ;
#25920=CARTESIAN_POINT ( 'NONE',  ( -9.827790563157511022E-16, 154.4429263765338192, 8.025000000000000355 ) ) ;
#25923=DIRECTION ( 'NONE',  ( 0.000000000000000000, 0.000000000000000000, -1.000000000000000000 ) ) ;
#25924=ORIENTED_EDGE ( 'NONE', *, *, #67353, .T. ) ;
#25925=CIRCLE ( 'NONE', #55146, 0.5000000000000004441 ) ;
#25926=CARTESIAN_POINT ( 'NONE',  ( 20.58979310427664444, 114.8389001175783051, -9.999999999999879208 ) ) ;
#25927=VERTEX_POINT ( 'NONE', #45126 ) ;
#25928=PRESENTATION_STYLE_ASSIGNMENT (( #63236 ) ) ;
#25930=FACE_OUTER_BOUND ( 'NONE', #27556, .T. ) ;
#25931=FACE_OUTER_BOUND ( 'NONE', #15188, .T. ) ;
#25935=AXIS2_PLACEMENT_3D ( 'NONE', #51962, #9754, #19586 ) ;
#25936=CARTESIAN_POINT ( 'NONE',  ( -4.716976649647097730, 120.2429263765338163, -6.492361379858953896 ) ) ;
#25937=DIRECTION ( 'NONE',  ( 0.000000000000000000, 0.000000000000000000, 1.000000000000000000 ) ) ;
#25940=DIRECTION ( 'NONE',  ( -1.000000000000000000, 0.000000000000000000, 0.000000000000000000 ) ) ;
#25941=SURFACE_STYLE_FILL_AREA ( #30518 ) ;
#25943=DIRECTION ( 'NONE',  ( -0.000000000000000000, -1.000000000000000000, -0.000000000000000000 ) ) ;
#25945=FILL_AREA_STYLE ('',( #4130 ) ) ;
#25957=DIRECTION ( 'NONE',  ( 1.000000000000000000, 0.000000000000000000, 0.000000000000000000 ) ) ;
#25958=VECTOR ( 'NONE', #69636, 1000.000000000000000 ) ;
#25959=EDGE_CURVE ( 'NONE', #22693, #19997, #12358, .T. ) ;
#25961=CARTESIAN_POINT ( 'NONE',  ( 9.058813317711338797, 127.9549999999999841, -2.943386871421372675 ) ) ;
#25964=DIRECTION ( 'NONE',  ( 0.000000000000000000, 1.000000000000000000, 0.000000000000000000 ) ) ;
#25967=EDGE_CURVE ( 'NONE', #28083, #12316, #50367, .T. ) ;
#25969=DIRECTION ( 'NONE',  ( 0.000000000000000000, 0.000000000000000000, -1.000000000000000000 ) ) ;
#25970=( NAMED_UNIT ( * ) SI_UNIT ( $, .STERADIAN. ) SOLID_ANGLE_UNIT ( ) );
#25971=VECTOR ( 'NONE', #60683, 1000.000000000000000 ) ;
#25976=( GEOMETRIC_REPRESENTATION_CONTEXT ( 3 ) GLOBAL_UNCERTAINTY_ASSIGNED_CONTEXT ( ( #34178 ) ) GLOBAL_UNIT_ASSIGNED_CONTEXT ( ( #19106, #30022, #46248 ) ) REPRESENTATION_CONTEXT ( 'NONE', 'WORKASPACE' ) );
#25977=EDGE_CURVE ( 'NONE', #28945, #44738, #66590, .T. ) ;
#25978=CARTESIAN_POINT ( 'NONE',  ( -40.99999999999997868, 10.49999999999998401, 3.500000000000000000 ) ) ;
#25980=CARTESIAN_POINT ( 'NONE',  ( 71.99999999999998579, 64.07124727947029896, 7.500000000000000000 ) ) ;
#25982=ORIENTED_EDGE ( 'NONE', *, *, #54155, .F. ) ;
#25983=DIRECTION ( 'NONE',  ( 1.000000000000000000, 0.000000000000000000, 0.000000000000000000 ) ) ;
#25984=VECTOR ( 'NONE', #63806, 1000.000000000000000 ) ;
#25986=VECTOR ( 'NONE', #24492, 1000.000000000000000 ) ;
#25988=( GEOMETRIC_REPRESENTATION_CONTEXT ( 3 ) GLOBAL_UNCERTAINTY_ASSIGNED_CONTEXT ( ( #57391 ) ) GLOBAL_UNIT_ASSIGNED_CONTEXT ( ( #33937, #12474, #49791 ) ) REPRESENTATION_CONTEXT ( 'NONE', 'WORKASPACE' ) );
#25989=PRESENTATION_STYLE_ASSIGNMENT (( #36944 ) ) ;
#25991=EDGE_LOOP ( 'NONE', ( #59750, #24231, #45119, #6738, #4533, #44812, #62250, #51024, #10631, #8313, #25419, #28561, #63334 ) ) ;
#25993=ORIENTED_EDGE ( 'NONE', *, *, #6076, .F. ) ;
#25994=CARTESIAN_POINT ( 'NONE',  ( 34.99999999999999289, 99.99999999999997158, 10.00000000000000000 ) ) ;
#25995=CARTESIAN_POINT ( 'NONE',  ( 2.607480562269093305, 128.7070736234661865, 8.024999999999986144 ) ) ;
#25997=CARTESIAN_POINT ( 'NONE',  ( 23.21231517720797655, 117.4999999999999716, 9.500000000000000000 ) ) ;
#25998=EDGE_LOOP ( 'NONE', ( #15108, #15862, #61465, #6018 ) ) ;
#26000=CARTESIAN_POINT ( 'NONE',  ( 8.102448949553181734, 147.3950000000000102, 5.886773742842750679 ) ) ;
#26003=VERTEX_POINT ( 'NONE', #47210 ) ;
#26004=VECTOR ( 'NONE', #20321, 1000.000000000000000 ) ;
#26005=CARTESIAN_POINT ( 'NONE',  ( 3.094860106618431583, 154.2049999999999272, 9.525000000000000355 ) ) ;
#26006=( NAMED_UNIT ( * ) SI_UNIT ( $, .STERADIAN. ) SOLID_ANGLE_UNIT ( ) );
#26007=CARTESIAN_POINT ( 'NONE',  ( 48.00000000000000000, 99.99999999999992895, -9.500000000000000000 ) ) ;
#26008=ORIENTED_EDGE ( 'NONE', *, *, #43959, .F. ) ;
#26009=CARTESIAN_POINT ( 'NONE',  ( -2.607480562269073765, 129.0929263765338249, -8.025000000000000355 ) ) ;
#26012=DIRECTION ( 'NONE',  ( -1.000000000000000000, 0.000000000000000000, 0.000000000000000000 ) ) ;
#26013=DIRECTION ( 'NONE',  ( 0.6842105263157866046, -0.7292845505553195995, 0.000000000000000000 ) ) ;
#26015=DIRECTION ( 'NONE',  ( -0.000000000000000000, 1.000000000000000000, -0.000000000000000000 ) ) ;
#26019=STYLED_ITEM ( 'NONE', ( #41869 ), #60505 ) ;
#26021=EDGE_LOOP ( 'NONE', ( #28858, #44502, #55637, #48906 ) ) ;
#26025=CARTESIAN_POINT ( 'NONE',  ( 74.99999999999998579, 19.84496280275742564, 6.370902851337289619 ) ) ;
#26028=ORIENTED_EDGE ( 'NONE', *, *, #5783, .F. ) ;
#26039=EDGE_CURVE ( 'NONE', #14945, #58906, #50877, .T. ) ;
#26041=DIRECTION ( 'NONE',  ( -1.000000000000000000, 0.000000000000000000, -0.000000000000000000 ) ) ;
#26042=ORIENTED_EDGE ( 'NONE', *, *, #58964, .T. ) ;
#26043=ADVANCED_FACE ( 'NONE', ( #67950 ), #12703, .F. ) ;
#26052=CIRCLE ( 'NONE', #65375, 4.999999999999997335 ) ;
#26054=CARTESIAN_POINT ( 'NONE',  ( -9.058813317711337021, 149.0449999999999875, -2.943386871421374895 ) ) ;
#26062=EDGE_CURVE ( 'NONE', #24423, #51540, #2566, .T. ) ;
#26066=DIRECTION ( 'NONE',  ( 0.000000000000000000, 0.000000000000000000, -1.000000000000000000 ) ) ;
#26070=VERTEX_POINT ( 'NONE', #19734 ) ;
#26071=SURFACE_SIDE_STYLE ('',( #16262 ) ) ;
#26074=CARTESIAN_POINT ( 'NONE',  ( -7.632228543268607446, 117.5429263765338135, -2.479861379858953718 ) ) ;
#26075=CARTESIAN_POINT ( 'NONE',  ( -45.00000000000000000, 9.291225313367151628, 6.640072787442719005 ) ) ;
#26077=CIRCLE ( 'NONE', #31706, 1.000000000000000888 ) ;
#26079=EDGE_LOOP ( 'NONE', ( #33140, #46948, #9227, #2724 ) ) ;
#26081=EDGE_LOOP ( 'NONE', ( #37356, #35701, #57336 ) ) ;
#26084=ORIENTED_EDGE ( 'NONE', *, *, #11167, .T. ) ;
#26085=AXIS2_PLACEMENT_3D ( 'NONE', #35463, #31187, #4100 ) ;
#26087=CARTESIAN_POINT ( 'NONE',  ( 5.598654528085805993, 120.2449999999999903, 7.705886871421374629 ) ) ;
#26093=CARTESIAN_POINT ( 'NONE',  ( -9.058813317711338797, 120.4549999999999983, 2.943386871421373563 ) ) ;
#26097=CARTESIAN_POINT ( 'NONE',  ( 3.094860106618435136, 149.4049999999999443, -9.525000000000000355 ) ) ;
#26099=CARTESIAN_POINT ( 'NONE',  ( -41.45364736693642982, 107.0151787721003842, 3.500000000000000444 ) ) ;
#26100=( GEOMETRIC_REPRESENTATION_CONTEXT ( 3 ) GLOBAL_UNCERTAINTY_ASSIGNED_CONTEXT ( ( #3178 ) ) GLOBAL_UNIT_ASSIGNED_CONTEXT ( ( #48494, #12179, #37948 ) ) REPRESENTATION_CONTEXT ( 'NONE', 'WORKASPACE' ) );
#26101=SPHERICAL_SURFACE ( 'NONE', #22792, 0.5000000000000000000 ) ;
#26104=CYLINDRICAL_SURFACE ( 'NONE', #64354, 5.000000000000004441 ) ;
#26107=CARTESIAN_POINT ( 'NONE',  ( 5.461490429277590763, 111.1023334488693735, 7.076668351203547758 ) ) ;
#26108=CARTESIAN_POINT ( 'NONE',  ( -60.00000000000000000, -2.024042244987997205E-14, -11.50000000000000000 ) ) ;
#26110=DIRECTION ( 'NONE',  ( 0.000000000000000000, 0.000000000000000000, 1.000000000000000000 ) ) ;
#26111=CARTESIAN_POINT ( 'NONE',  ( -40.99999999999997868, 10.49999999999998224, -3.000000000000000444 ) ) ;
#26112=VERTEX_POINT ( 'NONE', #20790 ) ;
#26115=ADVANCED_FACE ( 'NONE', ( #62629 ), #46879, .F. ) ;
#26116=FILL_AREA_STYLE_COLOUR ( '', #60575 ) ;
#26123=STYLED_ITEM ( 'NONE', ( #7098 ), #47136 ) ;
#26124=( GEOMETRIC_REPRESENTATION_CONTEXT ( 3 ) GLOBAL_UNCERTAINTY_ASSIGNED_CONTEXT ( ( #46811 ) ) GLOBAL_UNIT_ASSIGNED_CONTEXT ( ( #27617, #12845, #66671 ) ) REPRESENTATION_CONTEXT ( 'NONE', 'WORKASPACE' ) );
#26125=CARTESIAN_POINT ( 'NONE',  ( 10.01517768586949408, 150.6949999999999648, 1.839758294383810543E-15 ) ) ;
#26128=CARTESIAN_POINT ( 'NONE',  ( 34.99999999999999289, 99.99999999999998579, -9.500000000000000000 ) ) ;
#26130=DIRECTION ( 'NONE',  ( 0.000000000000000000, 0.000000000000000000, 1.000000000000000000 ) ) ;
#26131=( NAMED_UNIT ( * ) SI_UNIT ( $, .STERADIAN. ) SOLID_ANGLE_UNIT ( ) );
#26132=PRESENTATION_STYLE_ASSIGNMENT (( #14921 ) ) ;
#26133=FILL_AREA_STYLE_COLOUR ( '', #47152 ) ;
#26136=CARTESIAN_POINT ( 'NONE',  ( -1.166476076187854022E-15, 116.9449999999999932, 9.525000000000000355 ) ) ;
#26138=EDGE_CURVE ( 'NONE', #44039, #2827, #46450, .T. ) ;
#26141=AXIS2_PLACEMENT_3D ( 'NONE', #10977, #54224, #69384 ) ;
#26142=FILL_AREA_STYLE ('',( #25797 ) ) ;
#26144=EDGE_CURVE ( 'NONE', #8462, #58922, #11252, .T. ) ;
#26146=CARTESIAN_POINT ( 'NONE',  ( -71.62068965517239860, 36.41396814395972115, 7.500000000000000000 ) ) ;
#26148=( GEOMETRIC_REPRESENTATION_CONTEXT ( 3 ) GLOBAL_UNCERTAINTY_ASSIGNED_CONTEXT ( ( #51606 ) ) GLOBAL_UNIT_ASSIGNED_CONTEXT ( ( #11068, #467, #37170 ) ) REPRESENTATION_CONTEXT ( 'NONE', 'WORKASPACE' ) );
#26150=LINE ( 'NONE', #9998, #64970 ) ;
#26152=VERTEX_POINT ( 'NONE', #37351 ) ;
#26158=( NAMED_UNIT ( * ) SI_UNIT ( $, .STERADIAN. ) SOLID_ANGLE_UNIT ( ) );
#26161=EDGE_LOOP ( 'NONE', ( #9450, #40057, #52442, #19339 ) ) ;
#26165=ORIENTED_EDGE ( 'NONE', *, *, #53376, .F. ) ;
#26167=AXIS2_PLACEMENT_3D ( 'NONE', #15320, #32472, #32844 ) ;
#26169=CARTESIAN_POINT ( 'NONE',  ( 6.826472737025119919, 147.0070736234661695, 4.959722759717908325 ) ) ;
#26171=AXIS2_PLACEMENT_3D ( 'NONE', #31899, #55355, #23342 ) ;
#26176=VERTEX_POINT ( 'NONE', #5608 ) ;
#26177=( NAMED_UNIT ( * ) PLANE_ANGLE_UNIT ( ) SI_UNIT ( $, .RADIAN. ) );
#26182=CIRCLE ( 'NONE', #7119, 14.49999999999999822 ) ;
#26184=ORIENTED_EDGE ( 'NONE', *, *, #51315, .F. ) ;
#26188=FILL_AREA_STYLE_COLOUR ( '', #44735 ) ;
#26192=LINE ( 'NONE', #3669, #39285 ) ;
#26194=( GEOMETRIC_REPRESENTATION_CONTEXT ( 3 ) GLOBAL_UNCERTAINTY_ASSIGNED_CONTEXT ( ( #5340 ) ) GLOBAL_UNIT_ASSIGNED_CONTEXT ( ( #45102, #66149, #28142 ) ) REPRESENTATION_CONTEXT ( 'NONE', 'WORKASPACE' ) );
#26196=( NAMED_UNIT ( * ) PLANE_ANGLE_UNIT ( ) SI_UNIT ( $, .RADIAN. ) );
#26200=DIRECTION ( 'NONE',  ( 1.000000000000000000, 0.000000000000000000, 0.000000000000000000 ) ) ;
#26201=ORIENTED_EDGE ( 'NONE', *, *, #4506, .T. ) ;
#26204=LINE ( 'NONE', #52285, #56894 ) ;
#26206=CARTESIAN_POINT ( 'NONE',  ( -5.598654528085808657, 125.6449999999999818, 7.705886871421373741 ) ) ;
#26212=FACE_OUTER_BOUND ( 'NONE', #36456, .T. ) ;
#26215=CARTESIAN_POINT ( 'NONE',  ( 0.000000000000000000, 130.0570736234661524, -8.025000000000000355 ) ) ;
#26217=CARTESIAN_POINT ( 'NONE',  ( -74.99999999999998579, 50.00000000000000000, 7.000000000000000000 ) ) ;
#26220=( GEOMETRIC_REPRESENTATION_CONTEXT ( 3 ) GLOBAL_UNCERTAINTY_ASSIGNED_CONTEXT ( ( #26892 ) ) GLOBAL_UNIT_ASSIGNED_CONTEXT ( ( #67394, #2973, #33993 ) ) REPRESENTATION_CONTEXT ( 'NONE', 'WORKASPACE' ) );
#26222=AXIS2_PLACEMENT_3D ( 'NONE', #22649, #12076, #17052 ) ;
#26225=CARTESIAN_POINT ( 'NONE',  ( 44.15219150100328704, 9.717397167001077918, -3.137420992959917054 ) ) ;
#26228=MECHANICAL_DESIGN_GEOMETRIC_PRESENTATION_REPRESENTATION('',(#17288),#4969);
#26229=DIRECTION ( 'NONE',  ( -1.000000000000000000, 0.000000000000000000, 0.000000000000000000 ) ) ;
#26232=SURFACE_STYLE_USAGE ( .BOTH. , #5803 ) ;
#26235=( NAMED_UNIT ( * ) SI_UNIT ( $, .STERADIAN. ) SOLID_ANGLE_UNIT ( ) );
#26236=COLOUR_RGB ( '', 0.40784314, 0.44705882, 0.49803922) ;
#26237=FACE_OUTER_BOUND ( 'NONE', #57193, .T. ) ;
#26239=UNCERTAINTY_MEASURE_WITH_UNIT (LENGTH_MEASURE( 1.000000000000000082E-05 ), #43170, 'distance_accuracy_value', 'NONE');
#26243=COLOUR_RGB ( '', 0.09019608, 0.27058824, 0.51372549) ;
#26247=CIRCLE ( 'NONE', #18388, 0.5000000000000004441 ) ;
#26251=EDGE_LOOP ( 'NONE', ( #39152, #23759, #20583, #19355 ) ) ;
#26252=CARTESIAN_POINT ( 'NONE',  ( 7.632228543268607446, 111.1570736234661609, 2.479861379858954606 ) ) ;
#26256=( LENGTH_UNIT ( ) NAMED_UNIT ( * ) SI_UNIT ( .MILLI., .METRE. ) );
#26262=VERTEX_POINT ( 'NONE', #37702 ) ;
#26263=CARTESIAN_POINT ( 'NONE',  ( -10.01517768586949231, 120.3049999999999784, -6.132527647946036459E-16 ) ) ;
#26265=CARTESIAN_POINT ( 'NONE',  ( 45.00000000000000000, 10.69371294336137623, 6.585786437626905077 ) ) ;
#26266=( GEOMETRIC_REPRESENTATION_CONTEXT ( 3 ) GLOBAL_UNCERTAINTY_ASSIGNED_CONTEXT ( ( #4504 ) ) GLOBAL_UNIT_ASSIGNED_CONTEXT ( ( #53360, #16449, #38603 ) ) REPRESENTATION_CONTEXT ( 'NONE', 'WORKASPACE' ) );
#26267=DIRECTION ( 'NONE',  ( 1.000000000000000000, 0.000000000000000000, 0.000000000000000000 ) ) ;
#26269=EDGE_LOOP ( 'NONE', ( #50104, #21056, #53274, #10030 ) ) ;
#26271=ADVANCED_FACE ( 'NONE', ( #32351 ), #36359, .T. ) ;
#26273=CARTESIAN_POINT ( 'NONE',  ( -8.437984349512095861, 153.6929263765337907, -5.166775262442723748E-16 ) ) ;
#26274=DIRECTION ( 'NONE',  ( -1.099520432716498623E-15, 1.000000000000000000, 1.099520432716498623E-15 ) ) ;
#26278=ORIENTED_EDGE ( 'NONE', *, *, #55820, .F. ) ;
#26279=SURFACE_STYLE_FILL_AREA ( #35811 ) ;
#26280=DIRECTION ( 'NONE',  ( 0.000000000000000000, 1.000000000000000000, 0.000000000000000000 ) ) ;
#26281=DIRECTION ( 'NONE',  ( 1.000000000000000000, 0.000000000000000000, 0.000000000000000000 ) ) ;
#26282=( GEOMETRIC_REPRESENTATION_CONTEXT ( 3 ) GLOBAL_UNCERTAINTY_ASSIGNED_CONTEXT ( ( #352 ) ) GLOBAL_UNIT_ASSIGNED_CONTEXT ( ( #2968, #56127, #40684 ) ) REPRESENTATION_CONTEXT ( 'NONE', 'WORKASPACE' ) );
#26284=COLOUR_RGB ( '', 0.72549020, 0.75294118, 0.79215686) ;
#26285=FILL_AREA_STYLE ('',( #41462 ) ) ;
#26287=CARTESIAN_POINT ( 'NONE',  ( 20.57648123223228254, 154.9999999999999716, 10.27659574468085069 ) ) ;
#26288=DIRECTION ( 'NONE',  ( 1.000000000000000000, 0.000000000000000000, 0.000000000000000000 ) ) ;
#26290=ORIENTED_EDGE ( 'NONE', *, *, #55663, .F. ) ;
#26294=DIRECTION ( 'NONE',  ( 0.000000000000000000, 0.000000000000000000, 1.000000000000000000 ) ) ;
#26295=ORIENTED_EDGE ( 'NONE', *, *, #38092, .F. ) ;
#26297=FACE_OUTER_BOUND ( 'NONE', #57087, .T. ) ;
#26302=CYLINDRICAL_SURFACE ( 'NONE', #17863, 0.5000000000000004441 ) ;
#26310=CARTESIAN_POINT ( 'NONE',  ( 3.094860106618435136, 128.4049999999999443, -9.525000000000000355 ) ) ;
#26311=CARTESIAN_POINT ( 'NONE',  ( 20.57648123223228254, 114.4999999999999574, -10.27659574468085069 ) ) ;
#26314=ADVANCED_FACE ( 'NONE', ( #18932 ), #35157, .F. ) ;
#26315=UNCERTAINTY_MEASURE_WITH_UNIT (LENGTH_MEASURE( 1.000000000000000082E-05 ), #3529, 'distance_accuracy_value', 'NONE');
#26316=( NAMED_UNIT ( * ) PLANE_ANGLE_UNIT ( ) SI_UNIT ( $, .RADIAN. ) );
#26318=VERTEX_POINT ( 'NONE', #44699 ) ;
#26319=DIRECTION ( 'NONE',  ( 0.7071067811865352493, 0.000000000000000000, 0.7071067811865597852 ) ) ;
#26322=LINE ( 'NONE', #4878, #46547 ) ;
#26323=CARTESIAN_POINT ( 'NONE',  ( -69.99999999999998579, 50.00000000000000000, 11.50000000000003730 ) ) ;
#26324=CARTESIAN_POINT ( 'NONE',  ( -7.632228543268608334, 136.9570736234661581, 2.479861379858952830 ) ) ;
#26331=AXIS2_PLACEMENT_3D ( 'NONE', #21052, #15120, #62906 ) ;
#26332=CARTESIAN_POINT ( 'NONE',  ( -7.632228543268607446, 147.5429263765338135, -2.479861379858953718 ) ) ;
#26334=( BOUNDED_CURVE ( )  B_SPLINE_CURVE ( 2, ( #32142, #10357, #68756, #20547, #63795, #52919, #47695, #54952, #22273, #34552, #13093 ),
 .UNSPECIFIED., .F., .F. ) 
 B_SPLINE_CURVE_WITH_KNOTS ( ( 3, 2, 2, 2, 2, 3 ),
 ( 0.7352941176470586537, 0.7411764705882351034, 0.7470588235294115531, 0.7529411764705881138, 0.7588235294117645635, 0.7647058823529410132 ),
 .UNSPECIFIED. ) 
 CURVE ( )  GEOMETRIC_REPRESENTATION_ITEM ( )  RATIONAL_B_SPLINE_CURVE ( ( 1.000000000000001776, 0.9510565162951516438, 1.000000000000000000, 0.9510565162951535312, 1.000000000000000000, 0.9510565162951535312, 1.000000000000000000, 0.9510565162951535312, 1.000000000000000000, 0.9510565162951544194, 0.9999999999999991118 ) ) 
 REPRESENTATION_ITEM ( '' )  );
#26337=ORIENTED_EDGE ( 'NONE', *, *, #6896, .T. ) ;
#26339=ORIENTED_EDGE ( 'NONE', *, *, #23423, .F. ) ;
#26342=FACE_OUTER_BOUND ( 'NONE', #16851, .T. ) ;
#26343=ORIENTED_EDGE ( 'NONE', *, *, #28671, .F. ) ;
#26344=SURFACE_STYLE_FILL_AREA ( #4537 ) ;
#26348=CARTESIAN_POINT ( 'NONE',  ( 9.058813317711338797, 147.8449999999999989, -2.943386871421372675 ) ) ;
#26350=AXIS2_PLACEMENT_3D ( 'NONE', #10584, #10922, #33413 ) ;
#26354=CARTESIAN_POINT ( 'NONE',  ( 0.000000000000000000, 149.5550000000000068, -9.525000000000000355 ) ) ;
#26358=CARTESIAN_POINT ( 'NONE',  ( -4.716976649647097730, 129.2429263765338021, -6.492361379858953896 ) ) ;
#26359=LINE ( 'NONE', #47897, #26655 ) ;
#26360=UNCERTAINTY_MEASURE_WITH_UNIT (LENGTH_MEASURE( 1.000000000000000082E-05 ), #9467, 'distance_accuracy_value', 'NONE');
#26363=EDGE_CURVE ( 'NONE', #6589, #58485, #1449, .T. ) ;
#26365=ORIENTED_EDGE ( 'NONE', *, *, #25353, .F. ) ;
#26371=CARTESIAN_POINT ( 'NONE',  ( -71.50000000000000000, 14.49137674618942562, -10.00000000000000000 ) ) ;
#26374=EDGE_CURVE ( 'NONE', #52933, #25180, #39406, .T. ) ;
#26376=PRESENTATION_STYLE_ASSIGNMENT (( #32686 ) ) ;
#26377=UNCERTAINTY_MEASURE_WITH_UNIT (LENGTH_MEASURE( 1.000000000000000082E-05 ), #55393, 'distance_accuracy_value', 'NONE');
#26380=FILL_AREA_STYLE ('',( #32690 ) ) ;
#26381=CARTESIAN_POINT ( 'NONE',  ( 41.08036663239563069, 107.6296822352908009, 3.281244196345447062 ) ) ;
#26383=EDGE_LOOP ( 'NONE', ( #41916, #39582, #2533, #220, #27000 ) ) ;
#26386=DIRECTION ( 'NONE',  ( 0.000000000000000000, 0.000000000000000000, 1.000000000000000000 ) ) ;
#26388=STYLED_ITEM ( 'NONE', ( #22280 ), #38897 ) ;
#26394=SURFACE_SIDE_STYLE ('',( #32353 ) ) ;
#26395=AXIS2_PLACEMENT_3D ( 'NONE', #26516, #11732, #54637 ) ;
#26398=( NAMED_UNIT ( * ) SI_UNIT ( $, .STERADIAN. ) SOLID_ANGLE_UNIT ( ) );
#26399=CARTESIAN_POINT ( 'NONE',  ( 74.99999999999998579, 119.9999999999997584, 10.00000000000000000 ) ) ;
#26400=( LENGTH_UNIT ( ) NAMED_UNIT ( * ) SI_UNIT ( .MILLI., .METRE. ) );
#26402=CARTESIAN_POINT ( 'NONE',  ( -10.01517768586949231, 152.1949999999999932, -6.132527647946036459E-16 ) ) ;
#26405=UNCERTAINTY_MEASURE_WITH_UNIT (LENGTH_MEASURE( 1.000000000000000082E-05 ), #27549, 'distance_accuracy_value', 'NONE');
#26407=FILL_AREA_STYLE_COLOUR ( '', #21333 ) ;
#26411=CARTESIAN_POINT ( 'NONE',  ( 44.91886116991580735, 9.999999999999980460, -3.201362207699240514 ) ) ;
#26417=ORIENTED_EDGE ( 'NONE', *, *, #9856, .F. ) ;
#26420=DIRECTION ( 'NONE',  ( 0.000000000000000000, 0.000000000000000000, 1.000000000000000000 ) ) ;
#26422=CARTESIAN_POINT ( 'NONE',  ( -71.74137931034479720, 63.10081643261027295, 9.500000000000000000 ) ) ;
#26425=VERTEX_POINT ( 'NONE', #15104 ) ;
#26427=AXIS2_PLACEMENT_3D ( 'NONE', #62343, #57414, #14166 ) ;
#26429=CARTESIAN_POINT ( 'NONE',  ( -24.21231517720798010, 112.9999999999999858, -7.500000000000000000 ) ) ;
#26435=CARTESIAN_POINT ( 'NONE',  ( -5.598654528085808657, 116.6449999999999818, 7.705886871421373741 ) ) ;
#26441=FILL_AREA_STYLE_COLOUR ( '', #10606 ) ;
#26442=CARTESIAN_POINT ( 'NONE',  ( 9.058813317711338797, 124.9549999999999841, -2.943386871421372675 ) ) ;
#26446=CARTESIAN_POINT ( 'NONE',  ( -10.01517768586949231, 147.3049999999999500, -6.132527647946036459E-16 ) ) ;
#26447=UNCERTAINTY_MEASURE_WITH_UNIT (LENGTH_MEASURE( 1.000000000000000082E-05 ), #59536, 'distance_accuracy_value', 'NONE');
#26448=EDGE_CURVE ( 'NONE', #29261, #17063, #19645, .T. ) ;
#26449=CARTESIAN_POINT ( 'NONE',  ( 72.00000000000000000, 36.32520566882265456, -7.000000000000000000 ) ) ;
#26450=CARTESIAN_POINT ( 'NONE',  ( -75.00000000000000000, -2.215169945516535778E-14, 9.500000000000000000 ) ) ;
#26454=CARTESIAN_POINT ( 'NONE',  ( -15.48999599679679662, 118.4999999999999716, -7.000000000000000000 ) ) ;
#26457=CARTESIAN_POINT ( 'NONE',  ( 23.21231517720798010, 112.9999999999999858, -10.00000000000000000 ) ) ;
#26459=ADVANCED_FACE ( 'NONE', ( #20337 ), #68918, .T. ) ;
#26462=CIRCLE ( 'NONE', #18586, 0.5000000000000004441 ) ;
#26464=EDGE_CURVE ( 'NONE', #33977, #28720, #9457, .T. ) ;
#26465=( NAMED_UNIT ( * ) SI_UNIT ( $, .STERADIAN. ) SOLID_ANGLE_UNIT ( ) );
#26466=ORIENTED_EDGE ( 'NONE', *, *, #64673, .T. ) ;
#26473=CIRCLE ( 'NONE', #25317, 0.5000000000000004441 ) ;
#26476=CARTESIAN_POINT ( 'NONE',  ( 9.058813317711337021, 153.5449999999999875, 2.943386871421375783 ) ) ;
#26481=SURFACE_SIDE_STYLE ('',( #1692 ) ) ;
#26482=DIRECTION ( 'NONE',  ( -0.000000000000000000, -0.000000000000000000, 1.000000000000000000 ) ) ;
#26483=FACE_OUTER_BOUND ( 'NONE', #61782, .T. ) ;
#26485=CARTESIAN_POINT ( 'NONE',  ( 3.094860106618431583, 120.0949999999999704, 9.525000000000000355 ) ) ;
#26489=SURFACE_SIDE_STYLE ('',( #5364 ) ) ;
#26497=SURFACE_STYLE_FILL_AREA ( #37815 ) ;
#26503=( LENGTH_UNIT ( ) NAMED_UNIT ( * ) SI_UNIT ( .MILLI., .METRE. ) );
#26504=SURFACE_SIDE_STYLE ('',( #59195 ) ) ;
#26512=DIRECTION ( 'NONE',  ( -0.000000000000000000, -0.000000000000000000, 1.000000000000000000 ) ) ;
#26514=( NAMED_UNIT ( * ) PLANE_ANGLE_UNIT ( ) SI_UNIT ( $, .RADIAN. ) );
#26515=AXIS2_PLACEMENT_3D ( 'NONE', #18220, #1648, #39362 ) ;
#26516=CARTESIAN_POINT ( 'NONE',  ( 60.00000000000000000, 1.797044900979284448E-15, -6.500000000000000000 ) ) ;
#26517=CARTESIAN_POINT ( 'NONE',  ( -6.826472737025120807, 146.1070736234661354, 4.959722759717906548 ) ) ;
#26519=ORIENTED_EDGE ( 'NONE', *, *, #2960, .T. ) ;
#26522=UNCERTAINTY_MEASURE_WITH_UNIT (LENGTH_MEASURE( 1.000000000000000082E-05 ), #42779, 'distance_accuracy_value', 'NONE');
#26525=CYLINDRICAL_SURFACE ( 'NONE', #17561, 0.5000000000000004441 ) ;
#26526=AXIS2_PLACEMENT_3D ( 'NONE', #44995, #30486, #46384 ) ;
#26527=CARTESIAN_POINT ( 'NONE',  ( 2.607480562268992941, 143.7929263765338419, -8.025000000000060751 ) ) ;
#26528=DIRECTION ( 'NONE',  ( 0.000000000000000000, 0.000000000000000000, -1.000000000000000000 ) ) ;
#26531=COLOUR_RGB ( '', 0.31764706, 0.68627451, 0.89019608) ;
#26535=ORIENTED_EDGE ( 'NONE', *, *, #48945, .T. ) ;
#26537=DIRECTION ( 'NONE',  ( -0.000000000000000000, -0.000000000000000000, 1.000000000000000000 ) ) ;
#26543=ORIENTED_EDGE ( 'NONE', *, *, #46986, .F. ) ;
#26544=FILL_AREA_STYLE_COLOUR ( '', #26284 ) ;
#26546=FACE_OUTER_BOUND ( 'NONE', #60026, .T. ) ;
#26549=CARTESIAN_POINT ( 'NONE',  ( -5.598654528085808657, 122.6449999999999960, 7.705886871421373741 ) ) ;
#26554=DIRECTION ( 'NONE',  ( 1.224646799147353207E-16, 1.000000000000000000, -0.000000000000000000 ) ) ;
#26558=FACE_OUTER_BOUND ( 'NONE', #3668, .T. ) ;
#26568=SURFACE_STYLE_FILL_AREA ( #11438 ) ;
#26569=STYLED_ITEM ( 'NONE', ( #22377 ), #40225 ) ;
#26570=DIRECTION ( 'NONE',  ( 0.000000000000000000, 0.000000000000000000, 1.000000000000000000 ) ) ;
#26571=FILL_AREA_STYLE_COLOUR ( '', #24176 ) ;
#26579=CARTESIAN_POINT ( 'NONE',  ( -2.607480562269157254, 138.0929263765337680, -8.024999999999939959 ) ) ;
#26583=CARTESIAN_POINT ( 'NONE',  ( 8.437984349512095861, 111.3070736234661524, 1.550032578732817026E-15 ) ) ;
#26590=ORIENTED_EDGE ( 'NONE', *, *, #39502, .F. ) ;
#26591=STYLED_ITEM ( 'NONE', ( #25006 ), #65394 ) ;
#26596=CARTESIAN_POINT ( 'NONE',  ( 8.102448949553181734, 121.5049999999999670, 5.886773742842750679 ) ) ;
#26597=SURFACE_STYLE_FILL_AREA ( #42170 ) ;
#26600=ADVANCED_FACE ( 'NONE', ( #32271 ), #55433, .F. ) ;
#26603=VERTEX_POINT ( 'NONE', #36906 ) ;
#26604=CARTESIAN_POINT ( 'NONE',  ( 7.971717394532119805, 153.6808681617074228, -3.522481101206686560 ) ) ;
#26605=DIRECTION ( 'NONE',  ( -0.000000000000000000, -0.000000000000000000, -1.000000000000000000 ) ) ;
#26608=CARTESIAN_POINT ( 'NONE',  ( -6.826472737025120807, 159.3929263765338362, -4.959722759717907437 ) ) ;
#26609=( LENGTH_UNIT ( ) NAMED_UNIT ( * ) SI_UNIT ( .MILLI., .METRE. ) );
#26611=SURFACE_STYLE_USAGE ( .BOTH. , #48131 ) ;
#26612=CARTESIAN_POINT ( 'NONE',  ( 20.99026508940074010, 114.7786387612191703, -10.00000000000000000 ) ) ;
#26613=VERTEX_POINT ( 'NONE', #15778 ) ;
#26614=DIRECTION ( 'NONE',  ( 0.000000000000000000, -1.000000000000000000, 0.000000000000000000 ) ) ;
#26619=DIRECTION ( 'NONE',  ( 0.000000000000000000, 1.000000000000000000, -0.000000000000000000 ) ) ;
#26620=CARTESIAN_POINT ( 'NONE',  ( 2.607480562269034241, 116.7929263765338135, -8.025000000000032330 ) ) ;
#26621=CARTESIAN_POINT ( 'NONE',  ( -8.154247983011970291, 153.6870150848094170, 3.079081823141356367 ) ) ;
#26626=CARTESIAN_POINT ( 'NONE',  ( -74.99999999999998579, 50.00000000000000000, -12.00000000000000000 ) ) ;
#26627=DIRECTION ( 'NONE',  ( -0.000000000000000000, -0.000000000000000000, -1.000000000000000000 ) ) ;
#26630=SURFACE_STYLE_USAGE ( .BOTH. , #48153 ) ;
#26641=CARTESIAN_POINT ( 'NONE',  ( -75.47338799120147712, 36.01293665759187235, -9.580134848782680734 ) ) ;
#26645=CARTESIAN_POINT ( 'NONE',  ( -10.01517768586949231, 138.3049999999999500, -6.132527647946036459E-16 ) ) ;
#26646=STYLED_ITEM ( 'NONE', ( #67930 ), #3751 ) ;
#26651=EDGE_CURVE ( 'NONE', #12948, #35810, #17271, .T. ) ;
#26653=COLOUR_RGB ( '', 0.08235294, 0.09019608, 0.10196078) ;
#26655=VECTOR ( 'NONE', #42589, 1000.000000000000000 ) ;
#26656=ADVANCED_FACE ( 'NONE', ( #26297 ), #66689, .T. ) ;
#26663=CARTESIAN_POINT ( 'NONE',  ( -71.49999999999998579, 64.07124727947029896, -9.500000000000000000 ) ) ;
#26666=CARTESIAN_POINT ( 'NONE',  ( 60.00000000000000000, 117.4999999999999716, -9.500000000000000000 ) ) ;
#26671=ORIENTED_EDGE ( 'NONE', *, *, #51536, .T. ) ;
#26673=CARTESIAN_POINT ( 'NONE',  ( 20.77811424250900174, 115.1386898118646656, -10.00000000000000000 ) ) ;
#26674=ORIENTED_EDGE ( 'NONE', *, *, #68161, .F. ) ;
#26675=CARTESIAN_POINT ( 'NONE',  ( -71.18918918918917882, 14.09971791521133255, -7.000000000000000000 ) ) ;
#26676=CARTESIAN_POINT ( 'NONE',  ( -15.98999599679679839, 146.4999999999999716, -7.500000000000000000 ) ) ;
#26679=CARTESIAN_POINT ( 'NONE',  ( 3.094860106618431583, 150.0949999999999420, 9.525000000000000355 ) ) ;
#26683=DIRECTION ( 'NONE',  ( -1.000000000000000000, 0.000000000000000000, 0.000000000000000000 ) ) ;
#26686=ORIENTED_EDGE ( 'NONE', *, *, #3633, .F. ) ;
#26687=CARTESIAN_POINT ( 'NONE',  ( -4.716976649647098618, 130.1429263765338362, 6.492361379858953008 ) ) ;
#26688=DIRECTION ( 'NONE',  ( 1.000000000000000000, 0.000000000000000000, 0.000000000000000000 ) ) ;
#26689=CARTESIAN_POINT ( 'NONE',  ( -74.69171475799898019, 36.40799980539631520, -10.00000000000000000 ) ) ;
#26690=CONICAL_SURFACE ( 'NONE', #22251, 4.999999999999997335, 0.7853981633974587151 ) ;
#26691=DIRECTION ( 'NONE',  ( 0.000000000000000000, -1.000000000000000000, 0.000000000000000000 ) ) ;
#26704=( NAMED_UNIT ( * ) SI_UNIT ( $, .STERADIAN. ) SOLID_ANGLE_UNIT ( ) );
#26706=CYLINDRICAL_SURFACE ( 'NONE', #36139, 13.00000000000000178 ) ;
#26710=ORIENTED_EDGE ( 'NONE', *, *, #48415, .T. ) ;
#26718=DIRECTION ( 'NONE',  ( -0.000000000000000000, -1.000000000000000000, -0.000000000000000000 ) ) ;
#26719=LINE ( 'NONE', #48596, #41929 ) ;
#26722=( NAMED_UNIT ( * ) SI_UNIT ( $, .STERADIAN. ) SOLID_ANGLE_UNIT ( ) );
#26723=( NAMED_UNIT ( * ) PLANE_ANGLE_UNIT ( ) SI_UNIT ( $, .RADIAN. ) );
#26724=CARTESIAN_POINT ( 'NONE',  ( 7.632228543268608334, 126.4570736234661723, -2.479861379858951942 ) ) ;
#26726=CARTESIAN_POINT ( 'NONE',  ( -9.058813317711337021, 158.0449999999999875, -2.943386871421374895 ) ) ;
#26738=AXIS2_PLACEMENT_3D ( 'NONE', #54906, #59156, #38465 ) ;
#26740=EDGE_CURVE ( 'NONE', #55502, #12157, #28714, .T. ) ;
#26744=AXIS2_PLACEMENT_3D ( 'NONE', #56797, #18798, #34296 ) ;
#26745=ORIENTED_EDGE ( 'NONE', *, *, #33508, .F. ) ;
#26747=DIRECTION ( 'NONE',  ( 1.000000000000000000, 0.000000000000000000, 0.000000000000000000 ) ) ;
#26749=AXIS2_PLACEMENT_3D ( 'NONE', #11949, #22864, #49951 ) ;
#26750=SURFACE_SIDE_STYLE ('',( #38428 ) ) ;
#26752=EDGE_CURVE ( 'NONE', #8903, #37997, #34148, .T. ) ;
#26753=ORIENTED_EDGE ( 'NONE', *, *, #37615, .F. ) ;
#26755=EDGE_LOOP ( 'NONE', ( #18345, #14802, #52507, #61455 ) ) ;
#26760=CARTESIAN_POINT ( 'NONE',  ( 45.07697505292422591, 10.02565835097472480, 3.091949714863343246 ) ) ;
#26761=CARTESIAN_POINT ( 'NONE',  ( -10.01517768586949231, 122.1949999999999648, -6.132527647946036459E-16 ) ) ;
#26762=ORIENTED_EDGE ( 'NONE', *, *, #43270, .F. ) ;
#26763=CARTESIAN_POINT ( 'NONE',  ( 5.598654528085809545, 122.2549999999999955, -7.705886871421373741 ) ) ;
#26767=CARTESIAN_POINT ( 'NONE',  ( -40.99999999999998579, 107.7459666924148394, -3.000000000000003109 ) ) ;
#26769=CARTESIAN_POINT ( 'NONE',  ( 9.058813317711337021, 145.6549999999999727, 2.943386871421375783 ) ) ;
#26770=DIRECTION ( 'NONE',  ( 1.000000000000000000, 0.000000000000000000, 0.000000000000000000 ) ) ;
#26771=FACE_OUTER_BOUND ( 'NONE', #63956, .T. ) ;
#26774=FILL_AREA_STYLE_COLOUR ( '', #28679 ) ;
#26775=ORIENTED_EDGE ( 'NONE', *, *, #30807, .T. ) ;
#26778=SURFACE_STYLE_FILL_AREA ( #58825 ) ;
#26780=ORIENTED_EDGE ( 'NONE', *, *, #23669, .T. ) ;
#26781=CARTESIAN_POINT ( 'NONE',  ( 0.9728900412908074724, 111.9999999999999858, -7.965808808122197604 ) ) ;
#26782=MECHANICAL_DESIGN_GEOMETRIC_PRESENTATION_REPRESENTATION('',(#9958),#35797);
#26783=DIRECTION ( 'NONE',  ( 0.000000000000000000, -0.000000000000000000, 1.000000000000000000 ) ) ;
#26785=LINE ( 'NONE', #64799, #6253 ) ;
#26787=MECHANICAL_DESIGN_GEOMETRIC_PRESENTATION_REPRESENTATION('',(#39199),#11088);
#26789=ORIENTED_EDGE ( 'NONE', *, *, #64526, .T. ) ;
#26791=CARTESIAN_POINT ( 'NONE',  ( -44.99999999999998579, 119.9999999999999716, -10.00000000000000000 ) ) ;
#26793=CARTESIAN_POINT ( 'NONE',  ( -24.21231517720798010, 113.4999999999999858, 7.500000000000000000 ) ) ;
#26795=CARTESIAN_POINT ( 'NONE',  ( -48.00000000000000000, 14.49137674618942562, -7.500000000000000000 ) ) ;
#26797=CARTESIAN_POINT ( 'NONE',  ( 15.48999599679679662, 118.4999999999999716, 7.500000000000000000 ) ) ;
#26799=( NAMED_UNIT ( * ) SI_UNIT ( $, .STERADIAN. ) SOLID_ANGLE_UNIT ( ) );
#26800=DIRECTION ( 'NONE',  ( -1.000000000000000000, 0.000000000000000000, 0.000000000000000000 ) ) ;
#26802=CARTESIAN_POINT ( 'NONE',  ( 0.000000000000000000, 124.4449999999999932, -9.525000000000000355 ) ) ;
#26810=VECTOR ( 'NONE', #6150, 1000.000000000000000 ) ;
#26813=EDGE_CURVE ( 'NONE', #32066, #51449, #60692, .T. ) ;
#26814=MECHANICAL_DESIGN_GEOMETRIC_PRESENTATION_REPRESENTATION('',(#54895),#34668);
#26816=DIRECTION ( 'NONE',  ( -1.000000000000000000, 0.000000000000000000, 0.000000000000000000 ) ) ;
#26817=CARTESIAN_POINT ( 'NONE',  ( 71.50000000000000000, 35.92875272052971525, 7.500000000000000000 ) ) ;
#26818=ORIENTED_EDGE ( 'NONE', *, *, #46986, .T. ) ;
#26822=CIRCLE ( 'NONE', #12219, 5.500000000000005329 ) ;
#26824=( NAMED_UNIT ( * ) SI_UNIT ( $, .STERADIAN. ) SOLID_ANGLE_UNIT ( ) );
#26830=ORIENTED_EDGE ( 'NONE', *, *, #46109, .T. ) ;
#26832=SURFACE_SIDE_STYLE ('',( #32845 ) ) ;
#26833=CARTESIAN_POINT ( 'NONE',  ( 7.632228543268607446, 147.1570736234661751, 2.479861379858954606 ) ) ;
#26835=CARTESIAN_POINT ( 'NONE',  ( 44.79289321881345387, 10.55564175590368059, -3.499999999999999112 ) ) ;
#26837=AXIS2_PLACEMENT_3D ( 'NONE', #66276, #49431, #11782 ) ;
#26840=DIRECTION ( 'NONE',  ( 0.000000000000000000, 0.000000000000000000, 1.000000000000000000 ) ) ;
#26842=SURFACE_STYLE_FILL_AREA ( #54647 ) ;
#26846=EDGE_LOOP ( 'NONE', ( #15809, #54266, #45269, #25589 ) ) ;
#26847=AXIS2_PLACEMENT_3D ( 'NONE', #23099, #44588, #50180 ) ;
#26848=MECHANICAL_DESIGN_GEOMETRIC_PRESENTATION_REPRESENTATION('',(#53843),#3285);
#26850=EDGE_LOOP ( 'NONE', ( #61119, #66143, #19760, #1364 ) ) ;
#26851=CARTESIAN_POINT ( 'NONE',  ( 15.48999599679679662, 117.9999999999999716, -9.500000000000000000 ) ) ;
#26856=LINE ( 'NONE', #33558, #58424 ) ;
#26862=AXIS2_PLACEMENT_3D ( 'NONE', #66727, #1930, #40349 ) ;
#26865=PRESENTATION_STYLE_ASSIGNMENT (( #37520 ) ) ;
#26866=AXIS2_PLACEMENT_3D ( 'NONE', #56898, #14326, #40062 ) ;
#26869=CARTESIAN_POINT ( 'NONE',  ( -8.102448949553179958, 122.4949999999999903, 5.886773742842747126 ) ) ;
#26877=FACE_OUTER_BOUND ( 'NONE', #2512, .T. ) ;
#26878=CARTESIAN_POINT ( 'NONE',  ( 74.49999999999998579, 119.9999999999997584, -9.500000000000000000 ) ) ;
#26880=PRESENTATION_STYLE_ASSIGNMENT (( #5111 ) ) ;
#26882=CARTESIAN_POINT ( 'NONE',  ( 0.000000000000000000, 115.4999999999999574, 0.000000000000000000 ) ) ;
#26884=ADVANCED_FACE ( 'NONE', ( #19195 ), #46705, .T. ) ;
#26887=ORIENTED_EDGE ( 'NONE', *, *, #30301, .T. ) ;
#26889=EDGE_CURVE ( 'NONE', #18076, #15891, #30773, .T. ) ;
#26890=( NAMED_UNIT ( * ) SI_UNIT ( $, .STERADIAN. ) SOLID_ANGLE_UNIT ( ) );
#26892=UNCERTAINTY_MEASURE_WITH_UNIT (LENGTH_MEASURE( 1.000000000000000082E-05 ), #67394, 'distance_accuracy_value', 'NONE');
#26895=( LENGTH_UNIT ( ) NAMED_UNIT ( * ) SI_UNIT ( .MILLI., .METRE. ) );
#26905=CARTESIAN_POINT ( 'NONE',  ( -65.49999999999998579, 50.00000000000000000, 10.50000000000000000 ) ) ;
#26908=VECTOR ( 'NONE', #3088, 1000.000000000000000 ) ;
#26909=CARTESIAN_POINT ( 'NONE',  ( 60.00000000000000000, 1.797044900979284448E-15, 12.00000000000000000 ) ) ;
#26914=CARTESIAN_POINT ( 'NONE',  ( -8.437984349512095861, 112.8070736234661524, -5.166775262442723748E-16 ) ) ;
#26915=( GEOMETRIC_REPRESENTATION_CONTEXT ( 3 ) GLOBAL_UNCERTAINTY_ASSIGNED_CONTEXT ( ( #6718 ) ) GLOBAL_UNIT_ASSIGNED_CONTEXT ( ( #26995, #11188, #43599 ) ) REPRESENTATION_CONTEXT ( 'NONE', 'WORKASPACE' ) );
#26916=CARTESIAN_POINT ( 'NONE',  ( 7.632228543268608334, 138.4570736234661581, -2.479861379858951942 ) ) ;
#26917=CIRCLE ( 'NONE', #6765, 0.5000000000000004441 ) ;
#26918=FACE_OUTER_BOUND ( 'NONE', #59450, .T. ) ;
#26921=CARTESIAN_POINT ( 'NONE',  ( 45.00000000000000000, 9.639620389971918613, -6.999999999999999112 ) ) ;
#26925=CARTESIAN_POINT ( 'NONE',  ( 8.102448949553181734, 133.5049999999999670, 5.886773742842750679 ) ) ;
#26926=CYLINDRICAL_SURFACE ( 'NONE', #33322, 13.00000000000000533 ) ;
#26927=DIRECTION ( 'NONE',  ( 0.9486832980505138790, 0.3162277660168378857, -0.000000000000000000 ) ) ;
#26928=SURFACE_STYLE_USAGE ( .BOTH. , #36168 ) ;
#26930=VERTEX_POINT ( 'NONE', #37534 ) ;
#26931=COLOUR_RGB ( '', 0.09019608, 0.27058824, 0.51372549) ;
#26932=EDGE_CURVE ( 'NONE', #7058, #23699, #20607, .T. ) ;
#26933=CARTESIAN_POINT ( 'NONE',  ( 7.896365267660146792, 153.2229155959258549, 2.416370546020021770 ) ) ;
#26934=DIRECTION ( 'NONE',  ( 0.000000000000000000, 0.000000000000000000, -1.000000000000000000 ) ) ;
#26936=CARTESIAN_POINT ( 'NONE',  ( -4.716976649647098618, 154.1429263765338078, 6.492361379858953008 ) ) ;
#26940=CARTESIAN_POINT ( 'NONE',  ( 20.57648123223228254, 114.4999999999999574, -10.27659574468085069 ) ) ;
#26941=ORIENTED_EDGE ( 'NONE', *, *, #22347, .F. ) ;
#26942=CARTESIAN_POINT ( 'NONE',  ( -74.99999999999998579, 50.00000000000000000, 6.500000000000000000 ) ) ;
#26949=CARTESIAN_POINT ( 'NONE',  ( -74.99999999999998579, 50.00000000000000000, -7.500000000000000000 ) ) ;
#26952=DIRECTION ( 'NONE',  ( 0.000000000000000000, 0.000000000000000000, 1.000000000000000000 ) ) ;
#26953=EDGE_LOOP ( 'NONE', ( #20254, #5145, #41631, #21337 ) ) ;
#26954=ORIENTED_EDGE ( 'NONE', *, *, #1440, .T. ) ;
#26957=CARTESIAN_POINT ( 'NONE',  ( 60.00000000000000000, 1.797044900979284448E-15, -6.500000000000000000 ) ) ;
#26958=EDGE_CURVE ( 'NONE', #20549, #60894, #53986, .T. ) ;
#26959=CYLINDRICAL_SURFACE ( 'NONE', #39962, 0.5000000000000004441 ) ;
#26960=EDGE_LOOP ( 'NONE', ( #5831, #68376, #58050, #46567 ) ) ;
#26971=ORIENTED_EDGE ( 'NONE', *, *, #46976, .F. ) ;
#26973=ADVANCED_FACE ( 'NONE', ( #26558 ), #15693, .T. ) ;
#26980=MECHANICAL_DESIGN_GEOMETRIC_PRESENTATION_REPRESENTATION('',(#30349),#47343);
#26982=CARTESIAN_POINT ( 'NONE',  ( -5.598654528085808657, 141.7549999999999955, 7.705886871421373741 ) ) ;
#26986=CARTESIAN_POINT ( 'NONE',  ( 74.50000000000000000, 20.36037961002804053, -6.000000000000000000 ) ) ;
#26990=SURFACE_SIDE_STYLE ('',( #37634 ) ) ;
#26994=CARTESIAN_POINT ( 'NONE',  ( -7.632228543268607446, 132.5429263765338135, -2.479861379858953718 ) ) ;
#26995=( LENGTH_UNIT ( ) NAMED_UNIT ( * ) SI_UNIT ( .MILLI., .METRE. ) );
#26997=DIRECTION ( 'NONE',  ( -0.000000000000000000, -0.000000000000000000, 1.000000000000000000 ) ) ;
#27000=ORIENTED_EDGE ( 'NONE', *, *, #3124, .T. ) ;
#27001=ORIENTED_EDGE ( 'NONE', *, *, #28972, .T. ) ;
#27003=MECHANICAL_DESIGN_GEOMETRIC_PRESENTATION_REPRESENTATION('',(#34920),#56253);
#27006=CARTESIAN_POINT ( 'NONE',  ( 6.826472737025121695, 140.4929263765338021, -4.959722759717905660 ) ) ;
#27012=ORIENTED_EDGE ( 'NONE', *, *, #42275, .F. ) ;
#27014=DIRECTION ( 'NONE',  ( 0.000000000000000000, 0.000000000000000000, 1.000000000000000000 ) ) ;
#27015=ORIENTED_EDGE ( 'NONE', *, *, #40790, .T. ) ;
#27017=SURFACE_STYLE_USAGE ( .BOTH. , #42579 ) ;
#27018=( GEOMETRIC_REPRESENTATION_CONTEXT ( 3 ) GLOBAL_UNCERTAINTY_ASSIGNED_CONTEXT ( ( #67203 ) ) GLOBAL_UNIT_ASSIGNED_CONTEXT ( ( #25480, #31098, #63476 ) ) REPRESENTATION_CONTEXT ( 'NONE', 'WORKASPACE' ) );
#27019=CARTESIAN_POINT ( 'NONE',  ( 8.102448949553183510, 159.9950000000000330, -5.886773742842746238 ) ) ;
#27028=CARTESIAN_POINT ( 'NONE',  ( -9.827790563157511022E-16, 124.4429263765338192, 8.025000000000000355 ) ) ;
#27034=ORIENTED_EDGE ( 'NONE', *, *, #12332, .F. ) ;
#27036=ORIENTED_EDGE ( 'NONE', *, *, #49727, .F. ) ;
#27038=FACE_OUTER_BOUND ( 'NONE', #1685, .T. ) ;
#27045=CARTESIAN_POINT ( 'NONE',  ( -4.716976649647097730, 115.3570736234661638, -6.492361379858953896 ) ) ;
#27046=CARTESIAN_POINT ( 'NONE',  ( 41.12443333818617930, 107.5641524110674112, 3.336502945398295950 ) ) ;
#27054=DIRECTION ( 'NONE',  ( 0.000000000000000000, 0.000000000000000000, 1.000000000000000000 ) ) ;
#27058=DIRECTION ( 'NONE',  ( 0.000000000000000000, 0.000000000000000000, 1.000000000000000000 ) ) ;
#27060=( NAMED_UNIT ( * ) PLANE_ANGLE_UNIT ( ) SI_UNIT ( $, .RADIAN. ) );
#27062=ORIENTED_EDGE ( 'NONE', *, *, #66709, .F. ) ;
#27064=AXIS2_PLACEMENT_3D ( 'NONE', #43542, #42167, #59290 ) ;
#27073=CARTESIAN_POINT ( 'NONE',  ( -1.166476076187854022E-15, 112.0549999999999926, 9.525000000000000355 ) ) ;
#27076=CARTESIAN_POINT ( 'NONE',  ( 71.49999999999998579, 64.07124727947029896, 7.000000000000000000 ) ) ;
#27078=DIRECTION ( 'NONE',  ( -6.938893903907222067E-15, 1.000000000000000000, 0.000000000000000000 ) ) ;
#27079=UNCERTAINTY_MEASURE_WITH_UNIT (LENGTH_MEASURE( 1.000000000000000082E-05 ), #36697, 'distance_accuracy_value', 'NONE');
#27081=ORIENTED_EDGE ( 'NONE', *, *, #25095, .T. ) ;
#27085=AXIS2_PLACEMENT_3D ( 'NONE', #12831, #65610, #23733 ) ;
#27086=( NAMED_UNIT ( * ) PLANE_ANGLE_UNIT ( ) SI_UNIT ( $, .RADIAN. ) );
#27087=AXIS2_PLACEMENT_3D ( 'NONE', #52694, #15424, #14008 ) ;
#27088=FACE_OUTER_BOUND ( 'NONE', #25385, .T. ) ;
#27090=EDGE_LOOP ( 'NONE', ( #10684, #65405, #36384 ) ) ;
#27091=ORIENTED_EDGE ( 'NONE', *, *, #20909, .T. ) ;
#27095=CARTESIAN_POINT ( 'NONE',  ( -74.99999999999998579, 50.00000000000000000, -6.999999999999988454 ) ) ;
#27097=CARTESIAN_POINT ( 'NONE',  ( -45.00000000000000000, 8.537325437491110947, 6.129378421684276823 ) ) ;
#27099=ORIENTED_EDGE ( 'NONE', *, *, #51697, .T. ) ;
#27107=CARTESIAN_POINT ( 'NONE',  ( 3.094860106618435136, 121.2949999999999733, -9.525000000000000355 ) ) ;
#27111=CARTESIAN_POINT ( 'NONE',  ( -9.058813317711338797, 129.4549999999999841, 2.943386871421373563 ) ) ;
#27112=AXIS2_PLACEMENT_3D ( 'NONE', #4775, #47766, #57557 ) ;
#27115=CARTESIAN_POINT ( 'NONE',  ( -41.49999999999998579, 106.9282032302754999, -3.500000000000000888 ) ) ;
#27118=CARTESIAN_POINT ( 'NONE',  ( 3.094860106618431583, 145.2049999999999272, 9.525000000000000355 ) ) ;
#27119=FILL_AREA_STYLE_COLOUR ( '', #31089 ) ;
#27121=( LENGTH_UNIT ( ) NAMED_UNIT ( * ) SI_UNIT ( .MILLI., .METRE. ) );
#27122=DIRECTION ( 'NONE',  ( 1.000000000000000000, 0.000000000000000000, 0.000000000000000000 ) ) ;
#27123=SURFACE_SIDE_STYLE ('',( #10297 ) ) ;
#27130=( GEOMETRIC_REPRESENTATION_CONTEXT ( 3 ) GLOBAL_UNCERTAINTY_ASSIGNED_CONTEXT ( ( #21522 ) ) GLOBAL_UNIT_ASSIGNED_CONTEXT ( ( #33376, #53456, #27377 ) ) REPRESENTATION_CONTEXT ( 'NONE', 'WORKASPACE' ) );
#27131=ORIENTED_EDGE ( 'NONE', *, *, #1699, .T. ) ;
#27132=FILL_AREA_STYLE_COLOUR ( '', #67656 ) ;
#27133=UNCERTAINTY_MEASURE_WITH_UNIT (LENGTH_MEASURE( 1.000000000000000082E-05 ), #69280, 'distance_accuracy_value', 'NONE');
#27134=COLOUR_RGB ( '', 0.66274510, 0.83137255, 0.94901961) ;
#27135=EDGE_CURVE ( 'NONE', #26930, #22912, #1856, .T. ) ;
#27136=CYLINDRICAL_SURFACE ( 'NONE', #36381, 16.00000000000000000 ) ;
#27140=CARTESIAN_POINT ( 'NONE',  ( -45.91046102236034443, 9.422706725342738565, -3.407293203743047005 ) ) ;
#27147=SURFACE_SIDE_STYLE ('',( #53565 ) ) ;
#27150=DIRECTION ( 'NONE',  ( 1.000000000000000000, 0.000000000000000000, 0.000000000000000000 ) ) ;
#27154=AXIS2_PLACEMENT_3D ( 'NONE', #68783, #10389, #31111 ) ;
#27157=CARTESIAN_POINT ( 'NONE',  ( 5.598654528085809545, 133.1449999999999818, -7.705886871421373741 ) ) ;
#27159=CIRCLE ( 'NONE', #44056, 0.5000000000000004441 ) ;
#27160=CARTESIAN_POINT ( 'NONE',  ( 0.000000000000000000, 87.30187232391182306, 0.000000000000000000 ) ) ;
#27165=CARTESIAN_POINT ( 'NONE',  ( 72.50000000000000000, 35.92875272052971525, -9.500000000000000000 ) ) ;
#27169=DIRECTION ( 'NONE',  ( 0.000000000000000000, 0.000000000000000000, 1.000000000000000000 ) ) ;
#27171=STYLED_ITEM ( 'NONE', ( #27889 ), #35666 ) ;
#27174=DIRECTION ( 'NONE',  ( -0.000000000000000000, -0.000000000000000000, -1.000000000000000000 ) ) ;
#27177=FILL_AREA_STYLE ('',( #54277 ) ) ;
#27184=( NAMED_UNIT ( * ) SI_UNIT ( $, .STERADIAN. ) SOLID_ANGLE_UNIT ( ) );
#27186=CARTESIAN_POINT ( 'NONE',  ( 6.826472737025121695, 144.6070736234661638, -4.959722759717905660 ) ) ;
#27188=FACE_OUTER_BOUND ( 'NONE', #1417, .T. ) ;
#27191=CIRCLE ( 'NONE', #1302, 0.5000000000000004441 ) ;
#27194=CYLINDRICAL_SURFACE ( 'NONE', #52361, 0.5000000000000004441 ) ;
#27196=FACE_OUTER_BOUND ( 'NONE', #67924, .T. ) ;
#27203=ORIENTED_EDGE ( 'NONE', *, *, #14385, .T. ) ;
#27204=( LENGTH_UNIT ( ) NAMED_UNIT ( * ) SI_UNIT ( .MILLI., .METRE. ) );
#27205=AXIS2_PLACEMENT_3D ( 'NONE', #5584, #16546, #38006 ) ;
#27206=CARTESIAN_POINT ( 'NONE',  ( -74.99999999999998579, 50.00000000000000000, -9.500000000000001776 ) ) ;
#27207=CARTESIAN_POINT ( 'NONE',  ( -45.00000000000000000, 8.700918745341869709, -5.871692373102996854 ) ) ;
#27209=EDGE_LOOP ( 'NONE', ( #37985, #22473, #52827, #2359 ) ) ;
#27211=FILL_AREA_STYLE_COLOUR ( '', #38227 ) ;
#27220=COLOUR_RGB ( '', 0.40784314, 0.44705882, 0.49803922) ;
#27221=EDGE_CURVE ( 'NONE', #8394, #14677, #69330, .T. ) ;
#27222=CARTESIAN_POINT ( 'NONE',  ( 8.102448949553181734, 129.9950000000000045, -5.886773742842746238 ) ) ;
#27224=CIRCLE ( 'NONE', #10444, 18.50000000000000355 ) ;
#27226=DIRECTION ( 'NONE',  ( 1.000000000000000000, 0.000000000000000000, 0.000000000000000000 ) ) ;
#27227=VERTEX_POINT ( 'NONE', #58416 ) ;
#27228=CARTESIAN_POINT ( 'NONE',  ( -60.00000000000000000, -2.024042244987997205E-14, 12.00000000000000000 ) ) ;
#27230=( NAMED_UNIT ( * ) PLANE_ANGLE_UNIT ( ) SI_UNIT ( $, .RADIAN. ) );
#27233=CIRCLE ( 'NONE', #3620, 0.5000000000000004441 ) ;
#27241=CARTESIAN_POINT ( 'NONE',  ( 44.67254323996785104, 10.47540843667308508, -3.522617369932422804 ) ) ;
#27243=SURFACE_STYLE_USAGE ( .BOTH. , #33587 ) ;
#27244=CARTESIAN_POINT ( 'NONE',  ( 60.49999999999998579, 50.00000000000000000, 7.500000000000000000 ) ) ;
#27246=( GEOMETRIC_REPRESENTATION_CONTEXT ( 3 ) GLOBAL_UNCERTAINTY_ASSIGNED_CONTEXT ( ( #54642 ) ) GLOBAL_UNIT_ASSIGNED_CONTEXT ( ( #57357, #35212, #62288 ) ) REPRESENTATION_CONTEXT ( 'NONE', 'WORKASPACE' ) );
#27250=CARTESIAN_POINT ( 'NONE',  ( -9.827790563157511022E-16, 152.5570736234661524, 8.025000000000000355 ) ) ;
#27252=VECTOR ( 'NONE', #2936, 1000.000000000000000 ) ;
#27257=CIRCLE ( 'NONE', #254, 10.00000000000000533 ) ;
#27261=FILL_AREA_STYLE_COLOUR ( '', #45302 ) ;
#27264=CARTESIAN_POINT ( 'NONE',  ( -7.632228543268608334, 109.9570736234661581, 2.479861379858952830 ) ) ;
#27266=CARTESIAN_POINT ( 'NONE',  ( -19.89974874213240597, 115.4999999999999574, 10.00000000000000000 ) ) ;
#27267=PRESENTATION_STYLE_ASSIGNMENT (( #10786 ) ) ;
#27268=VERTEX_POINT ( 'NONE', #15205 ) ;
#27269=ORIENTED_EDGE ( 'NONE', *, *, #7488, .F. ) ;
#27274=EDGE_LOOP ( 'NONE', ( #8327, #17631, #7351, #42198 ) ) ;
#27275=CARTESIAN_POINT ( 'NONE',  ( -3.094860106618432471, 125.7049999999999841, -9.525000000000000355 ) ) ;
#27276=CARTESIAN_POINT ( 'NONE',  ( 12.72792206135785698, 114.9999999999999574, 10.50000000000000000 ) ) ;
#27285=CARTESIAN_POINT ( 'NONE',  ( 6.422934014168398598, 153.0000000000000000, 4.811085495980990778 ) ) ;
#27286=EDGE_CURVE ( 'NONE', #65459, #29444, #46613, .T. ) ;
#27289=CARTESIAN_POINT ( 'NONE',  ( -23.71231517720798365, 117.9999999999999716, -9.500000000000000000 ) ) ;
#27295=EDGE_LOOP ( 'NONE', ( #36542, #43688, #17261 ) ) ;
#27296=DIRECTION ( 'NONE',  ( 0.000000000000000000, 0.000000000000000000, 1.000000000000000000 ) ) ;
#27301=CARTESIAN_POINT ( 'NONE',  ( -44.99999999999998579, 119.9999999999999716, -10.00000000000000000 ) ) ;
#27303=STYLED_ITEM ( 'NONE', ( #43907 ), #47812 ) ;
#27308=LINE ( 'NONE', #26287, #66295 ) ;
#27309=CARTESIAN_POINT ( 'NONE',  ( -7.255760115451132641, 153.3522680034007237, -4.196031671614308678 ) ) ;
#27310=ORIENTED_EDGE ( 'NONE', *, *, #17580, .T. ) ;
#27311=SURFACE_STYLE_USAGE ( .BOTH. , #43570 ) ;
#27315=DIRECTION ( 'NONE',  ( 0.000000000000000000, 1.000000000000000000, 0.000000000000000000 ) ) ;
#27322=STYLED_ITEM ( 'NONE', ( #38973 ), #36751 ) ;
#27326=FILL_AREA_STYLE_COLOUR ( '', #15629 ) ;
#27328=CARTESIAN_POINT ( 'NONE',  ( 71.99999999999998579, 119.9999999999997868, 7.000000000000000000 ) ) ;
#27329=CARTESIAN_POINT ( 'NONE',  ( -7.632228543268607446, 150.5429263765338135, -2.479861379858953718 ) ) ;
#27336=CARTESIAN_POINT ( 'NONE',  ( 5.598654528085805993, 139.3549999999999898, 7.705886871421374629 ) ) ;
#27337=CARTESIAN_POINT ( 'NONE',  ( -2.607480562269074653, 127.2929263765337993, 8.025000000000000355 ) ) ;
#27338=LINE ( 'NONE', #38666, #5732 ) ;
#27339=EDGE_CURVE ( 'NONE', #51702, #25674, #27755, .T. ) ;
#27340=( GEOMETRIC_REPRESENTATION_CONTEXT ( 3 ) GLOBAL_UNCERTAINTY_ASSIGNED_CONTEXT ( ( #34927 ) ) GLOBAL_UNIT_ASSIGNED_CONTEXT ( ( #38990, #34687, #66720 ) ) REPRESENTATION_CONTEXT ( 'NONE', 'WORKASPACE' ) );
#27342=( NAMED_UNIT ( * ) SI_UNIT ( $, .STERADIAN. ) SOLID_ANGLE_UNIT ( ) );
#27345=CARTESIAN_POINT ( 'NONE',  ( -24.21231517720798010, 112.9999999999999858, 9.500000000000000000 ) ) ;
#27347=SURFACE_SIDE_STYLE ('',( #36333 ) ) ;
#27348=DIRECTION ( 'NONE',  ( 1.000000000000000000, -3.469446951953611033E-15, 0.000000000000000000 ) ) ;
#27352=COLOUR_RGB ( '', 0.72549020, 0.75294118, 0.79215686) ;
#27353=( NAMED_UNIT ( * ) SI_UNIT ( $, .STERADIAN. ) SOLID_ANGLE_UNIT ( ) );
#27354=( GEOMETRIC_REPRESENTATION_CONTEXT ( 3 ) GLOBAL_UNCERTAINTY_ASSIGNED_CONTEXT ( ( #36122 ) ) GLOBAL_UNIT_ASSIGNED_CONTEXT ( ( #50703, #13757, #29930 ) ) REPRESENTATION_CONTEXT ( 'NONE', 'WORKASPACE' ) );
#27355=( NAMED_UNIT ( * ) SI_UNIT ( $, .STERADIAN. ) SOLID_ANGLE_UNIT ( ) );
#27356=DIRECTION ( 'NONE',  ( 0.000000000000000000, 1.000000000000000000, 0.000000000000000000 ) ) ;
#27361=ORIENTED_EDGE ( 'NONE', *, *, #21290, .T. ) ;
#27363=CIRCLE ( 'NONE', #376, 5.000000000000004441 ) ;
#27364=EDGE_CURVE ( 'NONE', #48200, #43100, #3896, .T. ) ;
#27366=CARTESIAN_POINT ( 'NONE',  ( -72.00000000000000000, 35.92875272052971525, 7.500000000000000000 ) ) ;
#27367=CARTESIAN_POINT ( 'NONE',  ( 44.99999999999977973, 146.9999999999999716, -7.000000000000000000 ) ) ;
#27369=FILL_AREA_STYLE ('',( #31267 ) ) ;
#27371=CARTESIAN_POINT ( 'NONE',  ( 9.058813317711338797, 159.8449999999999989, -2.943386871421372675 ) ) ;
#27377=( NAMED_UNIT ( * ) SI_UNIT ( $, .STERADIAN. ) SOLID_ANGLE_UNIT ( ) );
#27378=DIRECTION ( 'NONE',  ( -0.000000000000000000, -0.000000000000000000, 1.000000000000000000 ) ) ;
#27381=EDGE_LOOP ( 'NONE', ( #27925, #47791, #2087, #24346 ) ) ;
#27382=CARTESIAN_POINT ( 'NONE',  ( 0.000000000000000000, 134.9429263765338192, -8.025000000000000355 ) ) ;
#27385=SURFACE_SIDE_STYLE ('',( #5941 ) ) ;
#27389=ORIENTED_EDGE ( 'NONE', *, *, #7555, .F. ) ;
#27391=CARTESIAN_POINT ( 'NONE',  ( -34.99999999999999289, 99.99999999999998579, -9.500000000000000000 ) ) ;
#27393=CARTESIAN_POINT ( 'NONE',  ( -72.49999999999998579, 64.07124727947029896, -9.500000000000000000 ) ) ;
#27397=FILL_AREA_STYLE ('',( #16894 ) ) ;
#27398=MECHANICAL_DESIGN_GEOMETRIC_PRESENTATION_REPRESENTATION('',(#43193),#39810);
#27399=VECTOR ( 'NONE', #35649, 1000.000000000000000 ) ;
#27402=DIRECTION ( 'NONE',  ( -0.000000000000000000, -0.000000000000000000, 1.000000000000000000 ) ) ;
#27403=DIRECTION ( 'NONE',  ( 0.7833176619561811327, 0.6216216216216277068, -4.313366480807242114E-15 ) ) ;
#27404=ORIENTED_EDGE ( 'NONE', *, *, #40958, .F. ) ;
#27406=CARTESIAN_POINT ( 'NONE',  ( -74.99999999999998579, 64.49137674618943095, 10.00000000000000000 ) ) ;
#27412=AXIS2_PLACEMENT_3D ( 'NONE', #1886, #23395, #13534 ) ;
#27413=AXIS2_PLACEMENT_3D ( 'NONE', #51270, #50237, #18215 ) ;
#27416=ORIENTED_EDGE ( 'NONE', *, *, #50529, .T. ) ;
#27422=CARTESIAN_POINT ( 'NONE',  ( 5.598654528085805993, 159.2450000000000045, 7.705886871421374629 ) ) ;
#27425=CARTESIAN_POINT ( 'NONE',  ( 0.000000000000000000, 112.0570736234661666, -8.025000000000000355 ) ) ;
#27435=CYLINDRICAL_SURFACE ( 'NONE', #61682, 0.5000000000000004441 ) ;
#27436=VECTOR ( 'NONE', #18968, 1000.000000000000000 ) ;
#27439=VERTEX_POINT ( 'NONE', #12992 ) ;
#27445=EDGE_CURVE ( 'NONE', #13795, #49593, #64587, .T. ) ;
#27448=FILL_AREA_STYLE ('',( #54198 ) ) ;
#27449=ORIENTED_EDGE ( 'NONE', *, *, #5453, .T. ) ;
#27452=EDGE_CURVE ( 'NONE', #3488, #63248, #56600, .T. ) ;
#27454=EDGE_CURVE ( 'NONE', #40506, #3912, #14016, .T. ) ;
#27457=FACE_OUTER_BOUND ( 'NONE', #60179, .T. ) ;
#27463=CARTESIAN_POINT ( 'NONE',  ( 8.102448949553181734, 135.3950000000000102, 5.886773742842750679 ) ) ;
#27465=CARTESIAN_POINT ( 'NONE',  ( 34.99999999999999289, 99.99999999999998579, 9.500000000000000000 ) ) ;
#27466=CARTESIAN_POINT ( 'NONE',  ( 8.102448949553181734, 131.1049999999999898, -5.886773742842746238 ) ) ;
#27467=EDGE_CURVE ( 'NONE', #27560, #22750, #11105, .T. ) ;
#27471=ORIENTED_EDGE ( 'NONE', *, *, #63585, .T. ) ;
#27472=CARTESIAN_POINT ( 'NONE',  ( -5.598654528085808657, 156.7549999999999670, 7.705886871421373741 ) ) ;
#27476=DIRECTION ( 'NONE',  ( 0.000000000000000000, 0.000000000000000000, 1.000000000000000000 ) ) ;
#27478=CARTESIAN_POINT ( 'NONE',  ( -68.49999999999998579, -1.919947267060472329E-14, -9.999999999999998224 ) ) ;
#27479=EDGE_CURVE ( 'NONE', #6631, #8903, #51135, .T. ) ;
#27480=EDGE_LOOP ( 'NONE', ( #3451, #63662, #21771, #9849, #63753, #26535, #66178, #3408, #13273, #59006, #63033, #61042, #62667 ) ) ;
#27485=AXIS2_PLACEMENT_3D ( 'NONE', #13812, #46570, #24687 ) ;
#27486=( BOUNDED_SURFACE ( )  B_SPLINE_SURFACE ( 3, 2, ( 
 ( #42507, #69213, #26940 ),
 ( #21014, #47815, #58645 ),
 ( #26612, #36553, #21702 ),
 ( #52692, #25926, #48132 ),
 ( #68875, #37239, #64260 ),
 ( #9787, #4456, #43219 ),
 ( #69540, #36185, #57970 ),
 ( #21343, #47456, #10471 ),
 ( #176, #53384, #4108 ),
 ( #57611, #52358, #9434 ) ),
 .UNSPECIFIED., .F., .F., .F. ) 
 B_SPLINE_SURFACE_WITH_KNOTS ( ( 4, 2, 2, 2, 4 ),
 ( 3, 3 ),
 ( 0.0006185862396527136518, 0.001034390655347180218, 0.001450195071041647001, 0.001865999486736113783, 0.002281803902430580566 ),
 ( 0.000000000000000000, 1.000000000000000000 ),
 .UNSPECIFIED. ) 
 GEOMETRIC_REPRESENTATION_ITEM ( )  RATIONAL_B_SPLINE_SURFACE ( (
 ( 1.000000000000000000, 0.8505317485662434729, 1.000000000000000000),
 ( 1.000000000000000000, 0.8505807179912472371, 1.000000000000000000),
 ( 1.000000000000000000, 0.8467906168084839980, 1.000000000000000000),
 ( 1.000000000000000000, 0.8327126069847174961, 1.000000000000000000),
 ( 1.000000000000000000, 0.8223235278808177506, 1.000000000000000000),
 ( 1.000000000000000000, 0.7965633808504525293, 1.000000000000000000),
 ( 1.000000000000000000, 0.7811310880225481590, 1.000000000000000000),
 ( 1.000000000000000000, 0.7464785550193693275, 1.000000000000000000),
 ( 1.000000000000000000, 0.7273804381889640291, 1.000000000000000000),
 ( 1.000000000000000000, 0.7071067811865585639, 1.000000000000000000) ) ) 
 REPRESENTATION_ITEM ( '' )  SURFACE ( )  );
#27487=CARTESIAN_POINT ( 'NONE',  ( 0.000000000000000000, 111.9999999999999858, 0.000000000000000000 ) ) ;
#27489=SURFACE_SIDE_STYLE ('',( #17994 ) ) ;
#27490=ADVANCED_FACE ( 'NONE', ( #3792 ), #20708, .T. ) ;
#27491=CYLINDRICAL_SURFACE ( 'NONE', #28193, 0.5000000000000004441 ) ;
#27492=PLANE ( 'NONE',  #11878 ) ;
#27494=CARTESIAN_POINT ( 'NONE',  ( -45.91408774410873406, 9.428127415005508993, -3.509045371196664931 ) ) ;
#27495=( NAMED_UNIT ( * ) PLANE_ANGLE_UNIT ( ) SI_UNIT ( $, .RADIAN. ) );
#27501=LINE ( 'NONE', #47664, #54991 ) ;
#27507=CARTESIAN_POINT ( 'NONE',  ( -3.094860106618434248, 125.7949999999999733, 9.525000000000000355 ) ) ;
#27512=CARTESIAN_POINT ( 'NONE',  ( 45.07697505292422591, 10.02565835097472480, 3.091949714863343246 ) ) ;
#27513=CARTESIAN_POINT ( 'NONE',  ( 71.99999999999998579, 64.07124727947029896, -9.500000000000000000 ) ) ;
#27516=AXIS2_PLACEMENT_3D ( 'NONE', #24347, #19426, #25057 ) ;
#27517=FILL_AREA_STYLE ('',( #6084 ) ) ;
#27518=AXIS2_PLACEMENT_3D ( 'NONE', #11317, #21528, #22225 ) ;
#27523=ORIENTED_EDGE ( 'NONE', *, *, #37709, .T. ) ;
#27528=DIRECTION ( 'NONE',  ( -0.000000000000000000, -0.000000000000000000, -1.000000000000000000 ) ) ;
#27541=PRESENTATION_STYLE_ASSIGNMENT (( #27871 ) ) ;
#27542=CARTESIAN_POINT ( 'NONE',  ( -4.716976649647097730, 148.3570736234661638, -6.492361379858953896 ) ) ;
#27543=TOROIDAL_SURFACE ( 'NONE', #52309, 14.49999999999999822, 0.5000000000000000000 ) ;
#27545=SURFACE_SIDE_STYLE ('',( #33535 ) ) ;
#27549=( LENGTH_UNIT ( ) NAMED_UNIT ( * ) SI_UNIT ( .MILLI., .METRE. ) );
#27554=DIRECTION ( 'NONE',  ( 0.000000000000000000, 0.000000000000000000, -1.000000000000000000 ) ) ;
#27555=VECTOR ( 'NONE', #68082, 1000.000000000000000 ) ;
#27556=EDGE_LOOP ( 'NONE', ( #17405, #9310, #41733, #15319 ) ) ;
#27557=CIRCLE ( 'NONE', #52318, 0.5000000000000004441 ) ;
#27560=VERTEX_POINT ( 'NONE', #5526 ) ;
#27561=FILL_AREA_STYLE_COLOUR ( '', #23809 ) ;
#27565=DIRECTION ( 'NONE',  ( 0.000000000000000000, 0.000000000000000000, 1.000000000000000000 ) ) ;
#27569=DIRECTION ( 'NONE',  ( -0.000000000000000000, -0.000000000000000000, -1.000000000000000000 ) ) ;
#27571=ORIENTED_EDGE ( 'NONE', *, *, #65186, .T. ) ;
#27573=FILL_AREA_STYLE_COLOUR ( '', #24037 ) ;
#27574=( GEOMETRIC_REPRESENTATION_CONTEXT ( 3 ) GLOBAL_UNCERTAINTY_ASSIGNED_CONTEXT ( ( #59439 ) ) GLOBAL_UNIT_ASSIGNED_CONTEXT ( ( #38360, #15504, #10208 ) ) REPRESENTATION_CONTEXT ( 'NONE', 'WORKASPACE' ) );
#27576=PLANE ( 'NONE',  #426 ) ;
#27579=CARTESIAN_POINT ( 'NONE',  ( -3.094860106618434248, 128.7949999999999875, 9.525000000000000355 ) ) ;
#27580=AXIS2_PLACEMENT_3D ( 'NONE', #2319, #4353, #63485 ) ;
#27583=EDGE_LOOP ( 'NONE', ( #61969, #3920, #4037, #66219 ) ) ;
#27586=CARTESIAN_POINT ( 'NONE',  ( -6.826472737025120807, 130.5070736234661695, -4.959722759717907437 ) ) ;
#27592=VERTEX_POINT ( 'NONE', #69572 ) ;
#27594=STYLED_ITEM ( 'NONE', ( #69151 ), #8662 ) ;
#27596=UNCERTAINTY_MEASURE_WITH_UNIT (LENGTH_MEASURE( 1.000000000000000082E-05 ), #6669, 'distance_accuracy_value', 'NONE');
#27598=( NAMED_UNIT ( * ) PLANE_ANGLE_UNIT ( ) SI_UNIT ( $, .RADIAN. ) );
#27600=DIRECTION ( 'NONE',  ( 0.8946296187927070820, 0.000000000000000000, 0.4468085106382997385 ) ) ;
#27602=SURFACE_STYLE_USAGE ( .BOTH. , #32540 ) ;
#27610=FACE_OUTER_BOUND ( 'NONE', #17096, .T. ) ;
#27616=CARTESIAN_POINT ( 'NONE',  ( -8.437984349512095861, 138.6929263765337907, -5.166775262442723748E-16 ) ) ;
#27617=( LENGTH_UNIT ( ) NAMED_UNIT ( * ) SI_UNIT ( .MILLI., .METRE. ) );
#27619=ORIENTED_EDGE ( 'NONE', *, *, #24154, .T. ) ;
#27620=DIRECTION ( 'NONE',  ( -1.000000000000000000, 0.000000000000000000, -0.000000000000000000 ) ) ;
#27621=( GEOMETRIC_REPRESENTATION_CONTEXT ( 3 ) GLOBAL_UNCERTAINTY_ASSIGNED_CONTEXT ( ( #50992 ) ) GLOBAL_UNIT_ASSIGNED_CONTEXT ( ( #43295, #63983, #58720 ) ) REPRESENTATION_CONTEXT ( 'NONE', 'WORKASPACE' ) );
#27622=CARTESIAN_POINT ( 'NONE',  ( -2.607480562269075097, 122.4070736234661467, 8.025000000000000355 ) ) ;
#27623=FILL_AREA_STYLE ('',( #17472 ) ) ;
#27625=CARTESIAN_POINT ( 'NONE',  ( -47.50000000000000000, 14.49137674618942562, -10.00000000000000000 ) ) ;
#27627=VERTEX_POINT ( 'NONE', #69247 ) ;
#27629=EDGE_CURVE ( 'NONE', #16451, #51449, #21043, .T. ) ;
#27644=EDGE_LOOP ( 'NONE', ( #39107, #43232, #15743, #64704, #20057, #57960 ) ) ;
#27649=AXIS2_PLACEMENT_3D ( 'NONE', #20487, #63404, #14181 ) ;
#27650=( LENGTH_UNIT ( ) NAMED_UNIT ( * ) SI_UNIT ( .MILLI., .METRE. ) );
#27654=FILL_AREA_STYLE ('',( #10815 ) ) ;
#27655=CARTESIAN_POINT ( 'NONE',  ( -6.780819373525727833, 153.3146089765552631, -4.862369566202410454 ) ) ;
#27656=EDGE_LOOP ( 'NONE', ( #10300, #68497, #31623, #29808 ) ) ;
#27658=DIRECTION ( 'NONE',  ( 0.000000000000000000, 0.000000000000000000, 1.000000000000000000 ) ) ;
#27659=( NAMED_UNIT ( * ) PLANE_ANGLE_UNIT ( ) SI_UNIT ( $, .RADIAN. ) );
#27665=DIRECTION ( 'NONE',  ( 0.000000000000000000, 0.000000000000000000, 1.000000000000000000 ) ) ;
#27668=ORIENTED_EDGE ( 'NONE', *, *, #53344, .F. ) ;
#27670=FACE_OUTER_BOUND ( 'NONE', #8798, .T. ) ;
#27671=SURFACE_SIDE_STYLE ('',( #39327 ) ) ;
#27675=CARTESIAN_POINT ( 'NONE',  ( 10.01517768586949231, 136.8049999999999500, 1.839758294383810543E-15 ) ) ;
#27679=UNCERTAINTY_MEASURE_WITH_UNIT (LENGTH_MEASURE( 1.000000000000000082E-05 ), #458, 'distance_accuracy_value', 'NONE');
#27681=DIRECTION ( 'NONE',  ( -0.000000000000000000, -0.000000000000000000, -1.000000000000000000 ) ) ;
#27682=EDGE_CURVE ( 'NONE', #40049, #61248, #21911, .T. ) ;
#27683=VERTEX_POINT ( 'NONE', #14521 ) ;
#27685=DIRECTION ( 'NONE',  ( 0.000000000000000000, 0.000000000000000000, -1.000000000000000000 ) ) ;
#27687=FILL_AREA_STYLE ('',( #10854 ) ) ;
#27690=DIRECTION ( 'NONE',  ( 1.000000000000000000, 0.000000000000000000, 0.000000000000000000 ) ) ;
#27694=ORIENTED_EDGE ( 'NONE', *, *, #19298, .F. ) ;
#27695=CARTESIAN_POINT ( 'NONE',  ( -9.827790563157511022E-16, 136.4429263765338192, 8.025000000000000355 ) ) ;
#27698=UNCERTAINTY_MEASURE_WITH_UNIT (LENGTH_MEASURE( 1.000000000000000082E-05 ), #36773, 'distance_accuracy_value', 'NONE');
#27700=FACE_OUTER_BOUND ( 'NONE', #15851, .T. ) ;
#27711=CARTESIAN_POINT ( 'NONE',  ( 12.72792206135785698, 114.9999999999999574, -10.50000000000000000 ) ) ;
#27712=( NAMED_UNIT ( * ) PLANE_ANGLE_UNIT ( ) SI_UNIT ( $, .RADIAN. ) );
#27714=ORIENTED_EDGE ( 'NONE', *, *, #44257, .T. ) ;
#27715=VERTEX_POINT ( 'NONE', #52195 ) ;
#27717=CARTESIAN_POINT ( 'NONE',  ( 7.647808743684392674, 154.4999999999999432, 5.677732506910178500 ) ) ;
#27718=DIRECTION ( 'NONE',  ( 0.000000000000000000, -0.000000000000000000, 1.000000000000000000 ) ) ;
#27721=CARTESIAN_POINT ( 'NONE',  ( -6.826472737025120807, 135.9929263765337737, 4.959722759717906548 ) ) ;
#27725=ORIENTED_EDGE ( 'NONE', *, *, #44284, .F. ) ;
#27728=DIRECTION ( 'NONE',  ( 0.000000000000000000, 0.000000000000000000, 1.000000000000000000 ) ) ;
#27729=CARTESIAN_POINT ( 'NONE',  ( 15.98999599679679839, 147.4999999999999716, 9.500000000000000000 ) ) ;
#27733=EDGE_LOOP ( 'NONE', ( #56841, #34987, #60095, #4178 ) ) ;
#27735=FACE_OUTER_BOUND ( 'NONE', #34724, .T. ) ;
#27736=CARTESIAN_POINT ( 'NONE',  ( 40.82744559481908908, 108.1269596360033205, 3.302666768370682515 ) ) ;
#27738=ORIENTED_EDGE ( 'NONE', *, *, #63070, .T. ) ;
#27739=DIRECTION ( 'NONE',  ( -7.080503983578803083E-17, 1.000000000000000000, 0.000000000000000000 ) ) ;
#27748=SURFACE_SIDE_STYLE ('',( #6316 ) ) ;
#27753=CARTESIAN_POINT ( 'NONE',  ( 74.99999999999998579, 50.00000000000000000, 7.000000000000000000 ) ) ;
#27755=LINE ( 'NONE', #60148, #48905 ) ;
#27760=CARTESIAN_POINT ( 'NONE',  ( -8.102448949553181734, 158.4950000000000045, 5.886773742842747126 ) ) ;
#27764=FACE_OUTER_BOUND ( 'NONE', #22819, .T. ) ;
#27766=UNCERTAINTY_MEASURE_WITH_UNIT (LENGTH_MEASURE( 1.000000000000000082E-05 ), #24801, 'distance_accuracy_value', 'NONE');
#27767=ADVANCED_FACE ( 'NONE', ( #62373 ), #28656, .T. ) ;
#27772=ADVANCED_FACE ( 'NONE', ( #52879 ), #68350, .F. ) ;
#27776=ORIENTED_EDGE ( 'NONE', *, *, #23613, .T. ) ;
#27778=DIRECTION ( 'NONE',  ( 1.000000000000000000, 0.000000000000000000, 0.000000000000000000 ) ) ;
#27780=EDGE_CURVE ( 'NONE', #52169, #46059, #10701, .T. ) ;
#27786=CARTESIAN_POINT ( 'NONE',  ( -45.00000000000000000, -2.024042244987997205E-14, -9.500000000000000000 ) ) ;
#27787=ORIENTED_EDGE ( 'NONE', *, *, #33197, .F. ) ;
#27789=ORIENTED_EDGE ( 'NONE', *, *, #33683, .T. ) ;
#27790=ORIENTED_EDGE ( 'NONE', *, *, #39512, .F. ) ;
#27791=DIRECTION ( 'NONE',  ( 0.000000000000000000, 0.000000000000000000, 1.000000000000000000 ) ) ;
#27795=CARTESIAN_POINT ( 'NONE',  ( -8.102448949553181734, 131.4950000000000045, 5.886773742842747126 ) ) ;
#27796=DIRECTION ( 'NONE',  ( 0.000000000000000000, 1.000000000000000000, -0.000000000000000000 ) ) ;
#27798=CARTESIAN_POINT ( 'NONE',  ( 9.058813317711338797, 127.9549999999999841, -2.943386871421372675 ) ) ;
#27802=ORIENTED_EDGE ( 'NONE', *, *, #33751, .T. ) ;
#27803=CARTESIAN_POINT ( 'NONE',  ( -5.598654528085806881, 158.8549999999999898, -7.705886871421374629 ) ) ;
#27805=UNCERTAINTY_MEASURE_WITH_UNIT (LENGTH_MEASURE( 1.000000000000000082E-05 ), #222, 'distance_accuracy_value', 'NONE');
#27806=VECTOR ( 'NONE', #53336, 1000.000000000000000 ) ;
#27808=STYLED_ITEM ( 'NONE', ( #10728 ), #41578 ) ;
#27810=LINE ( 'NONE', #39824, #29800 ) ;
#27814=( LENGTH_UNIT ( ) NAMED_UNIT ( * ) SI_UNIT ( .MILLI., .METRE. ) );
#27816=VERTEX_POINT ( 'NONE', #38468 ) ;
#27818=UNCERTAINTY_MEASURE_WITH_UNIT (LENGTH_MEASURE( 1.000000000000000082E-05 ), #43958, 'distance_accuracy_value', 'NONE');
#27820=( NAMED_UNIT ( * ) SI_UNIT ( $, .STERADIAN. ) SOLID_ANGLE_UNIT ( ) );
#27821=SURFACE_STYLE_USAGE ( .BOTH. , #44088 ) ;
#27832=CARTESIAN_POINT ( 'NONE',  ( -75.00000000000001421, 8.675277573170040668, -5.941086794572167484 ) ) ;
#27838=ADVANCED_FACE ( 'NONE', ( #65488 ), #42700, .T. ) ;
#27841=CARTESIAN_POINT ( 'NONE',  ( 10.01517768586949231, 126.6949999999999932, 1.839758294383810543E-15 ) ) ;
#27846=ADVANCED_FACE ( 'NONE', ( #21541 ), #27491, .F. ) ;
#27849=COLOUR_RGB ( '', 0.40784314, 0.44705882, 0.49803922) ;
#27855=DIRECTION ( 'NONE',  ( 1.000000000000000000, -8.881784197001254296E-16, 0.000000000000000000 ) ) ;
#27856=ORIENTED_EDGE ( 'NONE', *, *, #579, .F. ) ;
#27860=EDGE_CURVE ( 'NONE', #41276, #53774, #37274, .T. ) ;
#27866=ORIENTED_EDGE ( 'NONE', *, *, #20890, .T. ) ;
#27868=FILL_AREA_STYLE_COLOUR ( '', #68039 ) ;
#27869=DIRECTION ( 'NONE',  ( 1.000000000000000000, 0.000000000000000000, 0.000000000000000000 ) ) ;
#27870=COLOUR_RGB ( '', 0.66274510, 0.83137255, 0.94901961) ;
#27871=SURFACE_STYLE_USAGE ( .BOTH. , #5392 ) ;
#27872=CARTESIAN_POINT ( 'NONE',  ( 2.607480562269071989, 152.7070736234661297, 8.025000000000002132 ) ) ;
#27876=CARTESIAN_POINT ( 'NONE',  ( 4.716976649647099507, 137.6429263765338078, -6.492361379858953008 ) ) ;
#27878=UNCERTAINTY_MEASURE_WITH_UNIT (LENGTH_MEASURE( 1.000000000000000082E-05 ), #7861, 'distance_accuracy_value', 'NONE');
#27879=CARTESIAN_POINT ( 'NONE',  ( 0.000000000000000000, 133.0570736234661524, -8.025000000000000355 ) ) ;
#27880=( GEOMETRIC_REPRESENTATION_CONTEXT ( 3 ) GLOBAL_UNCERTAINTY_ASSIGNED_CONTEXT ( ( #10253 ) ) GLOBAL_UNIT_ASSIGNED_CONTEXT ( ( #65487, #37777, #32788 ) ) REPRESENTATION_CONTEXT ( 'NONE', 'WORKASPACE' ) );
#27881=AXIS2_PLACEMENT_3D ( 'NONE', #45890, #67318, #56776 ) ;
#27883=FACE_OUTER_BOUND ( 'NONE', #60354, .T. ) ;
#27885=DIRECTION ( 'NONE',  ( 1.000000000000000000, 0.000000000000000000, 0.000000000000000000 ) ) ;
#27886=PRESENTATION_STYLE_ASSIGNMENT (( #7168 ) ) ;
#27889=PRESENTATION_STYLE_ASSIGNMENT (( #60602 ) ) ;
#27894=DIRECTION ( 'NONE',  ( 8.659560562354879857E-17, 0.7071067811865517916, -0.7071067811865431318 ) ) ;
#27895=CARTESIAN_POINT ( 'NONE',  ( -45.90838419619620936, 9.403326511829279255, -6.097699930223750897 ) ) ;
#27899=CARTESIAN_POINT ( 'NONE',  ( -75.00000000000000000, 7.768687147774685720, 6.500000000000002665 ) ) ;
#27901=VERTEX_POINT ( 'NONE', #50029 ) ;
#27904=( LENGTH_UNIT ( ) NAMED_UNIT ( * ) SI_UNIT ( .MILLI., .METRE. ) );
#27905=FILL_AREA_STYLE_COLOUR ( '', #64787 ) ;
#27907=CARTESIAN_POINT ( 'NONE',  ( -9.058813317711337021, 131.0449999999999875, -2.943386871421374895 ) ) ;
#27909=EDGE_CURVE ( 'NONE', #25423, #52608, #60534, .T. ) ;
#27910=TOROIDAL_SURFACE ( 'NONE', #44861, 1.000000000000000000, 0.5000000000000000000 ) ;
#27911=DIRECTION ( 'NONE',  ( 1.000000000000000000, 0.000000000000000000, 0.000000000000000000 ) ) ;
#27913=( NAMED_UNIT ( * ) SI_UNIT ( $, .STERADIAN. ) SOLID_ANGLE_UNIT ( ) );
#27918=EDGE_CURVE ( 'NONE', #64235, #62518, #45472, .T. ) ;
#27920=( NAMED_UNIT ( * ) SI_UNIT ( $, .STERADIAN. ) SOLID_ANGLE_UNIT ( ) );
#27922=CIRCLE ( 'NONE', #3192, 0.5000000000000004441 ) ;
#27925=ORIENTED_EDGE ( 'NONE', *, *, #7543, .T. ) ;
#27928=CARTESIAN_POINT ( 'NONE',  ( 44.30330429060724384, 9.767768096869062333, -3.048789874180223070 ) ) ;
#27929=FACE_OUTER_BOUND ( 'NONE', #43701, .T. ) ;
#27932=( NAMED_UNIT ( * ) SI_UNIT ( $, .STERADIAN. ) SOLID_ANGLE_UNIT ( ) );
#27935=FACE_OUTER_BOUND ( 'NONE', #67522, .T. ) ;
#27939=SURFACE_STYLE_FILL_AREA ( #39258 ) ;
#27945=FACE_OUTER_BOUND ( 'NONE', #4433, .T. ) ;
#27953=CARTESIAN_POINT ( 'NONE',  ( 72.00000000000000000, 14.49137674618942562, 10.00000000000000000 ) ) ;
#27955=CARTESIAN_POINT ( 'NONE',  ( -6.826472737025120807, 127.5070736234661695, -4.959722759717907437 ) ) ;
#27956=CYLINDRICAL_SURFACE ( 'NONE', #19241, 0.5000000000000004441 ) ;
#27957=CARTESIAN_POINT ( 'NONE',  ( 75.00000000000000000, 19.84496280275719471, -6.370902851337238992 ) ) ;
#27958=B_SPLINE_CURVE_WITH_KNOTS ( 'NONE', 3,
 ( #9957, #9269, #63415, #4281, #51465, #8904, #63744, #62368, #26107, #3577, #14190, #3221, #31376, #9624, #36728, #24710, #57082, #42008, #47641, #25083, #51830, #19803, #68701, #41293, #62689, #14517, #31042, #30685, #52536, #25762, #25424, #46939, #20129, #41638, #63057, #36380, #69048, #47278, #20499, #15260, #16636, #53554, #701, #26781 ),
 .UNSPECIFIED., .F., .F.,
 ( 4, 2, 2, 2, 2, 2, 2, 2, 2, 2, 2, 2, 2, 2, 2, 2, 2, 2, 2, 2, 2, 4 ),
 ( 0.008690707667102838888, 0.01030713786529197443, 0.01192356806348110823, 0.01353999826167024204, 0.01515642845985937757, 0.01596464355895394621, 0.01677285865804851311, 0.01838928885623765386, 0.01919750395533222423, 0.02000571905442679460, 0.02162214925261593881, 0.02323857945080508303, 0.02404679454989964993, 0.02485500964899422377, 0.02647143984718336451, 0.02727965494627793142, 0.02808787004537250526, 0.02970430024356164600, 0.03051251534265621984, 0.03132073044175079368, 0.03293716063993993443, 0.03455359083812908211 ),
 .UNSPECIFIED. ) ;
#27960=ORIENTED_EDGE ( 'NONE', *, *, #42468, .F. ) ;
#27962=EDGE_LOOP ( 'NONE', ( #46157, #228, #53106, #17218, #48289 ) ) ;
#27964=ORIENTED_EDGE ( 'NONE', *, *, #5096, .F. ) ;
#27965=FILL_AREA_STYLE ('',( #16784 ) ) ;
#27969=CARTESIAN_POINT ( 'NONE',  ( 4.716976649647096842, 148.7429263765338021, 6.492361379858953896 ) ) ;
#27971=CIRCLE ( 'NONE', #6649, 22.50000000000000000 ) ;
#27973=AXIS2_PLACEMENT_3D ( 'NONE', #33900, #7525, #49759 ) ;
#27975=CARTESIAN_POINT ( 'NONE',  ( -4.716976649647097730, 123.2429263765338163, -6.492361379858953896 ) ) ;
#27977=ORIENTED_EDGE ( 'NONE', *, *, #8371, .F. ) ;
#27980=CIRCLE ( 'NONE', #10059, 5.500000000000005329 ) ;
#27982=ORIENTED_EDGE ( 'NONE', *, *, #38361, .T. ) ;
#27987=DIRECTION ( 'NONE',  ( -0.000000000000000000, 0.000000000000000000, 1.000000000000000000 ) ) ;
#27988=DIRECTION ( 'NONE',  ( 1.000000000000000000, 0.000000000000000000, 0.000000000000000000 ) ) ;
#27995=CARTESIAN_POINT ( 'NONE',  ( -7.968833018235937260, 153.7102887258889723, 3.588351662842281353 ) ) ;
#27997=DIRECTION ( 'NONE',  ( -0.9704308468600219006, 0.2413793103448194921, -0.000000000000000000 ) ) ;
#28002=DIRECTION ( 'NONE',  ( 0.000000000000000000, 0.000000000000000000, 1.000000000000000000 ) ) ;
#28006=STYLED_ITEM ( 'NONE', ( #47018 ), #58937 ) ;
#28008=FACE_OUTER_BOUND ( 'NONE', #68275, .T. ) ;
#28009=( LENGTH_UNIT ( ) NAMED_UNIT ( * ) SI_UNIT ( .MILLI., .METRE. ) );
#28015=AXIS2_PLACEMENT_3D ( 'NONE', #29321, #44862, #1146 ) ;
#28016=EDGE_CURVE ( 'NONE', #33323, #18360, #11132, .T. ) ;
#28018=CARTESIAN_POINT ( 'NONE',  ( 3.094860106618435136, 137.4050000000000296, -9.525000000000000355 ) ) ;
#28024=SURFACE_STYLE_FILL_AREA ( #39339 ) ;
#28026=AXIS2_PLACEMENT_3D ( 'NONE', #43809, #65219, #37154 ) ;
#28032=ORIENTED_EDGE ( 'NONE', *, *, #67061, .T. ) ;
#28033=CIRCLE ( 'NONE', #59495, 0.9999999999999991118 ) ;
#28036=FILL_AREA_STYLE_COLOUR ( '', #34887 ) ;
#28042=EDGE_LOOP ( 'NONE', ( #28759, #6307, #22374, #40389 ) ) ;
#28043=FILL_AREA_STYLE_COLOUR ( '', #47842 ) ;
#28044=DIRECTION ( 'NONE',  ( 1.000000000000000000, 0.000000000000000000, 0.000000000000000000 ) ) ;
#28046=CARTESIAN_POINT ( 'NONE',  ( 44.99999999999977973, 149.4999999999999716, 9.500000000000000000 ) ) ;
#28047=DIRECTION ( 'NONE',  ( 0.000000000000000000, 0.000000000000000000, 1.000000000000000000 ) ) ;
#28048=EDGE_LOOP ( 'NONE', ( #4932, #9599, #49566, #37304 ) ) ;
#28049=MECHANICAL_DESIGN_GEOMETRIC_PRESENTATION_REPRESENTATION('',(#19083),#21350);
#28050=CARTESIAN_POINT ( 'NONE',  ( 0.000000000000000000, 160.4449999999999932, -9.525000000000000355 ) ) ;
#28054=CARTESIAN_POINT ( 'NONE',  ( -15.98999599679679839, 146.4999999999999716, 7.000000000000000000 ) ) ;
#28056=CARTESIAN_POINT ( 'NONE',  ( 4.716976649647099507, 137.6429263765338078, -6.492361379858953008 ) ) ;
#28059=DIRECTION ( 'NONE',  ( 0.000000000000000000, 0.000000000000000000, 1.000000000000000000 ) ) ;
#28061=ORIENTED_EDGE ( 'NONE', *, *, #27364, .T. ) ;
#28063=STYLED_ITEM ( 'NONE', ( #66302 ), #21057 ) ;
#28067=CARTESIAN_POINT ( 'NONE',  ( -74.50000000000000000, 119.9999999999997726, 10.00000000000000000 ) ) ;
#28071=DIRECTION ( 'NONE',  ( -1.000000000000000000, 1.156482317317866302E-16, 0.000000000000000000 ) ) ;
#28072=CYLINDRICAL_SURFACE ( 'NONE', #29364, 0.5000000000000004441 ) ;
#28076=CARTESIAN_POINT ( 'NONE',  ( -45.00000000000000711, 8.164352767049518178, -6.987111781054301751 ) ) ;
#28079=ORIENTED_EDGE ( 'NONE', *, *, #61684, .F. ) ;
#28080=LINE ( 'NONE', #5604, #50822 ) ;
#28083=VERTEX_POINT ( 'NONE', #63331 ) ;
#28084=SURFACE_STYLE_FILL_AREA ( #1329 ) ;
#28085=ADVANCED_FACE ( 'NONE', ( #42606 ), #22149, .T. ) ;
#28087=( LENGTH_UNIT ( ) NAMED_UNIT ( * ) SI_UNIT ( .MILLI., .METRE. ) );
#28088=EDGE_CURVE ( 'NONE', #42340, #58089, #4927, .T. ) ;
#28092=DIRECTION ( 'NONE',  ( -1.000000000000000000, 0.000000000000000000, 0.000000000000000000 ) ) ;
#28094=ORIENTED_EDGE ( 'NONE', *, *, #47236, .F. ) ;
#28096=EDGE_CURVE ( 'NONE', #64569, #16390, #31659, .T. ) ;
#28098=DIRECTION ( 'NONE',  ( -1.000000000000000000, 0.000000000000000000, 0.000000000000000000 ) ) ;
#28103=ADVANCED_FACE ( 'NONE', ( #27735 ), #26706, .T. ) ;
#28105=CARTESIAN_POINT ( 'NONE',  ( -1.166476076187854022E-15, 158.9449999999999932, 9.525000000000000355 ) ) ;
#28108=( NAMED_UNIT ( * ) PLANE_ANGLE_UNIT ( ) SI_UNIT ( $, .RADIAN. ) );
#28110=CARTESIAN_POINT ( 'NONE',  ( 40.96656732556692049, 108.0254117342834377, -3.574171091744781759 ) ) ;
#28113=COLOUR_RGB ( '', 0.72549020, 0.75294118, 0.79215686) ;
#28119=ORIENTED_EDGE ( 'NONE', *, *, #30962, .F. ) ;
#28123=DIRECTION ( 'NONE',  ( 1.000000000000000000, 0.000000000000000000, 0.000000000000000000 ) ) ;
#28124=CARTESIAN_POINT ( 'NONE',  ( -45.50000000000000000, -2.024042244987997205E-14, 6.500000000000000000 ) ) ;
#28126=DIRECTION ( 'NONE',  ( 0.000000000000000000, 1.000000000000000000, 0.000000000000000000 ) ) ;
#28132=CARTESIAN_POINT ( 'NONE',  ( 0.000000000000000000, 109.9999999999999858, 0.000000000000000000 ) ) ;
#28135=CARTESIAN_POINT ( 'NONE',  ( -15.98999599679679839, 118.4999999999999716, -9.500000000000000000 ) ) ;
#28136=CARTESIAN_POINT ( 'NONE',  ( 0.000000000000000000, 127.4449999999999790, -9.525000000000000355 ) ) ;
#28137=COLOUR_RGB ( '', 0.40784314, 0.44705882, 0.49803922) ;
#28139=ORIENTED_EDGE ( 'NONE', *, *, #60466, .T. ) ;
#28140=CARTESIAN_POINT ( 'NONE',  ( 5.598654528085809545, 128.2549999999999670, -7.705886871421373741 ) ) ;
#28142=( NAMED_UNIT ( * ) SI_UNIT ( $, .STERADIAN. ) SOLID_ANGLE_UNIT ( ) );
#28143=EDGE_LOOP ( 'NONE', ( #17490, #3396, #34460, #30792 ) ) ;
#28144=CARTESIAN_POINT ( 'NONE',  ( -8.102448949553181734, 153.0050000000000239, -5.886773742842749790 ) ) ;
#28147=ORIENTED_EDGE ( 'NONE', *, *, #49026, .F. ) ;
#28149=FACE_OUTER_BOUND ( 'NONE', #27274, .T. ) ;
#28152=FILL_AREA_STYLE ('',( #1410 ) ) ;
#28159=STYLED_ITEM ( 'NONE', ( #21734 ), #12491 ) ;
#28162=FACE_OUTER_BOUND ( 'NONE', #44691, .T. ) ;
#28164=ORIENTED_EDGE ( 'NONE', *, *, #24059, .T. ) ;
#28172=ADVANCED_FACE ( 'NONE', ( #49589 ), #6971, .F. ) ;
#28174=CYLINDRICAL_SURFACE ( 'NONE', #40742, 4.999999999999997335 ) ;
#28175=DIRECTION ( 'NONE',  ( 1.000000000000000000, 0.000000000000000000, 0.000000000000000000 ) ) ;
#28178=CARTESIAN_POINT ( 'NONE',  ( -74.33437949985298587, 8.455502173247598563, -6.462386104487723770 ) ) ;
#28179=VERTEX_POINT ( 'NONE', #1995 ) ;
#28181=MECHANICAL_DESIGN_GEOMETRIC_PRESENTATION_REPRESENTATION('',(#55159),#49570);
#28183=CARTESIAN_POINT ( 'NONE',  ( -10.01517768586949231, 125.1950000000000074, -6.132527647946036459E-16 ) ) ;
#28186=AXIS2_PLACEMENT_3D ( 'NONE', #50482, #14234, #2210 ) ;
#28187=CARTESIAN_POINT ( 'NONE',  ( 10.01517768586949231, 145.8050000000000068, 1.839758294383810543E-15 ) ) ;
#28193=AXIS2_PLACEMENT_3D ( 'NONE', #1764, #7099, #66534 ) ;
#28195=DIRECTION ( 'NONE',  ( 1.000000000000000000, 0.000000000000000000, 0.000000000000000000 ) ) ;
#28196=EDGE_LOOP ( 'NONE', ( #27310, #35917, #29967, #54306 ) ) ;
#28198=ORIENTED_EDGE ( 'NONE', *, *, #34252, .F. ) ;
#28199=COLOUR_RGB ( '', 0.08235294, 0.09019608, 0.10196078) ;
#28204=COLOUR_RGB ( '', 0.40784314, 0.44705882, 0.49803922) ;
#28207=CARTESIAN_POINT ( 'NONE',  ( 44.37550316447022425, 9.999999999999982236, -3.428884149106774970 ) ) ;
#28210=ORIENTED_EDGE ( 'NONE', *, *, #10742, .F. ) ;
#28212=VERTEX_POINT ( 'NONE', #54823 ) ;
#28214=( NAMED_UNIT ( * ) SI_UNIT ( $, .STERADIAN. ) SOLID_ANGLE_UNIT ( ) );
#28215=CIRCLE ( 'NONE', #6863, 9.500000000000005329 ) ;
#28216=CYLINDRICAL_SURFACE ( 'NONE', #38799, 0.5000000000000004441 ) ;
#28217=CARTESIAN_POINT ( 'NONE',  ( -8.437984349512095861, 154.8070736234661524, -5.166775262442723748E-16 ) ) ;
#28218=CIRCLE ( 'NONE', #32725, 9.499999999999994671 ) ;
#28219=ORIENTED_EDGE ( 'NONE', *, *, #50135, .T. ) ;
#28222=AXIS2_PLACEMENT_3D ( 'NONE', #1171, #60657, #28988 ) ;
#28234=ADVANCED_FACE ( 'NONE', ( #55173 ), #52014, .F. ) ;
#28236=CARTESIAN_POINT ( 'NONE',  ( -45.00000000000000000, 9.708372641349546583, -6.050536800209449062 ) ) ;
#28242=CARTESIAN_POINT ( 'NONE',  ( -75.00000000000000000, 8.681424763010927137, 5.653729937179129195 ) ) ;
#28244=VERTEX_POINT ( 'NONE', #19267 ) ;
#28246=( NAMED_UNIT ( * ) PLANE_ANGLE_UNIT ( ) SI_UNIT ( $, .RADIAN. ) );
#28249=DIRECTION ( 'NONE',  ( 1.000000000000000000, 0.000000000000000000, 0.000000000000000000 ) ) ;
#28253=CARTESIAN_POINT ( 'NONE',  ( 10.01517768586949408, 132.6949999999999648, 1.839758294383810543E-15 ) ) ;
#28255=AXIS2_PLACEMENT_3D ( 'NONE', #69452, #21239, #25834 ) ;
#28256=STYLED_ITEM ( 'NONE', ( #34977 ), #13010 ) ;
#28257=EDGE_CURVE ( 'NONE', #13670, #22419, #58112, .T. ) ;
#28259=ORIENTED_EDGE ( 'NONE', *, *, #4913, .F. ) ;
#28262=DIRECTION ( 'NONE',  ( 1.000000000000000000, 0.000000000000000000, 0.000000000000000000 ) ) ;
#28263=( GEOMETRIC_REPRESENTATION_CONTEXT ( 3 ) GLOBAL_UNCERTAINTY_ASSIGNED_CONTEXT ( ( #18694 ) ) GLOBAL_UNIT_ASSIGNED_CONTEXT ( ( #60906, #43748, #54599 ) ) REPRESENTATION_CONTEXT ( 'NONE', 'WORKASPACE' ) );
#28264=( LENGTH_UNIT ( ) NAMED_UNIT ( * ) SI_UNIT ( .MILLI., .METRE. ) );
#28267=DIRECTION ( 'NONE',  ( -1.000000000000000000, 0.000000000000000000, 0.000000000000000000 ) ) ;
#28269=AXIS2_PLACEMENT_3D ( 'NONE', #2226, #29733, #40302 ) ;
#28276=PRESENTATION_STYLE_ASSIGNMENT (( #1160 ) ) ;
#28277=( LENGTH_UNIT ( ) NAMED_UNIT ( * ) SI_UNIT ( .MILLI., .METRE. ) );
#28280=COLOUR_RGB ( '', 0.72549020, 0.75294118, 0.79215686) ;
#28282=AXIS2_PLACEMENT_3D ( 'NONE', #60628, #18089, #39576 ) ;
#28285=CARTESIAN_POINT ( 'NONE',  ( -72.49999999999998579, 119.9999999999997868, 9.500000000000000000 ) ) ;
#28287=DIRECTION ( 'NONE',  ( 0.000000000000000000, -1.000000000000000000, 0.000000000000000000 ) ) ;
#28288=CARTESIAN_POINT ( 'NONE',  ( 9.827790563157511022E-16, 87.30187232391182306, -8.025000000000000355 ) ) ;
#28290=FILL_AREA_STYLE_COLOUR ( '', #24451 ) ;
#28294=DIRECTION ( 'NONE',  ( 0.000000000000000000, 0.000000000000000000, 1.000000000000000000 ) ) ;
#28301=COLOUR_RGB ( '', 0.31764706, 0.68627451, 0.89019608) ;
#28302=CARTESIAN_POINT ( 'NONE',  ( -4.716976649647098618, 119.2570736234661553, 6.492361379858953008 ) ) ;
#28304=( GEOMETRIC_REPRESENTATION_CONTEXT ( 3 ) GLOBAL_UNCERTAINTY_ASSIGNED_CONTEXT ( ( #46714 ) ) GLOBAL_UNIT_ASSIGNED_CONTEXT ( ( #14101, #61555, #51041 ) ) REPRESENTATION_CONTEXT ( 'NONE', 'WORKASPACE' ) );
#28306=DIRECTION ( 'NONE',  ( 0.000000000000000000, 0.000000000000000000, -1.000000000000000000 ) ) ;
#28308=CARTESIAN_POINT ( 'NONE',  ( 0.000000000000000000, 139.0570736234661808, -8.025000000000000355 ) ) ;
#28309=AXIS2_PLACEMENT_3D ( 'NONE', #63489, #10031, #47350 ) ;
#28310=DIRECTION ( 'NONE',  ( -0.000000000000000000, 0.000000000000000000, -1.000000000000000000 ) ) ;
#28316=FACE_OUTER_BOUND ( 'NONE', #58630, .T. ) ;
#28319=CARTESIAN_POINT ( 'NONE',  ( 0.000000000000000000, 134.9429263765338192, -8.025000000000000355 ) ) ;
#28321=ORIENTED_EDGE ( 'NONE', *, *, #8457, .F. ) ;
#28325=EDGE_CURVE ( 'NONE', #7688, #10952, #41828, .T. ) ;
#28326=SURFACE_STYLE_FILL_AREA ( #59663 ) ;
#28327=EDGE_LOOP ( 'NONE', ( #64958, #11469, #13039, #22229, #23403 ) ) ;
#28328=FACE_OUTER_BOUND ( 'NONE', #10780, .T. ) ;
#28329=EDGE_CURVE ( 'NONE', #60166, #7942, #8738, .T. ) ;
#28330=CIRCLE ( 'NONE', #25007, 0.5000000000000000000 ) ;
#28332=ORIENTED_EDGE ( 'NONE', *, *, #57598, .T. ) ;
#28335=ORIENTED_EDGE ( 'NONE', *, *, #24313, .F. ) ;
#28337=DIRECTION ( 'NONE',  ( 0.000000000000000000, 0.000000000000000000, 1.000000000000000000 ) ) ;
#28341=SURFACE_STYLE_USAGE ( .BOTH. , #66001 ) ;
#28345=COLOUR_RGB ( '', 0.08235294, 0.09019608, 0.10196078) ;
#28346=CARTESIAN_POINT ( 'NONE',  ( 51.49999999999998579, 2.837994680254535968E-15, 10.50000000000000000 ) ) ;
#28348=CARTESIAN_POINT ( 'NONE',  ( 6.826472737025121695, 122.4929263765338021, -4.959722759717905660 ) ) ;
#28350=EDGE_LOOP ( 'NONE', ( #63120, #6258, #19808, #31028 ) ) ;
#28352=CARTESIAN_POINT ( 'NONE',  ( -75.00000000000000000, 7.768687147774684831, 6.999999999999999112 ) ) ;
#28353=CARTESIAN_POINT ( 'NONE',  ( 15.98999599679679839, 118.4999999999999716, -7.500000000000000000 ) ) ;
#28357=ADVANCED_FACE ( 'NONE', ( #47103 ), #55220, .F. ) ;
#28358=VERTEX_POINT ( 'NONE', #52369 ) ;
#28359=CARTESIAN_POINT ( 'NONE',  ( 44.75458990717699947, 9.918196635725768928, 3.527112199763593914 ) ) ;
#28363=VECTOR ( 'NONE', #25759, 1000.000000000000000 ) ;
#28367=CARTESIAN_POINT ( 'NONE',  ( 9.058813317711338797, 142.9550000000000125, -2.943386871421372675 ) ) ;
#28368=CARTESIAN_POINT ( 'NONE',  ( 15.98999599679679839, 146.4999999999999716, -7.500000000000000000 ) ) ;
#28370=MECHANICAL_DESIGN_GEOMETRIC_PRESENTATION_REPRESENTATION('',(#50854),#3608);
#28371=CARTESIAN_POINT ( 'NONE',  ( 4.886038412224959160, 154.3548647706442409, 8.015157697667703474 ) ) ;
#28373=MECHANICAL_DESIGN_GEOMETRIC_PRESENTATION_REPRESENTATION('',(#32893),#67730);
#28376=CIRCLE ( 'NONE', #23894, 0.4999999999999994449 ) ;
#28377=DIRECTION ( 'NONE',  ( -0.000000000000000000, 1.000000000000000000, -0.000000000000000000 ) ) ;
#28380=( NAMED_UNIT ( * ) SI_UNIT ( $, .STERADIAN. ) SOLID_ANGLE_UNIT ( ) );
#28383=DIRECTION ( 'NONE',  ( -0.000000000000000000, -0.000000000000000000, 1.000000000000000000 ) ) ;
#28387=SURFACE_SIDE_STYLE ('',( #49545 ) ) ;
#28395=ORIENTED_EDGE ( 'NONE', *, *, #51536, .F. ) ;
#28401=SURFACE_SIDE_STYLE ('',( #33370 ) ) ;
#28405=AXIS2_PLACEMENT_3D ( 'NONE', #30861, #14705, #9082 ) ;
#28406=CARTESIAN_POINT ( 'NONE',  ( -9.159675819040165479, 110.5000000000000000, -2.649765445813976328 ) ) ;
#28410=CARTESIAN_POINT ( 'NONE',  ( 6.826472737025119919, 133.8929263765338078, 4.959722759717908325 ) ) ;
#28413=ADVANCED_FACE ( 'NONE', ( #36195 ), #57625, .T. ) ;
#28415=CARTESIAN_POINT ( 'NONE',  ( -34.99999999999999289, 99.99999999999998579, 9.500000000000000000 ) ) ;
#28418=CARTESIAN_POINT ( 'NONE',  ( 51.99999999999998579, 1.797044900979284448E-15, -11.50000000000000000 ) ) ;
#28420=( LENGTH_UNIT ( ) NAMED_UNIT ( * ) SI_UNIT ( .MILLI., .METRE. ) );
#28427=COLOUR_RGB ( '', 0.72549020, 0.75294118, 0.79215686) ;
#28430=EDGE_LOOP ( 'NONE', ( #23374, #49998, #23335, #68035 ) ) ;
#28435=FILL_AREA_STYLE_COLOUR ( '', #10662 ) ;
#28436=VERTEX_POINT ( 'NONE', #53710 ) ;
#28438=FILL_AREA_STYLE ('',( #39754 ) ) ;
#28442=FILL_AREA_STYLE_COLOUR ( '', #6180 ) ;
#28446=STYLED_ITEM ( 'NONE', ( #23918 ), #8906 ) ;
#28450=DIRECTION ( 'NONE',  ( 1.000000000000000000, 0.000000000000000000, 0.000000000000000000 ) ) ;
#28454=CARTESIAN_POINT ( 'NONE',  ( -3.094860106618434248, 117.9049999999999727, 9.525000000000000355 ) ) ;
#28458=DIRECTION ( 'NONE',  ( 0.000000000000000000, 0.000000000000000000, 1.000000000000000000 ) ) ;
#28459=CIRCLE ( 'NONE', #35227, 26.49999999999999645 ) ;
#28460=FILL_AREA_STYLE ('',( #22881 ) ) ;
#28462=UNCERTAINTY_MEASURE_WITH_UNIT (LENGTH_MEASURE( 1.000000000000000082E-05 ), #2439, 'distance_accuracy_value', 'NONE');
#28466=FILL_AREA_STYLE ('',( #65788 ) ) ;
#28467=ORIENTED_EDGE ( 'NONE', *, *, #8606, .F. ) ;
#28468=STYLED_ITEM ( 'NONE', ( #7828 ), #2312 ) ;
#28472=FILL_AREA_STYLE ('',( #39095 ) ) ;
#28473=CONICAL_SURFACE ( 'NONE', #62235, 8.025000000000000355, 0.7853981633974421728 ) ;
#28476=ORIENTED_EDGE ( 'NONE', *, *, #69259, .F. ) ;
#28477=ORIENTED_EDGE ( 'NONE', *, *, #20988, .T. ) ;
#28479=PRESENTATION_STYLE_ASSIGNMENT (( #6004 ) ) ;
#28480=MECHANICAL_DESIGN_GEOMETRIC_PRESENTATION_REPRESENTATION('',(#43180),#37561);
#28484=CIRCLE ( 'NONE', #37564, 0.5000000000000004441 ) ;
#28485=ORIENTED_EDGE ( 'NONE', *, *, #20745, .T. ) ;
#28488=AXIS2_PLACEMENT_3D ( 'NONE', #14314, #67424, #62141 ) ;
#28489=EDGE_CURVE ( 'NONE', #38619, #54121, #44524, .T. ) ;
#28490=ORIENTED_EDGE ( 'NONE', *, *, #55524, .F. ) ;
#28491=DIRECTION ( 'NONE',  ( -0.000000000000000000, -0.000000000000000000, 1.000000000000000000 ) ) ;
#28494=FACE_OUTER_BOUND ( 'NONE', #37349, .T. ) ;
#28496=DIRECTION ( 'NONE',  ( 0.000000000000000000, 0.000000000000000000, 1.000000000000000000 ) ) ;
#28497=CARTESIAN_POINT ( 'NONE',  ( 8.102448949553183510, 129.9950000000000045, -5.886773742842746238 ) ) ;
#28499=( BOUNDED_CURVE ( )  B_SPLINE_CURVE ( 2, ( #51225, #29033, #18840, #61066, #25176, #29400, #61741, #3322, #45964, #30089, #45288, #40010, #13567, #51924, #19183, #35036, #46693, #23784, #56487, #50535, #2257, #51562, #68109, #34347, #67391, #2971, #9008, #55796, #66705, #12883, #18522, #61403, #8322, #24460, #62103, #13218, #67747, #14276, #50875, #13930, #8660, #2634, #35398, #56849, #24808, #24131, #46328, #34675, #45639, #19547, #41044, #62459, #30422, #35740, #20595, #69142, #42111, #10404, #57537, #68440, #25860, #20948, #16045, #42445, #15682, #58230, #31479, #10052, #53317, #15358, #63506, #47369, #48070, #52287, #4046, #63835, #9718, #36812, #68804, #42800, #57897, #26869, #26549, #37164, #58573, #4751, #58929, #52627, #47748, #5101, #31130, #52963, #37522, #10739, #32187, #69473, #20237, #31827, #21263, #64188, #53638, #5423, #26206, #14633, #48407, #97, #30788, #41385, #62791, #36095, #9363, #25512, #4381, #36475, #47026, #41739, #63164, #15000, #39230, #64553, #59240, #6148, #11063, #27579, #38195, #12103, #6473, #33569, #33232, #32510, #33906, #27222, #1142, #50120, #49419, #55002, #55373, #16394, #27907, #11769, #60629, #5775, #21628, #48760, #43144, #49096, #17078, #22676, #12444, #28253, #44525, #59598, #43821, #38894, #1502, #37869, #65578, #60300, #17428, #23030, #21992, #64878, #781, #16731, #65229, #7195, #6830, #22325, #44179, #38557, #49764, #53974, #463, #59950, #43495, #65929, #54326, #11416, #32890, #54672, #17758, #28623, #45563, #24056, #56053, #8584, #12801, #34268, #51152, #39930, #2547, #29318, #66265, #13487, #34959, #18776, #23708, #61333, #62022, #2899, #24727, #13851, #13143, #66983, #46245, #67665, #40968, #35316, #28956, #24387, #45884, #67313, #19102, #35661, #62387, #30343, #56772, #7869, #1847, #50798, #18091, #40254, #40608, #51481, #34598, #66628, #18445, #23358, #3239, #30018, #14203, #19465, #57099, #8920, #61656, #39577, #56405, #8241, #44859, #29683, #60982, #55723, #7529, #50447, #2176, #45207, #68032, #15611, #31057, #25780, #46611, #36744, #52551, #58159, #58845, #15965, #42025, #19818, #69066, #63431, #63075, #42713, #58496, #5023, #20147, #4297, #20872, #31747, #41305, #26125, #42374, #47661, #53235, #52206, #52889, #41657, #63760, #62706, #51847, #37085, #47292, #9975, #68720, #10321, #14536, #9280, #36398, #36013, #26476, #14914, #30698, #3594, #57813, #15278, #4672, #48001, #20517 ),
 .UNSPECIFIED., .F., .F. ) 
 B_SPLINE_CURVE_WITH_KNOTS ( ( 3, 2, 2, 2, 2, 2, 2, 2, 2, 2, 2, 2, 2, 2, 2, 2, 2, 2, 2, 2, 2, 2, 2, 2, 2, 2, 2, 2, 2, 2, 2, 2, 2, 2, 2, 2, 2, 2, 2, 2, 2, 2, 2, 2, 2, 2, 2, 2, 2, 2, 2, 2, 2, 2, 2, 2, 2, 2, 2, 2, 2, 2, 2, 2, 2, 2, 2, 2, 2, 2, 2, 2, 2, 2, 2, 2, 2, 2, 2, 2, 2, 2, 2, 2, 2, 2, 2, 2, 2, 2, 2, 2, 2, 2, 2, 2, 2, 2, 2, 2, 2, 2, 2, 2, 2, 2, 2, 2, 2, 2, 2, 2, 2, 2, 2, 2, 2, 2, 2, 2, 2, 2, 2, 2, 2, 2, 2, 2, 2, 2, 2, 2, 2, 2, 2, 2, 2, 2, 2, 2, 2, 2, 2, 2, 2, 2, 2, 2, 3 ),
 ( 0.02068387785645816809, 0.02352941176470588203, 0.02941176470588235253, 0.03529411764705882304, 0.04117647058823529355, 0.04705882352941176405, 0.05294117647058824150, 0.05882352941176470507, 0.06470588235294118251, 0.07058823529411764608, 0.07647058823529412352, 0.08235294117647057321, 0.08823529411764706454, 0.09411764705882352811, 0.1000000000000000056, 0.1058823529411764691, 0.1117647058823529466, 0.1176470588235294101, 0.1235294117647058876, 0.1294117647058823650, 0.1352941176470588147, 0.1411764705882352922, 0.1470588235294117696, 0.1529411764705882470, 0.1588235294117646967, 0.1647058823529411742, 0.1705882352941176516, 0.1764705882352941568, 0.1823529411764705788, 0.1882352941176470562, 0.1941176470588235337, 0.2000000000000000111, 0.2058823529411764608, 0.2117647058823529382, 0.2176470588235294157, 0.2235294117647058931, 0.2294117647058823428, 0.2352941176470588203, 0.2411764705882352977, 0.2470588235294117752, 0.2529411764705882248, 0.2588235294117647300, 0.2647058823529411797, 0.2705882352941176294, 0.2764705882352941346, 0.2823529411764705843, 0.2882352941176470340, 0.2941176470588235392, 0.2999999999999999889, 0.3058823529411764941, 0.3117647058823529438, 0.3176470588235293935, 0.3235294117647059542, 0.3294117647058822929, 0.3352941176470587981, 0.3411764705882353033, 0.3470588235294117530, 0.3529411764705882582, 0.3588235294117647078, 0.3647058823529412130, 0.3705882352941176627, 0.3764705882352941124, 0.3823529411764705621, 0.3882352941176470673, 0.3941176470588235170, 0.4000000000000000222, 0.4058823529411764719, 0.4117647058823529216, 0.4176470588235294268, 0.4235294117647058765, 0.4294117647058823262, 0.4352941176470587759, 0.4411764705882352811, 0.4470588235294117863, 0.4529411764705882359, 0.4588235294117646856, 0.4647058823529411908, 0.4705882352941176960, 0.4764705882352940902, 0.4823529411764705954, 0.4882352941176470451, 0.4941176470588235503, 0.5000000000000000000, 0.5058823529411765607, 0.5117647058823528994, 0.5176470588235294601, 0.5235294117647059098, 0.5294117647058823595, 0.5352941176470588092, 0.5411764705882352589, 0.5470588235294118196, 0.5529411764705882693, 0.5588235294117647189, 0.5647058823529411686, 0.5705882352941176183, 0.5764705882352940680, 0.5823529411764706287, 0.5882352941176470784, 0.5941176470588235281, 0.5999999999999999778, 0.6058823529411764275, 0.6117647058823529882, 0.6176470588235294379, 0.6235294117647058876, 0.6294117647058823373, 0.6352941176470587870, 0.6411764705882353477, 0.6470588235294117974, 0.6529411764705882470, 0.6588235294117646967, 0.6647058823529411464, 0.6705882352941175961, 0.6764705882352941568, 0.6823529411764706065, 0.6882352941176470562, 0.6941176470588235059, 0.6999999999999999556, 0.7058823529411765163, 0.7117647058823529660, 0.7176470588235294157, 0.7235294117647058654, 0.7294117647058823151, 0.7352941176470588758, 0.7411764705882352144, 0.7470588235294117752, 0.7529411764705882248, 0.7588235294117646745, 0.7647058823529411242, 0.7705882352941177960, 0.7764705882352941346, 0.7823529411764704733, 0.7882352941176470340, 0.7941176470588234837, 0.8000000000000000444, 0.8058823529411764941, 0.8117647058823530548, 0.8176470588235293935, 0.8235294117647058432, 0.8294117647058824039, 0.8352941176470588536, 0.8411764705882353033, 0.8470588235294117530, 0.8529411764705883137, 0.8588235294117646523, 0.8647058823529412130, 0.8705882352941176627, 0.8764705882352941124, 0.8823529411764705621, 0.8834592151850780839 ),
 .UNSPECIFIED. ) 
 CURVE ( )  GEOMETRIC_REPRESENTATION_ITEM ( )  RATIONAL_B_SPLINE_CURVE ( ( 0.9755541358147095110, 0.9763240417801153370, 1.000000000000000000, 0.9510565162951535312, 1.000000000000000000, 0.9510565162951535312, 1.000000000000000000, 0.9510565162951535312, 1.000000000000000000, 0.9510565162951535312, 1.000000000000000000, 0.9510565162951535312, 1.000000000000000000, 0.9510565162951535312, 1.000000000000000000, 0.9510565162951535312, 1.000000000000000000, 0.9510565162951535312, 1.000000000000000000, 0.9510565162951535312, 1.000000000000000000, 0.9510565162951535312, 1.000000000000000000, 0.9510565162951535312, 1.000000000000000000, 0.9510565162951535312, 1.000000000000000000, 0.9510565162951535312, 1.000000000000000000, 0.9510565162951535312, 1.000000000000000000, 0.9510565162951535312, 1.000000000000000000, 0.9510565162951535312, 1.000000000000000000, 0.9510565162951535312, 1.000000000000000000, 0.9510565162951535312, 1.000000000000000000, 0.9510565162951535312, 1.000000000000000000, 0.9510565162951535312, 1.000000000000000000, 0.9510565162951535312, 1.000000000000000000, 0.9510565162951535312, 1.000000000000000000, 0.9510565162951535312, 1.000000000000000000, 0.9510565162951535312, 1.000000000000000000, 0.9510565162951535312, 1.000000000000000000, 0.9510565162951535312, 1.000000000000000000, 0.9510565162951535312, 1.000000000000000000, 0.9510565162951535312, 1.000000000000000000, 0.9510565162951535312, 1.000000000000000000, 0.9510565162951535312, 1.000000000000000000, 0.9510565162951535312, 1.000000000000000000, 0.9510565162951535312, 1.000000000000000000, 0.9510565162951535312, 1.000000000000000000, 0.9510565162951535312, 1.000000000000000000, 0.9510565162951535312, 1.000000000000000000, 0.9510565162951535312, 1.000000000000000000, 0.9510565162951535312, 1.000000000000000000, 0.9510565162951535312, 1.000000000000000000, 0.9510565162951535312, 1.000000000000000000, 0.9510565162951535312, 1.000000000000000000, 0.9510565162951535312, 1.000000000000000000, 0.9510565162951535312, 1.000000000000000000, 0.9510565162951535312, 1.000000000000000000, 0.9510565162951535312, 1.000000000000000000, 0.9510565162951535312, 1.000000000000000000, 0.9510565162951535312, 1.000000000000000000, 0.9510565162951535312, 1.000000000000000000, 0.9510565162951535312, 1.000000000000000000, 0.9510565162951535312, 1.000000000000000000, 0.9510565162951535312, 1.000000000000000000, 0.9510565162951535312, 1.000000000000000000, 0.9510565162951535312, 1.000000000000000000, 0.9510565162951535312, 1.000000000000000000, 0.9510565162951535312, 1.000000000000000000, 0.9510565162951535312, 1.000000000000000000, 0.9510565162951535312, 1.000000000000000000, 0.9510565162951535312, 1.000000000000000000, 0.9510565162951535312, 1.000000000000000000, 0.9510565162951535312, 1.000000000000000000, 0.9510565162951535312, 1.000000000000000000, 0.9510565162951535312, 1.000000000000000000, 0.9510565162951535312, 1.000000000000000000, 0.9510565162951535312, 1.000000000000000000, 0.9510565162951535312, 1.000000000000000000, 0.9510565162951535312, 1.000000000000000000, 0.9510565162951535312, 1.000000000000000000, 0.9510565162951535312, 1.000000000000000000, 0.9510565162951535312, 1.000000000000000000, 0.9510565162951535312, 1.000000000000000000, 0.9510565162951535312, 1.000000000000000000, 0.9510565162951535312, 1.000000000000000000, 0.9510565162951535312, 1.000000000000000000, 0.9510565162951535312, 1.000000000000000000, 0.9510565162951535312, 1.000000000000000000, 0.9510565162951535312, 1.000000000000000000, 0.9510565162951535312, 1.000000000000000000, 0.9510565162951535312, 1.000000000000000000, 0.9510565162951535312, 1.000000000000000000, 0.9510565162951535312, 1.000000000000000000, 0.9510565162951535312, 1.000000000000000000, 0.9510565162951535312, 1.000000000000000000, 0.9510565162951535312, 1.000000000000000000, 0.9510565162951535312, 1.000000000000000000, 0.9510565162951535312, 1.000000000000000000, 0.9510565162951535312, 1.000000000000000000, 0.9510565162951535312, 1.000000000000000000, 0.9510565162951535312, 1.000000000000000000, 0.9510565162951535312, 1.000000000000000000, 0.9510565162951535312, 1.000000000000000000, 0.9510565162951535312, 1.000000000000000000, 0.9510565162951535312, 1.000000000000000000, 0.9510565162951535312, 1.000000000000000000, 0.9510565162951535312, 1.000000000000000000, 0.9510565162951535312, 1.000000000000000000, 0.9510565162951535312, 1.000000000000000000, 0.9510565162951535312, 1.000000000000000000, 0.9510565162951535312, 1.000000000000000000, 0.9510565162951535312, 1.000000000000000000, 0.9510565162951535312, 1.000000000000000000, 0.9510565162951535312, 1.000000000000000000, 0.9510565162951535312, 1.000000000000000000, 0.9510565162951535312, 1.000000000000000000, 0.9510565162951535312, 1.000000000000000000, 0.9510565162951535312, 1.000000000000000000, 0.9510565162951535312, 1.000000000000000000, 0.9510565162951535312, 1.000000000000000000, 0.9510565162951535312, 1.000000000000000000, 0.9510565162951535312, 1.000000000000000000, 0.9510565162951535312, 1.000000000000000000, 0.9510565162951535312, 1.000000000000000000, 0.9510565162951535312, 1.000000000000000000, 0.9510565162951535312, 1.000000000000000000, 0.9510565162951535312, 1.000000000000000000, 0.9510565162951535312, 1.000000000000000000, 0.9510565162951535312, 1.000000000000000000, 0.9510565162951535312, 1.000000000000000000, 0.9510565162951535312, 1.000000000000000000, 0.9510565162951535312, 1.000000000000000000, 0.9510565162951535312, 1.000000000000000000, 0.9510565162951535312, 1.000000000000000000, 0.9510565162951535312, 1.000000000000000000, 0.9510565162951535312, 1.000000000000000000, 0.9510565162951535312, 1.000000000000000000, 0.9510565162951535312, 1.000000000000000000, 0.9510565162951535312, 1.000000000000000000, 0.9510565162951535312, 1.000000000000000000, 0.9510565162951535312, 1.000000000000000000, 0.9510565162951535312, 1.000000000000000000, 0.9510565162951535312, 1.000000000000000000, 0.9510565162951535312, 1.000000000000000000, 0.9510565162951535312, 1.000000000000000000, 0.9510565162951535312, 1.000000000000000000, 0.9510565162951535312, 1.000000000000000000, 0.9510565162951535312, 1.000000000000000000, 0.9510565162951535312, 1.000000000000000000, 0.9510565162951535312, 1.000000000000000000, 0.9510565162951535312, 1.000000000000000000, 0.9510565162951535312, 1.000000000000000000, 0.9510565162951535312, 1.000000000000000000, 0.9510565162951535312, 1.000000000000000000, 0.9510565162951535312, 1.000000000000000000, 0.9510565162951535312, 1.000000000000000000, 0.9510565162951535312, 1.000000000000000000, 0.9510565162951535312, 1.000000000000000000, 0.9510565162951535312, 1.000000000000000000, 0.9510565162951535312, 1.000000000000000000, 0.9907953663347257578, 0.9850529006435514434 ) ) 
 REPRESENTATION_ITEM ( '' )  );
#28500=COLOUR_RGB ( '', 0.66274510, 0.83137255, 0.94901961) ;
#28504=CARTESIAN_POINT ( 'NONE',  ( -1.166476076187854022E-15, 127.0549999999999784, 9.525000000000000355 ) ) ;
#28507=CARTESIAN_POINT ( 'NONE',  ( 40.99999999999998579, 108.0041655821620026, -3.000000000000000888 ) ) ;
#28509=CARTESIAN_POINT ( 'NONE',  ( 5.598654528085805993, 157.3549999999999898, 7.705886871421374629 ) ) ;
#28510=DIRECTION ( 'NONE',  ( -0.000000000000000000, -0.000000000000000000, -1.000000000000000000 ) ) ;
#28515=SURFACE_SIDE_STYLE ('',( #53875 ) ) ;
#28518=( NAMED_UNIT ( * ) PLANE_ANGLE_UNIT ( ) SI_UNIT ( $, .RADIAN. ) );
#28520=MECHANICAL_DESIGN_GEOMETRIC_PRESENTATION_REPRESENTATION('',(#10580),#9538);
#28521=STYLED_ITEM ( 'NONE', ( #16090 ), #61952 ) ;
#28525=ORIENTED_EDGE ( 'NONE', *, *, #58427, .T. ) ;
#28526=UNCERTAINTY_MEASURE_WITH_UNIT (LENGTH_MEASURE( 1.000000000000000082E-05 ), #3058, 'distance_accuracy_value', 'NONE');
#28527=( NAMED_UNIT ( * ) PLANE_ANGLE_UNIT ( ) SI_UNIT ( $, .RADIAN. ) );
#28529=DIRECTION ( 'NONE',  ( 0.000000000000000000, -0.000000000000000000, -1.000000000000000000 ) ) ;
#28535=COLOUR_RGB ( '', 0.66274510, 0.83137255, 0.94901961) ;
#28539=CARTESIAN_POINT ( 'NONE',  ( -74.99999999999998579, 50.00000000000000000, -9.500000000000001776 ) ) ;
#28540=MECHANICAL_DESIGN_GEOMETRIC_PRESENTATION_REPRESENTATION('',(#1536),#60034);
#28543=CIRCLE ( 'NONE', #56690, 0.5000000000000004441 ) ;
#28546=CARTESIAN_POINT ( 'NONE',  ( 3.094860106618431583, 129.0949999999999704, 9.525000000000000355 ) ) ;
#28549=( LENGTH_UNIT ( ) NAMED_UNIT ( * ) SI_UNIT ( .MILLI., .METRE. ) );
#28550=MECHANICAL_DESIGN_GEOMETRIC_PRESENTATION_REPRESENTATION('',(#49938),#48857);
#28558=( LENGTH_UNIT ( ) NAMED_UNIT ( * ) SI_UNIT ( .MILLI., .METRE. ) );
#28559=VERTEX_POINT ( 'NONE', #47463 ) ;
#28561=ORIENTED_EDGE ( 'NONE', *, *, #55032, .T. ) ;
#28568=CARTESIAN_POINT ( 'NONE',  ( 44.81371295029482837, 9.999999999999978684, -3.255911637198365405 ) ) ;
#28569=EDGE_CURVE ( 'NONE', #6428, #45911, #15769, .T. ) ;
#28576=FACE_OUTER_BOUND ( 'NONE', #16984, .T. ) ;
#28580=EDGE_CURVE ( 'NONE', #44927, #12184, #56052, .T. ) ;
#28581=CARTESIAN_POINT ( 'NONE',  ( 2.607480562269076430, 153.9070736234662036, -8.025000000000000355 ) ) ;
#28583=DIRECTION ( 'NONE',  ( 0.000000000000000000, 0.000000000000000000, 1.000000000000000000 ) ) ;
#28585=EDGE_CURVE ( 'NONE', #24967, #10181, #23796, .T. ) ;
#28590=CARTESIAN_POINT ( 'NONE',  ( 5.598654528085809545, 128.2549999999999670, -7.705886871421373741 ) ) ;
#28592=SURFACE_STYLE_FILL_AREA ( #7162 ) ;
#28594=DIRECTION ( 'NONE',  ( 0.000000000000000000, 0.000000000000000000, -1.000000000000000000 ) ) ;
#28595=CARTESIAN_POINT ( 'NONE',  ( 44.99999999999977973, 146.4999999999999716, -7.000000000000000000 ) ) ;
#28596=ORIENTED_EDGE ( 'NONE', *, *, #1046, .T. ) ;
#28606=FILL_AREA_STYLE_COLOUR ( '', #10477 ) ;
#28614=PRESENTATION_STYLE_ASSIGNMENT (( #12795 ) ) ;
#28615=FILL_AREA_STYLE_COLOUR ( '', #2696 ) ;
#28616=SURFACE_STYLE_FILL_AREA ( #12797 ) ;
#28617=DIRECTION ( 'NONE',  ( -0.000000000000000000, -0.000000000000000000, -1.000000000000000000 ) ) ;
#28618=AXIS2_PLACEMENT_3D ( 'NONE', #3017, #35084, #67100 ) ;
#28623=CARTESIAN_POINT ( 'NONE',  ( -8.102448949553179958, 137.4950000000000045, 5.886773742842747126 ) ) ;
#28625=EDGE_CURVE ( 'NONE', #5088, #44431, #50772, .T. ) ;
#28629=VECTOR ( 'NONE', #60710, 1000.000000000000000 ) ;
#28630=FILL_AREA_STYLE_COLOUR ( '', #16702 ) ;
#28631=SPHERICAL_SURFACE ( 'NONE', #17842, 0.5000000000000000000 ) ;
#28633=COLOUR_RGB ( '', 0.66274510, 0.83137255, 0.94901961) ;
#28636=SURFACE_SIDE_STYLE ('',( #50128 ) ) ;
#28639=DIRECTION ( 'NONE',  ( 1.000000000000000000, 0.000000000000000000, 0.000000000000000000 ) ) ;
#28641=AXIS2_PLACEMENT_3D ( 'NONE', #44489, #23323, #18739 ) ;
#28642=DIRECTION ( 'NONE',  ( 0.000000000000000000, -1.000000000000000000, 0.000000000000000000 ) ) ;
#28651=DIRECTION ( 'NONE',  ( -0.000000000000000000, 1.000000000000000000, -0.000000000000000000 ) ) ;
#28655=EDGE_CURVE ( 'NONE', #12255, #11851, #67639, .T. ) ;
#28656=TOROIDAL_SURFACE ( 'NONE', #23063, 7.500000000000011546, 0.5000000000000000000 ) ;
#28657=SURFACE_STYLE_FILL_AREA ( #12133 ) ;
#28659=CARTESIAN_POINT ( 'NONE',  ( -41.61090298506120888, 107.5097581389847647, 4.000000003093457046 ) ) ;
#28660=MECHANICAL_DESIGN_GEOMETRIC_PRESENTATION_REPRESENTATION('',(#42203),#12953);
#28662=ORIENTED_EDGE ( 'NONE', *, *, #52618, .F. ) ;
#28665=VECTOR ( 'NONE', #48895, 1000.000000000000000 ) ;
#28666=ORIENTED_EDGE ( 'NONE', *, *, #47146, .F. ) ;
#28669=CARTESIAN_POINT ( 'NONE',  ( 7.632228543268607446, 120.1570736234661609, 2.479861379858954606 ) ) ;
#28670=( NAMED_UNIT ( * ) SI_UNIT ( $, .STERADIAN. ) SOLID_ANGLE_UNIT ( ) );
#28671=EDGE_CURVE ( 'NONE', #28083, #2689, #26052, .T. ) ;
#28678=CARTESIAN_POINT ( 'NONE',  ( -45.00000000000000000, 9.708372675170618749, 6.000000000000000888 ) ) ;
#28679=COLOUR_RGB ( '', 0.09019608, 0.27058824, 0.51372549) ;
#28683=CIRCLE ( 'NONE', #37756, 0.5000000000000004441 ) ;
#28685=CARTESIAN_POINT ( 'NONE',  ( 45.54151037965569770, 9.791825115387426948, 6.500000000000000888 ) ) ;
#28687=STYLED_ITEM ( 'NONE', ( #43847 ), #32306 ) ;
#28689=FILL_AREA_STYLE ('',( #51547 ) ) ;
#28690=FACE_OUTER_BOUND ( 'NONE', #48176, .T. ) ;
#28692=ORIENTED_EDGE ( 'NONE', *, *, #4425, .T. ) ;
#28694=ORIENTED_EDGE ( 'NONE', *, *, #32371, .F. ) ;
#28696=DIRECTION ( 'NONE',  ( 1.000000000000000000, 0.000000000000000000, 0.000000000000000000 ) ) ;
#28697=CARTESIAN_POINT ( 'NONE',  ( -23.21231517720797655, 117.9999999999999716, 7.500000000000000000 ) ) ;
#28699=LINE ( 'NONE', #33645, #28629 ) ;
#28703=TOROIDAL_SURFACE ( 'NONE', #32140, 18.50000000000000355, 0.5000000000000000000 ) ;
#28707=EDGE_CURVE ( 'NONE', #20368, #12157, #28330, .T. ) ;
#28709=( LENGTH_UNIT ( ) NAMED_UNIT ( * ) SI_UNIT ( .MILLI., .METRE. ) );
#28710=AXIS2_PLACEMENT_3D ( 'NONE', #62872, #23868, #35478 ) ;
#28714=LINE ( 'NONE', #50546, #29685 ) ;
#28720=VERTEX_POINT ( 'NONE', #24055 ) ;
#28727=AXIS2_PLACEMENT_3D ( 'NONE', #22913, #22206, #43703 ) ;
#28730=CARTESIAN_POINT ( 'NONE',  ( -9.058813317711338797, 150.4550000000000125, 2.943386871421373563 ) ) ;
#28731=CARTESIAN_POINT ( 'NONE',  ( -75.00000000000000000, 7.768687147774684831, 6.999999999999999112 ) ) ;
#28733=AXIS2_PLACEMENT_3D ( 'NONE', #23276, #44773, #13398 ) ;
#28735=STYLED_ITEM ( 'NONE', ( #55147 ), #57156 ) ;
#28738=DIRECTION ( 'NONE',  ( -0.000000000000000000, -1.000000000000000000, -0.000000000000000000 ) ) ;
#28739=EDGE_CURVE ( 'NONE', #56203, #1355, #61655, .T. ) ;
#28740=CARTESIAN_POINT ( 'NONE',  ( -20.12916642283592950, 110.4999999999999858, 10.05319148936170137 ) ) ;
#28741=DIRECTION ( 'NONE',  ( -1.000000000000000000, 0.000000000000000000, 0.000000000000000000 ) ) ;
#28742=ADVANCED_FACE ( 'NONE', ( #66627 ), #34957, .T. ) ;
#28743=FILL_AREA_STYLE_COLOUR ( '', #28301 ) ;
#28745=ORIENTED_EDGE ( 'NONE', *, *, #19213, .T. ) ;
#28749=LINE ( 'NONE', #35783, #61942 ) ;
#28750=( NAMED_UNIT ( * ) PLANE_ANGLE_UNIT ( ) SI_UNIT ( $, .RADIAN. ) );
#28759=ORIENTED_EDGE ( 'NONE', *, *, #25278, .T. ) ;
#28763=MECHANICAL_DESIGN_GEOMETRIC_PRESENTATION_REPRESENTATION('',(#7404),#50145);
#28768=CARTESIAN_POINT ( 'NONE',  ( -74.50000000000000000, 7.768687147774688384, -6.500000000000000000 ) ) ;
#28770=DIRECTION ( 'NONE',  ( 0.000000000000000000, 1.000000000000000000, 0.000000000000000000 ) ) ;
#28772=CARTESIAN_POINT ( 'NONE',  ( 0.000000000000000000, 137.9429263765338192, -8.025000000000000355 ) ) ;
#28775=CARTESIAN_POINT ( 'NONE',  ( -74.99999999999998579, 50.00000000000000000, 12.00000000000000000 ) ) ;
#28777=CARTESIAN_POINT ( 'NONE',  ( -2.607480562269048896, 115.2929263765338135, 8.025000000000019895 ) ) ;
#28778=EDGE_LOOP ( 'NONE', ( #16467, #57576, #11053, #26084 ) ) ;
#28782=( GEOMETRIC_REPRESENTATION_CONTEXT ( 3 ) GLOBAL_UNCERTAINTY_ASSIGNED_CONTEXT ( ( #7941 ) ) GLOBAL_UNIT_ASSIGNED_CONTEXT ( ( #36733, #47991, #68018 ) ) REPRESENTATION_CONTEXT ( 'NONE', 'WORKASPACE' ) );
#28785=CARTESIAN_POINT ( 'NONE',  ( -44.99999999999977973, 149.4999999999999716, -10.00000000000000000 ) ) ;
#28787=FILL_AREA_STYLE_COLOUR ( '', #12850 ) ;
#28788=FACE_OUTER_BOUND ( 'NONE', #17383, .T. ) ;
#28791=CARTESIAN_POINT ( 'NONE',  ( -23.21231517720797655, 117.4999999999999716, -7.000000000000000000 ) ) ;
#28792=PRESENTATION_STYLE_ASSIGNMENT (( #49941 ) ) ;
#28796=CARTESIAN_POINT ( 'NONE',  ( 45.00000000000000000, 99.99999999999992895, -4.000000000000000000 ) ) ;
#28799=VERTEX_POINT ( 'NONE', #46952 ) ;
#28804=SURFACE_STYLE_USAGE ( .BOTH. , #13318 ) ;
#28806=CARTESIAN_POINT ( 'NONE',  ( 0.000000000000000000, 137.9429263765338192, -8.025000000000000355 ) ) ;
#28807=ADVANCED_FACE ( 'NONE', ( #68362 ), #37419, .T. ) ;
#28809=DIRECTION ( 'NONE',  ( -0.000000000000000000, -0.000000000000000000, 1.000000000000000000 ) ) ;
#28812=EDGE_CURVE ( 'NONE', #30560, #16813, #21010, .T. ) ;
#28814=EDGE_CURVE ( 'NONE', #9058, #65770, #46381, .T. ) ;
#28816=ADVANCED_FACE ( 'NONE', ( #16312 ), #1342, .F. ) ;
#28817=CARTESIAN_POINT ( 'NONE',  ( -5.598654528085806881, 116.8549999999999898, -7.705886871421374629 ) ) ;
#28822=( NAMED_UNIT ( * ) PLANE_ANGLE_UNIT ( ) SI_UNIT ( $, .RADIAN. ) );
#28825=( NAMED_UNIT ( * ) SI_UNIT ( $, .STERADIAN. ) SOLID_ANGLE_UNIT ( ) );
#28826=ORIENTED_EDGE ( 'NONE', *, *, #56619, .F. ) ;
#28829=ADVANCED_FACE ( 'NONE', ( #37791 ), #28174, .F. ) ;
#28831=SURFACE_SIDE_STYLE ('',( #7730 ) ) ;
#28832=DIRECTION ( 'NONE',  ( -1.000000000000000000, 0.000000000000000000, 0.000000000000000000 ) ) ;
#28833=ORIENTED_EDGE ( 'NONE', *, *, #39354, .F. ) ;
#28834=ORIENTED_EDGE ( 'NONE', *, *, #42401, .F. ) ;
#28840=PRESENTATION_STYLE_ASSIGNMENT (( #60853 ) ) ;
#28843=ORIENTED_EDGE ( 'NONE', *, *, #42284, .F. ) ;
#28846=SURFACE_STYLE_USAGE ( .BOTH. , #48983 ) ;
#28847=ORIENTED_EDGE ( 'NONE', *, *, #15594, .F. ) ;
#28849=ADVANCED_FACE ( 'NONE', ( #64468 ), #32432, .F. ) ;
#28850=CARTESIAN_POINT ( 'NONE',  ( -23.21231517720797655, 117.4999999999999716, 7.500000000000000000 ) ) ;
#28851=CARTESIAN_POINT ( 'NONE',  ( 5.598654528085805993, 138.2449999999999761, 7.705886871421374629 ) ) ;
#28853=CARTESIAN_POINT ( 'NONE',  ( -44.99999999999977973, 149.9999999999999716, 9.500000000000000000 ) ) ;
#28854=CARTESIAN_POINT ( 'NONE',  ( 9.058813317711338797, 142.9550000000000125, -2.943386871421372675 ) ) ;
#28856=CARTESIAN_POINT ( 'NONE',  ( 41.49999999999997868, 106.9282032302754999, -3.500000000000000888 ) ) ;
#28858=ORIENTED_EDGE ( 'NONE', *, *, #20834, .T. ) ;
#28859=CARTESIAN_POINT ( 'NONE',  ( 5.598654528085805993, 154.3549999999999898, 7.705886871421374629 ) ) ;
#28860=LINE ( 'NONE', #38452, #4105 ) ;
#28861=SURFACE_STYLE_USAGE ( .BOTH. , #7440 ) ;
#28863=AXIS2_PLACEMENT_3D ( 'NONE', #23093, #23411, #33630 ) ;
#28866=EDGE_LOOP ( 'NONE', ( #62712, #22152, #24612 ) ) ;
#28868=CARTESIAN_POINT ( 'NONE',  ( 60.00000000000000000, 1.797044900979284448E-15, -6.500000000000000000 ) ) ;
#28872=SURFACE_STYLE_USAGE ( .BOTH. , #56305 ) ;
#28873=FILL_AREA_STYLE ('',( #54232 ) ) ;
#28875=ORIENTED_EDGE ( 'NONE', *, *, #41104, .F. ) ;
#28877=( GEOMETRIC_REPRESENTATION_CONTEXT ( 3 ) GLOBAL_UNCERTAINTY_ASSIGNED_CONTEXT ( ( #20037 ) ) GLOBAL_UNIT_ASSIGNED_CONTEXT ( ( #52264, #25152, #46666 ) ) REPRESENTATION_CONTEXT ( 'NONE', 'WORKASPACE' ) );
#28878=LINE ( 'NONE', #55279, #48181 ) ;
#28883=DIRECTION ( 'NONE',  ( 0.000000000000000000, 0.000000000000000000, 1.000000000000000000 ) ) ;
#28884=SURFACE_STYLE_USAGE ( .BOTH. , #45129 ) ;
#28886=EDGE_CURVE ( 'NONE', #48195, #35826, #29519, .T. ) ;
#28892=CARTESIAN_POINT ( 'NONE',  ( 8.102448949553181734, 141.3949999999999818, 5.886773742842750679 ) ) ;
#28901=EDGE_CURVE ( 'NONE', #19491, #29473, #45128, .T. ) ;
#28902=COLOUR_RGB ( '', 0.72549020, 0.75294118, 0.79215686) ;
#28904=SURFACE_STYLE_USAGE ( .BOTH. , #56713 ) ;
#28905=ORIENTED_EDGE ( 'NONE', *, *, #53850, .F. ) ;
#28906=EDGE_LOOP ( 'NONE', ( #39967, #18319, #61852, #53223 ) ) ;
#28910=FILL_AREA_STYLE ('',( #66934 ) ) ;
#28913=COLOUR_RGB ( '', 0.31764706, 0.68627451, 0.89019608) ;
#28915=( GEOMETRIC_REPRESENTATION_CONTEXT ( 3 ) GLOBAL_UNCERTAINTY_ASSIGNED_CONTEXT ( ( #20763 ) ) GLOBAL_UNIT_ASSIGNED_CONTEXT ( ( #3119, #41204, #64706 ) ) REPRESENTATION_CONTEXT ( 'NONE', 'WORKASPACE' ) );
#28920=( NAMED_UNIT ( * ) SI_UNIT ( $, .STERADIAN. ) SOLID_ANGLE_UNIT ( ) );
#28922=SURFACE_STYLE_FILL_AREA ( #61296 ) ;
#28923=CARTESIAN_POINT ( 'NONE',  ( -7.632228543268607446, 151.6570736234661751, -2.479861379858953718 ) ) ;
#28925=FACE_OUTER_BOUND ( 'NONE', #15474, .T. ) ;
#28926=CARTESIAN_POINT ( 'NONE',  ( 3.094860106618435136, 113.4049999999999869, -9.525000000000000355 ) ) ;
#28929=CARTESIAN_POINT ( 'NONE',  ( -1.166476076187854022E-15, 133.0549999999999784, 9.525000000000000355 ) ) ;
#28931=SURFACE_STYLE_FILL_AREA ( #7505 ) ;
#28933=CARTESIAN_POINT ( 'NONE',  ( -45.50000000000000000, 99.99999999999992895, 10.00000000000000000 ) ) ;
#28938=DIRECTION ( 'NONE',  ( -0.000000000000000000, 1.000000000000000000, -0.000000000000000000 ) ) ;
#28940=CARTESIAN_POINT ( 'NONE',  ( -15.98999599679679839, 118.4999999999999716, -7.500000000000000000 ) ) ;
#28941=ORIENTED_EDGE ( 'NONE', *, *, #24134, .T. ) ;
#28944=SURFACE_STYLE_FILL_AREA ( #14195 ) ;
#28945=VERTEX_POINT ( 'NONE', #2097 ) ;
#28947=AXIS2_PLACEMENT_3D ( 'NONE', #4053, #32195, #47032 ) ;
#28948=CARTESIAN_POINT ( 'NONE',  ( -74.41756005331312451, 8.116436936526460144, 6.493641663363979077 ) ) ;
#28950=ORIENTED_EDGE ( 'NONE', *, *, #6042, .T. ) ;
#28953=CARTESIAN_POINT ( 'NONE',  ( 34.99999999999999289, 99.99999999999998579, 10.00000000000000000 ) ) ;
#28955=DIRECTION ( 'NONE',  ( 0.000000000000000000, 0.000000000000000000, 1.000000000000000000 ) ) ;
#28956=CARTESIAN_POINT ( 'NONE',  ( 9.058813317711337021, 141.5449999999999875, 2.943386871421375783 ) ) ;
#28958=PRESENTATION_STYLE_ASSIGNMENT (( #60631 ) ) ;
#28959=CARTESIAN_POINT ( 'NONE',  ( 15.98999599679679839, 146.4999999999999716, 7.500000000000000000 ) ) ;
#28964=DIRECTION ( 'NONE',  ( -0.000000000000000000, 1.000000000000000000, -0.000000000000000000 ) ) ;
#28970=CARTESIAN_POINT ( 'NONE',  ( 44.99999999999977973, 149.4999999999999716, 10.00000000000000000 ) ) ;
#28972=EDGE_CURVE ( 'NONE', #33857, #51702, #50863, .T. ) ;
#28981=CARTESIAN_POINT ( 'NONE',  ( 9.827790563157511022E-16, 87.30187232391182306, -8.025000000000000355 ) ) ;
#28986=( GEOMETRIC_REPRESENTATION_CONTEXT ( 3 ) GLOBAL_UNCERTAINTY_ASSIGNED_CONTEXT ( ( #15184 ) ) GLOBAL_UNIT_ASSIGNED_CONTEXT ( ( #8547, #3188, #3552 ) ) REPRESENTATION_CONTEXT ( 'NONE', 'WORKASPACE' ) );
#28988=DIRECTION ( 'NONE',  ( 1.000000000000000000, 0.000000000000000000, 0.000000000000000000 ) ) ;
#28993=DIRECTION ( 'NONE',  ( -0.000000000000000000, -1.000000000000000000, 0.000000000000000000 ) ) ;
#28994=CARTESIAN_POINT ( 'NONE',  ( 48.50000000000000000, 14.49137674618942562, 7.500000000000000000 ) ) ;
#28996=STYLED_ITEM ( 'NONE', ( #49323 ), #50993 ) ;
#28997=VECTOR ( 'NONE', #28964, 1000.000000000000000 ) ;
#28999=VERTEX_POINT ( 'NONE', #37000 ) ;
#29000=LINE ( 'NONE', #38324, #62340 ) ;
#29001=CARTESIAN_POINT ( 'NONE',  ( 2.755455298081543989E-15, 154.9999999999999716, 22.49999999999999645 ) ) ;
#29003=CARTESIAN_POINT ( 'NONE',  ( 0.000000000000000000, 133.0570736234661524, -8.025000000000000355 ) ) ;
#29005=CARTESIAN_POINT ( 'NONE',  ( 6.826472737025119919, 126.0070736234661695, 4.959722759717908325 ) ) ;
#29008=( NAMED_UNIT ( * ) PLANE_ANGLE_UNIT ( ) SI_UNIT ( $, .RADIAN. ) );
#29014=DIRECTION ( 'NONE',  ( 1.000000000000000000, 0.000000000000000000, 0.000000000000000000 ) ) ;
#29016=VERTEX_POINT ( 'NONE', #62304 ) ;
#29017=CARTESIAN_POINT ( 'NONE',  ( -20.54889675933014814, 114.6603872790887095, -10.28544290717500509 ) ) ;
#29020=ORIENTED_EDGE ( 'NONE', *, *, #38697, .T. ) ;
#29021=SURFACE_STYLE_FILL_AREA ( #28689 ) ;
#29024=DIRECTION ( 'NONE',  ( 0.000000000000000000, -1.000000000000000000, 0.000000000000000000 ) ) ;
#29026=EDGE_LOOP ( 'NONE', ( #27012, #13624, #44228, #9606 ) ) ;
#29029=LINE ( 'NONE', #23105, #11127 ) ;
#29030=SURFACE_STYLE_FILL_AREA ( #34343 ) ;
#29033=CARTESIAN_POINT ( 'NONE',  ( -6.778496103155775110, 110.5743167862572278, 6.848681790824214133 ) ) ;
#29038=CARTESIAN_POINT ( 'NONE',  ( -71.74137931034481142, 36.89918356738973415, -10.00000000000000000 ) ) ;
#29040=AXIS2_PLACEMENT_3D ( 'NONE', #9916, #63010, #47234 ) ;
#29042=CIRCLE ( 'NONE', #2032, 0.5000000000000004441 ) ;
#29045=PRESENTATION_STYLE_ASSIGNMENT (( #56495 ) ) ;
#29048=PRESENTATION_STYLE_ASSIGNMENT (( #26630 ) ) ;
#29055=CARTESIAN_POINT ( 'NONE',  ( 44.97648960591795486, 10.67803934730671322, 3.825005713026917942 ) ) ;
#29056=EDGE_CURVE ( 'NONE', #20549, #30521, #19423, .T. ) ;
#29057=PLANE ( 'NONE',  #13617 ) ;
#29062=CARTESIAN_POINT ( 'NONE',  ( -8.102448949553181734, 144.0050000000000239, -5.886773742842749790 ) ) ;
#29065=UNCERTAINTY_MEASURE_WITH_UNIT (LENGTH_MEASURE( 1.000000000000000082E-05 ), #28549, 'distance_accuracy_value', 'NONE');
#29070=DIRECTION ( 'NONE',  ( 0.2413793103448194644, 0.9704308468600220117, 0.000000000000000000 ) ) ;
#29071=COLOUR_RGB ( '', 0.09019608, 0.27058824, 0.51372549) ;
#29072=( NAMED_UNIT ( * ) SI_UNIT ( $, .STERADIAN. ) SOLID_ANGLE_UNIT ( ) );
#29073=( LENGTH_UNIT ( ) NAMED_UNIT ( * ) SI_UNIT ( .MILLI., .METRE. ) );
#29075=MECHANICAL_DESIGN_GEOMETRIC_PRESENTATION_REPRESENTATION('',(#37041),#21260);
#29079=FILL_AREA_STYLE_COLOUR ( '', #53952 ) ;
#29080=CIRCLE ( 'NONE', #32464, 0.9999999999999991118 ) ;
#29081=CARTESIAN_POINT ( 'NONE',  ( -23.71231517720798010, 117.9999999999999716, 9.500000000000000000 ) ) ;
#29084=LINE ( 'NONE', #40741, #58967 ) ;
#29085=SURFACE_SIDE_STYLE ('',( #2311 ) ) ;
#29087=CARTESIAN_POINT ( 'NONE',  ( 9.058813317711337021, 112.6549999999999869, 2.943386871421375783 ) ) ;
#29092=ORIENTED_EDGE ( 'NONE', *, *, #8371, .T. ) ;
#29094=CARTESIAN_POINT ( 'NONE',  ( -74.24150567752717222, 8.825695369645321975, -6.400617768950437991 ) ) ;
#29095=FILL_AREA_STYLE_COLOUR ( '', #17095 ) ;
#29099=CARTESIAN_POINT ( 'NONE',  ( -7.632228543268608334, 144.8429263765338249, 2.479861379858952830 ) ) ;
#29100=CARTESIAN_POINT ( 'NONE',  ( 0.000000000000000000, 114.4999999999999574, -23.00000000000000000 ) ) ;
#29101=( LENGTH_UNIT ( ) NAMED_UNIT ( * ) SI_UNIT ( .MILLI., .METRE. ) );
#29103=ADVANCED_FACE ( 'NONE', ( #59100 ), #47570, .F. ) ;
#29104=CARTESIAN_POINT ( 'NONE',  ( -7.632228543268608334, 114.8429263765338106, 2.479861379858952830 ) ) ;
#29106=VERTEX_POINT ( 'NONE', #53149 ) ;
#29108=ORIENTED_EDGE ( 'NONE', *, *, #23731, .F. ) ;
#29110=SURFACE_STYLE_FILL_AREA ( #37683 ) ;
#29111=DIRECTION ( 'NONE',  ( 0.000000000000000000, 0.000000000000000000, -1.000000000000000000 ) ) ;
#29112=CARTESIAN_POINT ( 'NONE',  ( 41.25908726609139165, 107.3516760703038102, -3.442203282073897253 ) ) ;
#29114=AXIS2_PLACEMENT_3D ( 'NONE', #61728, #51548, #29386 ) ;
#29118=EDGE_CURVE ( 'NONE', #52602, #21193, #26719, .T. ) ;
#29119=TOROIDAL_SURFACE ( 'NONE', #33612, 1.000000000000000000, 0.5000000000000000000 ) ;
#29123=VERTEX_POINT ( 'NONE', #37706 ) ;
#29124=ORIENTED_EDGE ( 'NONE', *, *, #42284, .T. ) ;
#29125=FACE_OUTER_BOUND ( 'NONE', #13752, .T. ) ;
#29128=SURFACE_STYLE_USAGE ( .BOTH. , #38725 ) ;
#29132=SURFACE_STYLE_FILL_AREA ( #61845 ) ;
#29136=EDGE_CURVE ( 'NONE', #58906, #14945, #51979, .T. ) ;
#29139=CIRCLE ( 'NONE', #41549, 7.500000000000000000 ) ;
#29141=ORIENTED_EDGE ( 'NONE', *, *, #50584, .F. ) ;
#29148=CARTESIAN_POINT ( 'NONE',  ( 7.616319612703724040, 154.5000000000000568, -5.787195445650213266 ) ) ;
#29152=CARTESIAN_POINT ( 'NONE',  ( 3.094860106618431583, 118.2049999999999699, 9.525000000000000355 ) ) ;
#29157=UNCERTAINTY_MEASURE_WITH_UNIT (LENGTH_MEASURE( 1.000000000000000082E-05 ), #64529, 'distance_accuracy_value', 'NONE');
#29158=STYLED_ITEM ( 'NONE', ( #13422 ), #16001 ) ;
#29159=CARTESIAN_POINT ( 'NONE',  ( 41.72783051798698040, 107.4000574072429259, -4.000000000000000888 ) ) ;
#29163=DIRECTION ( 'NONE',  ( 0.000000000000000000, 0.000000000000000000, 1.000000000000000000 ) ) ;
#29164=( GEOMETRIC_REPRESENTATION_CONTEXT ( 3 ) GLOBAL_UNCERTAINTY_ASSIGNED_CONTEXT ( ( #35431 ) ) GLOBAL_UNIT_ASSIGNED_CONTEXT ( ( #35504, #68908, #62217 ) ) REPRESENTATION_CONTEXT ( 'NONE', 'WORKASPACE' ) );
#29167=( NAMED_UNIT ( * ) SI_UNIT ( $, .STERADIAN. ) SOLID_ANGLE_UNIT ( ) );
#29172=CARTESIAN_POINT ( 'NONE',  ( -15.48999599679679662, 146.4999999999999716, 7.000000000000000000 ) ) ;
#29173=EDGE_CURVE ( 'NONE', #19777, #2072, #27233, .T. ) ;
#29175=DIRECTION ( 'NONE',  ( 1.000000000000000000, 0.000000000000000000, 0.000000000000000000 ) ) ;
#29177=CARTESIAN_POINT ( 'NONE',  ( 71.49999999999998579, 119.9999999999997868, -7.000000000000000000 ) ) ;
#29181=VERTEX_POINT ( 'NONE', #53812 ) ;
#29183=FACE_OUTER_BOUND ( 'NONE', #27295, .T. ) ;
#29184=DIRECTION ( 'NONE',  ( 0.000000000000000000, 0.000000000000000000, 1.000000000000000000 ) ) ;
#29186=CIRCLE ( 'NONE', #6755, 10.00000000000000178 ) ;
#29190=CARTESIAN_POINT ( 'NONE',  ( 0.000000000000000000, 136.4449999999999932, -9.525000000000000355 ) ) ;
#29192=ORIENTED_EDGE ( 'NONE', *, *, #46439, .T. ) ;
#29193=ADVANCED_FACE ( 'NONE', ( #5610 ), #12641, .F. ) ;
#29194=CARTESIAN_POINT ( 'NONE',  ( 3.094860106618435136, 137.4049999999999727, -9.525000000000000355 ) ) ;
#29196=STYLED_ITEM ( 'NONE', ( #12916 ), #33173 ) ;
#29197=FILL_AREA_STYLE_COLOUR ( '', #55420 ) ;
#29199=CARTESIAN_POINT ( 'NONE',  ( -9.827790563157511022E-16, 112.4429263765338192, 8.025000000000000355 ) ) ;
#29201=UNCERTAINTY_MEASURE_WITH_UNIT (LENGTH_MEASURE( 1.000000000000000082E-05 ), #10176, 'distance_accuracy_value', 'NONE');
#29204=SURFACE_STYLE_USAGE ( .BOTH. , #3483 ) ;
#29206=ADVANCED_FACE ( 'NONE', ( #37354 ), #38032, .F. ) ;
#29207=VERTEX_POINT ( 'NONE', #34441 ) ;
#29209=( NAMED_UNIT ( * ) SI_UNIT ( $, .STERADIAN. ) SOLID_ANGLE_UNIT ( ) );
#29212=VECTOR ( 'NONE', #46080, 1000.000000000000000 ) ;
#29217=CARTESIAN_POINT ( 'NONE',  ( -45.50000000000000000, 1.797044900979284448E-15, 9.500000000000000000 ) ) ;
#29224=SURFACE_STYLE_USAGE ( .BOTH. , #61253 ) ;
#29225=ORIENTED_EDGE ( 'NONE', *, *, #60826, .F. ) ;
#29233=CARTESIAN_POINT ( 'NONE',  ( -24.21231517720798010, 113.4999999999999858, -7.000000000000000000 ) ) ;
#29238=CIRCLE ( 'NONE', #55044, 0.5000000000000004441 ) ;
#29239=CARTESIAN_POINT ( 'NONE',  ( -74.41717294046213738, 8.118038230903733776, -6.493553718642556483 ) ) ;
#29243=CARTESIAN_POINT ( 'NONE',  ( -8.102448949553181734, 140.4949999999999761, 5.886773742842747126 ) ) ;
#29245=STYLED_ITEM ( 'NONE', ( #45918 ), #21212 ) ;
#29248=EDGE_CURVE ( 'NONE', #38790, #15297, #28376, .T. ) ;
#29249=( GEOMETRIC_REPRESENTATION_CONTEXT ( 3 ) GLOBAL_UNCERTAINTY_ASSIGNED_CONTEXT ( ( #13738 ) ) GLOBAL_UNIT_ASSIGNED_CONTEXT ( ( #66394, #28750, #54454 ) ) REPRESENTATION_CONTEXT ( 'NONE', 'WORKASPACE' ) );
#29258=CARTESIAN_POINT ( 'NONE',  ( 44.99999999999998579, 119.9999999999999716, 9.500000000000000000 ) ) ;
#29260=DIRECTION ( 'NONE',  ( -1.000000000000000000, 0.000000000000000000, 0.000000000000000000 ) ) ;
#29261=VERTEX_POINT ( 'NONE', #33407 ) ;
#29265=CYLINDRICAL_SURFACE ( 'NONE', #5702, 0.5000000000000004441 ) ;
#29266=CARTESIAN_POINT ( 'NONE',  ( -48.00000000000000000, 99.99999999999992895, -7.000000000000000000 ) ) ;
#29267=FILL_AREA_STYLE ('',( #44480 ) ) ;
#29269=FACE_OUTER_BOUND ( 'NONE', #8215, .T. ) ;
#29270=ORIENTED_EDGE ( 'NONE', *, *, #45705, .F. ) ;
#29273=SURFACE_SIDE_STYLE ('',( #56730 ) ) ;
#29276=TOROIDAL_SURFACE ( 'NONE', #16971, 14.49999999999999822, 0.5000000000000000000 ) ;
#29278=PRESENTATION_STYLE_ASSIGNMENT (( #7831 ) ) ;
#29279=CARTESIAN_POINT ( 'NONE',  ( -8.437984349512095861, 157.8070736234661240, -5.166775262442723748E-16 ) ) ;
#29283=DIRECTION ( 'NONE',  ( 1.000000000000000000, 0.000000000000000000, 0.000000000000000000 ) ) ;
#29286=CARTESIAN_POINT ( 'NONE',  ( -79.99999999999998579, 50.00000000000000000, 11.50000000000003730 ) ) ;
#29287=CARTESIAN_POINT ( 'NONE',  ( 8.102448949553183510, 125.1049999999999756, -5.886773742842746238 ) ) ;
#29288=UNCERTAINTY_MEASURE_WITH_UNIT (LENGTH_MEASURE( 1.000000000000000082E-05 ), #66486, 'distance_accuracy_value', 'NONE');
#29289=CARTESIAN_POINT ( 'NONE',  ( 0.000000000000000000, 133.0570736234661524, -8.025000000000000355 ) ) ;
#29290=PRESENTATION_STYLE_ASSIGNMENT (( #1818 ) ) ;
#29294=STYLED_ITEM ( 'NONE', ( #11020 ), #21278 ) ;
#29295=ORIENTED_EDGE ( 'NONE', *, *, #33508, .T. ) ;
#29296=DIRECTION ( 'NONE',  ( -1.000000000000000000, 0.000000000000000000, 0.000000000000000000 ) ) ;
#29297=( NAMED_UNIT ( * ) SI_UNIT ( $, .STERADIAN. ) SOLID_ANGLE_UNIT ( ) );
#29300=CARTESIAN_POINT ( 'NONE',  ( -65.99999999999998579, 50.00000000000000000, 11.50000000000000000 ) ) ;
#29305=CARTESIAN_POINT ( 'NONE',  ( 0.000000000000000000, 87.30187232391182306, 0.000000000000000000 ) ) ;
#29308=ORIENTED_EDGE ( 'NONE', *, *, #9946, .F. ) ;
#29310=CARTESIAN_POINT ( 'NONE',  ( -75.00000000000000000, 8.421502636539848652, 6.236752812775003818 ) ) ;
#29313=CIRCLE ( 'NONE', #55163, 17.00000000000000000 ) ;
#29316=CARTESIAN_POINT ( 'NONE',  ( -74.99999999999998579, 50.00000000000000000, -9.500000000000000000 ) ) ;
#29318=CARTESIAN_POINT ( 'NONE',  ( 8.102448949553181734, 138.9949999999999761, -5.886773742842746238 ) ) ;
#29320=ORIENTED_EDGE ( 'NONE', *, *, #6946, .F. ) ;
#29321=CARTESIAN_POINT ( 'NONE',  ( 34.99999999999999289, 99.99999999999998579, -7.500000000000000000 ) ) ;
#29322=DIRECTION ( 'NONE',  ( -1.000000000000000000, 0.000000000000000000, 0.000000000000000000 ) ) ;
#29325=FACE_OUTER_BOUND ( 'NONE', #16935, .T. ) ;
#29326=FACE_OUTER_BOUND ( 'NONE', #20485, .T. ) ;
#29330=CARTESIAN_POINT ( 'NONE',  ( -10.01517768586949231, 113.1949999999999790, -6.132527647946036459E-16 ) ) ;
#29333=CIRCLE ( 'NONE', #3491, 0.5000000000000004441 ) ;
#29334=CARTESIAN_POINT ( 'NONE',  ( 72.49999999999998579, 119.9999999999997868, -9.500000000000000000 ) ) ;
#29338=CARTESIAN_POINT ( 'NONE',  ( 20.71231517720798010, 146.9999999999999716, -7.000000000000000000 ) ) ;
#29342=STYLED_ITEM ( 'NONE', ( #11507 ), #11509 ) ;
#29344=DIRECTION ( 'NONE',  ( 0.000000000000000000, 1.000000000000000000, 0.000000000000000000 ) ) ;
#29352=( LENGTH_UNIT ( ) NAMED_UNIT ( * ) SI_UNIT ( .MILLI., .METRE. ) );
#29353=CARTESIAN_POINT ( 'NONE',  ( -40.99999999999998579, 107.7459666864129417, 3.076101031310321421 ) ) ;
#29357=VERTEX_POINT ( 'NONE', #59448 ) ;
#29358=CARTESIAN_POINT ( 'NONE',  ( -65.49999999999997158, -1.956686671034893189E-14, 12.00000000000000000 ) ) ;
#29360=ORIENTED_EDGE ( 'NONE', *, *, #37502, .F. ) ;
#29362=COLOUR_RGB ( '', 0.72549020, 0.75294118, 0.79215686) ;
#29363=CARTESIAN_POINT ( 'NONE',  ( 6.826472737025121695, 132.6070736234661638, -4.959722759717905660 ) ) ;
#29364=AXIS2_PLACEMENT_3D ( 'NONE', #66433, #61156, #17588 ) ;
#29368=ORIENTED_EDGE ( 'NONE', *, *, #17277, .F. ) ;
#29372=LINE ( 'NONE', #56109, #21648 ) ;
#29373=AXIS2_PLACEMENT_3D ( 'NONE', #46825, #36613, #4519 ) ;
#29375=DIRECTION ( 'NONE',  ( 0.000000000000000000, 0.000000000000000000, -1.000000000000000000 ) ) ;
#29379=CIRCLE ( 'NONE', #53006, 9.499999999999994671 ) ;
#29380=DIRECTION ( 'NONE',  ( 0.000000000000000000, 0.000000000000000000, 1.000000000000000000 ) ) ;
#29382=AXIS2_PLACEMENT_3D ( 'NONE', #27244, #48432, #11788 ) ;
#29386=DIRECTION ( 'NONE',  ( 0.000000000000000000, 0.000000000000000000, -1.000000000000000000 ) ) ;
#29389=ADVANCED_FACE ( 'NONE', ( #27088 ), #44037, .F. ) ;
#29391=EDGE_LOOP ( 'NONE', ( #30415, #36263, #55599, #3741 ) ) ;
#29393=VERTEX_POINT ( 'NONE', #33096 ) ;
#29395=( NAMED_UNIT ( * ) PLANE_ANGLE_UNIT ( ) SI_UNIT ( $, .RADIAN. ) );
#29400=CARTESIAN_POINT ( 'NONE',  ( 3.094860106618431583, 111.0949999999999704, 9.525000000000000355 ) ) ;
#29407=CIRCLE ( 'NONE', #61995, 0.5000000000000004441 ) ;
#29409=SURFACE_SIDE_STYLE ('',( #23439 ) ) ;
#29411=FILL_AREA_STYLE ('',( #43912 ) ) ;
#29415=SURFACE_STYLE_FILL_AREA ( #3333 ) ;
#29416=VECTOR ( 'NONE', #33065, 1000.000000000000000 ) ;
#29419=ORIENTED_EDGE ( 'NONE', *, *, #36591, .F. ) ;
#29428=CARTESIAN_POINT ( 'NONE',  ( -8.102448949553181734, 147.0049999999999955, -5.886773742842749790 ) ) ;
#29430=AXIS2_PLACEMENT_3D ( 'NONE', #67090, #50917, #6586 ) ;
#29432=FILL_AREA_STYLE ('',( #7989 ) ) ;
#29434=MECHANICAL_DESIGN_GEOMETRIC_PRESENTATION_REPRESENTATION('',(#22724),#1318);
#29435=CIRCLE ( 'NONE', #41847, 0.5000000000000004441 ) ;
#29436=CYLINDRICAL_SURFACE ( 'NONE', #23596, 0.5000000000000004441 ) ;
#29438=CIRCLE ( 'NONE', #28309, 0.5000000000000004441 ) ;
#29439=DIRECTION ( 'NONE',  ( -0.4468085106382997385, -0.000000000000000000, -0.8946296187927071930 ) ) ;
#29441=LINE ( 'NONE', #55124, #57701 ) ;
#29442=DIRECTION ( 'NONE',  ( 0.000000000000000000, 0.000000000000000000, 1.000000000000000000 ) ) ;
#29444=VERTEX_POINT ( 'NONE', #48966 ) ;
#29449=ADVANCED_FACE ( 'NONE', ( #32372 ), #43686, .T. ) ;
#29452=FILL_AREA_STYLE_COLOUR ( '', #27352 ) ;
#29454=VERTEX_POINT ( 'NONE', #61520 ) ;
#29455=FILL_AREA_STYLE ('',( #7648 ) ) ;
#29464=CARTESIAN_POINT ( 'NONE',  ( -34.99999999999999289, 99.99999999999998579, 7.500000000000000000 ) ) ;
#29469=CARTESIAN_POINT ( 'NONE',  ( -4.251564707942288912, 110.4999999999999858, -8.568970148020829569 ) ) ;
#29470=SURFACE_SIDE_STYLE ('',( #40397 ) ) ;
#29473=VERTEX_POINT ( 'NONE', #18305 ) ;
#29474=CARTESIAN_POINT ( 'NONE',  ( -4.716976649647097730, 147.2429263765338305, -6.492361379858953896 ) ) ;
#29475=DIRECTION ( 'NONE',  ( 0.000000000000000000, 0.000000000000000000, -1.000000000000000000 ) ) ;
#29482=( NAMED_UNIT ( * ) PLANE_ANGLE_UNIT ( ) SI_UNIT ( $, .RADIAN. ) );
#29485=DIRECTION ( 'NONE',  ( 1.000000000000000000, 1.009293658750142399E-15, 0.000000000000000000 ) ) ;
#29486=AXIS2_PLACEMENT_3D ( 'NONE', #13396, #30608, #2450 ) ;
#29489=FILL_AREA_STYLE ('',( #28787 ) ) ;
#29492=SURFACE_STYLE_FILL_AREA ( #25254 ) ;
#29493=CIRCLE ( 'NONE', #68832, 0.5000000000000004441 ) ;
#29496=ORIENTED_EDGE ( 'NONE', *, *, #50915, .T. ) ;
#29499=( NAMED_UNIT ( * ) SI_UNIT ( $, .STERADIAN. ) SOLID_ANGLE_UNIT ( ) );
#29503=EDGE_LOOP ( 'NONE', ( #3839, #38595, #32082, #39140 ) ) ;
#29504=AXIS2_PLACEMENT_3D ( 'NONE', #4813, #52344, #47800 ) ;
#29505=CYLINDRICAL_SURFACE ( 'NONE', #6823, 0.5000000000000004441 ) ;
#29506=( NAMED_UNIT ( * ) SI_UNIT ( $, .STERADIAN. ) SOLID_ANGLE_UNIT ( ) );
#29508=MECHANICAL_DESIGN_GEOMETRIC_PRESENTATION_REPRESENTATION('',(#53134),#24994);
#29513=VECTOR ( 'NONE', #33139, 1000.000000000000000 ) ;
#29515=SURFACE_STYLE_FILL_AREA ( #45736 ) ;
#29518=LINE ( 'NONE', #2374, #21329 ) ;
#29519=CIRCLE ( 'NONE', #46441, 0.5000000000000004441 ) ;
#29521=CARTESIAN_POINT ( 'NONE',  ( -10.01517768586949231, 117.3049999999999784, -6.132527647946036459E-16 ) ) ;
#29529=DIRECTION ( 'NONE',  ( 1.000000000000000000, 0.000000000000000000, 0.000000000000000000 ) ) ;
#29530=( GEOMETRIC_REPRESENTATION_CONTEXT ( 3 ) GLOBAL_UNCERTAINTY_ASSIGNED_CONTEXT ( ( #39198 ) ) GLOBAL_UNIT_ASSIGNED_CONTEXT ( ( #5256, #58393, #26704 ) ) REPRESENTATION_CONTEXT ( 'NONE', 'WORKASPACE' ) );
#29531=ADVANCED_FACE ( 'NONE', ( #34468 ), #17950, .T. ) ;
#29533=CARTESIAN_POINT ( 'NONE',  ( -60.00000000000000000, -2.024042244987997205E-14, -6.500000000000000000 ) ) ;
#29535=CIRCLE ( 'NONE', #23915, 1.000000000000000888 ) ;
#29536=ORIENTED_EDGE ( 'NONE', *, *, #17635, .F. ) ;
#29537=AXIS2_PLACEMENT_3D ( 'NONE', #67022, #51520, #41005 ) ;
#29538=CARTESIAN_POINT ( 'NONE',  ( -80.49999999999998579, 50.00000000000000000, 6.500000000000000000 ) ) ;
#29539=LINE ( 'NONE', #29172, #45479 ) ;
#29553=( GEOMETRIC_REPRESENTATION_CONTEXT ( 3 ) GLOBAL_UNCERTAINTY_ASSIGNED_CONTEXT ( ( #44829 ) ) GLOBAL_UNIT_ASSIGNED_CONTEXT ( ( #25654, #9854, #5236 ) ) REPRESENTATION_CONTEXT ( 'NONE', 'WORKASPACE' ) );
#29558=CARTESIAN_POINT ( 'NONE',  ( 10.01517768586949231, 135.6949999999999932, 1.839758294383810543E-15 ) ) ;
#29561=CARTESIAN_POINT ( 'NONE',  ( -8.102448949553179958, 144.0049999999999955, -5.886773742842749790 ) ) ;
#29562=FACE_OUTER_BOUND ( 'NONE', #24506, .T. ) ;
#29563=EDGE_CURVE ( 'NONE', #61539, #4364, #44231, .T. ) ;
#29564=CARTESIAN_POINT ( 'NONE',  ( 41.61090298506073992, 107.5097581389851911, -4.000000003092934797 ) ) ;
#29566=CARTESIAN_POINT ( 'NONE',  ( 7.632228543268608334, 119.3429263765338249, -2.479861379858951942 ) ) ;
#29567=DIRECTION ( 'NONE',  ( 0.000000000000000000, 0.000000000000000000, 1.000000000000000000 ) ) ;
#29568=( NAMED_UNIT ( * ) PLANE_ANGLE_UNIT ( ) SI_UNIT ( $, .RADIAN. ) );
#29569=AXIS2_PLACEMENT_3D ( 'NONE', #1747, #3476, #67199 ) ;
#29570=AXIS2_PLACEMENT_3D ( 'NONE', #68922, #58026, #41172 ) ;
#29571=DIRECTION ( 'NONE',  ( 0.000000000000000000, 0.000000000000000000, 1.000000000000000000 ) ) ;
#29576=DIRECTION ( 'NONE',  ( -0.000000000000000000, 1.000000000000000000, -0.000000000000000000 ) ) ;
#29577=CYLINDRICAL_SURFACE ( 'NONE', #43505, 8.025000000000000355 ) ;
#29582=VECTOR ( 'NONE', #67485, 1000.000000000000000 ) ;
#29583=FILL_AREA_STYLE_COLOUR ( '', #50995 ) ;
#29584=DIRECTION ( 'NONE',  ( -0.000000000000000000, -1.000000000000000000, -0.000000000000000000 ) ) ;
#29585=CARTESIAN_POINT ( 'NONE',  ( 44.99999999999999289, 9.801220280675213559, -6.455927277197755387 ) ) ;
#29589=FILL_AREA_STYLE_COLOUR ( '', #12042 ) ;
#29590=CARTESIAN_POINT ( 'NONE',  ( 60.99999999999998579, 50.00000000000000000, -7.500000000000000000 ) ) ;
#29592=ORIENTED_EDGE ( 'NONE', *, *, #18557, .T. ) ;
#29594=VECTOR ( 'NONE', #30091, 1000.000000000000000 ) ;
#29598=EDGE_CURVE ( 'NONE', #8720, #30297, #53190, .T. ) ;
#29599=( GEOMETRIC_REPRESENTATION_CONTEXT ( 3 ) GLOBAL_UNCERTAINTY_ASSIGNED_CONTEXT ( ( #53656 ) ) GLOBAL_UNIT_ASSIGNED_CONTEXT ( ( #15595, #5010, #26465 ) ) REPRESENTATION_CONTEXT ( 'NONE', 'WORKASPACE' ) );
#29600=CARTESIAN_POINT ( 'NONE',  ( -75.00000000000000000, 9.518682052516130199, -6.447728916822595302 ) ) ;
#29602=DIRECTION ( 'NONE',  ( 1.000000000000000000, 0.000000000000000000, 0.000000000000000000 ) ) ;
#29604=CIRCLE ( 'NONE', #48884, 0.4999999999999994449 ) ;
#29605=CARTESIAN_POINT ( 'NONE',  ( -10.01517768586949231, 143.1949999999999932, -6.132527647946036459E-16 ) ) ;
#29608=DIRECTION ( 'NONE',  ( -1.000000000000000000, 0.000000000000000000, 0.000000000000000000 ) ) ;
#29613=EDGE_CURVE ( 'NONE', #49361, #15159, #42239, .T. ) ;
#29621=EDGE_CURVE ( 'NONE', #12107, #60087, #20005, .T. ) ;
#29622=( NAMED_UNIT ( * ) SI_UNIT ( $, .STERADIAN. ) SOLID_ANGLE_UNIT ( ) );
#29623=CARTESIAN_POINT ( 'NONE',  ( -20.94636006565341191, 149.9999999999999716, -9.500000000000000000 ) ) ;
#29624=ORIENTED_EDGE ( 'NONE', *, *, #37497, .F. ) ;
#29626=AXIS2_PLACEMENT_3D ( 'NONE', #21878, #16957, #37759 ) ;
#29628=EDGE_CURVE ( 'NONE', #45809, #53118, #21406, .T. ) ;
#29629=( NAMED_UNIT ( * ) PLANE_ANGLE_UNIT ( ) SI_UNIT ( $, .RADIAN. ) );
#29633=( LENGTH_UNIT ( ) NAMED_UNIT ( * ) SI_UNIT ( .MILLI., .METRE. ) );
#29637=CARTESIAN_POINT ( 'NONE',  ( -2.607480562269158586, 143.4070736234661751, 8.024999999999939959 ) ) ;
#29638=ORIENTED_EDGE ( 'NONE', *, *, #32399, .F. ) ;
#29642=CARTESIAN_POINT ( 'NONE',  ( -20.44220712062818635, 115.3857587453612865, -10.00000000000000000 ) ) ;
#29644=EDGE_CURVE ( 'NONE', #7407, #49325, #66395, .T. ) ;
#29646=MECHANICAL_DESIGN_GEOMETRIC_PRESENTATION_REPRESENTATION('',(#28521),#26266);
#29648=CARTESIAN_POINT ( 'NONE',  ( 7.632228543268607446, 159.1570736234661467, 2.479861379858954606 ) ) ;
#29649=TOROIDAL_SURFACE ( 'NONE', #38679, 17.50000000000000000, 0.5000000000000000000 ) ;
#29650=ORIENTED_EDGE ( 'NONE', *, *, #43099, .T. ) ;
#29652=CARTESIAN_POINT ( 'NONE',  ( 15.98999599679679839, 118.4999999999999716, -9.500000000000000000 ) ) ;
#29654=EDGE_CURVE ( 'NONE', #30209, #28559, #26247, .T. ) ;
#29655=DIRECTION ( 'NONE',  ( 0.000000000000000000, 0.000000000000000000, 1.000000000000000000 ) ) ;
#29656=CARTESIAN_POINT ( 'NONE',  ( 5.598654528085809545, 137.2549999999999955, -7.705886871421373741 ) ) ;
#29658=CARTESIAN_POINT ( 'NONE',  ( 20.06812647026248086, 114.9888238951376991, 10.44321692355803144 ) ) ;
#29660=SURFACE_SIDE_STYLE ('',( #67643 ) ) ;
#29663=CARTESIAN_POINT ( 'NONE',  ( -34.99999999999992895, 109.9999999999999858, 10.00000000000000000 ) ) ;
#29664=CARTESIAN_POINT ( 'NONE',  ( 74.50000000000000000, -2.220952357103124925E-14, -9.500000000000000000 ) ) ;
#29668=CARTESIAN_POINT ( 'NONE',  ( -44.99999999999977263, 147.4999999999999716, -9.500000000000000000 ) ) ;
#29669=MECHANICAL_DESIGN_GEOMETRIC_PRESENTATION_REPRESENTATION('',(#63358),#11690);
#29674=( LENGTH_UNIT ( ) NAMED_UNIT ( * ) SI_UNIT ( .MILLI., .METRE. ) );
#29679=FILL_AREA_STYLE ('',( #46949 ) ) ;
#29683=CARTESIAN_POINT ( 'NONE',  ( -10.01517768586949408, 146.1949999999999648, -6.132527647946036459E-16 ) ) ;
#29685=VECTOR ( 'NONE', #6555, 1000.000000000000000 ) ;
#29694=CARTESIAN_POINT ( 'NONE',  ( -9.058813317711337021, 110.0449999999999875, -2.943386871421374895 ) ) ;
#29698=CARTESIAN_POINT ( 'NONE',  ( 74.65811388300841145, 19.88603796100278487, -6.500000000000000000 ) ) ;
#29699=EDGE_LOOP ( 'NONE', ( #50277, #56467, #55686, #29536 ) ) ;
#29702=EDGE_CURVE ( 'NONE', #16496, #62518, #67845, .T. ) ;
#29705=ADVANCED_FACE ( 'NONE', ( #580 ), #6262, .T. ) ;
#29706=EDGE_CURVE ( 'NONE', #4654, #3912, #34137, .T. ) ;
#29710=SURFACE_STYLE_USAGE ( .BOTH. , #45588 ) ;
#29711=CARTESIAN_POINT ( 'NONE',  ( 65.00000000000000000, 1.797044900979284448E-15, -12.00000000000000000 ) ) ;
#29718=AXIS2_PLACEMENT_3D ( 'NONE', #63616, #4498, #4868 ) ;
#29719=CARTESIAN_POINT ( 'NONE',  ( -9.827790563157511022E-16, 122.5570736234661524, 8.025000000000000355 ) ) ;
#29720=CARTESIAN_POINT ( 'NONE',  ( -41.08002123031664610, 107.6301924976384470, 3.280722492564424719 ) ) ;
#29722=STYLED_ITEM ( 'NONE', ( #25989 ), #30729 ) ;
#29723=CARTESIAN_POINT ( 'NONE',  ( -41.49999999999997868, 9.999999999999978684, 3.000000000000000000 ) ) ;
#29725=DIRECTION ( 'NONE',  ( -0.03448275862069643399, 0.9994052928406507164, -3.469446951953618922E-15 ) ) ;
#29728=SURFACE_STYLE_FILL_AREA ( #45248 ) ;
#29729=CARTESIAN_POINT ( 'NONE',  ( 4.716976649647096842, 131.8570736234661638, 6.492361379858953896 ) ) ;
#29733=DIRECTION ( 'NONE',  ( -0.000000000000000000, -0.000000000000000000, -1.000000000000000000 ) ) ;
#29737=SURFACE_STYLE_FILL_AREA ( #41360 ) ;
#29738=CARTESIAN_POINT ( 'NONE',  ( 6.826472737025119919, 150.0070736234661695, 4.959722759717908325 ) ) ;
#29739=EDGE_CURVE ( 'NONE', #62495, #69341, #26322, .T. ) ;
#29740=CYLINDRICAL_SURFACE ( 'NONE', #51992, 16.00000000000000000 ) ;
#29748=UNCERTAINTY_MEASURE_WITH_UNIT (LENGTH_MEASURE( 1.000000000000000082E-05 ), #19720, 'distance_accuracy_value', 'NONE');
#29749=EDGE_LOOP ( 'NONE', ( #15164, #5262, #20749, #40077 ) ) ;
#29751=CARTESIAN_POINT ( 'NONE',  ( 71.50000000000000000, 35.92875272052971525, 7.500000000000000000 ) ) ;
#29753=( NAMED_UNIT ( * ) SI_UNIT ( $, .STERADIAN. ) SOLID_ANGLE_UNIT ( ) );
#29755=PRESENTATION_STYLE_ASSIGNMENT (( #14270 ) ) ;
#29756=AXIS2_PLACEMENT_3D ( 'NONE', #53615, #26528, #43116 ) ;
#29757=ORIENTED_EDGE ( 'NONE', *, *, #7322, .F. ) ;
#29767=VECTOR ( 'NONE', #35063, 1000.000000000000000 ) ;
#29771=SURFACE_STYLE_USAGE ( .BOTH. , #12532 ) ;
#29772=CARTESIAN_POINT ( 'NONE',  ( 71.49999999999998579, 64.07124727947029896, -7.500000000000000000 ) ) ;
#29776=CARTESIAN_POINT ( 'NONE',  ( -6.962908620255356063, 111.9337395095162719, 4.200728263596600343 ) ) ;
#29780=ORIENTED_EDGE ( 'NONE', *, *, #37585, .T. ) ;
#29783=MECHANICAL_DESIGN_GEOMETRIC_PRESENTATION_REPRESENTATION('',(#6178),#45544);
#29784=FACE_OUTER_BOUND ( 'NONE', #54225, .T. ) ;
#29785=FACE_OUTER_BOUND ( 'NONE', #29904, .T. ) ;
#29789=VECTOR ( 'NONE', #57043, 1000.000000000000000 ) ;
#29792=CARTESIAN_POINT ( 'NONE',  ( -5.598654528085808657, 150.7549999999999955, 7.705886871421373741 ) ) ;
#29799=ADVANCED_FACE ( 'NONE', ( #37983 ), #69593, .T. ) ;
#29800=VECTOR ( 'NONE', #18344, 1000.000000000000000 ) ;
#29808=ORIENTED_EDGE ( 'NONE', *, *, #44298, .F. ) ;
#29809=( NAMED_UNIT ( * ) SI_UNIT ( $, .STERADIAN. ) SOLID_ANGLE_UNIT ( ) );
#29811=CARTESIAN_POINT ( 'NONE',  ( -10.01517768586949231, 114.3049999999999926, -6.132527647946036459E-16 ) ) ;
#29822=CARTESIAN_POINT ( 'NONE',  ( -6.826472737025120807, 141.9929263765338305, 4.959722759717906548 ) ) ;
#29823=FILL_AREA_STYLE ('',( #18901 ) ) ;
#29825=CIRCLE ( 'NONE', #47881, 0.4999999999999993339 ) ;
#29827=ORIENTED_EDGE ( 'NONE', *, *, #24059, .F. ) ;
#29829=CYLINDRICAL_SURFACE ( 'NONE', #39457, 23.00000000000000000 ) ;
#29831=DIRECTION ( 'NONE',  ( -0.8946296187927070820, 0.000000000000000000, -0.4468085106382997385 ) ) ;
#29832=CARTESIAN_POINT ( 'NONE',  ( -60.00000000000000000, -2.024042244987997205E-14, 11.50000000000003020 ) ) ;
#29833=STYLED_ITEM ( 'NONE', ( #16529 ), #5619 ) ;
#29835=PLANE ( 'NONE',  #39869 ) ;
#29838=CARTESIAN_POINT ( 'NONE',  ( 75.00000000000000000, 19.99999999999997868, -6.500000000000000000 ) ) ;
#29840=EDGE_LOOP ( 'NONE', ( #13156, #1049, #43375, #22288 ) ) ;
#29841=ORIENTED_EDGE ( 'NONE', *, *, #1851, .F. ) ;
#29842=DIRECTION ( 'NONE',  ( -7.080503983578803083E-17, 1.000000000000000000, 0.000000000000000000 ) ) ;
#29849=SURFACE_SIDE_STYLE ('',( #62545 ) ) ;
#29851=AXIS2_PLACEMENT_3D ( 'NONE', #11227, #4558, #26013 ) ;
#29852=EDGE_CURVE ( 'NONE', #54470, #21703, #23994, .T. ) ;
#29858=VERTEX_POINT ( 'NONE', #34711 ) ;
#29860=DIRECTION ( 'NONE',  ( -1.000000000000000000, 0.000000000000000000, 0.000000000000000000 ) ) ;
#29868=CARTESIAN_POINT ( 'NONE',  ( 5.598654528085809545, 119.2549999999999812, -7.705886871421373741 ) ) ;
#29870=EDGE_CURVE ( 'NONE', #26003, #58118, #333, .T. ) ;
#29873=EDGE_CURVE ( 'NONE', #37046, #20411, #29441, .T. ) ;
#29877=SURFACE_STYLE_USAGE ( .BOTH. , #46815 ) ;
#29882=CARTESIAN_POINT ( 'NONE',  ( 24.21231517720798010, 113.4999999999999858, 7.000000000000000000 ) ) ;
#29888=DIRECTION ( 'NONE',  ( 0.000000000000000000, 0.000000000000000000, 1.000000000000000000 ) ) ;
#29891=VERTEX_POINT ( 'NONE', #2674 ) ;
#29895=SURFACE_STYLE_USAGE ( .BOTH. , #24955 ) ;
#29904=EDGE_LOOP ( 'NONE', ( #41006, #68283, #44295, #5975 ) ) ;
#29905=CARTESIAN_POINT ( 'NONE',  ( 44.28021770739999852, 9.999999999999980460, -3.500000000000000000 ) ) ;
#29908=CARTESIAN_POINT ( 'NONE',  ( 8.102448949553181734, 138.3950000000000102, 5.886773742842750679 ) ) ;
#29910=VECTOR ( 'NONE', #17051, 1000.000000000000000 ) ;
#29913=CARTESIAN_POINT ( 'NONE',  ( -9.058813317711338797, 138.4549999999999841, 2.943386871421373563 ) ) ;
#29914=DIRECTION ( 'NONE',  ( 0.7713892158398705234, 0.000000000000000000, -0.6363636363636357984 ) ) ;
#29916=CARTESIAN_POINT ( 'NONE',  ( -7.632228543268608334, 114.8429263765338106, 2.479861379858952830 ) ) ;
#29917=LINE ( 'NONE', #67917, #16627 ) ;
#29918=UNCERTAINTY_MEASURE_WITH_UNIT (LENGTH_MEASURE( 1.000000000000000082E-05 ), #25578, 'distance_accuracy_value', 'NONE');
#29921=ORIENTED_EDGE ( 'NONE', *, *, #54271, .T. ) ;
#29922=DIRECTION ( 'NONE',  ( 0.000000000000000000, 1.000000000000000000, 0.000000000000000000 ) ) ;
#29923=ORIENTED_EDGE ( 'NONE', *, *, #53993, .F. ) ;
#29925=CARTESIAN_POINT ( 'NONE',  ( 20.20444455447386645, 114.9652390998742533, 10.39771284005833252 ) ) ;
#29926=DIRECTION ( 'NONE',  ( -0.000000000000000000, -0.000000000000000000, 1.000000000000000000 ) ) ;
#29928=ORIENTED_EDGE ( 'NONE', *, *, #55047, .T. ) ;
#29929=UNCERTAINTY_MEASURE_WITH_UNIT (LENGTH_MEASURE( 1.000000000000000082E-05 ), #47582, 'distance_accuracy_value', 'NONE');
#29930=( NAMED_UNIT ( * ) SI_UNIT ( $, .STERADIAN. ) SOLID_ANGLE_UNIT ( ) );
#29932=CARTESIAN_POINT ( 'NONE',  ( 74.52070078832272770, 19.38218994716120847, 6.500000000000000888 ) ) ;
#29933=ORIENTED_EDGE ( 'NONE', *, *, #5769, .T. ) ;
#29934=( NAMED_UNIT ( * ) SI_UNIT ( $, .STERADIAN. ) SOLID_ANGLE_UNIT ( ) );
#29935=ORIENTED_EDGE ( 'NONE', *, *, #14294, .F. ) ;
#29940=DIRECTION ( 'NONE',  ( 0.000000000000000000, 0.000000000000000000, 1.000000000000000000 ) ) ;
#29945=( LENGTH_UNIT ( ) NAMED_UNIT ( * ) SI_UNIT ( .MILLI., .METRE. ) );
#29948=ORIENTED_EDGE ( 'NONE', *, *, #58004, .F. ) ;
#29952=CARTESIAN_POINT ( 'NONE',  ( -9.058813317711337021, 137.0449999999999875, -2.943386871421374895 ) ) ;
#29954=EDGE_CURVE ( 'NONE', #18076, #32404, #13256, .T. ) ;
#29955=CARTESIAN_POINT ( 'NONE',  ( -83.99999999999997158, 50.00000000000000000, 10.50000000000000000 ) ) ;
#29957=DIRECTION ( 'NONE',  ( -1.000000000000000000, 0.000000000000000000, -0.000000000000000000 ) ) ;
#29958=CARTESIAN_POINT ( 'NONE',  ( -41.49999999999998579, 106.9282032302754999, -3.500000000000000000 ) ) ;
#29960=EDGE_CURVE ( 'NONE', #60536, #54396, #39749, .T. ) ;
#29963=SURFACE_STYLE_FILL_AREA ( #8528 ) ;
#29967=ORIENTED_EDGE ( 'NONE', *, *, #7692, .F. ) ;
#29969=ORIENTED_EDGE ( 'NONE', *, *, #30038, .F. ) ;
#29970=CARTESIAN_POINT ( 'NONE',  ( 34.99999999999992895, 112.4999999999999858, -10.00000000000000000 ) ) ;
#29971=FILL_AREA_STYLE ('',( #2494 ) ) ;
#29972=CARTESIAN_POINT ( 'NONE',  ( -45.58282705953852343, 8.118038230903730224, 6.493553718642735006 ) ) ;
#29973=DIRECTION ( 'NONE',  ( -0.2413793103448194644, 0.9704308468600220117, 0.000000000000000000 ) ) ;
#29976=CIRCLE ( 'NONE', #69323, 0.5000000000000006661 ) ;
#29978=DIRECTION ( 'NONE',  ( 0.000000000000000000, 0.000000000000000000, 1.000000000000000000 ) ) ;
#29979=( NAMED_UNIT ( * ) SI_UNIT ( $, .STERADIAN. ) SOLID_ANGLE_UNIT ( ) );
#29983=CARTESIAN_POINT ( 'NONE',  ( -5.598654528085806881, 112.7449999999999903, -7.705886871421374629 ) ) ;
#29985=EDGE_LOOP ( 'NONE', ( #14441, #17838, #48650, #68103 ) ) ;
#29986=DIRECTION ( 'NONE',  ( -1.000000000000000000, 0.000000000000000000, 0.000000000000000000 ) ) ;
#29987=CARTESIAN_POINT ( 'NONE',  ( -3.094860106618434248, 111.9049999999999869, 9.525000000000000355 ) ) ;
#29989=CARTESIAN_POINT ( 'NONE',  ( -74.50000000000000000, -2.220952357103124925E-14, -6.500000000000000000 ) ) ;
#29991=CARTESIAN_POINT ( 'NONE',  ( 9.058813317711338797, 136.9549999999999841, -2.943386871421372675 ) ) ;
#29993=( LENGTH_UNIT ( ) NAMED_UNIT ( * ) SI_UNIT ( .MILLI., .METRE. ) );
#29995=( NAMED_UNIT ( * ) SI_UNIT ( $, .STERADIAN. ) SOLID_ANGLE_UNIT ( ) );
#29996=SURFACE_STYLE_FILL_AREA ( #42350 ) ;
#29997=FILL_AREA_STYLE ('',( #35987 ) ) ;
#29998=ORIENTED_EDGE ( 'NONE', *, *, #61239, .F. ) ;
#29999=( LENGTH_UNIT ( ) NAMED_UNIT ( * ) SI_UNIT ( .MILLI., .METRE. ) );
#30001=ORIENTED_EDGE ( 'NONE', *, *, #14220, .F. ) ;
#30005=DIRECTION ( 'NONE',  ( 0.000000000000000000, 0.000000000000000000, -1.000000000000000000 ) ) ;
#30010=DIRECTION ( 'NONE',  ( 0.000000000000000000, 0.000000000000000000, 1.000000000000000000 ) ) ;
#30012=EDGE_LOOP ( 'NONE', ( #60018, #37590, #7524, #8812 ) ) ;
#30014=CARTESIAN_POINT ( 'NONE',  ( -8.437984349512095861, 118.8070736234661524, -5.166775262442723748E-16 ) ) ;
#30015=CYLINDRICAL_SURFACE ( 'NONE', #962, 23.00000000000000000 ) ;
#30017=CARTESIAN_POINT ( 'NONE',  ( -44.50000000000000000, 10.49999999999998224, -4.000000000000000000 ) ) ;
#30018=CARTESIAN_POINT ( 'NONE',  ( 10.01517768586949408, 144.6949999999999932, 1.839758294383810543E-15 ) ) ;
#30022=( NAMED_UNIT ( * ) PLANE_ANGLE_UNIT ( ) SI_UNIT ( $, .RADIAN. ) );
#30023=( GEOMETRIC_REPRESENTATION_CONTEXT ( 3 ) GLOBAL_UNCERTAINTY_ASSIGNED_CONTEXT ( ( #66471 ) ) GLOBAL_UNIT_ASSIGNED_CONTEXT ( ( #53700, #43216, #59307 ) ) REPRESENTATION_CONTEXT ( 'NONE', 'WORKASPACE' ) );
#30025=SURFACE_STYLE_FILL_AREA ( #14546 ) ;
#30029=SURFACE_STYLE_FILL_AREA ( #34968 ) ;
#30030=CARTESIAN_POINT ( 'NONE',  ( -1.166476076187854022E-15, 113.9449999999999932, 9.525000000000000355 ) ) ;
#30032=EDGE_CURVE ( 'NONE', #37399, #39381, #1491, .T. ) ;
#30034=SURFACE_SIDE_STYLE ('',( #25452 ) ) ;
#30036=CARTESIAN_POINT ( 'NONE',  ( -71.18918918918917882, 14.09971791521133255, -9.500000000000000000 ) ) ;
#30037=CARTESIAN_POINT ( 'NONE',  ( 71.50000000000000000, 35.92875272052971525, 7.000000000000000000 ) ) ;
#30038=EDGE_CURVE ( 'NONE', #60303, #2848, #49872, .T. ) ;
#30043=CARTESIAN_POINT ( 'NONE',  ( 0.000000000000000000, 87.30187232391182306, 8.025000000000000355 ) ) ;
#30048=CARTESIAN_POINT ( 'NONE',  ( 45.50000000000000000, -1.469576158976824618E-14, 6.999999999999999112 ) ) ;
#30049=CARTESIAN_POINT ( 'NONE',  ( 7.632228543268608334, 123.4570736234661581, -2.479861379858951942 ) ) ;
#30051=DIRECTION ( 'NONE',  ( -0.000000000000000000, 1.000000000000000000, 0.000000000000000000 ) ) ;
#30054=( NAMED_UNIT ( * ) SI_UNIT ( $, .STERADIAN. ) SOLID_ANGLE_UNIT ( ) );
#30055=DIRECTION ( 'NONE',  ( 0.000000000000000000, 0.000000000000000000, 1.000000000000000000 ) ) ;
#30056=ORIENTED_EDGE ( 'NONE', *, *, #40850, .F. ) ;
#30057=( BOUNDED_CURVE ( )  B_SPLINE_CURVE ( 3, ( #17572, #66417, #49565, #55155 ),
 .UNSPECIFIED., .F., .F. ) 
 B_SPLINE_CURVE_WITH_KNOTS ( ( 4, 4 ),
 ( 1.570796326794883901, 3.141592653589793116 ),
 .UNSPECIFIED. ) 
 CURVE ( )  GEOMETRIC_REPRESENTATION_ITEM ( )  RATIONAL_B_SPLINE_CURVE ( ( 1.000000000000000000, 0.8047378541243619399, 0.8047378541243619399, 1.000000000000000000 ) ) 
 REPRESENTATION_ITEM ( '' )  );
#30058=CARTESIAN_POINT ( 'NONE',  ( -4.716976649647098618, 131.2570736234661695, 6.492361379858953008 ) ) ;
#30063=CARTESIAN_POINT ( 'NONE',  ( 75.00000000000000000, 19.58219357181276266, -6.973972669042648675 ) ) ;
#30068=DIRECTION ( 'NONE',  ( 1.000000000000000000, 0.000000000000000000, 0.000000000000000000 ) ) ;
#30069=LINE ( 'NONE', #51538, #66564 ) ;
#30073=DIRECTION ( 'NONE',  ( -1.000000000000000000, 0.000000000000000000, -0.000000000000000000 ) ) ;
#30075=ORIENTED_EDGE ( 'NONE', *, *, #59164, .T. ) ;
#30076=FILL_AREA_STYLE ('',( #67378 ) ) ;
#30081=( NAMED_UNIT ( * ) PLANE_ANGLE_UNIT ( ) SI_UNIT ( $, .RADIAN. ) );
#30082=ORIENTED_EDGE ( 'NONE', *, *, #48887, .T. ) ;
#30087=( NAMED_UNIT ( * ) SI_UNIT ( $, .STERADIAN. ) SOLID_ANGLE_UNIT ( ) );
#30089=CARTESIAN_POINT ( 'NONE',  ( 10.01517768586949408, 111.6949999999999932, 1.839758294383810543E-15 ) ) ;
#30091=DIRECTION ( 'NONE',  ( -0.000000000000000000, -0.000000000000000000, 1.000000000000000000 ) ) ;
#30093=SURFACE_STYLE_FILL_AREA ( #4755 ) ;
#30105=EDGE_LOOP ( 'NONE', ( #23839, #29928, #53486, #57802, #40486, #65723, #51017, #1633, #17980, #67752, #14626, #59468, #2937 ) ) ;
#30109=DIRECTION ( 'NONE',  ( 1.000000000000000000, -1.734723475976805517E-15, 0.000000000000000000 ) ) ;
#30111=CIRCLE ( 'NONE', #28947, 0.5000000000000004441 ) ;
#30113=CARTESIAN_POINT ( 'NONE',  ( 8.102448949553183510, 155.1049999999999898, -5.886773742842746238 ) ) ;
#30114=EDGE_CURVE ( 'NONE', #38290, #21071, #21797, .T. ) ;
#30118=DIRECTION ( 'NONE',  ( 1.000000000000000000, -1.776356839400250465E-15, 0.000000000000000000 ) ) ;
#30119=DIRECTION ( 'NONE',  ( 0.000000000000000000, 0.000000000000000000, 1.000000000000000000 ) ) ;
#30120=DIRECTION ( 'NONE',  ( 0.000000000000000000, 1.000000000000000000, 0.000000000000000000 ) ) ;
#30121=STYLED_ITEM ( 'NONE', ( #23987 ), #67921 ) ;
#30122=CARTESIAN_POINT ( 'NONE',  ( -74.99999999999998579, 50.00000000000000000, 7.000000000000000000 ) ) ;
#30124=ORIENTED_EDGE ( 'NONE', *, *, #34801, .T. ) ;
#30129=CIRCLE ( 'NONE', #8833, 0.5000000000000004441 ) ;
#30131=SURFACE_SIDE_STYLE ('',( #62150 ) ) ;
#30132=FILL_AREA_STYLE_COLOUR ( '', #8421 ) ;
#30134=CARTESIAN_POINT ( 'NONE',  ( -8.102448949553181734, 111.0049999999999955, -5.886773742842749790 ) ) ;
#30135=LINE ( 'NONE', #3737, #614 ) ;
#30136=ORIENTED_EDGE ( 'NONE', *, *, #19290, .F. ) ;
#30139=SURFACE_SIDE_STYLE ('',( #13629 ) ) ;
#30143=AXIS2_PLACEMENT_3D ( 'NONE', #42872, #11140, #32587 ) ;
#30145=CARTESIAN_POINT ( 'NONE',  ( -9.271665717542465046, 110.5000000000000142, -2.225342505666574322 ) ) ;
#30148=SURFACE_STYLE_USAGE ( .BOTH. , #46757 ) ;
#30150=CARTESIAN_POINT ( 'NONE',  ( 2.607480562269076430, 140.7929263765337851, -8.025000000000000355 ) ) ;
#30152=COLOUR_RGB ( '', 0.40784314, 0.44705882, 0.49803922) ;
#30155=ORIENTED_EDGE ( 'NONE', *, *, #18407, .T. ) ;
#30158=DIRECTION ( 'NONE',  ( 0.000000000000000000, 0.000000000000000000, -1.000000000000000000 ) ) ;
#30160=CARTESIAN_POINT ( 'NONE',  ( -20.57648123223228254, 114.4999999999999574, 10.27659574468085069 ) ) ;
#30161=DIRECTION ( 'NONE',  ( 1.000000000000000000, 0.000000000000000000, 0.000000000000000000 ) ) ;
#30162=AXIS2_PLACEMENT_3D ( 'NONE', #26817, #59186, #48352 ) ;
#30166=LINE ( 'NONE', #8041, #63527 ) ;
#30169=AXIS2_PLACEMENT_3D ( 'NONE', #28353, #23798, #61082 ) ;
#30171=SURFACE_STYLE_FILL_AREA ( #56221 ) ;
#30173=( NAMED_UNIT ( * ) SI_UNIT ( $, .STERADIAN. ) SOLID_ANGLE_UNIT ( ) );
#30174=DIRECTION ( 'NONE',  ( 1.000000000000000000, 0.000000000000000000, 0.000000000000000000 ) ) ;
#30183=DIRECTION ( 'NONE',  ( -0.000000000000000000, -0.000000000000000000, -1.000000000000000000 ) ) ;
#30184=CARTESIAN_POINT ( 'NONE',  ( 4.716976649647099507, 117.7570736234661553, -6.492361379858953008 ) ) ;
#30187=AXIS2_PLACEMENT_3D ( 'NONE', #37872, #21631, #17082 ) ;
#30189=CARTESIAN_POINT ( 'NONE',  ( 5.598654528085809545, 128.2549999999999670, -7.705886871421373741 ) ) ;
#30191=CARTESIAN_POINT ( 'NONE',  ( -75.00000000000000000, 7.768687147774688384, -6.999999999999999112 ) ) ;
#30192=AXIS2_PLACEMENT_3D ( 'NONE', #32612, #64973, #17523 ) ;
#30194=DIRECTION ( 'NONE',  ( 1.000000000000000000, 0.000000000000000000, 0.000000000000000000 ) ) ;
#30196=( GEOMETRIC_REPRESENTATION_CONTEXT ( 3 ) GLOBAL_UNCERTAINTY_ASSIGNED_CONTEXT ( ( #25497 ) ) GLOBAL_UNIT_ASSIGNED_CONTEXT ( ( #41734, #25508, #68435 ) ) REPRESENTATION_CONTEXT ( 'NONE', 'WORKASPACE' ) );
#30203=( GEOMETRIC_REPRESENTATION_CONTEXT ( 3 ) GLOBAL_UNCERTAINTY_ASSIGNED_CONTEXT ( ( #5286 ) ) GLOBAL_UNIT_ASSIGNED_CONTEXT ( ( #37377, #27086, #48620 ) ) REPRESENTATION_CONTEXT ( 'NONE', 'WORKASPACE' ) );
#30209=VERTEX_POINT ( 'NONE', #22275 ) ;
#30213=CARTESIAN_POINT ( 'NONE',  ( -2.607480562269157254, 147.0929263765338249, -8.024999999999939959 ) ) ;
#30223=CARTESIAN_POINT ( 'NONE',  ( 44.50000000000000000, 10.36037961002804408, -3.500000000000000000 ) ) ;
#30224=CARTESIAN_POINT ( 'NONE',  ( -47.50000000000000000, 14.49137674618942562, -9.500000000000000000 ) ) ;
#30225=ORIENTED_EDGE ( 'NONE', *, *, #7555, .T. ) ;
#30227=CARTESIAN_POINT ( 'NONE',  ( -8.102448949553181734, 136.8949999999999534, -5.886773742842749790 ) ) ;
#30229=ORIENTED_EDGE ( 'NONE', *, *, #48415, .F. ) ;
#30230=CARTESIAN_POINT ( 'NONE',  ( 0.000000000000000000, 146.5549999999999784, -9.525000000000000355 ) ) ;
#30232=CARTESIAN_POINT ( 'NONE',  ( -4.716976649647097730, 120.2429263765338163, -6.492361379858953896 ) ) ;
#30233=SURFACE_SIDE_STYLE ('',( #35559 ) ) ;
#30235=ADVANCED_FACE ( 'NONE', ( #4796 ), #44481, .F. ) ;
#30238=EDGE_CURVE ( 'NONE', #36309, #12165, #11724, .T. ) ;
#30239=CARTESIAN_POINT ( 'NONE',  ( 72.00000000000000000, 13.41640786499872284, -9.500000000000000000 ) ) ;
#30240=ORIENTED_EDGE ( 'NONE', *, *, #41920, .F. ) ;
#30242=SURFACE_SIDE_STYLE ('',( #9875 ) ) ;
#30247=DIRECTION ( 'NONE',  ( 0.6216216216216311485, -0.7833176619561784682, 0.000000000000000000 ) ) ;
#30248=CIRCLE ( 'NONE', #37045, 0.5000000000000004441 ) ;
#30250=PRESENTATION_STYLE_ASSIGNMENT (( #51055 ) ) ;
#30253=CARTESIAN_POINT ( 'NONE',  ( 74.65811388300841145, 19.88603796100278132, 6.000000000000000000 ) ) ;
#30254=DIRECTION ( 'NONE',  ( -0.000000000000000000, 1.000000000000000000, -0.000000000000000000 ) ) ;
#30255=VERTEX_POINT ( 'NONE', #61289 ) ;
#30257=FACE_OUTER_BOUND ( 'NONE', #37465, .T. ) ;
#30261=( NAMED_UNIT ( * ) PLANE_ANGLE_UNIT ( ) SI_UNIT ( $, .RADIAN. ) );
#30264=SURFACE_STYLE_USAGE ( .BOTH. , #25686 ) ;
#30271=( LENGTH_UNIT ( ) NAMED_UNIT ( * ) SI_UNIT ( .MILLI., .METRE. ) );
#30272=CARTESIAN_POINT ( 'NONE',  ( 9.058813317711337021, 135.5449999999999875, 2.943386871421375783 ) ) ;
#30276=CARTESIAN_POINT ( 'NONE',  ( -9.827790563157511022E-16, 145.4429263765338192, 8.025000000000000355 ) ) ;
#30277=CIRCLE ( 'NONE', #65146, 0.5000000000000004441 ) ;
#30278=VERTEX_POINT ( 'NONE', #66937 ) ;
#30283=CONICAL_SURFACE ( 'NONE', #39335, 5.499999999999976907, 0.7853981633974309595 ) ;
#30284=FILL_AREA_STYLE_COLOUR ( '', #28199 ) ;
#30285=EDGE_LOOP ( 'NONE', ( #24312, #62180, #62524, #45334 ) ) ;
#30287=ORIENTED_EDGE ( 'NONE', *, *, #21562, .F. ) ;
#30288=AXIS2_PLACEMENT_3D ( 'NONE', #17960, #45433, #66853 ) ;
#30289=SURFACE_SIDE_STYLE ('',( #56718 ) ) ;
#30290=( GEOMETRIC_REPRESENTATION_CONTEXT ( 3 ) GLOBAL_UNCERTAINTY_ASSIGNED_CONTEXT ( ( #16625 ) ) GLOBAL_UNIT_ASSIGNED_CONTEXT ( ( #3002, #13963, #18871 ) ) REPRESENTATION_CONTEXT ( 'NONE', 'WORKASPACE' ) );
#30294=AXIS2_PLACEMENT_3D ( 'NONE', #61365, #8959, #24419 ) ;
#30297=VERTEX_POINT ( 'NONE', #56352 ) ;
#30298=DIRECTION ( 'NONE',  ( 1.000000000000000000, 0.000000000000000000, 0.000000000000000000 ) ) ;
#30299=CARTESIAN_POINT ( 'NONE',  ( -15.48999599679679662, 118.4999999999999716, 7.500000000000000000 ) ) ;
#30301=EDGE_CURVE ( 'NONE', #48146, #60196, #24009, .T. ) ;
#30305=CARTESIAN_POINT ( 'NONE',  ( 3.094860106618435136, 112.2949999999999733, -9.525000000000000355 ) ) ;
#30312=CARTESIAN_POINT ( 'NONE',  ( -40.99999999999998579, 108.0041655821620168, -3.000000000000004441 ) ) ;
#30314=CARTESIAN_POINT ( 'NONE',  ( -3.094860106618432471, 137.7049999999999841, -9.525000000000000355 ) ) ;
#30316=( NAMED_UNIT ( * ) SI_UNIT ( $, .STERADIAN. ) SOLID_ANGLE_UNIT ( ) );
#30319=CARTESIAN_POINT ( 'NONE',  ( 19.98288066869250201, 115.0281754944747235, 9.999999999997170264 ) ) ;
#30321=EDGE_CURVE ( 'NONE', #11929, #30560, #52481, .T. ) ;
#30322=SURFACE_STYLE_FILL_AREA ( #29997 ) ;
#30324=DIRECTION ( 'NONE',  ( -0.000000000000000000, -0.000000000000000000, -1.000000000000000000 ) ) ;
#30329=DIRECTION ( 'NONE',  ( 0.000000000000000000, 0.000000000000000000, 1.000000000000000000 ) ) ;
#30334=( LENGTH_UNIT ( ) NAMED_UNIT ( * ) SI_UNIT ( .MILLI., .METRE. ) );
#30341=COLOUR_RGB ( '', 0.09019608, 0.27058824, 0.51372549) ;
#30343=CARTESIAN_POINT ( 'NONE',  ( -3.094860106618432471, 142.5949999999999989, -9.525000000000000355 ) ) ;
#30348=DIRECTION ( 'NONE',  ( 0.000000000000000000, -1.000000000000000000, 0.000000000000000000 ) ) ;
#30349=STYLED_ITEM ( 'NONE', ( #45515 ), #52525 ) ;
#30353=CARTESIAN_POINT ( 'NONE',  ( -9.058813317711338797, 110.3449999999999847, 2.943386871421373563 ) ) ;
#30358=ORIENTED_EDGE ( 'NONE', *, *, #47156, .T. ) ;
#30359=ADVANCED_FACE ( 'NONE', ( #29269 ), #56638, .F. ) ;
#30364=AXIS2_PLACEMENT_3D ( 'NONE', #19571, #56870, #30109 ) ;
#30371=( NAMED_UNIT ( * ) PLANE_ANGLE_UNIT ( ) SI_UNIT ( $, .RADIAN. ) );
#30372=DIRECTION ( 'NONE',  ( 0.000000000000000000, 0.000000000000000000, -1.000000000000000000 ) ) ;
#30376=FILL_AREA_STYLE ('',( #19143 ) ) ;
#30377=EDGE_CURVE ( 'NONE', #40156, #13502, #37608, .T. ) ;
#30385=ORIENTED_EDGE ( 'NONE', *, *, #23124, .T. ) ;
#30387=( GEOMETRIC_REPRESENTATION_CONTEXT ( 3 ) GLOBAL_UNCERTAINTY_ASSIGNED_CONTEXT ( ( #49001 ) ) GLOBAL_UNIT_ASSIGNED_CONTEXT ( ( #26256, #42838, #53678 ) ) REPRESENTATION_CONTEXT ( 'NONE', 'WORKASPACE' ) );
#30389=CARTESIAN_POINT ( 'NONE',  ( -6.826472737025120807, 133.5070736234661410, -4.959722759717907437 ) ) ;
#30394=COLOUR_RGB ( '', 0.09019608, 0.27058824, 0.51372549) ;
#30395=ORIENTED_EDGE ( 'NONE', *, *, #24615, .T. ) ;
#30397=SURFACE_STYLE_FILL_AREA ( #16624 ) ;
#30398=SURFACE_SIDE_STYLE ('',( #7584 ) ) ;
#30399=ADVANCED_FACE ( 'NONE', ( #63379 ), #63713, .F. ) ;
#30400=ORIENTED_EDGE ( 'NONE', *, *, #12769, .T. ) ;
#30401=CARTESIAN_POINT ( 'NONE',  ( -74.99999999999998579, 50.00000000000000000, -6.500000000000000000 ) ) ;
#30404=AXIS2_PLACEMENT_3D ( 'NONE', #64588, #31158, #16434 ) ;
#30406=CARTESIAN_POINT ( 'NONE',  ( -40.99999999999998579, 107.7459666690149902, -3.075798416731281293 ) ) ;
#30411=DIRECTION ( 'NONE',  ( 0.000000000000000000, 0.000000000000000000, 1.000000000000000000 ) ) ;
#30413=CARTESIAN_POINT ( 'NONE',  ( 44.50000000000000000, 10.36037961002804408, -3.500000000000000000 ) ) ;
#30414=DIRECTION ( 'NONE',  ( 3.469446951953611033E-15, 0.000000000000000000, -1.000000000000000000 ) ) ;
#30415=ORIENTED_EDGE ( 'NONE', *, *, #50668, .T. ) ;
#30420=STYLED_ITEM ( 'NONE', ( #69255 ), #59708 ) ;
#30422=CARTESIAN_POINT ( 'NONE',  ( 5.598654528085809545, 118.1449999999999818, -7.705886871421373741 ) ) ;
#30425=CARTESIAN_POINT ( 'NONE',  ( 4.716976649647096842, 112.7429263765338163, 6.492361379858953896 ) ) ;
#30429=ORIENTED_EDGE ( 'NONE', *, *, #37632, .T. ) ;
#30432=DIRECTION ( 'NONE',  ( -0.000000000000000000, -0.000000000000000000, 1.000000000000000000 ) ) ;
#30436=CARTESIAN_POINT ( 'NONE',  ( -0.8084438751943111567, 110.6282398156186986, -9.370611995446433085 ) ) ;
#30437=AXIS2_PLACEMENT_3D ( 'NONE', #39794, #40136, #14395 ) ;
#30440=VERTEX_POINT ( 'NONE', #60173 ) ;
#30442=AXIS2_PLACEMENT_3D ( 'NONE', #32222, #20980, #37566 ) ;
#30445=PRESENTATION_STYLE_ASSIGNMENT (( #16064 ) ) ;
#30451=CARTESIAN_POINT ( 'NONE',  ( 9.058813317711338797, 151.9550000000000125, -2.943386871421372675 ) ) ;
#30457=CIRCLE ( 'NONE', #28186, 0.5000000000000004441 ) ;
#30462=CARTESIAN_POINT ( 'NONE',  ( -2.525713312987405423, 110.7492558248162737, 8.932758862731871474 ) ) ;
#30464=STYLED_ITEM ( 'NONE', ( #58397 ), #28103 ) ;
#30469=( NAMED_UNIT ( * ) PLANE_ANGLE_UNIT ( ) SI_UNIT ( $, .RADIAN. ) );
#30470=ORIENTED_EDGE ( 'NONE', *, *, #1916, .T. ) ;
#30471=ORIENTED_EDGE ( 'NONE', *, *, #12634, .F. ) ;
#30472=DIRECTION ( 'NONE',  ( 0.000000000000000000, -0.000000000000000000, 1.000000000000000000 ) ) ;
#30473=AXIS2_PLACEMENT_3D ( 'NONE', #1441, #17705, #26816 ) ;
#30480=ADVANCED_FACE ( 'NONE', ( #43014 ), #65665, .T. ) ;
#30484=VERTEX_POINT ( 'NONE', #670 ) ;
#30485=CARTESIAN_POINT ( 'NONE',  ( -5.598654528085806881, 116.8549999999999898, -7.705886871421374629 ) ) ;
#30486=DIRECTION ( 'NONE',  ( 0.000000000000000000, 0.000000000000000000, 1.000000000000000000 ) ) ;
#30487=EDGE_LOOP ( 'NONE', ( #35302, #33402, #19232, #60986 ) ) ;
#30492=CARTESIAN_POINT ( 'NONE',  ( 44.91886116991580735, 9.999999999999980460, 3.201362207699192997 ) ) ;
#30494=CARTESIAN_POINT ( 'NONE',  ( 71.50000000000000000, 14.49137674618942562, 9.500000000000000000 ) ) ;
#30496=CARTESIAN_POINT ( 'NONE',  ( -2.607480562269073765, 141.0929263765338249, -8.025000000000000355 ) ) ;
#30497=DIRECTION ( 'NONE',  ( -0.000000000000000000, -0.000000000000000000, -1.000000000000000000 ) ) ;
#30498=VECTOR ( 'NONE', #56435, 1000.000000000000000 ) ;
#30501=EDGE_LOOP ( 'NONE', ( #23014, #13560, #13969, #55410 ) ) ;
#30503=CARTESIAN_POINT ( 'NONE',  ( -9.827790563157511022E-16, 127.4429263765338192, 8.025000000000000355 ) ) ;
#30504=PLANE ( 'NONE',  #30143 ) ;
#30508=( NAMED_UNIT ( * ) PLANE_ANGLE_UNIT ( ) SI_UNIT ( $, .RADIAN. ) );
#30509=EDGE_CURVE ( 'NONE', #30255, #21436, #38602, .T. ) ;
#30512=DIRECTION ( 'NONE',  ( 1.000000000000000000, 0.000000000000000000, 0.000000000000000000 ) ) ;
#30514=DIRECTION ( 'NONE',  ( -1.000000000000000000, 0.000000000000000000, 0.000000000000000000 ) ) ;
#30515=ORIENTED_EDGE ( 'NONE', *, *, #48985, .F. ) ;
#30516=VERTEX_POINT ( 'NONE', #3098 ) ;
#30517=FACE_BOUND ( 'NONE', #55068, .T. ) ;
#30518=FILL_AREA_STYLE ('',( #4844 ) ) ;
#30520=CARTESIAN_POINT ( 'NONE',  ( 60.00000000000000000, 1.797044900979284448E-15, 9.500000000000000000 ) ) ;
#30521=VERTEX_POINT ( 'NONE', #29177 ) ;
#30522=( LENGTH_UNIT ( ) NAMED_UNIT ( * ) SI_UNIT ( .MILLI., .METRE. ) );
#30526=MECHANICAL_DESIGN_GEOMETRIC_PRESENTATION_REPRESENTATION('',(#41786),#48574);
#30529=ORIENTED_EDGE ( 'NONE', *, *, #48963, .F. ) ;
#30532=VECTOR ( 'NONE', #67333, 1000.000000000000000 ) ;
#30533=PRESENTATION_STYLE_ASSIGNMENT (( #57284 ) ) ;
#30541=CARTESIAN_POINT ( 'NONE',  ( -3.094860106618434248, 123.9049999999999727, 9.525000000000000355 ) ) ;
#30543=CARTESIAN_POINT ( 'NONE',  ( 20.54906699372407175, 114.6596276111864228, -10.28538896680103853 ) ) ;
#30547=UNCERTAINTY_MEASURE_WITH_UNIT (LENGTH_MEASURE( 1.000000000000000082E-05 ), #20589, 'distance_accuracy_value', 'NONE');
#30553=CARTESIAN_POINT ( 'NONE',  ( -7.632228543268608334, 145.9570736234661581, 2.479861379858952830 ) ) ;
#30560=VERTEX_POINT ( 'NONE', #7054 ) ;
#30561=SURFACE_STYLE_FILL_AREA ( #9145 ) ;
#30566=VECTOR ( 'NONE', #33144, 1000.000000000000000 ) ;
#30567=SURFACE_STYLE_USAGE ( .BOTH. , #14398 ) ;
#30572=ORIENTED_EDGE ( 'NONE', *, *, #64102, .T. ) ;
#30577=PRESENTATION_STYLE_ASSIGNMENT (( #61903 ) ) ;
#30578=ORIENTED_EDGE ( 'NONE', *, *, #22261, .T. ) ;
#30580=CARTESIAN_POINT ( 'NONE',  ( -8.102448949553181734, 146.4950000000000045, 5.886773742842747126 ) ) ;
#30581=ORIENTED_EDGE ( 'NONE', *, *, #51054, .T. ) ;
#30583=CARTESIAN_POINT ( 'NONE',  ( -10.01517768586949408, 147.3049999999999500, -6.132527647946036459E-16 ) ) ;
#30585=PRESENTATION_STYLE_ASSIGNMENT (( #58052 ) ) ;
#30587=CARTESIAN_POINT ( 'NONE',  ( -2.607480562269075097, 112.2929263765337993, 8.025000000000000355 ) ) ;
#30588=SURFACE_STYLE_FILL_AREA ( #45782 ) ;
#30589=UNCERTAINTY_MEASURE_WITH_UNIT (LENGTH_MEASURE( 1.000000000000000082E-05 ), #44578, 'distance_accuracy_value', 'NONE');
#30590=CARTESIAN_POINT ( 'NONE',  ( -68.49999999999998579, -1.919947267060472329E-14, 10.00000000000000000 ) ) ;
#30593=LINE ( 'NONE', #35895, #35491 ) ;
#30597=CARTESIAN_POINT ( 'NONE',  ( 23.71231517720798010, 113.4999999999999858, 7.500000000000000000 ) ) ;
#30598=ORIENTED_EDGE ( 'NONE', *, *, #15538, .T. ) ;
#30602=AXIS2_PLACEMENT_3D ( 'NONE', #66164, #17334, #54577 ) ;
#30606=UNCERTAINTY_MEASURE_WITH_UNIT (LENGTH_MEASURE( 1.000000000000000082E-05 ), #20747, 'distance_accuracy_value', 'NONE');
#30608=DIRECTION ( 'NONE',  ( 0.000000000000000000, 0.000000000000000000, 1.000000000000000000 ) ) ;
#30610=CARTESIAN_POINT ( 'NONE',  ( 75.00000000000000000, 19.58219357181275555, 6.973972669042709960 ) ) ;
#30611=ORIENTED_EDGE ( 'NONE', *, *, #17123, .F. ) ;
#30613=DIRECTION ( 'NONE',  ( 1.387778780781444413E-14, -1.000000000000000000, 0.000000000000000000 ) ) ;
#30614=STYLED_ITEM ( 'NONE', ( #22049 ), #6977 ) ;
#30615=MECHANICAL_DESIGN_GEOMETRIC_PRESENTATION_REPRESENTATION('',(#4808),#9304);
#30619=AXIS2_PLACEMENT_3D ( 'NONE', #23437, #17834, #35044 ) ;
#30620=CARTESIAN_POINT ( 'NONE',  ( -41.49999999999997868, 10.49999999999998224, 3.000000000000000000 ) ) ;
#30625=COLOUR_RGB ( '', 0.31764706, 0.68627451, 0.89019608) ;
#30626=CARTESIAN_POINT ( 'NONE',  ( 60.00000000000000000, 115.4999999999999574, -10.00000000000000000 ) ) ;
#30628=CARTESIAN_POINT ( 'NONE',  ( -10.01517768586949231, 149.1950000000000216, -6.132527647946036459E-16 ) ) ;
#30630=EDGE_CURVE ( 'NONE', #11216, #5105, #49990, .T. ) ;
#30632=DIRECTION ( 'NONE',  ( 0.000000000000000000, 0.000000000000000000, -1.000000000000000000 ) ) ;
#30633=UNCERTAINTY_MEASURE_WITH_UNIT (LENGTH_MEASURE( 1.000000000000000082E-05 ), #2426, 'distance_accuracy_value', 'NONE');
#30635=CIRCLE ( 'NONE', #40827, 26.49999999999999645 ) ;
#30636=ORIENTED_EDGE ( 'NONE', *, *, #65878, .F. ) ;
#30641=EDGE_CURVE ( 'NONE', #51351, #51980, #30815, .T. ) ;
#30645=FACE_OUTER_BOUND ( 'NONE', #10993, .T. ) ;
#30646=ORIENTED_EDGE ( 'NONE', *, *, #44284, .T. ) ;
#30653=CARTESIAN_POINT ( 'NONE',  ( 6.826472737025119919, 118.8929263765337936, 4.959722759717908325 ) ) ;
#30661=ORIENTED_EDGE ( 'NONE', *, *, #52765, .F. ) ;
#30666=DIRECTION ( 'NONE',  ( 1.000000000000000000, 0.000000000000000000, 0.000000000000000000 ) ) ;
#30667=CARTESIAN_POINT ( 'NONE',  ( -3.094860106618432471, 112.5949999999999989, -9.525000000000000355 ) ) ;
#30668=ORIENTED_EDGE ( 'NONE', *, *, #60745, .F. ) ;
#30670=CARTESIAN_POINT ( 'NONE',  ( -5.598654528085808657, 120.7549999999999812, 7.705886871421373741 ) ) ;
#30673=CARTESIAN_POINT ( 'NONE',  ( 3.094860106618435136, 140.4050000000000011, -9.525000000000000355 ) ) ;
#30675=CARTESIAN_POINT ( 'NONE',  ( 15.98999599679679839, 146.4999999999999716, -7.500000000000000000 ) ) ;
#30677=SURFACE_STYLE_USAGE ( .BOTH. , #3944 ) ;
#30681=FILL_AREA_STYLE_COLOUR ( '', #27220 ) ;
#30685=CARTESIAN_POINT ( 'NONE',  ( 8.003604573459384142, 111.5754815414098289, -2.762566347670379674 ) ) ;
#30688=FILL_AREA_STYLE_COLOUR ( '', #62369 ) ;
#30691=FACE_OUTER_BOUND ( 'NONE', #38058, .T. ) ;
#30693=AXIS2_PLACEMENT_3D ( 'NONE', #56440, #13881, #35348 ) ;
#30698=CARTESIAN_POINT ( 'NONE',  ( 9.058813317711338797, 153.8449999999999704, -2.943386871421372675 ) ) ;
#30702=AXIS2_PLACEMENT_3D ( 'NONE', #62584, #46466, #68932 ) ;
#30705=DIRECTION ( 'NONE',  ( -1.000000000000000000, 0.000000000000000000, 3.469446951953610639E-15 ) ) ;
#30707=( NAMED_UNIT ( * ) SI_UNIT ( $, .STERADIAN. ) SOLID_ANGLE_UNIT ( ) );
#30711=CARTESIAN_POINT ( 'NONE',  ( -5.598654528085808657, 116.6449999999999818, 7.705886871421373741 ) ) ;
#30719=DIRECTION ( 'NONE',  ( 0.000000000000000000, 0.000000000000000000, 1.000000000000000000 ) ) ;
#30729=ADVANCED_FACE ( 'NONE', ( #8098 ), #65516, .F. ) ;
#30730=AXIS2_PLACEMENT_3D ( 'NONE', #20018, #52755, #19685 ) ;
#30738=DIRECTION ( 'NONE',  ( -0.000000000000000000, 0.000000000000000000, 1.000000000000000000 ) ) ;
#30743=AXIS2_PLACEMENT_3D ( 'NONE', #7816, #8867, #41259 ) ;
#30746=FILL_AREA_STYLE ('',( #62751 ) ) ;
#30747=VERTEX_POINT ( 'NONE', #68580 ) ;
#30750=DIRECTION ( 'NONE',  ( -1.000000000000000000, 0.000000000000000000, 0.000000000000000000 ) ) ;
#30751=CARTESIAN_POINT ( 'NONE',  ( -7.632228543268607446, 130.6570736234661467, -2.479861379858953718 ) ) ;
#30752=SURFACE_STYLE_USAGE ( .BOTH. , #51892 ) ;
#30759=ORIENTED_EDGE ( 'NONE', *, *, #16800, .T. ) ;
#30760=COLOUR_RGB ( '', 0.08235294, 0.09019608, 0.10196078) ;
#30766=VERTEX_POINT ( 'NONE', #3458 ) ;
#30767=COLOUR_RGB ( '', 0.66274510, 0.83137255, 0.94901961) ;
#30768=FILL_AREA_STYLE_COLOUR ( '', #3600 ) ;
#30770=ORIENTED_EDGE ( 'NONE', *, *, #58684, .F. ) ;
#30773=CIRCLE ( 'NONE', #56595, 0.5000000000000004441 ) ;
#30775=EDGE_LOOP ( 'NONE', ( #58713, #59540, #13627, #60051 ) ) ;
#30777=( NAMED_UNIT ( * ) SI_UNIT ( $, .STERADIAN. ) SOLID_ANGLE_UNIT ( ) );
#30779=SURFACE_STYLE_USAGE ( .BOTH. , #67737 ) ;
#30780=ORIENTED_EDGE ( 'NONE', *, *, #7480, .F. ) ;
#30783=CARTESIAN_POINT ( 'NONE',  ( -71.62068965517238439, 63.58603185604027885, -7.000000000000000000 ) ) ;
#30784=CARTESIAN_POINT ( 'NONE',  ( 48.00000000000000000, 99.99999999999992895, 7.500000000000000000 ) ) ;
#30788=CARTESIAN_POINT ( 'NONE',  ( 5.598654528085805993, 126.2449999999999903, 7.705886871421374629 ) ) ;
#30790=CARTESIAN_POINT ( 'NONE',  ( 6.826472737025119919, 112.8929263765338078, 4.959722759717908325 ) ) ;
#30791=CARTESIAN_POINT ( 'NONE',  ( -71.50000000000000000, 35.92875272052971525, -7.500000000000000000 ) ) ;
#30792=ORIENTED_EDGE ( 'NONE', *, *, #62562, .F. ) ;
#30794=CARTESIAN_POINT ( 'NONE',  ( 45.00000000000000000, -1.469576158976824618E-14, 6.999999999999999112 ) ) ;
#30800=CARTESIAN_POINT ( 'NONE',  ( -75.00000000000000000, 8.749900610107138377, 6.882725987574753290 ) ) ;
#30807=EDGE_CURVE ( 'NONE', #53177, #4250, #68906, .T. ) ;
#30808=DIRECTION ( 'NONE',  ( -0.7833176619561811327, 0.6216216216216278179, -0.000000000000000000 ) ) ;
#30815=CIRCLE ( 'NONE', #36500, 0.5000000000000004441 ) ;
#30817=CARTESIAN_POINT ( 'NONE',  ( -3.094860106618432471, 152.7049999999999841, -9.525000000000000355 ) ) ;
#30819=ADVANCED_FACE ( 'NONE', ( #9842 ), #66677, .F. ) ;
#30820=PRESENTATION_STYLE_ASSIGNMENT (( #37555 ) ) ;
#30825=COLOUR_RGB ( '', 0.09019608, 0.27058824, 0.51372549) ;
#30827=( NAMED_UNIT ( * ) SI_UNIT ( $, .STERADIAN. ) SOLID_ANGLE_UNIT ( ) );
#30830=AXIS2_PLACEMENT_3D ( 'NONE', #25313, #9156, #68240 ) ;
#30835=CARTESIAN_POINT ( 'NONE',  ( -20.55652580482692926, 114.6393193824117844, 10.28299520148690682 ) ) ;
#30837=STYLED_ITEM ( 'NONE', ( #47914 ), #1993 ) ;
#30838=SURFACE_STYLE_USAGE ( .BOTH. , #35784 ) ;
#30839=EDGE_LOOP ( 'NONE', ( #60500, #61904, #57847, #12236 ) ) ;
#30840=VERTEX_POINT ( 'NONE', #53099 ) ;
#30843=CARTESIAN_POINT ( 'NONE',  ( 74.50000000000000000, 3.473944261090200865E-15, -10.00000000000000000 ) ) ;
#30844=EDGE_LOOP ( 'NONE', ( #33194, #25527, #65010 ) ) ;
#30845=CARTESIAN_POINT ( 'NONE',  ( 3.094860106618435136, 116.4049999999999869, -9.525000000000000355 ) ) ;
#30849=CYLINDRICAL_SURFACE ( 'NONE', #9233, 23.00000000000000000 ) ;
#30856=AXIS2_PLACEMENT_3D ( 'NONE', #8687, #25534, #13958 ) ;
#30857=ORIENTED_EDGE ( 'NONE', *, *, #37615, .T. ) ;
#30858=CARTESIAN_POINT ( 'NONE',  ( 8.437984349512095861, 158.1929263765337623, 1.550032578732817026E-15 ) ) ;
#30860=ADVANCED_FACE ( 'NONE', ( #67893 ), #15818, .F. ) ;
#30861=CARTESIAN_POINT ( 'NONE',  ( -74.50000000000000000, -2.208799022165584366E-14, 9.500000000000000000 ) ) ;
#30862=DIRECTION ( 'NONE',  ( -1.000000000000000000, -0.000000000000000000, -0.000000000000000000 ) ) ;
#30864=CARTESIAN_POINT ( 'NONE',  ( 0.000000000000000000, 154.9999999999999716, -23.00000000000000000 ) ) ;
#30866=SURFACE_STYLE_USAGE ( .BOTH. , #9436 ) ;
#30867=FILL_AREA_STYLE ('',( #21018 ) ) ;
#30868=SURFACE_SIDE_STYLE ('',( #64265 ) ) ;
#30872=AXIS2_PLACEMENT_3D ( 'NONE', #31381, #57803, #26110 ) ;
#30881=EDGE_LOOP ( 'NONE', ( #67063, #28061, #23686 ) ) ;
#30887=AXIS2_PLACEMENT_3D ( 'NONE', #23837, #66758, #18576 ) ;
#30897=CARTESIAN_POINT ( 'NONE',  ( -74.82043395980159062, 36.18002821201687169, -9.907562454915460393 ) ) ;
#30898=EDGE_CURVE ( 'NONE', #53938, #30278, #48890, .T. ) ;
#30900=CARTESIAN_POINT ( 'NONE',  ( -1.166476076187854022E-15, 130.0549999999999784, 9.525000000000000355 ) ) ;
#30903=MECHANICAL_DESIGN_GEOMETRIC_PRESENTATION_REPRESENTATION('',(#35439),#47857);
#30905=DIRECTION ( 'NONE',  ( 0.000000000000000000, 1.000000000000000000, -0.000000000000000000 ) ) ;
#30909=PRESENTATION_STYLE_ASSIGNMENT (( #29877 ) ) ;
#30915=CARTESIAN_POINT ( 'NONE',  ( 4.716976649647099507, 135.7570736234661695, -6.492361379858953008 ) ) ;
#30917=FILL_AREA_STYLE_COLOUR ( '', #19284 ) ;
#30919=ORIENTED_EDGE ( 'NONE', *, *, #49800, .T. ) ;
#30920=DIRECTION ( 'NONE',  ( 0.000000000000000000, 0.000000000000000000, 1.000000000000000000 ) ) ;
#30921=DIRECTION ( 'NONE',  ( 0.000000000000000000, -1.000000000000000000, 0.000000000000000000 ) ) ;
#30922=( GEOMETRIC_REPRESENTATION_CONTEXT ( 3 ) GLOBAL_UNCERTAINTY_ASSIGNED_CONTEXT ( ( #9613 ) ) GLOBAL_UNIT_ASSIGNED_CONTEXT ( ( #60216, #61252, #44772 ) ) REPRESENTATION_CONTEXT ( 'NONE', 'WORKASPACE' ) );
#30923=MECHANICAL_DESIGN_GEOMETRIC_PRESENTATION_REPRESENTATION('',(#50041),#57918);
#30925=DIRECTION ( 'NONE',  ( -0.000000000000000000, -0.000000000000000000, 1.000000000000000000 ) ) ;
#30936=MECHANICAL_DESIGN_GEOMETRIC_PRESENTATION_REPRESENTATION('',(#56770),#41071);
#30938=CARTESIAN_POINT ( 'NONE',  ( 9.058813317711337021, 153.5449999999999875, 2.943386871421375783 ) ) ;
#30940=ADVANCED_FACE ( 'NONE', ( #37653 ), #59049, .F. ) ;
#30942=CARTESIAN_POINT ( 'NONE',  ( 9.058813317711338797, 148.9550000000000125, -2.943386871421372675 ) ) ;
#30943=SURFACE_SIDE_STYLE ('',( #64345 ) ) ;
#30944=FILL_AREA_STYLE ('',( #57695 ) ) ;
#30946=CARTESIAN_POINT ( 'NONE',  ( 0.000000000000000000, 125.9429263765338192, -8.025000000000000355 ) ) ;
#30950=AXIS2_PLACEMENT_3D ( 'NONE', #36262, #245, #4177 ) ;
#30951=CARTESIAN_POINT ( 'NONE',  ( -34.99999999999999289, 99.99999999999998579, -3.500000000000000000 ) ) ;
#30953=CARTESIAN_POINT ( 'NONE',  ( 41.05151532188900632, 107.6719357445258538, 3.224518739502659770 ) ) ;
#30956=( NAMED_UNIT ( * ) SI_UNIT ( $, .STERADIAN. ) SOLID_ANGLE_UNIT ( ) );
#30959=ORIENTED_EDGE ( 'NONE', *, *, #9728, .T. ) ;
#30960=PRESENTATION_STYLE_ASSIGNMENT (( #9544 ) ) ;
#30961=CIRCLE ( 'NONE', #36601, 5.499999999999976907 ) ;
#30962=EDGE_CURVE ( 'NONE', #44609, #30484, #34393, .T. ) ;
#30966=CARTESIAN_POINT ( 'NONE',  ( 6.826472737025121695, 146.4929263765338305, -4.959722759717905660 ) ) ;
#30970=SURFACE_SIDE_STYLE ('',( #67580 ) ) ;
#30976=PRESENTATION_STYLE_ASSIGNMENT (( #30264 ) ) ;
#30978=DIRECTION ( 'NONE',  ( 0.000000000000000000, 0.000000000000000000, 1.000000000000000000 ) ) ;
#30979=ORIENTED_EDGE ( 'NONE', *, *, #39590, .F. ) ;
#30981=CARTESIAN_POINT ( 'NONE',  ( -74.11218598454972550, 9.325134922070571264, -6.185423913763112402 ) ) ;
#30984=PRESENTATION_STYLE_ASSIGNMENT (( #66909 ) ) ;
#30988=CARTESIAN_POINT ( 'NONE',  ( -8.102448949553181734, 149.4949999999999761, 5.886773742842747126 ) ) ;
#30990=DIRECTION ( 'NONE',  ( 1.000000000000000000, 0.000000000000000000, 0.000000000000000000 ) ) ;
#30995=VERTEX_POINT ( 'NONE', #23157 ) ;
#30999=( LENGTH_UNIT ( ) NAMED_UNIT ( * ) SI_UNIT ( .MILLI., .METRE. ) );
#31002=COLOUR_RGB ( '', 0.40784314, 0.44705882, 0.49803922) ;
#31003=PRESENTATION_STYLE_ASSIGNMENT (( #68308 ) ) ;
#31004=EDGE_LOOP ( 'NONE', ( #42882, #55419, #67278 ) ) ;
#31006=ORIENTED_EDGE ( 'NONE', *, *, #33980, .F. ) ;
#31007=EDGE_CURVE ( 'NONE', #45578, #21243, #39697, .T. ) ;
#31010=CARTESIAN_POINT ( 'NONE',  ( -45.00000000000000000, 9.708372675170622301, 6.000000000000001776 ) ) ;
#31016=SURFACE_SIDE_STYLE ('',( #47961 ) ) ;
#31021=CARTESIAN_POINT ( 'NONE',  ( 0.000000000000000000, 124.4449999999999932, -9.525000000000000355 ) ) ;
#31022=VECTOR ( 'NONE', #19925, 1000.000000000000000 ) ;
#31023=ORIENTED_EDGE ( 'NONE', *, *, #7488, .T. ) ;
#31025=CARTESIAN_POINT ( 'NONE',  ( 9.058813317711337021, 124.6549999999999869, 2.943386871421375783 ) ) ;
#31028=ORIENTED_EDGE ( 'NONE', *, *, #43266, .F. ) ;
#31029=CARTESIAN_POINT ( 'NONE',  ( -9.058813317711338797, 135.4549999999999841, 2.943386871421373563 ) ) ;
#31031=MECHANICAL_DESIGN_GEOMETRIC_PRESENTATION_REPRESENTATION('',(#61355),#33303);
#31038=CARTESIAN_POINT ( 'NONE',  ( 0.000000000000000000, 124.0570736234661524, -8.025000000000000355 ) ) ;
#31039=LINE ( 'NONE', #62686, #19407 ) ;
#31042=CARTESIAN_POINT ( 'NONE',  ( 8.253986449296842665, 111.5397190885544347, -1.986321737243862406 ) ) ;
#31048=VERTEX_POINT ( 'NONE', #41960 ) ;
#31051=EDGE_CURVE ( 'NONE', #2414, #55582, #15223, .T. ) ;
#31053=ORIENTED_EDGE ( 'NONE', *, *, #26374, .F. ) ;
#31057=CARTESIAN_POINT ( 'NONE',  ( 9.058813317711337021, 147.5449999999999875, 2.943386871421375783 ) ) ;
#31060=DIRECTION ( 'NONE',  ( 0.000000000000000000, 0.000000000000000000, -1.000000000000000000 ) ) ;
#31061=DIRECTION ( 'NONE',  ( 0.000000000000000000, 0.000000000000000000, 1.000000000000000000 ) ) ;
#31064=ADVANCED_FACE ( 'NONE', ( #53176 ), #46542, .T. ) ;
#31067=CARTESIAN_POINT ( 'NONE',  ( 8.102448949553183510, 123.9949999999999903, -5.886773742842746238 ) ) ;
#31070=DIRECTION ( 'NONE',  ( 0.000000000000000000, 0.000000000000000000, 1.000000000000000000 ) ) ;
#31072=ORIENTED_EDGE ( 'NONE', *, *, #56238, .T. ) ;
#31081=( NAMED_UNIT ( * ) PLANE_ANGLE_UNIT ( ) SI_UNIT ( $, .RADIAN. ) );
#31082=ORIENTED_EDGE ( 'NONE', *, *, #32902, .T. ) ;
#31085=CARTESIAN_POINT ( 'NONE',  ( 44.99999999999998579, 119.9999999999999716, -10.00000000000000000 ) ) ;
#31088=DIRECTION ( 'NONE',  ( -0.000000000000000000, -1.000000000000000000, 0.000000000000000000 ) ) ;
#31089=COLOUR_RGB ( '', 0.66274510, 0.83137255, 0.94901961) ;
#31093=FILL_AREA_STYLE ('',( #13531 ) ) ;
#31096=SURFACE_SIDE_STYLE ('',( #46655 ) ) ;
#31097=CARTESIAN_POINT ( 'NONE',  ( 4.716976649647096842, 143.8570736234661638, 6.492361379858953896 ) ) ;
#31098=( NAMED_UNIT ( * ) PLANE_ANGLE_UNIT ( ) SI_UNIT ( $, .RADIAN. ) );
#31106=EDGE_CURVE ( 'NONE', #15830, #33977, #20685, .T. ) ;
#31108=DIRECTION ( 'NONE',  ( 1.000000000000000000, 0.000000000000000000, 0.000000000000000000 ) ) ;
#31110=ORIENTED_EDGE ( 'NONE', *, *, #66213, .F. ) ;
#31111=DIRECTION ( 'NONE',  ( 0.000000000000000000, 0.000000000000000000, 1.000000000000000000 ) ) ;
#31113=UNCERTAINTY_MEASURE_WITH_UNIT (LENGTH_MEASURE( 1.000000000000000082E-05 ), #40578, 'distance_accuracy_value', 'NONE');
#31118=FACE_OUTER_BOUND ( 'NONE', #33996, .T. ) ;
#31119=( LENGTH_UNIT ( ) NAMED_UNIT ( * ) SI_UNIT ( .MILLI., .METRE. ) );
#31122=FACE_OUTER_BOUND ( 'NONE', #55425, .T. ) ;
#31125=DIRECTION ( 'NONE',  ( 0.000000000000000000, 0.000000000000000000, -1.000000000000000000 ) ) ;
#31127=CYLINDRICAL_SURFACE ( 'NONE', #59143, 0.5000000000000004441 ) ;
#31130=CARTESIAN_POINT ( 'NONE',  ( 9.058813317711338797, 123.8449999999999847, -2.943386871421372675 ) ) ;
#31132=CARTESIAN_POINT ( 'NONE',  ( 7.632228543268607446, 113.0429263765338135, 2.479861379858954606 ) ) ;
#31134=ORIENTED_EDGE ( 'NONE', *, *, #30238, .T. ) ;
#31136=CARTESIAN_POINT ( 'NONE',  ( 44.43085292287548071, 10.23783787917552246, 3.499999999999995115 ) ) ;
#31138=FILL_AREA_STYLE_COLOUR ( '', #37776 ) ;
#31139=AXIS2_PLACEMENT_3D ( 'NONE', #42270, #59391, #26688 ) ;
#31145=ORIENTED_EDGE ( 'NONE', *, *, #25626, .F. ) ;
#31149=DIRECTION ( 'NONE',  ( 0.000000000000000000, 0.000000000000000000, 1.000000000000000000 ) ) ;
#31150=UNCERTAINTY_MEASURE_WITH_UNIT (LENGTH_MEASURE( 1.000000000000000082E-05 ), #66588, 'distance_accuracy_value', 'NONE');
#31153=CARTESIAN_POINT ( 'NONE',  ( -10.01517768586949231, 159.3049999999999784, -6.132527647946036459E-16 ) ) ;
#31155=PRESENTATION_STYLE_ASSIGNMENT (( #9749 ) ) ;
#31156=UNCERTAINTY_MEASURE_WITH_UNIT (LENGTH_MEASURE( 1.000000000000000082E-05 ), #61759, 'distance_accuracy_value', 'NONE');
#31158=DIRECTION ( 'NONE',  ( 0.000000000000000000, 1.000000000000000000, 0.000000000000000000 ) ) ;
#31161=FACE_OUTER_BOUND ( 'NONE', #13361, .T. ) ;
#31164=CARTESIAN_POINT ( 'NONE',  ( 71.99999999999998579, 119.9999999999997868, -9.500000000000000000 ) ) ;
#31168=( BOUNDED_CURVE ( )  B_SPLINE_CURVE ( 3, ( #16410, #21280, #37883, #48081 ),
 .UNSPECIFIED., .F., .F. ) 
 B_SPLINE_CURVE_WITH_KNOTS ( ( 4, 4 ),
 ( 0.000000000000000000, 1.570796326794893227 ),
 .UNSPECIFIED. ) 
 CURVE ( )  GEOMETRIC_REPRESENTATION_ITEM ( )  RATIONAL_B_SPLINE_CURVE ( ( 1.000000000000000000, 0.8047378541243658256, 0.8047378541243658256, 1.000000000000000000 ) ) 
 REPRESENTATION_ITEM ( '' )  );
#31172=FILL_AREA_STYLE ('',( #41093 ) ) ;
#31179=ORIENTED_EDGE ( 'NONE', *, *, #5546, .F. ) ;
#31180=CARTESIAN_POINT ( 'NONE',  ( 0.000000000000000000, 116.5549999999999926, -9.525000000000000355 ) ) ;
#31182=DIRECTION ( 'NONE',  ( 1.000000000000000000, 0.000000000000000000, 0.000000000000000000 ) ) ;
#31187=DIRECTION ( 'NONE',  ( 0.000000000000000000, 1.000000000000000000, -0.000000000000000000 ) ) ;
#31188=DIRECTION ( 'NONE',  ( -0.000000000000000000, 1.000000000000000000, -0.000000000000000000 ) ) ;
#31190=CARTESIAN_POINT ( 'NONE',  ( -4.716976649647098618, 157.1429263765338078, 6.492361379858953008 ) ) ;
#31191=SURFACE_SIDE_STYLE ('',( #168 ) ) ;
#31194=VERTEX_POINT ( 'NONE', #22694 ) ;
#31195=( NAMED_UNIT ( * ) PLANE_ANGLE_UNIT ( ) SI_UNIT ( $, .RADIAN. ) );
#31198=FACE_OUTER_BOUND ( 'NONE', #42082, .T. ) ;
#31200=CARTESIAN_POINT ( 'NONE',  ( 44.99999999999998579, 119.9999999999999716, 7.500000000000000000 ) ) ;
#31202=FACE_OUTER_BOUND ( 'NONE', #1720, .T. ) ;
#31205=CARTESIAN_POINT ( 'NONE',  ( -74.08452722063037754, 9.430195807687217879, 6.039972492249782832 ) ) ;
#31207=DIRECTION ( 'NONE',  ( -1.000000000000000000, 0.000000000000000000, -0.000000000000000000 ) ) ;
#31209=CARTESIAN_POINT ( 'NONE',  ( 0.000000000000000000, 87.30187232391182306, 0.000000000000000000 ) ) ;
#31210=ORIENTED_EDGE ( 'NONE', *, *, #35340, .F. ) ;
#31211=ORIENTED_EDGE ( 'NONE', *, *, #7543, .F. ) ;
#31212=DIRECTION ( 'NONE',  ( -1.000000000000000000, 0.000000000000000000, 0.000000000000000000 ) ) ;
#31216=CARTESIAN_POINT ( 'NONE',  ( 74.50000000000000000, 19.30628705663858469, 6.500000000000000000 ) ) ;
#31220=DIRECTION ( 'NONE',  ( 1.000000000000000000, 0.000000000000000000, 0.000000000000000000 ) ) ;
#31222=VECTOR ( 'NONE', #48095, 1000.000000000000000 ) ;
#31224=ORIENTED_EDGE ( 'NONE', *, *, #1863, .T. ) ;
#31231=CARTESIAN_POINT ( 'NONE',  ( -74.77251601432477912, 35.95471203479432631, -9.923951063487390201 ) ) ;
#31233=CARTESIAN_POINT ( 'NONE',  ( -5.598654528085806881, 122.8549999999999898, -7.705886871421374629 ) ) ;
#31235=DIRECTION ( 'NONE',  ( 1.000000000000000000, 0.000000000000000000, 0.000000000000000000 ) ) ;
#31238=UNCERTAINTY_MEASURE_WITH_UNIT (LENGTH_MEASURE( 1.000000000000000082E-05 ), #46990, 'distance_accuracy_value', 'NONE');
#31243=FILL_AREA_STYLE ('',( #62577 ) ) ;
#31244=DIRECTION ( 'NONE',  ( 0.000000000000000000, 0.000000000000000000, -1.000000000000000000 ) ) ;
#31247=ORIENTED_EDGE ( 'NONE', *, *, #56645, .T. ) ;
#31248=FILL_AREA_STYLE_COLOUR ( '', #12715 ) ;
#31252=FILL_AREA_STYLE ('',( #53439 ) ) ;
#31255=MECHANICAL_DESIGN_GEOMETRIC_PRESENTATION_REPRESENTATION('',(#39200),#38054);
#31256=DIRECTION ( 'NONE',  ( 1.000000000000000000, 0.000000000000000000, 0.000000000000000000 ) ) ;
#31261=SURFACE_STYLE_USAGE ( .BOTH. , #69605 ) ;
#31264=( NAMED_UNIT ( * ) SI_UNIT ( $, .STERADIAN. ) SOLID_ANGLE_UNIT ( ) );
#31267=FILL_AREA_STYLE_COLOUR ( '', #15294 ) ;
#31268=CARTESIAN_POINT ( 'NONE',  ( -1.166476076187854022E-15, 149.9449999999999932, 9.525000000000000355 ) ) ;
#31270=EDGE_CURVE ( 'NONE', #13709, #4040, #56630, .T. ) ;
#31274=CARTESIAN_POINT ( 'NONE',  ( 5.598654528085809545, 152.2549999999999670, -7.705886871421373741 ) ) ;
#31275=EDGE_CURVE ( 'NONE', #20368, #19233, #40953, .T. ) ;
#31276=SURFACE_STYLE_USAGE ( .BOTH. , #30943 ) ;
#31277=CARTESIAN_POINT ( 'NONE',  ( -71.50000000000000000, 35.92875272052971525, 7.000000000000000000 ) ) ;
#31279=CARTESIAN_POINT ( 'NONE',  ( 4.716976649647099507, 125.6429263765338220, -6.492361379858953008 ) ) ;
#31283=SURFACE_STYLE_FILL_AREA ( #68955 ) ;
#31287=CARTESIAN_POINT ( 'NONE',  ( -40.83001745922079806, 108.1251451958518146, -3.311254650320285542 ) ) ;
#31292=CARTESIAN_POINT ( 'NONE',  ( 12.72792206135785875, 115.4999999999999574, 10.00000000000000000 ) ) ;
#31294=VERTEX_POINT ( 'NONE', #53163 ) ;
#31295=SURFACE_SIDE_STYLE ('',( #62616 ) ) ;
#31296=UNCERTAINTY_MEASURE_WITH_UNIT (LENGTH_MEASURE( 1.000000000000000082E-05 ), #54723, 'distance_accuracy_value', 'NONE');
#31297=AXIS2_PLACEMENT_3D ( 'NONE', #18939, #36217, #29860 ) ;
#31301=SURFACE_SIDE_STYLE ('',( #63333 ) ) ;
#31305=VECTOR ( 'NONE', #26952, 1000.000000000000000 ) ;
#31308=ORIENTED_EDGE ( 'NONE', *, *, #20898, .T. ) ;
#31310=DIRECTION ( 'NONE',  ( 0.000000000000000000, 0.000000000000000000, -1.000000000000000000 ) ) ;
#31315=ORIENTED_EDGE ( 'NONE', *, *, #63836, .F. ) ;
#31316=DIRECTION ( 'NONE',  ( 0.000000000000000000, 0.000000000000000000, 1.000000000000000000 ) ) ;
#31317=COLOUR_RGB ( '', 0.40784314, 0.44705882, 0.49803922) ;
#31322=CARTESIAN_POINT ( 'NONE',  ( -9.058813317711337021, 146.0449999999999875, -2.943386871421374895 ) ) ;
#31324=( NAMED_UNIT ( * ) PLANE_ANGLE_UNIT ( ) SI_UNIT ( $, .RADIAN. ) );
#31326=UNCERTAINTY_MEASURE_WITH_UNIT (LENGTH_MEASURE( 1.000000000000000082E-05 ), #60743, 'distance_accuracy_value', 'NONE');
#31327=CIRCLE ( 'NONE', #23490, 0.5000000000000004441 ) ;
#31331=CARTESIAN_POINT ( 'NONE',  ( 74.99999999999998579, 50.00000000000000000, -9.500000000000000000 ) ) ;
#31333=CARTESIAN_POINT ( 'NONE',  ( 44.99999999999977973, 149.9999999999999716, -9.500000000000000000 ) ) ;
#31335=PRESENTATION_STYLE_ASSIGNMENT (( #52834 ) ) ;
#31339=FILL_AREA_STYLE_COLOUR ( '', #2643 ) ;
#31342=CARTESIAN_POINT ( 'NONE',  ( -45.76754978044866817, 8.860682567649741159, 6.389379348043552120 ) ) ;
#31344=( LENGTH_UNIT ( ) NAMED_UNIT ( * ) SI_UNIT ( .MILLI., .METRE. ) );
#31346=ORIENTED_EDGE ( 'NONE', *, *, #23418, .F. ) ;
#31349=ADVANCED_FACE ( 'NONE', ( #3893 ), #54360, .T. ) ;
#31352=EDGE_LOOP ( 'NONE', ( #59327, #61320, #44663, #45449 ) ) ;
#31355=CARTESIAN_POINT ( 'NONE',  ( -3.094860106618434248, 116.7949999999999591, 9.525000000000000355 ) ) ;
#31356=FILL_AREA_STYLE_COLOUR ( '', #4744 ) ;
#31357=CIRCLE ( 'NONE', #2120, 5.499999999999976907 ) ;
#31361=CARTESIAN_POINT ( 'NONE',  ( -5.598654528085808657, 117.7549999999999812, 7.705886871421373741 ) ) ;
#31365=ORIENTED_EDGE ( 'NONE', *, *, #69206, .T. ) ;
#31366=CARTESIAN_POINT ( 'NONE',  ( 8.102448949553183510, 146.1049999999999898, -5.886773742842746238 ) ) ;
#31367=UNCERTAINTY_MEASURE_WITH_UNIT (LENGTH_MEASURE( 1.000000000000000082E-05 ), #59264, 'distance_accuracy_value', 'NONE');
#31371=ORIENTED_EDGE ( 'NONE', *, *, #25177, .F. ) ;
#31373=LINE ( 'NONE', #69045, #28363 ) ;
#31376=CARTESIAN_POINT ( 'NONE',  ( 6.766228288048925954, 111.1834974234494098, 5.697616492254868881 ) ) ;
#31379=SURFACE_STYLE_USAGE ( .BOTH. , #10986 ) ;
#31381=CARTESIAN_POINT ( 'NONE',  ( -21.02379604162863913, 109.9999999999999858, 10.50000000000000000 ) ) ;
#31395=DIRECTION ( 'NONE',  ( -0.000000000000000000, -1.000000000000000000, -0.000000000000000000 ) ) ;
#31400=PRESENTATION_STYLE_ASSIGNMENT (( #32119 ) ) ;
#31404=CARTESIAN_POINT ( 'NONE',  ( -3.094860106618434248, 119.7949999999999733, 9.525000000000000355 ) ) ;
#31407=AXIS2_PLACEMENT_3D ( 'NONE', #56039, #13474, #7853 ) ;
#31408=CARTESIAN_POINT ( 'NONE',  ( 65.00000000000000000, 1.797044900979284448E-15, 11.50000000000003730 ) ) ;
#31409=VECTOR ( 'NONE', #33190, 1000.000000000000000 ) ;
#31416=CARTESIAN_POINT ( 'NONE',  ( -20.57648123223239622, 114.4999999999999574, -10.27659574468085246 ) ) ;
#31420=STYLED_ITEM ( 'NONE', ( #13338 ), #16422 ) ;
#31423=EDGE_CURVE ( 'NONE', #54731, #28244, #6114, .T. ) ;
#31424=PRESENTATION_STYLE_ASSIGNMENT (( #20900 ) ) ;
#31425=( NAMED_UNIT ( * ) SI_UNIT ( $, .STERADIAN. ) SOLID_ANGLE_UNIT ( ) );
#31429=EDGE_CURVE ( 'NONE', #12421, #56786, #16111, .T. ) ;
#31438=CARTESIAN_POINT ( 'NONE',  ( 8.437984349512095861, 138.3070736234661808, 1.550032578732817026E-15 ) ) ;
#31441=VECTOR ( 'NONE', #52823, 1000.000000000000000 ) ;
#31445=CARTESIAN_POINT ( 'NONE',  ( -15.98999599679679839, 117.9999999999999716, 7.500000000000000000 ) ) ;
#31446=ORIENTED_EDGE ( 'NONE', *, *, #31423, .T. ) ;
#31449=CARTESIAN_POINT ( 'NONE',  ( 8.437984349512095861, 143.1929263765337907, 1.550032578732816828E-15 ) ) ;
#31453=COLOUR_RGB ( '', 0.66274510, 0.83137255, 0.94901961) ;
#31455=CARTESIAN_POINT ( 'NONE',  ( 15.48999599679679662, 118.4999999999999716, -7.500000000000000000 ) ) ;
#31457=CIRCLE ( 'NONE', #8988, 0.5000000000000004441 ) ;
#31461=CIRCLE ( 'NONE', #10151, 0.5000000000000004441 ) ;
#31464=FILL_AREA_STYLE_COLOUR ( '', #23563 ) ;
#31465=AXIS2_PLACEMENT_3D ( 'NONE', #1179, #12839, #65619 ) ;
#31467=CARTESIAN_POINT ( 'NONE',  ( -74.08452722063037754, 9.430195807687217879, 6.000000000000000888 ) ) ;
#31469=CARTESIAN_POINT ( 'NONE',  ( -20.71231517720797655, 149.4999999999999716, 10.00000000000000000 ) ) ;
#31474=CARTESIAN_POINT ( 'NONE',  ( -40.96656732556692759, 108.0254117342835229, 3.574171091744781315 ) ) ;
#31479=CARTESIAN_POINT ( 'NONE',  ( 5.598654528085805993, 120.2449999999999903, 7.705886871421374629 ) ) ;
#31483=ORIENTED_EDGE ( 'NONE', *, *, #53682, .F. ) ;
#31488=DIRECTION ( 'NONE',  ( 1.000000000000000000, 0.000000000000000000, -0.000000000000000000 ) ) ;
#31489=DIRECTION ( 'NONE',  ( 0.000000000000000000, 0.000000000000000000, 1.000000000000000000 ) ) ;
#31492=CIRCLE ( 'NONE', #2206, 23.00000000000000000 ) ;
#31493=EDGE_LOOP ( 'NONE', ( #62539, #63229, #37322, #41288 ) ) ;
#31494=CARTESIAN_POINT ( 'NONE',  ( -9.827790563157511022E-16, 128.5570736234661524, 8.025000000000000355 ) ) ;
#31499=CARTESIAN_POINT ( 'NONE',  ( 5.598654528085809545, 158.2549999999999670, -7.705886871421373741 ) ) ;
#31504=MECHANICAL_DESIGN_GEOMETRIC_PRESENTATION_REPRESENTATION('',(#4541),#7916);
#31506=AXIS2_PLACEMENT_3D ( 'NONE', #33356, #54784, #22810 ) ;
#31514=SURFACE_STYLE_FILL_AREA ( #42145 ) ;
#31515=ADVANCED_FACE ( 'NONE', ( #54521 ), #40999, .F. ) ;
#31517=CARTESIAN_POINT ( 'NONE',  ( -2.607480562268991608, 139.2929263765338419, 8.025000000000060751 ) ) ;
#31523=EDGE_CURVE ( 'NONE', #61248, #57942, #28543, .T. ) ;
#31524=AXIS2_PLACEMENT_3D ( 'NONE', #46642, #2928, #61693 ) ;
#31525=CARTESIAN_POINT ( 'NONE',  ( -9.827790563157511022E-16, 110.5570736234661524, 8.025000000000000355 ) ) ;
#31528=CARTESIAN_POINT ( 'NONE',  ( -20.17763807713225432, 115.4773716707933460, 10.00000000000000000 ) ) ;
#31533=EDGE_CURVE ( 'NONE', #19777, #15724, #8437, .T. ) ;
#31537=CARTESIAN_POINT ( 'NONE',  ( 3.094860106618431583, 121.2049999999999841, 9.525000000000000355 ) ) ;
#31538=DIRECTION ( 'NONE',  ( 1.000000000000000000, 0.000000000000000000, 0.000000000000000000 ) ) ;
#31539=FILL_AREA_STYLE ('',( #10109 ) ) ;
#31540=TOROIDAL_SURFACE ( 'NONE', #34915, 1.000000000000000000, 0.5000000000000000000 ) ;
#31544=CARTESIAN_POINT ( 'NONE',  ( 1.613420992953035871, 154.3163448595890088, -9.236620315407188642 ) ) ;
#31545=SURFACE_STYLE_USAGE ( .BOTH. , #41446 ) ;
#31548=CARTESIAN_POINT ( 'NONE',  ( 7.632228543268608334, 158.3429263765338249, -2.479861379858951942 ) ) ;
#31550=AXIS2_PLACEMENT_3D ( 'NONE', #16506, #48173, #20716 ) ;
#31552=DIRECTION ( 'NONE',  ( -0.000000000000000000, 1.000000000000000000, -0.000000000000000000 ) ) ;
#31553=CIRCLE ( 'NONE', #59670, 0.5000000000000004441 ) ;
#31556=CARTESIAN_POINT ( 'NONE',  ( 2.607480562269071989, 127.5929263765338249, 8.025000000000002132 ) ) ;
#31558=DIRECTION ( 'NONE',  ( 0.000000000000000000, 0.000000000000000000, 1.000000000000000000 ) ) ;
#31561=DIRECTION ( 'NONE',  ( 0.000000000000000000, -1.000000000000000000, 0.000000000000000000 ) ) ;
#31562=LINE ( 'NONE', #36194, #22774 ) ;
#31567=COLOUR_RGB ( '', 0.08235294, 0.09019608, 0.10196078) ;
#31572=FILL_AREA_STYLE_COLOUR ( '', #38295 ) ;
#31574=DIRECTION ( 'NONE',  ( 1.000000000000000000, 0.000000000000000000, 0.000000000000000000 ) ) ;
#31579=CIRCLE ( 'NONE', #35971, 0.5000000000000004441 ) ;
#31587=CYLINDRICAL_SURFACE ( 'NONE', #46152, 0.5000000000000004441 ) ;
#31589=CARTESIAN_POINT ( 'NONE',  ( -74.72360438755690382, 36.39190877706418092, -9.990989611936115011 ) ) ;
#31591=CARTESIAN_POINT ( 'NONE',  ( 3.094860106618435136, 131.4049999999999727, -9.525000000000000355 ) ) ;
#31592=CARTESIAN_POINT ( 'NONE',  ( 74.50000000000000000, 19.30628705663858469, 6.500000000000000000 ) ) ;
#31596=EDGE_CURVE ( 'NONE', #52352, #56993, #50640, .T. ) ;
#31600=ORIENTED_EDGE ( 'NONE', *, *, #12713, .T. ) ;
#31601=AXIS2_PLACEMENT_3D ( 'NONE', #63183, #26229, #14654 ) ;
#31606=EDGE_CURVE ( 'NONE', #59067, #53774, #14999, .T. ) ;
#31610=ORIENTED_EDGE ( 'NONE', *, *, #31007, .T. ) ;
#31612=CYLINDRICAL_SURFACE ( 'NONE', #10474, 18.00000000000000355 ) ;
#31616=EDGE_CURVE ( 'NONE', #16451, #62857, #35908, .T. ) ;
#31621=ORIENTED_EDGE ( 'NONE', *, *, #19725, .F. ) ;
#31623=ORIENTED_EDGE ( 'NONE', *, *, #39926, .F. ) ;
#31624=DIRECTION ( 'NONE',  ( -0.000000000000000000, -0.000000000000000000, -1.000000000000000000 ) ) ;
#31626=VERTEX_POINT ( 'NONE', #3800 ) ;
#31628=ORIENTED_EDGE ( 'NONE', *, *, #34952, .T. ) ;
#31631=CARTESIAN_POINT ( 'NONE',  ( 3.094860106618435136, 145.2949999999999875, -9.525000000000000355 ) ) ;
#31632=FACE_OUTER_BOUND ( 'NONE', #9555, .T. ) ;
#31634=COLOUR_RGB ( '', 0.09019608, 0.27058824, 0.51372549) ;
#31636=CARTESIAN_POINT ( 'NONE',  ( -1.166476076187854022E-15, 148.0549999999999784, 9.525000000000000355 ) ) ;
#31640=CARTESIAN_POINT ( 'NONE',  ( 6.826472737025119919, 124.8929263765338220, 4.959722759717908325 ) ) ;
#31646=VERTEX_POINT ( 'NONE', #57293 ) ;
#31647=CARTESIAN_POINT ( 'NONE',  ( -40.96599324808799736, 108.0258340745533161, -3.573232801688257076 ) ) ;
#31648=ORIENTED_EDGE ( 'NONE', *, *, #66709, .T. ) ;
#31650=B_SPLINE_CURVE_WITH_KNOTS ( 'NONE', 3,
 ( #48199, #54111, #4893, #22118, #64330, #26673, #63976, #58042, #21775, #9848 ),
 .UNSPECIFIED., .F., .F.,
 ( 4, 2, 2, 2, 4 ),
 ( 0.000000000000000000, 0.0004159702800446777042, 0.0008319405600893554084, 0.001247910840134033167, 0.001663881120178710817 ),
 .UNSPECIFIED. ) ;
#31652=CARTESIAN_POINT ( 'NONE',  ( 60.00000000000000000, 110.4999999999999858, 9.500000000000000000 ) ) ;
#31655=CARTESIAN_POINT ( 'NONE',  ( -48.50000000000000000, 14.49137674618942562, -7.000000000000000000 ) ) ;
#31659=LINE ( 'NONE', #42287, #23757 ) ;
#31663=ORIENTED_EDGE ( 'NONE', *, *, #49641, .F. ) ;
#31666=CARTESIAN_POINT ( 'NONE',  ( -15.98999599679679839, 146.4999999999999716, -7.500000000000000000 ) ) ;
#31668=VERTEX_POINT ( 'NONE', #56955 ) ;
#31670=DIRECTION ( 'NONE',  ( -1.000000000000000000, 0.000000000000000000, 0.000000000000000000 ) ) ;
#31672=FILL_AREA_STYLE ('',( #36996 ) ) ;
#31673=CIRCLE ( 'NONE', #20433, 1.000000000000000888 ) ;
#31678=COLOUR_RGB ( '', 0.31764706, 0.68627451, 0.89019608) ;
#31682=EDGE_CURVE ( 'NONE', #6337, #51799, #21845, .T. ) ;
#31684=CARTESIAN_POINT ( 'NONE',  ( 5.598654528085809545, 151.1449999999999818, -7.705886871421373741 ) ) ;
#31688=EDGE_CURVE ( 'NONE', #61072, #18963, #66776, .T. ) ;
#31691=VERTEX_POINT ( 'NONE', #31592 ) ;
#31695=DIRECTION ( 'NONE',  ( 0.000000000000000000, 0.000000000000000000, 1.000000000000000000 ) ) ;
#31698=DIRECTION ( 'NONE',  ( 0.000000000000000000, 0.000000000000000000, 1.000000000000000000 ) ) ;
#31700=VERTEX_POINT ( 'NONE', #25616 ) ;
#31702=DIRECTION ( 'NONE',  ( 1.000000000000000000, 0.000000000000000000, 0.000000000000000000 ) ) ;
#31706=AXIS2_PLACEMENT_3D ( 'NONE', #45618, #50173, #29014 ) ;
#31711=DIRECTION ( 'NONE',  ( 1.000000000000000000, 0.000000000000000000, 0.000000000000000000 ) ) ;
#31712=( GEOMETRIC_REPRESENTATION_CONTEXT ( 3 ) GLOBAL_UNCERTAINTY_ASSIGNED_CONTEXT ( ( #48376 ) ) GLOBAL_UNIT_ASSIGNED_CONTEXT ( ( #64071, #33456, #60508 ) ) REPRESENTATION_CONTEXT ( 'NONE', 'WORKASPACE' ) );
#31716=CARTESIAN_POINT ( 'NONE',  ( -8.102448949553181734, 122.4949999999999903, 5.886773742842747126 ) ) ;
#31717=CARTESIAN_POINT ( 'NONE',  ( 75.00000000000000000, 20.36037961002804053, 6.000000000000000888 ) ) ;
#31718=STYLED_ITEM ( 'NONE', ( #48737 ), #54644 ) ;
#31720=CARTESIAN_POINT ( 'NONE',  ( -1.166476076187854022E-15, 124.0549999999999784, 9.525000000000000355 ) ) ;
#31722=CARTESIAN_POINT ( 'NONE',  ( -40.78947371891996454, 108.1536491252650052, -3.151596837137513596 ) ) ;
#31724=CARTESIAN_POINT ( 'NONE',  ( -5.598654528085806881, 146.8549999999999898, -7.705886871421374629 ) ) ;
#31726=CARTESIAN_POINT ( 'NONE',  ( 60.00000000000000000, 1.797044900979284448E-15, -10.00000000000000000 ) ) ;
#31727=STYLED_ITEM ( 'NONE', ( #11503 ), #19120 ) ;
#31729=ORIENTED_EDGE ( 'NONE', *, *, #28707, .T. ) ;
#31730=CARTESIAN_POINT ( 'NONE',  ( -79.99999999999998579, 50.00000000000000000, 11.50000000000003730 ) ) ;
#31731=CARTESIAN_POINT ( 'NONE',  ( 74.59262096826685706, 19.64589727361707361, -6.500000000000001776 ) ) ;
#31735=EDGE_CURVE ( 'NONE', #5084, #32321, #2701, .T. ) ;
#31737=ORIENTED_EDGE ( 'NONE', *, *, #52172, .T. ) ;
#31740=( NAMED_UNIT ( * ) PLANE_ANGLE_UNIT ( ) SI_UNIT ( $, .RADIAN. ) );
#31744=SURFACE_STYLE_USAGE ( .BOTH. , #42372 ) ;
#31746=DIRECTION ( 'NONE',  ( 0.000000000000000000, 1.000000000000000000, 0.000000000000000000 ) ) ;
#31747=CARTESIAN_POINT ( 'NONE',  ( 8.102448949553179958, 150.3949999999999818, 5.886773742842750679 ) ) ;
#31753=DIRECTION ( 'NONE',  ( 0.000000000000000000, 1.000000000000000000, 0.000000000000000000 ) ) ;
#31756=EDGE_CURVE ( 'NONE', #24967, #17136, #60037, .T. ) ;
#31759=EDGE_CURVE ( 'NONE', #32017, #41477, #69052, .T. ) ;
#31760=CARTESIAN_POINT ( 'NONE',  ( -3.094860106618434248, 116.7949999999999591, 9.525000000000000355 ) ) ;
#31774=MECHANICAL_DESIGN_GEOMETRIC_PRESENTATION_REPRESENTATION('',(#30614),#16093);
#31775=AXIS2_PLACEMENT_3D ( 'NONE', #59793, #28092, #61175 ) ;
#31777=EDGE_CURVE ( 'NONE', #33694, #37046, #35404, .T. ) ;
#31789=CARTESIAN_POINT ( 'NONE',  ( -60.00000000000000000, -2.024042244987997205E-14, -10.49999999999999822 ) ) ;
#31794=COLOUR_RGB ( '', 0.72549020, 0.75294118, 0.79215686) ;
#31795=COLOUR_RGB ( '', 0.09019608, 0.27058824, 0.51372549) ;
#31797=CARTESIAN_POINT ( 'NONE',  ( 2.607480562269076430, 144.9070736234661751, -8.025000000000000355 ) ) ;
#31799=ORIENTED_EDGE ( 'NONE', *, *, #30509, .T. ) ;
#31803=ORIENTED_EDGE ( 'NONE', *, *, #39826, .F. ) ;
#31809=DIRECTION ( 'NONE',  ( -0.000000000000000000, -0.000000000000000000, -1.000000000000000000 ) ) ;
#31812=DIRECTION ( 'NONE',  ( -1.000000000000000000, 0.000000000000000000, 0.000000000000000000 ) ) ;
#31815=ORIENTED_EDGE ( 'NONE', *, *, #17446, .T. ) ;
#31822=CARTESIAN_POINT ( 'NONE',  ( -40.49999999999998579, 107.7459666924148394, 3.000000000000000000 ) ) ;
#31827=CARTESIAN_POINT ( 'NONE',  ( -8.102448949553179958, 124.8949999999999960, -5.886773742842749790 ) ) ;
#31829=CIRCLE ( 'NONE', #342, 8.999999999999994671 ) ;
#31831=DIRECTION ( 'NONE',  ( 0.000000000000000000, 0.000000000000000000, 1.000000000000000000 ) ) ;
#31833=( LENGTH_UNIT ( ) NAMED_UNIT ( * ) SI_UNIT ( .MILLI., .METRE. ) );
#31836=FILL_AREA_STYLE ('',( #48417 ) ) ;
#31843=COLOUR_RGB ( '', 0.08235294, 0.09019608, 0.10196078) ;
#31846=VERTEX_POINT ( 'NONE', #38308 ) ;
#31850=SURFACE_STYLE_FILL_AREA ( #53337 ) ;
#31855=( NAMED_UNIT ( * ) SI_UNIT ( $, .STERADIAN. ) SOLID_ANGLE_UNIT ( ) );
#31857=MECHANICAL_DESIGN_GEOMETRIC_PRESENTATION_REPRESENTATION('',(#57688),#321);
#31858=( NAMED_UNIT ( * ) PLANE_ANGLE_UNIT ( ) SI_UNIT ( $, .RADIAN. ) );
#31865=VECTOR ( 'NONE', #43973, 1000.000000000000000 ) ;
#31867=CARTESIAN_POINT ( 'NONE',  ( -23.21231517720797655, 117.4999999999999716, 10.00000000000000000 ) ) ;
#31869=DIRECTION ( 'NONE',  ( 1.000000000000000000, 0.000000000000000000, 0.000000000000000000 ) ) ;
#31873=EDGE_CURVE ( 'NONE', #4798, #30297, #66371, .T. ) ;
#31874=CARTESIAN_POINT ( 'NONE',  ( -2.607480562269073765, 118.2070736234661439, -8.025000000000000355 ) ) ;
#31885=CARTESIAN_POINT ( 'NONE',  ( -20.88896767935282739, 150.0000000000000284, 9.626543325103073201 ) ) ;
#31886=ORIENTED_EDGE ( 'NONE', *, *, #51616, .T. ) ;
#31887=CARTESIAN_POINT ( 'NONE',  ( -8.102448949553181734, 123.6049999999999756, 5.886773742842747126 ) ) ;
#31895=FILL_AREA_STYLE_COLOUR ( '', #53077 ) ;
#31896=FILL_AREA_STYLE ('',( #47444 ) ) ;
#31898=CARTESIAN_POINT ( 'NONE',  ( 2.607480562269071989, 157.5929263765338249, 8.025000000000002132 ) ) ;
#31899=CARTESIAN_POINT ( 'NONE',  ( 0.000000000000000000, 114.9999999999999574, 0.000000000000000000 ) ) ;
#31902=EDGE_CURVE ( 'NONE', #29357, #43960, #37650, .T. ) ;
#31905=CARTESIAN_POINT ( 'NONE',  ( -19.89974874213239886, 114.9999999999999574, 10.49999999999999645 ) ) ;
#31906=CYLINDRICAL_SURFACE ( 'NONE', #69210, 7.999999999999992895 ) ;
#31908=PRESENTATION_STYLE_ASSIGNMENT (( #10475 ) ) ;
#31910=DIRECTION ( 'NONE',  ( 0.000000000000000000, 0.000000000000000000, 1.000000000000000000 ) ) ;
#31913=( NAMED_UNIT ( * ) SI_UNIT ( $, .STERADIAN. ) SOLID_ANGLE_UNIT ( ) );
#31916=DIRECTION ( 'NONE',  ( 7.080503983578803083E-17, -1.000000000000000000, -0.000000000000000000 ) ) ;
#31920=CARTESIAN_POINT ( 'NONE',  ( -23.21231517720797655, 117.4999999999999716, 9.500000000000000000 ) ) ;
#31924=DIRECTION ( 'NONE',  ( -1.000000000000000000, 0.000000000000000000, 0.000000000000000000 ) ) ;
#31926=( NAMED_UNIT ( * ) SI_UNIT ( $, .STERADIAN. ) SOLID_ANGLE_UNIT ( ) );
#31940=CARTESIAN_POINT ( 'NONE',  ( -24.21231517720798010, 112.9999999999999858, -7.500000000000000000 ) ) ;
#31941=CARTESIAN_POINT ( 'NONE',  ( -74.86949037884366476, 35.76270116634893270, -9.842748219889633887 ) ) ;
#31942=EDGE_CURVE ( 'NONE', #48466, #14271, #33148, .T. ) ;
#31945=CARTESIAN_POINT ( 'NONE',  ( 3.094860106618435136, 134.4049999999999443, -9.525000000000000355 ) ) ;
#31952=( NAMED_UNIT ( * ) SI_UNIT ( $, .STERADIAN. ) SOLID_ANGLE_UNIT ( ) );
#31953=CARTESIAN_POINT ( 'NONE',  ( -15.98999599679679839, 146.4999999999999716, 9.500000000000000000 ) ) ;
#31955=CYLINDRICAL_SURFACE ( 'NONE', #46079, 15.00000000000000000 ) ;
#31956=VECTOR ( 'NONE', #59455, 1000.000000000000000 ) ;
#31959=DIRECTION ( 'NONE',  ( 1.000000000000000000, 0.000000000000000000, -1.040834085586083310E-14 ) ) ;
#31964=STYLED_ITEM ( 'NONE', ( #65781 ), #31515 ) ;
#31966=CARTESIAN_POINT ( 'NONE',  ( 71.49999999999998579, 119.9999999999997868, 7.000000000000000000 ) ) ;
#31971=VERTEX_POINT ( 'NONE', #67079 ) ;
#31973=( NAMED_UNIT ( * ) SI_UNIT ( $, .STERADIAN. ) SOLID_ANGLE_UNIT ( ) );
#31974=ORIENTED_EDGE ( 'NONE', *, *, #42011, .F. ) ;
#31976=DIRECTION ( 'NONE',  ( -0.000000000000000000, -0.000000000000000000, -1.000000000000000000 ) ) ;
#31977=ORIENTED_EDGE ( 'NONE', *, *, #55194, .F. ) ;
#31979=CARTESIAN_POINT ( 'NONE',  ( 3.094860106618435136, 151.2949999999999875, -9.525000000000000355 ) ) ;
#31985=SURFACE_STYLE_USAGE ( .BOTH. , #22130 ) ;
#31988=CARTESIAN_POINT ( 'NONE',  ( -6.826472737025120807, 129.3929263765338362, -4.959722759717907437 ) ) ;
#31990=UNCERTAINTY_MEASURE_WITH_UNIT (LENGTH_MEASURE( 1.000000000000000082E-05 ), #38482, 'distance_accuracy_value', 'NONE');
#31991=CIRCLE ( 'NONE', #65682, 0.5000000000000004441 ) ;
#31992=SURFACE_STYLE_USAGE ( .BOTH. , #58382 ) ;
#31998=MECHANICAL_DESIGN_GEOMETRIC_PRESENTATION_REPRESENTATION('',(#47781),#43316);
#32005=UNCERTAINTY_MEASURE_WITH_UNIT (LENGTH_MEASURE( 1.000000000000000082E-05 ), #11715, 'distance_accuracy_value', 'NONE');
#32008=DIRECTION ( 'NONE',  ( 1.000000000000000000, 0.000000000000000000, 0.000000000000000000 ) ) ;
#32010=EDGE_CURVE ( 'NONE', #19250, #63248, #37711, .T. ) ;
#32011=AXIS2_PLACEMENT_3D ( 'NONE', #1228, #38977, #65659 ) ;
#32012=ORIENTED_EDGE ( 'NONE', *, *, #47488, .T. ) ;
#32017=VERTEX_POINT ( 'NONE', #56510 ) ;
#32024=TOROIDAL_SURFACE ( 'NONE', #6159, 7.500000000000011546, 0.5000000000000000000 ) ;
#32026=FILL_AREA_STYLE_COLOUR ( '', #53144 ) ;
#32028=CIRCLE ( 'NONE', #16345, 0.5000000000000004441 ) ;
#32037=CARTESIAN_POINT ( 'NONE',  ( -10.01517768586949231, 146.1949999999999648, -6.132527647946036459E-16 ) ) ;
#32040=UNCERTAINTY_MEASURE_WITH_UNIT (LENGTH_MEASURE( 1.000000000000000082E-05 ), #12933, 'distance_accuracy_value', 'NONE');
#32042=CARTESIAN_POINT ( 'NONE',  ( 72.00000000000000000, 36.32520566882265456, -7.500000000000000000 ) ) ;
#32044=ORIENTED_EDGE ( 'NONE', *, *, #60106, .F. ) ;
#32048=CARTESIAN_POINT ( 'NONE',  ( -21.02379604162863913, 109.9999999999999858, -10.50000000000000000 ) ) ;
#32049=AXIS2_PLACEMENT_3D ( 'NONE', #37187, #26570, #11792 ) ;
#32053=ORIENTED_EDGE ( 'NONE', *, *, #956, .F. ) ;
#32054=ORIENTED_EDGE ( 'NONE', *, *, #22570, .F. ) ;
#32057=UNCERTAINTY_MEASURE_WITH_UNIT (LENGTH_MEASURE( 1.000000000000000082E-05 ), #49599, 'distance_accuracy_value', 'NONE');
#32059=CARTESIAN_POINT ( 'NONE',  ( -48.50000000000000000, 99.99999999999992895, 7.500000000000000000 ) ) ;
#32063=EDGE_LOOP ( 'NONE', ( #45258, #61048, #25356, #65360 ) ) ;
#32066=VERTEX_POINT ( 'NONE', #28731 ) ;
#32068=DIRECTION ( 'NONE',  ( 0.000000000000000000, 0.000000000000000000, 1.000000000000000000 ) ) ;
#32069=ORIENTED_EDGE ( 'NONE', *, *, #20176, .F. ) ;
#32070=COLOUR_RGB ( '', 0.72549020, 0.75294118, 0.79215686) ;
#32073=CARTESIAN_POINT ( 'NONE',  ( 10.01517768586949231, 123.6949999999999932, 1.839758294383810543E-15 ) ) ;
#32075=MECHANICAL_DESIGN_GEOMETRIC_PRESENTATION_REPRESENTATION('',(#17486),#14113);
#32077=CARTESIAN_POINT ( 'NONE',  ( 10.01517768586949408, 118.8049999999999926, 1.839758294383810543E-15 ) ) ;
#32079=CIRCLE ( 'NONE', #55632, 8.000000000000007105 ) ;
#32081=DIRECTION ( 'NONE',  ( 0.000000000000000000, 0.000000000000000000, -1.000000000000000000 ) ) ;
#32082=ORIENTED_EDGE ( 'NONE', *, *, #2071, .F. ) ;
#32083=CARTESIAN_POINT ( 'NONE',  ( -3.094860106618432471, 149.7049999999999272, -9.525000000000000355 ) ) ;
#32085=UNCERTAINTY_MEASURE_WITH_UNIT (LENGTH_MEASURE( 1.000000000000000082E-05 ), #6399, 'distance_accuracy_value', 'NONE');
#32086=FILL_AREA_STYLE ('',( #43398 ) ) ;
#32087=CARTESIAN_POINT ( 'NONE',  ( 68.00000000000000000, 2.776762340297169183E-15, 10.50000000000000000 ) ) ;
#32088=FACE_OUTER_BOUND ( 'NONE', #47252, .T. ) ;
#32089=ADVANCED_FACE ( 'NONE', ( #17854 ), #7985, .F. ) ;
#32091=EDGE_LOOP ( 'NONE', ( #13989, #11283, #63155, #19564 ) ) ;
#32092=SURFACE_STYLE_FILL_AREA ( #57793 ) ;
#32098=MECHANICAL_DESIGN_GEOMETRIC_PRESENTATION_REPRESENTATION('',(#14130),#44491);
#32100=PRESENTATION_STYLE_ASSIGNMENT (( #31379 ) ) ;
#32101=DIRECTION ( 'NONE',  ( 1.000000000000000000, 0.000000000000000000, 0.000000000000000000 ) ) ;
#32105=SURFACE_SIDE_STYLE ('',( #15270 ) ) ;
#32107=ORIENTED_EDGE ( 'NONE', *, *, #67820, .T. ) ;
#32108=DIRECTION ( 'NONE',  ( -0.000000000000000000, 1.000000000000000000, -0.000000000000000000 ) ) ;
#32109=EDGE_CURVE ( 'NONE', #45911, #49280, #24136, .T. ) ;
#32113=VECTOR ( 'NONE', #55504, 1000.000000000000000 ) ;
#32117=ORIENTED_EDGE ( 'NONE', *, *, #63078, .F. ) ;
#32119=SURFACE_STYLE_USAGE ( .BOTH. , #63769 ) ;
#32121=CARTESIAN_POINT ( 'NONE',  ( -1.166476076187854022E-15, 119.9449999999999790, 9.525000000000000355 ) ) ;
#32125=CIRCLE ( 'NONE', #46797, 13.00000000000000178 ) ;
#32126=FILL_AREA_STYLE ('',( #20885 ) ) ;
#32131=DIRECTION ( 'NONE',  ( 0.000000000000000000, 0.000000000000000000, 1.000000000000000000 ) ) ;
#32132=CARTESIAN_POINT ( 'NONE',  ( -20.71462257042833599, 114.4999999999999574, -10.00000000000000000 ) ) ;
#32140=AXIS2_PLACEMENT_3D ( 'NONE', #62468, #57187, #3689 ) ;
#32142=CARTESIAN_POINT ( 'NONE',  ( -9.827790563157511022E-16, 146.5570736234661524, 8.025000000000000355 ) ) ;
#32148=CARTESIAN_POINT ( 'NONE',  ( 47.50000000000000000, 14.49137674618942562, -10.00000000000000000 ) ) ;
#32149=DIRECTION ( 'NONE',  ( -0.000000000000000000, -0.000000000000000000, 1.000000000000000000 ) ) ;
#32152=CARTESIAN_POINT ( 'NONE',  ( 7.632228543268608334, 144.4570736234661581, -2.479861379858951942 ) ) ;
#32153=ORIENTED_EDGE ( 'NONE', *, *, #53382, .F. ) ;
#32156=UNCERTAINTY_MEASURE_WITH_UNIT (LENGTH_MEASURE( 1.000000000000000082E-05 ), #29999, 'distance_accuracy_value', 'NONE');
#32159=DIRECTION ( 'NONE',  ( 0.2413793103448194644, -0.9704308468600220117, 0.000000000000000000 ) ) ;
#32161=MECHANICAL_DESIGN_GEOMETRIC_PRESENTATION_REPRESENTATION('',(#10825),#20926);
#32163=ADVANCED_FACE ( 'NONE', ( #24841 ), #46356, .F. ) ;
#32167=SURFACE_STYLE_USAGE ( .BOTH. , #3742 ) ;
#32172=SURFACE_STYLE_FILL_AREA ( #21247 ) ;
#32173=DIRECTION ( 'NONE',  ( -0.000000000000000000, -0.000000000000000000, -1.000000000000000000 ) ) ;
#32174=EDGE_CURVE ( 'NONE', #52175, #19166, #66841, .T. ) ;
#32178=SURFACE_STYLE_FILL_AREA ( #21252 ) ;
#32183=EDGE_CURVE ( 'NONE', #5042, #38669, #480, .T. ) ;
#32185=CYLINDRICAL_SURFACE ( 'NONE', #51376, 17.00000000000000000 ) ;
#32187=CARTESIAN_POINT ( 'NONE',  ( 0.000000000000000000, 124.4449999999999932, -9.525000000000000355 ) ) ;
#32193=PRESENTATION_STYLE_ASSIGNMENT (( #15688 ) ) ;
#32195=DIRECTION ( 'NONE',  ( 1.000000000000000000, 0.000000000000000000, -0.000000000000000000 ) ) ;
#32197=( GEOMETRIC_REPRESENTATION_CONTEXT ( 3 ) GLOBAL_UNCERTAINTY_ASSIGNED_CONTEXT ( ( #27679 ) ) GLOBAL_UNIT_ASSIGNED_CONTEXT ( ( #458, #33566, #10737 ) ) REPRESENTATION_CONTEXT ( 'NONE', 'WORKASPACE' ) );
#32210=DIRECTION ( 'NONE',  ( 0.000000000000000000, 0.000000000000000000, 1.000000000000000000 ) ) ;
#32213=PRESENTATION_STYLE_ASSIGNMENT (( #37553 ) ) ;
#32214=( LENGTH_UNIT ( ) NAMED_UNIT ( * ) SI_UNIT ( .MILLI., .METRE. ) );
#32218=EDGE_CURVE ( 'NONE', #4086, #41081, #69098, .T. ) ;
#32219=COLOUR_RGB ( '', 0.31764706, 0.68627451, 0.89019608) ;
#32222=CARTESIAN_POINT ( 'NONE',  ( 74.50000000000000000, -2.220952357103124925E-14, 6.999999999999999112 ) ) ;
#32224=SURFACE_STYLE_USAGE ( .BOTH. , #58264 ) ;
#32227=CARTESIAN_POINT ( 'NONE',  ( -4.716976649647097730, 115.3570736234661638, -6.492361379858953896 ) ) ;
#32229=CARTESIAN_POINT ( 'NONE',  ( 2.607480562268992941, 138.9070736234661751, -8.025000000000060751 ) ) ;
#32230=FACE_OUTER_BOUND ( 'NONE', #13086, .T. ) ;
#32237=CARTESIAN_POINT ( 'NONE',  ( 45.65811388300841855, 10.21937129433612235, -4.000000000000000000 ) ) ;
#32238=ORIENTED_EDGE ( 'NONE', *, *, #48162, .T. ) ;
#32240=CARTESIAN_POINT ( 'NONE',  ( -8.102448949553181734, 126.0049999999999812, -5.886773742842749790 ) ) ;
#32245=ORIENTED_EDGE ( 'NONE', *, *, #54761, .T. ) ;
#32246=CARTESIAN_POINT ( 'NONE',  ( 6.612677335615305907, 153.8894900351841102, -5.991805610726354203 ) ) ;
#32249=CARTESIAN_POINT ( 'NONE',  ( -7.632228543268607446, 150.5429263765338135, -2.479861379858953718 ) ) ;
#32251=ADVANCED_FACE ( 'NONE', ( #69168 ), #53342, .T. ) ;
#32252=( NAMED_UNIT ( * ) SI_UNIT ( $, .STERADIAN. ) SOLID_ANGLE_UNIT ( ) );
#32253=COLOUR_RGB ( '', 0.66274510, 0.83137255, 0.94901961) ;
#32254=PRESENTATION_STYLE_ASSIGNMENT (( #26611 ) ) ;
#32261=SURFACE_SIDE_STYLE ('',( #21712 ) ) ;
#32263=CARTESIAN_POINT ( 'NONE',  ( 4.716976649647099507, 116.6429263765338078, -6.492361379858953008 ) ) ;
#32264=CARTESIAN_POINT ( 'NONE',  ( -8.442136150874093303, 153.4966052368478131, -1.192225150237072651 ) ) ;
#32266=ORIENTED_EDGE ( 'NONE', *, *, #66561, .F. ) ;
#32269=ORIENTED_EDGE ( 'NONE', *, *, #47742, .T. ) ;
#32271=FACE_OUTER_BOUND ( 'NONE', #65845, .T. ) ;
#32272=EDGE_CURVE ( 'NONE', #18360, #9629, #50195, .T. ) ;
#32276=ADVANCED_FACE ( 'NONE', ( #64213 ), #11444, .F. ) ;
#32277=ORIENTED_EDGE ( 'NONE', *, *, #36348, .T. ) ;
#32283=CARTESIAN_POINT ( 'NONE',  ( -74.97675674235969723, 35.55359242983254831, -9.655596932388807119 ) ) ;
#32287=CARTESIAN_POINT ( 'NONE',  ( 3.094860106618435136, 140.4050000000000011, -9.525000000000000355 ) ) ;
#32294=EDGE_LOOP ( 'NONE', ( #23502, #46765, #4531, #51624 ) ) ;
#32296=AXIS2_PLACEMENT_3D ( 'NONE', #55392, #6163, #6851 ) ;
#32298=DIRECTION ( 'NONE',  ( 0.000000000000000000, -1.000000000000000000, -0.000000000000000000 ) ) ;
#32299=( NAMED_UNIT ( * ) SI_UNIT ( $, .STERADIAN. ) SOLID_ANGLE_UNIT ( ) );
#32300=EDGE_CURVE ( 'NONE', #59919, #43730, #59039, .T. ) ;
#32301=CARTESIAN_POINT ( 'NONE',  ( -2.607480562268991608, 137.4070736234661467, 8.025000000000060751 ) ) ;
#32302=VERTEX_POINT ( 'NONE', #49123 ) ;
#32305=CARTESIAN_POINT ( 'NONE',  ( -60.00000000000000000, -2.024042244987997205E-14, -7.000000000000000000 ) ) ;
#32306=ADVANCED_FACE ( 'NONE', ( #54353 ), #33260, .T. ) ;
#32307=DIRECTION ( 'NONE',  ( -0.000000000000000000, 1.000000000000000000, -0.000000000000000000 ) ) ;
#32309=ORIENTED_EDGE ( 'NONE', *, *, #26740, .T. ) ;
#32312=CARTESIAN_POINT ( 'NONE',  ( 7.632228543268608334, 129.4570736234661581, -2.479861379858951942 ) ) ;
#32315=PRESENTATION_STYLE_ASSIGNMENT (( #63645 ) ) ;
#32317=ORIENTED_EDGE ( 'NONE', *, *, #54933, .F. ) ;
#32318=LINE ( 'NONE', #21080, #44526 ) ;
#32320=( LENGTH_UNIT ( ) NAMED_UNIT ( * ) SI_UNIT ( .MILLI., .METRE. ) );
#32321=VERTEX_POINT ( 'NONE', #56086 ) ;
#32324=( LENGTH_UNIT ( ) NAMED_UNIT ( * ) SI_UNIT ( .MILLI., .METRE. ) );
#32325=COLOUR_RGB ( '', 0.40784314, 0.44705882, 0.49803922) ;
#32328=CARTESIAN_POINT ( 'NONE',  ( 2.607480562269071989, 124.5929263765337964, 8.025000000000002132 ) ) ;
#32329=CARTESIAN_POINT ( 'NONE',  ( -75.40896791924967602, 36.04473888234530676, -9.698837509433410276 ) ) ;
#32330=AXIS2_PLACEMENT_3D ( 'NONE', #27206, #49081, #44509 ) ;
#32344=CARTESIAN_POINT ( 'NONE',  ( 41.01803665359489770, 107.7206116573237580, 3.151333386623630606 ) ) ;
#32346=ORIENTED_EDGE ( 'NONE', *, *, #36815, .F. ) ;
#32347=FACE_OUTER_BOUND ( 'NONE', #36851, .T. ) ;
#32349=ORIENTED_EDGE ( 'NONE', *, *, #31756, .F. ) ;
#32351=FACE_OUTER_BOUND ( 'NONE', #21901, .T. ) ;
#32353=SURFACE_STYLE_FILL_AREA ( #58761 ) ;
#32354=EDGE_CURVE ( 'NONE', #54975, #23306, #42234, .T. ) ;
#32357=CARTESIAN_POINT ( 'NONE',  ( 0.000000000000000000, 87.30187232391182306, 8.025000000000000355 ) ) ;
#32358=LINE ( 'NONE', #5277, #55089 ) ;
#32359=DIRECTION ( 'NONE',  ( 0.000000000000000000, -1.000000000000000000, 0.000000000000000000 ) ) ;
#32361=CARTESIAN_POINT ( 'NONE',  ( -8.102448949553181734, 157.8950000000000102, -5.886773742842749790 ) ) ;
#32363=SURFACE_SIDE_STYLE ('',( #59109 ) ) ;
#32367=( LENGTH_UNIT ( ) NAMED_UNIT ( * ) SI_UNIT ( .MILLI., .METRE. ) );
#32371=EDGE_CURVE ( 'NONE', #66072, #52602, #50475, .T. ) ;
#32372=FACE_OUTER_BOUND ( 'NONE', #55596, .T. ) ;
#32373=FACE_OUTER_BOUND ( 'NONE', #52787, .T. ) ;
#32376=FACE_OUTER_BOUND ( 'NONE', #36290, .T. ) ;
#32379=CARTESIAN_POINT ( 'NONE',  ( -45.00000000000000000, 9.518682052515954339, 6.447728916822488721 ) ) ;
#32381=AXIS2_PLACEMENT_3D ( 'NONE', #61172, #18624, #44701 ) ;
#32386=EDGE_CURVE ( 'NONE', #20808, #10638, #33595, .T. ) ;
#32390=EDGE_LOOP ( 'NONE', ( #8490, #58916, #47941, #6397 ) ) ;
#32393=CARTESIAN_POINT ( 'NONE',  ( -60.00000000000000000, -2.024042244987997205E-14, -12.00000000000000000 ) ) ;
#32394=CARTESIAN_POINT ( 'NONE',  ( 9.058813317711338797, 123.8449999999999847, -2.943386871421372675 ) ) ;
#32395=SURFACE_STYLE_USAGE ( .BOTH. , #15572 ) ;
#32396=EDGE_LOOP ( 'NONE', ( #32838, #49550, #26745, #13359 ) ) ;
#32397=LINE ( 'NONE', #16617, #20642 ) ;
#32398=CARTESIAN_POINT ( 'NONE',  ( 9.058813317711337021, 133.6550000000000011, 2.943386871421375783 ) ) ;
#32399=EDGE_CURVE ( 'NONE', #26318, #31846, #18797, .T. ) ;
#32404=VERTEX_POINT ( 'NONE', #18119 ) ;
#32405=CARTESIAN_POINT ( 'NONE',  ( 5.598654528085805993, 145.3549999999999898, 7.705886871421374629 ) ) ;
#32407=SURFACE_STYLE_FILL_AREA ( #32086 ) ;
#32410=CARTESIAN_POINT ( 'NONE',  ( 15.98999599679679839, 146.4999999999999716, 7.500000000000000000 ) ) ;
#32411=DIRECTION ( 'NONE',  ( -1.000000000000000000, 4.336808689941999001E-16, -0.000000000000000000 ) ) ;
#32416=( NAMED_UNIT ( * ) SI_UNIT ( $, .STERADIAN. ) SOLID_ANGLE_UNIT ( ) );
#32432=PLANE ( 'NONE',  #10410 ) ;
#32438=SURFACE_STYLE_FILL_AREA ( #64814 ) ;
#32439=DIRECTION ( 'NONE',  ( -0.000000000000000000, -0.000000000000000000, 1.000000000000000000 ) ) ;
#32441=CARTESIAN_POINT ( 'NONE',  ( -9.058813317711338797, 131.3449999999999989, 2.943386871421373563 ) ) ;
#32448=AXIS2_PLACEMENT_3D ( 'NONE', #66632, #24060, #65932 ) ;
#32454=( NAMED_UNIT ( * ) PLANE_ANGLE_UNIT ( ) SI_UNIT ( $, .RADIAN. ) );
#32455=VERTEX_POINT ( 'NONE', #12472 ) ;
#32457=AXIS2_PLACEMENT_3D ( 'NONE', #19177, #52623, #4375 ) ;
#32458=DIRECTION ( 'NONE',  ( 1.000000000000000000, 0.000000000000000000, 0.000000000000000000 ) ) ;
#32459=EDGE_CURVE ( 'NONE', #23204, #20924, #32079, .T. ) ;
#32460=CARTESIAN_POINT ( 'NONE',  ( -74.99999999999998579, 50.00000000000000000, 6.999999999999988454 ) ) ;
#32462=SURFACE_SIDE_STYLE ('',( #10356 ) ) ;
#32464=AXIS2_PLACEMENT_3D ( 'NONE', #32048, #985, #48962 ) ;
#32465=ADVANCED_FACE ( 'NONE', ( #6860 ), #44201, .F. ) ;
#32467=EDGE_CURVE ( 'NONE', #45842, #52933, #22436, .T. ) ;
#32472=DIRECTION ( 'NONE',  ( 0.000000000000000000, 0.000000000000000000, 1.000000000000000000 ) ) ;
#32473=( LENGTH_UNIT ( ) NAMED_UNIT ( * ) SI_UNIT ( .MILLI., .METRE. ) );
#32475=CARTESIAN_POINT ( 'NONE',  ( 2.607480562269071989, 146.7070736234661013, 8.025000000000002132 ) ) ;
#32478=CARTESIAN_POINT ( 'NONE',  ( 8.437984349512095861, 137.1929263765338192, 1.550032578732816828E-15 ) ) ;
#32481=AXIS2_PLACEMENT_3D ( 'NONE', #4766, #53330, #9736 ) ;
#32484=PRESENTATION_STYLE_ASSIGNMENT (( #11038 ) ) ;
#32487=SURFACE_SIDE_STYLE ('',( #58904 ) ) ;
#32488=ORIENTED_EDGE ( 'NONE', *, *, #4924, .T. ) ;
#32489=MECHANICAL_DESIGN_GEOMETRIC_PRESENTATION_REPRESENTATION('',(#59452),#11163);
#32492=ORIENTED_EDGE ( 'NONE', *, *, #6903, .T. ) ;
#32496=ORIENTED_EDGE ( 'NONE', *, *, #33058, .T. ) ;
#32497=FILL_AREA_STYLE_COLOUR ( '', #64005 ) ;
#32498=ORIENTED_EDGE ( 'NONE', *, *, #62353, .T. ) ;
#32506=( NAMED_UNIT ( * ) SI_UNIT ( $, .STERADIAN. ) SOLID_ANGLE_UNIT ( ) );
#32509=CIRCLE ( 'NONE', #10051, 0.5000000000000004441 ) ;
#32510=CARTESIAN_POINT ( 'NONE',  ( 10.01517768586949408, 129.6949999999999648, 1.839758294383810543E-15 ) ) ;
#32516=VECTOR ( 'NONE', #26319, 1000.000000000000000 ) ;
#32519=SURFACE_SIDE_STYLE ('',( #5108 ) ) ;
#32522=FILL_AREA_STYLE ('',( #16739 ) ) ;
#32524=FILL_AREA_STYLE ('',( #11075 ) ) ;
#32530=CARTESIAN_POINT ( 'NONE',  ( 45.00000000000000000, 10.69371294334678879, -3.912397846414704450 ) ) ;
#32531=( NAMED_UNIT ( * ) PLANE_ANGLE_UNIT ( ) SI_UNIT ( $, .RADIAN. ) );
#32535=DIRECTION ( 'NONE',  ( 1.000000000000000000, -0.000000000000000000, 0.000000000000000000 ) ) ;
#32536=AXIS2_PLACEMENT_3D ( 'NONE', #63085, #46963, #16915 ) ;
#32538=EDGE_CURVE ( 'NONE', #35876, #6894, #64577, .T. ) ;
#32540=SURFACE_SIDE_STYLE ('',( #37554 ) ) ;
#32541=DIRECTION ( 'NONE',  ( 1.000000000000000000, 0.000000000000000000, 0.000000000000000000 ) ) ;
#32542=( GEOMETRIC_REPRESENTATION_CONTEXT ( 3 ) GLOBAL_UNCERTAINTY_ASSIGNED_CONTEXT ( ( #11673 ) ) GLOBAL_UNIT_ASSIGNED_CONTEXT ( ( #5090, #69464, #30777 ) ) REPRESENTATION_CONTEXT ( 'NONE', 'WORKASPACE' ) );
#32546=EDGE_CURVE ( 'NONE', #15417, #56786, #67693, .T. ) ;
#32553=TOROIDAL_SURFACE ( 'NONE', #24666, 22.50000000000000000, 0.5000000000000000000 ) ;
#32557=CARTESIAN_POINT ( 'NONE',  ( -2.607480562269075097, 116.4070736234661609, 8.025000000000000355 ) ) ;
#32558=CARTESIAN_POINT ( 'NONE',  ( -20.51842522107655142, 114.9046575010689821, 10.00000000000000000 ) ) ;
#32561=SURFACE_SIDE_STYLE ('',( #5465 ) ) ;
#32562=AXIS2_PLACEMENT_3D ( 'NONE', #37903, #21662, #11097 ) ;
#32563=ORIENTED_EDGE ( 'NONE', *, *, #45145, .F. ) ;
#32569=CARTESIAN_POINT ( 'NONE',  ( -5.598654528085806881, 128.8549999999999898, -7.705886871421374629 ) ) ;
#32571=CARTESIAN_POINT ( 'NONE',  ( -19.89974874213239886, 114.9999999999999574, -10.49999999999999645 ) ) ;
#32572=( GEOMETRIC_REPRESENTATION_CONTEXT ( 3 ) GLOBAL_UNCERTAINTY_ASSIGNED_CONTEXT ( ( #43990 ) ) GLOBAL_UNIT_ASSIGNED_CONTEXT ( ( #58330, #1254, #23455 ) ) REPRESENTATION_CONTEXT ( 'NONE', 'WORKASPACE' ) );
#32573=DIRECTION ( 'NONE',  ( 0.000000000000000000, 0.000000000000000000, 1.000000000000000000 ) ) ;
#32576=( GEOMETRIC_REPRESENTATION_CONTEXT ( 3 ) GLOBAL_UNCERTAINTY_ASSIGNED_CONTEXT ( ( #32646 ) ) GLOBAL_UNIT_ASSIGNED_CONTEXT ( ( #32367, #4604, #9910 ) ) REPRESENTATION_CONTEXT ( 'NONE', 'WORKASPACE' ) );
#32578=FACE_OUTER_BOUND ( 'NONE', #28048, .T. ) ;
#32581=( LENGTH_UNIT ( ) NAMED_UNIT ( * ) SI_UNIT ( .MILLI., .METRE. ) );
#32582=( GEOMETRIC_REPRESENTATION_CONTEXT ( 3 ) GLOBAL_UNCERTAINTY_ASSIGNED_CONTEXT ( ( #56512 ) ) GLOBAL_UNIT_ASSIGNED_CONTEXT ( ( #37966, #64977, #10154 ) ) REPRESENTATION_CONTEXT ( 'NONE', 'WORKASPACE' ) );
#32583=CARTESIAN_POINT ( 'NONE',  ( -12.72792206135785698, 115.4999999999999574, -10.50000000000000000 ) ) ;
#32587=DIRECTION ( 'NONE',  ( 0.000000000000000000, 0.000000000000000000, -1.000000000000000000 ) ) ;
#32592=ADVANCED_FACE ( 'NONE', ( #21932 ), #58178, .T. ) ;
#32595=CARTESIAN_POINT ( 'NONE',  ( 6.826472737025121695, 116.4929263765338021, -4.959722759717905660 ) ) ;
#32596=CARTESIAN_POINT ( 'NONE',  ( -8.487565887160236855, 153.5087057588630159, -0.9261705213943872694 ) ) ;
#32603=DIRECTION ( 'NONE',  ( 0.000000000000000000, -1.000000000000000000, 0.000000000000000000 ) ) ;
#32609=STYLED_ITEM ( 'NONE', ( #51354 ), #34512 ) ;
#32612=CARTESIAN_POINT ( 'NONE',  ( 0.000000000000000000, 87.30187232391182306, 0.000000000000000000 ) ) ;
#32613=EDGE_CURVE ( 'NONE', #16463, #2411, #38898, .T. ) ;
#32616=DIRECTION ( 'NONE',  ( 0.000000000000000000, 0.000000000000000000, 1.000000000000000000 ) ) ;
#32624=CARTESIAN_POINT ( 'NONE',  ( -3.094860106618434248, 138.9049999999999727, 9.525000000000000355 ) ) ;
#32626=VECTOR ( 'NONE', #16833, 1000.000000000000000 ) ;
#32631=SURFACE_STYLE_USAGE ( .BOTH. , #26990 ) ;
#32634=EDGE_CURVE ( 'NONE', #66255, #21253, #37713, .T. ) ;
#32638=CARTESIAN_POINT ( 'NONE',  ( 45.00000000000000000, 10.25709351175097694, -6.999999999999998224 ) ) ;
#32641=CARTESIAN_POINT ( 'NONE',  ( -2.607480562269157254, 136.2070736234661581, -8.024999999999939959 ) ) ;
#32643=VERTEX_POINT ( 'NONE', #37472 ) ;
#32644=CARTESIAN_POINT ( 'NONE',  ( -6.826472737025120807, 135.3929263765338362, -4.959722759717907437 ) ) ;
#32646=UNCERTAINTY_MEASURE_WITH_UNIT (LENGTH_MEASURE( 1.000000000000000082E-05 ), #32367, 'distance_accuracy_value', 'NONE');
#32647=COLOUR_RGB ( '', 0.66274510, 0.83137255, 0.94901961) ;
#32649=FILL_AREA_STYLE ('',( #33691 ) ) ;
#32653=FILL_AREA_STYLE ('',( #61121 ) ) ;
#32654=DIRECTION ( 'NONE',  ( -0.000000000000000000, -0.000000000000000000, -1.000000000000000000 ) ) ;
#32656=SURFACE_SIDE_STYLE ('',( #33699 ) ) ;
#32658=ORIENTED_EDGE ( 'NONE', *, *, #32546, .F. ) ;
#32659=( GEOMETRIC_REPRESENTATION_CONTEXT ( 3 ) GLOBAL_UNCERTAINTY_ASSIGNED_CONTEXT ( ( #36451 ) ) GLOBAL_UNIT_ASSIGNED_CONTEXT ( ( #48361, #15997, #53595 ) ) REPRESENTATION_CONTEXT ( 'NONE', 'WORKASPACE' ) );
#32661=COLOUR_RGB ( '', 0.31764706, 0.68627451, 0.89019608) ;
#32662=CARTESIAN_POINT ( 'NONE',  ( -1.166476076187854022E-15, 155.9449999999999932, 9.525000000000000355 ) ) ;
#32665=VECTOR ( 'NONE', #19923, 1000.000000000000000 ) ;
#32672=CARTESIAN_POINT ( 'NONE',  ( 4.716976649647096842, 133.7429263765338021, 6.492361379858953896 ) ) ;
#32674=CARTESIAN_POINT ( 'NONE',  ( -47.50000000000000000, 14.49137674618942562, 9.500000000000000000 ) ) ;
#32675=FILL_AREA_STYLE_COLOUR ( '', #43382 ) ;
#32677=STYLED_ITEM ( 'NONE', ( #25928 ), #17923 ) ;
#32679=ORIENTED_EDGE ( 'NONE', *, *, #62968, .F. ) ;
#32683=DIRECTION ( 'NONE',  ( -1.000000000000000000, 0.000000000000000000, 0.000000000000000000 ) ) ;
#32686=SURFACE_STYLE_USAGE ( .BOTH. , #37687 ) ;
#32690=FILL_AREA_STYLE_COLOUR ( '', #32744 ) ;
#32691=SURFACE_STYLE_FILL_AREA ( #43325 ) ;
#32692=ORIENTED_EDGE ( 'NONE', *, *, #16570, .F. ) ;
#32694=ORIENTED_EDGE ( 'NONE', *, *, #66553, .F. ) ;
#32695=CARTESIAN_POINT ( 'NONE',  ( -45.00000000000000000, 9.696054906849926880, 3.569578952172539399 ) ) ;
#32702=VECTOR ( 'NONE', #41961, 1000.000000000000114 ) ;
#32707=EDGE_CURVE ( 'NONE', #3021, #20470, #62448, .T. ) ;
#32709=FILL_AREA_STYLE_COLOUR ( '', #42554 ) ;
#32711=DIRECTION ( 'NONE',  ( -0.000000000000000000, -0.000000000000000000, -1.000000000000000000 ) ) ;
#32712=( BOUNDED_SURFACE ( )  B_SPLINE_SURFACE ( 3, 2, ( 
 ( #66935, #13439, #19767 ),
 ( #13800, #35260, #56722 ),
 ( #29972, #51436, #3181 ),
 ( #24674, #46196, #14158 ),
 ( #35616, #57052, #41263 ),
 ( #59122, #27097, #52843 ),
 ( #37390, #5299, #48629 ),
 ( #31342, #21860, #4620 ),
 ( #21146, #63712, #64057 ),
 ( #42653, #57767, #26075 ),
 ( #326, #58793, #36340 ),
 ( #42328, #64763, #43372 ),
 ( #53518, #52503, #32379 ),
 ( #48269, #58115, #9593 ),
 ( #4246, #53848, #20823 ),
 ( #25724, #63377, #47246 ),
 ( #16266, #68666, #37740 ),
 ( #10610, #10943, #36698 ),
 ( #20465, #69687, #15561 ),
 ( #41969, #37034, #31010 ) ),
 .UNSPECIFIED., .F., .F., .F. ) 
 B_SPLINE_SURFACE_WITH_KNOTS ( ( 4, 2, 2, 2, 2, 2, 2, 2, 2, 4 ),
 ( 3, 3 ),
 ( 0.001620365016234687986, 0.002207270000664790163, 0.002500722492879841469, 0.002794174985094892774, 0.003087627477309944080, 0.003381079969524994951, 0.003527806215632520170, 0.003674532461740045823, 0.003821258707847571476, 0.003967984953955097129 ),
 ( 0.000000000000000000, 1.000000000000000000 ),
 .UNSPECIFIED. ) 
 GEOMETRIC_REPRESENTATION_ITEM ( )  RATIONAL_B_SPLINE_SURFACE ( (
 ( 1.000000000000000000, 0.7071067811865530128, 1.000000000000000000),
 ( 1.000000000000000000, 0.6778671762787942257, 1.000000000000000000),
 ( 1.000000000000000000, 0.6467717707946214478, 1.000000000000000000),
 ( 1.000000000000000000, 0.5961086003390576593, 1.000000000000000000),
 ( 1.000000000000000000, 0.5785481842583619638, 1.000000000000000000),
 ( 1.000000000000000000, 0.5417514570912689287, 1.000000000000000000),
 ( 1.000000000000000000, 0.5224568997727286890, 1.000000000000000000),
 ( 1.000000000000000000, 0.4825437615630544519, 1.000000000000000000),
 ( 1.000000000000000000, 0.4617081702730074788, 1.000000000000000000),
 ( 1.000000000000000000, 0.4191790061641540999, 1.000000000000000000),
 ( 1.000000000000000000, 0.3974966599963052905, 1.000000000000000000),
 ( 1.000000000000000000, 0.3653498311554732592, 1.000000000000000000),
 ( 1.000000000000000000, 0.3548631489840464726, 1.000000000000000000),
 ( 1.000000000000000000, 0.3350876751767114525, 1.000000000000000000),
 ( 1.000000000000000000, 0.3256829922529743682, 1.000000000000000000),
 ( 1.000000000000000000, 0.3094849113515740768, 1.000000000000000000),
 ( 1.000000000000000000, 0.3027429446060538876, 1.000000000000000000),
 ( 1.000000000000000000, 0.2932846354086147134, 1.000000000000000000),
 ( 1.000000000000000000, 0.2906862528186607841, 1.000000000000000000),
 ( 1.000000000000000000, 0.2907356542125085763, 1.000000000000000000) ) ) 
 REPRESENTATION_ITEM ( '' )  SURFACE ( )  );
#32716=ADVANCED_FACE ( 'NONE', ( #53587 ), #5370, .F. ) ;
#32718=CARTESIAN_POINT ( 'NONE',  ( -10.01517768586949231, 158.1949999999999932, -6.132527647946036459E-16 ) ) ;
#32725=AXIS2_PLACEMENT_3D ( 'NONE', #17792, #33947, #2213 ) ;
#32731=VECTOR ( 'NONE', #3266, 1000.000000000000000 ) ;
#32733=EDGE_CURVE ( 'NONE', #39825, #56654, #3988, .T. ) ;
#32735=( LENGTH_UNIT ( ) NAMED_UNIT ( * ) SI_UNIT ( .MILLI., .METRE. ) );
#32737=ORIENTED_EDGE ( 'NONE', *, *, #52618, .T. ) ;
#32741=CIRCLE ( 'NONE', #11399, 13.99999999999999822 ) ;
#32742=DIRECTION ( 'NONE',  ( 0.000000000000000000, 0.000000000000000000, 1.000000000000000000 ) ) ;
#32744=COLOUR_RGB ( '', 0.72549020, 0.75294118, 0.79215686) ;
#32746=SURFACE_STYLE_USAGE ( .BOTH. , #17787 ) ;
#32749=EDGE_LOOP ( 'NONE', ( #4624, #65922, #1280, #24777 ) ) ;
#32751=ORIENTED_EDGE ( 'NONE', *, *, #55673, .T. ) ;
#32752=LINE ( 'NONE', #34139, #43674 ) ;
#32756=EDGE_CURVE ( 'NONE', #15520, #58139, #42285, .T. ) ;
#32757=DIRECTION ( 'NONE',  ( 1.000000000000000000, 0.000000000000000000, 0.000000000000000000 ) ) ;
#32758=CARTESIAN_POINT ( 'NONE',  ( -5.598654528085806881, 127.7450000000000045, -7.705886871421374629 ) ) ;
#32763=CARTESIAN_POINT ( 'NONE',  ( 9.058813317711338797, 130.9549999999999841, -2.943386871421372675 ) ) ;
#32767=CARTESIAN_POINT ( 'NONE',  ( -41.08036663239577990, 107.6296822352908151, -3.281244196345766806 ) ) ;
#32770=CARTESIAN_POINT ( 'NONE',  ( 5.598654528085809545, 143.2549999999999955, -7.705886871421373741 ) ) ;
#32776=DIRECTION ( 'NONE',  ( 0.7833176619561906806, -0.6216216216216158275, 0.000000000000000000 ) ) ;
#32778=( NAMED_UNIT ( * ) PLANE_ANGLE_UNIT ( ) SI_UNIT ( $, .RADIAN. ) );
#32781=( NAMED_UNIT ( * ) SI_UNIT ( $, .STERADIAN. ) SOLID_ANGLE_UNIT ( ) );
#32783=MECHANICAL_DESIGN_GEOMETRIC_PRESENTATION_REPRESENTATION('',(#4703),#56363);
#32785=CARTESIAN_POINT ( 'NONE',  ( 54.99999999999999289, 1.797044900979284448E-15, 6.999999999999988454 ) ) ;
#32786=UNCERTAINTY_MEASURE_WITH_UNIT (LENGTH_MEASURE( 1.000000000000000082E-05 ), #39919, 'distance_accuracy_value', 'NONE');
#32787=STYLED_ITEM ( 'NONE', ( #53116 ), #54527 ) ;
#32788=( NAMED_UNIT ( * ) SI_UNIT ( $, .STERADIAN. ) SOLID_ANGLE_UNIT ( ) );
#32790=DIRECTION ( 'NONE',  ( 0.000000000000000000, 0.000000000000000000, -1.000000000000000000 ) ) ;
#32793=ORIENTED_EDGE ( 'NONE', *, *, #28901, .F. ) ;
#32794=CARTESIAN_POINT ( 'NONE',  ( -71.99999999999998579, 119.9999999999997868, -7.000000000000000000 ) ) ;
#32797=CARTESIAN_POINT ( 'NONE',  ( 60.00000000000000000, 1.797044900979284448E-15, -9.500000000000000000 ) ) ;
#32800=CYLINDRICAL_SURFACE ( 'NONE', #22437, 8.000000000000014211 ) ;
#32801=CARTESIAN_POINT ( 'NONE',  ( -48.50000000000000000, 14.49137674618942562, 9.500000000000000000 ) ) ;
#32802=FILL_AREA_STYLE_COLOUR ( '', #30825 ) ;
#32804=AXIS2_PLACEMENT_3D ( 'NONE', #62188, #45715, #41826 ) ;
#32809=DIRECTION ( 'NONE',  ( 0.000000000000000000, 0.000000000000000000, 1.000000000000000000 ) ) ;
#32813=CARTESIAN_POINT ( 'NONE',  ( 0.000000000000000000, 127.4449999999999790, -9.525000000000000355 ) ) ;
#32815=CIRCLE ( 'NONE', #8110, 0.5000000000000004441 ) ;
#32817=DIRECTION ( 'NONE',  ( 0.000000000000000000, 0.000000000000000000, -1.000000000000000000 ) ) ;
#32820=AXIS2_PLACEMENT_3D ( 'NONE', #59809, #43678, #33421 ) ;
#32827=SURFACE_STYLE_FILL_AREA ( #6089 ) ;
#32832=DIRECTION ( 'NONE',  ( -0.6216216216216191581, -0.7833176619561879050, 0.000000000000000000 ) ) ;
#32833=CARTESIAN_POINT ( 'NONE',  ( 60.00000000000000000, -2.024042244987997205E-14, 7.500000000000000000 ) ) ;
#32834=MECHANICAL_DESIGN_GEOMETRIC_PRESENTATION_REPRESENTATION('',(#16047),#163);
#32835=DIRECTION ( 'NONE',  ( 1.000000000000000000, 0.000000000000000000, 0.000000000000000000 ) ) ;
#32837=DIRECTION ( 'NONE',  ( -0.000000000000000000, 1.000000000000000000, 0.000000000000000000 ) ) ;
#32838=ORIENTED_EDGE ( 'NONE', *, *, #58785, .T. ) ;
#32841=ORIENTED_EDGE ( 'NONE', *, *, #66319, .F. ) ;
#32844=DIRECTION ( 'NONE',  ( 1.000000000000000000, 0.000000000000000000, 0.000000000000000000 ) ) ;
#32845=SURFACE_STYLE_FILL_AREA ( #10698 ) ;
#32847=CARTESIAN_POINT ( 'NONE',  ( -6.826472737025120807, 154.5070736234661410, -4.959722759717907437 ) ) ;
#32856=ORIENTED_EDGE ( 'NONE', *, *, #20413, .F. ) ;
#32857=( NAMED_UNIT ( * ) PLANE_ANGLE_UNIT ( ) SI_UNIT ( $, .RADIAN. ) );
#32859=FILL_AREA_STYLE ('',( #43117 ) ) ;
#32860=CARTESIAN_POINT ( 'NONE',  ( -15.98999599679679839, 118.4999999999999716, 7.500000000000000000 ) ) ;
#32862=CIRCLE ( 'NONE', #35275, 0.5000000000000004441 ) ;
#32868=CIRCLE ( 'NONE', #27205, 8.000000000000007105 ) ;
#32869=CARTESIAN_POINT ( 'NONE',  ( 15.98999599679679839, 146.4999999999999716, 7.500000000000000000 ) ) ;
#32870=CARTESIAN_POINT ( 'NONE',  ( -45.00000000000000711, 8.681424763011792223, -5.653729937179757137 ) ) ;
#32872=( NAMED_UNIT ( * ) PLANE_ANGLE_UNIT ( ) SI_UNIT ( $, .RADIAN. ) );
#32874=ORIENTED_EDGE ( 'NONE', *, *, #58964, .F. ) ;
#32875=AXIS2_PLACEMENT_3D ( 'NONE', #59928, #33549, #33213 ) ;
#32877=FACE_OUTER_BOUND ( 'NONE', #58500, .T. ) ;
#32890=CARTESIAN_POINT ( 'NONE',  ( -9.058813317711337021, 137.0449999999999875, -2.943386871421374895 ) ) ;
#32893=STYLED_ITEM ( 'NONE', ( #2074 ), #55054 ) ;
#32897=DIRECTION ( 'NONE',  ( 0.000000000000000000, 0.000000000000000000, 1.000000000000000000 ) ) ;
#32899=DIRECTION ( 'NONE',  ( -0.000000000000000000, -1.000000000000000000, 0.000000000000000000 ) ) ;
#32902=EDGE_CURVE ( 'NONE', #58801, #28436, #18631, .T. ) ;
#32905=VECTOR ( 'NONE', #41747, 1000.000000000000000 ) ;
#32910=EDGE_CURVE ( 'NONE', #63831, #38837, #66933, .T. ) ;
#32912=CARTESIAN_POINT ( 'NONE',  ( 45.43546989188915575, 10.14515663062970319, -3.347022959407288223 ) ) ;
#32913=( GEOMETRIC_REPRESENTATION_CONTEXT ( 3 ) GLOBAL_UNCERTAINTY_ASSIGNED_CONTEXT ( ( #17398 ) ) GLOBAL_UNIT_ASSIGNED_CONTEXT ( ( #61940, #51405, #8508 ) ) REPRESENTATION_CONTEXT ( 'NONE', 'WORKASPACE' ) );
#32916=FILL_AREA_STYLE ('',( #37186 ) ) ;
#32917=AXIS2_PLACEMENT_3D ( 'NONE', #35569, #57009, #30247 ) ;
#32919=DIRECTION ( 'NONE',  ( -1.000000000000000000, 0.000000000000000000, 0.000000000000000000 ) ) ;
#32921=STYLED_ITEM ( 'NONE', ( #47824 ), #47693 ) ;
#32922=SURFACE_STYLE_FILL_AREA ( #59627 ) ;
#32929=DIRECTION ( 'NONE',  ( -1.000000000000000000, 0.000000000000000000, 0.000000000000000000 ) ) ;
#32934=CARTESIAN_POINT ( 'NONE',  ( 7.632228543268607446, 114.1570736234661609, 2.479861379858954606 ) ) ;
#32938=CARTESIAN_POINT ( 'NONE',  ( 74.63815776008156888, 19.81286551027084997, -6.251809480268889274 ) ) ;
#32939=DIRECTION ( 'NONE',  ( -0.000000000000000000, -0.000000000000000000, 1.000000000000000000 ) ) ;
#32940=ORIENTED_EDGE ( 'NONE', *, *, #12347, .F. ) ;
#32941=VERTEX_POINT ( 'NONE', #2844 ) ;
#32945=ORIENTED_EDGE ( 'NONE', *, *, #59710, .F. ) ;
#32946=DIRECTION ( 'NONE',  ( -0.000000000000000000, -0.000000000000000000, 1.000000000000000000 ) ) ;
#32948=CARTESIAN_POINT ( 'NONE',  ( -9.827790563157511022E-16, 148.4429263765338476, 8.025000000000000355 ) ) ;
#32952=CARTESIAN_POINT ( 'NONE',  ( 6.856148508274209519, 153.8597198435754478, -5.665282084007170482 ) ) ;
#32957=FILL_AREA_STYLE ('',( #65649 ) ) ;
#32958=DIRECTION ( 'NONE',  ( 1.000000000000000000, -0.000000000000000000, -0.000000000000000000 ) ) ;
#32960=ORIENTED_EDGE ( 'NONE', *, *, #37502, .T. ) ;
#32962=ADVANCED_FACE ( 'NONE', ( #14475 ), #35250, .T. ) ;
#32964=LINE ( 'NONE', #22396, #43982 ) ;
#32966=FACE_BOUND ( 'NONE', #45108, .T. ) ;
#32970=CARTESIAN_POINT ( 'NONE',  ( -74.99999999999998579, 50.00000000000000000, 12.00000000000000000 ) ) ;
#32973=CARTESIAN_POINT ( 'NONE',  ( -8.325601791849269517, 153.4724253098392239, -1.721597945495230153 ) ) ;
#32976=FACE_OUTER_BOUND ( 'NONE', #41349, .T. ) ;
#32977=ORIENTED_EDGE ( 'NONE', *, *, #42331, .F. ) ;
#32978=SURFACE_STYLE_USAGE ( .BOTH. , #64966 ) ;
#32979=AXIS2_PLACEMENT_3D ( 'NONE', #9313, #62416, #3271 ) ;
#32981=CARTESIAN_POINT ( 'NONE',  ( 0.000000000000000000, 111.9999999999999858, 0.000000000000000000 ) ) ;
#32984=EDGE_CURVE ( 'NONE', #66646, #17220, #34836, .T. ) ;
#32987=CARTESIAN_POINT ( 'NONE',  ( 44.47787316461987928, 9.825957721539955614, 3.000913084730184366 ) ) ;
#32989=CARTESIAN_POINT ( 'NONE',  ( -6.826472737025120807, 150.3929263765338078, -4.959722759717907437 ) ) ;
#32995=CARTESIAN_POINT ( 'NONE',  ( 3.094860106618431583, 133.2049999999999841, 9.525000000000000355 ) ) ;
#32998=CARTESIAN_POINT ( 'NONE',  ( 7.647808743684392674, 154.4999999999999432, 5.677732506910178500 ) ) ;
#33000=SURFACE_STYLE_FILL_AREA ( #16155 ) ;
#33005=( NAMED_UNIT ( * ) SI_UNIT ( $, .STERADIAN. ) SOLID_ANGLE_UNIT ( ) );
#33006=DIRECTION ( 'NONE',  ( 0.000000000000000000, 1.000000000000000000, 0.000000000000000000 ) ) ;
#33007=CARTESIAN_POINT ( 'NONE',  ( 0.000000000000000000, 131.9429263765338192, -8.025000000000000355 ) ) ;
#33008=ORIENTED_EDGE ( 'NONE', *, *, #11042, .F. ) ;
#33009=ORIENTED_EDGE ( 'NONE', *, *, #51404, .T. ) ;
#33011=DIRECTION ( 'NONE',  ( 0.000000000000000000, -1.000000000000000000, 0.000000000000000000 ) ) ;
#33012=EDGE_CURVE ( 'NONE', #12588, #16496, #63011, .T. ) ;
#33014=AXIS2_PLACEMENT_3D ( 'NONE', #50358, #54582, #60533 ) ;
#33015=DIRECTION ( 'NONE',  ( 1.000000000000000000, 0.000000000000000000, 0.000000000000000000 ) ) ;
#33016=CARTESIAN_POINT ( 'NONE',  ( 23.71231517720798010, 112.9999999999999858, -7.500000000000000000 ) ) ;
#33024=CARTESIAN_POINT ( 'NONE',  ( -20.94636006565341191, 149.9999999999999716, 9.500000000000000000 ) ) ;
#33027=CIRCLE ( 'NONE', #12829, 5.000000000000004441 ) ;
#33029=CARTESIAN_POINT ( 'NONE',  ( -9.058813317711337021, 158.0449999999999875, -2.943386871421374895 ) ) ;
#33035=DIRECTION ( 'NONE',  ( 1.000000000000000000, 0.000000000000000000, 0.000000000000000000 ) ) ;
#33036=FILL_AREA_STYLE ('',( #17235 ) ) ;
#33040=CARTESIAN_POINT ( 'NONE',  ( 8.437984349512095861, 131.1929263765338192, 1.550032578732817026E-15 ) ) ;
#33045=FACE_OUTER_BOUND ( 'NONE', #19693, .T. ) ;
#33046=ADVANCED_FACE ( 'NONE', ( #61965 ), #45828, .T. ) ;
#33049=ORIENTED_EDGE ( 'NONE', *, *, #14168, .T. ) ;
#33051=FILL_AREA_STYLE ('',( #64359 ) ) ;
#33054=CARTESIAN_POINT ( 'NONE',  ( 23.21231517720797655, 117.9999999999999716, 7.000000000000000000 ) ) ;
#33055=VERTEX_POINT ( 'NONE', #17202 ) ;
#33057=CIRCLE ( 'NONE', #57765, 0.5000000000000004441 ) ;
#33058=EDGE_CURVE ( 'NONE', #60543, #42295, #44968, .T. ) ;
#33061=CARTESIAN_POINT ( 'NONE',  ( 41.84210526315788314, 107.2928455055531458, 4.000000000000000888 ) ) ;
#33063=ORIENTED_EDGE ( 'NONE', *, *, #9393, .F. ) ;
#33065=DIRECTION ( 'NONE',  ( 0.000000000000000000, 0.000000000000000000, 1.000000000000000000 ) ) ;
#33068=DIRECTION ( 'NONE',  ( 0.000000000000000000, -1.000000000000000000, -0.000000000000000000 ) ) ;
#33073=SURFACE_STYLE_USAGE ( .BOTH. , #26394 ) ;
#33075=ORIENTED_EDGE ( 'NONE', *, *, #20413, .T. ) ;
#33080=DIRECTION ( 'NONE',  ( -0.000000000000000000, 1.000000000000000000, -0.000000000000000000 ) ) ;
#33082=CARTESIAN_POINT ( 'NONE',  ( 8.102448949553181734, 156.3950000000000102, 5.886773742842750679 ) ) ;
#33084=DIRECTION ( 'NONE',  ( 0.000000000000000000, 1.000000000000000000, -0.000000000000000000 ) ) ;
#33085=CIRCLE ( 'NONE', #43277, 0.5000000000000004441 ) ;
#33087=DIRECTION ( 'NONE',  ( -1.000000000000000000, 0.000000000000000000, 0.000000000000000000 ) ) ;
#33089=SURFACE_STYLE_USAGE ( .BOTH. , #22884 ) ;
#33095=( GEOMETRIC_REPRESENTATION_CONTEXT ( 3 ) GLOBAL_UNCERTAINTY_ASSIGNED_CONTEXT ( ( #42681 ) ) GLOBAL_UNIT_ASSIGNED_CONTEXT ( ( #12308, #64418, #5646 ) ) REPRESENTATION_CONTEXT ( 'NONE', 'WORKASPACE' ) );
#33096=CARTESIAN_POINT ( 'NONE',  ( -34.99999999999992895, 112.4999999999999858, 10.00000000000000000 ) ) ;
#33101=DIRECTION ( 'NONE',  ( 1.000000000000000000, 0.000000000000000000, 0.000000000000000000 ) ) ;
#33102=EDGE_CURVE ( 'NONE', #60684, #7860, #31461, .T. ) ;
#33108=VERTEX_POINT ( 'NONE', #27345 ) ;
#33112=ORIENTED_EDGE ( 'NONE', *, *, #48035, .T. ) ;
#33114=DIRECTION ( 'NONE',  ( 0.000000000000000000, 0.000000000000000000, 1.000000000000000000 ) ) ;
#33116=AXIS2_PLACEMENT_3D ( 'NONE', #12067, #11025, #60266 ) ;
#33119=DIRECTION ( 'NONE',  ( -0.9486832980505138790, -0.3162277660168378857, 0.000000000000000000 ) ) ;
#33120=CARTESIAN_POINT ( 'NONE',  ( 3.094860106618431583, 132.0949999999999989, 9.525000000000000355 ) ) ;
#33121=FILL_AREA_STYLE ('',( #12321 ) ) ;
#33125=CARTESIAN_POINT ( 'NONE',  ( 8.102448949553179958, 130.5049999999999955, 5.886773742842750679 ) ) ;
#33128=CARTESIAN_POINT ( 'NONE',  ( -74.99999999999998579, 64.49137674618943095, 9.500000000000000000 ) ) ;
#33130=CARTESIAN_POINT ( 'NONE',  ( -4.716976649647097730, 111.2429263765338163, -6.492361379858953896 ) ) ;
#33133=DIRECTION ( 'NONE',  ( 1.000000000000000000, 0.000000000000000000, 0.000000000000000000 ) ) ;
#33134=ADVANCED_FACE ( 'NONE', ( #11887 ), #46127, .T. ) ;
#33138=STYLED_ITEM ( 'NONE', ( #4272 ), #57712 ) ;
#33139=DIRECTION ( 'NONE',  ( 1.000000000000000000, -0.000000000000000000, 0.000000000000000000 ) ) ;
#33140=ORIENTED_EDGE ( 'NONE', *, *, #11434, .F. ) ;
#33143=ORIENTED_EDGE ( 'NONE', *, *, #69031, .F. ) ;
#33144=DIRECTION ( 'NONE',  ( -0.7071067811865549002, 0.000000000000000000, -0.7071067811865401342 ) ) ;
#33146=FILL_AREA_STYLE ('',( #11674 ) ) ;
#33148=CIRCLE ( 'NONE', #68001, 0.5000000000000004441 ) ;
#33149=SURFACE_SIDE_STYLE ('',( #65132 ) ) ;
#33150=CARTESIAN_POINT ( 'NONE',  ( -45.00000000000000000, 9.708372675170618749, 3.611004237778676185 ) ) ;
#33151=( BOUNDED_CURVE ( )  B_SPLINE_CURVE ( 2, ( #29719, #35698, #25132, #13886, #14580, #46645, #30049, #67016, #3274, #19848, #62054 ),
 .UNSPECIFIED., .F., .F. ) 
 B_SPLINE_CURVE_WITH_KNOTS ( ( 3, 2, 2, 2, 2, 3 ),
 ( 0.2647058823529411242, 0.2705882352941175739, 0.2764705882352940791, 0.2823529411764705843, 0.2882352941176470340, 0.2941176470588235392 ),
 .UNSPECIFIED. ) 
 CURVE ( )  GEOMETRIC_REPRESENTATION_ITEM ( )  RATIONAL_B_SPLINE_CURVE ( ( 1.000000000000000666, 0.9510565162951531981, 1.000000000000000000, 0.9510565162951535312, 1.000000000000000000, 0.9510565162951535312, 1.000000000000000000, 0.9510565162951535312, 1.000000000000000000, 0.9510565162951535312, 1.000000000000000000 ) ) 
 REPRESENTATION_ITEM ( '' )  );
#33154=CARTESIAN_POINT ( 'NONE',  ( -45.21668476461162101, 8.382617247524212445, -3.000000000000000000 ) ) ;
#33158=PRESENTATION_STYLE_ASSIGNMENT (( #59166 ) ) ;
#33160=COLOUR_RGB ( '', 0.66274510, 0.83137255, 0.94901961) ;
#33162=CARTESIAN_POINT ( 'NONE',  ( -75.00000000000000000, 8.553059399042478361, -6.924772212933357984 ) ) ;
#33163=ORIENTED_EDGE ( 'NONE', *, *, #48945, .F. ) ;
#33164=FACE_OUTER_BOUND ( 'NONE', #40636, .T. ) ;
#33165=DIRECTION ( 'NONE',  ( 1.000000000000000000, 0.000000000000000000, 0.000000000000000000 ) ) ;
#33169=CARTESIAN_POINT ( 'NONE',  ( -8.102448949553181734, 130.8949999999999818, -5.886773742842749790 ) ) ;
#33173=ADVANCED_FACE ( 'NONE', ( #1945 ), #36015, .T. ) ;
#33174=CARTESIAN_POINT ( 'NONE',  ( -15.98999599679679839, 146.4999999999999716, 7.000000000000000000 ) ) ;
#33180=DIRECTION ( 'NONE',  ( 1.000000000000000000, 0.000000000000000000, 0.000000000000000000 ) ) ;
#33187=PRESENTATION_STYLE_ASSIGNMENT (( #21581 ) ) ;
#33188=AXIS2_PLACEMENT_3D ( 'NONE', #5122, #64583, #65255 ) ;
#33190=DIRECTION ( 'NONE',  ( 0.000000000000000000, -1.000000000000000000, 0.000000000000000000 ) ) ;
#33192=ORIENTED_EDGE ( 'NONE', *, *, #37858, .T. ) ;
#33194=ORIENTED_EDGE ( 'NONE', *, *, #14593, .F. ) ;
#33197=EDGE_CURVE ( 'NONE', #7813, #14819, #66743, .T. ) ;
#33199=CYLINDRICAL_SURFACE ( 'NONE', #17425, 0.5000000000000004441 ) ;
#33200=CARTESIAN_POINT ( 'NONE',  ( -4.716976649647097730, 157.3570736234661638, -6.492361379858953896 ) ) ;
#33201=AXIS2_PLACEMENT_3D ( 'NONE', #50199, #44946, #18173 ) ;
#33206=SURFACE_SIDE_STYLE ('',( #59211 ) ) ;
#33209=( NAMED_UNIT ( * ) SI_UNIT ( $, .STERADIAN. ) SOLID_ANGLE_UNIT ( ) );
#33212=CARTESIAN_POINT ( 'NONE',  ( 44.99999999999998579, 119.9999999999999716, 7.000000000000000000 ) ) ;
#33213=DIRECTION ( 'NONE',  ( 0.000000000000000000, 0.000000000000000000, -1.000000000000000000 ) ) ;
#33221=ORIENTED_EDGE ( 'NONE', *, *, #8206, .T. ) ;
#33222=EDGE_CURVE ( 'NONE', #38944, #42646, #51727, .T. ) ;
#33224=CARTESIAN_POINT ( 'NONE',  ( -75.00000000000000000, 8.747695062214207340, 6.883368695986967545 ) ) ;
#33228=FILL_AREA_STYLE_COLOUR ( '', #17353 ) ;
#33229=STYLED_ITEM ( 'NONE', ( #615 ), #58308 ) ;
#33230=CARTESIAN_POINT ( 'NONE',  ( -75.00000000000000000, -2.215169945516535778E-14, 10.00000000000000000 ) ) ;
#33232=CARTESIAN_POINT ( 'NONE',  ( 9.058813317711337021, 129.5449999999999875, 2.943386871421375783 ) ) ;
#33233=TOROIDAL_SURFACE ( 'NONE', #6255, 9.499999999999996447, 0.5000000000000000000 ) ;
#33238=DIRECTION ( 'NONE',  ( -1.000000000000000000, 0.000000000000000000, 0.000000000000000000 ) ) ;
#33239=DIRECTION ( 'NONE',  ( -0.000000000000000000, -0.000000000000000000, -1.000000000000000000 ) ) ;
#33241=DIRECTION ( 'NONE',  ( 0.000000000000000000, -0.000000000000000000, 1.000000000000000000 ) ) ;
#33244=( NAMED_UNIT ( * ) PLANE_ANGLE_UNIT ( ) SI_UNIT ( $, .RADIAN. ) );
#33247=ORIENTED_EDGE ( 'NONE', *, *, #27221, .F. ) ;
#33249=( LENGTH_UNIT ( ) NAMED_UNIT ( * ) SI_UNIT ( .MILLI., .METRE. ) );
#33251=FILL_AREA_STYLE ('',( #23376 ) ) ;
#33253=UNCERTAINTY_MEASURE_WITH_UNIT (LENGTH_MEASURE( 1.000000000000000082E-05 ), #49269, 'distance_accuracy_value', 'NONE');
#33255=( LENGTH_UNIT ( ) NAMED_UNIT ( * ) SI_UNIT ( .MILLI., .METRE. ) );
#33257=MECHANICAL_DESIGN_GEOMETRIC_PRESENTATION_REPRESENTATION('',(#55748),#11901);
#33260=CYLINDRICAL_SURFACE ( 'NONE', #6211, 0.5000000000000004441 ) ;
#33261=COLOUR_RGB ( '', 0.31764706, 0.68627451, 0.89019608) ;
#33262=DIRECTION ( 'NONE',  ( 1.156482317317866302E-16, -1.000000000000000000, 0.000000000000000000 ) ) ;
#33270=VECTOR ( 'NONE', #12938, 1000.000000000000000 ) ;
#33272=ORIENTED_EDGE ( 'NONE', *, *, #31873, .F. ) ;
#33278=AXIS2_PLACEMENT_3D ( 'NONE', #19078, #56378, #13120 ) ;
#33279=CARTESIAN_POINT ( 'NONE',  ( -6.826472737025120807, 125.1070736234661638, 4.959722759717906548 ) ) ;
#33281=CARTESIAN_POINT ( 'NONE',  ( 6.826472737025121695, 138.6070736234661638, -4.959722759717905660 ) ) ;
#33282=CARTESIAN_POINT ( 'NONE',  ( 34.99999999999999289, 99.99999999999998579, -7.500000000000000000 ) ) ;
#33283=ORIENTED_EDGE ( 'NONE', *, *, #29702, .T. ) ;
#33284=ORIENTED_EDGE ( 'NONE', *, *, #37126, .T. ) ;
#33289=DIRECTION ( 'NONE',  ( 1.000000000000000000, 0.000000000000000000, 0.000000000000000000 ) ) ;
#33292=EDGE_CURVE ( 'NONE', #2723, #16561, #15717, .T. ) ;
#33293=CARTESIAN_POINT ( 'NONE',  ( 7.632228543268608334, 134.3429263765337964, -2.479861379858951942 ) ) ;
#33297=EDGE_CURVE ( 'NONE', #4250, #54470, #65053, .T. ) ;
#33298=SURFACE_SIDE_STYLE ('',( #28326 ) ) ;
#33300=ORIENTED_EDGE ( 'NONE', *, *, #61045, .T. ) ;
#33301=DIRECTION ( 'NONE',  ( -1.000000000000000000, 0.000000000000000000, -0.000000000000000000 ) ) ;
#33303=( GEOMETRIC_REPRESENTATION_CONTEXT ( 3 ) GLOBAL_UNCERTAINTY_ASSIGNED_CONTEXT ( ( #58683 ) ) GLOBAL_UNIT_ASSIGNED_CONTEXT ( ( #52363, #4830, #25579 ) ) REPRESENTATION_CONTEXT ( 'NONE', 'WORKASPACE' ) );
#33308=ORIENTED_EDGE ( 'NONE', *, *, #42011, .T. ) ;
#33312=FACE_OUTER_BOUND ( 'NONE', #1494, .T. ) ;
#33316=CARTESIAN_POINT ( 'NONE',  ( -8.527945164174161263, 153.6178632149283487, 1.507062088730512617 ) ) ;
#33317=EDGE_LOOP ( 'NONE', ( #55613, #57050, #10316, #50673 ) ) ;
#33318=CARTESIAN_POINT ( 'NONE',  ( -79.99999999999998579, 50.00000000000000000, -6.999999999999988454 ) ) ;
#33321=( NAMED_UNIT ( * ) SI_UNIT ( $, .STERADIAN. ) SOLID_ANGLE_UNIT ( ) );
#33322=AXIS2_PLACEMENT_3D ( 'NONE', #38948, #32946, #33964 ) ;
#33323=VERTEX_POINT ( 'NONE', #37196 ) ;
#33326=CARTESIAN_POINT ( 'NONE',  ( -6.422934014168760974, 111.9999999999999858, 4.811085495980506721 ) ) ;
#33329=ORIENTED_EDGE ( 'NONE', *, *, #3531, .T. ) ;
#33330=SURFACE_SIDE_STYLE ('',( #38653 ) ) ;
#33331=CARTESIAN_POINT ( 'NONE',  ( 45.00320036294371562, 10.00106678764790225, 3.045234739864684403 ) ) ;
#33338=CARTESIAN_POINT ( 'NONE',  ( 0.000000000000000000, 134.5549999999999784, -9.525000000000000355 ) ) ;
#33339=CARTESIAN_POINT ( 'NONE',  ( -7.632228543268607446, 126.5429263765337993, -2.479861379858953718 ) ) ;
#33340=UNCERTAINTY_MEASURE_WITH_UNIT (LENGTH_MEASURE( 1.000000000000000082E-05 ), #4079, 'distance_accuracy_value', 'NONE');
#33341=( NAMED_UNIT ( * ) SI_UNIT ( $, .STERADIAN. ) SOLID_ANGLE_UNIT ( ) );
#33343=ORIENTED_EDGE ( 'NONE', *, *, #25255, .T. ) ;
#33345=DIRECTION ( 'NONE',  ( 0.000000000000000000, 1.000000000000000000, 0.000000000000000000 ) ) ;
#33346=STYLED_ITEM ( 'NONE', ( #46690 ), #65115 ) ;
#33349=EDGE_CURVE ( 'NONE', #33822, #53938, #47774, .T. ) ;
#33350=CARTESIAN_POINT ( 'NONE',  ( 44.99999999999998579, 119.9999999999999716, 9.500000000000000000 ) ) ;
#33356=CARTESIAN_POINT ( 'NONE',  ( 21.02379604162863913, 110.4999999999999858, 9.500000000000000000 ) ) ;
#33357=EDGE_CURVE ( 'NONE', #40163, #54309, #39394, .T. ) ;
#33359=EDGE_LOOP ( 'NONE', ( #9618, #14454, #14367, #89 ) ) ;
#33361=ORIENTED_EDGE ( 'NONE', *, *, #25816, .F. ) ;
#33362=CARTESIAN_POINT ( 'NONE',  ( 60.00000000000000000, 110.4999999999999858, -10.00000000000000000 ) ) ;
#33365=EDGE_LOOP ( 'NONE', ( #32793, #51191, #19806, #30082 ) ) ;
#33370=SURFACE_STYLE_FILL_AREA ( #44322 ) ;
#33371=CARTESIAN_POINT ( 'NONE',  ( 3.094860106618431583, 159.0949999999999420, 9.525000000000000355 ) ) ;
#33376=( LENGTH_UNIT ( ) NAMED_UNIT ( * ) SI_UNIT ( .MILLI., .METRE. ) );
#33378=EDGE_CURVE ( 'NONE', #14708, #27627, #25538, .T. ) ;
#33380=CARTESIAN_POINT ( 'NONE',  ( -2.607480562269073765, 135.0929263765338249, -8.025000000000000355 ) ) ;
#33381=DIRECTION ( 'NONE',  ( 0.000000000000000000, 0.000000000000000000, 1.000000000000000000 ) ) ;
#33382=DIRECTION ( 'NONE',  ( 0.000000000000000000, -1.000000000000000000, 0.000000000000000000 ) ) ;
#33386=ORIENTED_EDGE ( 'NONE', *, *, #56809, .F. ) ;
#33390=SURFACE_SIDE_STYLE ('',( #66431 ) ) ;
#33391=( NAMED_UNIT ( * ) PLANE_ANGLE_UNIT ( ) SI_UNIT ( $, .RADIAN. ) );
#33392=UNCERTAINTY_MEASURE_WITH_UNIT (LENGTH_MEASURE( 1.000000000000000082E-05 ), #42824, 'distance_accuracy_value', 'NONE');
#33394=DIRECTION ( 'NONE',  ( -1.000000000000000000, 0.000000000000000000, 0.000000000000000000 ) ) ;
#33395=CARTESIAN_POINT ( 'NONE',  ( -45.00000000000000000, 9.372904743120717086, -6.583929160757660881 ) ) ;
#33396=EDGE_LOOP ( 'NONE', ( #42030, #55097 ) ) ;
#33397=STYLED_ITEM ( 'NONE', ( #32254 ), #58687 ) ;
#33402=ORIENTED_EDGE ( 'NONE', *, *, #63392, .T. ) ;
#33403=DIRECTION ( 'NONE',  ( -1.000000000000000000, 1.224646799147349509E-16, 0.000000000000000000 ) ) ;
#33405=CARTESIAN_POINT ( 'NONE',  ( -48.50000000000000000, 14.49137674618942562, 7.500000000000000000 ) ) ;
#33407=CARTESIAN_POINT ( 'NONE',  ( 23.21231517720797655, 117.9999999999999716, 7.500000000000000000 ) ) ;
#33413=DIRECTION ( 'NONE',  ( 0.000000000000000000, 0.000000000000000000, 1.000000000000000000 ) ) ;
#33415=CARTESIAN_POINT ( 'NONE',  ( -60.00000000000000000, -2.024042244987997205E-14, 11.50000000000003020 ) ) ;
#33417=CARTESIAN_POINT ( 'NONE',  ( -5.598654528085806881, 110.8549999999999756, -7.705886871421374629 ) ) ;
#33419=DIRECTION ( 'NONE',  ( -1.000000000000000000, 0.000000000000000000, 0.000000000000000000 ) ) ;
#33421=DIRECTION ( 'NONE',  ( -1.000000000000000000, 1.224646799147349509E-16, 0.000000000000000000 ) ) ;
#33422=UNCERTAINTY_MEASURE_WITH_UNIT (LENGTH_MEASURE( 1.000000000000000082E-05 ), #49212, 'distance_accuracy_value', 'NONE');
#33424=CARTESIAN_POINT ( 'NONE',  ( 70.87837837837835764, 13.70805908423323949, 10.00000000000000000 ) ) ;
#33425=LINE ( 'NONE', #54856, #52165 ) ;
#33426=ORIENTED_EDGE ( 'NONE', *, *, #38092, .T. ) ;
#33435=FACE_OUTER_BOUND ( 'NONE', #49646, .T. ) ;
#33437=( GEOMETRIC_REPRESENTATION_CONTEXT ( 3 ) GLOBAL_UNCERTAINTY_ASSIGNED_CONTEXT ( ( #15034 ) ) GLOBAL_UNIT_ASSIGNED_CONTEXT ( ( #28009, #23134, #50553 ) ) REPRESENTATION_CONTEXT ( 'NONE', 'WORKASPACE' ) );
#33438=DIRECTION ( 'NONE',  ( 0.000000000000000000, -1.000000000000000000, 0.000000000000000000 ) ) ;
#33439=DIRECTION ( 'NONE',  ( 0.000000000000000000, 0.000000000000000000, -1.000000000000000000 ) ) ;
#33440=CIRCLE ( 'NONE', #25590, 0.5000000000000004441 ) ;
#33442=VECTOR ( 'NONE', #17915, 1000.000000000000000 ) ;
#33443=DIRECTION ( 'NONE',  ( -0.000000000000000000, -0.000000000000000000, -1.000000000000000000 ) ) ;
#33447=ORIENTED_EDGE ( 'NONE', *, *, #37640, .T. ) ;
#33450=EDGE_LOOP ( 'NONE', ( #33272, #772, #5165, #32945 ) ) ;
#33452=MECHANICAL_DESIGN_GEOMETRIC_PRESENTATION_REPRESENTATION('',(#15511),#1941);
#33454=DIRECTION ( 'NONE',  ( 1.000000000000000000, 0.000000000000000000, 0.000000000000000000 ) ) ;
#33455=CARTESIAN_POINT ( 'NONE',  ( -8.102448949553181734, 127.8949999999999534, -5.886773742842749790 ) ) ;
#33456=( NAMED_UNIT ( * ) PLANE_ANGLE_UNIT ( ) SI_UNIT ( $, .RADIAN. ) );
#33460=CARTESIAN_POINT ( 'NONE',  ( 3.094860106618431583, 127.2049999999999841, 9.525000000000000355 ) ) ;
#33463=CARTESIAN_POINT ( 'NONE',  ( 41.84210526315787604, 107.2928455055531600, -4.000000000000000888 ) ) ;
#33465=CARTESIAN_POINT ( 'NONE',  ( 8.102448949553181734, 157.5050000000000239, 5.886773742842750679 ) ) ;
#33466=CARTESIAN_POINT ( 'NONE',  ( 0.000000000000000000, 149.9999999999999716, 0.000000000000000000 ) ) ;
#33469=CARTESIAN_POINT ( 'NONE',  ( -79.99999999999998579, 50.00000000000000000, -12.00000000000000000 ) ) ;
#33473=SURFACE_SIDE_STYLE ('',( #61241 ) ) ;
#33477=EDGE_LOOP ( 'NONE', ( #52943, #63422, #10581, #1907, #48715 ) ) ;
#33479=DIRECTION ( 'NONE',  ( -1.000000000000000000, 0.000000000000000000, -0.000000000000000000 ) ) ;
#33481=ORIENTED_EDGE ( 'NONE', *, *, #53747, .F. ) ;
#33482=CARTESIAN_POINT ( 'NONE',  ( -45.90821385068745286, 9.419345871351781696, -3.356457195962587736 ) ) ;
#33483=DIRECTION ( 'NONE',  ( 0.000000000000000000, 0.000000000000000000, 1.000000000000000000 ) ) ;
#33487=DIRECTION ( 'NONE',  ( 1.000000000000000000, 0.000000000000000000, 0.000000000000000000 ) ) ;
#33488=DIRECTION ( 'NONE',  ( -0.000000000000000000, -0.000000000000000000, -1.000000000000000000 ) ) ;
#33491=CARTESIAN_POINT ( 'NONE',  ( -74.50000000000000000, 7.768687147774688384, -6.500000000000000888 ) ) ;
#33495=COLOUR_RGB ( '', 0.66274510, 0.83137255, 0.94901961) ;
#33496=CARTESIAN_POINT ( 'NONE',  ( 0.000000000000000000, 130.4449999999999648, -9.525000000000000355 ) ) ;
#33507=STYLED_ITEM ( 'NONE', ( #43754 ), #67661 ) ;
#33508=EDGE_CURVE ( 'NONE', #38783, #68819, #34891, .T. ) ;
#33509=ADVANCED_FACE ( 'NONE', ( #43858 ), #64141, .F. ) ;
#33510=DIRECTION ( 'NONE',  ( 0.000000000000000000, 1.000000000000000000, 0.000000000000000000 ) ) ;
#33512=ORIENTED_EDGE ( 'NONE', *, *, #15128, .F. ) ;
#33515=ORIENTED_EDGE ( 'NONE', *, *, #35673, .T. ) ;
#33517=CARTESIAN_POINT ( 'NONE',  ( -48.50000000000000000, 14.49137674618942384, -7.500000000000000000 ) ) ;
#33520=AXIS2_PLACEMENT_3D ( 'NONE', #53492, #64735, #48600 ) ;
#33521=PRESENTATION_STYLE_ASSIGNMENT (( #16683 ) ) ;
#33529=ORIENTED_EDGE ( 'NONE', *, *, #3257, .F. ) ;
#33530=FILL_AREA_STYLE_COLOUR ( '', #59477 ) ;
#33531=( NAMED_UNIT ( * ) PLANE_ANGLE_UNIT ( ) SI_UNIT ( $, .RADIAN. ) );
#33532=AXIS2_PLACEMENT_3D ( 'NONE', #61619, #62668, #30298 ) ;
#33533=CARTESIAN_POINT ( 'NONE',  ( -4.716976649647097730, 154.3570736234661922, -6.492361379858953896 ) ) ;
#33534=ORIENTED_EDGE ( 'NONE', *, *, #17449, .F. ) ;
#33535=SURFACE_STYLE_FILL_AREA ( #17045 ) ;
#33537=( BOUNDED_CURVE ( )  B_SPLINE_CURVE ( 2, ( #12646, #54522, #27425 ),
 .UNSPECIFIED., .F., .T. ) 
 B_SPLINE_CURVE_WITH_KNOTS ( ( 3, 3 ),
 ( 0.05767644037838164095, 0.05882352941176476058 ),
 .UNSPECIFIED. ) 
 CURVE ( )  GEOMETRIC_REPRESENTATION_ITEM ( )  RATIONAL_B_SPLINE_CURVE ( ( 0.9846338866368906650, 0.9904557693197236778, 1.000000000000000444 ) ) 
 REPRESENTATION_ITEM ( '' )  );
#33539=DIRECTION ( 'NONE',  ( -1.000000000000000000, 1.387778780781444571E-14, 0.000000000000000000 ) ) ;
#33540=AXIS2_PLACEMENT_3D ( 'NONE', #22704, #6493, #17108 ) ;
#33542=DIRECTION ( 'NONE',  ( 1.000000000000000000, 0.000000000000000000, 0.000000000000000000 ) ) ;
#33549=DIRECTION ( 'NONE',  ( 0.000000000000000000, -1.000000000000000000, 0.000000000000000000 ) ) ;
#33552=EDGE_LOOP ( 'NONE', ( #5654, #52929, #21519, #67489 ) ) ;
#33553=( NAMED_UNIT ( * ) SI_UNIT ( $, .STERADIAN. ) SOLID_ANGLE_UNIT ( ) );
#33556=CARTESIAN_POINT ( 'NONE',  ( -45.00000000000000000, 9.675838479951684334, -6.195399861057250490 ) ) ;
#33558=CARTESIAN_POINT ( 'NONE',  ( -69.49999999999997158, 50.00000000000000000, 6.499999999999999112 ) ) ;
#33560=DIRECTION ( 'NONE',  ( 0.000000000000000000, -1.000000000000000000, 0.000000000000000000 ) ) ;
#33564=( LENGTH_UNIT ( ) NAMED_UNIT ( * ) SI_UNIT ( .MILLI., .METRE. ) );
#33566=( NAMED_UNIT ( * ) PLANE_ANGLE_UNIT ( ) SI_UNIT ( $, .RADIAN. ) );
#33569=CARTESIAN_POINT ( 'NONE',  ( 8.102448949553179958, 129.3949999999999818, 5.886773742842750679 ) ) ;
#33571=FILL_AREA_STYLE_COLOUR ( '', #67363 ) ;
#33573=( NAMED_UNIT ( * ) SI_UNIT ( $, .STERADIAN. ) SOLID_ANGLE_UNIT ( ) );
#33574=( LENGTH_UNIT ( ) NAMED_UNIT ( * ) SI_UNIT ( .MILLI., .METRE. ) );
#33576=PRESENTATION_STYLE_ASSIGNMENT (( #60990 ) ) ;
#33579=CARTESIAN_POINT ( 'NONE',  ( 15.98999599679679839, 118.4999999999999716, 7.500000000000000000 ) ) ;
#33582=CIRCLE ( 'NONE', #42620, 13.49999999999999822 ) ;
#33586=TOROIDAL_SURFACE ( 'NONE', #50467, 17.50000000000000000, 0.5000000000000000000 ) ;
#33587=SURFACE_SIDE_STYLE ('',( #18108 ) ) ;
#33595=LINE ( 'NONE', #44552, #45581 ) ;
#33596=TOROIDAL_SURFACE ( 'NONE', #37062, 29.50000000000000000, 0.5000000000000000000 ) ;
#33597=CARTESIAN_POINT ( 'NONE',  ( 71.49999999999998579, 64.07124727947029896, 7.000000000000000000 ) ) ;
#33602=FILL_AREA_STYLE ('',( #60330 ) ) ;
#33603=CARTESIAN_POINT ( 'NONE',  ( -40.99999999999998579, 107.7459666924148394, 3.000000000000000444 ) ) ;
#33604=AXIS2_PLACEMENT_3D ( 'NONE', #43577, #16821, #44950 ) ;
#33605=ADVANCED_FACE ( 'NONE', ( #57490 ), #20189, .F. ) ;
#33608=LINE ( 'NONE', #29001, #52006 ) ;
#33611=CARTESIAN_POINT ( 'NONE',  ( -7.632228543268607446, 124.6570736234661609, -2.479861379858953718 ) ) ;
#33612=AXIS2_PLACEMENT_3D ( 'NONE', #14217, #35331, #35680 ) ;
#33613=CARTESIAN_POINT ( 'NONE',  ( -23.71231517720798010, 117.4999999999999716, -9.500000000000000000 ) ) ;
#33614=CARTESIAN_POINT ( 'NONE',  ( 6.826472737025119919, 138.0070736234661410, 4.959722759717908325 ) ) ;
#33615=CARTESIAN_POINT ( 'NONE',  ( 68.00000000000000000, 2.776762340297168394E-15, 12.00000000000000000 ) ) ;
#33618=ORIENTED_EDGE ( 'NONE', *, *, #4, .F. ) ;
#33619=CARTESIAN_POINT ( 'NONE',  ( -60.00000000000000000, -2.024042244987997205E-14, 12.00000000000000000 ) ) ;
#33624=DIRECTION ( 'NONE',  ( 0.000000000000000000, -1.000000000000000000, 0.000000000000000000 ) ) ;
#33629=CIRCLE ( 'NONE', #5538, 14.49999999999999822 ) ;
#33630=DIRECTION ( 'NONE',  ( 1.000000000000000000, 0.000000000000000000, 0.000000000000000000 ) ) ;
#33632=MECHANICAL_DESIGN_GEOMETRIC_PRESENTATION_REPRESENTATION('',(#49422),#42677);
#33634=LINE ( 'NONE', #27289, #53858 ) ;
#33635=CARTESIAN_POINT ( 'NONE',  ( -75.48275862068965125, 63.99167409976912069, -41.30495168499704306 ) ) ;
#33636=AXIS2_PLACEMENT_3D ( 'NONE', #47946, #69345, #29529 ) ;
#33640=DIRECTION ( 'NONE',  ( -1.000000000000000000, 0.000000000000000000, 0.000000000000000000 ) ) ;
#33645=CARTESIAN_POINT ( 'NONE',  ( -75.00000000000000000, 35.50862325381056905, 10.00000000000000000 ) ) ;
#33646=TOROIDAL_SURFACE ( 'NONE', #21286, 1.000000000000000000, 0.5000000000000000000 ) ;
#33650=ORIENTED_EDGE ( 'NONE', *, *, #35571, .F. ) ;
#33653=SPHERICAL_SURFACE ( 'NONE', #42522, 0.5000000000000000000 ) ;
#33655=ORIENTED_EDGE ( 'NONE', *, *, #13731, .F. ) ;
#33659=EDGE_CURVE ( 'NONE', #66900, #5467, #19849, .T. ) ;
#33662=CIRCLE ( 'NONE', #3284, 0.5000000000000004441 ) ;
#33664=PRESENTATION_STYLE_ASSIGNMENT (( #22779 ) ) ;
#33665=CARTESIAN_POINT ( 'NONE',  ( 44.88867800444037215, 10.61949827965496240, 3.673511479703632787 ) ) ;
#33666=CARTESIAN_POINT ( 'NONE',  ( -6.826472737025120807, 150.9929263765338305, 4.959722759717906548 ) ) ;
#33672=CARTESIAN_POINT ( 'NONE',  ( 0.000000000000000000, 146.5549999999999784, -9.525000000000000355 ) ) ;
#33673=CARTESIAN_POINT ( 'NONE',  ( -15.98999599679679839, 146.9999999999999716, 10.00000000000000000 ) ) ;
#33675=CARTESIAN_POINT ( 'NONE',  ( 2.525713312988952630, 154.2507441751838542, 8.932758862731519756 ) ) ;
#33680=COLOUR_RGB ( '', 0.09019608, 0.27058824, 0.51372549) ;
#33682=DIRECTION ( 'NONE',  ( 0.000000000000000000, 0.000000000000000000, -1.000000000000000000 ) ) ;
#33683=EDGE_CURVE ( 'NONE', #20924, #34097, #61672, .T. ) ;
#33685=CARTESIAN_POINT ( 'NONE',  ( 34.99999999999999289, 99.99999999999998579, 7.000000000000000000 ) ) ;
#33687=ORIENTED_EDGE ( 'NONE', *, *, #49595, .T. ) ;
#33689=EDGE_LOOP ( 'NONE', ( #7521, #31365, #62344, #18136 ) ) ;
#33691=FILL_AREA_STYLE_COLOUR ( '', #38457 ) ;
#33694=VERTEX_POINT ( 'NONE', #43097 ) ;
#33697=PRESENTATION_STYLE_ASSIGNMENT (( #18219 ) ) ;
#33698=EDGE_LOOP ( 'NONE', ( #57868, #16270, #28950, #2330 ) ) ;
#33699=SURFACE_STYLE_FILL_AREA ( #65717 ) ;
#33705=ORIENTED_EDGE ( 'NONE', *, *, #66048, .T. ) ;
#33706=CARTESIAN_POINT ( 'NONE',  ( -74.08841914795480932, 9.415459729490459395, -6.077763577362910397 ) ) ;
#33707=EDGE_LOOP ( 'NONE', ( #18954, #6347, #4003, #39567 ) ) ;
#33708=CARTESIAN_POINT ( 'NONE',  ( -4.716976649647097730, 138.2429263765338305, -6.492361379858953896 ) ) ;
#33709=DIRECTION ( 'NONE',  ( 0.000000000000000000, 0.000000000000000000, -1.000000000000000000 ) ) ;
#33710=DIRECTION ( 'NONE',  ( 0.000000000000000000, 0.000000000000000000, -1.000000000000000000 ) ) ;
#33712=ORIENTED_EDGE ( 'NONE', *, *, #18916, .T. ) ;
#33713=AXIS2_PLACEMENT_3D ( 'NONE', #66665, #53751, #18481 ) ;
#33717=CARTESIAN_POINT ( 'NONE',  ( -60.00000000000000000, -2.024042244987997205E-14, -6.500000000000000000 ) ) ;
#33718=SURFACE_STYLE_FILL_AREA ( #39051 ) ;
#33720=CARTESIAN_POINT ( 'NONE',  ( 40.99999999999997868, 9.999999999999978684, 3.000000000000000000 ) ) ;
#33721=AXIS2_PLACEMENT_3D ( 'NONE', #9841, #4529, #47515 ) ;
#33724=CARTESIAN_POINT ( 'NONE',  ( -4.716976649647098618, 116.2570736234661553, 6.492361379858953008 ) ) ;
#33733=DIRECTION ( 'NONE',  ( 0.000000000000000000, 0.000000000000000000, -1.000000000000000000 ) ) ;
#33736=EDGE_CURVE ( 'NONE', #6686, #29473, #32509, .T. ) ;
#33739=FILL_AREA_STYLE ('',( #28442 ) ) ;
#33740=CIRCLE ( 'NONE', #36030, 23.00000000000000000 ) ;
#33742=EDGE_CURVE ( 'NONE', #63218, #62320, #29139, .T. ) ;
#33750=DIRECTION ( 'NONE',  ( 0.000000000000000000, 0.000000000000000000, -1.000000000000000000 ) ) ;
#33751=EDGE_CURVE ( 'NONE', #48904, #37089, #37042, .T. ) ;
#33754=CARTESIAN_POINT ( 'NONE',  ( 5.598654528085805993, 156.2450000000000045, 7.705886871421374629 ) ) ;
#33757=CARTESIAN_POINT ( 'NONE',  ( 0.000000000000000000, 110.4999999999999858, 0.000000000000000000 ) ) ;
#33762=SURFACE_STYLE_FILL_AREA ( #28466 ) ;
#33770=COLOUR_RGB ( '', 0.31764706, 0.68627451, 0.89019608) ;
#33772=ORIENTED_EDGE ( 'NONE', *, *, #2305, .F. ) ;
#33777=PRESENTATION_STYLE_ASSIGNMENT (( #39102 ) ) ;
#33779=PRESENTATION_STYLE_ASSIGNMENT (( #11638 ) ) ;
#33784=DIRECTION ( 'NONE',  ( -0.000000000000000000, -0.000000000000000000, -1.000000000000000000 ) ) ;
#33787=COLOUR_RGB ( '', 0.08235294, 0.09019608, 0.10196078) ;
#33790=CARTESIAN_POINT ( 'NONE',  ( 5.598654528085805993, 129.2450000000000045, 7.705886871421374629 ) ) ;
#33791=SURFACE_STYLE_USAGE ( .BOTH. , #54557 ) ;
#33797=CARTESIAN_POINT ( 'NONE',  ( 10.01517768586949408, 130.8049999999999784, 1.839758294383810543E-15 ) ) ;
#33799=CARTESIAN_POINT ( 'NONE',  ( 41.39002736484397360, 107.1345546009599445, -3.500000000000000000 ) ) ;
#33801=CARTESIAN_POINT ( 'NONE',  ( -1.166476076187854022E-15, 160.0550000000000068, 9.525000000000000355 ) ) ;
#33803=( GEOMETRIC_REPRESENTATION_CONTEXT ( 3 ) GLOBAL_UNCERTAINTY_ASSIGNED_CONTEXT ( ( #41073 ) ) GLOBAL_UNIT_ASSIGNED_CONTEXT ( ( #38916, #55746, #50471 ) ) REPRESENTATION_CONTEXT ( 'NONE', 'WORKASPACE' ) );
#33804=PLANE ( 'NONE',  #24349 ) ;
#33805=DIRECTION ( 'NONE',  ( 0.000000000000000000, 0.000000000000000000, 1.000000000000000000 ) ) ;
#33807=ORIENTED_EDGE ( 'NONE', *, *, #20186, .F. ) ;
#33808=ORIENTED_EDGE ( 'NONE', *, *, #32467, .T. ) ;
#33809=SURFACE_STYLE_FILL_AREA ( #28152 ) ;
#33817=DIRECTION ( 'NONE',  ( 0.000000000000000000, 1.000000000000000000, -0.000000000000000000 ) ) ;
#33819=ORIENTED_EDGE ( 'NONE', *, *, #15552, .F. ) ;
#33822=VERTEX_POINT ( 'NONE', #53596 ) ;
#33825=LINE ( 'NONE', #51409, #46621 ) ;
#33826=EDGE_CURVE ( 'NONE', #44582, #48466, #27971, .T. ) ;
#33828=CARTESIAN_POINT ( 'NONE',  ( -75.00000000000000000, 8.121151660576289899, -6.396433738442264705 ) ) ;
#33830=PRESENTATION_STYLE_ASSIGNMENT (( #12365 ) ) ;
#33832=DIRECTION ( 'NONE',  ( -1.000000000000000000, 0.000000000000000000, 0.000000000000000000 ) ) ;
#33833=CARTESIAN_POINT ( 'NONE',  ( -8.102448949553181734, 127.8949999999999534, -5.886773742842749790 ) ) ;
#33837=SURFACE_STYLE_USAGE ( .BOTH. , #54931 ) ;
#33843=FACE_OUTER_BOUND ( 'NONE', #55713, .T. ) ;
#33845=CARTESIAN_POINT ( 'NONE',  ( 60.00000000000000000, -2.024042244987997205E-14, -10.00000000000000000 ) ) ;
#33846=ORIENTED_EDGE ( 'NONE', *, *, #25431, .F. ) ;
#33849=CARTESIAN_POINT ( 'NONE',  ( -45.57140627820939471, 8.073499555448574228, 6.499999999999999112 ) ) ;
#33852=STYLED_ITEM ( 'NONE', ( #38169 ), #45950 ) ;
#33856=COLOUR_RGB ( '', 0.66274510, 0.83137255, 0.94901961) ;
#33857=VERTEX_POINT ( 'NONE', #61288 ) ;
#33860=SURFACE_STYLE_FILL_AREA ( #50078 ) ;
#33861=SURFACE_STYLE_USAGE ( .BOTH. , #65891 ) ;
#33863=AXIS2_PLACEMENT_3D ( 'NONE', #14175, #61630, #13455 ) ;
#33864=CARTESIAN_POINT ( 'NONE',  ( -8.437984349512095861, 148.8070736234661240, -5.166775262442723748E-16 ) ) ;
#33866=AXIS2_PLACEMENT_3D ( 'NONE', #3638, #30051, #35354 ) ;
#33870=CARTESIAN_POINT ( 'NONE',  ( -9.827790563157511022E-16, 122.5570736234661524, 8.025000000000000355 ) ) ;
#33872=CARTESIAN_POINT ( 'NONE',  ( -9.058813317711337021, 129.1550000000000011, -2.943386871421374895 ) ) ;
#33873=CIRCLE ( 'NONE', #67592, 10.49999999999999822 ) ;
#33878=CARTESIAN_POINT ( 'NONE',  ( 67.50000000000000000, 1.797044900979284448E-15, -11.50000000000000000 ) ) ;
#33881=LINE ( 'NONE', #17736, #21577 ) ;
#33885=AXIS2_PLACEMENT_3D ( 'NONE', #50608, #45026, #2345 ) ;
#33887=CARTESIAN_POINT ( 'NONE',  ( -45.00000000000000000, 9.289150624329689521, -6.641434857031669026 ) ) ;
#33891=CARTESIAN_POINT ( 'NONE',  ( -65.50000000000000000, -1.956686671034892874E-14, -6.500000000000000000 ) ) ;
#33894=EDGE_CURVE ( 'NONE', #6686, #8720, #61612, .T. ) ;
#33897=EDGE_LOOP ( 'NONE', ( #62644, #64357, #36260, #23234, #18463, #37495, #45186, #42276, #82, #19529, #28745, #45344, #29192, #48234, #21670, #44511, #49836, #46090, #43204, #37315, #64508, #12789, #14606, #56799, #55949, #52093, #25734, #44898, #65332, #8898, #59378, #34184, #28843, #33655 ) ) ;
#33900=CARTESIAN_POINT ( 'NONE',  ( -24.21231517720798010, 113.4999999999999858, 10.00000000000000000 ) ) ;
#33902=DIRECTION ( 'NONE',  ( 0.000000000000000000, 0.000000000000000000, 1.000000000000000000 ) ) ;
#33904=( GEOMETRIC_REPRESENTATION_CONTEXT ( 3 ) GLOBAL_UNCERTAINTY_ASSIGNED_CONTEXT ( ( #217 ) ) GLOBAL_UNIT_ASSIGNED_CONTEXT ( ( #32735, #53839, #11630 ) ) REPRESENTATION_CONTEXT ( 'NONE', 'WORKASPACE' ) );
#33906=CARTESIAN_POINT ( 'NONE',  ( 9.058813317711338797, 129.8449999999999989, -2.943386871421372675 ) ) ;
#33908=MECHANICAL_DESIGN_GEOMETRIC_PRESENTATION_REPRESENTATION('',(#5825),#28304);
#33910=( NAMED_UNIT ( * ) PLANE_ANGLE_UNIT ( ) SI_UNIT ( $, .RADIAN. ) );
#33913=EDGE_CURVE ( 'NONE', #25661, #64306, #44163, .T. ) ;
#33915=SURFACE_STYLE_FILL_AREA ( #6840 ) ;
#33919=CIRCLE ( 'NONE', #39591, 13.99999999999999822 ) ;
#33923=MECHANICAL_DESIGN_GEOMETRIC_PRESENTATION_REPRESENTATION('',(#27171),#3557);
#33925=ORIENTED_EDGE ( 'NONE', *, *, #6667, .F. ) ;
#33927=PRESENTATION_STYLE_ASSIGNMENT (( #23049 ) ) ;
#33930=MECHANICAL_DESIGN_GEOMETRIC_PRESENTATION_REPRESENTATION('',(#23790),#18169);
#33935=FILL_AREA_STYLE ('',( #38919 ) ) ;
#33937=( LENGTH_UNIT ( ) NAMED_UNIT ( * ) SI_UNIT ( .MILLI., .METRE. ) );
#33941=( NAMED_UNIT ( * ) SI_UNIT ( $, .STERADIAN. ) SOLID_ANGLE_UNIT ( ) );
#33944=PRESENTATION_STYLE_ASSIGNMENT (( #18128 ) ) ;
#33946=MECHANICAL_DESIGN_GEOMETRIC_PRESENTATION_REPRESENTATION('',(#6992),#39615);
#33947=DIRECTION ( 'NONE',  ( -0.000000000000000000, -0.000000000000000000, -1.000000000000000000 ) ) ;
#33950=CARTESIAN_POINT ( 'NONE',  ( -75.48275862068965125, 63.99167409976912069, -41.30495168499704306 ) ) ;
#33953=CARTESIAN_POINT ( 'NONE',  ( -2.607480562269075097, 128.4070736234661183, 8.025000000000000355 ) ) ;
#33954=ADVANCED_FACE ( 'NONE', ( #1800, #50072 ), #60578, .F. ) ;
#33957=CARTESIAN_POINT ( 'NONE',  ( -74.50000000000001421, 36.50926243676796190, 10.00000000000000000 ) ) ;
#33958=VECTOR ( 'NONE', #56832, 1000.000000000000000 ) ;
#33959=SURFACE_STYLE_FILL_AREA ( #148 ) ;
#33960=ORIENTED_EDGE ( 'NONE', *, *, #35437, .T. ) ;
#33964=DIRECTION ( 'NONE',  ( 1.000000000000000000, 0.000000000000000000, 0.000000000000000000 ) ) ;
#33965=SURFACE_STYLE_FILL_AREA ( #7930 ) ;
#33966=AXIS2_PLACEMENT_3D ( 'NONE', #13037, #59843, #2057 ) ;
#33968=CARTESIAN_POINT ( 'NONE',  ( 6.826472737025119919, 148.8929263765338078, 4.959722759717908325 ) ) ;
#33974=CARTESIAN_POINT ( 'NONE',  ( 45.50000000000000000, 9.639620389971918613, 6.500000000000000888 ) ) ;
#33976=UNCERTAINTY_MEASURE_WITH_UNIT (LENGTH_MEASURE( 1.000000000000000082E-05 ), #54648, 'distance_accuracy_value', 'NONE');
#33977=VERTEX_POINT ( 'NONE', #51104 ) ;
#33978=CARTESIAN_POINT ( 'NONE',  ( 8.437984349512095861, 161.1929263765338192, 1.550032578732817026E-15 ) ) ;
#33979=EDGE_CURVE ( 'NONE', #30440, #19491, #7867, .T. ) ;
#33980=EDGE_CURVE ( 'NONE', #3150, #64454, #69286, .T. ) ;
#33983=EDGE_CURVE ( 'NONE', #11216, #68346, #62661, .T. ) ;
#33984=COLOUR_RGB ( '', 0.40784314, 0.44705882, 0.49803922) ;
#33992=CIRCLE ( 'NONE', #16062, 0.5000000000000004441 ) ;
#33993=( NAMED_UNIT ( * ) SI_UNIT ( $, .STERADIAN. ) SOLID_ANGLE_UNIT ( ) );
#33996=EDGE_LOOP ( 'NONE', ( #42437, #45682, #18724, #59494, #25826, #37924, #64370 ) ) ;
#33997=CARTESIAN_POINT ( 'NONE',  ( 6.826472737025119919, 121.8929263765338220, 4.959722759717908325 ) ) ;
#33998=EDGE_CURVE ( 'NONE', #67765, #33822, #31457, .T. ) ;
#33999=FILL_AREA_STYLE ('',( #16817 ) ) ;
#34001=ORIENTED_EDGE ( 'NONE', *, *, #16304, .F. ) ;
#34008=ORIENTED_EDGE ( 'NONE', *, *, #6743, .T. ) ;
#34010=AXIS2_PLACEMENT_3D ( 'NONE', #12954, #23500, #56910 ) ;
#34011=CARTESIAN_POINT ( 'NONE',  ( 44.30330429060720121, 9.767768096869062333, 3.048789874180130255 ) ) ;
#34012=SURFACE_STYLE_FILL_AREA ( #52721 ) ;
#34018=CARTESIAN_POINT ( 'NONE',  ( 5.598654528085809545, 143.2549999999999955, -7.705886871421373741 ) ) ;
#34019=EDGE_CURVE ( 'NONE', #62248, #5399, #42728, .T. ) ;
#34025=UNCERTAINTY_MEASURE_WITH_UNIT (LENGTH_MEASURE( 1.000000000000000082E-05 ), #30271, 'distance_accuracy_value', 'NONE');
#34029=CARTESIAN_POINT ( 'NONE',  ( 0.000000000000000000, 114.4999999999999574, 0.000000000000000000 ) ) ;
#34030=AXIS2_PLACEMENT_3D ( 'NONE', #30494, #61808, #14333 ) ;
#34032=LINE ( 'NONE', #1628, #4603 ) ;
#34033=COLOUR_RGB ( '', 0.66274510, 0.83137255, 0.94901961) ;
#34034=( NAMED_UNIT ( * ) PLANE_ANGLE_UNIT ( ) SI_UNIT ( $, .RADIAN. ) );
#34040=COLOUR_RGB ( '', 0.09019608, 0.27058824, 0.51372549) ;
#34041=FILL_AREA_STYLE ('',( #39355 ) ) ;
#34042=SURFACE_STYLE_FILL_AREA ( #50235 ) ;
#34050=DIRECTION ( 'NONE',  ( -0.000000000000000000, -0.000000000000000000, -1.000000000000000000 ) ) ;
#34051=ORIENTED_EDGE ( 'NONE', *, *, #17948, .F. ) ;
#34053=AXIS2_PLACEMENT_3D ( 'NONE', #21066, #69596, #53437 ) ;
#34054=AXIS2_PLACEMENT_3D ( 'NONE', #40294, #30055, #3281 ) ;
#34061=CARTESIAN_POINT ( 'NONE',  ( 44.99999999999998579, 119.9999999999999716, -7.500000000000000000 ) ) ;
#34064=ORIENTED_EDGE ( 'NONE', *, *, #40198, .F. ) ;
#34065=CARTESIAN_POINT ( 'NONE',  ( 2.607480562269076430, 137.7929263765338135, -8.025000000000000355 ) ) ;
#34068=DIRECTION ( 'NONE',  ( 1.000000000000000000, 0.000000000000000000, 0.000000000000000000 ) ) ;
#34073=ORIENTED_EDGE ( 'NONE', *, *, #18816, .T. ) ;
#34076=DIRECTION ( 'NONE',  ( 0.000000000000000000, 0.000000000000000000, 1.000000000000000000 ) ) ;
#34078=AXIS2_PLACEMENT_3D ( 'NONE', #31652, #58065, #63326 ) ;
#34082=MECHANICAL_DESIGN_GEOMETRIC_PRESENTATION_REPRESENTATION('',(#42029),#10600);
#34086=STYLED_ITEM ( 'NONE', ( #36715 ), #6209 ) ;
#34087=CARTESIAN_POINT ( 'NONE',  ( -20.77811424250900174, 115.1386898118646656, 10.00000000000000000 ) ) ;
#34091=LINE ( 'NONE', #17917, #10145 ) ;
#34093=DIRECTION ( 'NONE',  ( -0.000000000000000000, -0.000000000000000000, -1.000000000000000000 ) ) ;
#34097=VERTEX_POINT ( 'NONE', #57408 ) ;
#34098=COLOUR_RGB ( '', 0.31764706, 0.68627451, 0.89019608) ;
#34099=SPHERICAL_SURFACE ( 'NONE', #40348, 0.5000000000000000000 ) ;
#34104=DIRECTION ( 'NONE',  ( -1.000000000000000000, -0.000000000000000000, -0.000000000000000000 ) ) ;
#34105=DIRECTION ( 'NONE',  ( 0.000000000000000000, 0.000000000000000000, 1.000000000000000000 ) ) ;
#34107=CARTESIAN_POINT ( 'NONE',  ( 9.058813317711338797, 121.9549999999999841, -2.943386871421372675 ) ) ;
#34110=DIRECTION ( 'NONE',  ( 0.000000000000000000, 0.000000000000000000, 1.000000000000000000 ) ) ;
#34112=UNCERTAINTY_MEASURE_WITH_UNIT (LENGTH_MEASURE( 1.000000000000000082E-05 ), #56750, 'distance_accuracy_value', 'NONE');
#34113=FILL_AREA_STYLE_COLOUR ( '', #26931 ) ;
#34114=AXIS2_PLACEMENT_3D ( 'NONE', #64098, #36730, #5341 ) ;
#34115=SURFACE_STYLE_USAGE ( .BOTH. , #34798 ) ;
#34126=DIRECTION ( 'NONE',  ( -1.000000000000000000, 0.000000000000000000, 0.000000000000000000 ) ) ;
#34127=SURFACE_STYLE_FILL_AREA ( #59823 ) ;
#34128=CIRCLE ( 'NONE', #17299, 8.000000000000000000 ) ;
#34130=FILL_AREA_STYLE ('',( #12663 ) ) ;
#34137=CIRCLE ( 'NONE', #12791, 29.50000000000000000 ) ;
#34138=ORIENTED_EDGE ( 'NONE', *, *, #59182, .T. ) ;
#34139=CARTESIAN_POINT ( 'NONE',  ( -48.00000000000000000, 99.99999999999992895, 7.000000000000000000 ) ) ;
#34143=CIRCLE ( 'NONE', #38665, 0.5000000000000004441 ) ;
#34146=CARTESIAN_POINT ( 'NONE',  ( 5.598654528085809545, 127.1449999999999818, -7.705886871421373741 ) ) ;
#34148=CIRCLE ( 'NONE', #42095, 0.5000000000000004441 ) ;
#34149=ORIENTED_EDGE ( 'NONE', *, *, #48996, .F. ) ;
#34152=CARTESIAN_POINT ( 'NONE',  ( -9.058813317711337021, 138.1550000000000011, -2.943386871421374895 ) ) ;
#34154=CARTESIAN_POINT ( 'NONE',  ( 41.13907225104257037, 107.8972693614197169, -3.376186789259871812 ) ) ;
#34156=CARTESIAN_POINT ( 'NONE',  ( 8.102448949553183510, 161.1049999999999613, -5.886773742842746238 ) ) ;
#34165=EDGE_LOOP ( 'NONE', ( #57605, #59820, #8160, #17963 ) ) ;
#34167=CARTESIAN_POINT ( 'NONE',  ( 60.00000000000000000, -2.024042244987997205E-14, -7.000000000000000000 ) ) ;
#34171=( GEOMETRIC_REPRESENTATION_CONTEXT ( 3 ) GLOBAL_UNCERTAINTY_ASSIGNED_CONTEXT ( ( #68562 ) ) GLOBAL_UNIT_ASSIGNED_CONTEXT ( ( #51975, #57949, #68150 ) ) REPRESENTATION_CONTEXT ( 'NONE', 'WORKASPACE' ) );
#34176=ORIENTED_EDGE ( 'NONE', *, *, #69259, .T. ) ;
#34177=PRESENTATION_STYLE_ASSIGNMENT (( #28872 ) ) ;
#34178=UNCERTAINTY_MEASURE_WITH_UNIT (LENGTH_MEASURE( 1.000000000000000082E-05 ), #19106, 'distance_accuracy_value', 'NONE');
#34180=CARTESIAN_POINT ( 'NONE',  ( -65.99999999999998579, 50.00000000000000000, -10.49999999999999822 ) ) ;
#34184=ORIENTED_EDGE ( 'NONE', *, *, #9889, .T. ) ;
#34186=CARTESIAN_POINT ( 'NONE',  ( -45.91025672304794369, 9.422403540771759012, -3.407313310066902190 ) ) ;
#34189=DIRECTION ( 'NONE',  ( 0.000000000000000000, 1.000000000000000000, 0.000000000000000000 ) ) ;
#34190=AXIS2_PLACEMENT_3D ( 'NONE', #2252, #39302, #61061 ) ;
#34191=( BOUNDED_CURVE ( )  B_SPLINE_CURVE ( 2, ( #676, #1735, #22205 ),
 .UNSPECIFIED., .F., .F. ) 
 B_SPLINE_CURVE_WITH_KNOTS ( ( 3, 3 ),
 ( 0.8235294117647057321, 0.8246765007980889628 ),
 .UNSPECIFIED. ) 
 CURVE ( )  GEOMETRIC_REPRESENTATION_ITEM ( )  RATIONAL_B_SPLINE_CURVE ( ( 1.000000000000000888, 0.9904557693197235668, 0.9846338866368905540 ) ) 
 REPRESENTATION_ITEM ( '' )  );
#34193=CARTESIAN_POINT ( 'NONE',  ( 44.99999999999977973, 149.4999999999999716, -9.500000000000000000 ) ) ;
#34197=CYLINDRICAL_SURFACE ( 'NONE', #23341, 0.5000000000000004441 ) ;
#34199=AXIS2_PLACEMENT_3D ( 'NONE', #38848, #39182, #15722 ) ;
#34200=CARTESIAN_POINT ( 'NONE',  ( -5.598654528085808657, 134.6449999999999818, 7.705886871421373741 ) ) ;
#34202=DIRECTION ( 'NONE',  ( 0.000000000000000000, 0.000000000000000000, 1.000000000000000000 ) ) ;
#34204=CARTESIAN_POINT ( 'NONE',  ( -23.21231517720797655, 117.4999999999999716, -9.500000000000000000 ) ) ;
#34212=( NAMED_UNIT ( * ) SI_UNIT ( $, .STERADIAN. ) SOLID_ANGLE_UNIT ( ) );
#34213=VERTEX_POINT ( 'NONE', #20824 ) ;
#34214=CARTESIAN_POINT ( 'NONE',  ( 15.98999599679679839, 117.4999999999999716, -10.00000000000000000 ) ) ;
#34217=LINE ( 'NONE', #50397, #54006 ) ;
#34218=CARTESIAN_POINT ( 'NONE',  ( 44.70258591656318714, 9.999999999999980460, -3.296040418704463182 ) ) ;
#34220=CARTESIAN_POINT ( 'NONE',  ( -8.437984349512095861, 142.8070736234661808, -5.166775262442723748E-16 ) ) ;
#34221=ORIENTED_EDGE ( 'NONE', *, *, #31682, .F. ) ;
#34223=( GEOMETRIC_REPRESENTATION_CONTEXT ( 3 ) GLOBAL_UNCERTAINTY_ASSIGNED_CONTEXT ( ( #24286 ) ) GLOBAL_UNIT_ASSIGNED_CONTEXT ( ( #62426, #68762, #30054 ) ) REPRESENTATION_CONTEXT ( 'NONE', 'WORKASPACE' ) );
#34225=( NAMED_UNIT ( * ) SI_UNIT ( $, .STERADIAN. ) SOLID_ANGLE_UNIT ( ) );
#34228=DIRECTION ( 'NONE',  ( 0.000000000000000000, 0.000000000000000000, 1.000000000000000000 ) ) ;
#34230=CARTESIAN_POINT ( 'NONE',  ( 7.632228543268608334, 156.4570736234661581, -2.479861379858951942 ) ) ;
#34231=COLOUR_RGB ( '', 0.08235294, 0.09019608, 0.10196078) ;
#34233=ORIENTED_EDGE ( 'NONE', *, *, #42809, .T. ) ;
#34234=CARTESIAN_POINT ( 'NONE',  ( 21.02379604162863913, 114.4999999999999574, -10.00000000000000000 ) ) ;
#34237=CARTESIAN_POINT ( 'NONE',  ( -7.632228543268607446, 121.6570736234661609, -2.479861379858953718 ) ) ;
#34238=CARTESIAN_POINT ( 'NONE',  ( -10.01517768586949231, 132.3049999999999500, -6.132527647946036459E-16 ) ) ;
#34239=UNCERTAINTY_MEASURE_WITH_UNIT (LENGTH_MEASURE( 1.000000000000000082E-05 ), #24472, 'distance_accuracy_value', 'NONE');
#34242=LINE ( 'NONE', #56026, #37704 ) ;
#34244=FILL_AREA_STYLE_COLOUR ( '', #66532 ) ;
#34245=ORIENTED_EDGE ( 'NONE', *, *, #52288, .T. ) ;
#34246=( NAMED_UNIT ( * ) PLANE_ANGLE_UNIT ( ) SI_UNIT ( $, .RADIAN. ) );
#34247=SURFACE_STYLE_FILL_AREA ( #66960 ) ;
#34251=CARTESIAN_POINT ( 'NONE',  ( -45.00000000000000000, 9.656580361551753811, -6.242521039668959659 ) ) ;
#34252=EDGE_CURVE ( 'NONE', #52169, #5042, #15725, .T. ) ;
#34257=AXIS2_PLACEMENT_3D ( 'NONE', #67148, #18936, #61850 ) ;
#34258=CARTESIAN_POINT ( 'NONE',  ( -75.00000000000000000, 8.707403661853380328, 5.727618941855547874 ) ) ;
#34262=DIRECTION ( 'NONE',  ( 0.000000000000000000, 0.000000000000000000, 1.000000000000000000 ) ) ;
#34264=VECTOR ( 'NONE', #39090, 1000.000000000000000 ) ;
#34266=COLOUR_RGB ( '', 0.40784314, 0.44705882, 0.49803922) ;
#34268=CARTESIAN_POINT ( 'NONE',  ( 8.102448949553179958, 138.3949999999999818, 5.886773742842750679 ) ) ;
#34271=SPHERICAL_SURFACE ( 'NONE', #66461, 0.5000000000000000000 ) ;
#34274=DIRECTION ( 'NONE',  ( 0.000000000000000000, 1.000000000000000000, 0.000000000000000000 ) ) ;
#34276=CIRCLE ( 'NONE', #27516, 0.5000000000000004441 ) ;
#34283=CIRCLE ( 'NONE', #15200, 0.5000000000000004441 ) ;
#34287=DIRECTION ( 'NONE',  ( -1.000000000000000000, 0.000000000000000000, 0.000000000000000000 ) ) ;
#34293=B_SPLINE_CURVE_WITH_KNOTS ( 'NONE', 3,
 ( #62485, #24843, #35767, #24160 ),
 .UNSPECIFIED., .F., .F.,
 ( 4, 4 ),
 ( 6.735063895479954530E-16, 0.001113530544794672211 ),
 .UNSPECIFIED. ) ;
#34295=DIRECTION ( 'NONE',  ( 1.000000000000000000, 0.000000000000000000, 0.000000000000000000 ) ) ;
#34296=DIRECTION ( 'NONE',  ( 1.000000000000000000, 0.000000000000000000, 0.000000000000000000 ) ) ;
#34300=AXIS2_PLACEMENT_3D ( 'NONE', #5342, #10987, #6390 ) ;
#34302=CIRCLE ( 'NONE', #43357, 0.5000000000000004441 ) ;
#34304=SURFACE_SIDE_STYLE ('',( #34635 ) ) ;
#34305=CARTESIAN_POINT ( 'NONE',  ( -41.01786561352938065, 107.7208547478748528, 3.150777047984529844 ) ) ;
#34310=ORIENTED_EDGE ( 'NONE', *, *, #22888, .F. ) ;
#34312=AXIS2_PLACEMENT_3D ( 'NONE', #21238, #4350, #32159 ) ;
#34316=CARTESIAN_POINT ( 'NONE',  ( 4.716976649647099507, 120.7570736234661553, -6.492361379858953008 ) ) ;
#34317=EDGE_CURVE ( 'NONE', #14638, #3378, #14609, .T. ) ;
#34318=CARTESIAN_POINT ( 'NONE',  ( -23.21231517720798010, 117.9999999999999716, -10.00000000000000000 ) ) ;
#34319=CARTESIAN_POINT ( 'NONE',  ( 75.00000000000000000, 19.83714805418753002, -6.873786395979923469 ) ) ;
#34323=COLOUR_RGB ( '', 0.40784314, 0.44705882, 0.49803922) ;
#34328=EDGE_CURVE ( 'NONE', #44609, #33108, #65157, .T. ) ;
#34333=CYLINDRICAL_SURFACE ( 'NONE', #50862, 0.5000000000000000000 ) ;
#34335=EDGE_CURVE ( 'NONE', #23161, #20703, #50321, .T. ) ;
#34338=CARTESIAN_POINT ( 'NONE',  ( -15.98999599679679839, 147.4999999999999716, -9.500000000000000000 ) ) ;
#34340=FILL_AREA_STYLE_COLOUR ( '', #35298 ) ;
#34343=FILL_AREA_STYLE ('',( #45635 ) ) ;
#34344=CARTESIAN_POINT ( 'NONE',  ( -75.48275862068965125, 36.00832590023089352, -9.500000000000001776 ) ) ;
#34346=DIRECTION ( 'NONE',  ( 0.000000000000000000, 0.000000000000000000, 1.000000000000000000 ) ) ;
#34347=CARTESIAN_POINT ( 'NONE',  ( -3.094860106618434248, 113.7949999999999875, 9.525000000000000355 ) ) ;
#34350=CARTESIAN_POINT ( 'NONE',  ( -74.50000000000001421, 1.735173206890468129E-14, 9.500000000000000000 ) ) ;
#34354=DIRECTION ( 'NONE',  ( 1.000000000000000000, 0.000000000000000000, 0.000000000000000000 ) ) ;
#34360=DIRECTION ( 'NONE',  ( -1.000000000000000000, 0.000000000000000000, 0.000000000000000000 ) ) ;
#34367=DIRECTION ( 'NONE',  ( 1.000000000000000000, 8.881784197001252323E-16, 0.000000000000000000 ) ) ;
#34368=FACE_BOUND ( 'NONE', #47440, .T. ) ;
#34374=CARTESIAN_POINT ( 'NONE',  ( -1.166476076187854022E-15, 145.0549999999999784, 9.525000000000000355 ) ) ;
#34382=DIRECTION ( 'NONE',  ( 7.080503983578803083E-17, 1.000000000000000000, -0.000000000000000000 ) ) ;
#34388=FILL_AREA_STYLE_COLOUR ( '', #44305 ) ;
#34390=COLOUR_RGB ( '', 0.09019608, 0.27058824, 0.51372549) ;
#34393=LINE ( 'NONE', #29081, #38656 ) ;
#34396=ORIENTED_EDGE ( 'NONE', *, *, #31606, .T. ) ;
#34397=AXIS2_PLACEMENT_3D ( 'NONE', #49931, #38369, #23508 ) ;
#34398=VERTEX_POINT ( 'NONE', #57675 ) ;
#34399=CARTESIAN_POINT ( 'NONE',  ( 0.000000000000000000, 113.5549999999999926, -9.525000000000000355 ) ) ;
#34400=CARTESIAN_POINT ( 'NONE',  ( -20.12916642283592950, 109.9999999999999858, 10.05319148936170137 ) ) ;
#34407=CARTESIAN_POINT ( 'NONE',  ( -74.08452722063037754, 9.430195807687216103, -6.000000000000000000 ) ) ;
#34408=( LENGTH_UNIT ( ) NAMED_UNIT ( * ) SI_UNIT ( .MILLI., .METRE. ) );
#34411=CARTESIAN_POINT ( 'NONE',  ( -4.716976649647097730, 144.2429263765338305, -6.492361379858953896 ) ) ;
#34415=CARTESIAN_POINT ( 'NONE',  ( -44.99999999999977973, 146.9999999999999716, -9.500000000000000000 ) ) ;
#34418=EDGE_LOOP ( 'NONE', ( #65460, #31224, #69468, #32658, #43243 ) ) ;
#34419=CARTESIAN_POINT ( 'NONE',  ( 0.000000000000000000, 154.9999999999999716, 0.000000000000000000 ) ) ;
#34420=CARTESIAN_POINT ( 'NONE',  ( -20.57648123223228609, 114.5810881445910070, 10.27659574468085246 ) ) ;
#34421=CARTESIAN_POINT ( 'NONE',  ( -44.99999999999998579, 119.9999999999999716, 10.00000000000000000 ) ) ;
#34426=ORIENTED_EDGE ( 'NONE', *, *, #38670, .F. ) ;
#34429=CARTESIAN_POINT ( 'NONE',  ( -45.00000000000000000, 9.519990751839808141, -6.451194676399504502 ) ) ;
#34430=VERTEX_POINT ( 'NONE', #3823 ) ;
#34431=ORIENTED_EDGE ( 'NONE', *, *, #5614, .T. ) ;
#34432=LINE ( 'NONE', #40094, #48610 ) ;
#34433=DIRECTION ( 'NONE',  ( 0.000000000000000000, 0.000000000000000000, 1.000000000000000000 ) ) ;
#34440=CARTESIAN_POINT ( 'NONE',  ( -34.99999999999992895, 113.4999999999999858, -7.000000000000000000 ) ) ;
#34441=CARTESIAN_POINT ( 'NONE',  ( 0.000000000000000000, 130.0570736234661524, -8.025000000000000355 ) ) ;
#34442=PRESENTATION_STYLE_ASSIGNMENT (( #28804 ) ) ;
#34443=EDGE_LOOP ( 'NONE', ( #24802, #56121, #33819, #56101 ) ) ;
#34445=CARTESIAN_POINT ( 'NONE',  ( 6.826472737025121695, 117.6070736234661638, -4.959722759717905660 ) ) ;
#34447=CARTESIAN_POINT ( 'NONE',  ( -54.50000000000002132, -1.956686671034893189E-14, -12.00000000000000000 ) ) ;
#34451=CARTESIAN_POINT ( 'NONE',  ( 8.102448949553183510, 116.1049999999999756, -5.886773742842746238 ) ) ;
#34454=EDGE_CURVE ( 'NONE', #28212, #40785, #57281, .T. ) ;
#34457=( NAMED_UNIT ( * ) SI_UNIT ( $, .STERADIAN. ) SOLID_ANGLE_UNIT ( ) );
#34459=PRESENTATION_STYLE_ASSIGNMENT (( #34115 ) ) ;
#34460=ORIENTED_EDGE ( 'NONE', *, *, #16638, .F. ) ;
#34461=EDGE_CURVE ( 'NONE', #36214, #67765, #61528, .T. ) ;
#34467=DIRECTION ( 'NONE',  ( 0.000000000000000000, 1.000000000000000000, -0.000000000000000000 ) ) ;
#34468=FACE_OUTER_BOUND ( 'NONE', #41389, .T. ) ;
#34470=ORIENTED_EDGE ( 'NONE', *, *, #4330, .F. ) ;
#34471=VERTEX_POINT ( 'NONE', #25637 ) ;
#34473=CYLINDRICAL_SURFACE ( 'NONE', #43217, 0.5000000000000004441 ) ;
#34475=( NAMED_UNIT ( * ) PLANE_ANGLE_UNIT ( ) SI_UNIT ( $, .RADIAN. ) );
#34479=EDGE_CURVE ( 'NONE', #34864, #23185, #34816, .T. ) ;
#34485=( NAMED_UNIT ( * ) PLANE_ANGLE_UNIT ( ) SI_UNIT ( $, .RADIAN. ) );
#34486=ORIENTED_EDGE ( 'NONE', *, *, #37221, .F. ) ;
#34489=CARTESIAN_POINT ( 'NONE',  ( 0.000000000000000000, 142.4449999999999932, -9.525000000000000355 ) ) ;
#34490=( NAMED_UNIT ( * ) PLANE_ANGLE_UNIT ( ) SI_UNIT ( $, .RADIAN. ) );
#34493=CARTESIAN_POINT ( 'NONE',  ( 3.094860106618431583, 142.2049999999999557, 9.525000000000000355 ) ) ;
#34497=ORIENTED_EDGE ( 'NONE', *, *, #23142, .T. ) ;
#34498=CARTESIAN_POINT ( 'NONE',  ( -8.102448949553181734, 159.6050000000000182, 5.886773742842747126 ) ) ;
#34502=DIRECTION ( 'NONE',  ( 0.000000000000000000, 1.000000000000000000, -0.000000000000000000 ) ) ;
#34505=( LENGTH_UNIT ( ) NAMED_UNIT ( * ) SI_UNIT ( .MILLI., .METRE. ) );
#34508=FACE_BOUND ( 'NONE', #69320, .T. ) ;
#34511=ORIENTED_EDGE ( 'NONE', *, *, #59710, .T. ) ;
#34512=ADVANCED_FACE ( 'NONE', ( #8096 ), #35868, .T. ) ;
#34513=DIRECTION ( 'NONE',  ( 1.000000000000000000, 0.000000000000000000, 0.000000000000000000 ) ) ;
#34514=CARTESIAN_POINT ( 'NONE',  ( -15.48999599679679662, 146.9999999999999716, 9.500000000000000000 ) ) ;
#34515=CARTESIAN_POINT ( 'NONE',  ( 45.00000000000000000, 10.58011009419028881, -6.521986687992749943 ) ) ;
#34517=VERTEX_POINT ( 'NONE', #48190 ) ;
#34521=ORIENTED_EDGE ( 'NONE', *, *, #42798, .T. ) ;
#34525=CARTESIAN_POINT ( 'NONE',  ( -75.00000000000000000, 7.768687147774687496, -6.500000000000000888 ) ) ;
#34530=CARTESIAN_POINT ( 'NONE',  ( 0.000000000000000000, 136.4449999999999932, -9.525000000000000355 ) ) ;
#34532=EDGE_CURVE ( 'NONE', #44642, #49404, #42924, .T. ) ;
#34533=CARTESIAN_POINT ( 'NONE',  ( 54.50000000000002132, 1.797044900979284448E-15, -12.00000000000000000 ) ) ;
#34541=EDGE_CURVE ( 'NONE', #66756, #5601, #39391, .T. ) ;
#34545=ORIENTED_EDGE ( 'NONE', *, *, #67393, .T. ) ;
#34548=ADVANCED_FACE ( 'NONE', ( #58707 ), #48538, .F. ) ;
#34549=SURFACE_STYLE_USAGE ( .BOTH. , #30289 ) ;
#34552=CARTESIAN_POINT ( 'NONE',  ( 2.607480562269118174, 147.9070736234661467, -8.024999999999970157 ) ) ;
#34555=CARTESIAN_POINT ( 'NONE',  ( -6.826472737025120807, 142.5070736234661410, -4.959722759717907437 ) ) ;
#34556=EDGE_CURVE ( 'NONE', #69397, #43530, #46120, .T. ) ;
#34557=ORIENTED_EDGE ( 'NONE', *, *, #58090, .F. ) ;
#34559=ORIENTED_EDGE ( 'NONE', *, *, #69029, .F. ) ;
#34560=CARTESIAN_POINT ( 'NONE',  ( -19.89974874213240597, 115.4999999999999574, -10.00000000000000000 ) ) ;
#34562=( NAMED_UNIT ( * ) PLANE_ANGLE_UNIT ( ) SI_UNIT ( $, .RADIAN. ) );
#34564=CARTESIAN_POINT ( 'NONE',  ( 0.000000000000000000, 112.4449999999999932, -9.525000000000000355 ) ) ;
#34565=VERTEX_POINT ( 'NONE', #17871 ) ;
#34566=DIRECTION ( 'NONE',  ( 1.156482317317873451E-16, -1.000000000000000000, -0.000000000000000000 ) ) ;
#34569=CARTESIAN_POINT ( 'NONE',  ( 8.102448949553183510, 128.1049999999999898, -5.886773742842746238 ) ) ;
#34571=( LENGTH_UNIT ( ) NAMED_UNIT ( * ) SI_UNIT ( .MILLI., .METRE. ) );
#34572=CARTESIAN_POINT ( 'NONE',  ( 20.56347600517836938, 115.3187862480272372, 10.00000000000000000 ) ) ;
#34573=CARTESIAN_POINT ( 'NONE',  ( 71.50000000000000000, 35.92875272052971525, -7.500000000000000000 ) ) ;
#34575=FACE_OUTER_BOUND ( 'NONE', #30844, .T. ) ;
#34577=ORIENTED_EDGE ( 'NONE', *, *, #18955, .F. ) ;
#34579=CARTESIAN_POINT ( 'NONE',  ( -69.99999999999998579, 50.00000000000000000, -12.00000000000000000 ) ) ;
#34581=LINE ( 'NONE', #66613, #27399 ) ;
#34586=ORIENTED_EDGE ( 'NONE', *, *, #36440, .F. ) ;
#34587=MECHANICAL_DESIGN_GEOMETRIC_PRESENTATION_REPRESENTATION('',(#39104),#60392);
#34589=CARTESIAN_POINT ( 'NONE',  ( -75.00000000000000000, 8.700918745341546412, 5.871692373102170848 ) ) ;
#34591=EDGE_LOOP ( 'NONE', ( #10265, #9860, #2075, #47107 ) ) ;
#34593=FACE_OUTER_BOUND ( 'NONE', #49247, .T. ) ;
#34595=AXIS2_PLACEMENT_3D ( 'NONE', #10077, #57565, #52319 ) ;
#34597=SURFACE_STYLE_USAGE ( .BOTH. , #13142 ) ;
#34598=CARTESIAN_POINT ( 'NONE',  ( -1.166476076187854022E-15, 143.9449999999999932, 9.525000000000000355 ) ) ;
#34602=CARTESIAN_POINT ( 'NONE',  ( 4.716976649647096842, 119.8570736234661638, 6.492361379858953896 ) ) ;
#34607=CARTESIAN_POINT ( 'NONE',  ( -8.102448949553181734, 113.4949999999999619, 5.886773742842747126 ) ) ;
#34609=ADVANCED_FACE ( 'NONE', ( #39356 ), #5639, .F. ) ;
#34613=ADVANCED_FACE ( 'NONE', ( #55133 ), #18213, .F. ) ;
#34627=DIRECTION ( 'NONE',  ( 1.000000000000000000, 0.000000000000000000, 0.000000000000000000 ) ) ;
#34628=DIRECTION ( 'NONE',  ( 1.000000000000000000, 0.000000000000000000, 0.000000000000000000 ) ) ;
#34631=COLOUR_RGB ( '', 0.08235294, 0.09019608, 0.10196078) ;
#34635=SURFACE_STYLE_FILL_AREA ( #33602 ) ;
#34637=AXIS2_PLACEMENT_3D ( 'NONE', #105, #32897, #54333 ) ;
#34640=DIRECTION ( 'NONE',  ( -0.000000000000000000, 1.000000000000000000, -0.000000000000000000 ) ) ;
#34644=CARTESIAN_POINT ( 'NONE',  ( 4.716976649647099507, 126.7570736234661695, -6.492361379858953008 ) ) ;
#34650=DIRECTION ( 'NONE',  ( 1.000000000000000000, -0.000000000000000000, 0.000000000000000000 ) ) ;
#34654=ORIENTED_EDGE ( 'NONE', *, *, #56396, .T. ) ;
#34655=EDGE_CURVE ( 'NONE', #67791, #38837, #4012, .T. ) ;
#34658=AXIS2_PLACEMENT_3D ( 'NONE', #5276, #37359, #10240 ) ;
#34663=CONICAL_SURFACE ( 'NONE', #896, 5.500000000000005329, 0.7853981633974309595 ) ;
#34665=VERTEX_POINT ( 'NONE', #42074 ) ;
#34666=FACE_OUTER_BOUND ( 'NONE', #33317, .T. ) ;
#34668=( GEOMETRIC_REPRESENTATION_CONTEXT ( 3 ) GLOBAL_UNCERTAINTY_ASSIGNED_CONTEXT ( ( #52600 ) ) GLOBAL_UNIT_ASSIGNED_CONTEXT ( ( #22081, #44621, #43581 ) ) REPRESENTATION_CONTEXT ( 'NONE', 'WORKASPACE' ) );
#34670=DIRECTION ( 'NONE',  ( 1.000000000000000000, 0.000000000000000000, 0.000000000000000000 ) ) ;
#34675=CARTESIAN_POINT ( 'NONE',  ( 8.102448949553179958, 117.3949999999999818, 5.886773742842750679 ) ) ;
#34676=COLOUR_RGB ( '', 0.40784314, 0.44705882, 0.49803922) ;
#34677=( BOUNDED_SURFACE ( )  B_SPLINE_SURFACE ( 3, 2, ( 
 ( #38021, #38378, #630 ),
 ( #53798, #64368, #22150 ),
 ( #27736, #59409, #32344 ),
 ( #69312, #16217, #26381 ),
 ( #43646, #5600, #27046 ),
 ( #11242, #280, #65039 ),
 ( #944, #11589, #4928 ),
 ( #33061, #48227, #6306 ) ),
 .UNSPECIFIED., .F., .F., .F. ) 
 B_SPLINE_SURFACE_WITH_KNOTS ( ( 4, 2, 2, 4 ),
 ( 3, 3 ),
 ( 0.0005765750791842491792, 0.001029553238931483865, 0.001482531398678718334, 0.002388487718173187488 ),
 ( 0.000000000000000000, 1.000000000000000000 ),
 .UNSPECIFIED. ) 
 GEOMETRIC_REPRESENTATION_ITEM ( )  RATIONAL_B_SPLINE_SURFACE ( (
 ( 1.000000000000000000, 0.8885233166386380388, 1.000000000000000000),
 ( 1.000000000000000000, 0.8885760224879465374, 1.000000000000000000),
 ( 1.000000000000000000, 0.8838232350071849597, 1.000000000000000000),
 ( 1.000000000000000000, 0.8662144792540281690, 1.000000000000000000),
 ( 1.000000000000000000, 0.8532605865699290915, 1.000000000000000000),
 ( 1.000000000000000000, 0.8046051514202448018, 1.000000000000000000),
 ( 1.000000000000000000, 0.7601637718248979159, 1.000000000000000000),
 ( 1.000000000000000000, 0.7071067811865546782, 1.000000000000000000) ) ) 
 REPRESENTATION_ITEM ( '' )  SURFACE ( )  );
#34679=SURFACE_STYLE_FILL_AREA ( #44607 ) ;
#34683=CARTESIAN_POINT ( 'NONE',  ( 44.91886116991580735, 9.999999999999980460, -3.201362207699240514 ) ) ;
#34687=( NAMED_UNIT ( * ) PLANE_ANGLE_UNIT ( ) SI_UNIT ( $, .RADIAN. ) );
#34690=CIRCLE ( 'NONE', #5449, 0.5000000000000004441 ) ;
#34693=ADVANCED_FACE ( 'NONE', ( #47338 ), #1728, .F. ) ;
#34701=CARTESIAN_POINT ( 'NONE',  ( -3.094860106618432471, 149.7049999999999272, -9.525000000000000355 ) ) ;
#34706=( NAMED_UNIT ( * ) SI_UNIT ( $, .STERADIAN. ) SOLID_ANGLE_UNIT ( ) );
#34707=EDGE_CURVE ( 'NONE', #33857, #16450, #50658, .T. ) ;
#34711=CARTESIAN_POINT ( 'NONE',  ( -9.827790563157511022E-16, 116.5570736234661666, 8.025000000000000355 ) ) ;
#34712=ORIENTED_EDGE ( 'NONE', *, *, #52356, .T. ) ;
#34713=AXIS2_PLACEMENT_3D ( 'NONE', #2314, #50931, #23840 ) ;
#34716=AXIS2_PLACEMENT_3D ( 'NONE', #63197, #30120, #68138 ) ;
#34718=CARTESIAN_POINT ( 'NONE',  ( -44.99999999999999289, 9.585601099689366578, 6.373959028214387423 ) ) ;
#34724=EDGE_LOOP ( 'NONE', ( #32977, #52379, #2537, #28525 ) ) ;
#34726=ORIENTED_EDGE ( 'NONE', *, *, #9867, .T. ) ;
#34728=B_SPLINE_CURVE_WITH_KNOTS ( 'NONE', 3,
 ( #48805, #22369, #44572, #1888, #23077, #60000 ),
 .UNSPECIFIED., .F., .F.,
 ( 4, 2, 4 ),
 ( 0.000000000000000000, 0.0004110251708232767233, 0.0008220503416465534466 ),
 .UNSPECIFIED. ) ;
#34732=VECTOR ( 'NONE', #2991, 1000.000000000000000 ) ;
#34733=ADVANCED_FACE ( 'NONE', ( #52334 ), #47708, .F. ) ;
#34734=EDGE_LOOP ( 'NONE', ( #46734, #37158, #29638, #29320 ) ) ;
#34736=CARTESIAN_POINT ( 'NONE',  ( -1.751052283315748914, 110.4999999999999432, -9.372962259333457169 ) ) ;
#34738=FACE_OUTER_BOUND ( 'NONE', #45512, .T. ) ;
#34740=CARTESIAN_POINT ( 'NONE',  ( -4.716976649647098618, 142.1429263765338078, 6.492361379858953008 ) ) ;
#34741=( NAMED_UNIT ( * ) PLANE_ANGLE_UNIT ( ) SI_UNIT ( $, .RADIAN. ) );
#34742=( NAMED_UNIT ( * ) SI_UNIT ( $, .STERADIAN. ) SOLID_ANGLE_UNIT ( ) );
#34746=LINE ( 'NONE', #45366, #54257 ) ;
#34749=CARTESIAN_POINT ( 'NONE',  ( 74.49999999999998579, 119.9999999999997584, 10.00000000000000000 ) ) ;
#34751=DIRECTION ( 'NONE',  ( 1.000000000000000000, 0.000000000000000000, 0.000000000000000000 ) ) ;
#34756=FILL_AREA_STYLE_COLOUR ( '', #31634 ) ;
#34758=FACE_OUTER_BOUND ( 'NONE', #65184, .T. ) ;
#34762=CYLINDRICAL_SURFACE ( 'NONE', #69667, 0.5000000000000004441 ) ;
#34765=AXIS2_PLACEMENT_3D ( 'NONE', #46614, #46955, #20152 ) ;
#34769=FACE_OUTER_BOUND ( 'NONE', #2913, .T. ) ;
#34779=CARTESIAN_POINT ( 'NONE',  ( -74.99999999999998579, 50.00000000000000000, -41.30495168499704306 ) ) ;
#34780=MECHANICAL_DESIGN_GEOMETRIC_PRESENTATION_REPRESENTATION('',(#65100),#13436);
#34784=CARTESIAN_POINT ( 'NONE',  ( 71.50000000000000000, 14.49137674618942562, 9.500000000000000000 ) ) ;
#34785=AXIS2_PLACEMENT_3D ( 'NONE', #25434, #3586, #67657 ) ;
#34790=ADVANCED_FACE ( 'NONE', ( #42485 ), #16447, .F. ) ;
#34792=CARTESIAN_POINT ( 'NONE',  ( -5.598654528085808657, 114.7549999999999812, 7.705886871421373741 ) ) ;
#34798=SURFACE_SIDE_STYLE ('',( #33762 ) ) ;
#34801=EDGE_CURVE ( 'NONE', #54030, #15520, #34728, .T. ) ;
#34804=VECTOR ( 'NONE', #11610, 1000.000000000000000 ) ;
#34807=CARTESIAN_POINT ( 'NONE',  ( 48.50000000000000000, 14.49137674618942562, -9.500000000000000000 ) ) ;
#34810=VECTOR ( 'NONE', #60290, 1000.000000000000000 ) ;
#34811=COLOUR_RGB ( '', 0.40784314, 0.44705882, 0.49803922) ;
#34813=DIRECTION ( 'NONE',  ( -1.000000000000000000, 0.000000000000000000, 0.000000000000000000 ) ) ;
#34814=CIRCLE ( 'NONE', #60611, 0.5000000000000004441 ) ;
#34815=CYLINDRICAL_SURFACE ( 'NONE', #66406, 0.5000000000000004441 ) ;
#34816=LINE ( 'NONE', #56270, #12375 ) ;
#34824=( NAMED_UNIT ( * ) SI_UNIT ( $, .STERADIAN. ) SOLID_ANGLE_UNIT ( ) );
#34830=CARTESIAN_POINT ( 'NONE',  ( 8.102448949553183510, 144.9950000000000045, -5.886773742842746238 ) ) ;
#34833=CARTESIAN_POINT ( 'NONE',  ( -74.50000000000000000, -1.856352308976905642E-14, -6.999999999999999112 ) ) ;
#34834=CARTESIAN_POINT ( 'NONE',  ( -10.01517768586949408, 141.3050000000000068, -6.132527647946036459E-16 ) ) ;
#34836=CIRCLE ( 'NONE', #42781, 0.5000000000000004441 ) ;
#34837=DIRECTION ( 'NONE',  ( -0.000000000000000000, -0.000000000000000000, -1.000000000000000000 ) ) ;
#34839=CARTESIAN_POINT ( 'NONE',  ( 2.607480562269071989, 115.5929263765337964, 8.025000000000002132 ) ) ;
#34841=UNCERTAINTY_MEASURE_WITH_UNIT (LENGTH_MEASURE( 1.000000000000000082E-05 ), #5003, 'distance_accuracy_value', 'NONE');
#34858=DIRECTION ( 'NONE',  ( 0.000000000000000000, 0.000000000000000000, -1.000000000000000000 ) ) ;
#34860=FACE_OUTER_BOUND ( 'NONE', #30881, .T. ) ;
#34861=VERTEX_POINT ( 'NONE', #33613 ) ;
#34862=CIRCLE ( 'NONE', #4512, 0.4999999999999994449 ) ;
#34863=ADVANCED_FACE ( 'NONE', ( #12852 ), #27956, .T. ) ;
#34864=VERTEX_POINT ( 'NONE', #1192 ) ;
#34871=EDGE_CURVE ( 'NONE', #23185, #2421, #66312, .T. ) ;
#34872=STYLED_ITEM ( 'NONE', ( #30909 ), #59600 ) ;
#34880=EDGE_CURVE ( 'NONE', #5601, #54750, #41758, .T. ) ;
#34881=CARTESIAN_POINT ( 'NONE',  ( 8.102448949553183510, 141.9950000000000045, -5.886773742842746238 ) ) ;
#34886=DIRECTION ( 'NONE',  ( -0.7071067811865352493, 0.000000000000000000, -0.7071067811865597852 ) ) ;
#34887=COLOUR_RGB ( '', 0.09019608, 0.27058824, 0.51372549) ;
#34888=UNCERTAINTY_MEASURE_WITH_UNIT (LENGTH_MEASURE( 1.000000000000000082E-05 ), #21575, 'distance_accuracy_value', 'NONE');
#34891=CIRCLE ( 'NONE', #53957, 0.5000000000000004441 ) ;
#34895=TOROIDAL_SURFACE ( 'NONE', #24782, 10.50000000000000533, 0.5000000000000000000 ) ;
#34898=ORIENTED_EDGE ( 'NONE', *, *, #68149, .F. ) ;
#34901=EDGE_CURVE ( 'NONE', #41057, #24214, #1555, .T. ) ;
#34904=SURFACE_STYLE_FILL_AREA ( #28910 ) ;
#34909=ORIENTED_EDGE ( 'NONE', *, *, #1051, .T. ) ;
#34911=ORIENTED_EDGE ( 'NONE', *, *, #9666, .F. ) ;
#34912=CARTESIAN_POINT ( 'NONE',  ( 6.422934014168398598, 153.0000000000000000, 4.811085495980990778 ) ) ;
#34913=DIRECTION ( 'NONE',  ( 1.000000000000000000, 1.387778780781444571E-14, -0.000000000000000000 ) ) ;
#34914=ORIENTED_EDGE ( 'NONE', *, *, #54271, .F. ) ;
#34915=AXIS2_PLACEMENT_3D ( 'NONE', #36927, #10851, #572 ) ;
#34917=DIRECTION ( 'NONE',  ( 0.000000000000000000, 0.000000000000000000, 1.000000000000000000 ) ) ;
#34918=CARTESIAN_POINT ( 'NONE',  ( 8.102448949553183510, 114.9949999999999903, -5.886773742842746238 ) ) ;
#34920=STYLED_ITEM ( 'NONE', ( #3194 ), #45092 ) ;
#34922=LINE ( 'NONE', #39540, #45168 ) ;
#34923=AXIS2_PLACEMENT_3D ( 'NONE', #48602, #68635, #9566 ) ;
#34925=DIRECTION ( 'NONE',  ( 0.000000000000000000, 0.000000000000000000, 1.000000000000000000 ) ) ;
#34926=CARTESIAN_POINT ( 'NONE',  ( 3.094860106618435136, 137.4050000000000296, -9.525000000000000355 ) ) ;
#34927=UNCERTAINTY_MEASURE_WITH_UNIT (LENGTH_MEASURE( 1.000000000000000082E-05 ), #38990, 'distance_accuracy_value', 'NONE');
#34928=CYLINDRICAL_SURFACE ( 'NONE', #3734, 0.5000000000000004441 ) ;
#34933=COLOUR_RGB ( '', 0.09019608, 0.27058824, 0.51372549) ;
#34934=CYLINDRICAL_SURFACE ( 'NONE', #14931, 0.5000000000000004441 ) ;
#34936=SURFACE_SIDE_STYLE ('',( #14186 ) ) ;
#34938=COLOUR_RGB ( '', 0.31764706, 0.68627451, 0.89019608) ;
#34939=EDGE_LOOP ( 'NONE', ( #34176, #55516, #50782, #30395 ) ) ;
#34948=FILL_AREA_STYLE_COLOUR ( '', #26531 ) ;
#34951=( LENGTH_UNIT ( ) NAMED_UNIT ( * ) SI_UNIT ( .MILLI., .METRE. ) );
#34952=EDGE_CURVE ( 'NONE', #10613, #37052, #51895, .T. ) ;
#34954=ORIENTED_EDGE ( 'NONE', *, *, #29056, .F. ) ;
#34955=CARTESIAN_POINT ( 'NONE',  ( 0.000000000000000000, 109.9999999999999858, -9.525000000000000355 ) ) ;
#34957=CYLINDRICAL_SURFACE ( 'NONE', #64257, 0.5000000000000004441 ) ;
#34958=AXIS2_PLACEMENT_3D ( 'NONE', #62487, #14306, #35769 ) ;
#34959=CARTESIAN_POINT ( 'NONE',  ( 0.000000000000000000, 139.4449999999999932, -9.525000000000000355 ) ) ;
#34965=CYLINDRICAL_SURFACE ( 'NONE', #27881, 13.99999999999999822 ) ;
#34968=FILL_AREA_STYLE ('',( #8932 ) ) ;
#34969=PRESENTATION_STYLE_ASSIGNMENT (( #51491 ) ) ;
#34977=PRESENTATION_STYLE_ASSIGNMENT (( #3260 ) ) ;
#34979=( BOUNDED_CURVE ( )  B_SPLINE_CURVE ( 2, ( #47718, #41710, #63134, #58547, #14972, #31449, #10709, #36455, #20568, #26527, #9697 ),
 .UNSPECIFIED., .F., .F. ) 
 B_SPLINE_CURVE_WITH_KNOTS ( ( 3, 2, 2, 2, 2, 3 ),
 ( 0.6176470588235297710, 0.6235294117647062206, 0.6294117647058826703, 0.6352941176470590090, 0.6411764705882355697, 0.6470588235294120194 ),
 .UNSPECIFIED. ) 
 CURVE ( )  GEOMETRIC_REPRESENTATION_ITEM ( )  RATIONAL_B_SPLINE_CURVE ( ( 0.9999999999999972244, 0.9510565162951563067, 1.000000000000000000, 0.9510565162951535312, 1.000000000000000000, 0.9510565162951535312, 1.000000000000000000, 0.9510565162951535312, 1.000000000000000000, 0.9510565162951516438, 1.000000000000001776 ) ) 
 REPRESENTATION_ITEM ( '' )  );
#34984=TOROIDAL_SURFACE ( 'NONE', #4648, 1.000000000000000000, 0.5000000000000000000 ) ;
#34985=DIRECTION ( 'NONE',  ( 0.000000000000000000, -1.000000000000000000, 0.000000000000000000 ) ) ;
#34987=ORIENTED_EDGE ( 'NONE', *, *, #3056, .T. ) ;
#34991=DIRECTION ( 'NONE',  ( -0.000000000000000000, 1.000000000000000000, 0.000000000000000000 ) ) ;
#34995=DIRECTION ( 'NONE',  ( 0.000000000000000000, 1.000000000000000000, 0.000000000000000000 ) ) ;
#34996=ORIENTED_EDGE ( 'NONE', *, *, #51635, .F. ) ;
#34998=DIRECTION ( 'NONE',  ( -0.9994052928406508274, -0.03448275862069643399, -0.000000000000000000 ) ) ;
#35001=EDGE_LOOP ( 'NONE', ( #39114, #66434, #57482, #11059 ) ) ;
#35004=CARTESIAN_POINT ( 'NONE',  ( 2.607480562269071989, 137.7070736234661013, 8.025000000000002132 ) ) ;
#35008=CARTESIAN_POINT ( 'NONE',  ( 34.99999999999992895, 113.4999999999999858, -7.000000000000000000 ) ) ;
#35009=DIRECTION ( 'NONE',  ( -1.000000000000000000, 0.000000000000000000, 0.000000000000000000 ) ) ;
#35011=SURFACE_SIDE_STYLE ('',( #33965 ) ) ;
#35013=MECHANICAL_DESIGN_GEOMETRIC_PRESENTATION_REPRESENTATION('',(#53004),#33904);
#35019=MECHANICAL_DESIGN_GEOMETRIC_PRESENTATION_REPRESENTATION('',(#41788),#13730);
#35026=ADVANCED_FACE ( 'NONE', ( #35712 ), #47390, .F. ) ;
#35027=VERTEX_POINT ( 'NONE', #56821 ) ;
#35031=PRESENTATION_STYLE_ASSIGNMENT (( #17823 ) ) ;
#35032=FACE_OUTER_BOUND ( 'NONE', #5061, .T. ) ;
#35036=CARTESIAN_POINT ( 'NONE',  ( -3.094860106618432471, 112.5949999999999847, -9.525000000000000355 ) ) ;
#35039=PRESENTATION_STYLE_ASSIGNMENT (( #60713 ) ) ;
#35040=EDGE_CURVE ( 'NONE', #57704, #8462, #28215, .T. ) ;
#35044=DIRECTION ( 'NONE',  ( 1.000000000000000000, 0.000000000000000000, 0.000000000000000000 ) ) ;
#35049=SURFACE_STYLE_USAGE ( .BOTH. , #57910 ) ;
#35055=COLOUR_RGB ( '', 0.72549020, 0.75294118, 0.79215686) ;
#35056=CYLINDRICAL_SURFACE ( 'NONE', #6477, 8.000000000000014211 ) ;
#35062=CARTESIAN_POINT ( 'NONE',  ( -9.058813317711337021, 150.1549999999999727, -2.943386871421374895 ) ) ;
#35063=DIRECTION ( 'NONE',  ( -0.000000000000000000, 0.000000000000000000, 1.000000000000000000 ) ) ;
#35066=DIRECTION ( 'NONE',  ( 1.000000000000000000, 0.000000000000000000, 0.000000000000000000 ) ) ;
#35068=VECTOR ( 'NONE', #49270, 1000.000000000000000 ) ;
#35071=( GEOMETRIC_REPRESENTATION_CONTEXT ( 3 ) GLOBAL_UNCERTAINTY_ASSIGNED_CONTEXT ( ( #10376 ) ) GLOBAL_UNIT_ASSIGNED_CONTEXT ( ( #14979, #25156, #5082 ) ) REPRESENTATION_CONTEXT ( 'NONE', 'WORKASPACE' ) );
#35072=( NAMED_UNIT ( * ) PLANE_ANGLE_UNIT ( ) SI_UNIT ( $, .RADIAN. ) );
#35073=CIRCLE ( 'NONE', #49703, 0.5000000000000004441 ) ;
#35074=DIRECTION ( 'NONE',  ( 0.000000000000000000, 0.000000000000000000, 1.000000000000000000 ) ) ;
#35078=( GEOMETRIC_REPRESENTATION_CONTEXT ( 3 ) GLOBAL_UNCERTAINTY_ASSIGNED_CONTEXT ( ( #65828 ) ) GLOBAL_UNIT_ASSIGNED_CONTEXT ( ( #41809, #68866, #52350 ) ) REPRESENTATION_CONTEXT ( 'NONE', 'WORKASPACE' ) );
#35081=DIRECTION ( 'NONE',  ( 0.000000000000000000, 0.000000000000000000, -1.000000000000000000 ) ) ;
#35084=DIRECTION ( 'NONE',  ( 0.000000000000000000, 0.000000000000000000, 1.000000000000000000 ) ) ;
#35086=CARTESIAN_POINT ( 'NONE',  ( -5.598654528085806881, 113.8549999999999898, -7.705886871421374629 ) ) ;
#35087=LINE ( 'NONE', #13988, #42319 ) ;
#35088=ORIENTED_EDGE ( 'NONE', *, *, #51381, .F. ) ;
#35094=ORIENTED_EDGE ( 'NONE', *, *, #45772, .F. ) ;
#35102=ORIENTED_EDGE ( 'NONE', *, *, #53552, .T. ) ;
#35103=CARTESIAN_POINT ( 'NONE',  ( 2.607480562269071989, 145.5929263765338249, 8.025000000000002132 ) ) ;
#35107=DIRECTION ( 'NONE',  ( 0.000000000000000000, 0.000000000000000000, 1.000000000000000000 ) ) ;
#35108=VERTEX_POINT ( 'NONE', #10704 ) ;
#35109=CARTESIAN_POINT ( 'NONE',  ( 48.00000000000000000, 99.99999999999992895, 9.500000000000000000 ) ) ;
#35112=DIRECTION ( 'NONE',  ( -0.000000000000000000, -0.000000000000000000, -1.000000000000000000 ) ) ;
#35114=FACE_OUTER_BOUND ( 'NONE', #25343, .T. ) ;
#35115=FACE_OUTER_BOUND ( 'NONE', #45091, .T. ) ;
#35116=CONICAL_SURFACE ( 'NONE', #21656, 5.000000000000004441, 0.7853981633974579379 ) ;
#35119=ORIENTED_EDGE ( 'NONE', *, *, #35156, .T. ) ;
#35120=FILL_AREA_STYLE_COLOUR ( '', #64687 ) ;
#35122=EDGE_CURVE ( 'NONE', #40785, #34213, #36787, .T. ) ;
#35123=CARTESIAN_POINT ( 'NONE',  ( -74.86954670510183973, 36.13097948458331388, 9.842709678231122084 ) ) ;
#35126=CIRCLE ( 'NONE', #4790, 8.500000000000007105 ) ;
#35127=ORIENTED_EDGE ( 'NONE', *, *, #11278, .F. ) ;
#35129=SURFACE_STYLE_FILL_AREA ( #56224 ) ;
#35135=CARTESIAN_POINT ( 'NONE',  ( -15.48999599679679662, 117.9999999999999716, -9.500000000000000000 ) ) ;
#35139=ORIENTED_EDGE ( 'NONE', *, *, #51054, .F. ) ;
#35140=VECTOR ( 'NONE', #63737, 1000.000000000000000 ) ;
#35145=CARTESIAN_POINT ( 'NONE',  ( 3.021204673494646276, 154.5000000000000568, -9.043681037409140089 ) ) ;
#35146=DIRECTION ( 'NONE',  ( 1.224646799147353207E-16, 1.000000000000000000, -0.000000000000000000 ) ) ;
#35150=CARTESIAN_POINT ( 'NONE',  ( -10.01517768586949231, 120.3049999999999784, -6.132527647946036459E-16 ) ) ;
#35152=MECHANICAL_DESIGN_GEOMETRIC_PRESENTATION_REPRESENTATION('',(#48701),#26148);
#35156=EDGE_CURVE ( 'NONE', #65484, #58922, #43179, .T. ) ;
#35157=TOROIDAL_SURFACE ( 'NONE', #18394, 16.50000000000000000, 0.5000000000000000000 ) ;
#35162=DIRECTION ( 'NONE',  ( 1.000000000000000000, 0.000000000000000000, 0.000000000000000000 ) ) ;
#35174=ORIENTED_EDGE ( 'NONE', *, *, #1440, .F. ) ;
#35186=DIRECTION ( 'NONE',  ( -0.7071067811865549002, 8.659560562355022838E-17, 0.7071067811865401342 ) ) ;
#35187=CARTESIAN_POINT ( 'NONE',  ( -9.058813317711337021, 143.0449999999999875, -2.943386871421374895 ) ) ;
#35188=( GEOMETRIC_REPRESENTATION_CONTEXT ( 3 ) GLOBAL_UNCERTAINTY_ASSIGNED_CONTEXT ( ( #28462 ) ) GLOBAL_UNIT_ASSIGNED_CONTEXT ( ( #2439, #28518, #29209 ) ) REPRESENTATION_CONTEXT ( 'NONE', 'WORKASPACE' ) );
#35191=CARTESIAN_POINT ( 'NONE',  ( 0.000000000000000000, 137.5549999999999784, -9.525000000000000355 ) ) ;
#35194=DIRECTION ( 'NONE',  ( 0.000000000000000000, 0.000000000000000000, 1.000000000000000000 ) ) ;
#35196=CARTESIAN_POINT ( 'NONE',  ( 6.826472737025119919, 115.8929263765338220, 4.959722759717908325 ) ) ;
#35197=LINE ( 'NONE', #24980, #62573 ) ;
#35199=MECHANICAL_DESIGN_GEOMETRIC_PRESENTATION_REPRESENTATION('',(#38606),#10552);
#35202=DIRECTION ( 'NONE',  ( 0.000000000000000000, 0.000000000000000000, 1.000000000000000000 ) ) ;
#35204=LINE ( 'NONE', #30239, #17256 ) ;
#35212=( NAMED_UNIT ( * ) PLANE_ANGLE_UNIT ( ) SI_UNIT ( $, .RADIAN. ) );
#35213=B_SPLINE_CURVE_WITH_KNOTS ( 'NONE', 3,
 ( #33150, #54908, #6736, #5686, #37434, #49324 ),
 .UNSPECIFIED., .F., .F.,
 ( 4, 2, 4 ),
 ( 0.000000000000000000, 0.0003110656624534448192, 0.0006221313249068896383 ),
 .UNSPECIFIED. ) ;
#35214=( GEOMETRIC_REPRESENTATION_CONTEXT ( 3 ) GLOBAL_UNCERTAINTY_ASSIGNED_CONTEXT ( ( #56023 ) ) GLOBAL_UNIT_ASSIGNED_CONTEXT ( ( #14360, #35830, #3781 ) ) REPRESENTATION_CONTEXT ( 'NONE', 'WORKASPACE' ) );
#35215=DIRECTION ( 'NONE',  ( -0.000000000000000000, -1.000000000000000000, -0.000000000000000000 ) ) ;
#35218=( NAMED_UNIT ( * ) SI_UNIT ( $, .STERADIAN. ) SOLID_ANGLE_UNIT ( ) );
#35219=DIRECTION ( 'NONE',  ( 0.000000000000000000, 0.000000000000000000, -1.000000000000000000 ) ) ;
#35222=EDGE_LOOP ( 'NONE', ( #6637, #12670, #56179, #44453 ) ) ;
#35227=AXIS2_PLACEMENT_3D ( 'NONE', #16859, #11204, #6270 ) ;
#35229=AXIS2_PLACEMENT_3D ( 'NONE', #23321, #6443, #27869 ) ;
#35232=ORIENTED_EDGE ( 'NONE', *, *, #66159, .F. ) ;
#35234=CARTESIAN_POINT ( 'NONE',  ( -34.99999999999992895, 109.9999999999999858, 9.500000000000000000 ) ) ;
#35236=AXIS2_PLACEMENT_3D ( 'NONE', #31085, #27174, #411 ) ;
#35237=CARTESIAN_POINT ( 'NONE',  ( 3.094860106618435136, 136.2949999999999875, -9.525000000000000355 ) ) ;
#35241=EDGE_CURVE ( 'NONE', #47060, #58906, #42077, .T. ) ;
#35242=LINE ( 'NONE', #61595, #24491 ) ;
#35249=AXIS2_PLACEMENT_3D ( 'NONE', #12562, #23150, #55488 ) ;
#35250=CYLINDRICAL_SURFACE ( 'NONE', #14615, 0.5000000000000004441 ) ;
#35254=CIRCLE ( 'NONE', #62208, 1.000000000000000000 ) ;
#35257=VECTOR ( 'NONE', #62774, 1000.000000000000000 ) ;
#35260=CARTESIAN_POINT ( 'NONE',  ( -45.00000000000000711, 7.952411872162973516, 6.456960098914690249 ) ) ;
#35262=CARTESIAN_POINT ( 'NONE',  ( -2.607480562268989832, 142.2070736234661297, -8.025000000000060751 ) ) ;
#35269=FILL_AREA_STYLE ('',( #24014 ) ) ;
#35272=COLOUR_RGB ( '', 0.08235294, 0.09019608, 0.10196078) ;
#35273=CARTESIAN_POINT ( 'NONE',  ( 0.000000000000000000, 114.4999999999999574, 22.50000000000000000 ) ) ;
#35274=CARTESIAN_POINT ( 'NONE',  ( 6.826472737025119919, 159.0070736234661695, 4.959722759717908325 ) ) ;
#35275=AXIS2_PLACEMENT_3D ( 'NONE', #3864, #62971, #25348 ) ;
#35277=SURFACE_SIDE_STYLE ('',( #24022 ) ) ;
#35278=CARTESIAN_POINT ( 'NONE',  ( -3.094860106618432471, 113.7049999999999699, -9.525000000000000355 ) ) ;
#35281=SURFACE_SIDE_STYLE ('',( #46576 ) ) ;
#35283=CARTESIAN_POINT ( 'NONE',  ( 0.000000000000000000, 137.5549999999999784, -9.525000000000000355 ) ) ;
#35284=( NAMED_UNIT ( * ) PLANE_ANGLE_UNIT ( ) SI_UNIT ( $, .RADIAN. ) );
#35285=DIRECTION ( 'NONE',  ( 0.000000000000000000, 1.000000000000000000, 0.000000000000000000 ) ) ;
#35286=EDGE_CURVE ( 'NONE', #53126, #19860, #50319, .T. ) ;
#35289=( NAMED_UNIT ( * ) PLANE_ANGLE_UNIT ( ) SI_UNIT ( $, .RADIAN. ) );
#35293=( NAMED_UNIT ( * ) PLANE_ANGLE_UNIT ( ) SI_UNIT ( $, .RADIAN. ) );
#35294=SURFACE_STYLE_USAGE ( .BOTH. , #61313 ) ;
#35296=ORIENTED_EDGE ( 'NONE', *, *, #11718, .T. ) ;
#35298=COLOUR_RGB ( '', 0.66274510, 0.83137255, 0.94901961) ;
#35299=LINE ( 'NONE', #45189, #41411 ) ;
#35300=DIRECTION ( 'NONE',  ( -0.000000000000000000, -0.000000000000000000, -1.000000000000000000 ) ) ;
#35302=ORIENTED_EDGE ( 'NONE', *, *, #50611, .T. ) ;
#35305=STYLED_ITEM ( 'NONE', ( #42330 ), #30399 ) ;
#35308=ORIENTED_EDGE ( 'NONE', *, *, #66953, .T. ) ;
#35309=ADVANCED_FACE ( 'NONE', ( #27188 ), #5794, .F. ) ;
#35311=SURFACE_STYLE_USAGE ( .BOTH. , #40250 ) ;
#35316=CARTESIAN_POINT ( 'NONE',  ( 8.102448949553179958, 141.3949999999999818, 5.886773742842750679 ) ) ;
#35323=CARTESIAN_POINT ( 'NONE',  ( 8.437984349512095861, 120.3070736234661382, 1.550032578732816828E-15 ) ) ;
#35327=CARTESIAN_POINT ( 'NONE',  ( 5.598654528085805993, 111.2449999999999761, 7.705886871421374629 ) ) ;
#35331=DIRECTION ( 'NONE',  ( 0.000000000000000000, 0.000000000000000000, 1.000000000000000000 ) ) ;
#35338=( GEOMETRIC_REPRESENTATION_CONTEXT ( 3 ) GLOBAL_UNCERTAINTY_ASSIGNED_CONTEXT ( ( #51038 ) ) GLOBAL_UNIT_ASSIGNED_CONTEXT ( ( #55225, #22902, #60847 ) ) REPRESENTATION_CONTEXT ( 'NONE', 'WORKASPACE' ) );
#35339=( NAMED_UNIT ( * ) SI_UNIT ( $, .STERADIAN. ) SOLID_ANGLE_UNIT ( ) );
#35340=EDGE_CURVE ( 'NONE', #48195, #30995, #34922, .T. ) ;
#35341=COLOUR_RGB ( '', 0.08235294, 0.09019608, 0.10196078) ;
#35348=DIRECTION ( 'NONE',  ( 1.000000000000000000, 0.000000000000000000, 0.000000000000000000 ) ) ;
#35354=DIRECTION ( 'NONE',  ( 0.000000000000000000, 0.000000000000000000, 1.000000000000000000 ) ) ;
#35355=EDGE_CURVE ( 'NONE', #30255, #1355, #31673, .T. ) ;
#35356=ORIENTED_EDGE ( 'NONE', *, *, #63543, .F. ) ;
#35363=CARTESIAN_POINT ( 'NONE',  ( 4.716976649647096842, 128.8570736234661638, 6.492361379858953896 ) ) ;
#35364=VECTOR ( 'NONE', #1696, 1000.000000000000000 ) ;
#35365=MECHANICAL_DESIGN_GEOMETRIC_PRESENTATION_REPRESENTATION('',(#22919),#1554);
#35366=VERTEX_POINT ( 'NONE', #56370 ) ;
#35367=CARTESIAN_POINT ( 'NONE',  ( 60.00000000000000000, 1.797044900979284448E-15, 6.999999999999988454 ) ) ;
#35369=SURFACE_SIDE_STYLE ('',( #44907 ) ) ;
#35376=CIRCLE ( 'NONE', #5037, 10.50000000000000178 ) ;
#35383=UNCERTAINTY_MEASURE_WITH_UNIT (LENGTH_MEASURE( 1.000000000000000082E-05 ), #51450, 'distance_accuracy_value', 'NONE');
#35387=AXIS2_PLACEMENT_3D ( 'NONE', #4207, #14817, #4572 ) ;
#35388=CARTESIAN_POINT ( 'NONE',  ( 44.99999999999998579, 119.9999999999999716, -9.500000000000000000 ) ) ;
#35390=FACE_OUTER_BOUND ( 'NONE', #17065, .T. ) ;
#35391=EDGE_LOOP ( 'NONE', ( #5691, #22617, #32692, #13914 ) ) ;
#35394=CARTESIAN_POINT ( 'NONE',  ( -41.49999999999998579, 106.9282032302754999, -3.500000000000000000 ) ) ;
#35398=CARTESIAN_POINT ( 'NONE',  ( -5.598654528085808657, 116.6449999999999818, 7.705886871421373741 ) ) ;
#35399=( GEOMETRIC_REPRESENTATION_CONTEXT ( 3 ) GLOBAL_UNCERTAINTY_ASSIGNED_CONTEXT ( ( #39778 ) ) GLOBAL_UNIT_ASSIGNED_CONTEXT ( ( #12068, #22994, #65894 ) ) REPRESENTATION_CONTEXT ( 'NONE', 'WORKASPACE' ) );
#35404=( BOUNDED_CURVE ( )  B_SPLINE_CURVE ( 2, ( #5533, #15794, #54086, #59347, #33339, #44289, #37973, #10509, #10845, #27337, #49529 ),
 .UNSPECIFIED., .F., .F. ) 
 B_SPLINE_CURVE_WITH_KNOTS ( ( 3, 2, 2, 2, 2, 3 ),
 ( 0.2941176470588235392, 0.2999999999999999889, 0.3058823529411764941, 0.3117647058823529438, 0.3176470588235293935, 0.3235294117647058987 ),
 .UNSPECIFIED. ) 
 CURVE ( )  GEOMETRIC_REPRESENTATION_ITEM ( )  RATIONAL_B_SPLINE_CURVE ( ( 1.000000000000000000, 0.9510565162951535312, 1.000000000000000000, 0.9510565162951535312, 1.000000000000000000, 0.9510565162951535312, 1.000000000000000000, 0.9510565162951535312, 1.000000000000000000, 0.9510565162951535312, 1.000000000000000000 ) ) 
 REPRESENTATION_ITEM ( '' )  );
#35405=SURFACE_STYLE_USAGE ( .BOTH. , #52632 ) ;
#35408=FILL_AREA_STYLE ('',( #3331 ) ) ;
#35411=CARTESIAN_POINT ( 'NONE',  ( -7.971148328998627797, 111.3190071099407845, -3.524084523217378973 ) ) ;
#35417=CIRCLE ( 'NONE', #16359, 0.5000000000000004441 ) ;
#35419=FACE_OUTER_BOUND ( 'NONE', #5266, .T. ) ;
#35423=COLOUR_RGB ( '', 0.09019608, 0.27058824, 0.51372549) ;
#35425=CARTESIAN_POINT ( 'NONE',  ( -9.058813317711337021, 153.1549999999999727, -2.943386871421374895 ) ) ;
#35427=EDGE_CURVE ( 'NONE', #6580, #38434, #10350, .T. ) ;
#35430=CARTESIAN_POINT ( 'NONE',  ( 24.21231517720798010, 113.4999999999999858, -7.500000000000000000 ) ) ;
#35431=UNCERTAINTY_MEASURE_WITH_UNIT (LENGTH_MEASURE( 1.000000000000000082E-05 ), #35504, 'distance_accuracy_value', 'NONE');
#35435=AXIS2_PLACEMENT_3D ( 'NONE', #17718, #66222, #2129 ) ;
#35437=EDGE_CURVE ( 'NONE', #65858, #22750, #52190, .T. ) ;
#35438=ADVANCED_FACE ( 'NONE', ( #16191 ), #8075, .T. ) ;
#35439=STYLED_ITEM ( 'NONE', ( #59493 ), #57848 ) ;
#35441=ORIENTED_EDGE ( 'NONE', *, *, #29173, .F. ) ;
#35443=DIRECTION ( 'NONE',  ( 1.000000000000000000, 0.000000000000000000, 0.000000000000000000 ) ) ;
#35444=ADVANCED_FACE ( 'NONE', ( #21425 ), #6611, .F. ) ;
#35448=AXIS2_PLACEMENT_3D ( 'NONE', #8262, #40634, #14941 ) ;
#35452=FACE_OUTER_BOUND ( 'NONE', #57453, .T. ) ;
#35454=ORIENTED_EDGE ( 'NONE', *, *, #495, .F. ) ;
#35456=DIRECTION ( 'NONE',  ( 0.000000000000000000, 0.000000000000000000, -1.000000000000000000 ) ) ;
#35458=DIRECTION ( 'NONE',  ( 1.000000000000000000, 0.000000000000000000, 0.000000000000000000 ) ) ;
#35463=CARTESIAN_POINT ( 'NONE',  ( 23.21231517720798010, 1.797044900979284448E-15, -9.500000000000000000 ) ) ;
#35464=DIRECTION ( 'NONE',  ( -1.000000000000000000, -7.080503983578803083E-17, 0.000000000000000000 ) ) ;
#35466=CARTESIAN_POINT ( 'NONE',  ( -7.632228543268608334, 147.8429263765338249, 2.479861379858952830 ) ) ;
#35468=( NAMED_UNIT ( * ) PLANE_ANGLE_UNIT ( ) SI_UNIT ( $, .RADIAN. ) );
#35470=CARTESIAN_POINT ( 'NONE',  ( -23.71231517720798010, 112.9999999999999858, -7.500000000000000000 ) ) ;
#35473=CARTESIAN_POINT ( 'NONE',  ( -20.54906699372407530, 114.6596276111864654, 10.28538896680104209 ) ) ;
#35474=CARTESIAN_POINT ( 'NONE',  ( -67.49999999999998579, -1.929132118054077781E-14, 12.00000000000000000 ) ) ;
#35477=CARTESIAN_POINT ( 'NONE',  ( 8.437984349512095861, 141.3070736234661808, 1.550032578732816828E-15 ) ) ;
#35478=DIRECTION ( 'NONE',  ( 0.000000000000000000, 0.000000000000000000, 1.000000000000000000 ) ) ;
#35482=EDGE_LOOP ( 'NONE', ( #31145, #50581, #14723, #67949, #2153, #53464, #65102, #35871, #20510, #59729 ) ) ;
#35486=DIRECTION ( 'NONE',  ( 0.000000000000000000, 0.000000000000000000, 1.000000000000000000 ) ) ;
#35487=ORIENTED_EDGE ( 'NONE', *, *, #17449, .T. ) ;
#35490=PRESENTATION_STYLE_ASSIGNMENT (( #62206 ) ) ;
#35491=VECTOR ( 'NONE', #19713, 1000.000000000000000 ) ;
#35495=CARTESIAN_POINT ( 'NONE',  ( 41.72781494893835230, 107.4000720140338387, 3.999999999999999112 ) ) ;
#35499=( NAMED_UNIT ( * ) PLANE_ANGLE_UNIT ( ) SI_UNIT ( $, .RADIAN. ) );
#35503=CARTESIAN_POINT ( 'NONE',  ( 9.158309064922752540, 154.5000000000000568, -2.653638227437481678 ) ) ;
#35504=( LENGTH_UNIT ( ) NAMED_UNIT ( * ) SI_UNIT ( .MILLI., .METRE. ) );
#35507=CARTESIAN_POINT ( 'NONE',  ( -5.598654528085806881, 128.8549999999999898, -7.705886871421374629 ) ) ;
#35510=ADVANCED_FACE ( 'NONE', ( #51284 ), #65362, .T. ) ;
#35512=B_SPLINE_CURVE_WITH_KNOTS ( 'NONE', 3,
 ( #11497, #48838, #532, #22061 ),
 .UNSPECIFIED., .F., .F.,
 ( 4, 4 ),
 ( -4.672407068502317808E-06, 0.0001893522667583549335 ),
 .UNSPECIFIED. ) ;
#35515=CIRCLE ( 'NONE', #41164, 5.000000000000004441 ) ;
#35524=EDGE_CURVE ( 'NONE', #17063, #20808, #7663, .T. ) ;
#35525=CARTESIAN_POINT ( 'NONE',  ( 8.437984349512095861, 135.3070736234661524, 1.550032578732816828E-15 ) ) ;
#35527=VECTOR ( 'NONE', #55338, 1000.000000000000000 ) ;
#35528=DIRECTION ( 'NONE',  ( 1.000000000000000000, 8.881784197001252323E-16, 0.000000000000000000 ) ) ;
#35531=CARTESIAN_POINT ( 'NONE',  ( -44.50000000000000000, 9.499999999999980460, 3.000000000000000000 ) ) ;
#35535=DIRECTION ( 'NONE',  ( 1.000000000000000000, 0.000000000000000000, 0.000000000000000000 ) ) ;
#35539=ORIENTED_EDGE ( 'NONE', *, *, #20001, .F. ) ;
#35540=CARTESIAN_POINT ( 'NONE',  ( 67.50000000000000000, 1.797044900979284448E-15, -12.00000000000000000 ) ) ;
#35545=DIRECTION ( 'NONE',  ( 0.000000000000000000, 1.000000000000000000, 0.000000000000000000 ) ) ;
#35549=CARTESIAN_POINT ( 'NONE',  ( -5.598654528085806881, 139.7449999999999761, -7.705886871421374629 ) ) ;
#35553=CARTESIAN_POINT ( 'NONE',  ( 5.598654528085805993, 136.3550000000000182, 7.705886871421374629 ) ) ;
#35555=CYLINDRICAL_SURFACE ( 'NONE', #48792, 0.5000000000000004441 ) ;
#35557=CARTESIAN_POINT ( 'NONE',  ( -2.607480562269075097, 115.2929263765338135, 8.025000000000000355 ) ) ;
#35558=UNCERTAINTY_MEASURE_WITH_UNIT (LENGTH_MEASURE( 1.000000000000000082E-05 ), #503, 'distance_accuracy_value', 'NONE');
#35559=SURFACE_STYLE_FILL_AREA ( #14099 ) ;
#35560=CARTESIAN_POINT ( 'NONE',  ( 72.00000000000000000, 14.49137674618942562, -9.500000000000000000 ) ) ;
#35564=VERTEX_POINT ( 'NONE', #8020 ) ;
#35568=ORIENTED_EDGE ( 'NONE', *, *, #4174, .F. ) ;
#35569=CARTESIAN_POINT ( 'NONE',  ( -70.87837837837835764, 13.70805908423324126, -9.500000000000000000 ) ) ;
#35570=UNCERTAINTY_MEASURE_WITH_UNIT (LENGTH_MEASURE( 1.000000000000000082E-05 ), #7978, 'distance_accuracy_value', 'NONE');
#35571=EDGE_CURVE ( 'NONE', #62679, #49132, #46326, .T. ) ;
#35572=CYLINDRICAL_SURFACE ( 'NONE', #43164, 0.5000000000000004441 ) ;
#35574=CARTESIAN_POINT ( 'NONE',  ( 72.49999999999998579, 63.67479433117734544, 10.00000000000000000 ) ) ;
#35575=DIRECTION ( 'NONE',  ( -1.000000000000000000, 0.000000000000000000, 0.000000000000000000 ) ) ;
#35576=ORIENTED_EDGE ( 'NONE', *, *, #3623, .T. ) ;
#35578=ORIENTED_EDGE ( 'NONE', *, *, #29702, .F. ) ;
#35580=( LENGTH_UNIT ( ) NAMED_UNIT ( * ) SI_UNIT ( .MILLI., .METRE. ) );
#35587=EDGE_LOOP ( 'NONE', ( #26780, #36183, #38598, #36233 ) ) ;
#35588=CARTESIAN_POINT ( 'NONE',  ( -75.00000000000000000, 8.545765431912627719, -5.556277950132133547 ) ) ;
#35595=CARTESIAN_POINT ( 'NONE',  ( 10.01517768586949231, 138.6949999999999932, 1.839758294383810543E-15 ) ) ;
#35599=UNCERTAINTY_MEASURE_WITH_UNIT (LENGTH_MEASURE( 1.000000000000000082E-05 ), #3811, 'distance_accuracy_value', 'NONE');
#35600=ADVANCED_FACE ( 'NONE', ( #57242 ), #3745, .T. ) ;
#35604=PRESENTATION_STYLE_ASSIGNMENT (( #24661 ) ) ;
#35606=EDGE_CURVE ( 'NONE', #3817, #42106, #39594, .T. ) ;
#35607=DIRECTION ( 'NONE',  ( 1.000000000000000000, 0.000000000000000000, 0.000000000000000000 ) ) ;
#35609=ORIENTED_EDGE ( 'NONE', *, *, #43501, .F. ) ;
#35610=CARTESIAN_POINT ( 'NONE',  ( 48.50000000000000000, 14.49137674618942562, 7.000000000000000000 ) ) ;
#35611=ORIENTED_EDGE ( 'NONE', *, *, #24200, .T. ) ;
#35615=FILL_AREA_STYLE ('',( #19417 ) ) ;
#35616=CARTESIAN_POINT ( 'NONE',  ( -45.66562050014668728, 8.455502173247500863, 6.462386104487610083 ) ) ;
#35619=AXIS2_PLACEMENT_3D ( 'NONE', #35922, #56680, #19377 ) ;
#35620=EDGE_LOOP ( 'NONE', ( #66894, #66618, #687 ) ) ;
#35622=CIRCLE ( 'NONE', #28863, 13.49999999999999822 ) ;
#35623=VERTEX_POINT ( 'NONE', #4447 ) ;
#35624=CARTESIAN_POINT ( 'NONE',  ( -20.99060317843563794, 114.7782486714346533, -10.00000000000000178 ) ) ;
#35625=CYLINDRICAL_SURFACE ( 'NONE', #38833, 0.5000000000000004441 ) ;
#35628=SURFACE_STYLE_USAGE ( .BOTH. , #2858 ) ;
#35630=CARTESIAN_POINT ( 'NONE',  ( 3.094860106618431583, 111.0949999999999704, 9.525000000000000355 ) ) ;
#35633=CARTESIAN_POINT ( 'NONE',  ( 9.058813317711338797, 112.9549999999999841, -2.943386871421372675 ) ) ;
#35636=CARTESIAN_POINT ( 'NONE',  ( -5.598654528085806881, 134.8549999999999898, -7.705886871421374629 ) ) ;
#35638=CARTESIAN_POINT ( 'NONE',  ( -23.21231517720797655, 117.4999999999999716, 7.000000000000000000 ) ) ;
#35639=CIRCLE ( 'NONE', #40128, 15.00000000000000000 ) ;
#35640=CARTESIAN_POINT ( 'NONE',  ( -41.40613950039011826, 107.1008216811760718, 3.493724300021677553 ) ) ;
#35642=EDGE_LOOP ( 'NONE', ( #30155, #18599, #40083, #44233 ) ) ;
#35643=CARTESIAN_POINT ( 'NONE',  ( 74.99999999999998579, 50.00000000000000000, -7.000000000000000000 ) ) ;
#35648=EDGE_CURVE ( 'NONE', #13986, #8875, #62036, .T. ) ;
#35649=DIRECTION ( 'NONE',  ( -0.000000000000000000, -0.000000000000000000, -1.000000000000000000 ) ) ;
#35652=SURFACE_SIDE_STYLE ('',( #25428 ) ) ;
#35653=EDGE_LOOP ( 'NONE', ( #13023, #55813, #58945, #52306 ) ) ;
#35656=ORIENTED_EDGE ( 'NONE', *, *, #54933, .T. ) ;
#35658=DIRECTION ( 'NONE',  ( -0.000000000000000000, -0.000000000000000000, -1.000000000000000000 ) ) ;
#35661=CARTESIAN_POINT ( 'NONE',  ( 3.094860106618435136, 142.2950000000000159, -9.525000000000000355 ) ) ;
#35663=PRODUCT_DEFINITION ( 'UNKNOWN', '', #25901, #16431 ) ;
#35666=ADVANCED_FACE ( 'NONE', ( #65907 ), #55702, .F. ) ;
#35673=EDGE_CURVE ( 'NONE', #7860, #44595, #33881, .T. ) ;
#35677=( LENGTH_UNIT ( ) NAMED_UNIT ( * ) SI_UNIT ( .MILLI., .METRE. ) );
#35680=DIRECTION ( 'NONE',  ( 1.000000000000000000, 0.000000000000000000, 0.000000000000000000 ) ) ;
#35682=( NAMED_UNIT ( * ) SI_UNIT ( $, .STERADIAN. ) SOLID_ANGLE_UNIT ( ) );
#35683=EDGE_CURVE ( 'NONE', #9536, #63831, #5158, .T. ) ;
#35684=CARTESIAN_POINT ( 'NONE',  ( -15.98999599679679839, 117.9999999999999716, 7.000000000000000000 ) ) ;
#35688=( GEOMETRIC_REPRESENTATION_CONTEXT ( 3 ) GLOBAL_UNCERTAINTY_ASSIGNED_CONTEXT ( ( #7988 ) ) GLOBAL_UNIT_ASSIGNED_CONTEXT ( ( #17776, #60647, #39599 ) ) REPRESENTATION_CONTEXT ( 'NONE', 'WORKASPACE' ) );
#35690=AXIS2_PLACEMENT_3D ( 'NONE', #60776, #12596, #33381 ) ;
#35691=CARTESIAN_POINT ( 'NONE',  ( -15.98999599679679839, 146.4999999999999716, 7.500000000000000000 ) ) ;
#35693=ORIENTED_EDGE ( 'NONE', *, *, #45859, .F. ) ;
#35698=CARTESIAN_POINT ( 'NONE',  ( 2.607480562269051116, 122.7070736234661439, 8.025000000000016342 ) ) ;
#35701=ORIENTED_EDGE ( 'NONE', *, *, #722, .F. ) ;
#35703=DIRECTION ( 'NONE',  ( -1.000000000000000000, 0.000000000000000000, 0.000000000000000000 ) ) ;
#35704=SURFACE_STYLE_FILL_AREA ( #30746 ) ;
#35706=FACE_OUTER_BOUND ( 'NONE', #56424, .T. ) ;
#35707=EDGE_CURVE ( 'NONE', #45578, #65484, #60885, .T. ) ;
#35709=CARTESIAN_POINT ( 'NONE',  ( -7.632228543268607446, 136.6570736234661467, -2.479861379858953718 ) ) ;
#35710=FILL_AREA_STYLE ('',( #19859 ) ) ;
#35711=ORIENTED_EDGE ( 'NONE', *, *, #2660, .F. ) ;
#35712=FACE_OUTER_BOUND ( 'NONE', #45125, .T. ) ;
#35715=AXIS2_PLACEMENT_3D ( 'NONE', #37147, #32173, #48390 ) ;
#35719=( NAMED_UNIT ( * ) PLANE_ANGLE_UNIT ( ) SI_UNIT ( $, .RADIAN. ) );
#35720=AXIS2_PLACEMENT_3D ( 'NONE', #40359, #57204, #45666 ) ;
#35722=EDGE_LOOP ( 'NONE', ( #15596, #51060, #45342, #68700 ) ) ;
#35724=DIRECTION ( 'NONE',  ( -0.000000000000000000, -0.000000000000000000, 1.000000000000000000 ) ) ;
#35726=CARTESIAN_POINT ( 'NONE',  ( 75.00000000000000000, 20.36037961002804053, 10.00000000000000000 ) ) ;
#35727=VERTEX_POINT ( 'NONE', #64251 ) ;
#35728=CIRCLE ( 'NONE', #23362, 0.5000000000000004441 ) ;
#35731=CARTESIAN_POINT ( 'NONE',  ( -48.00000000000000000, 99.99999999999992895, -7.500000000000000000 ) ) ;
#35735=FACE_OUTER_BOUND ( 'NONE', #34939, .T. ) ;
#35736=CARTESIAN_POINT ( 'NONE',  ( -9.827790563157511022E-16, 127.4429263765338192, 8.025000000000000355 ) ) ;
#35739=CARTESIAN_POINT ( 'NONE',  ( 34.99999999999992895, 110.4999999999999858, 9.500000000000000000 ) ) ;
#35740=CARTESIAN_POINT ( 'NONE',  ( 3.094860106618435136, 118.2949999999999875, -9.525000000000000355 ) ) ;
#35749=CARTESIAN_POINT ( 'NONE',  ( 74.99999999999998579, 119.9999999999997584, -9.500000000000000000 ) ) ;
#35751=EDGE_CURVE ( 'NONE', #49404, #10212, #36227, .T. ) ;
#35756=EDGE_LOOP ( 'NONE', ( #53788, #34431, #44172, #6885 ) ) ;
#35761=AXIS2_PLACEMENT_3D ( 'NONE', #52537, #15593, #38800 ) ;
#35762=( GEOMETRIC_REPRESENTATION_CONTEXT ( 3 ) GLOBAL_UNCERTAINTY_ASSIGNED_CONTEXT ( ( #21302 ) ) GLOBAL_UNIT_ASSIGNED_CONTEXT ( ( #23714, #24394, #2553 ) ) REPRESENTATION_CONTEXT ( 'NONE', 'WORKASPACE' ) );
#35765=CARTESIAN_POINT ( 'NONE',  ( 8.102448949553181734, 160.5049999999999386, 5.886773742842750679 ) ) ;
#35767=CARTESIAN_POINT ( 'NONE',  ( -0.3711768842070180541, 154.5000000000000284, -9.524999999999986144 ) ) ;
#35769=DIRECTION ( 'NONE',  ( 0.000000000000000000, 0.000000000000000000, -1.000000000000000000 ) ) ;
#35770=CARTESIAN_POINT ( 'NONE',  ( -0.7252983342185689297, 110.8245556577202962, 9.200444342279737953 ) ) ;
#35771=AXIS2_PLACEMENT_3D ( 'NONE', #48941, #53489, #10917 ) ;
#35773=ADVANCED_FACE ( 'NONE', ( #40587 ), #3217, .F. ) ;
#35776=VERTEX_POINT ( 'NONE', #41289 ) ;
#35779=ADVANCED_FACE ( 'NONE', ( #2526 ), #66605, .T. ) ;
#35783=CARTESIAN_POINT ( 'NONE',  ( 75.00000000000000000, -2.215169945516535778E-14, 6.999999999999999112 ) ) ;
#35784=SURFACE_SIDE_STYLE ('',( #9763 ) ) ;
#35785=ORIENTED_EDGE ( 'NONE', *, *, #26138, .T. ) ;
#35787=EDGE_LOOP ( 'NONE', ( #58612, #31134, #28032, #1744, #42168, #37581, #53958, #27964, #40845, #53090, #3986, #41165, #30429, #6047, #11812, #61814 ) ) ;
#35788=FACE_OUTER_BOUND ( 'NONE', #65382, .T. ) ;
#35790=CARTESIAN_POINT ( 'NONE',  ( -1.166476076187854022E-15, 115.0549999999999926, 9.525000000000000355 ) ) ;
#35793=AXIS2_PLACEMENT_3D ( 'NONE', #40216, #3924, #14491 ) ;
#35796=ORIENTED_EDGE ( 'NONE', *, *, #41201, .F. ) ;
#35797=( GEOMETRIC_REPRESENTATION_CONTEXT ( 3 ) GLOBAL_UNCERTAINTY_ASSIGNED_CONTEXT ( ( #44085 ) ) GLOBAL_UNIT_ASSIGNED_CONTEXT ( ( #48135, #37938, #69218 ) ) REPRESENTATION_CONTEXT ( 'NONE', 'WORKASPACE' ) );
#35801=CARTESIAN_POINT ( 'NONE',  ( 4.716976649647099507, 140.6429263765338078, -6.492361379858953008 ) ) ;
#35803=DIRECTION ( 'NONE',  ( 0.000000000000000000, -1.000000000000000000, 0.000000000000000000 ) ) ;
#35804=STYLED_ITEM ( 'NONE', ( #59263 ), #51078 ) ;
#35806=DIRECTION ( 'NONE',  ( 1.000000000000000000, 0.000000000000000000, 0.000000000000000000 ) ) ;
#35808=EDGE_CURVE ( 'NONE', #66756, #11552, #35989, .T. ) ;
#35809=SURFACE_STYLE_FILL_AREA ( #14341 ) ;
#35810=VERTEX_POINT ( 'NONE', #14513 ) ;
#35811=FILL_AREA_STYLE ('',( #9087 ) ) ;
#35825=CARTESIAN_POINT ( 'NONE',  ( -74.50000000000000000, 7.768687147774688384, -6.999999999999999112 ) ) ;
#35826=VERTEX_POINT ( 'NONE', #18422 ) ;
#35828=ADVANCED_FACE ( 'NONE', ( #66959 ), #61312, .T. ) ;
#35830=( NAMED_UNIT ( * ) PLANE_ANGLE_UNIT ( ) SI_UNIT ( $, .RADIAN. ) );
#35833=ADVANCED_FACE ( 'NONE', ( #46587 ), #62685, .T. ) ;
#35835=( BOUNDED_CURVE ( )  B_SPLINE_CURVE ( 2, ( #44583, #55782, #27975, #7589, #39291, #55071, #6895, #50516, #49480, #17143, #60694 ),
 .UNSPECIFIED., .F., .F. ) 
 B_SPLINE_CURVE_WITH_KNOTS ( ( 3, 2, 2, 2, 2, 3 ),
 ( 0.2352941176470587370, 0.2411764705882352144, 0.2470588235294116919, 0.2529411764705881693, 0.2588235294117646745, 0.2647058823529411242 ),
 .UNSPECIFIED. ) 
 CURVE ( )  GEOMETRIC_REPRESENTATION_ITEM ( )  RATIONAL_B_SPLINE_CURVE ( ( 1.000000000000000666, 0.9510565162951529761, 1.000000000000000000, 0.9510565162951535312, 1.000000000000000000, 0.9510565162951535312, 1.000000000000000000, 0.9510565162951535312, 1.000000000000000000, 0.9510565162951539753, 0.9999999999999995559 ) ) 
 REPRESENTATION_ITEM ( '' )  );
#35837=ORIENTED_EDGE ( 'NONE', *, *, #50316, .F. ) ;
#35839=ADVANCED_FACE ( 'NONE', ( #64091 ), #25420, .T. ) ;
#35840=MECHANICAL_DESIGN_GEOMETRIC_PRESENTATION_REPRESENTATION('',(#15626),#5463);
#35841=FACE_OUTER_BOUND ( 'NONE', #24800, .T. ) ;
#35843=DIRECTION ( 'NONE',  ( 7.080503983578803083E-17, -1.000000000000000000, 0.000000000000000000 ) ) ;
#35845=EDGE_CURVE ( 'NONE', #40883, #61513, #1384, .T. ) ;
#35847=CARTESIAN_POINT ( 'NONE',  ( -8.102448949553181734, 123.6049999999999756, 5.886773742842747126 ) ) ;
#35849=CARTESIAN_POINT ( 'NONE',  ( -75.00000000000000000, 9.119539144243724138, -6.744166081069411511 ) ) ;
#35850=COLOUR_RGB ( '', 0.09019608, 0.27058824, 0.51372549) ;
#35858=CARTESIAN_POINT ( 'NONE',  ( -4.716976649647098618, 146.2570736234661410, 6.492361379858953008 ) ) ;
#35862=CARTESIAN_POINT ( 'NONE',  ( -71.50000000000000000, 35.92875272052971525, 7.500000000000000000 ) ) ;
#35864=COLOUR_RGB ( '', 0.08235294, 0.09019608, 0.10196078) ;
#35866=DIRECTION ( 'NONE',  ( 0.000000000000000000, 0.000000000000000000, 1.000000000000000000 ) ) ;
#35867=CARTESIAN_POINT ( 'NONE',  ( -15.48999599679679662, 117.9999999999999716, 9.500000000000000000 ) ) ;
#35868=CYLINDRICAL_SURFACE ( 'NONE', #51722, 0.5000000000000004441 ) ;
#35869=TOROIDAL_SURFACE ( 'NONE', #5504, 1.000000000000000000, 0.5000000000000000000 ) ;
#35871=ORIENTED_EDGE ( 'NONE', *, *, #34454, .T. ) ;
#35874=DIRECTION ( 'NONE',  ( -0.000000000000000000, -0.000000000000000000, 1.000000000000000000 ) ) ;
#35876=VERTEX_POINT ( 'NONE', #31038 ) ;
#35878=PLANE ( 'NONE',  #60178 ) ;
#35880=CIRCLE ( 'NONE', #5517, 0.5000000000000000000 ) ;
#35881=CIRCLE ( 'NONE', #38175, 0.5000000000000004441 ) ;
#35883=CARTESIAN_POINT ( 'NONE',  ( 10.01517768586949231, 138.6949999999999932, 1.839758294383810543E-15 ) ) ;
#35885=FILL_AREA_STYLE ('',( #14413 ) ) ;
#35886=CARTESIAN_POINT ( 'NONE',  ( 5.598654528085809545, 146.2549999999999955, -7.705886871421373741 ) ) ;
#35887=DIRECTION ( 'NONE',  ( 0.000000000000000000, 1.000000000000000000, 0.000000000000000000 ) ) ;
#35888=COLOUR_RGB ( '', 0.31764706, 0.68627451, 0.89019608) ;
#35889=( LENGTH_UNIT ( ) NAMED_UNIT ( * ) SI_UNIT ( .MILLI., .METRE. ) );
#35891=CARTESIAN_POINT ( 'NONE',  ( -4.716976649647098618, 121.1429263765338220, 6.492361379858953008 ) ) ;
#35892=( NAMED_UNIT ( * ) PLANE_ANGLE_UNIT ( ) SI_UNIT ( $, .RADIAN. ) );
#35893=PRESENTATION_STYLE_ASSIGNMENT (( #14797 ) ) ;
#35895=CARTESIAN_POINT ( 'NONE',  ( 15.48999599679679662, 118.4999999999999716, 7.000000000000000000 ) ) ;
#35897=EDGE_CURVE ( 'NONE', #35826, #60834, #18852, .T. ) ;
#35898=AXIS2_PLACEMENT_3D ( 'NONE', #50210, #12902, #34367 ) ;
#35903=CARTESIAN_POINT ( 'NONE',  ( -23.71231517720798010, 117.4999999999999716, 7.000000000000000000 ) ) ;
#35908=B_SPLINE_CURVE_WITH_KNOTS ( 'NONE', 3,
 ( #52045, #68556, #47856, #14750, #47493, #19663, #35849, #15460, #52730, #4147, #20712, #30191 ),
 .UNSPECIFIED., .F., .F.,
 ( 4, 2, 2, 2, 2, 4 ),
 ( 0.000000000000000000, 0.0002999083533514613608, 0.0005998167067029227216, 0.001199633413405845443, 0.001799450120108768165, 0.002399266826811690886 ),
 .UNSPECIFIED. ) ;
#35916=LINE ( 'NONE', #52114, #10779 ) ;
#35917=ORIENTED_EDGE ( 'NONE', *, *, #12783, .F. ) ;
#35919=EDGE_CURVE ( 'NONE', #68848, #4324, #53216, .T. ) ;
#35920=ORIENTED_EDGE ( 'NONE', *, *, #10355, .F. ) ;
#35921=CARTESIAN_POINT ( 'NONE',  ( 44.99999999999977263, 147.4999999999999716, 9.500000000000000000 ) ) ;
#35922=CARTESIAN_POINT ( 'NONE',  ( -71.50000000000000000, 14.49137674618942562, 10.00000000000000000 ) ) ;
#35924=VERTEX_POINT ( 'NONE', #44766 ) ;
#35926=CARTESIAN_POINT ( 'NONE',  ( 74.99999999999998579, 50.00000000000000000, -7.000000000000000000 ) ) ;
#35927=ADVANCED_FACE ( 'NONE', ( #6727 ), #54207, .T. ) ;
#35940=CARTESIAN_POINT ( 'NONE',  ( 10.01517768586949231, 147.6949999999999932, 1.839758294383810543E-15 ) ) ;
#35943=CARTESIAN_POINT ( 'NONE',  ( -72.00000000000000000, 13.41640786499872284, -7.500000000000000000 ) ) ;
#35948=( NAMED_UNIT ( * ) PLANE_ANGLE_UNIT ( ) SI_UNIT ( $, .RADIAN. ) );
#35953=CARTESIAN_POINT ( 'NONE',  ( 1.227708416145219032E-15, 154.9999999999999716, -10.02499999999997904 ) ) ;
#35956=VERTEX_POINT ( 'NONE', #16970 ) ;
#35959=ADVANCED_FACE ( 'NONE', ( #1032 ), #63205, .F. ) ;
#35962=CARTESIAN_POINT ( 'NONE',  ( 71.74137931034479720, 63.10081643261027295, -9.500000000000000000 ) ) ;
#35963=CIRCLE ( 'NONE', #41604, 0.5000000000000004441 ) ;
#35967=VERTEX_POINT ( 'NONE', #17669 ) ;
#35968=CYLINDRICAL_SURFACE ( 'NONE', #49267, 0.5000000000000004441 ) ;
#35969=CARTESIAN_POINT ( 'NONE',  ( 44.99999999999977973, 146.9999999999999716, -9.500000000000000000 ) ) ;
#35971=AXIS2_PLACEMENT_3D ( 'NONE', #36045, #30738, #20544 ) ;
#35972=VECTOR ( 'NONE', #54843, 1000.000000000000000 ) ;
#35974=CARTESIAN_POINT ( 'NONE',  ( -10.01517768586949231, 110.1949999999999648, -6.132527647946036459E-16 ) ) ;
#35975=AXIS2_PLACEMENT_3D ( 'NONE', #13001, #39089, #60158 ) ;
#35979=CARTESIAN_POINT ( 'NONE',  ( 8.102448949553179958, 121.5049999999999670, 5.886773742842750679 ) ) ;
#35983=CARTESIAN_POINT ( 'NONE',  ( -9.058813317711338797, 138.4549999999999841, 2.943386871421373563 ) ) ;
#35984=( NAMED_UNIT ( * ) SI_UNIT ( $, .STERADIAN. ) SOLID_ANGLE_UNIT ( ) );
#35987=FILL_AREA_STYLE_COLOUR ( '', #56468 ) ;
#35989=LINE ( 'NONE', #29663, #59839 ) ;
#35990=DIRECTION ( 'NONE',  ( -0.000000000000000000, -0.000000000000000000, 1.000000000000000000 ) ) ;
#36001=DIRECTION ( 'NONE',  ( 0.000000000000000000, 0.000000000000000000, 1.000000000000000000 ) ) ;
#36009=DIRECTION ( 'NONE',  ( 1.000000000000000000, 0.000000000000000000, 0.000000000000000000 ) ) ;
#36012=AXIS2_PLACEMENT_3D ( 'NONE', #13714, #25307, #19683 ) ;
#36013=CARTESIAN_POINT ( 'NONE',  ( 8.102448949553179958, 153.3950000000000102, 5.886773742842750679 ) ) ;
#36015=TOROIDAL_SURFACE ( 'NONE', #7922, 1.000000000000000000, 0.5000000000000000000 ) ;
#36024=CARTESIAN_POINT ( 'NONE',  ( 8.102448949553183510, 117.9949999999999761, -5.886773742842746238 ) ) ;
#36028=PRESENTATION_STYLE_ASSIGNMENT (( #47676 ) ) ;
#36030=AXIS2_PLACEMENT_3D ( 'NONE', #46813, #36231, #58686 ) ;
#36032=CARTESIAN_POINT ( 'NONE',  ( 72.00000000000000000, 35.92875272052971525, -7.500000000000000000 ) ) ;
#36037=LINE ( 'NONE', #9302, #23065 ) ;
#36038=CARTESIAN_POINT ( 'NONE',  ( -2.607480562269074653, 125.4070736234661467, 8.025000000000000355 ) ) ;
#36039=DIRECTION ( 'NONE',  ( -0.000000000000000000, -0.000000000000000000, -1.000000000000000000 ) ) ;
#36044=( LENGTH_UNIT ( ) NAMED_UNIT ( * ) SI_UNIT ( .MILLI., .METRE. ) );
#36045=CARTESIAN_POINT ( 'NONE',  ( -71.50000000000000000, 14.49137674618942562, -7.500000000000000000 ) ) ;
#36055=( NAMED_UNIT ( * ) SI_UNIT ( $, .STERADIAN. ) SOLID_ANGLE_UNIT ( ) );
#36059=CARTESIAN_POINT ( 'NONE',  ( -9.827790563157511022E-16, 131.5570736234661524, 8.025000000000000355 ) ) ;
#36062=EDGE_LOOP ( 'NONE', ( #29092, #20541 ) ) ;
#36068=DIRECTION ( 'NONE',  ( -0.000000000000000000, -0.000000000000000000, -1.000000000000000000 ) ) ;
#36069=ADVANCED_FACE ( 'NONE', ( #24625 ), #55627, .T. ) ;
#36070=CARTESIAN_POINT ( 'NONE',  ( -74.99999999999998579, 50.00000000000000000, 7.500000000000000000 ) ) ;
#36071=( NAMED_UNIT ( * ) PLANE_ANGLE_UNIT ( ) SI_UNIT ( $, .RADIAN. ) );
#36075=VERTEX_POINT ( 'NONE', #19002 ) ;
#36076=AXIS2_PLACEMENT_3D ( 'NONE', #3351, #41075, #24845 ) ;
#36078=LINE ( 'NONE', #4030, #43630 ) ;
#36080=UNCERTAINTY_MEASURE_WITH_UNIT (LENGTH_MEASURE( 1.000000000000000082E-05 ), #61400, 'distance_accuracy_value', 'NONE');
#36082=DIRECTION ( 'NONE',  ( 0.000000000000000000, 0.000000000000000000, -1.000000000000000000 ) ) ;
#36083=DIRECTION ( 'NONE',  ( -1.000000000000000000, -0.000000000000000000, -0.000000000000000000 ) ) ;
#36087=CARTESIAN_POINT ( 'NONE',  ( -74.99999999999998579, 50.00000000000000000, -11.50000000000000000 ) ) ;
#36091=DIRECTION ( 'NONE',  ( 1.000000000000000000, 0.000000000000000000, 0.000000000000000000 ) ) ;
#36092=CARTESIAN_POINT ( 'NONE',  ( -45.50000000000000000, -1.469576158976824302E-14, -9.500000000000000000 ) ) ;
#36095=CARTESIAN_POINT ( 'NONE',  ( 10.01517768586949408, 126.6950000000000074, 1.839758294383810543E-15 ) ) ;
#36098=CARTESIAN_POINT ( 'NONE',  ( 0.000000000000000000, 114.9999999999999574, 16.50000000000000000 ) ) ;
#36099=AXIS2_PLACEMENT_3D ( 'NONE', #36495, #64207, #25877 ) ;
#36102=VERTEX_POINT ( 'NONE', #51049 ) ;
#36105=DIRECTION ( 'NONE',  ( 0.000000000000000000, 0.000000000000000000, -1.000000000000000000 ) ) ;
#36106=SURFACE_STYLE_FILL_AREA ( #35408 ) ;
#36108=DIRECTION ( 'NONE',  ( -0.000000000000000000, -0.000000000000000000, -1.000000000000000000 ) ) ;
#36110=CARTESIAN_POINT ( 'NONE',  ( -75.00000000000000000, 8.554728201919930441, 6.928664365919924961 ) ) ;
#36115=( GEOMETRIC_REPRESENTATION_CONTEXT ( 3 ) GLOBAL_UNCERTAINTY_ASSIGNED_CONTEXT ( ( #35558 ) ) GLOBAL_UNIT_ASSIGNED_CONTEXT ( ( #503, #22033, #28670 ) ) REPRESENTATION_CONTEXT ( 'NONE', 'WORKASPACE' ) );
#36116=ORIENTED_EDGE ( 'NONE', *, *, #19374, .F. ) ;
#36118=CARTESIAN_POINT ( 'NONE',  ( 44.24703880899743069, 10.19173881602633536, -3.568710496479958749 ) ) ;
#36120=DIRECTION ( 'NONE',  ( 0.000000000000000000, -1.000000000000000000, 0.000000000000000000 ) ) ;
#36121=( NAMED_UNIT ( * ) SI_UNIT ( $, .STERADIAN. ) SOLID_ANGLE_UNIT ( ) );
#36122=UNCERTAINTY_MEASURE_WITH_UNIT (LENGTH_MEASURE( 1.000000000000000082E-05 ), #50703, 'distance_accuracy_value', 'NONE');
#36127=CARTESIAN_POINT ( 'NONE',  ( 9.058813317711337021, 154.6549999999999727, 2.943386871421375783 ) ) ;
#36128=DIRECTION ( 'NONE',  ( 1.000000000000000000, 0.000000000000000000, 0.000000000000000000 ) ) ;
#36131=UNCERTAINTY_MEASURE_WITH_UNIT (LENGTH_MEASURE( 1.000000000000000082E-05 ), #53572, 'distance_accuracy_value', 'NONE');
#36134=CARTESIAN_POINT ( 'NONE',  ( 60.00000000000000000, 1.797044900979284448E-15, -10.00000000000000000 ) ) ;
#36139=AXIS2_PLACEMENT_3D ( 'NONE', #21450, #27402, #64367 ) ;
#36144=ORIENTED_EDGE ( 'NONE', *, *, #29960, .T. ) ;
#36151=CARTESIAN_POINT ( 'NONE',  ( -20.57648122633967347, 114.5694469452588038, 10.27659575647942169 ) ) ;
#36155=ORIENTED_EDGE ( 'NONE', *, *, #22716, .F. ) ;
#36161=CARTESIAN_POINT ( 'NONE',  ( -24.21231517720798365, 117.4999999999999716, 7.000000000000000000 ) ) ;
#36162=ORIENTED_EDGE ( 'NONE', *, *, #67853, .F. ) ;
#36164=CARTESIAN_POINT ( 'NONE',  ( -8.102448949553181734, 120.6049999999999756, 5.886773742842747126 ) ) ;
#36166=VERTEX_POINT ( 'NONE', #31292 ) ;
#36168=SURFACE_SIDE_STYLE ('',( #53691 ) ) ;
#36174=ADVANCED_FACE ( 'NONE', ( #69305 ), #41913, .T. ) ;
#36177=CARTESIAN_POINT ( 'NONE',  ( 6.826472737025119919, 157.8929263765338078, 4.959722759717908325 ) ) ;
#36181=COLOUR_RGB ( '', 0.08235294, 0.09019608, 0.10196078) ;
#36183=ORIENTED_EDGE ( 'NONE', *, *, #59164, .F. ) ;
#36185=CARTESIAN_POINT ( 'NONE',  ( 20.26251832593580104, 115.0246525964671207, -10.00000000000000178 ) ) ;
#36186=VERTEX_POINT ( 'NONE', #36646 ) ;
#36187=( NAMED_UNIT ( * ) PLANE_ANGLE_UNIT ( ) SI_UNIT ( $, .RADIAN. ) );
#36188=CARTESIAN_POINT ( 'NONE',  ( 47.50000000000000000, 14.49137674618942562, 9.500000000000000000 ) ) ;
#36192=DIRECTION ( 'NONE',  ( -0.000000000000000000, 1.000000000000000000, -0.000000000000000000 ) ) ;
#36193=CARTESIAN_POINT ( 'NONE',  ( -72.00000000000000000, 36.32520566882265456, 7.500000000000000000 ) ) ;
#36194=CARTESIAN_POINT ( 'NONE',  ( 45.00000000000000000, 9.999999999999982236, 6.000000000000000888 ) ) ;
#36195=FACE_OUTER_BOUND ( 'NONE', #53558, .T. ) ;
#36196=DIRECTION ( 'NONE',  ( -1.000000000000000000, 0.000000000000000000, 0.000000000000000000 ) ) ;
#36199=AXIS2_PLACEMENT_3D ( 'NONE', #68422, #35724, #48054 ) ;
#36201=CARTESIAN_POINT ( 'NONE',  ( -71.49999999999998579, 64.07124727947029896, -7.000000000000000000 ) ) ;
#36202=FACE_OUTER_BOUND ( 'NONE', #5216, .T. ) ;
#36203=CARTESIAN_POINT ( 'NONE',  ( -34.99999999999999289, 99.99999999999998579, 10.00000000000000000 ) ) ;
#36205=DIRECTION ( 'NONE',  ( 0.000000000000000000, 0.000000000000000000, -1.000000000000000000 ) ) ;
#36208=CARTESIAN_POINT ( 'NONE',  ( 34.99999999999992895, 112.9999999999999858, -7.500000000000000000 ) ) ;
#36214=VERTEX_POINT ( 'NONE', #9876 ) ;
#36217=DIRECTION ( 'NONE',  ( -0.000000000000000000, -0.000000000000000000, -1.000000000000000000 ) ) ;
#36220=CARTESIAN_POINT ( 'NONE',  ( 7.911516905016148904, 154.4999999999999432, 5.322522116219993826 ) ) ;
#36223=CARTESIAN_POINT ( 'NONE',  ( 10.01517768586949231, 124.8049999999999642, 1.839758294383810543E-15 ) ) ;
#36227=CIRCLE ( 'NONE', #57536, 26.49999999999999645 ) ;
#36229=UNCERTAINTY_MEASURE_WITH_UNIT (LENGTH_MEASURE( 1.000000000000000082E-05 ), #22598, 'distance_accuracy_value', 'NONE');
#36231=DIRECTION ( 'NONE',  ( 0.000000000000000000, 1.000000000000000000, -0.000000000000000000 ) ) ;
#36233=ORIENTED_EDGE ( 'NONE', *, *, #33012, .F. ) ;
#36236=( NAMED_UNIT ( * ) SI_UNIT ( $, .STERADIAN. ) SOLID_ANGLE_UNIT ( ) );
#36239=EDGE_CURVE ( 'NONE', #34430, #69671, #56511, .T. ) ;
#36242=ORIENTED_EDGE ( 'NONE', *, *, #14223, .T. ) ;
#36243=ORIENTED_EDGE ( 'NONE', *, *, #60745, .T. ) ;
#36246=UNCERTAINTY_MEASURE_WITH_UNIT (LENGTH_MEASURE( 1.000000000000000082E-05 ), #15037, 'distance_accuracy_value', 'NONE');
#36251=AXIS2_PLACEMENT_3D ( 'NONE', #40170, #66167, #23956 ) ;
#36252=( NAMED_UNIT ( * ) SI_UNIT ( $, .STERADIAN. ) SOLID_ANGLE_UNIT ( ) );
#36256=ORIENTED_EDGE ( 'NONE', *, *, #67963, .F. ) ;
#36259=EDGE_CURVE ( 'NONE', #50952, #29891, #9341, .T. ) ;
#36260=ORIENTED_EDGE ( 'NONE', *, *, #68555, .F. ) ;
#36262=CARTESIAN_POINT ( 'NONE',  ( 60.00000000000000000, 1.797044900979284448E-15, 10.50000000000000000 ) ) ;
#36263=ORIENTED_EDGE ( 'NONE', *, *, #24154, .F. ) ;
#36264=DIRECTION ( 'NONE',  ( 0.000000000000000000, 0.000000000000000000, 1.000000000000000000 ) ) ;
#36265=CARTESIAN_POINT ( 'NONE',  ( -9.058813317711338797, 146.3449999999999989, 2.943386871421373563 ) ) ;
#36269=CARTESIAN_POINT ( 'NONE',  ( 6.778496103158111019, 154.4256832137428717, 6.848681790822515936 ) ) ;
#36270=( NAMED_UNIT ( * ) PLANE_ANGLE_UNIT ( ) SI_UNIT ( $, .RADIAN. ) );
#36271=DIRECTION ( 'NONE',  ( 1.000000000000000000, 0.000000000000000000, 0.000000000000000000 ) ) ;
#36273=CARTESIAN_POINT ( 'NONE',  ( 7.632228543268607446, 116.0429263765338277, 2.479861379858954606 ) ) ;
#36275=UNCERTAINTY_MEASURE_WITH_UNIT (LENGTH_MEASURE( 1.000000000000000082E-05 ), #14419, 'distance_accuracy_value', 'NONE');
#36278=CARTESIAN_POINT ( 'NONE',  ( 45.00000000000000000, 10.69371294336137979, 6.000000000000000888 ) ) ;
#36281=ORIENTED_EDGE ( 'NONE', *, *, #41645, .F. ) ;
#36282=COLOUR_RGB ( '', 0.09019608, 0.27058824, 0.51372549) ;
#36283=CARTESIAN_POINT ( 'NONE',  ( 40.99999999999997868, 107.7459666924147967, 3.050022167383940719 ) ) ;
#36284=ORIENTED_EDGE ( 'NONE', *, *, #5147, .F. ) ;
#36289=MECHANICAL_DESIGN_GEOMETRIC_PRESENTATION_REPRESENTATION('',(#10442),#5895);
#36290=EDGE_LOOP ( 'NONE', ( #53514, #27269, #45192, #38970 ) ) ;
#36291=SURFACE_STYLE_FILL_AREA ( #47556 ) ;
#36292=UNCERTAINTY_MEASURE_WITH_UNIT (LENGTH_MEASURE( 1.000000000000000082E-05 ), #7679, 'distance_accuracy_value', 'NONE');
#36293=TOROIDAL_SURFACE ( 'NONE', #26141, 10.49999999999999822, 0.5000000000000000000 ) ;
#36297=CARTESIAN_POINT ( 'NONE',  ( 2.607480562268992941, 146.7929263765338419, -8.025000000000060751 ) ) ;
#36299=EDGE_LOOP ( 'NONE', ( #27449, #5519, #12503, #30780 ) ) ;
#36301=( NAMED_UNIT ( * ) PLANE_ANGLE_UNIT ( ) SI_UNIT ( $, .RADIAN. ) );
#36304=EDGE_LOOP ( 'NONE', ( #36366, #39657, #23847, #49539 ) ) ;
#36305=LINE ( 'NONE', #57726, #46119 ) ;
#36306=CARTESIAN_POINT ( 'NONE',  ( -66.49999999999998579, 50.00000000000000000, 11.50000000000000000 ) ) ;
#36309=VERTEX_POINT ( 'NONE', #5948 ) ;
#36315=CARTESIAN_POINT ( 'NONE',  ( 3.094860106618431583, 147.0949999999999704, 9.525000000000000355 ) ) ;
#36329=CIRCLE ( 'NONE', #60977, 0.5000000000000004441 ) ;
#36330=EDGE_CURVE ( 'NONE', #12034, #40909, #26182, .T. ) ;
#36333=SURFACE_STYLE_FILL_AREA ( #27687 ) ;
#36335=AXIS2_PLACEMENT_3D ( 'NONE', #22490, #65400, #22844 ) ;
#36338=UNCERTAINTY_MEASURE_WITH_UNIT (LENGTH_MEASURE( 1.000000000000000082E-05 ), #39730, 'distance_accuracy_value', 'NONE');
#36339=( NAMED_UNIT ( * ) SI_UNIT ( $, .STERADIAN. ) SOLID_ANGLE_UNIT ( ) );
#36340=CARTESIAN_POINT ( 'NONE',  ( -45.00000000000000000, 9.372809501821778966, 6.584099566153143179 ) ) ;
#36344=CONICAL_SURFACE ( 'NONE', #52098, 5.000000000000004441, 0.7853981633974587151 ) ;
#36347=MECHANICAL_DESIGN_GEOMETRIC_PRESENTATION_REPRESENTATION('',(#18342),#59894);
#36348=EDGE_CURVE ( 'NONE', #11645, #28799, #1430, .T. ) ;
#36349=ORIENTED_EDGE ( 'NONE', *, *, #14593, .T. ) ;
#36350=AXIS2_PLACEMENT_3D ( 'NONE', #27228, #64884, #59245 ) ;
#36351=CARTESIAN_POINT ( 'NONE',  ( -21.02379604162863913, 110.4999999999999858, 10.50000000000000000 ) ) ;
#36353=EDGE_CURVE ( 'NONE', #31691, #28799, #16553, .T. ) ;
#36358=CARTESIAN_POINT ( 'NONE',  ( 3.094860106618435136, 118.2949999999999875, -9.525000000000000355 ) ) ;
#36359=CONICAL_SURFACE ( 'NONE', #68864, 22.49999999999999645, 0.7853981633974239651 ) ;
#36362=CARTESIAN_POINT ( 'NONE',  ( 8.102448949553181734, 122.1049999999999898, -5.886773742842746238 ) ) ;
#36363=EDGE_CURVE ( 'NONE', #27627, #31626, #11579, .T. ) ;
#36366=ORIENTED_EDGE ( 'NONE', *, *, #13098, .T. ) ;
#36367=CARTESIAN_POINT ( 'NONE',  ( 9.058813317711338797, 142.9550000000000125, -2.943386871421372675 ) ) ;
#36368=UNCERTAINTY_MEASURE_WITH_UNIT (LENGTH_MEASURE( 1.000000000000000082E-05 ), #45424, 'distance_accuracy_value', 'NONE');
#36369=DIRECTION ( 'NONE',  ( 1.000000000000000000, 0.000000000000000000, 0.000000000000000000 ) ) ;
#36372=ORIENTED_EDGE ( 'NONE', *, *, #26144, .F. ) ;
#36376=( NAMED_UNIT ( * ) PLANE_ANGLE_UNIT ( ) SI_UNIT ( $, .RADIAN. ) );
#36380=CARTESIAN_POINT ( 'NONE',  ( 5.237322049151770464, 111.7848139822559972, -6.367445604021527039 ) ) ;
#36381=AXIS2_PLACEMENT_3D ( 'NONE', #48668, #15951, #55633 ) ;
#36383=SURFACE_STYLE_USAGE ( .BOTH. , #21540 ) ;
#36384=ORIENTED_EDGE ( 'NONE', *, *, #40363, .T. ) ;
#36387=ORIENTED_EDGE ( 'NONE', *, *, #68811, .F. ) ;
#36391=CIRCLE ( 'NONE', #18376, 5.500000000000005329 ) ;
#36396=CIRCLE ( 'NONE', #23984, 0.4999999999999991118 ) ;
#36398=CARTESIAN_POINT ( 'NONE',  ( 5.598654528085805993, 153.2450000000000045, 7.705886871421374629 ) ) ;
#36403=ORIENTED_EDGE ( 'NONE', *, *, #12347, .T. ) ;
#36404=DIRECTION ( 'NONE',  ( 0.000000000000000000, 0.000000000000000000, -1.000000000000000000 ) ) ;
#36408=AXIS2_PLACEMENT_3D ( 'NONE', #65701, #35074, #47415 ) ;
#36410=CARTESIAN_POINT ( 'NONE',  ( 8.102448949553181734, 123.3949999999999676, 5.886773742842750679 ) ) ;
#36413=SURFACE_STYLE_USAGE ( .BOTH. , #3984 ) ;
#36414=AXIS2_PLACEMENT_3D ( 'NONE', #55809, #28002, #49512 ) ;
#36422=CARTESIAN_POINT ( 'NONE',  ( -44.99154893936434263, 9.591540374752314690, -3.105018539189321913 ) ) ;
#36424=AXIS2_PLACEMENT_3D ( 'NONE', #584, #17212, #22109 ) ;
#36426=DIRECTION ( 'NONE',  ( -0.6216216216216311485, -0.7833176619561784682, 0.000000000000000000 ) ) ;
#36427=DIRECTION ( 'NONE',  ( 0.000000000000000000, 1.000000000000000000, -0.000000000000000000 ) ) ;
#36432=MECHANICAL_DESIGN_GEOMETRIC_PRESENTATION_REPRESENTATION('',(#17339),#27354);
#36433=DIRECTION ( 'NONE',  ( 1.000000000000000000, 0.000000000000000000, 0.000000000000000000 ) ) ;
#36437=CONICAL_SURFACE ( 'NONE', #38687, 5.000000000000004441, 0.7853981633974587151 ) ;
#36440=EDGE_CURVE ( 'NONE', #69284, #68902, #64362, .T. ) ;
#36441=CARTESIAN_POINT ( 'NONE',  ( 71.49999999999998579, 99.99999999999998579, -7.000000000000000000 ) ) ;
#36445=CARTESIAN_POINT ( 'NONE',  ( -8.437984349512095861, 136.8070736234661808, -5.166775262442723748E-16 ) ) ;
#36451=UNCERTAINTY_MEASURE_WITH_UNIT (LENGTH_MEASURE( 1.000000000000000082E-05 ), #48361, 'distance_accuracy_value', 'NONE');
#36453=ORIENTED_EDGE ( 'NONE', *, *, #24318, .F. ) ;
#36455=CARTESIAN_POINT ( 'NONE',  ( 6.826472737025121695, 143.4929263765338305, -4.959722759717905660 ) ) ;
#36456=EDGE_LOOP ( 'NONE', ( #16049, #8051, #59153, #15376 ) ) ;
#36459=ORIENTED_EDGE ( 'NONE', *, *, #29248, .T. ) ;
#36460=( GEOMETRIC_REPRESENTATION_CONTEXT ( 3 ) GLOBAL_UNCERTAINTY_ASSIGNED_CONTEXT ( ( #34239 ) ) GLOBAL_UNIT_ASSIGNED_CONTEXT ( ( #24472, #13942, #51937 ) ) REPRESENTATION_CONTEXT ( 'NONE', 'WORKASPACE' ) );
#36461=( NAMED_UNIT ( * ) PLANE_ANGLE_UNIT ( ) SI_UNIT ( $, .RADIAN. ) );
#36466=FILL_AREA_STYLE_COLOUR ( '', #4249 ) ;
#36467=ORIENTED_EDGE ( 'NONE', *, *, #64613, .T. ) ;
#36475=CARTESIAN_POINT ( 'NONE',  ( 3.094860106618435136, 127.2949999999999875, -9.525000000000000355 ) ) ;
#36481=SURFACE_STYLE_FILL_AREA ( #9727 ) ;
#36482=DIRECTION ( 'NONE',  ( -0.000000000000000000, -0.000000000000000000, -1.000000000000000000 ) ) ;
#36484=( LENGTH_UNIT ( ) NAMED_UNIT ( * ) SI_UNIT ( .MILLI., .METRE. ) );
#36486=CARTESIAN_POINT ( 'NONE',  ( -75.00000000000000000, 9.708372675170620525, 6.000000000000000888 ) ) ;
#36490=( BOUNDED_CURVE ( )  B_SPLINE_CURVE ( 2, ( #12531, #51231, #12890, #33997, #67398, #66008, #23116, #28348, #18844, #2977, #45971 ),
 .UNSPECIFIED., .F., .F. ) 
 B_SPLINE_CURVE_WITH_KNOTS ( ( 3, 2, 2, 2, 2, 3 ),
 ( 0.2058823529411763498, 0.2117647058823528272, 0.2176470588235293047, 0.2235294117647058099, 0.2294117647058822596, 0.2352941176470587370 ),
 .UNSPECIFIED. ) 
 CURVE ( )  GEOMETRIC_REPRESENTATION_ITEM ( )  RATIONAL_B_SPLINE_CURVE ( ( 1.000000000000000888, 0.9510565162951526430, 1.000000000000000000, 0.9510565162951535312, 1.000000000000000000, 0.9510565162951535312, 1.000000000000000000, 0.9510565162951535312, 1.000000000000000000, 0.9510565162951541973, 0.9999999999999993339 ) ) 
 REPRESENTATION_ITEM ( '' )  );
#36491=ORIENTED_EDGE ( 'NONE', *, *, #61075, .F. ) ;
#36494=CARTESIAN_POINT ( 'NONE',  ( -79.99999999999998579, 50.00000000000000000, -12.00000000000000000 ) ) ;
#36495=CARTESIAN_POINT ( 'NONE',  ( -75.50000000000000000, 64.49137674618943095, 9.500000000000001776 ) ) ;
#36500=AXIS2_PLACEMENT_3D ( 'NONE', #46107, #51013, #13021 ) ;
#36502=ADVANCED_FACE ( 'NONE', ( #35114 ), #49862, .T. ) ;
#36503=CARTESIAN_POINT ( 'NONE',  ( 0.000000000000000000, 152.5550000000000068, -9.525000000000000355 ) ) ;
#36505=SURFACE_STYLE_FILL_AREA ( #69171 ) ;
#36512=DIRECTION ( 'NONE',  ( 0.000000000000000000, 0.000000000000000000, 1.000000000000000000 ) ) ;
#36513=CARTESIAN_POINT ( 'NONE',  ( -74.99999999999998579, 50.00000000000000000, -7.000000000000000000 ) ) ;
#36515=EDGE_CURVE ( 'NONE', #12616, #44582, #36396, .T. ) ;
#36516=DIRECTION ( 'NONE',  ( 1.000000000000000000, -0.000000000000000000, -0.000000000000000000 ) ) ;
#36517=ORIENTED_EDGE ( 'NONE', *, *, #2748, .F. ) ;
#36524=EDGE_CURVE ( 'NONE', #44927, #4250, #62413, .T. ) ;
#36531=DIRECTION ( 'NONE',  ( 0.000000000000000000, -1.000000000000000000, 0.000000000000000000 ) ) ;
#36532=AXIS2_PLACEMENT_3D ( 'NONE', #45927, #19504, #35703 ) ;
#36535=CARTESIAN_POINT ( 'NONE',  ( 5.598654528085805993, 118.3549999999999898, 7.705886871421374629 ) ) ;
#36537=CARTESIAN_POINT ( 'NONE',  ( 45.00000000000000000, 9.639620389971920389, 6.999999999999999112 ) ) ;
#36538=COLOUR_RGB ( '', 0.40784314, 0.44705882, 0.49803922) ;
#36542=ORIENTED_EDGE ( 'NONE', *, *, #16409, .T. ) ;
#36543=AXIS2_PLACEMENT_3D ( 'NONE', #57419, #9247, #30666 ) ;
#36544=CARTESIAN_POINT ( 'NONE',  ( -9.451804584015965460, 110.5000000000000426, 1.257324542065831441 ) ) ;
#36545=SURFACE_STYLE_USAGE ( .BOTH. , #21336 ) ;
#36548=CARTESIAN_POINT ( 'NONE',  ( -6.826472737025120807, 156.9929263765338305, 4.959722759717906548 ) ) ;
#36551=FACE_OUTER_BOUND ( 'NONE', #41210, .T. ) ;
#36552=ORIENTED_EDGE ( 'NONE', *, *, #12714, .F. ) ;
#36553=CARTESIAN_POINT ( 'NONE',  ( 20.68718488045382742, 114.6829008731431543, -10.00000000000011724 ) ) ;
#36554=EDGE_LOOP ( 'NONE', ( #45957, #28335, #40924, #20133 ) ) ;
#36555=SURFACE_SIDE_STYLE ('',( #26279 ) ) ;
#36558=DIRECTION ( 'NONE',  ( 0.000000000000000000, -1.000000000000000000, -0.000000000000000000 ) ) ;
#36563=CARTESIAN_POINT ( 'NONE',  ( -74.99999999999998579, 50.00000000000000000, 9.500000000000000000 ) ) ;
#36567=EDGE_LOOP ( 'NONE', ( #9048, #54218 ) ) ;
#36573=SURFACE_SIDE_STYLE ('',( #15100 ) ) ;
#36580=( GEOMETRIC_REPRESENTATION_CONTEXT ( 3 ) GLOBAL_UNCERTAINTY_ASSIGNED_CONTEXT ( ( #11436 ) ) GLOBAL_UNIT_ASSIGNED_CONTEXT ( ( #1647, #60088, #11550 ) ) REPRESENTATION_CONTEXT ( 'NONE', 'WORKASPACE' ) );
#36583=SURFACE_SIDE_STYLE ('',( #57283 ) ) ;
#36588=CARTESIAN_POINT ( 'NONE',  ( 9.189246016727048882, 154.4999999999999432, 2.545277832678562557 ) ) ;
#36590=CARTESIAN_POINT ( 'NONE',  ( -75.41277076832422210, 36.04285368632835684, -9.691745530926853647 ) ) ;
#36591=EDGE_CURVE ( 'NONE', #12165, #4746, #42023, .T. ) ;
#36594=EDGE_CURVE ( 'NONE', #11684, #44405, #24204, .T. ) ;
#36595=CARTESIAN_POINT ( 'NONE',  ( -8.102448949553181734, 126.6050000000000040, 5.886773742842747126 ) ) ;
#36598=AXIS2_PLACEMENT_3D ( 'NONE', #23947, #44430, #45107 ) ;
#36601=AXIS2_PLACEMENT_3D ( 'NONE', #14786, #36264, #57689 ) ;
#36603=DIRECTION ( 'NONE',  ( 1.000000000000000000, -6.938893903907222067E-15, 0.000000000000000000 ) ) ;
#36605=EDGE_CURVE ( 'NONE', #22912, #28559, #45712, .T. ) ;
#36606=( GEOMETRIC_REPRESENTATION_CONTEXT ( 3 ) GLOBAL_UNCERTAINTY_ASSIGNED_CONTEXT ( ( #31367 ) ) GLOBAL_UNIT_ASSIGNED_CONTEXT ( ( #59264, #38224, #26235 ) ) REPRESENTATION_CONTEXT ( 'NONE', 'WORKASPACE' ) );
#36608=CARTESIAN_POINT ( 'NONE',  ( 23.21231517720797655, 117.4999999999999716, -7.000000000000000000 ) ) ;
#36609=ADVANCED_FACE ( 'NONE', ( #23862 ), #15032, .F. ) ;
#36613=DIRECTION ( 'NONE',  ( -1.000000000000000000, -3.469446951953610639E-15, -0.000000000000000000 ) ) ;
#36622=DIRECTION ( 'NONE',  ( -0.000000000000000000, -0.000000000000000000, 1.000000000000000000 ) ) ;
#36625=CARTESIAN_POINT ( 'NONE',  ( -71.50000000000000000, 14.49137674618942562, 7.000000000000000000 ) ) ;
#36626=( LENGTH_UNIT ( ) NAMED_UNIT ( * ) SI_UNIT ( .MILLI., .METRE. ) );
#36627=ORIENTED_EDGE ( 'NONE', *, *, #57435, .F. ) ;
#36628=AXIS2_PLACEMENT_3D ( 'NONE', #54063, #22766, #38289 ) ;
#36630=CARTESIAN_POINT ( 'NONE',  ( -1.166476076187854022E-15, 146.9449999999999932, 9.525000000000000355 ) ) ;
#36633=CARTESIAN_POINT ( 'NONE',  ( -5.598654528085808657, 147.7549999999999955, 7.705886871421373741 ) ) ;
#36635=ORIENTED_EDGE ( 'NONE', *, *, #9867, .F. ) ;
#36636=CARTESIAN_POINT ( 'NONE',  ( 2.607480562269076430, 128.7929263765338135, -8.025000000000000355 ) ) ;
#36637=DIRECTION ( 'NONE',  ( 0.000000000000000000, 0.000000000000000000, -1.000000000000000000 ) ) ;
#36639=CARTESIAN_POINT ( 'NONE',  ( 45.65811388300841855, 10.21937129433612235, -6.000000000000000000 ) ) ;
#36644=( GEOMETRIC_REPRESENTATION_CONTEXT ( 3 ) GLOBAL_UNCERTAINTY_ASSIGNED_CONTEXT ( ( #46676 ) ) GLOBAL_UNIT_ASSIGNED_CONTEXT ( ( #8, #64458, #22235 ) ) REPRESENTATION_CONTEXT ( 'NONE', 'WORKASPACE' ) );
#36645=( LENGTH_UNIT ( ) NAMED_UNIT ( * ) SI_UNIT ( .MILLI., .METRE. ) );
#36646=CARTESIAN_POINT ( 'NONE',  ( -48.50000000000000000, 99.99999999999992895, 7.000000000000000000 ) ) ;
#36648=ORIENTED_EDGE ( 'NONE', *, *, #3352, .F. ) ;
#36651=LINE ( 'NONE', #10904, #369 ) ;
#36653=CARTESIAN_POINT ( 'NONE',  ( 75.00000000000000000, 19.95407619327928828, 6.799666827783449108 ) ) ;
#36661=ADVANCED_FACE ( 'NONE', ( #25930 ), #65556, .F. ) ;
#36663=CARTESIAN_POINT ( 'NONE',  ( -24.21231517720798010, 112.4999999999999858, -9.500000000000000000 ) ) ;
#36664=ORIENTED_EDGE ( 'NONE', *, *, #55922, .T. ) ;
#36665=CIRCLE ( 'NONE', #25361, 0.5000000000000004441 ) ;
#36667=SURFACE_STYLE_FILL_AREA ( #37710 ) ;
#36671=CARTESIAN_POINT ( 'NONE',  ( 2.607480562269075985, 126.9070736234661467, -8.025000000000000355 ) ) ;
#36672=AXIS2_PLACEMENT_3D ( 'NONE', #56213, #61827, #34076 ) ;
#36673=ADVANCED_FACE ( 'NONE', ( #68877 ), #25250, .F. ) ;
#36674=CARTESIAN_POINT ( 'NONE',  ( -1.166476076187854022E-15, 146.9449999999999932, 9.525000000000000355 ) ) ;
#36677=STYLED_ITEM ( 'NONE', ( #32484 ), #49822 ) ;
#36679=STYLED_ITEM ( 'NONE', ( #24140 ), #5396 ) ;
#36686=FILL_AREA_STYLE ('',( #45586 ) ) ;
#36689=FILL_AREA_STYLE_COLOUR ( '', #2178 ) ;
#36691=( NAMED_UNIT ( * ) SI_UNIT ( $, .STERADIAN. ) SOLID_ANGLE_UNIT ( ) );
#36697=( LENGTH_UNIT ( ) NAMED_UNIT ( * ) SI_UNIT ( .MILLI., .METRE. ) );
#36698=CARTESIAN_POINT ( 'NONE',  ( -45.00000000000000000, 9.701644063436994259, 6.099264075924462958 ) ) ;
#36699=CARTESIAN_POINT ( 'NONE',  ( 23.21231517720797655, 117.4999999999999716, -9.500000000000000000 ) ) ;
#36701=ORIENTED_EDGE ( 'NONE', *, *, #42500, .T. ) ;
#36705=SURFACE_STYLE_USAGE ( .BOTH. , #16274 ) ;
#36706=ORIENTED_EDGE ( 'NONE', *, *, #39558, .F. ) ;
#36709=CARTESIAN_POINT ( 'NONE',  ( 3.094860106618435136, 124.2949999999999733, -9.525000000000000355 ) ) ;
#36710=FACE_BOUND ( 'NONE', #21076, .T. ) ;
#36713=CARTESIAN_POINT ( 'NONE',  ( 3.094860106618435136, 119.4049999999999727, -9.525000000000000355 ) ) ;
#36715=PRESENTATION_STYLE_ASSIGNMENT (( #3203 ) ) ;
#36716=PRODUCT_DEFINITION_SHAPE ( 'NONE', 'NONE',  #35663 ) ;
#36718=CARTESIAN_POINT ( 'NONE',  ( -3.094860106618432471, 143.7050000000000125, -9.525000000000000355 ) ) ;
#36721=STYLED_ITEM ( 'NONE', ( #40159 ), #50223 ) ;
#36724=DIRECTION ( 'NONE',  ( 0.000000000000000000, 1.000000000000000000, 0.000000000000000000 ) ) ;
#36727=EDGE_LOOP ( 'NONE', ( #50694, #62121, #59781, #17706 ) ) ;
#36728=CARTESIAN_POINT ( 'NONE',  ( 7.514523004098860426, 111.2423389163705139, 4.578433682763816570 ) ) ;
#36729=DIRECTION ( 'NONE',  ( 1.000000000000000000, 0.000000000000000000, 0.000000000000000000 ) ) ;
#36730=DIRECTION ( 'NONE',  ( -1.000000000000000000, -0.000000000000000000, -0.000000000000000000 ) ) ;
#36733=( LENGTH_UNIT ( ) NAMED_UNIT ( * ) SI_UNIT ( .MILLI., .METRE. ) );
#36734=ORIENTED_EDGE ( 'NONE', *, *, #27454, .T. ) ;
#36744=CARTESIAN_POINT ( 'NONE',  ( 8.102448949553181734, 147.9949999999999193, -5.886773742842746238 ) ) ;
#36751=ADVANCED_FACE ( 'NONE', ( #33312 ), #44251, .F. ) ;
#36753=CARTESIAN_POINT ( 'NONE',  ( 5.598654528085809545, 118.1449999999999818, -7.705886871421373741 ) ) ;
#36761=DIRECTION ( 'NONE',  ( -0.000000000000000000, 1.000000000000000000, -0.000000000000000000 ) ) ;
#36762=STYLED_ITEM ( 'NONE', ( #56846 ), #65101 ) ;
#36763=EDGE_CURVE ( 'NONE', #11295, #7436, #43902, .T. ) ;
#36766=CARTESIAN_POINT ( 'NONE',  ( 72.49999999999998579, 64.07124727947029896, 10.00000000000000000 ) ) ;
#36773=( LENGTH_UNIT ( ) NAMED_UNIT ( * ) SI_UNIT ( .MILLI., .METRE. ) );
#36780=FILL_AREA_STYLE ('',( #20551 ) ) ;
#36783=DIRECTION ( 'NONE',  ( 1.000000000000000000, 0.000000000000000000, 0.000000000000000000 ) ) ;
#36784=CARTESIAN_POINT ( 'NONE',  ( -2.607480562269075097, 140.4070736234661751, 8.025000000000000355 ) ) ;
#36787=LINE ( 'NONE', #53281, #25984 ) ;
#36790=FILL_AREA_STYLE_COLOUR ( '', #49019 ) ;
#36791=DIRECTION ( 'NONE',  ( 0.000000000000000000, 0.000000000000000000, 1.000000000000000000 ) ) ;
#36792=FACE_OUTER_BOUND ( 'NONE', #62854, .T. ) ;
#36794=ORIENTED_EDGE ( 'NONE', *, *, #57620, .F. ) ;
#36798=FACE_OUTER_BOUND ( 'NONE', #14247, .T. ) ;
#36799=LINE ( 'NONE', #47729, #63767 ) ;
#36805=ORIENTED_EDGE ( 'NONE', *, *, #9393, .T. ) ;
#36812=CARTESIAN_POINT ( 'NONE',  ( -8.102448949553179958, 121.8949999999999818, -5.886773742842749790 ) ) ;
#36813=EDGE_CURVE ( 'NONE', #56663, #3150, #35512, .T. ) ;
#36815=EDGE_CURVE ( 'NONE', #60196, #51351, #52139, .T. ) ;
#36818=ADVANCED_FACE ( 'NONE', ( #32966, #54401 ), #45284, .F. ) ;
#36819=CARTESIAN_POINT ( 'NONE',  ( 44.50000000000000000, 10.36037961002804408, 3.500000000000000000 ) ) ;
#36820=CARTESIAN_POINT ( 'NONE',  ( -15.98999599679679839, 117.9999999999999716, -10.00000000000000000 ) ) ;
#36824=ADVANCED_FACE ( 'NONE', ( #35032 ), #24032, .F. ) ;
#36826=CYLINDRICAL_SURFACE ( 'NONE', #32481, 8.025000000000000355 ) ;
#36834=( NAMED_UNIT ( * ) PLANE_ANGLE_UNIT ( ) SI_UNIT ( $, .RADIAN. ) );
#36835=UNCERTAINTY_MEASURE_WITH_UNIT (LENGTH_MEASURE( 1.000000000000000082E-05 ), #38466, 'distance_accuracy_value', 'NONE');
#36837=CARTESIAN_POINT ( 'NONE',  ( -9.058813317711337021, 156.1550000000000011, -2.943386871421374895 ) ) ;
#36838=FILL_AREA_STYLE ('',( #37895 ) ) ;
#36851=EDGE_LOOP ( 'NONE', ( #25352, #15201, #53755, #24603 ) ) ;
#36852=VERTEX_POINT ( 'NONE', #55792 ) ;
#36853=TOROIDAL_SURFACE ( 'NONE', #4240, 10.50000000000000533, 0.5000000000000000000 ) ;
#36854=CARTESIAN_POINT ( 'NONE',  ( 6.826472737025119919, 114.0070736234661695, 4.959722759717908325 ) ) ;
#36856=SURFACE_SIDE_STYLE ('',( #15397 ) ) ;
#36857=DIRECTION ( 'NONE',  ( 1.000000000000000000, 0.000000000000000000, 0.000000000000000000 ) ) ;
#36858=COLOUR_RGB ( '', 0.40784314, 0.44705882, 0.49803922) ;
#36862=MECHANICAL_DESIGN_GEOMETRIC_PRESENTATION_REPRESENTATION('',(#27808),#43824);
#36864=CARTESIAN_POINT ( 'NONE',  ( -20.83146879675249963, 149.9524772093542708, 9.749920261344563244 ) ) ;
#36866=CARTESIAN_POINT ( 'NONE',  ( 9.058813317711337021, 115.6549999999999869, 2.943386871421375783 ) ) ;
#36868=PRESENTATION_STYLE_ASSIGNMENT (( #42171 ) ) ;
#36872=CARTESIAN_POINT ( 'NONE',  ( 6.088690765491501011, 153.9475726876337376, -6.602727378241971756 ) ) ;
#36873=UNCERTAINTY_MEASURE_WITH_UNIT (LENGTH_MEASURE( 1.000000000000000082E-05 ), #68256, 'distance_accuracy_value', 'NONE');
#36875=CARTESIAN_POINT ( 'NONE',  ( 4.716976649647099507, 155.6429263765338078, -6.492361379858953008 ) ) ;
#36878=CARTESIAN_POINT ( 'NONE',  ( -20.88905466131707200, 149.9999999999999432, -9.626351540309148191 ) ) ;
#36882=CYLINDRICAL_SURFACE ( 'NONE', #39505, 0.5000000000000004441 ) ;
#36890=EDGE_CURVE ( 'NONE', #25507, #49241, #33027, .T. ) ;
#36891=DIRECTION ( 'NONE',  ( 0.000000000000000000, 0.000000000000000000, 1.000000000000000000 ) ) ;
#36893=CARTESIAN_POINT ( 'NONE',  ( -40.99999999999997868, 9.999999999999980460, 3.000000000000000000 ) ) ;
#36896=MECHANICAL_DESIGN_GEOMETRIC_PRESENTATION_REPRESENTATION('',(#819),#10999);
#36899=VECTOR ( 'NONE', #20955, 1000.000000000000000 ) ;
#36901=DIRECTION ( 'NONE',  ( 0.000000000000000000, 0.000000000000000000, 1.000000000000000000 ) ) ;
#36902=( NAMED_UNIT ( * ) SI_UNIT ( $, .STERADIAN. ) SOLID_ANGLE_UNIT ( ) );
#36904=SURFACE_STYLE_FILL_AREA ( #68535 ) ;
#36906=CARTESIAN_POINT ( 'NONE',  ( -12.72792206135785520, 114.9999999999999574, 10.50000000000000000 ) ) ;
#36910=CIRCLE ( 'NONE', #41416, 0.5000000000000004441 ) ;
#36917=CARTESIAN_POINT ( 'NONE',  ( 8.570369358082762901, 154.5000000000000000, 4.179281154892271033 ) ) ;
#36919=SURFACE_SIDE_STYLE ('',( #57646 ) ) ;
#36921=CARTESIAN_POINT ( 'NONE',  ( 10.01517768586949231, 130.8049999999999784, 1.839758294383810543E-15 ) ) ;
#36922=CARTESIAN_POINT ( 'NONE',  ( -74.50000000000000000, 64.49137674618943095, 9.500000000000000000 ) ) ;
#36924=CARTESIAN_POINT ( 'NONE',  ( 45.50000000000000000, 99.99999999999992895, -10.00000000000000000 ) ) ;
#36925=UNCERTAINTY_MEASURE_WITH_UNIT (LENGTH_MEASURE( 1.000000000000000082E-05 ), #56067, 'distance_accuracy_value', 'NONE');
#36927=CARTESIAN_POINT ( 'NONE',  ( -75.50000000000000000, 64.49137674618943095, 9.500000000000001776 ) ) ;
#36930=DIRECTION ( 'NONE',  ( -1.156482317317873451E-16, -1.000000000000000000, 0.000000000000000000 ) ) ;
#36932=DIRECTION ( 'NONE',  ( 0.000000000000000000, 0.000000000000000000, -1.000000000000000000 ) ) ;
#36934=CIRCLE ( 'NONE', #6540, 0.5000000000000004441 ) ;
#36936=PRESENTATION_STYLE_ASSIGNMENT (( #9499 ) ) ;
#36942=DIRECTION ( 'NONE',  ( 0.000000000000000000, 0.000000000000000000, 1.000000000000000000 ) ) ;
#36944=SURFACE_STYLE_USAGE ( .BOTH. , #63970 ) ;
#36945=MECHANICAL_DESIGN_GEOMETRIC_PRESENTATION_REPRESENTATION('',(#41412),#43685);
#36950=CARTESIAN_POINT ( 'NONE',  ( 6.826472737025121695, 129.6070736234661638, -4.959722759717905660 ) ) ;
#36957=CARTESIAN_POINT ( 'NONE',  ( 9.058813317711337021, 150.5449999999999875, 2.943386871421375783 ) ) ;
#36960=VERTEX_POINT ( 'NONE', #35394 ) ;
#36962=CARTESIAN_POINT ( 'NONE',  ( -9.058813317711338797, 153.4549999999999841, 2.943386871421373563 ) ) ;
#36963=( NAMED_UNIT ( * ) SI_UNIT ( $, .STERADIAN. ) SOLID_ANGLE_UNIT ( ) );
#36966=CARTESIAN_POINT ( 'NONE',  ( 7.632228543268607446, 128.0429263765338135, 2.479861379858954606 ) ) ;
#36967=CARTESIAN_POINT ( 'NONE',  ( -72.49999999999998579, 64.07124727947029896, 10.00000000000000000 ) ) ;
#36968=UNCERTAINTY_MEASURE_WITH_UNIT (LENGTH_MEASURE( 1.000000000000000082E-05 ), #43826, 'distance_accuracy_value', 'NONE');
#36969=CARTESIAN_POINT ( 'NONE',  ( -74.88655845637370589, 36.30736609777607526, -9.975975838750319014 ) ) ;
#36973=FILL_AREA_STYLE_COLOUR ( '', #5884 ) ;
#36981=UNCERTAINTY_MEASURE_WITH_UNIT (LENGTH_MEASURE( 1.000000000000000082E-05 ), #11403, 'distance_accuracy_value', 'NONE');
#36985=( NAMED_UNIT ( * ) SI_UNIT ( $, .STERADIAN. ) SOLID_ANGLE_UNIT ( ) );
#36995=DIRECTION ( 'NONE',  ( 1.000000000000000000, 0.000000000000000000, 0.000000000000000000 ) ) ;
#36996=FILL_AREA_STYLE_COLOUR ( '', #11054 ) ;
#36997=STYLED_ITEM ( 'NONE', ( #43244 ), #20089 ) ;
#37000=CARTESIAN_POINT ( 'NONE',  ( 0.000000000000000000, 113.9429263765338192, -8.025000000000000355 ) ) ;
#37002=STYLED_ITEM ( 'NONE', ( #57169 ), #4509 ) ;
#37004=( BOUNDED_CURVE ( )  B_SPLINE_CURVE ( 2, ( #5544, #43598, #11534, #48179, #26994, #20721, #64989, #37638, #42235, #37980, #53430 ),
 .UNSPECIFIED., .F., .F. ) 
 B_SPLINE_CURVE_WITH_KNOTS ( ( 3, 2, 2, 2, 2, 3 ),
 ( 0.4117647058823530326, 0.4176470588235295378, 0.4235294117647059875, 0.4294117647058824372, 0.4352941176470589424, 0.4411764705882353921 ),
 .UNSPECIFIED. ) 
 CURVE ( )  GEOMETRIC_REPRESENTATION_ITEM ( )  RATIONAL_B_SPLINE_CURVE ( ( 0.9999999999999991118, 0.9510565162951544194, 1.000000000000000000, 0.9510565162951535312, 1.000000000000000000, 0.9510565162951535312, 1.000000000000000000, 0.9510565162951535312, 1.000000000000000000, 0.9510565162951526430, 1.000000000000000888 ) ) 
 REPRESENTATION_ITEM ( '' )  );
#37005=DIRECTION ( 'NONE',  ( 0.000000000000000000, 1.000000000000000000, 0.000000000000000000 ) ) ;
#37006=ADVANCED_FACE ( 'NONE', ( #14997 ), #8334, .T. ) ;
#37013=CARTESIAN_POINT ( 'NONE',  ( 3.094860106618431583, 150.0949999999999420, 9.525000000000000355 ) ) ;
#37015=SURFACE_STYLE_FILL_AREA ( #47223 ) ;
#37016=STYLED_ITEM ( 'NONE', ( #62113 ), #14700 ) ;
#37018=UNCERTAINTY_MEASURE_WITH_UNIT (LENGTH_MEASURE( 1.000000000000000082E-05 ), #49008, 'distance_accuracy_value', 'NONE');
#37019=MECHANICAL_DESIGN_GEOMETRIC_PRESENTATION_REPRESENTATION('',(#58305),#6608);
#37028=CARTESIAN_POINT ( 'NONE',  ( 0.000000000000000000, 154.9999999999999716, 0.000000000000000000 ) ) ;
#37030=ORIENTED_EDGE ( 'NONE', *, *, #14168, .F. ) ;
#37034=CARTESIAN_POINT ( 'NONE',  ( -45.00000000000000000, 8.062885781073939384, 6.000000000000002665 ) ) ;
#37036=CIRCLE ( 'NONE', #20097, 8.999999999999994671 ) ;
#37041=STYLED_ITEM ( 'NONE', ( #62154 ), #10382 ) ;
#37042=CIRCLE ( 'NONE', #54947, 7.500000000000007105 ) ;
#37043=CARTESIAN_POINT ( 'NONE',  ( -9.058813317711337021, 122.0449999999999875, -2.943386871421374895 ) ) ;
#37045=AXIS2_PLACEMENT_3D ( 'NONE', #56446, #25474, #57859 ) ;
#37046=VERTEX_POINT ( 'NONE', #35736 ) ;
#37047=EDGE_CURVE ( 'NONE', #15297, #40156, #20592, .T. ) ;
#37048=( LENGTH_UNIT ( ) NAMED_UNIT ( * ) SI_UNIT ( .MILLI., .METRE. ) );
#37049=CARTESIAN_POINT ( 'NONE',  ( -9.058813317711338797, 117.4549999999999841, 2.943386871421373563 ) ) ;
#37051=CARTESIAN_POINT ( 'NONE',  ( -41.03182778381239615, 107.9802461459568690, -3.207526698639570295 ) ) ;
#37052=VERTEX_POINT ( 'NONE', #57170 ) ;
#37053=CARTESIAN_POINT ( 'NONE',  ( -3.094860106618434248, 144.9050000000000011, 9.525000000000000355 ) ) ;
#37054=UNCERTAINTY_MEASURE_WITH_UNIT (LENGTH_MEASURE( 1.000000000000000082E-05 ), #10221, 'distance_accuracy_value', 'NONE');
#37060=( LENGTH_UNIT ( ) NAMED_UNIT ( * ) SI_UNIT ( .MILLI., .METRE. ) );
#37061=ORIENTED_EDGE ( 'NONE', *, *, #32707, .F. ) ;
#37062=AXIS2_PLACEMENT_3D ( 'NONE', #23364, #2554, #40260 ) ;
#37064=( NAMED_UNIT ( * ) PLANE_ANGLE_UNIT ( ) SI_UNIT ( $, .RADIAN. ) );
#37075=CIRCLE ( 'NONE', #3276, 0.5000000000000004441 ) ;
#37076=ADVANCED_FACE ( 'NONE', ( #25509 ), #47022, .F. ) ;
#37079=ORIENTED_EDGE ( 'NONE', *, *, #47898, .F. ) ;
#37082=AXIS2_PLACEMENT_3D ( 'NONE', #17492, #11487, #38621 ) ;
#37085=CARTESIAN_POINT ( 'NONE',  ( -10.01517768586949408, 152.1949999999999932, -6.132527647946036459E-16 ) ) ;
#37089=VERTEX_POINT ( 'NONE', #37866 ) ;
#37091=CARTESIAN_POINT ( 'NONE',  ( 49.12162162162162105, 13.70805908423323238, 10.00000000000000000 ) ) ;
#37093=AXIS2_PLACEMENT_3D ( 'NONE', #2179, #49767, #23710 ) ;
#37096=CARTESIAN_POINT ( 'NONE',  ( 9.058813317711337021, 120.5449999999999875, 2.943386871421375783 ) ) ;
#37098=VECTOR ( 'NONE', #29576, 1000.000000000000000 ) ;
#37099=CIRCLE ( 'NONE', #40433, 0.5000000000000004441 ) ;
#37100=EDGE_CURVE ( 'NONE', #53532, #67533, #33085, .T. ) ;
#37102=CARTESIAN_POINT ( 'NONE',  ( -9.827790563157511022E-16, 145.4429263765338192, 8.025000000000000355 ) ) ;
#37111=CARTESIAN_POINT ( 'NONE',  ( -20.68758241885016247, 114.6823486699484107, -10.00000000000000178 ) ) ;
#37126=EDGE_CURVE ( 'NONE', #37491, #13013, #59594, .T. ) ;
#37127=FACE_OUTER_BOUND ( 'NONE', #68412, .T. ) ;
#37128=CARTESIAN_POINT ( 'NONE',  ( 0.000000000000000000, 87.30187232391182306, 0.000000000000000000 ) ) ;
#37130=CARTESIAN_POINT ( 'NONE',  ( -9.827790563157511022E-16, 140.5570736234661524, 8.025000000000000355 ) ) ;
#37131=ORIENTED_EDGE ( 'NONE', *, *, #31688, .T. ) ;
#37132=CARTESIAN_POINT ( 'NONE',  ( 34.99999999999999289, 99.99999999999997158, -3.500000000000000000 ) ) ;
#37134=UNCERTAINTY_MEASURE_WITH_UNIT (LENGTH_MEASURE( 1.000000000000000082E-05 ), #37584, 'distance_accuracy_value', 'NONE');
#37135=CARTESIAN_POINT ( 'NONE',  ( 4.716976649647096842, 131.8570736234661638, 6.492361379858953896 ) ) ;
#37137=CARTESIAN_POINT ( 'NONE',  ( -44.99999999999977973, 149.9999999999999716, -9.500000000000000000 ) ) ;
#37142=MECHANICAL_DESIGN_GEOMETRIC_PRESENTATION_REPRESENTATION('',(#28063),#20211);
#37143=EDGE_LOOP ( 'NONE', ( #28596, #31346, #1968, #33846 ) ) ;
#37147=CARTESIAN_POINT ( 'NONE',  ( -60.00000000000000000, -2.024042244987997205E-14, 10.00000000000000000 ) ) ;
#37148=STYLED_ITEM ( 'NONE', ( #31335 ), #33134 ) ;
#37151=AXIS2_PLACEMENT_3D ( 'NONE', #65264, #23390, #55403 ) ;
#37154=DIRECTION ( 'NONE',  ( 1.000000000000000000, 0.000000000000000000, 0.000000000000000000 ) ) ;
#37158=ORIENTED_EDGE ( 'NONE', *, *, #23603, .T. ) ;
#37159=PRESENTATION_STYLE_ASSIGNMENT (( #64875 ) ) ;
#37161=DIRECTION ( 'NONE',  ( -0.000000000000000000, 0.000000000000000000, -1.000000000000000000 ) ) ;
#37163=CIRCLE ( 'NONE', #53973, 0.5000000000000004441 ) ;
#37164=CARTESIAN_POINT ( 'NONE',  ( -3.094860106618434248, 122.7949999999999875, 9.525000000000000355 ) ) ;
#37167=CARTESIAN_POINT ( 'NONE',  ( -44.99999999999998579, 119.9999999999999716, -9.500000000000000000 ) ) ;
#37170=( NAMED_UNIT ( * ) SI_UNIT ( $, .STERADIAN. ) SOLID_ANGLE_UNIT ( ) );
#37175=SURFACE_STYLE_FILL_AREA ( #32522 ) ;
#37179=COLOUR_RGB ( '', 0.31764706, 0.68627451, 0.89019608) ;
#37184=CYLINDRICAL_SURFACE ( 'NONE', #31601, 0.5000000000000004441 ) ;
#37186=FILL_AREA_STYLE_COLOUR ( '', #10225 ) ;
#37187=CARTESIAN_POINT ( 'NONE',  ( -44.50000000000000000, 9.499999999999980460, 3.500000000000000000 ) ) ;
#37191=MECHANICAL_DESIGN_GEOMETRIC_PRESENTATION_REPRESENTATION('',(#15833),#27018);
#37196=CARTESIAN_POINT ( 'NONE',  ( 0.000000000000000000, 151.0570736234661524, -8.025000000000000355 ) ) ;
#37200=EDGE_CURVE ( 'NONE', #67825, #21253, #10400, .T. ) ;
#37204=( LENGTH_UNIT ( ) NAMED_UNIT ( * ) SI_UNIT ( .MILLI., .METRE. ) );
#37205=AXIS2_PLACEMENT_3D ( 'NONE', #61773, #23817, #35066 ) ;
#37206=CARTESIAN_POINT ( 'NONE',  ( 4.716976649647096842, 110.8570736234661496, 6.492361379858953896 ) ) ;
#37209=FACE_OUTER_BOUND ( 'NONE', #26021, .T. ) ;
#37210=( GEOMETRIC_REPRESENTATION_CONTEXT ( 3 ) GLOBAL_UNCERTAINTY_ASSIGNED_CONTEXT ( ( #26239 ) ) GLOBAL_UNIT_ASSIGNED_CONTEXT ( ( #43170, #27598, #15704 ) ) REPRESENTATION_CONTEXT ( 'NONE', 'WORKASPACE' ) );
#37212=ORIENTED_EDGE ( 'NONE', *, *, #33751, .F. ) ;
#37215=ADVANCED_FACE ( 'NONE', ( #16729 ), #27576, .F. ) ;
#37218=CARTESIAN_POINT ( 'NONE',  ( 5.598654528085809545, 116.2549999999999812, -7.705886871421373741 ) ) ;
#37220=DIRECTION ( 'NONE',  ( 0.000000000000000000, 0.000000000000000000, -1.000000000000000000 ) ) ;
#37221=EDGE_CURVE ( 'NONE', #20613, #9417, #6106, .T. ) ;
#37223=FILL_AREA_STYLE ('',( #9774 ) ) ;
#37226=CARTESIAN_POINT ( 'NONE',  ( 8.255084434212841771, 153.3156119838025404, 1.257250715558700493 ) ) ;
#37231=ORIENTED_EDGE ( 'NONE', *, *, #48092, .T. ) ;
#37232=CARTESIAN_POINT ( 'NONE',  ( -8.437984349512095861, 156.6929263765338476, -5.166775262442723748E-16 ) ) ;
#37234=PRESENTATION_STYLE_ASSIGNMENT (( #53031 ) ) ;
#37235=CIRCLE ( 'NONE', #23729, 0.5000000000000004441 ) ;
#37237=CARTESIAN_POINT ( 'NONE',  ( 71.62068965517239860, 36.41396814395972115, 9.500000000000000000 ) ) ;
#37239=CARTESIAN_POINT ( 'NONE',  ( 20.51842522107655142, 114.9046575010689821, -10.00000000000000000 ) ) ;
#37243=CARTESIAN_POINT ( 'NONE',  ( 21.02379604162863558, 114.4999999999999574, 10.50000000000000000 ) ) ;
#37245=VECTOR ( 'NONE', #13537, 1000.000000000000000 ) ;
#37247=AXIS2_PLACEMENT_3D ( 'NONE', #68479, #51261, #36512 ) ;
#37248=CARTESIAN_POINT ( 'NONE',  ( -74.10000901193289735, 9.371467124235303814, 6.143012557965066733 ) ) ;
#37249=( LENGTH_UNIT ( ) NAMED_UNIT ( * ) SI_UNIT ( .MILLI., .METRE. ) );
#37253=ORIENTED_EDGE ( 'NONE', *, *, #17214, .F. ) ;
#37255=FACE_OUTER_BOUND ( 'NONE', #46987, .T. ) ;
#37265=( GEOMETRIC_REPRESENTATION_CONTEXT ( 3 ) GLOBAL_UNCERTAINTY_ASSIGNED_CONTEXT ( ( #27698 ) ) GLOBAL_UNIT_ASSIGNED_CONTEXT ( ( #36773, #58881, #26824 ) ) REPRESENTATION_CONTEXT ( 'NONE', 'WORKASPACE' ) );
#37267=CARTESIAN_POINT ( 'NONE',  ( 60.00000000000000000, 1.797044900979284448E-15, 12.00000000000000000 ) ) ;
#37273=FILL_AREA_STYLE_COLOUR ( '', #60700 ) ;
#37274=CIRCLE ( 'NONE', #1196, 23.00000000000000000 ) ;
#37275=CARTESIAN_POINT ( 'NONE',  ( -75.23309145305536560, 36.13215102747564345, -9.842748219394650278 ) ) ;
#37277=CARTESIAN_POINT ( 'NONE',  ( -3.094860106618434248, 135.9050000000000011, 9.525000000000000355 ) ) ;
#37279=CARTESIAN_POINT ( 'NONE',  ( 41.49999999999997868, 9.999999999999980460, -3.000000000000000444 ) ) ;
#37282=FILL_AREA_STYLE ('',( #63954 ) ) ;
#37286=DIRECTION ( 'NONE',  ( 0.000000000000000000, 0.000000000000000000, 1.000000000000000000 ) ) ;
#37292=EDGE_LOOP ( 'NONE', ( #23278, #36701, #32012, #42258 ) ) ;
#37293=CARTESIAN_POINT ( 'NONE',  ( -45.64578147489630311, 8.378235220106981629, -6.482771786488845223 ) ) ;
#37295=CARTESIAN_POINT ( 'NONE',  ( 8.437984349512095861, 131.1929263765338192, 1.550032578732816828E-15 ) ) ;
#37302=ORIENTED_EDGE ( 'NONE', *, *, #57270, .T. ) ;
#37304=ORIENTED_EDGE ( 'NONE', *, *, #69358, .F. ) ;
#37307=DIRECTION ( 'NONE',  ( 0.000000000000000000, 0.000000000000000000, -1.000000000000000000 ) ) ;
#37308=ORIENTED_EDGE ( 'NONE', *, *, #31942, .F. ) ;
#37312=( BOUNDED_CURVE ( )  B_SPLINE_CURVE ( 2, ( #11869, #22083, #43247, #32989, #27329, #54424, #44624, #33666, #6244, #55108, #44278 ),
 .UNSPECIFIED., .F., .F. ) 
 B_SPLINE_CURVE_WITH_KNOTS ( ( 3, 2, 2, 2, 2, 3 ),
 ( 0.7647058823529415683, 0.7705882352941180180, 0.7764705882352943567, 0.7823529411764706953, 0.7882352941176470340, 0.7941176470588233727 ),
 .UNSPECIFIED. ) 
 CURVE ( )  GEOMETRIC_REPRESENTATION_ITEM ( )  RATIONAL_B_SPLINE_CURVE ( ( 0.9999999999999963363, 0.9510565162951571949, 1.000000000000000000, 0.9510565162951535312, 1.000000000000000000, 0.9510565162951535312, 1.000000000000000000, 0.9510565162951535312, 1.000000000000000000, 0.9510565162951544194, 0.9999999999999991118 ) ) 
 REPRESENTATION_ITEM ( '' )  );
#37313=CARTESIAN_POINT ( 'NONE',  ( -8.102448949553181734, 148.8950000000000102, -5.886773742842749790 ) ) ;
#37315=ORIENTED_EDGE ( 'NONE', *, *, #48140, .T. ) ;
#37316=STYLED_ITEM ( 'NONE', ( #56211 ), #25190 ) ;
#37318=CARTESIAN_POINT ( 'NONE',  ( 8.102448949553181734, 146.1049999999999898, -5.886773742842746238 ) ) ;
#37319=SURFACE_STYLE_FILL_AREA ( #10884 ) ;
#37320=EDGE_CURVE ( 'NONE', #2072, #9170, #39225, .T. ) ;
#37322=ORIENTED_EDGE ( 'NONE', *, *, #30807, .F. ) ;
#37323=CARTESIAN_POINT ( 'NONE',  ( -7.632228543268608334, 129.8429263765338249, 2.479861379858952830 ) ) ;
#37324=CARTESIAN_POINT ( 'NONE',  ( 72.50000000000000000, 14.49137674618942562, -10.00000000000000000 ) ) ;
#37334=CIRCLE ( 'NONE', #6944, 0.5000000000000004441 ) ;
#37339=DIRECTION ( 'NONE',  ( 1.000000000000000000, 1.867193268687763645E-14, 0.000000000000000000 ) ) ;
#37340=FILL_AREA_STYLE_COLOUR ( '', #65279 ) ;
#37342=ORIENTED_EDGE ( 'NONE', *, *, #27135, .F. ) ;
#37343=CIRCLE ( 'NONE', #1264, 5.000000000000004441 ) ;
#37349=EDGE_LOOP ( 'NONE', ( #59757, #17016, #16195, #68408 ) ) ;
#37350=DIRECTION ( 'NONE',  ( 0.000000000000000000, 0.000000000000000000, -1.000000000000000000 ) ) ;
#37351=CARTESIAN_POINT ( 'NONE',  ( -45.91547277936962956, 9.430195807687216103, 6.000000000000000888 ) ) ;
#37353=( LENGTH_UNIT ( ) NAMED_UNIT ( * ) SI_UNIT ( .MILLI., .METRE. ) );
#37354=FACE_OUTER_BOUND ( 'NONE', #28196, .T. ) ;
#37356=ORIENTED_EDGE ( 'NONE', *, *, #63543, .T. ) ;
#37358=TOROIDAL_SURFACE ( 'NONE', #46330, 9.499999999999996447, 0.5000000000000000000 ) ;
#37359=DIRECTION ( 'NONE',  ( -0.000000000000000000, -0.000000000000000000, -1.000000000000000000 ) ) ;
#37360=FILL_AREA_STYLE ('',( #37712 ) ) ;
#37365=CARTESIAN_POINT ( 'NONE',  ( 8.102448949553181734, 144.3950000000000102, 5.886773742842750679 ) ) ;
#37369=CARTESIAN_POINT ( 'NONE',  ( 23.71231517720798010, 117.4999999999999716, 9.500000000000000000 ) ) ;
#37377=( LENGTH_UNIT ( ) NAMED_UNIT ( * ) SI_UNIT ( .MILLI., .METRE. ) );
#37378=CIRCLE ( 'NONE', #23855, 0.4999999999999994449 ) ;
#37383=ORIENTED_EDGE ( 'NONE', *, *, #53850, .T. ) ;
#37384=ORIENTED_EDGE ( 'NONE', *, *, #2748, .T. ) ;
#37388=EDGE_CURVE ( 'NONE', #6724, #25927, #54402, .T. ) ;
#37389=DIRECTION ( 'NONE',  ( 1.000000000000000000, 0.000000000000000000, 0.000000000000000000 ) ) ;
#37390=CARTESIAN_POINT ( 'NONE',  ( -45.72743705490865551, 8.702587636786784486, 6.424237564332099026 ) ) ;
#37391=CIRCLE ( 'NONE', #14919, 16.94999999999999218 ) ;
#37397=DIRECTION ( 'NONE',  ( 0.000000000000000000, 0.000000000000000000, 1.000000000000000000 ) ) ;
#37399=VERTEX_POINT ( 'NONE', #18087 ) ;
#37402=AXIS2_PLACEMENT_3D ( 'NONE', #62003, #24367, #67645 ) ;
#37404=CARTESIAN_POINT ( 'NONE',  ( 5.598654528085809545, 121.1449999999999818, -7.705886871421373741 ) ) ;
#37406=( GEOMETRIC_REPRESENTATION_CONTEXT ( 3 ) GLOBAL_UNCERTAINTY_ASSIGNED_CONTEXT ( ( #5989 ) ) GLOBAL_UNIT_ASSIGNED_CONTEXT ( ( #54474, #6286, #59755 ) ) REPRESENTATION_CONTEXT ( 'NONE', 'WORKASPACE' ) );
#37407=ORIENTED_EDGE ( 'NONE', *, *, #7213, .F. ) ;
#37408=CARTESIAN_POINT ( 'NONE',  ( -45.00000000000000000, 10.49999999999998579, 3.000000000000000000 ) ) ;
#37409=CARTESIAN_POINT ( 'NONE',  ( 5.598654528085805993, 121.3549999999999898, 7.705886871421374629 ) ) ;
#37412=STYLED_ITEM ( 'NONE', ( #19949 ), #6906 ) ;
#37414=LINE ( 'NONE', #37763, #12738 ) ;
#37416=CARTESIAN_POINT ( 'NONE',  ( 9.058813317711337021, 148.6549999999999727, 2.943386871421375783 ) ) ;
#37417=PRESENTATION_STYLE_ASSIGNMENT (( #9337 ) ) ;
#37419=TOROIDAL_SURFACE ( 'NONE', #8153, 1.000000000000000000, 0.5000000000000000000 ) ;
#37421=FACE_BOUND ( 'NONE', #40165, .T. ) ;
#37424=ORIENTED_EDGE ( 'NONE', *, *, #25278, .F. ) ;
#37428=CYLINDRICAL_SURFACE ( 'NONE', #36251, 0.5000000000000004441 ) ;
#37432=( GEOMETRIC_REPRESENTATION_CONTEXT ( 3 ) GLOBAL_UNCERTAINTY_ASSIGNED_CONTEXT ( ( #60696 ) ) GLOBAL_UNIT_ASSIGNED_CONTEXT ( ( #67726, #1896, #50505 ) ) REPRESENTATION_CONTEXT ( 'NONE', 'WORKASPACE' ) );
#37433=FILL_AREA_STYLE ('',( #63746 ) ) ;
#37434=CARTESIAN_POINT ( 'NONE',  ( -44.99154893936432842, 9.591540374752312914, 3.105576841506459296 ) ) ;
#37435=ORIENTED_EDGE ( 'NONE', *, *, #56368, .F. ) ;
#37436=AXIS2_PLACEMENT_3D ( 'NONE', #3495, #68615, #24996 ) ;
#37438=PRESENTATION_STYLE_ASSIGNMENT (( #53889 ) ) ;
#37441=DIRECTION ( 'NONE',  ( 0.000000000000000000, 0.000000000000000000, -1.000000000000000000 ) ) ;
#37442=PRESENTATION_STYLE_ASSIGNMENT (( #31744 ) ) ;
#37445=AXIS2_PLACEMENT_3D ( 'NONE', #58966, #16440, #5821 ) ;
#37446=FILL_AREA_STYLE ('',( #3970 ) ) ;
#37451=ORIENTED_EDGE ( 'NONE', *, *, #56368, .T. ) ;
#37452=COLOUR_RGB ( '', 0.09019608, 0.27058824, 0.51372549) ;
#37453=FACE_OUTER_BOUND ( 'NONE', #63652, .T. ) ;
#37456=CARTESIAN_POINT ( 'NONE',  ( -8.102448949553181734, 122.4949999999999903, 5.886773742842747126 ) ) ;
#37457=STYLED_ITEM ( 'NONE', ( #47174 ), #22837 ) ;
#37459=MECHANICAL_DESIGN_GEOMETRIC_PRESENTATION_REPRESENTATION('',(#25045),#7067);
#37461=AXIS2_PLACEMENT_3D ( 'NONE', #60206, #17666, #55623 ) ;
#37465=EDGE_LOOP ( 'NONE', ( #56649, #2263, #66158, #47092 ) ) ;
#37468=AXIS2_PLACEMENT_3D ( 'NONE', #4448, #11128, #48127 ) ;
#37472=CARTESIAN_POINT ( 'NONE',  ( -40.78947368421051323, 108.1536491499103505, 3.000000000000000000 ) ) ;
#37476=EDGE_LOOP ( 'NONE', ( #42315, #32498, #66090, #49751 ) ) ;
#37484=EDGE_LOOP ( 'NONE', ( #64785, #68670, #31977, #27787 ) ) ;
#37486=CARTESIAN_POINT ( 'NONE',  ( 71.62068965517239860, 36.41396814395972115, 7.000000000000000000 ) ) ;
#37487=CARTESIAN_POINT ( 'NONE',  ( -49.12162162162162105, 13.70805908423323238, -10.00000000000000000 ) ) ;
#37488=VECTOR ( 'NONE', #26512, 1000.000000000000000 ) ;
#37489=CARTESIAN_POINT ( 'NONE',  ( 0.000000000000000000, 142.0570736234661524, -8.025000000000000355 ) ) ;
#37490=CIRCLE ( 'NONE', #52012, 0.5000000000000004441 ) ;
#37491=VERTEX_POINT ( 'NONE', #27786 ) ;
#37492=DIRECTION ( 'NONE',  ( -1.000000000000000000, 0.000000000000000000, 0.000000000000000000 ) ) ;
#37495=ORIENTED_EDGE ( 'NONE', *, *, #58442, .T. ) ;
#37496=CARTESIAN_POINT ( 'NONE',  ( 75.00000000000000000, 19.92376017841765545, -7.000000000000002665 ) ) ;
#37497=EDGE_CURVE ( 'NONE', #28799, #1094, #39852, .T. ) ;
#37502=EDGE_CURVE ( 'NONE', #42518, #66900, #60031, .T. ) ;
#37507=DIRECTION ( 'NONE',  ( 0.000000000000000000, 1.000000000000000000, -0.000000000000000000 ) ) ;
#37509=AXIS2_PLACEMENT_3D ( 'NONE', #3824, #57676, #58035 ) ;
#37513=DIRECTION ( 'NONE',  ( 0.000000000000000000, 0.000000000000000000, -1.000000000000000000 ) ) ;
#37517=ORIENTED_EDGE ( 'NONE', *, *, #61606, .F. ) ;
#37519=( LENGTH_UNIT ( ) NAMED_UNIT ( * ) SI_UNIT ( .MILLI., .METRE. ) );
#37520=SURFACE_STYLE_USAGE ( .BOTH. , #1139 ) ;
#37522=CARTESIAN_POINT ( 'NONE',  ( 5.598654528085809545, 124.1449999999999960, -7.705886871421373741 ) ) ;
#37524=AXIS2_PLACEMENT_3D ( 'NONE', #46067, #41840, #4132 ) ;
#37526=CARTESIAN_POINT ( 'NONE',  ( 45.00000000000000000, 9.999999999999980460, -6.999999999999999112 ) ) ;
#37528=( NAMED_UNIT ( * ) PLANE_ANGLE_UNIT ( ) SI_UNIT ( $, .RADIAN. ) );
#37529=LINE ( 'NONE', #10408, #51473 ) ;
#37531=CARTESIAN_POINT ( 'NONE',  ( 15.98999599679679839, 147.4999999999999716, -10.00000000000000000 ) ) ;
#37532=CIRCLE ( 'NONE', #58820, 0.5000000000000004441 ) ;
#37534=CARTESIAN_POINT ( 'NONE',  ( -72.00000000000000000, 35.92875272052971525, 9.500000000000000000 ) ) ;
#37539=TOROIDAL_SURFACE ( 'NONE', #22933, 1.000000000000000000, 0.5000000000000000000 ) ;
#37540=CIRCLE ( 'NONE', #20611, 8.000000000000007105 ) ;
#37542=ORIENTED_EDGE ( 'NONE', *, *, #56790, .F. ) ;
#37545=( GEOMETRIC_REPRESENTATION_CONTEXT ( 3 ) GLOBAL_UNCERTAINTY_ASSIGNED_CONTEXT ( ( #40316 ) ) GLOBAL_UNIT_ASSIGNED_CONTEXT ( ( #55326, #17720, #1097 ) ) REPRESENTATION_CONTEXT ( 'NONE', 'WORKASPACE' ) );
#37546=ADVANCED_FACE ( 'NONE', ( #11291 ), #52241, .F. ) ;
#37548=UNCERTAINTY_MEASURE_WITH_UNIT (LENGTH_MEASURE( 1.000000000000000082E-05 ), #59572, 'distance_accuracy_value', 'NONE');
#37552=CARTESIAN_POINT ( 'NONE',  ( 5.598654528085809545, 161.2549999999999955, -7.705886871421373741 ) ) ;
#37553=SURFACE_STYLE_USAGE ( .BOTH. , #21297 ) ;
#37554=SURFACE_STYLE_FILL_AREA ( #37896 ) ;
#37555=SURFACE_STYLE_USAGE ( .BOTH. , #42137 ) ;
#37561=( GEOMETRIC_REPRESENTATION_CONTEXT ( 3 ) GLOBAL_UNCERTAINTY_ASSIGNED_CONTEXT ( ( #68004 ) ) GLOBAL_UNIT_ASSIGNED_CONTEXT ( ( #20803, #31324, #64039 ) ) REPRESENTATION_CONTEXT ( 'NONE', 'WORKASPACE' ) );
#37564=AXIS2_PLACEMENT_3D ( 'NONE', #4904, #10547, #53777 ) ;
#37566=DIRECTION ( 'NONE',  ( -1.000000000000000000, -1.156482317317866302E-16, 0.000000000000000000 ) ) ;
#37567=LINE ( 'NONE', #59273, #22869 ) ;
#37568=( NAMED_UNIT ( * ) SI_UNIT ( $, .STERADIAN. ) SOLID_ANGLE_UNIT ( ) );
#37570=PRESENTATION_STYLE_ASSIGNMENT (( #48106 ) ) ;
#37572=CARTESIAN_POINT ( 'NONE',  ( 7.632228543268608334, 114.4570736234661581, -2.479861379858951942 ) ) ;
#37574=FILL_AREA_STYLE ('',( #44573 ) ) ;
#37575=CYLINDRICAL_SURFACE ( 'NONE', #13927, 0.5000000000000004441 ) ;
#37581=ORIENTED_EDGE ( 'NONE', *, *, #29706, .T. ) ;
#37582=CARTESIAN_POINT ( 'NONE',  ( -5.598654528085808657, 126.7549999999999812, 7.705886871421373741 ) ) ;
#37583=ORIENTED_EDGE ( 'NONE', *, *, #49187, .F. ) ;
#37584=( LENGTH_UNIT ( ) NAMED_UNIT ( * ) SI_UNIT ( .MILLI., .METRE. ) );
#37585=EDGE_CURVE ( 'NONE', #5467, #1094, #13889, .T. ) ;
#37588=DIRECTION ( 'NONE',  ( 1.000000000000000000, 0.000000000000000000, 0.000000000000000000 ) ) ;
#37590=ORIENTED_EDGE ( 'NONE', *, *, #42966, .F. ) ;
#37591=CARTESIAN_POINT ( 'NONE',  ( 2.607480562269071989, 154.5929263765338249, 8.025000000000002132 ) ) ;
#37598=PRESENTATION_STYLE_ASSIGNMENT (( #16118 ) ) ;
#37599=( NAMED_UNIT ( * ) PLANE_ANGLE_UNIT ( ) SI_UNIT ( $, .RADIAN. ) );
#37602=CARTESIAN_POINT ( 'NONE',  ( 2.607480562269098634, 115.5929263765338249, 8.024999999999984368 ) ) ;
#37603=CARTESIAN_POINT ( 'NONE',  ( -2.139872436712106474, 154.0569316272727178, 8.842724602598590167 ) ) ;
#37608=CIRCLE ( 'NONE', #17356, 13.99999999999999822 ) ;
#37611=DIRECTION ( 'NONE',  ( 0.000000000000000000, -1.000000000000000000, -0.000000000000000000 ) ) ;
#37614=CARTESIAN_POINT ( 'NONE',  ( -12.72792206135785165, 115.4999999999999574, -10.00000000000000000 ) ) ;
#37615=EDGE_CURVE ( 'NONE', #26930, #1355, #17292, .T. ) ;
#37624=DIRECTION ( 'NONE',  ( 0.000000000000000000, -1.000000000000000000, 0.000000000000000000 ) ) ;
#37625=MECHANICAL_DESIGN_GEOMETRIC_PRESENTATION_REPRESENTATION('',(#45458),#64542);
#37628=CARTESIAN_POINT ( 'NONE',  ( -9.058813317711338797, 138.4549999999999841, 2.943386871421373563 ) ) ;
#37632=EDGE_CURVE ( 'NONE', #54750, #24087, #39725, .T. ) ;
#37634=SURFACE_STYLE_FILL_AREA ( #4873 ) ;
#37636=ORIENTED_EDGE ( 'NONE', *, *, #48160, .T. ) ;
#37638=CARTESIAN_POINT ( 'NONE',  ( -6.826472737025120807, 132.9929263765338021, 4.959722759717906548 ) ) ;
#37640=EDGE_CURVE ( 'NONE', #43100, #41477, #53593, .T. ) ;
#37642=( LENGTH_UNIT ( ) NAMED_UNIT ( * ) SI_UNIT ( .MILLI., .METRE. ) );
#37643=CARTESIAN_POINT ( 'NONE',  ( 45.00000000000000000, 10.69371294336137801, -6.000000000000000000 ) ) ;
#37647=STYLED_ITEM ( 'NONE', ( #6144 ), #37215 ) ;
#37648=CARTESIAN_POINT ( 'NONE',  ( 71.49999999999998579, 99.99999999999998579, 7.500000000000000000 ) ) ;
#37649=MECHANICAL_DESIGN_GEOMETRIC_PRESENTATION_REPRESENTATION('',(#3883),#9501);
#37650=CIRCLE ( 'NONE', #58987, 0.5000000000000004441 ) ;
#37651=CARTESIAN_POINT ( 'NONE',  ( -8.437984349512095861, 147.6929263765338192, -5.166775262442723748E-16 ) ) ;
#37652=( NAMED_UNIT ( * ) PLANE_ANGLE_UNIT ( ) SI_UNIT ( $, .RADIAN. ) );
#37653=FACE_OUTER_BOUND ( 'NONE', #51701, .T. ) ;
#37658=CARTESIAN_POINT ( 'NONE',  ( -34.99999999999999289, 99.99999999999998579, -7.000000000000000000 ) ) ;
#37659=CARTESIAN_POINT ( 'NONE',  ( -75.00000000000000000, -2.215169945516535778E-14, 10.00000000000000000 ) ) ;
#37663=VERTEX_POINT ( 'NONE', #48357 ) ;
#37665=CARTESIAN_POINT ( 'NONE',  ( 8.102448949553183510, 147.9949999999999761, -5.886773742842746238 ) ) ;
#37667=ORIENTED_EDGE ( 'NONE', *, *, #24318, .T. ) ;
#37669=SURFACE_STYLE_USAGE ( .BOTH. , #43302 ) ;
#37671=ORIENTED_EDGE ( 'NONE', *, *, #17580, .F. ) ;
#37672=CARTESIAN_POINT ( 'NONE',  ( 2.607480562269071989, 127.5929263765338249, 8.025000000000002132 ) ) ;
#37675=CIRCLE ( 'NONE', #34257, 0.5000000000000004441 ) ;
#37677=DIRECTION ( 'NONE',  ( 0.000000000000000000, 0.2503800040544373884, 0.9681476403781088536 ) ) ;
#37680=VERTEX_POINT ( 'NONE', #58880 ) ;
#37681=CARTESIAN_POINT ( 'NONE',  ( -34.99999999999992895, 110.4999999999999858, 9.500000000000000000 ) ) ;
#37683=FILL_AREA_STYLE ('',( #11932 ) ) ;
#37684=DIRECTION ( 'NONE',  ( -1.000000000000000000, 0.000000000000000000, 0.000000000000000000 ) ) ;
#37687=SURFACE_SIDE_STYLE ('',( #22145 ) ) ;
#37688=UNCERTAINTY_MEASURE_WITH_UNIT (LENGTH_MEASURE( 1.000000000000000082E-05 ), #12808, 'distance_accuracy_value', 'NONE');
#37691=( NAMED_UNIT ( * ) PLANE_ANGLE_UNIT ( ) SI_UNIT ( $, .RADIAN. ) );
#37692=( NAMED_UNIT ( * ) PLANE_ANGLE_UNIT ( ) SI_UNIT ( $, .RADIAN. ) );
#37696=DIRECTION ( 'NONE',  ( 0.000000000000000000, 0.000000000000000000, 1.000000000000000000 ) ) ;
#37698=MECHANICAL_DESIGN_GEOMETRIC_PRESENTATION_REPRESENTATION('',(#12917),#50059);
#37699=ORIENTED_EDGE ( 'NONE', *, *, #33349, .T. ) ;
#37700=DIRECTION ( 'NONE',  ( 1.000000000000000000, 0.000000000000000000, 0.000000000000000000 ) ) ;
#37702=CARTESIAN_POINT ( 'NONE',  ( 45.00000000000000000, 10.69371294336137801, 6.000000000000000888 ) ) ;
#37703=PRESENTATION_STYLE_ASSIGNMENT (( #49249 ) ) ;
#37704=VECTOR ( 'NONE', #2873, 1000.000000000000000 ) ;
#37705=EDGE_CURVE ( 'NONE', #7479, #16380, #43115, .T. ) ;
#37706=CARTESIAN_POINT ( 'NONE',  ( 44.99999999999977973, 146.9999999999999716, -7.500000000000000000 ) ) ;
#37709=EDGE_CURVE ( 'NONE', #23604, #41301, #22894, .T. ) ;
#37710=FILL_AREA_STYLE ('',( #32709 ) ) ;
#37711=CIRCLE ( 'NONE', #46643, 5.499999999999976907 ) ;
#37712=FILL_AREA_STYLE_COLOUR ( '', #53012 ) ;
#37713=( BOUNDED_CURVE ( )  B_SPLINE_CURVE ( 2, ( #65164, #43443, #49044, #734, #22265, #52908, #37812, #64134, #64827, #63787, #16673 ),
 .UNSPECIFIED., .F., .F. ) 
 B_SPLINE_CURVE_WITH_KNOTS ( ( 3, 2, 2, 2, 2, 3 ),
 ( 0.7647058823529410132, 0.7705882352941175739, 0.7764705882352940236, 0.7823529411764704733, 0.7882352941176469230, 0.7941176470588233727 ),
 .UNSPECIFIED. ) 
 CURVE ( )  GEOMETRIC_REPRESENTATION_ITEM ( )  RATIONAL_B_SPLINE_CURVE ( ( 1.000000000000000888, 0.9510565162951526430, 1.000000000000000000, 0.9510565162951535312, 1.000000000000000000, 0.9510565162951535312, 1.000000000000000000, 0.9510565162951535312, 1.000000000000000000, 0.9510565162951544194, 0.9999999999999991118 ) ) 
 REPRESENTATION_ITEM ( '' )  );
#37717=CARTESIAN_POINT ( 'NONE',  ( -9.058813317711338797, 111.4549999999999841, 2.943386871421373563 ) ) ;
#37725=COLOUR_RGB ( '', 0.31764706, 0.68627451, 0.89019608) ;
#37731=SURFACE_STYLE_USAGE ( .BOTH. , #59815 ) ;
#37738=CARTESIAN_POINT ( 'NONE',  ( 0.000000000000000000, 152.9999999999999716, 0.000000000000000000 ) ) ;
#37740=CARTESIAN_POINT ( 'NONE',  ( -45.00000000000000000, 9.675769070491668344, 6.195678411461557289 ) ) ;
#37750=ORIENTED_EDGE ( 'NONE', *, *, #50744, .F. ) ;
#37751=CIRCLE ( 'NONE', #19715, 0.5000000000000004441 ) ;
#37754=CARTESIAN_POINT ( 'NONE',  ( -8.102448949553181734, 124.8949999999999960, -5.886773742842749790 ) ) ;
#37755=( LENGTH_UNIT ( ) NAMED_UNIT ( * ) SI_UNIT ( .MILLI., .METRE. ) );
#37756=AXIS2_PLACEMENT_3D ( 'NONE', #28135, #23581, #60186 ) ;
#37759=DIRECTION ( 'NONE',  ( -1.000000000000000000, 0.000000000000000000, 0.000000000000000000 ) ) ;
#37760=CARTESIAN_POINT ( 'NONE',  ( -3.094860106618434248, 132.9050000000000011, 9.525000000000000355 ) ) ;
#37763=CARTESIAN_POINT ( 'NONE',  ( -71.99999999999998579, 119.9999999999997868, 7.500000000000000000 ) ) ;
#37765=CARTESIAN_POINT ( 'NONE',  ( -9.058813317711337021, 144.1549999999999727, -2.943386871421374895 ) ) ;
#37767=UNCERTAINTY_MEASURE_WITH_UNIT (LENGTH_MEASURE( 1.000000000000000082E-05 ), #39524, 'distance_accuracy_value', 'NONE');
#37771=CARTESIAN_POINT ( 'NONE',  ( 19.89974874213240597, 115.4999999999999574, 10.50000000000000000 ) ) ;
#37775=UNCERTAINTY_MEASURE_WITH_UNIT (LENGTH_MEASURE( 1.000000000000000082E-05 ), #23177, 'distance_accuracy_value', 'NONE');
#37776=COLOUR_RGB ( '', 0.08235294, 0.09019608, 0.10196078) ;
#37777=( NAMED_UNIT ( * ) PLANE_ANGLE_UNIT ( ) SI_UNIT ( $, .RADIAN. ) );
#37778=FILL_AREA_STYLE_COLOUR ( '', #57673 ) ;
#37779=FILL_AREA_STYLE_COLOUR ( '', #18584 ) ;
#37780=DIRECTION ( 'NONE',  ( 1.156482317317873451E-16, 1.000000000000000000, -0.000000000000000000 ) ) ;
#37785=SURFACE_STYLE_FILL_AREA ( #54237 ) ;
#37791=FACE_OUTER_BOUND ( 'NONE', #7424, .T. ) ;
#37792=PRESENTATION_STYLE_ASSIGNMENT (( #49333 ) ) ;
#37798=FILL_AREA_STYLE_COLOUR ( '', #35864 ) ;
#37801=CARTESIAN_POINT ( 'NONE',  ( -3.094860106618434248, 131.7950000000000159, 9.525000000000000355 ) ) ;
#37805=CIRCLE ( 'NONE', #62442, 0.5000000000000004441 ) ;
#37808=FILL_AREA_STYLE_COLOUR ( '', #53885 ) ;
#37812=CARTESIAN_POINT ( 'NONE',  ( -7.632228543268608334, 148.9570736234661581, 2.479861379858952830 ) ) ;
#37815=FILL_AREA_STYLE ('',( #53266 ) ) ;
#37816=ORIENTED_EDGE ( 'NONE', *, *, #1377, .T. ) ;
#37821=CARTESIAN_POINT ( 'NONE',  ( 4.716976649647096842, 151.7429263765338021, 6.492361379858953896 ) ) ;
#37824=CIRCLE ( 'NONE', #34397, 0.5000000000000004441 ) ;
#37827=ORIENTED_EDGE ( 'NONE', *, *, #34019, .F. ) ;
#37829=SURFACE_SIDE_STYLE ('',( #47701 ) ) ;
#37832=CARTESIAN_POINT ( 'NONE',  ( -2.607480562269073765, 139.2070736234661581, -8.025000000000000355 ) ) ;
#37838=UNCERTAINTY_MEASURE_WITH_UNIT (LENGTH_MEASURE( 1.000000000000000082E-05 ), #65126, 'distance_accuracy_value', 'NONE');
#37840=VERTEX_POINT ( 'NONE', #21220 ) ;
#37843=LINE ( 'NONE', #38866, #42379 ) ;
#37845=ORIENTED_EDGE ( 'NONE', *, *, #17046, .F. ) ;
#37848=ORIENTED_EDGE ( 'NONE', *, *, #58912, .T. ) ;
#37849=DIRECTION ( 'NONE',  ( 1.000000000000000000, -0.000000000000000000, 0.000000000000000000 ) ) ;
#37850=EDGE_CURVE ( 'NONE', #7517, #1721, #36391, .T. ) ;
#37853=EDGE_CURVE ( 'NONE', #42295, #44642, #29604, .T. ) ;
#37854=EDGE_LOOP ( 'NONE', ( #36349, #12063, #53444, #37424 ) ) ;
#37856=LINE ( 'NONE', #33891, #34810 ) ;
#37858=EDGE_CURVE ( 'NONE', #26152, #23161, #22120, .T. ) ;
#37860=LINE ( 'NONE', #69467, #55955 ) ;
#37865=CARTESIAN_POINT ( 'NONE',  ( -41.49999999999998579, 108.0000000000000000, 3.500000000000000000 ) ) ;
#37866=CARTESIAN_POINT ( 'NONE',  ( 52.49999999999998579, 2.746146170318484607E-15, -12.00000000000000000 ) ) ;
#37869=CARTESIAN_POINT ( 'NONE',  ( -3.094860106618432471, 133.5949999999999989, -9.525000000000000355 ) ) ;
#37872=CARTESIAN_POINT ( 'NONE',  ( 40.49999999999998579, 107.7459666924148252, 3.000000000000000000 ) ) ;
#37875=FACE_OUTER_BOUND ( 'NONE', #23246, .T. ) ;
#37883=CARTESIAN_POINT ( 'NONE',  ( 75.00000000000000000, 19.92376017841764479, 7.000000000000000000 ) ) ;
#37884=CARTESIAN_POINT ( 'NONE',  ( 41.84210526315788314, 107.2928455055531600, 4.000000000000000000 ) ) ;
#37886=CIRCLE ( 'NONE', #27649, 23.00000000000000355 ) ;
#37889=SURFACE_SIDE_STYLE ('',( #53995 ) ) ;
#37895=FILL_AREA_STYLE_COLOUR ( '', #31317 ) ;
#37896=FILL_AREA_STYLE ('',( #48783 ) ) ;
#37897=LINE ( 'NONE', #22354, #62654 ) ;
#37901=DIRECTION ( 'NONE',  ( 0.000000000000000000, -1.000000000000000000, 0.000000000000000000 ) ) ;
#37903=CARTESIAN_POINT ( 'NONE',  ( -74.99999999999998579, 50.00000000000000000, 7.500000000000000000 ) ) ;
#37904=DIRECTION ( 'NONE',  ( -0.000000000000000000, -1.000000000000000000, -0.000000000000000000 ) ) ;
#37907=CARTESIAN_POINT ( 'NONE',  ( 60.00000000000000000, 115.4999999999999574, -10.00000000000000000 ) ) ;
#37908=ORIENTED_EDGE ( 'NONE', *, *, #26363, .T. ) ;
#37909=CARTESIAN_POINT ( 'NONE',  ( 2.607480562269071989, 113.7070736234661439, 8.025000000000002132 ) ) ;
#37910=CARTESIAN_POINT ( 'NONE',  ( -20.22778885548742522, 114.9430298377684210, 10.39013442403998866 ) ) ;
#37918=CARTESIAN_POINT ( 'NONE',  ( -9.058813317711337021, 132.1550000000000011, -2.943386871421374895 ) ) ;
#37924=ORIENTED_EDGE ( 'NONE', *, *, #40632, .T. ) ;
#37927=SURFACE_SIDE_STYLE ('',( #59301 ) ) ;
#37931=DIRECTION ( 'NONE',  ( 0.000000000000000000, -1.000000000000000000, 0.000000000000000000 ) ) ;
#37933=EDGE_CURVE ( 'NONE', #14708, #67110, #55406, .T. ) ;
#37936=ORIENTED_EDGE ( 'NONE', *, *, #6833, .T. ) ;
#37938=( NAMED_UNIT ( * ) PLANE_ANGLE_UNIT ( ) SI_UNIT ( $, .RADIAN. ) );
#37940=FILL_AREA_STYLE ('',( #48483 ) ) ;
#37944=CARTESIAN_POINT ( 'NONE',  ( 8.437984349512095861, 116.1929263765338192, 1.550032578732816828E-15 ) ) ;
#37946=VERTEX_POINT ( 'NONE', #2121 ) ;
#37948=( NAMED_UNIT ( * ) SI_UNIT ( $, .STERADIAN. ) SOLID_ANGLE_UNIT ( ) );
#37949=PLANE ( 'NONE',  #2877 ) ;
#37950=EDGE_CURVE ( 'NONE', #51702, #48200, #25092, .T. ) ;
#37954=DIRECTION ( 'NONE',  ( 0.000000000000000000, 0.000000000000000000, -1.000000000000000000 ) ) ;
#37957=DIRECTION ( 'NONE',  ( 1.000000000000000000, 0.000000000000000000, 0.000000000000000000 ) ) ;
#37963=SURFACE_SIDE_STYLE ('',( #34012 ) ) ;
#37966=( LENGTH_UNIT ( ) NAMED_UNIT ( * ) SI_UNIT ( .MILLI., .METRE. ) );
#37968=( GEOMETRIC_REPRESENTATION_CONTEXT ( 3 ) GLOBAL_UNCERTAINTY_ASSIGNED_CONTEXT ( ( #60831 ) ) GLOBAL_UNIT_ASSIGNED_CONTEXT ( ( #47089, #50947, #45706 ) ) REPRESENTATION_CONTEXT ( 'NONE', 'WORKASPACE' ) );
#37970=CARTESIAN_POINT ( 'NONE',  ( 8.102448949553181734, 136.5049999999999386, 5.886773742842750679 ) ) ;
#37971=STYLED_ITEM ( 'NONE', ( #6998 ), #3964 ) ;
#37973=CARTESIAN_POINT ( 'NONE',  ( -7.632228543268608334, 126.8429263765338249, 2.479861379858952830 ) ) ;
#37975=CARTESIAN_POINT ( 'NONE',  ( -74.99999999999998579, 36.00000000000000711, 9.500000000000001776 ) ) ;
#37977=CARTESIAN_POINT ( 'NONE',  ( 74.50000000000000000, 20.36037961002804408, 6.000000000000000888 ) ) ;
#37978=FILL_AREA_STYLE_COLOUR ( '', #23621 ) ;
#37979=ORIENTED_EDGE ( 'NONE', *, *, #23978, .F. ) ;
#37980=CARTESIAN_POINT ( 'NONE',  ( -2.607480562269032909, 133.2929263765337851, 8.025000000000032330 ) ) ;
#37983=FACE_OUTER_BOUND ( 'NONE', #66976, .T. ) ;
#37985=ORIENTED_EDGE ( 'NONE', *, *, #64581, .F. ) ;
#37987=FACE_OUTER_BOUND ( 'NONE', #46683, .T. ) ;
#37991=VERTEX_POINT ( 'NONE', #67981 ) ;
#37992=CARTESIAN_POINT ( 'NONE',  ( -80.49999999999995737, 50.00000000000000000, -12.00000000000000000 ) ) ;
#37993=ORIENTED_EDGE ( 'NONE', *, *, #1855, .F. ) ;
#37996=ADVANCED_FACE ( 'NONE', ( #13089 ), #46193, .T. ) ;
#37997=VERTEX_POINT ( 'NONE', #29970 ) ;
#38002=ORIENTED_EDGE ( 'NONE', *, *, #64247, .T. ) ;
#38003=CARTESIAN_POINT ( 'NONE',  ( 4.716976649647099507, 134.6429263765338362, -6.492361379858953008 ) ) ;
#38004=VECTOR ( 'NONE', #37507, 1000.000000000000000 ) ;
#38006=DIRECTION ( 'NONE',  ( 1.000000000000000000, 0.000000000000000000, 0.000000000000000000 ) ) ;
#38007=EDGE_CURVE ( 'NONE', #49241, #25507, #27363, .T. ) ;
#38008=CARTESIAN_POINT ( 'NONE',  ( 0.000000000000000000, 110.7489631882669130, -8.775000000000002132 ) ) ;
#38011=EDGE_LOOP ( 'NONE', ( #39751, #66245, #16400, #26365 ) ) ;
#38014=( NAMED_UNIT ( * ) SI_UNIT ( $, .STERADIAN. ) SOLID_ANGLE_UNIT ( ) );
#38020=SURFACE_SIDE_STYLE ('',( #64013 ) ) ;
#38021=CARTESIAN_POINT ( 'NONE',  ( 40.78947368421051323, 108.1536491499103363, 2.999999999999999112 ) ) ;
#38030=FACE_OUTER_BOUND ( 'NONE', #33396, .T. ) ;
#38032=CYLINDRICAL_SURFACE ( 'NONE', #31775, 0.5000000000000004441 ) ;
#38038=FILL_AREA_STYLE_COLOUR ( '', #5552 ) ;
#38040=CARTESIAN_POINT ( 'NONE',  ( 9.058813317711338797, 112.9549999999999841, -2.943386871421372675 ) ) ;
#38042=CARTESIAN_POINT ( 'NONE',  ( -7.632228543268608334, 112.9570736234661581, 2.479861379858952830 ) ) ;
#38054=( GEOMETRIC_REPRESENTATION_CONTEXT ( 3 ) GLOBAL_UNCERTAINTY_ASSIGNED_CONTEXT ( ( #10080 ) ) GLOBAL_UNIT_ASSIGNED_CONTEXT ( ( #7202, #59960, #60635 ) ) REPRESENTATION_CONTEXT ( 'NONE', 'WORKASPACE' ) );
#38056=ORIENTED_EDGE ( 'NONE', *, *, #3300, .F. ) ;
#38057=STYLED_ITEM ( 'NONE', ( #38141 ), #14526 ) ;
#38058=EDGE_LOOP ( 'NONE', ( #16017, #32488, #59130, #10000 ) ) ;
#38060=LINE ( 'NONE', #16599, #31956 ) ;
#38065=VECTOR ( 'NONE', #14734, 1000.000000000000000 ) ;
#38071=ORIENTED_EDGE ( 'NONE', *, *, #35355, .F. ) ;
#38072=LINE ( 'NONE', #38770, #4275 ) ;
#38073=CYLINDRICAL_SURFACE ( 'NONE', #47853, 8.025000000000000355 ) ;
#38077=CARTESIAN_POINT ( 'NONE',  ( -8.102448949553181734, 134.4949999999999477, 5.886773742842747126 ) ) ;
#38083=CARTESIAN_POINT ( 'NONE',  ( 5.598654528085809545, 134.2549999999999955, -7.705886871421373741 ) ) ;
#38085=CIRCLE ( 'NONE', #33520, 15.00000000000000000 ) ;
#38088=ORIENTED_EDGE ( 'NONE', *, *, #23423, .T. ) ;
#38089=CARTESIAN_POINT ( 'NONE',  ( 8.102448949553181734, 148.5049999999999955, 5.886773742842750679 ) ) ;
#38090=CARTESIAN_POINT ( 'NONE',  ( -71.50000000000000000, 35.92875272052971525, -9.500000000000000000 ) ) ;
#38091=DIRECTION ( 'NONE',  ( -0.000000000000000000, -1.000000000000000000, -0.000000000000000000 ) ) ;
#38092=EDGE_CURVE ( 'NONE', #1094, #42518, #4617, .T. ) ;
#38093=SURFACE_STYLE_USAGE ( .BOTH. , #27123 ) ;
#38097=ORIENTED_EDGE ( 'NONE', *, *, #28886, .F. ) ;
#38101=EDGE_CURVE ( 'NONE', #55126, #7860, #20821, .T. ) ;
#38102=ORIENTED_EDGE ( 'NONE', *, *, #8280, .F. ) ;
#38103=SURFACE_STYLE_USAGE ( .BOTH. , #64796 ) ;
#38105=SURFACE_STYLE_FILL_AREA ( #33146 ) ;
#38107=FACE_OUTER_BOUND ( 'NONE', #2528, .T. ) ;
#38108=SURFACE_STYLE_USAGE ( .BOTH. , #58486 ) ;
#38113=( GEOMETRIC_REPRESENTATION_CONTEXT ( 3 ) GLOBAL_UNCERTAINTY_ASSIGNED_CONTEXT ( ( #36131 ) ) GLOBAL_UNIT_ASSIGNED_CONTEXT ( ( #53572, #5358, #26799 ) ) REPRESENTATION_CONTEXT ( 'NONE', 'WORKASPACE' ) );
#38114=SURFACE_STYLE_USAGE ( .BOTH. , #32105 ) ;
#38118=DIRECTION ( 'NONE',  ( 1.000000000000000000, 0.000000000000000000, 0.000000000000000000 ) ) ;
#38123=COLOUR_RGB ( '', 0.09019608, 0.27058824, 0.51372549) ;
#38124=FACE_OUTER_BOUND ( 'NONE', #67098, .T. ) ;
#38129=CARTESIAN_POINT ( 'NONE',  ( -5.598654528085806881, 133.7450000000000045, -7.705886871421374629 ) ) ;
#38131=DIRECTION ( 'NONE',  ( 0.000000000000000000, 1.000000000000000000, 0.000000000000000000 ) ) ;
#38132=CARTESIAN_POINT ( 'NONE',  ( 40.99999999999997868, 9.999999999999978684, -3.500000000000000000 ) ) ;
#38138=CIRCLE ( 'NONE', #26862, 0.5000000000000004441 ) ;
#38139=CARTESIAN_POINT ( 'NONE',  ( 60.00000000000000000, 1.797044900979284448E-15, 6.999999999999999112 ) ) ;
#38140=ORIENTED_EDGE ( 'NONE', *, *, #36363, .T. ) ;
#38141=PRESENTATION_STYLE_ASSIGNMENT (( #54267 ) ) ;
#38152=ADVANCED_FACE ( 'NONE', ( #41599 ), #36437, .F. ) ;
#38155=SURFACE_STYLE_FILL_AREA ( #36780 ) ;
#38156=EDGE_CURVE ( 'NONE', #42076, #21155, #20461, .T. ) ;
#38159=CARTESIAN_POINT ( 'NONE',  ( 4.716976649647099507, 156.7570736234661695, -6.492361379858953008 ) ) ;
#38163=CARTESIAN_POINT ( 'NONE',  ( 4.716976649647096842, 136.7429263765338305, 6.492361379858953896 ) ) ;
#38165=VECTOR ( 'NONE', #44017, 1000.000000000000000 ) ;
#38167=ORIENTED_EDGE ( 'NONE', *, *, #43665, .F. ) ;
#38169=PRESENTATION_STYLE_ASSIGNMENT (( #64855 ) ) ;
#38171=EDGE_CURVE ( 'NONE', #44039, #8600, #6059, .T. ) ;
#38172=( NAMED_UNIT ( * ) SI_UNIT ( $, .STERADIAN. ) SOLID_ANGLE_UNIT ( ) );
#38173=ORIENTED_EDGE ( 'NONE', *, *, #12769, .F. ) ;
#38175=AXIS2_PLACEMENT_3D ( 'NONE', #62451, #14266, #8998 ) ;
#38178=DIRECTION ( 'NONE',  ( -0.4468085106382997385, -0.000000000000000000, -0.8946296187927071930 ) ) ;
#38179=( NAMED_UNIT ( * ) SI_UNIT ( $, .STERADIAN. ) SOLID_ANGLE_UNIT ( ) );
#38180=CARTESIAN_POINT ( 'NONE',  ( -45.84227902758264150, 9.150846973920693017, -6.292314909081791363 ) ) ;
#38189=FACE_OUTER_BOUND ( 'NONE', #23955, .T. ) ;
#38193=TOROIDAL_SURFACE ( 'NONE', #31407, 7.500000000000011546, 0.5000000000000000000 ) ;
#38195=CARTESIAN_POINT ( 'NONE',  ( -1.166476076187854022E-15, 128.9449999999999648, 9.525000000000000355 ) ) ;
#38196=COLOUR_RGB ( '', 0.40784314, 0.44705882, 0.49803922) ;
#38200=CARTESIAN_POINT ( 'NONE',  ( -15.48999599679679662, 146.9999999999999716, -7.500000000000000000 ) ) ;
#38204=DIRECTION ( 'NONE',  ( -0.000000000000000000, -0.000000000000000000, -1.000000000000000000 ) ) ;
#38206=SURFACE_SIDE_STYLE ('',( #37175 ) ) ;
#38207=SURFACE_STYLE_FILL_AREA ( #60996 ) ;
#38211=EDGE_LOOP ( 'NONE', ( #11540, #52761, #25162, #24171, #33247, #57706, #41511, #59811, #61203, #1590 ) ) ;
#38212=VECTOR ( 'NONE', #17004, 1000.000000000000000 ) ;
#38215=FILL_AREA_STYLE_COLOUR ( '', #36858 ) ;
#38217=UNCERTAINTY_MEASURE_WITH_UNIT (LENGTH_MEASURE( 1.000000000000000082E-05 ), #8485, 'distance_accuracy_value', 'NONE');
#38219=( LENGTH_UNIT ( ) NAMED_UNIT ( * ) SI_UNIT ( .MILLI., .METRE. ) );
#38220=VECTOR ( 'NONE', #34104, 1000.000000000000000 ) ;
#38222=FACE_OUTER_BOUND ( 'NONE', #54502, .T. ) ;
#38224=( NAMED_UNIT ( * ) PLANE_ANGLE_UNIT ( ) SI_UNIT ( $, .RADIAN. ) );
#38225=CYLINDRICAL_SURFACE ( 'NONE', #22645, 8.999999999999994671 ) ;
#38226=MECHANICAL_DESIGN_GEOMETRIC_PRESENTATION_REPRESENTATION('',(#20196),#5569);
#38227=COLOUR_RGB ( '', 0.31764706, 0.68627451, 0.89019608) ;
#38234=ADVANCED_FACE ( 'NONE', ( #4971 ), #28473, .F. ) ;
#38236=ADVANCED_FACE ( 'NONE', ( #64413 ), #65801, .F. ) ;
#38237=ORIENTED_EDGE ( 'NONE', *, *, #45705, .T. ) ;
#38239=COLOUR_RGB ( '', 0.40784314, 0.44705882, 0.49803922) ;
#38240=PRESENTATION_STYLE_ASSIGNMENT (( #64916 ) ) ;
#38241=AXIS2_PLACEMENT_3D ( 'NONE', #44697, #38386, #33403 ) ;
#38243=CARTESIAN_POINT ( 'NONE',  ( -8.437984349512095861, 115.8070736234661524, -5.166775262442723748E-16 ) ) ;
#38246=CARTESIAN_POINT ( 'NONE',  ( -60.00000000000000000, -2.024042244987997205E-14, 12.00000000000000000 ) ) ;
#38248=SURFACE_SIDE_STYLE ('',( #10447 ) ) ;
#38249=ADVANCED_FACE ( 'NONE', ( #44731 ), #39848, .F. ) ;
#38257=ADVANCED_FACE ( 'NONE', ( #33435 ), #16937, .F. ) ;
#38259=CARTESIAN_POINT ( 'NONE',  ( 2.607480562269155921, 148.5929263765338249, 8.024999999999941735 ) ) ;
#38262=AXIS2_PLACEMENT_3D ( 'NONE', #64399, #54179, #59112 ) ;
#38264=CARTESIAN_POINT ( 'NONE',  ( 7.295185304185720199, 153.7998498338025684, -4.982187544324071737 ) ) ;
#38268=UNCERTAINTY_MEASURE_WITH_UNIT (LENGTH_MEASURE( 1.000000000000000082E-05 ), #67368, 'distance_accuracy_value', 'NONE');
#38270=CARTESIAN_POINT ( 'NONE',  ( 7.632228543268608334, 161.3429263765338249, -2.479861379858951942 ) ) ;
#38271=SURFACE_STYLE_USAGE ( .BOTH. , #1903 ) ;
#38272=AXIS2_PLACEMENT_3D ( 'NONE', #23453, #66731, #22783 ) ;
#38273=SURFACE_STYLE_USAGE ( .BOTH. , #21340 ) ;
#38277=ORIENTED_EDGE ( 'NONE', *, *, #33998, .F. ) ;
#38280=DIRECTION ( 'NONE',  ( 1.000000000000000000, 0.000000000000000000, 0.000000000000000000 ) ) ;
#38282=AXIS2_PLACEMENT_3D ( 'NONE', #25260, #68187, #30514 ) ;
#38284=COLOUR_RGB ( '', 0.40784314, 0.44705882, 0.49803922) ;
#38286=CARTESIAN_POINT ( 'NONE',  ( -7.863253753129167301, 153.7221554051249370, 3.841316429231163010 ) ) ;
#38287=EDGE_LOOP ( 'NONE', ( #17678, #14725, #37061, #54464 ) ) ;
#38289=DIRECTION ( 'NONE',  ( 1.000000000000000000, 0.000000000000000000, 0.000000000000000000 ) ) ;
#38290=VERTEX_POINT ( 'NONE', #54869 ) ;
#38295=COLOUR_RGB ( '', 0.09019608, 0.27058824, 0.51372549) ;
#38300=SURFACE_STYLE_USAGE ( .BOTH. , #60387 ) ;
#38301=DIRECTION ( 'NONE',  ( 0.000000000000000000, 0.000000000000000000, 1.000000000000000000 ) ) ;
#38307=CARTESIAN_POINT ( 'NONE',  ( -5.598654528085808657, 132.7549999999999955, 7.705886871421373741 ) ) ;
#38308=CARTESIAN_POINT ( 'NONE',  ( 71.18918918918917882, 14.09971791521133255, 7.500000000000000000 ) ) ;
#38314=ORIENTED_EDGE ( 'NONE', *, *, #37705, .F. ) ;
#38315=EDGE_CURVE ( 'NONE', #48372, #56046, #38060, .T. ) ;
#38320=CARTESIAN_POINT ( 'NONE',  ( 34.99999999999992895, 112.9999999999999858, -7.000000000000000000 ) ) ;
#38321=ORIENTED_EDGE ( 'NONE', *, *, #31942, .T. ) ;
#38323=LINE ( 'NONE', #17867, #65592 ) ;
#38324=CARTESIAN_POINT ( 'NONE',  ( -40.99999999999997868, 10.49999999999998224, 3.500000000000000000 ) ) ;
#38328=CARTESIAN_POINT ( 'NONE',  ( -45.48309787872866394, 9.683080749504641815, 3.000000000000000000 ) ) ;
#38331=CARTESIAN_POINT ( 'NONE',  ( 2.607480562268992941, 140.7929263765338419, -8.025000000000060751 ) ) ;
#38337=FACE_OUTER_BOUND ( 'NONE', #68166, .T. ) ;
#38344=SURFACE_STYLE_USAGE ( .BOTH. , #28401 ) ;
#38346=CARTESIAN_POINT ( 'NONE',  ( -10.01517768586949231, 158.1949999999999932, -6.132527647946036459E-16 ) ) ;
#38347=DIRECTION ( 'NONE',  ( 1.000000000000000000, 0.000000000000000000, 0.000000000000000000 ) ) ;
#38352=( LENGTH_UNIT ( ) NAMED_UNIT ( * ) SI_UNIT ( .MILLI., .METRE. ) );
#38356=CARTESIAN_POINT ( 'NONE',  ( 4.716976649647096842, 136.7429263765338305, 6.492361379858953896 ) ) ;
#38357=DIRECTION ( 'NONE',  ( 1.000000000000000000, 0.000000000000000000, 0.000000000000000000 ) ) ;
#38359=CARTESIAN_POINT ( 'NONE',  ( -20.71231517720798010, 146.9999999999999716, 7.500000000000000000 ) ) ;
#38360=( LENGTH_UNIT ( ) NAMED_UNIT ( * ) SI_UNIT ( .MILLI., .METRE. ) );
#38361=EDGE_CURVE ( 'NONE', #28358, #47977, #58887, .T. ) ;
#38362=ORIENTED_EDGE ( 'NONE', *, *, #44451, .T. ) ;
#38367=SURFACE_SIDE_STYLE ('',( #48572 ) ) ;
#38369=DIRECTION ( 'NONE',  ( 0.000000000000000000, 1.000000000000000000, 0.000000000000000000 ) ) ;
#38371=DIRECTION ( 'NONE',  ( 0.000000000000000000, -0.000000000000000000, 1.000000000000000000 ) ) ;
#38377=CARTESIAN_POINT ( 'NONE',  ( -74.99999999999998579, 118.4999999999999716, 7.000000000000000000 ) ) ;
#38378=CARTESIAN_POINT ( 'NONE',  ( 40.99999999999998579, 108.0041655821620026, 3.000000000000000000 ) ) ;
#38379=ORIENTED_EDGE ( 'NONE', *, *, #41484, .F. ) ;
#38386=DIRECTION ( 'NONE',  ( 1.224646799147353207E-16, 1.000000000000000000, -0.000000000000000000 ) ) ;
#38389=FACE_OUTER_BOUND ( 'NONE', #23345, .T. ) ;
#38390=CIRCLE ( 'NONE', #5774, 0.5000000000000004441 ) ;
#38391=DIRECTION ( 'NONE',  ( -1.000000000000000000, 0.000000000000000000, 0.000000000000000000 ) ) ;
#38394=AXIS2_PLACEMENT_3D ( 'NONE', #18980, #52341, #50002 ) ;
#38395=( GEOMETRIC_REPRESENTATION_CONTEXT ( 3 ) GLOBAL_UNCERTAINTY_ASSIGNED_CONTEXT ( ( #35570 ) ) GLOBAL_UNIT_ASSIGNED_CONTEXT ( ( #7978, #2989, #24831 ) ) REPRESENTATION_CONTEXT ( 'NONE', 'WORKASPACE' ) );
#38397=CARTESIAN_POINT ( 'NONE',  ( -41.49999999999997868, 9.999999999999978684, -3.000000000000000444 ) ) ;
#38401=CARTESIAN_POINT ( 'NONE',  ( -3.094860106618432471, 110.7049999999999983, -9.525000000000000355 ) ) ;
#38405=( NAMED_UNIT ( * ) SI_UNIT ( $, .STERADIAN. ) SOLID_ANGLE_UNIT ( ) );
#38409=UNCERTAINTY_MEASURE_WITH_UNIT (LENGTH_MEASURE( 1.000000000000000082E-05 ), #13108, 'distance_accuracy_value', 'NONE');
#38410=APPLICATION_CONTEXT ( 'automotive_design' ) ;
#38411=ORIENTED_EDGE ( 'NONE', *, *, #14128, .F. ) ;
#38417=EDGE_CURVE ( 'NONE', #52608, #21468, #29539, .T. ) ;
#38419=PRESENTATION_STYLE_ASSIGNMENT (( #65076 ) ) ;
#38422=STYLED_ITEM ( 'NONE', ( #41690 ), #17186 ) ;
#38425=( NAMED_UNIT ( * ) SI_UNIT ( $, .STERADIAN. ) SOLID_ANGLE_UNIT ( ) );
#38427=AXIS2_PLACEMENT_3D ( 'NONE', #69311, #59779, #53138 ) ;
#38428=SURFACE_STYLE_FILL_AREA ( #38763 ) ;
#38434=VERTEX_POINT ( 'NONE', #19324 ) ;
#38435=LINE ( 'NONE', #65091, #22283 ) ;
#38436=( LENGTH_UNIT ( ) NAMED_UNIT ( * ) SI_UNIT ( .MILLI., .METRE. ) );
#38440=CARTESIAN_POINT ( 'NONE',  ( 8.102448949553183510, 132.9949999999999477, -5.886773742842746238 ) ) ;
#38445=CARTESIAN_POINT ( 'NONE',  ( 3.094860106618435136, 131.4050000000000011, -9.525000000000000355 ) ) ;
#38446=AXIS2_PLACEMENT_3D ( 'NONE', #68377, #5626, #27078 ) ;
#38451=CARTESIAN_POINT ( 'NONE',  ( -9.058813317711337021, 159.1550000000000011, -2.943386871421374895 ) ) ;
#38452=CARTESIAN_POINT ( 'NONE',  ( 9.827790563157511022E-16, 87.30187232391182306, -8.025000000000000355 ) ) ;
#38453=UNCERTAINTY_MEASURE_WITH_UNIT (LENGTH_MEASURE( 1.000000000000000082E-05 ), #57078, 'distance_accuracy_value', 'NONE');
#38454=MECHANICAL_DESIGN_GEOMETRIC_PRESENTATION_REPRESENTATION('',(#51914),#11421);
#38455=AXIS2_PLACEMENT_3D ( 'NONE', #48242, #53817, #4588 ) ;
#38457=COLOUR_RGB ( '', 0.31764706, 0.68627451, 0.89019608) ;
#38462=ORIENTED_EDGE ( 'NONE', *, *, #40356, .F. ) ;
#38463=UNCERTAINTY_MEASURE_WITH_UNIT (LENGTH_MEASURE( 1.000000000000000082E-05 ), #29674, 'distance_accuracy_value', 'NONE');
#38464=MECHANICAL_DESIGN_GEOMETRIC_PRESENTATION_REPRESENTATION('',(#20438),#24877);
#38465=DIRECTION ( 'NONE',  ( 1.000000000000000000, 0.000000000000000000, 0.000000000000000000 ) ) ;
#38466=( LENGTH_UNIT ( ) NAMED_UNIT ( * ) SI_UNIT ( .MILLI., .METRE. ) );
#38467=B_SPLINE_CURVE_WITH_KNOTS ( 'NONE', 3,
 ( #103, #49098, #21269, #20951 ),
 .UNSPECIFIED., .F., .F.,
 ( 4, 4 ),
 ( 0.01934061289150207363, 0.02044444614850437353 ),
 .UNSPECIFIED. ) ;
#38468=CARTESIAN_POINT ( 'NONE',  ( 47.50000000000000000, 14.49137674618942562, 10.00000000000000000 ) ) ;
#38469=DIRECTION ( 'NONE',  ( -0.000000000000000000, -0.000000000000000000, -1.000000000000000000 ) ) ;
#38470=AXIS2_PLACEMENT_3D ( 'NONE', #407, #1443, #65169 ) ;
#38472=CARTESIAN_POINT ( 'NONE',  ( -45.50000000000000000, 7.768687147774684831, -6.999999999999999112 ) ) ;
#38479=CARTESIAN_POINT ( 'NONE',  ( 74.99999999999998579, 50.00000000000000000, 9.500000000000000000 ) ) ;
#38482=( LENGTH_UNIT ( ) NAMED_UNIT ( * ) SI_UNIT ( .MILLI., .METRE. ) );
#38489=CARTESIAN_POINT ( 'NONE',  ( -1.166476076187854022E-15, 125.9449999999999790, 9.525000000000000355 ) ) ;
#38501=VERTEX_POINT ( 'NONE', #62581 ) ;
#38502=DIRECTION ( 'NONE',  ( -1.000000000000000000, 0.000000000000000000, 0.000000000000000000 ) ) ;
#38505=EDGE_CURVE ( 'NONE', #6097, #52429, #49963, .T. ) ;
#38507=CARTESIAN_POINT ( 'NONE',  ( -45.64543621907380100, 8.376853334107021709, 6.482973932537276163 ) ) ;
#38511=CARTESIAN_POINT ( 'NONE',  ( -60.00000000000000000, -2.024042244987997205E-14, -10.49999999999999822 ) ) ;
#38512=CARTESIAN_POINT ( 'NONE',  ( -60.00000000000000000, -2.024042244987997205E-14, -12.00000000000000000 ) ) ;
#38513=DIRECTION ( 'NONE',  ( 0.9486832980505138790, 0.3162277660168378857, -0.000000000000000000 ) ) ;
#38514=ADVANCED_FACE ( 'NONE', ( #18311 ), #34473, .F. ) ;
#38515=ORIENTED_EDGE ( 'NONE', *, *, #6287, .T. ) ;
#38518=MECHANICAL_DESIGN_GEOMETRIC_PRESENTATION_REPRESENTATION('',(#31727),#26100);
#38519=PRESENTATION_STYLE_ASSIGNMENT (( #60263 ) ) ;
#38523=CARTESIAN_POINT ( 'NONE',  ( -2.607480562269073765, 154.2070736234661865, -8.025000000000000355 ) ) ;
#38524=AXIS2_PLACEMENT_3D ( 'NONE', #29233, #67229, #45482 ) ;
#38525=ORIENTED_EDGE ( 'NONE', *, *, #20988, .F. ) ;
#38529=VECTOR ( 'NONE', #44084, 1000.000000000000000 ) ;
#38530=CARTESIAN_POINT ( 'NONE',  ( 4.716976649647099507, 132.7570736234661695, -6.492361379858953008 ) ) ;
#38531=( NAMED_UNIT ( * ) SI_UNIT ( $, .STERADIAN. ) SOLID_ANGLE_UNIT ( ) );
#38541=CARTESIAN_POINT ( 'NONE',  ( -44.99999999999999289, 8.674606743306377155, -5.942398972768217824 ) ) ;
#38543=FACE_OUTER_BOUND ( 'NONE', #10379, .T. ) ;
#38546=CARTESIAN_POINT ( 'NONE',  ( 45.00000000000000000, 10.00436330937237095, -6.147562757271016309 ) ) ;
#38547=CARTESIAN_POINT ( 'NONE',  ( -75.00000000000000000, 8.162286782231385374, 6.987283332039738504 ) ) ;
#38549=ORIENTED_EDGE ( 'NONE', *, *, #7588, .F. ) ;
#38551=STYLED_ITEM ( 'NONE', ( #39119 ), #22661 ) ;
#38552=CYLINDRICAL_SURFACE ( 'NONE', #7275, 0.5000000000000004441 ) ;
#38554=CARTESIAN_POINT ( 'NONE',  ( -71.50000000000000000, 14.49137674618942562, -9.500000000000000000 ) ) ;
#38556=COLOUR_RGB ( '', 0.08235294, 0.09019608, 0.10196078) ;
#38557=CARTESIAN_POINT ( 'NONE',  ( 10.01517768586949408, 135.6949999999999932, 1.839758294383810543E-15 ) ) ;
#38559=( NAMED_UNIT ( * ) SI_UNIT ( $, .STERADIAN. ) SOLID_ANGLE_UNIT ( ) );
#38561=CARTESIAN_POINT ( 'NONE',  ( -7.647808743681030030, 110.5000000000002984, 5.677732506914710875 ) ) ;
#38563=CARTESIAN_POINT ( 'NONE',  ( -72.49999999999998579, 64.07124727947029896, 9.500000000000000000 ) ) ;
#38567=CARTESIAN_POINT ( 'NONE',  ( -45.50000000000000000, -2.024042244987997205E-14, -9.500000000000000000 ) ) ;
#38578=AXIS2_PLACEMENT_3D ( 'NONE', #29217, #55630, #12344 ) ;
#38583=EDGE_CURVE ( 'NONE', #27901, #60674, #54799, .T. ) ;
#38585=COLOUR_RGB ( '', 0.09019608, 0.27058824, 0.51372549) ;
#38586=SURFACE_STYLE_USAGE ( .BOTH. , #54354 ) ;
#38593=CARTESIAN_POINT ( 'NONE',  ( 0.000000000000000000, 87.30187232391182306, 0.000000000000000000 ) ) ;
#38595=ORIENTED_EDGE ( 'NONE', *, *, #29621, .F. ) ;
#38597=CARTESIAN_POINT ( 'NONE',  ( 71.50000000000000000, 14.49137674618942562, -7.500000000000000000 ) ) ;
#38598=ORIENTED_EDGE ( 'NONE', *, *, #39982, .F. ) ;
#38600=CARTESIAN_POINT ( 'NONE',  ( -7.632228543268607446, 121.6570736234661609, -2.479861379858953718 ) ) ;
#38602=CIRCLE ( 'NONE', #51077, 13.49999999999999822 ) ;
#38603=( NAMED_UNIT ( * ) SI_UNIT ( $, .STERADIAN. ) SOLID_ANGLE_UNIT ( ) );
#38606=STYLED_ITEM ( 'NONE', ( #30585 ), #6454 ) ;
#38609=SURFACE_STYLE_FILL_AREA ( #27965 ) ;
#38611=CARTESIAN_POINT ( 'NONE',  ( 2.607480562268909008, 149.7929263765338135, -8.025000000000122924 ) ) ;
#38619=VERTEX_POINT ( 'NONE', #9838 ) ;
#38620=CARTESIAN_POINT ( 'NONE',  ( 74.50000000000000000, -2.135340797662720349E-14, -9.500000000000000000 ) ) ;
#38621=DIRECTION ( 'NONE',  ( 7.080503983578803083E-17, 1.000000000000000000, 0.000000000000000000 ) ) ;
#38622=ORIENTED_EDGE ( 'NONE', *, *, #26958, .F. ) ;
#38629=COLOUR_RGB ( '', 0.40784314, 0.44705882, 0.49803922) ;
#38631=LINE ( 'NONE', #18164, #17327 ) ;
#38634=CARTESIAN_POINT ( 'NONE',  ( -7.398101581744998434, 153.3646217335120809, -3.965660541892891189 ) ) ;
#38641=CYLINDRICAL_SURFACE ( 'NONE', #24864, 0.5000000000000004441 ) ;
#38651=VECTOR ( 'NONE', #15422, 1000.000000000000000 ) ;
#38653=SURFACE_STYLE_FILL_AREA ( #21732 ) ;
#38654=SURFACE_STYLE_FILL_AREA ( #6565 ) ;
#38655=DIRECTION ( 'NONE',  ( 0.000000000000000000, 0.000000000000000000, -1.000000000000000000 ) ) ;
#38656=VECTOR ( 'NONE', #6965, 1000.000000000000000 ) ;
#38658=DIRECTION ( 'NONE',  ( 0.000000000000000000, 1.000000000000000000, 0.000000000000000000 ) ) ;
#38662=CARTESIAN_POINT ( 'NONE',  ( -5.598654528085806881, 140.8549999999999898, -7.705886871421374629 ) ) ;
#38664=ADVANCED_FACE ( 'NONE', ( #2593 ), #48534, .T. ) ;
#38665=AXIS2_PLACEMENT_3D ( 'NONE', #44063, #59479, #41719 ) ;
#38666=CARTESIAN_POINT ( 'NONE',  ( 54.49999999999999289, 2.470600640510329340E-15, -6.500000000000000000 ) ) ;
#38669=VERTEX_POINT ( 'NONE', #48885 ) ;
#38670=EDGE_CURVE ( 'NONE', #40163, #1577, #29000, .T. ) ;
#38671=SURFACE_SIDE_STYLE ('',( #9918 ) ) ;
#38673=DIRECTION ( 'NONE',  ( 0.000000000000000000, -0.000000000000000000, 1.000000000000000000 ) ) ;
#38674=EDGE_LOOP ( 'NONE', ( #60525, #58752, #921 ) ) ;
#38678=SURFACE_SIDE_STYLE ('',( #59730 ) ) ;
#38679=AXIS2_PLACEMENT_3D ( 'NONE', #8143, #67936, #34513 ) ;
#38685=FILL_AREA_STYLE ('',( #28043 ) ) ;
#38686=CYLINDRICAL_SURFACE ( 'NONE', #26515, 0.5000000000000004441 ) ;
#38687=AXIS2_PLACEMENT_3D ( 'NONE', #27095, #58440, #31702 ) ;
#38693=CARTESIAN_POINT ( 'NONE',  ( -8.102448949553181734, 155.4950000000000045, 5.886773742842747126 ) ) ;
#38696=AXIS2_PLACEMENT_3D ( 'NONE', #44932, #8653, #18837 ) ;
#38697=EDGE_CURVE ( 'NONE', #68077, #65971, #470, .T. ) ;
#38702=VERTEX_POINT ( 'NONE', #66670 ) ;
#38703=CARTESIAN_POINT ( 'NONE',  ( 6.826472737025119919, 130.8929263765338362, 4.959722759717908325 ) ) ;
#38708=DIRECTION ( 'NONE',  ( 0.000000000000000000, 1.000000000000000000, -0.000000000000000000 ) ) ;
#38713=CIRCLE ( 'NONE', #42090, 0.4999999999999994449 ) ;
#38715=DIRECTION ( 'NONE',  ( 0.000000000000000000, 0.000000000000000000, 1.000000000000000000 ) ) ;
#38716=ORIENTED_EDGE ( 'NONE', *, *, #56725, .T. ) ;
#38717=STYLED_ITEM ( 'NONE', ( #9734 ), #26884 ) ;
#38721=CARTESIAN_POINT ( 'NONE',  ( -45.00000000000000000, 9.290263934145977842, -6.640705990143890070 ) ) ;
#38722=ORIENTED_EDGE ( 'NONE', *, *, #28972, .F. ) ;
#38723=ORIENTED_EDGE ( 'NONE', *, *, #45391, .F. ) ;
#38724=CARTESIAN_POINT ( 'NONE',  ( -44.99742101275325012, 9.654581538856286116, 3.431521703149617242 ) ) ;
#38725=SURFACE_SIDE_STYLE ('',( #17263 ) ) ;
#38727=AXIS2_PLACEMENT_3D ( 'NONE', #34193, #39494, #53150 ) ;
#38731=SURFACE_STYLE_USAGE ( .BOTH. , #49949 ) ;
#38740=FACE_OUTER_BOUND ( 'NONE', #34165, .T. ) ;
#38742=ADVANCED_FACE ( 'NONE', ( #4005 ), #46989, .F. ) ;
#38744=CARTESIAN_POINT ( 'NONE',  ( -9.058813317711338797, 155.3449999999999704, 2.943386871421373563 ) ) ;
#38746=DIRECTION ( 'NONE',  ( 0.000000000000000000, 0.000000000000000000, -1.000000000000000000 ) ) ;
#38747=CARTESIAN_POINT ( 'NONE',  ( -2.607480562269157254, 141.0929263765338533, -8.024999999999939959 ) ) ;
#38748=STYLED_ITEM ( 'NONE', ( #51509 ), #37546 ) ;
#38751=ORIENTED_EDGE ( 'NONE', *, *, #34532, .T. ) ;
#38753=AXIS2_PLACEMENT_3D ( 'NONE', #3430, #25964, #68914 ) ;
#38756=CARTESIAN_POINT ( 'NONE',  ( 0.000000000000000000, 87.30187232391182306, 0.000000000000000000 ) ) ;
#38763=FILL_AREA_STYLE ('',( #43696 ) ) ;
#38765=ORIENTED_EDGE ( 'NONE', *, *, #48092, .F. ) ;
#38770=CARTESIAN_POINT ( 'NONE',  ( 0.000000000000000000, 154.9999999999999716, -23.00000000000000000 ) ) ;
#38776=FILL_AREA_STYLE ('',( #45093 ) ) ;
#38777=CARTESIAN_POINT ( 'NONE',  ( -5.598654528085806881, 133.7450000000000045, -7.705886871421374629 ) ) ;
#38778=SURFACE_STYLE_FILL_AREA ( #33121 ) ;
#38781=CARTESIAN_POINT ( 'NONE',  ( -9.058813317711337021, 126.1549999999999869, -2.943386871421374895 ) ) ;
#38783=VERTEX_POINT ( 'NONE', #13530 ) ;
#38784=CARTESIAN_POINT ( 'NONE',  ( 3.094860106618435136, 158.4049999999999727, -9.525000000000000355 ) ) ;
#38788=STYLED_ITEM ( 'NONE', ( #39618 ), #38664 ) ;
#38790=VERTEX_POINT ( 'NONE', #57134 ) ;
#38791=AXIS2_PLACEMENT_3D ( 'NONE', #7165, #60953, #28594 ) ;
#38792=FILL_AREA_STYLE_COLOUR ( '', #7071 ) ;
#38799=AXIS2_PLACEMENT_3D ( 'NONE', #17721, #39192, #45169 ) ;
#38800=DIRECTION ( 'NONE',  ( 0.6842105263157866046, 0.7292845505553195995, 0.000000000000000000 ) ) ;
#38801=EDGE_CURVE ( 'NONE', #32321, #6265, #63450, .T. ) ;
#38802=( NAMED_UNIT ( * ) SI_UNIT ( $, .STERADIAN. ) SOLID_ANGLE_UNIT ( ) );
#38805=ORIENTED_EDGE ( 'NONE', *, *, #39333, .T. ) ;
#38806=CARTESIAN_POINT ( 'NONE',  ( -44.99154893936432842, 9.591540374752314690, -3.000000000000000444 ) ) ;
#38812=PRESENTATION_STYLE_ASSIGNMENT (( #22597 ) ) ;
#38813=FILL_AREA_STYLE ('',( #39154 ) ) ;
#38816=AXIS2_PLACEMENT_3D ( 'NONE', #46421, #25943, #3776 ) ;
#38818=VERTEX_POINT ( 'NONE', #58190 ) ;
#38819=CARTESIAN_POINT ( 'NONE',  ( -75.50000000000000000, 64.49137674618943095, -9.500000000000001776 ) ) ;
#38820=PRESENTATION_STYLE_ASSIGNMENT (( #6406 ) ) ;
#38823=AXIS2_PLACEMENT_3D ( 'NONE', #42821, #54691, #27600 ) ;
#38824=CARTESIAN_POINT ( 'NONE',  ( -5.598654528085808657, 128.6449999999999818, 7.705886871421373741 ) ) ;
#38826=COLOUR_RGB ( '', 0.09019608, 0.27058824, 0.51372549) ;
#38833=AXIS2_PLACEMENT_3D ( 'NONE', #64771, #10277, #32068 ) ;
#38835=STYLED_ITEM ( 'NONE', ( #46582 ), #57826 ) ;
#38836=FACE_OUTER_BOUND ( 'NONE', #49295, .T. ) ;
#38837=VERTEX_POINT ( 'NONE', #32148 ) ;
#38842=VECTOR ( 'NONE', #33119, 1000.000000000000000 ) ;
#38848=CARTESIAN_POINT ( 'NONE',  ( -74.99999999999998579, 50.00000000000000000, -11.50000000000001066 ) ) ;
#38854=FILL_AREA_STYLE ('',( #54633 ) ) ;
#38855=DIRECTION ( 'NONE',  ( 0.000000000000000000, 0.000000000000000000, -1.000000000000000000 ) ) ;
#38856=PRESENTATION_STYLE_ASSIGNMENT (( #1808 ) ) ;
#38857=CARTESIAN_POINT ( 'NONE',  ( -6.826472737025120807, 152.1070736234661354, 4.959722759717906548 ) ) ;
#38863=MECHANICAL_DESIGN_GEOMETRIC_PRESENTATION_REPRESENTATION('',(#16423),#61307);
#38865=DIRECTION ( 'NONE',  ( 1.000000000000000000, 0.000000000000000000, 0.000000000000000000 ) ) ;
#38866=CARTESIAN_POINT ( 'NONE',  ( -23.71231517720798010, 112.9999999999999858, 9.500000000000000000 ) ) ;
#38869=ORIENTED_EDGE ( 'NONE', *, *, #32386, .F. ) ;
#38870=MECHANICAL_DESIGN_GEOMETRIC_PRESENTATION_REPRESENTATION('',(#29833),#602);
#38874=VERTEX_POINT ( 'NONE', #16690 ) ;
#38875=PLANE ( 'NONE',  #21558 ) ;
#38876=LINE ( 'NONE', #66966, #48101 ) ;
#38877=CARTESIAN_POINT ( 'NONE',  ( -45.82429090095276791, 9.081512406228320344, -6.320717432316791395 ) ) ;
#38879=SURFACE_STYLE_USAGE ( .BOTH. , #49402 ) ;
#38881=COLOUR_RGB ( '', 0.08235294, 0.09019608, 0.10196078) ;
#38882=CARTESIAN_POINT ( 'NONE',  ( -75.00000000000000000, 7.768687147774684831, 7.000000000000004441 ) ) ;
#38886=DIRECTION ( 'NONE',  ( 0.000000000000000000, 0.000000000000000000, -1.000000000000000000 ) ) ;
#38888=DIRECTION ( 'NONE',  ( -0.000000000000000000, -0.000000000000000000, 1.000000000000000000 ) ) ;
#38890=STYLED_ITEM ( 'NONE', ( #18357 ), #1791 ) ;
#38891=FILL_AREA_STYLE ('',( #27905 ) ) ;
#38894=CARTESIAN_POINT ( 'NONE',  ( 3.094860106618435136, 133.2949999999999875, -9.525000000000000355 ) ) ;
#38895=AXIS2_PLACEMENT_3D ( 'NONE', #39711, #61130, #55855 ) ;
#38897=ADVANCED_FACE ( 'NONE', ( #69438 ), #5736, .T. ) ;
#38898=CIRCLE ( 'NONE', #54563, 8.000000000000000000 ) ;
#38901=FILL_AREA_STYLE ('',( #18780 ) ) ;
#38902=DIRECTION ( 'NONE',  ( 0.000000000000000000, 0.000000000000000000, 1.000000000000000000 ) ) ;
#38903=ADVANCED_FACE ( 'NONE', ( #45163 ), #39889, .T. ) ;
#38906=CARTESIAN_POINT ( 'NONE',  ( 15.48999599679679662, 117.9999999999999716, 9.500000000000000000 ) ) ;
#38909=EDGE_LOOP ( 'NONE', ( #62356, #39012, #785, #33283 ) ) ;
#38911=CARTESIAN_POINT ( 'NONE',  ( 45.00320036294424852, 10.00106678764806567, -3.045234739864692397 ) ) ;
#38912=SURFACE_SIDE_STYLE ('',( #65599 ) ) ;
#38916=( LENGTH_UNIT ( ) NAMED_UNIT ( * ) SI_UNIT ( .MILLI., .METRE. ) );
#38919=FILL_AREA_STYLE_COLOUR ( '', #52292 ) ;
#38922=CIRCLE ( 'NONE', #20915, 1.000000000000000888 ) ;
#38928=DIRECTION ( 'NONE',  ( -0.000000000000000000, -0.000000000000000000, -1.000000000000000000 ) ) ;
#38931=SURFACE_SIDE_STYLE ('',( #48791 ) ) ;
#38932=AXIS2_PLACEMENT_3D ( 'NONE', #55853, #7652, #57956 ) ;
#38933=DIRECTION ( 'NONE',  ( 0.000000000000000000, 0.000000000000000000, 1.000000000000000000 ) ) ;
#38936=DIRECTION ( 'NONE',  ( 0.000000000000000000, 0.000000000000000000, 1.000000000000000000 ) ) ;
#38940=CARTESIAN_POINT ( 'NONE',  ( 8.437984349512095861, 126.3070736234661666, 1.550032578732817026E-15 ) ) ;
#38941=SURFACE_SIDE_STYLE ('',( #12494 ) ) ;
#38942=CARTESIAN_POINT ( 'NONE',  ( 74.65811388299935913, 19.88603796099976506, -6.065461639931112536 ) ) ;
#38943=DIRECTION ( 'NONE',  ( -0.000000000000000000, -0.000000000000000000, -1.000000000000000000 ) ) ;
#38944=VERTEX_POINT ( 'NONE', #12753 ) ;
#38948=CARTESIAN_POINT ( 'NONE',  ( 34.99999999999999289, 99.99999999999998579, 7.000000000000000000 ) ) ;
#38950=EDGE_CURVE ( 'NONE', #29016, #8709, #17476, .T. ) ;
#38958=UNCERTAINTY_MEASURE_WITH_UNIT (LENGTH_MEASURE( 1.000000000000000082E-05 ), #32581, 'distance_accuracy_value', 'NONE');
#38960=CARTESIAN_POINT ( 'NONE',  ( -4.716976649647098618, 160.1429263765338362, 6.492361379858953008 ) ) ;
#38962=ADVANCED_FACE ( 'NONE', ( #1459 ), #2505, .F. ) ;
#38966=VERTEX_POINT ( 'NONE', #30299 ) ;
#38970=ORIENTED_EDGE ( 'NONE', *, *, #39501, .F. ) ;
#38972=MECHANICAL_DESIGN_GEOMETRIC_PRESENTATION_REPRESENTATION('',(#63629),#62512);
#38973=PRESENTATION_STYLE_ASSIGNMENT (( #65656 ) ) ;
#38977=DIRECTION ( 'NONE',  ( 0.000000000000000000, 0.000000000000000000, 1.000000000000000000 ) ) ;
#38980=EDGE_CURVE ( 'NONE', #29123, #54714, #51161, .T. ) ;
#38983=CARTESIAN_POINT ( 'NONE',  ( 34.99999999999992895, 109.9999999999999858, 10.00000000000000000 ) ) ;
#38987=CIRCLE ( 'NONE', #43472, 8.025000000000000355 ) ;
#38990=( LENGTH_UNIT ( ) NAMED_UNIT ( * ) SI_UNIT ( .MILLI., .METRE. ) );
#39002=CARTESIAN_POINT ( 'NONE',  ( -3.094860106618434248, 147.9049999999999727, 9.525000000000000355 ) ) ;
#39005=UNCERTAINTY_MEASURE_WITH_UNIT (LENGTH_MEASURE( 1.000000000000000082E-05 ), #29073, 'distance_accuracy_value', 'NONE');
#39006=B_SPLINE_CURVE_WITH_KNOTS ( 'NONE', 3,
 ( #68884, #31205, #57263, #37248, #52700, #68186, #19964, #58307, #20684, #14719, #10131, #57624 ),
 .UNSPECIFIED., .F., .F.,
 ( 4, 2, 2, 2, 2, 4 ),
 ( 0.000000000000000000, 0.0001178293706450991933, 0.0002356587412901983865, 0.0004713174825804007304, 0.0009426349651608007018, 0.001885269930321605523 ),
 .UNSPECIFIED. ) ;
#39009=ORIENTED_EDGE ( 'NONE', *, *, #34880, .F. ) ;
#39011=DIRECTION ( 'NONE',  ( -0.000000000000000000, -0.000000000000000000, -1.000000000000000000 ) ) ;
#39012=ORIENTED_EDGE ( 'NONE', *, *, #55012, .T. ) ;
#39014=CARTESIAN_POINT ( 'NONE',  ( -4.716976649647098618, 136.1429263765338362, 6.492361379858953008 ) ) ;
#39017=CARTESIAN_POINT ( 'NONE',  ( -41.84210526315788314, 107.2928455055531600, 4.000000000000000000 ) ) ;
#39021=SURFACE_STYLE_FILL_AREA ( #32653 ) ;
#39022=( GEOMETRIC_REPRESENTATION_CONTEXT ( 3 ) GLOBAL_UNCERTAINTY_ASSIGNED_CONTEXT ( ( #36275 ) ) GLOBAL_UNIT_ASSIGNED_CONTEXT ( ( #14419, #35892, #13379 ) ) REPRESENTATION_CONTEXT ( 'NONE', 'WORKASPACE' ) );
#39023=EDGE_CURVE ( 'NONE', #63887, #9536, #34276, .T. ) ;
#39027=ORIENTED_EDGE ( 'NONE', *, *, #27918, .T. ) ;
#39028=FILL_AREA_STYLE_COLOUR ( '', #41147 ) ;
#39029=FILL_AREA_STYLE_COLOUR ( '', #46284 ) ;
#39032=EDGE_CURVE ( 'NONE', #7249, #38874, #40923, .T. ) ;
#39034=CARTESIAN_POINT ( 'NONE',  ( -8.091123032493692691, 110.4999999999999858, -5.044978548556969145 ) ) ;
#39035=FILL_AREA_STYLE ('',( #17570 ) ) ;
#39039=CARTESIAN_POINT ( 'NONE',  ( -4.716976649647097730, 135.2429263765338305, -6.492361379858953896 ) ) ;
#39040=FACE_OUTER_BOUND ( 'NONE', #47790, .T. ) ;
#39049=SURFACE_SIDE_STYLE ('',( #29110 ) ) ;
#39051=FILL_AREA_STYLE ('',( #11236 ) ) ;
#39053=FILL_AREA_STYLE_COLOUR ( '', #45503 ) ;
#39057=EDGE_CURVE ( 'NONE', #20853, #4364, #46205, .T. ) ;
#39059=FILL_AREA_STYLE_COLOUR ( '', #34811 ) ;
#39063=CARTESIAN_POINT ( 'NONE',  ( -45.21668476452690300, 8.382617247417337936, 3.141345821310664643 ) ) ;
#39068=FACE_OUTER_BOUND ( 'NONE', #12216, .T. ) ;
#39077=DIRECTION ( 'NONE',  ( -0.000000000000000000, -0.000000000000000000, 1.000000000000000000 ) ) ;
#39078=MECHANICAL_DESIGN_GEOMETRIC_PRESENTATION_REPRESENTATION('',(#21059),#54726);
#39081=CARTESIAN_POINT ( 'NONE',  ( 10.01517768586949231, 156.6949999999999932, 1.839758294383810543E-15 ) ) ;
#39083=CARTESIAN_POINT ( 'NONE',  ( 0.000000000000000000, 112.0570736234661666, -8.025000000000000355 ) ) ;
#39084=CARTESIAN_POINT ( 'NONE',  ( -7.632228543268607446, 141.5429263765338135, -2.479861379858953718 ) ) ;
#39085=CARTESIAN_POINT ( 'NONE',  ( 71.50000000000000000, 35.92875272052971525, -7.000000000000000000 ) ) ;
#39087=UNCERTAINTY_MEASURE_WITH_UNIT (LENGTH_MEASURE( 1.000000000000000082E-05 ), #68008, 'distance_accuracy_value', 'NONE');
#39088=EDGE_CURVE ( 'NONE', #42646, #44927, #60134, .T. ) ;
#39089=DIRECTION ( 'NONE',  ( -0.000000000000000000, -0.000000000000000000, -1.000000000000000000 ) ) ;
#39090=DIRECTION ( 'NONE',  ( -0.000000000000000000, -0.000000000000000000, -1.000000000000000000 ) ) ;
#39095=FILL_AREA_STYLE_COLOUR ( '', #49370 ) ;
#39097=SURFACE_STYLE_USAGE ( .BOTH. , #18306 ) ;
#39098=ORIENTED_EDGE ( 'NONE', *, *, #18808, .T. ) ;
#39101=VECTOR ( 'NONE', #19741, 1000.000000000000000 ) ;
#39102=SURFACE_STYLE_USAGE ( .BOTH. , #55586 ) ;
#39104=STYLED_ITEM ( 'NONE', ( #17412 ), #50731 ) ;
#39106=AXIS2_PLACEMENT_3D ( 'NONE', #2980, #24468, #58236 ) ;
#39107=ORIENTED_EDGE ( 'NONE', *, *, #10012, .F. ) ;
#39114=ORIENTED_EDGE ( 'NONE', *, *, #22888, .T. ) ;
#39118=CARTESIAN_POINT ( 'NONE',  ( -9.058813317711337021, 131.0449999999999875, -2.943386871421374895 ) ) ;
#39119=PRESENTATION_STYLE_ASSIGNMENT (( #33791 ) ) ;
#39121=CARTESIAN_POINT ( 'NONE',  ( 3.094860106618435136, 128.4049999999999727, -9.525000000000000355 ) ) ;
#39122=ADVANCED_FACE ( 'NONE', ( #57775 ), #35625, .T. ) ;
#39124=CARTESIAN_POINT ( 'NONE',  ( 41.01786561352940907, 107.7208547478738012, -3.150777047984585799 ) ) ;
#39125=VERTEX_POINT ( 'NONE', #64065 ) ;
#39126=CARTESIAN_POINT ( 'NONE',  ( -10.01517768586949231, 156.3049999999999500, -6.132527647946036459E-16 ) ) ;
#39127=DIRECTION ( 'NONE',  ( -0.000000000000000000, 1.000000000000000000, -0.000000000000000000 ) ) ;
#39128=UNCERTAINTY_MEASURE_WITH_UNIT (LENGTH_MEASURE( 1.000000000000000082E-05 ), #54976, 'distance_accuracy_value', 'NONE');
#39129=AXIS2_PLACEMENT_3D ( 'NONE', #15296, #52225, #30719 ) ;
#39134=DIRECTION ( 'NONE',  ( -0.000000000000000000, -0.000000000000000000, 1.000000000000000000 ) ) ;
#39135=EDGE_CURVE ( 'NONE', #60144, #10312, #65760, .T. ) ;
#39138=PRESENTATION_STYLE_ASSIGNMENT (( #60883 ) ) ;
#39140=ORIENTED_EDGE ( 'NONE', *, *, #69644, .F. ) ;
#39142=UNCERTAINTY_MEASURE_WITH_UNIT (LENGTH_MEASURE( 1.000000000000000082E-05 ), #22990, 'distance_accuracy_value', 'NONE');
#39143=FILL_AREA_STYLE_COLOUR ( '', #41888 ) ;
#39144=ADVANCED_FACE ( 'NONE', ( #15919 ), #38073, .F. ) ;
#39147=ORIENTED_EDGE ( 'NONE', *, *, #67762, .F. ) ;
#39148=ORIENTED_EDGE ( 'NONE', *, *, #62968, .T. ) ;
#39149=CARTESIAN_POINT ( 'NONE',  ( -45.00000000000000000, 9.708372675170616972, -3.611004237778681958 ) ) ;
#39152=ORIENTED_EDGE ( 'NONE', *, *, #24941, .T. ) ;
#39154=FILL_AREA_STYLE_COLOUR ( '', #13964 ) ;
#39155=CARTESIAN_POINT ( 'NONE',  ( -75.00000000000000000, 8.537325437491082525, -6.129378421684882561 ) ) ;
#39156=ORIENTED_EDGE ( 'NONE', *, *, #52042, .T. ) ;
#39157=CARTESIAN_POINT ( 'NONE',  ( 20.71231517720798010, 149.9999999999999716, -10.00000000000000000 ) ) ;
#39158=CONICAL_SURFACE ( 'NONE', #57090, 8.025000000000000355, 0.7853981633974491672 ) ;
#39159=PLANE ( 'NONE',  #15643 ) ;
#39160=CIRCLE ( 'NONE', #23347, 5.500000000000005329 ) ;
#39161=CARTESIAN_POINT ( 'NONE',  ( -9.058813317711338797, 125.3449999999999847, 2.943386871421373563 ) ) ;
#39163=LINE ( 'NONE', #34533, #61760 ) ;
#39164=STYLED_ITEM ( 'NONE', ( #35893 ), #655 ) ;
#39172=ORIENTED_EDGE ( 'NONE', *, *, #50296, .F. ) ;
#39177=DIRECTION ( 'NONE',  ( -0.000000000000000000, -0.000000000000000000, -1.000000000000000000 ) ) ;
#39179=FACE_OUTER_BOUND ( 'NONE', #1476, .T. ) ;
#39182=DIRECTION ( 'NONE',  ( -0.000000000000000000, -0.000000000000000000, -1.000000000000000000 ) ) ;
#39188=ORIENTED_EDGE ( 'NONE', *, *, #34871, .T. ) ;
#39192=DIRECTION ( 'NONE',  ( 1.000000000000000000, -4.336808689941999001E-16, 0.000000000000000000 ) ) ;
#39193=CARTESIAN_POINT ( 'NONE',  ( 6.826472737025119919, 156.0070736234661695, 4.959722759717908325 ) ) ;
#39195=EDGE_LOOP ( 'NONE', ( #19868, #68245, #19363, #67610 ) ) ;
#39197=CARTESIAN_POINT ( 'NONE',  ( 3.094860106618435136, 125.4050000000000011, -9.525000000000000355 ) ) ;
#39198=UNCERTAINTY_MEASURE_WITH_UNIT (LENGTH_MEASURE( 1.000000000000000082E-05 ), #5256, 'distance_accuracy_value', 'NONE');
#39199=STYLED_ITEM ( 'NONE', ( #9581 ), #51228 ) ;
#39200=STYLED_ITEM ( 'NONE', ( #788 ), #66391 ) ;
#39202=ADVANCED_FACE ( 'NONE', ( #21154 ), #2051, .F. ) ;
#39204=VERTEX_POINT ( 'NONE', #69021 ) ;
#39205=CIRCLE ( 'NONE', #48202, 0.5000000000000004441 ) ;
#39206=DIRECTION ( 'NONE',  ( 0.000000000000000000, 0.000000000000000000, 1.000000000000000000 ) ) ;
#39210=FACE_OUTER_BOUND ( 'NONE', #8716, .T. ) ;
#39215=FILL_AREA_STYLE ('',( #17745 ) ) ;
#39222=CARTESIAN_POINT ( 'NONE',  ( 20.12916642283592950, 109.9999999999999858, -10.05319148936170137 ) ) ;
#39224=DIRECTION ( 'NONE',  ( -0.000000000000000000, -0.000000000000000000, -1.000000000000000000 ) ) ;
#39225=LINE ( 'NONE', #54998, #24084 ) ;
#39226=CARTESIAN_POINT ( 'NONE',  ( -40.49999999999998579, 107.7459666924148394, 10.00000000000000000 ) ) ;
#39228=EDGE_CURVE ( 'NONE', #46742, #34097, #68083, .T. ) ;
#39230=CARTESIAN_POINT ( 'NONE',  ( -9.058813317711337021, 128.0449999999999875, -2.943386871421374895 ) ) ;
#39232=MECHANICAL_DESIGN_GEOMETRIC_PRESENTATION_REPRESENTATION('',(#7753),#68424);
#39234=ORIENTED_EDGE ( 'NONE', *, *, #4593, .F. ) ;
#39237=COLOUR_RGB ( '', 0.72549020, 0.75294118, 0.79215686) ;
#39242=COLOUR_RGB ( '', 0.66274510, 0.83137255, 0.94901961) ;
#39243=AXIS2_PLACEMENT_3D ( 'NONE', #42575, #63978, #53448 ) ;
#39247=( BOUNDED_CURVE ( )  B_SPLINE_CURVE ( 2, ( #56715, #46189, #50391, #8865, #66928, #50740, #61968, #18392, #61282, #8536, #24669 ),
 .UNSPECIFIED., .F., .F. ) 
 B_SPLINE_CURVE_WITH_KNOTS ( ( 3, 2, 2, 2, 2, 3 ),
 ( 0.3529411764705882582, 0.3588235294117647078, 0.3647058823529411575, 0.3705882352941177182, 0.3764705882352941679, 0.3823529411764706176 ),
 .UNSPECIFIED. ) 
 CURVE ( )  GEOMETRIC_REPRESENTATION_ITEM ( )  RATIONAL_B_SPLINE_CURVE ( ( 1.000000000000000000, 0.9510565162951535312, 1.000000000000000000, 0.9510565162951535312, 1.000000000000000000, 0.9510565162951535312, 1.000000000000000000, 0.9510565162951535312, 1.000000000000000000, 0.9510565162951530871, 1.000000000000000444 ) ) 
 REPRESENTATION_ITEM ( '' )  );
#39252=SURFACE_STYLE_FILL_AREA ( #8859 ) ;
#39256=AXIS2_PLACEMENT_3D ( 'NONE', #21560, #26800, #48333 ) ;
#39258=FILL_AREA_STYLE ('',( #1532 ) ) ;
#39266=COLOUR_RGB ( '', 0.40784314, 0.44705882, 0.49803922) ;
#39268=ADVANCED_FACE ( 'NONE', ( #12315 ), #56826, .F. ) ;
#39272=ORIENTED_EDGE ( 'NONE', *, *, #19865, .T. ) ;
#39274=CARTESIAN_POINT ( 'NONE',  ( 6.826472737025121695, 123.6070736234661496, -4.959722759717905660 ) ) ;
#39276=DIRECTION ( 'NONE',  ( -0.000000000000000000, -0.000000000000000000, -1.000000000000000000 ) ) ;
#39277=AXIS2_PLACEMENT_3D ( 'NONE', #62389, #57102, #8924 ) ;
#39280=LINE ( 'NONE', #45261, #25971 ) ;
#39285=VECTOR ( 'NONE', #21251, 1000.000000000000000 ) ;
#39290=( GEOMETRIC_REPRESENTATION_CONTEXT ( 3 ) GLOBAL_UNCERTAINTY_ASSIGNED_CONTEXT ( ( #50860 ) ) GLOBAL_UNIT_ASSIGNED_CONTEXT ( ( #27904, #22672, #1137 ) ) REPRESENTATION_CONTEXT ( 'NONE', 'WORKASPACE' ) );
#39291=CARTESIAN_POINT ( 'NONE',  ( -7.632228543268607446, 123.5429263765338135, -2.479861379858953718 ) ) ;
#39292=CARTESIAN_POINT ( 'NONE',  ( 45.00000000000000000, 9.916356254361542000, 6.999999999944074069 ) ) ;
#39294=CARTESIAN_POINT ( 'NONE',  ( 0.000000000000000000, 161.9429263765338192, -8.025000000000000355 ) ) ;
#39301=DIRECTION ( 'NONE',  ( 0.000000000000000000, 0.000000000000000000, 1.000000000000000000 ) ) ;
#39302=DIRECTION ( 'NONE',  ( 0.000000000000000000, 0.000000000000000000, 1.000000000000000000 ) ) ;
#39304=( GEOMETRIC_REPRESENTATION_CONTEXT ( 3 ) GLOBAL_UNCERTAINTY_ASSIGNED_CONTEXT ( ( #43322 ) ) GLOBAL_UNIT_ASSIGNED_CONTEXT ( ( #26400, #4952, #15537 ) ) REPRESENTATION_CONTEXT ( 'NONE', 'WORKASPACE' ) );
#39305=DIRECTION ( 'NONE',  ( -1.000000000000000000, 0.000000000000000000, 0.000000000000000000 ) ) ;
#39306=FACE_OUTER_BOUND ( 'NONE', #47364, .T. ) ;
#39310=CARTESIAN_POINT ( 'NONE',  ( 45.50000000000000000, 9.639620389971920389, 6.500000000000000000 ) ) ;
#39312=DIRECTION ( 'NONE',  ( 0.000000000000000000, 0.000000000000000000, -1.000000000000000000 ) ) ;
#39313=DIRECTION ( 'NONE',  ( 1.000000000000000000, 0.000000000000000000, -0.000000000000000000 ) ) ;
#39325=( NAMED_UNIT ( * ) SI_UNIT ( $, .STERADIAN. ) SOLID_ANGLE_UNIT ( ) );
#39327=SURFACE_STYLE_FILL_AREA ( #43584 ) ;
#39331=CARTESIAN_POINT ( 'NONE',  ( -5.598654528085806881, 146.8549999999999898, -7.705886871421374629 ) ) ;
#39332=FILL_AREA_STYLE_COLOUR ( '', #6165 ) ;
#39333=EDGE_CURVE ( 'NONE', #56654, #39825, #6248, .T. ) ;
#39334=CIRCLE ( 'NONE', #14604, 0.5000000000000004441 ) ;
#39335=AXIS2_PLACEMENT_3D ( 'NONE', #64760, #65080, #59822 ) ;
#39338=CARTESIAN_POINT ( 'NONE',  ( 60.00000000000000000, 1.797044900979284448E-15, -10.49999999999999822 ) ) ;
#39339=FILL_AREA_STYLE ('',( #49880 ) ) ;
#39345=CARTESIAN_POINT ( 'NONE',  ( 20.71231517720798010, 149.9999999999999716, -10.00000000000000000 ) ) ;
#39347=ADVANCED_FACE ( 'NONE', ( #44743, #13030, #54204, #27457 ), #35878, .F. ) ;
#39348=DIRECTION ( 'NONE',  ( -1.000000000000000000, 0.000000000000000000, 0.000000000000000000 ) ) ;
#39349=ORIENTED_EDGE ( 'NONE', *, *, #18581, .T. ) ;
#39351=SURFACE_STYLE_USAGE ( .BOTH. , #38678 ) ;
#39354=EDGE_CURVE ( 'NONE', #61898, #2846, #61277, .T. ) ;
#39355=FILL_AREA_STYLE_COLOUR ( '', #22636 ) ;
#39356=FACE_OUTER_BOUND ( 'NONE', #2125, .T. ) ;
#39357=VECTOR ( 'NONE', #69248, 1000.000000000000000 ) ;
#39358=CARTESIAN_POINT ( 'NONE',  ( 45.65811388300841855, 10.21937129433612057, -6.500000000000000000 ) ) ;
#39362=DIRECTION ( 'NONE',  ( 0.000000000000000000, 0.000000000000000000, -1.000000000000000000 ) ) ;
#39365=DIRECTION ( 'NONE',  ( 0.000000000000000000, 0.000000000000000000, 1.000000000000000000 ) ) ;
#39369=ORIENTED_EDGE ( 'NONE', *, *, #57027, .T. ) ;
#39370=ORIENTED_EDGE ( 'NONE', *, *, #24599, .T. ) ;
#39371=CARTESIAN_POINT ( 'NONE',  ( -74.10731665482167330, 9.343685333619710320, -6.169793031889357238 ) ) ;
#39373=STYLED_ITEM ( 'NONE', ( #65435 ), #44762 ) ;
#39374=PRESENTATION_STYLE_ASSIGNMENT (( #1659 ) ) ;
#39376=CARTESIAN_POINT ( 'NONE',  ( -4.716976649647097730, 132.2429263765338021, -6.492361379858953896 ) ) ;
#39380=CARTESIAN_POINT ( 'NONE',  ( 60.00000000000000000, 112.4999999999999858, -9.500000000000000000 ) ) ;
#39381=VERTEX_POINT ( 'NONE', #8469 ) ;
#39382=MECHANICAL_DESIGN_GEOMETRIC_PRESENTATION_REPRESENTATION('',(#24722),#42772);
#39385=DIRECTION ( 'NONE',  ( -1.000000000000000000, 0.000000000000000000, 0.000000000000000000 ) ) ;
#39386=CIRCLE ( 'NONE', #13483, 5.000000000000004441 ) ;
#39387=CARTESIAN_POINT ( 'NONE',  ( -6.826472737025120807, 140.1070736234661638, 4.959722759717906548 ) ) ;
#39388=CARTESIAN_POINT ( 'NONE',  ( -71.99999999999998579, 119.9999999999997868, -9.500000000000000000 ) ) ;
#39390=( NAMED_UNIT ( * ) SI_UNIT ( $, .STERADIAN. ) SOLID_ANGLE_UNIT ( ) );
#39391=CIRCLE ( 'NONE', #50607, 9.999999999999998224 ) ;
#39393=CARTESIAN_POINT ( 'NONE',  ( -66.49999999999998579, 50.00000000000000000, -12.00000000000000000 ) ) ;
#39394=CIRCLE ( 'NONE', #21373, 0.5000000000000004441 ) ;
#39399=VERTEX_POINT ( 'NONE', #52079 ) ;
#39400=CARTESIAN_POINT ( 'NONE',  ( -45.89905495956738690, 9.405628579031734660, 2.999999999999999556 ) ) ;
#39404=DIRECTION ( 'NONE',  ( 0.000000000000000000, 1.000000000000000000, 0.000000000000000000 ) ) ;
#39406=LINE ( 'NONE', #12625, #56527 ) ;
#39411=DIRECTION ( 'NONE',  ( 1.000000000000000000, -0.000000000000000000, -0.000000000000000000 ) ) ;
#39416=CARTESIAN_POINT ( 'NONE',  ( 6.826472737025119919, 117.0070736234661410, 4.959722759717908325 ) ) ;
#39417=CARTESIAN_POINT ( 'NONE',  ( 6.402811457828279984, 154.5000000000000284, -7.065455983348243763 ) ) ;
#39422=CARTESIAN_POINT ( 'NONE',  ( 0.000000000000000000, 119.5549999999999926, -9.525000000000000355 ) ) ;
#39431=CARTESIAN_POINT ( 'NONE',  ( 41.84210526315788314, 107.2928455055531600, -4.000000000000000000 ) ) ;
#39435=MECHANICAL_DESIGN_GEOMETRIC_PRESENTATION_REPRESENTATION('',(#1104),#17088);
#39445=EDGE_CURVE ( 'NONE', #61513, #64160, #19338, .T. ) ;
#39449=DIRECTION ( 'NONE',  ( 0.000000000000000000, 0.000000000000000000, 1.000000000000000000 ) ) ;
#39450=( LENGTH_UNIT ( ) NAMED_UNIT ( * ) SI_UNIT ( .MILLI., .METRE. ) );
#39454=ORIENTED_EDGE ( 'NONE', *, *, #69490, .T. ) ;
#39456=EDGE_LOOP ( 'NONE', ( #16568, #63340, #10933 ) ) ;
#39457=AXIS2_PLACEMENT_3D ( 'NONE', #34419, #55530, #51298 ) ;
#39458=SURFACE_SIDE_STYLE ('',( #40147 ) ) ;
#39459=FACE_OUTER_BOUND ( 'NONE', #48388, .T. ) ;
#39460=CARTESIAN_POINT ( 'NONE',  ( 3.094860106618435136, 130.2949999999999591, -9.525000000000000355 ) ) ;
#39462=CIRCLE ( 'NONE', #55119, 8.000000000000007105 ) ;
#39464=CARTESIAN_POINT ( 'NONE',  ( 45.50000000000000000, 10.69371294336137801, 6.000000000000000888 ) ) ;
#39465=CARTESIAN_POINT ( 'NONE',  ( 8.102448949553181734, 143.1049999999999613, -5.886773742842746238 ) ) ;
#39468=CARTESIAN_POINT ( 'NONE',  ( 8.102448949553183510, 155.1049999999999898, -5.886773742842746238 ) ) ;
#39470=DIRECTION ( 'NONE',  ( -1.000000000000000000, 0.000000000000000000, 0.000000000000000000 ) ) ;
#39471=( NAMED_UNIT ( * ) SI_UNIT ( $, .STERADIAN. ) SOLID_ANGLE_UNIT ( ) );
#39474=SURFACE_STYLE_USAGE ( .BOTH. , #22931 ) ;
#39476=DIRECTION ( 'NONE',  ( 0.000000000000000000, 1.000000000000000000, 0.000000000000000000 ) ) ;
#39478=( NAMED_UNIT ( * ) PLANE_ANGLE_UNIT ( ) SI_UNIT ( $, .RADIAN. ) );
#39485=FACE_OUTER_BOUND ( 'NONE', #46129, .T. ) ;
#39488=DIRECTION ( 'NONE',  ( 0.000000000000000000, 1.000000000000000000, 0.000000000000000000 ) ) ;
#39489=CARTESIAN_POINT ( 'NONE',  ( -45.91547277936962246, 9.430195807687212550, -3.611004237778682402 ) ) ;
#39491=ORIENTED_EDGE ( 'NONE', *, *, #13182, .F. ) ;
#39493=CARTESIAN_POINT ( 'NONE',  ( 74.50000000000000000, 19.30628705663858113, -6.999999999999999112 ) ) ;
#39494=DIRECTION ( 'NONE',  ( 1.000000000000000000, -0.000000000000000000, 0.000000000000000000 ) ) ;
#39496=ORIENTED_EDGE ( 'NONE', *, *, #11238, .F. ) ;
#39497=CARTESIAN_POINT ( 'NONE',  ( -65.49999999999998579, 50.00000000000000000, 10.00000000000000000 ) ) ;
#39501=EDGE_CURVE ( 'NONE', #27268, #10308, #62438, .T. ) ;
#39502=EDGE_CURVE ( 'NONE', #12316, #29106, #59072, .T. ) ;
#39503=CARTESIAN_POINT ( 'NONE',  ( -3.094860106618434248, 134.7949999999999875, 9.525000000000000355 ) ) ;
#39505=AXIS2_PLACEMENT_3D ( 'NONE', #58300, #57254, #30158 ) ;
#39508=LINE ( 'NONE', #8524, #63826 ) ;
#39512=EDGE_CURVE ( 'NONE', #30840, #46101, #52324, .T. ) ;
#39515=ORIENTED_EDGE ( 'NONE', *, *, #62891, .T. ) ;
#39520=MECHANICAL_DESIGN_GEOMETRIC_PRESENTATION_REPRESENTATION('',(#28159),#63037);
#39522=DIRECTION ( 'NONE',  ( 1.000000000000000000, 0.000000000000000000, 0.000000000000000000 ) ) ;
#39524=( LENGTH_UNIT ( ) NAMED_UNIT ( * ) SI_UNIT ( .MILLI., .METRE. ) );
#39526=( GEOMETRIC_REPRESENTATION_CONTEXT ( 3 ) GLOBAL_UNCERTAINTY_ASSIGNED_CONTEXT ( ( #17992 ) ) GLOBAL_UNIT_ASSIGNED_CONTEXT ( ( #45566, #49170, #11858 ) ) REPRESENTATION_CONTEXT ( 'NONE', 'WORKASPACE' ) );
#39527=ORIENTED_EDGE ( 'NONE', *, *, #8296, .T. ) ;
#39531=STYLED_ITEM ( 'NONE', ( #2302 ), #22165 ) ;
#39536=CARTESIAN_POINT ( 'NONE',  ( -2.607480562269075097, 155.4070736234661467, 8.025000000000000355 ) ) ;
#39537=COLOUR_RGB ( '', 0.31764706, 0.68627451, 0.89019608) ;
#39539=DIRECTION ( 'NONE',  ( 0.2413793103448194644, -0.9704308468600220117, 0.000000000000000000 ) ) ;
#39540=CARTESIAN_POINT ( 'NONE',  ( 75.00000000000000000, -2.215169945516535778E-14, -6.999999999999999112 ) ) ;
#39543=CARTESIAN_POINT ( 'NONE',  ( -3.094860106618432471, 131.7049999999999557, -9.525000000000000355 ) ) ;
#39549=SURFACE_STYLE_USAGE ( .BOTH. , #1822 ) ;
#39553=DIRECTION ( 'NONE',  ( 0.000000000000000000, 0.000000000000000000, 1.000000000000000000 ) ) ;
#39556=( BOUNDED_SURFACE ( )  B_SPLINE_SURFACE ( 3, 2, ( 
 ( #14178, #30312, #26767 ),
 ( #31722, #42678, #30406 ),
 ( #54565, #37051, #21166 ),
 ( #65108, #44067, #32767 ),
 ( #21517, #43035, #11658 ),
 ( #16962, #6373, #58815 ),
 ( #59485, #10630, #4991 ),
 ( #15932, #59849, #27115 ) ),
 .UNSPECIFIED., .F., .F., .F. ) 
 B_SPLINE_SURFACE_WITH_KNOTS ( ( 4, 2, 2, 4 ),
 ( 3, 3 ),
 ( 0.0005765750791842532991, 0.001029553238931489936, 0.001482531398678726357, 0.002388487718173199631 ),
 ( 0.000000000000000000, 1.000000000000000000 ),
 .UNSPECIFIED. ) 
 GEOMETRIC_REPRESENTATION_ITEM ( )  RATIONAL_B_SPLINE_SURFACE ( (
 ( 1.000000000000000000, 0.8885233166386380388, 1.000000000000000000),
 ( 1.000000000000000000, 0.8885760224879380997, 1.000000000000000000),
 ( 1.000000000000000000, 0.8838232350071987264, 1.000000000000000000),
 ( 1.000000000000000000, 0.8662144792540084071, 1.000000000000000000),
 ( 1.000000000000000000, 0.8532605865698873471, 1.000000000000000000),
 ( 1.000000000000000000, 0.8046051514203296229, 1.000000000000000000),
 ( 1.000000000000000000, 0.7601637718248414055, 1.000000000000000000),
 ( 1.000000000000000000, 0.7071067811865441310, 1.000000000000000000) ) ) 
 REPRESENTATION_ITEM ( '' )  SURFACE ( )  );
#39558=EDGE_CURVE ( 'NONE', #17220, #36075, #39983, .T. ) ;
#39562=CARTESIAN_POINT ( 'NONE',  ( -44.99999999999998579, 119.9999999999999716, -7.000000000000000000 ) ) ;
#39566=SURFACE_SIDE_STYLE ('',( #28944 ) ) ;
#39567=ORIENTED_EDGE ( 'NONE', *, *, #65434, .T. ) ;
#39569=CARTESIAN_POINT ( 'NONE',  ( -74.17570909904742393, 9.081512406228229750, 6.320717432316669715 ) ) ;
#39572=CARTESIAN_POINT ( 'NONE',  ( -2.607480562269116842, 119.4070736234661609, 8.024999999999970157 ) ) ;
#39576=DIRECTION ( 'NONE',  ( -1.000000000000000000, 0.000000000000000000, 0.000000000000000000 ) ) ;
#39577=CARTESIAN_POINT ( 'NONE',  ( -3.094860106618432471, 145.5949999999999704, -9.525000000000000355 ) ) ;
#39580=AXIS2_PLACEMENT_3D ( 'NONE', #63092, #10930, #46969 ) ;
#39581=FACE_OUTER_BOUND ( 'NONE', #32063, .T. ) ;
#39582=ORIENTED_EDGE ( 'NONE', *, *, #47146, .T. ) ;
#39587=EDGE_CURVE ( 'NONE', #12513, #64724, #9648, .T. ) ;
#39590=EDGE_CURVE ( 'NONE', #22472, #61072, #24270, .T. ) ;
#39591=AXIS2_PLACEMENT_3D ( 'NONE', #5142, #3729, #36857 ) ;
#39594=CIRCLE ( 'NONE', #45220, 0.5000000000000004441 ) ;
#39599=( NAMED_UNIT ( * ) SI_UNIT ( $, .STERADIAN. ) SOLID_ANGLE_UNIT ( ) );
#39603=FILL_AREA_STYLE_COLOUR ( '', #58513 ) ;
#39606=STYLED_ITEM ( 'NONE', ( #38812 ), #28807 ) ;
#39607=CARTESIAN_POINT ( 'NONE',  ( 44.99999999999977973, 146.9999999999999716, 7.500000000000000000 ) ) ;
#39609=DIRECTION ( 'NONE',  ( 0.000000000000000000, 0.000000000000000000, 1.000000000000000000 ) ) ;
#39611=DIRECTION ( 'NONE',  ( -1.000000000000000000, 0.000000000000000000, 0.000000000000000000 ) ) ;
#39614=CARTESIAN_POINT ( 'NONE',  ( 44.50000000000000000, 99.99999999999992895, 3.500000000000000000 ) ) ;
#39615=( GEOMETRIC_REPRESENTATION_CONTEXT ( 3 ) GLOBAL_UNCERTAINTY_ASSIGNED_CONTEXT ( ( #37838 ) ) GLOBAL_UNIT_ASSIGNED_CONTEXT ( ( #65126, #12019, #13394 ) ) REPRESENTATION_CONTEXT ( 'NONE', 'WORKASPACE' ) );
#39618=PRESENTATION_STYLE_ASSIGNMENT (( #11199 ) ) ;
#39620=( GEOMETRIC_REPRESENTATION_CONTEXT ( 3 ) GLOBAL_UNCERTAINTY_ASSIGNED_CONTEXT ( ( #39005 ) ) GLOBAL_UNIT_ASSIGNED_CONTEXT ( ( #29073, #55125, #28380 ) ) REPRESENTATION_CONTEXT ( 'NONE', 'WORKASPACE' ) );
#39622=CARTESIAN_POINT ( 'NONE',  ( -9.827790563157511022E-16, 125.5570736234661524, 8.025000000000000355 ) ) ;
#39624=DIRECTION ( 'NONE',  ( 0.000000000000000000, 0.000000000000000000, 1.000000000000000000 ) ) ;
#39625=ORIENTED_EDGE ( 'NONE', *, *, #1122, .T. ) ;
#39632=CARTESIAN_POINT ( 'NONE',  ( -19.89974874213239886, 114.9999999999999574, -10.49999999999999645 ) ) ;
#39636=( NAMED_UNIT ( * ) PLANE_ANGLE_UNIT ( ) SI_UNIT ( $, .RADIAN. ) );
#39638=COLOUR_RGB ( '', 0.40784314, 0.44705882, 0.49803922) ;
#39639=DIRECTION ( 'NONE',  ( -0.7713892158398705234, 0.000000000000000000, -0.6363636363636357984 ) ) ;
#39643=ORIENTED_EDGE ( 'NONE', *, *, #12286, .F. ) ;
#39648=DIRECTION ( 'NONE',  ( 1.000000000000000000, 0.000000000000000000, 0.000000000000000000 ) ) ;
#39652=LINE ( 'NONE', #17831, #2067 ) ;
#39654=STYLED_ITEM ( 'NONE', ( #30960 ), #24930 ) ;
#39655=CARTESIAN_POINT ( 'NONE',  ( -65.49999999999997158, -2.024042244987997205E-14, -12.00000000000000000 ) ) ;
#39657=ORIENTED_EDGE ( 'NONE', *, *, #50296, .T. ) ;
#39661=LINE ( 'NONE', #66356, #42643 ) ;
#39667=CARTESIAN_POINT ( 'NONE',  ( -84.49999999999997158, 50.00000000000000000, 10.50000000000000000 ) ) ;
#39669=CARTESIAN_POINT ( 'NONE',  ( 44.45130529142682008, 9.817101763808558701, 3.473322258837134413 ) ) ;
#39670=PRESENTATION_STYLE_ASSIGNMENT (( #12903 ) ) ;
#39675=ADVANCED_FACE ( 'NONE', ( #15829 ), #16437, .T. ) ;
#39677=CARTESIAN_POINT ( 'NONE',  ( 3.094860106618431583, 142.2050000000000125, 9.525000000000000355 ) ) ;
#39678=DIRECTION ( 'NONE',  ( 1.000000000000000000, 0.000000000000000000, 0.000000000000000000 ) ) ;
#39680=CARTESIAN_POINT ( 'NONE',  ( 4.564701690884894525, 154.3402519334510998, 8.185492600732468205 ) ) ;
#39681=UNCERTAINTY_MEASURE_WITH_UNIT (LENGTH_MEASURE( 1.000000000000000082E-05 ), #28709, 'distance_accuracy_value', 'NONE');
#39690=DIRECTION ( 'NONE',  ( 0.000000000000000000, -2.430666987508117145E-16, 1.000000000000000000 ) ) ;
#39692=ORIENTED_EDGE ( 'NONE', *, *, #52660, .T. ) ;
#39693=EDGE_CURVE ( 'NONE', #19860, #21246, #21416, .T. ) ;
#39696=FILL_AREA_STYLE ('',( #50234 ) ) ;
#39697=LINE ( 'NONE', #39358, #56574 ) ;
#39698=FACE_OUTER_BOUND ( 'NONE', #36299, .T. ) ;
#39705=CARTESIAN_POINT ( 'NONE',  ( 8.102448949553183510, 113.1049999999999898, -5.886773742842746238 ) ) ;
#39708=STYLED_ITEM ( 'NONE', ( #9723 ), #48029 ) ;
#39709=MECHANICAL_DESIGN_GEOMETRIC_PRESENTATION_REPRESENTATION('',(#11557),#50889);
#39711=CARTESIAN_POINT ( 'NONE',  ( -34.99999999999999289, 99.99999999999998579, 3.500000000000000000 ) ) ;
#39719=EDGE_LOOP ( 'NONE', ( #61572, #65719, #11693, #17751, #35711, #4615, #34559, #18359 ) ) ;
#39720=CARTESIAN_POINT ( 'NONE',  ( 2.607480562269071989, 142.5929263765337680, 8.025000000000002132 ) ) ;
#39725=CIRCLE ( 'NONE', #30693, 10.49999999999999822 ) ;
#39730=( LENGTH_UNIT ( ) NAMED_UNIT ( * ) SI_UNIT ( .MILLI., .METRE. ) );
#39736=SURFACE_STYLE_USAGE ( .BOTH. , #33390 ) ;
#39744=ORIENTED_EDGE ( 'NONE', *, *, #41484, .T. ) ;
#39745=SURFACE_STYLE_FILL_AREA ( #24216 ) ;
#39747=CARTESIAN_POINT ( 'NONE',  ( 41.49999999999998579, 106.9282032302754999, 3.500000000000000000 ) ) ;
#39749=CIRCLE ( 'NONE', #36408, 0.5000000000000004441 ) ;
#39751=ORIENTED_EDGE ( 'NONE', *, *, #6200, .F. ) ;
#39754=FILL_AREA_STYLE_COLOUR ( '', #33787 ) ;
#39764=LINE ( 'NONE', #8761, #50 ) ;
#39768=CARTESIAN_POINT ( 'NONE',  ( 45.50000000000000000, -1.469576158976824618E-14, 6.999999999999999112 ) ) ;
#39772=CARTESIAN_POINT ( 'NONE',  ( 0.000000000000000000, 122.5549999999999784, -9.525000000000000355 ) ) ;
#39775=( GEOMETRIC_REPRESENTATION_CONTEXT ( 3 ) GLOBAL_UNCERTAINTY_ASSIGNED_CONTEXT ( ( #48088 ) ) GLOBAL_UNIT_ASSIGNED_CONTEXT ( ( #1634, #23154, #27353 ) ) REPRESENTATION_CONTEXT ( 'NONE', 'WORKASPACE' ) );
#39778=UNCERTAINTY_MEASURE_WITH_UNIT (LENGTH_MEASURE( 1.000000000000000082E-05 ), #12068, 'distance_accuracy_value', 'NONE');
#39788=( NAMED_UNIT ( * ) PLANE_ANGLE_UNIT ( ) SI_UNIT ( $, .RADIAN. ) );
#39790=EDGE_LOOP ( 'NONE', ( #15065, #45620, #31211, #9059 ) ) ;
#39791=STYLED_ITEM ( 'NONE', ( #23779 ), #36818 ) ;
#39792=PRESENTATION_STYLE_ASSIGNMENT (( #23566 ) ) ;
#39793=TOROIDAL_SURFACE ( 'NONE', #38696, 1.000000000000000000, 0.5000000000000000000 ) ;
#39794=CARTESIAN_POINT ( 'NONE',  ( 0.000000000000000000, 87.30187232391182306, 0.000000000000000000 ) ) ;
#39802=ORIENTED_EDGE ( 'NONE', *, *, #36813, .F. ) ;
#39808=CARTESIAN_POINT ( 'NONE',  ( -1.166476076187854022E-15, 137.9449999999999932, 9.525000000000000355 ) ) ;
#39810=( GEOMETRIC_REPRESENTATION_CONTEXT ( 3 ) GLOBAL_UNCERTAINTY_ASSIGNED_CONTEXT ( ( #46927 ) ) GLOBAL_UNIT_ASSIGNED_CONTEXT ( ( #53646, #59250, #4393 ) ) REPRESENTATION_CONTEXT ( 'NONE', 'WORKASPACE' ) );
#39811=ORIENTED_EDGE ( 'NONE', *, *, #53170, .F. ) ;
#39814=CARTESIAN_POINT ( 'NONE',  ( 9.058813317711337021, 136.6550000000000011, 2.943386871421375783 ) ) ;
#39818=CARTESIAN_POINT ( 'NONE',  ( 3.094860106618435136, 155.4050000000000011, -9.525000000000000355 ) ) ;
#39820=UNCERTAINTY_MEASURE_WITH_UNIT (LENGTH_MEASURE( 1.000000000000000082E-05 ), #34408, 'distance_accuracy_value', 'NONE');
#39823=SURFACE_STYLE_FILL_AREA ( #55618 ) ;
#39824=CARTESIAN_POINT ( 'NONE',  ( -15.48999599679679662, 118.4999999999999716, 10.00000000000000000 ) ) ;
#39825=VERTEX_POINT ( 'NONE', #11906 ) ;
#39826=EDGE_CURVE ( 'NONE', #23699, #47153, #55714, .T. ) ;
#39830=STYLED_ITEM ( 'NONE', ( #62843 ), #61849 ) ;
#39831=SURFACE_STYLE_FILL_AREA ( #50351 ) ;
#39838=( LENGTH_UNIT ( ) NAMED_UNIT ( * ) SI_UNIT ( .MILLI., .METRE. ) );
#39840=FILL_AREA_STYLE ('',( #27211 ) ) ;
#39841=( NAMED_UNIT ( * ) SI_UNIT ( $, .STERADIAN. ) SOLID_ANGLE_UNIT ( ) );
#39843=EDGE_CURVE ( 'NONE', #29123, #4364, #55144, .T. ) ;
#39848=TOROIDAL_SURFACE ( 'NONE', #64507, 8.499999999999998224, 0.5000000000000000000 ) ;
#39852=CIRCLE ( 'NONE', #55570, 14.49999999999999822 ) ;
#39853=DIRECTION ( 'NONE',  ( 0.000000000000000000, 0.000000000000000000, 1.000000000000000000 ) ) ;
#39854=AXIS2_PLACEMENT_3D ( 'NONE', #57864, #30750, #51890 ) ;
#39856=FACE_OUTER_BOUND ( 'NONE', #27733, .T. ) ;
#39857=AXIS2_PLACEMENT_3D ( 'NONE', #33757, #33084, #16587 ) ;
#39858=ORIENTED_EDGE ( 'NONE', *, *, #39693, .F. ) ;
#39859=CARTESIAN_POINT ( 'NONE',  ( 12.34222745343792127, 115.4999999999999574, -10.18181818181818166 ) ) ;
#39863=CARTESIAN_POINT ( 'NONE',  ( 9.058813317711337021, 141.5449999999999875, 2.943386871421375783 ) ) ;
#39865=DIRECTION ( 'NONE',  ( 0.000000000000000000, 0.000000000000000000, 1.000000000000000000 ) ) ;
#39868=( NAMED_UNIT ( * ) PLANE_ANGLE_UNIT ( ) SI_UNIT ( $, .RADIAN. ) );
#39869=AXIS2_PLACEMENT_3D ( 'NONE', #3043, #40773, #67468 ) ;
#39873=AXIS2_PLACEMENT_3D ( 'NONE', #54595, #33488, #1423 ) ;
#39874=DIRECTION ( 'NONE',  ( 0.000000000000000000, 0.000000000000000000, 1.000000000000000000 ) ) ;
#39877=ORIENTED_EDGE ( 'NONE', *, *, #46750, .T. ) ;
#39882=PRESENTATION_STYLE_ASSIGNMENT (( #8186 ) ) ;
#39883=SURFACE_SIDE_STYLE ('',( #66578 ) ) ;
#39889=SPHERICAL_SURFACE ( 'NONE', #24165, 0.5000000000000000000 ) ;
#39890=CARTESIAN_POINT ( 'NONE',  ( -47.50000000000000000, 14.49137674618942562, 10.00000000000000000 ) ) ;
#39891=CARTESIAN_POINT ( 'NONE',  ( 5.598654528085805993, 114.2449999999999903, 7.705886871421374629 ) ) ;
#39892=CIRCLE ( 'NONE', #27485, 5.499999999999976907 ) ;
#39893=VERTEX_POINT ( 'NONE', #50932 ) ;
#39895=CARTESIAN_POINT ( 'NONE',  ( 5.598654528085809545, 113.2549999999999812, -7.705886871421373741 ) ) ;
#39898=CARTESIAN_POINT ( 'NONE',  ( 3.094860106618431583, 124.2049999999999841, 9.525000000000000355 ) ) ;
#39899=UNCERTAINTY_MEASURE_WITH_UNIT (LENGTH_MEASURE( 1.000000000000000082E-05 ), #279, 'distance_accuracy_value', 'NONE');
#39900=CARTESIAN_POINT ( 'NONE',  ( 6.826472737025121695, 132.6070736234661638, -4.959722759717905660 ) ) ;
#39901=SURFACE_SIDE_STYLE ('',( #28592 ) ) ;
#39902=CARTESIAN_POINT ( 'NONE',  ( 20.77895614775982125, 115.1380991538496801, 10.00000000000000000 ) ) ;
#39904=SURFACE_STYLE_FILL_AREA ( #51733 ) ;
#39905=DIRECTION ( 'NONE',  ( 1.000000000000000000, 0.000000000000000000, -0.000000000000000000 ) ) ;
#39907=PRESENTATION_STYLE_ASSIGNMENT (( #56382 ) ) ;
#39909=VERTEX_POINT ( 'NONE', #9066 ) ;
#39910=DIRECTION ( 'NONE',  ( 0.9704308468600219006, 0.2413793103448194921, -0.000000000000000000 ) ) ;
#39917=DIRECTION ( 'NONE',  ( 0.000000000000000000, 0.000000000000000000, 1.000000000000000000 ) ) ;
#39919=( LENGTH_UNIT ( ) NAMED_UNIT ( * ) SI_UNIT ( .MILLI., .METRE. ) );
#39921=AXIS2_PLACEMENT_3D ( 'NONE', #11257, #49601, #65423 ) ;
#39922=CARTESIAN_POINT ( 'NONE',  ( -75.00000000000001421, 8.382277537376792154, 5.549490760430561664 ) ) ;
#39926=EDGE_CURVE ( 'NONE', #10308, #27268, #7466, .T. ) ;
#39929=SURFACE_STYLE_FILL_AREA ( #7868 ) ;
#39930=CARTESIAN_POINT ( 'NONE',  ( 10.01517768586949408, 138.6949999999999932, 1.839758294383810543E-15 ) ) ;
#39933=CYLINDRICAL_SURFACE ( 'NONE', #37093, 0.5000000000000004441 ) ;
#39936=CARTESIAN_POINT ( 'NONE',  ( 2.607480562269030688, 119.7070736234661581, 8.025000000000034106 ) ) ;
#39937=SURFACE_STYLE_USAGE ( .BOTH. , #60636 ) ;
#39940=CARTESIAN_POINT ( 'NONE',  ( 9.058813317711337021, 114.5449999999999733, 2.943386871421375783 ) ) ;
#39944=LINE ( 'NONE', #27328, #21208 ) ;
#39948=LINE ( 'NONE', #24746, #55953 ) ;
#39949=FILL_AREA_STYLE ('',( #51171 ) ) ;
#39952=( BOUNDED_CURVE ( )  B_SPLINE_CURVE ( 2, ( #56972, #30213, #51706, #24954, #26332, #37651, #58352, #47157, #59048, #9840, #4528 ),
 .UNSPECIFIED., .F., .F. ) 
 B_SPLINE_CURVE_WITH_KNOTS ( ( 3, 2, 2, 2, 2, 3 ),
 ( 0.7058823529411767383, 0.7117647058823531880, 0.7176470588235296377, 0.7235294117647060874, 0.7294117647058825371, 0.7352941176470590978 ),
 .UNSPECIFIED. ) 
 CURVE ( )  GEOMETRIC_REPRESENTATION_ITEM ( )  RATIONAL_B_SPLINE_CURVE ( ( 0.9999999999999981126, 0.9510565162951554186, 1.000000000000000000, 0.9510565162951535312, 1.000000000000000000, 0.9510565162951535312, 1.000000000000000000, 0.9510565162951535312, 1.000000000000000000, 0.9510565162951516438, 1.000000000000001776 ) ) 
 REPRESENTATION_ITEM ( '' )  );
#39955=CARTESIAN_POINT ( 'NONE',  ( -21.02379604162863558, 109.9999999999999858, -9.500000000000000000 ) ) ;
#39959=MECHANICAL_DESIGN_GEOMETRIC_PRESENTATION_REPRESENTATION('',(#43354),#7337);
#39960=DIRECTION ( 'NONE',  ( 0.000000000000000000, 0.000000000000000000, 1.000000000000000000 ) ) ;
#39962=AXIS2_PLACEMENT_3D ( 'NONE', #59687, #26627, #31924 ) ;
#39963=CARTESIAN_POINT ( 'NONE',  ( -9.827790563157511022E-16, 151.4429263765338192, 8.025000000000000355 ) ) ;
#39964=SURFACE_SIDE_STYLE ('',( #50485 ) ) ;
#39966=STYLED_ITEM ( 'NONE', ( #51424 ), #64125 ) ;
#39967=ORIENTED_EDGE ( 'NONE', *, *, #17022, .F. ) ;
#39969=LINE ( 'NONE', #61372, #60957 ) ;
#39972=CARTESIAN_POINT ( 'NONE',  ( -6.826472737025120807, 133.5070736234661410, -4.959722759717907437 ) ) ;
#39973=AXIS2_PLACEMENT_3D ( 'NONE', #43910, #59008, #44264 ) ;
#39974=CARTESIAN_POINT ( 'NONE',  ( -8.437984349512095861, 124.8070736234661382, -5.166775262442723748E-16 ) ) ;
#39978=LINE ( 'NONE', #51529, #41854 ) ;
#39982=EDGE_CURVE ( 'NONE', #16496, #35564, #5182, .T. ) ;
#39983=CIRCLE ( 'NONE', #57937, 0.5000000000000004441 ) ;
#39984=DIRECTION ( 'NONE',  ( -0.000000000000000000, -0.000000000000000000, -1.000000000000000000 ) ) ;
#39985=EDGE_CURVE ( 'NONE', #9513, #9272, #3020, .T. ) ;
#39989=ORIENTED_EDGE ( 'NONE', *, *, #16163, .T. ) ;
#39993=EDGE_CURVE ( 'NONE', #6265, #8139, #35087, .T. ) ;
#39998=EDGE_CURVE ( 'NONE', #17419, #26003, #30135, .T. ) ;
#40001=DIRECTION ( 'NONE',  ( 0.000000000000000000, 0.000000000000000000, -1.000000000000000000 ) ) ;
#40002=EDGE_LOOP ( 'NONE', ( #3911, #49080, #65647, #41184 ) ) ;
#40005=SURFACE_STYLE_FILL_AREA ( #56482 ) ;
#40006=PRESENTATION_STYLE_ASSIGNMENT (( #23106 ) ) ;
#40007=FILL_AREA_STYLE_COLOUR ( '', #22100 ) ;
#40010=CARTESIAN_POINT ( 'NONE',  ( 8.102448949553181734, 111.9949999999999761, -5.886773742842746238 ) ) ;
#40012=STYLED_ITEM ( 'NONE', ( #4391 ), #8571 ) ;
#40016=EDGE_LOOP ( 'NONE', ( #10326, #69138, #20424, #23258 ) ) ;
#40018=CARTESIAN_POINT ( 'NONE',  ( 45.07697505292422591, 10.02565835097472480, -3.091949714863345910 ) ) ;
#40019=COLOUR_RGB ( '', 0.09019608, 0.27058824, 0.51372549) ;
#40028=AXIS2_PLACEMENT_3D ( 'NONE', #43290, #10872, #59373 ) ;
#40036=CARTESIAN_POINT ( 'NONE',  ( -10.01517768586949231, 147.3049999999999500, -6.132527647946036459E-16 ) ) ;
#40040=MECHANICAL_DESIGN_GEOMETRIC_PRESENTATION_REPRESENTATION('',(#4029),#58001);
#40042=CARTESIAN_POINT ( 'NONE',  ( -19.98523465219084017, 114.9999999999999574, -10.47102667436386625 ) ) ;
#40043=CARTESIAN_POINT ( 'NONE',  ( 60.00000000000000000, 1.797044900979284448E-15, 10.00000000000000000 ) ) ;
#40045=B_SPLINE_CURVE_WITH_KNOTS ( 'NONE', 3,
 ( #40018, #61409, #13226, #34683 ),
 .UNSPECIFIED., .F., .F.,
 ( 4, 4 ),
 ( -4.672407068503224980E-06, 0.0001893522667583410015 ),
 .UNSPECIFIED. ) ;
#40049=VERTEX_POINT ( 'NONE', #34400 ) ;
#40052=EDGE_CURVE ( 'NONE', #23279, #35924, #22024, .T. ) ;
#40057=ORIENTED_EDGE ( 'NONE', *, *, #41772, .F. ) ;
#40059=PRESENTATION_STYLE_ASSIGNMENT (( #57230 ) ) ;
#40061=ORIENTED_EDGE ( 'NONE', *, *, #4708, .F. ) ;
#40062=DIRECTION ( 'NONE',  ( 1.000000000000000000, 0.000000000000000000, 0.000000000000000000 ) ) ;
#40070=ORIENTED_EDGE ( 'NONE', *, *, #58912, .F. ) ;
#40077=ORIENTED_EDGE ( 'NONE', *, *, #55047, .F. ) ;
#40078=CARTESIAN_POINT ( 'NONE',  ( -2.607480562269075097, 142.2929263765338135, 8.025000000000000355 ) ) ;
#40081=VECTOR ( 'NONE', #46302, 1000.000000000000000 ) ;
#40083=ORIENTED_EDGE ( 'NONE', *, *, #11882, .T. ) ;
#40084=DIRECTION ( 'NONE',  ( 0.000000000000000000, 0.000000000000000000, 1.000000000000000000 ) ) ;
#40086=PRESENTATION_STYLE_ASSIGNMENT (( #39736 ) ) ;
#40087=DIRECTION ( 'NONE',  ( -0.7071067811865549002, 0.000000000000000000, -0.7071067811865402453 ) ) ;
#40089=( LENGTH_UNIT ( ) NAMED_UNIT ( * ) SI_UNIT ( .MILLI., .METRE. ) );
#40090=DIRECTION ( 'NONE',  ( 0.6842105263157866046, -0.7292845505553195995, 0.000000000000000000 ) ) ;
#40091=DIRECTION ( 'NONE',  ( 1.000000000000000000, 0.000000000000000000, 0.000000000000000000 ) ) ;
#40094=CARTESIAN_POINT ( 'NONE',  ( -24.21231517720798010, 112.9999999999999858, -10.00000000000000000 ) ) ;
#40105=EDGE_CURVE ( 'NONE', #40506, #3770, #25560, .T. ) ;
#40106=DIRECTION ( 'NONE',  ( -0.000000000000000000, -0.000000000000000000, 1.000000000000000000 ) ) ;
#40114=FILL_AREA_STYLE ('',( #18635 ) ) ;
#40117=CARTESIAN_POINT ( 'NONE',  ( 5.598654528085809545, 116.2549999999999812, -7.705886871421373741 ) ) ;
#40120=( GEOMETRIC_REPRESENTATION_CONTEXT ( 3 ) GLOBAL_UNCERTAINTY_ASSIGNED_CONTEXT ( ( #64398 ) ) GLOBAL_UNIT_ASSIGNED_CONTEXT ( ( #15169, #67920, #51735 ) ) REPRESENTATION_CONTEXT ( 'NONE', 'WORKASPACE' ) );
#40122=CYLINDRICAL_SURFACE ( 'NONE', #49479, 0.5000000000000004441 ) ;
#40123=CARTESIAN_POINT ( 'NONE',  ( 71.62068965517239860, 36.41396814395972115, 7.500000000000000000 ) ) ;
#40128=AXIS2_PLACEMENT_3D ( 'NONE', #54891, #28510, #60198 ) ;
#40130=ADVANCED_FACE ( 'NONE', ( #19945 ), #41239, .F. ) ;
#40134=CARTESIAN_POINT ( 'NONE',  ( -24.21231517720798010, 113.4999999999999858, -7.500000000000000000 ) ) ;
#40136=DIRECTION ( 'NONE',  ( -0.000000000000000000, 1.000000000000000000, -0.000000000000000000 ) ) ;
#40139=( NAMED_UNIT ( * ) PLANE_ANGLE_UNIT ( ) SI_UNIT ( $, .RADIAN. ) );
#40143=ADVANCED_FACE ( 'NONE', ( #64243 ), #10793, .F. ) ;
#40147=SURFACE_STYLE_FILL_AREA ( #14688 ) ;
#40148=( NAMED_UNIT ( * ) PLANE_ANGLE_UNIT ( ) SI_UNIT ( $, .RADIAN. ) );
#40149=CARTESIAN_POINT ( 'NONE',  ( 9.058813317711337021, 135.5449999999999875, 2.943386871421375783 ) ) ;
#40152=CYLINDRICAL_SURFACE ( 'NONE', #43190, 0.5000000000000004441 ) ;
#40153=CARTESIAN_POINT ( 'NONE',  ( 5.598654528085809545, 143.2549999999999955, -7.705886871421373741 ) ) ;
#40156=VERTEX_POINT ( 'NONE', #15738 ) ;
#40157=CARTESIAN_POINT ( 'NONE',  ( 0.000000000000000000, 116.9429263765338192, -8.025000000000000355 ) ) ;
#40158=FACE_OUTER_BOUND ( 'NONE', #68433, .T. ) ;
#40159=PRESENTATION_STYLE_ASSIGNMENT (( #28861 ) ) ;
#40161=PRESENTATION_STYLE_ASSIGNMENT (( #23946 ) ) ;
#40163=VERTEX_POINT ( 'NONE', #23085 ) ;
#40165=EDGE_LOOP ( 'NONE', ( #64800, #5000, #24636, #33063, #6273, #50270, #59830, #62594, #7742, #21150, #14818, #19287, #22816, #52869, #33529, #18009, #38002, #21417, #39527 ) ) ;
#40166=DIRECTION ( 'NONE',  ( -0.000000000000000000, 1.000000000000000000, -0.000000000000000000 ) ) ;
#40167=DIRECTION ( 'NONE',  ( 1.000000000000000000, 0.000000000000000000, 0.000000000000000000 ) ) ;
#40170=CARTESIAN_POINT ( 'NONE',  ( 45.50000000000000000, -1.469576158976824618E-14, -9.500000000000000000 ) ) ;
#40173=ORIENTED_EDGE ( 'NONE', *, *, #20275, .T. ) ;
#40176=CARTESIAN_POINT ( 'NONE',  ( 60.00000000000000000, 1.797044900979284448E-15, -6.500000000000000000 ) ) ;
#40179=FILL_AREA_STYLE ('',( #2460 ) ) ;
#40181=( NAMED_UNIT ( * ) SI_UNIT ( $, .STERADIAN. ) SOLID_ANGLE_UNIT ( ) );
#40182=CARTESIAN_POINT ( 'NONE',  ( -75.00000000000000000, 8.456227461324047567, -6.943431694471518867 ) ) ;
#40183=ORIENTED_EDGE ( 'NONE', *, *, #23603, .F. ) ;
#40184=DIRECTION ( 'NONE',  ( 1.156482317317873451E-16, -1.000000000000000000, 0.000000000000000000 ) ) ;
#40186=CARTESIAN_POINT ( 'NONE',  ( 8.102448949553181734, 138.3950000000000102, 5.886773742842750679 ) ) ;
#40194=CIRCLE ( 'NONE', #9864, 0.5000000000000004441 ) ;
#40197=SURFACE_STYLE_USAGE ( .BOTH. , #8531 ) ;
#40198=EDGE_CURVE ( 'NONE', #65770, #9058, #65900, .T. ) ;
#40200=ORIENTED_EDGE ( 'NONE', *, *, #1377, .F. ) ;
#40203=FILL_AREA_STYLE_COLOUR ( '', #3753 ) ;
#40205=SURFACE_STYLE_FILL_AREA ( #29971 ) ;
#40211=AXIS2_PLACEMENT_3D ( 'NONE', #41377, #53629, #63827 ) ;
#40216=CARTESIAN_POINT ( 'NONE',  ( 0.000000000000000000, 114.4999999999999574, 0.000000000000000000 ) ) ;
#40222=CARTESIAN_POINT ( 'NONE',  ( 0.000000000000000000, 109.4449999999999932, -9.525000000000000355 ) ) ;
#40224=CARTESIAN_POINT ( 'NONE',  ( -3.094860106618434248, 114.9049999999999727, 9.525000000000000355 ) ) ;
#40225=ADVANCED_FACE ( 'NONE', ( #28316 ), #26926, .T. ) ;
#40228=CARTESIAN_POINT ( 'NONE',  ( 5.598654528085805993, 136.3550000000000182, 7.705886871421374629 ) ) ;
#40229=DIRECTION ( 'NONE',  ( 0.000000000000000000, 0.000000000000000000, -1.000000000000000000 ) ) ;
#40230=( NAMED_UNIT ( * ) SI_UNIT ( $, .STERADIAN. ) SOLID_ANGLE_UNIT ( ) );
#40233=VERTEX_POINT ( 'NONE', #54715 ) ;
#40234=SURFACE_SIDE_STYLE ('',( #18756 ) ) ;
#40239=CARTESIAN_POINT ( 'NONE',  ( -45.00000000000000000, 7.951225523244941584, -6.457238017239539829 ) ) ;
#40244=VERTEX_POINT ( 'NONE', #27276 ) ;
#40245=AXIS2_PLACEMENT_3D ( 'NONE', #29772, #45973, #56139 ) ;
#40250=SURFACE_SIDE_STYLE ('',( #3236 ) ) ;
#40254=CARTESIAN_POINT ( 'NONE',  ( -8.102448949553179958, 143.4949999999999477, 5.886773742842747126 ) ) ;
#40257=DIRECTION ( 'NONE',  ( -0.000000000000000000, -0.000000000000000000, 1.000000000000000000 ) ) ;
#40260=DIRECTION ( 'NONE',  ( 1.000000000000000000, 0.000000000000000000, 0.000000000000000000 ) ) ;
#40263=DIRECTION ( 'NONE',  ( -1.000000000000000000, 0.000000000000000000, 0.000000000000000000 ) ) ;
#40266=DIRECTION ( 'NONE',  ( 0.000000000000000000, 0.000000000000000000, 1.000000000000000000 ) ) ;
#40268=CARTESIAN_POINT ( 'NONE',  ( -15.98999599679679839, 146.9999999999999716, -9.500000000000000000 ) ) ;
#40270=LINE ( 'NONE', #28981, #66454 ) ;
#40278=AXIS2_PLACEMENT_3D ( 'NONE', #17644, #33784, #12314 ) ;
#40279=FILL_AREA_STYLE_COLOUR ( '', #63817 ) ;
#40287=CARTESIAN_POINT ( 'NONE',  ( 71.99999999999998579, 64.07124727947029896, 7.500000000000000000 ) ) ;
#40289=CARTESIAN_POINT ( 'NONE',  ( -45.00000000000000000, 7.768687147774684831, 6.999999999999999112 ) ) ;
#40294=CARTESIAN_POINT ( 'NONE',  ( 60.00000000000000000, 1.797044900979284448E-15, -10.49999999999999822 ) ) ;
#40296=CARTESIAN_POINT ( 'NONE',  ( -8.437984349512095861, 133.8070736234661524, -5.166775262442723748E-16 ) ) ;
#40298=CARTESIAN_POINT ( 'NONE',  ( -2.607480562269075097, 134.4070736234661467, 8.025000000000000355 ) ) ;
#40302=DIRECTION ( 'NONE',  ( 1.000000000000000000, 0.000000000000000000, 0.000000000000000000 ) ) ;
#40304=CARTESIAN_POINT ( 'NONE',  ( 12.34222745343792127, 149.9999999999999716, 10.18181818181818166 ) ) ;
#40307=DIRECTION ( 'NONE',  ( -0.000000000000000000, 0.000000000000000000, -1.000000000000000000 ) ) ;
#40316=UNCERTAINTY_MEASURE_WITH_UNIT (LENGTH_MEASURE( 1.000000000000000082E-05 ), #55326, 'distance_accuracy_value', 'NONE');
#40318=( NAMED_UNIT ( * ) PLANE_ANGLE_UNIT ( ) SI_UNIT ( $, .RADIAN. ) );
#40325=COLOUR_RGB ( '', 0.08235294, 0.09019608, 0.10196078) ;
#40326=SURFACE_STYLE_FILL_AREA ( #67055 ) ;
#40342=CARTESIAN_POINT ( 'NONE',  ( -75.00000000000001421, 7.967268226264176967, 6.999999999999999112 ) ) ;
#40343=CARTESIAN_POINT ( 'NONE',  ( -7.294180917968233757, 111.2000015091183940, -4.983928513604040766 ) ) ;
#40345=COLOUR_RGB ( '', 0.72549020, 0.75294118, 0.79215686) ;
#40348=AXIS2_PLACEMENT_3D ( 'NONE', #64476, #31753, #21917 ) ;
#40349=DIRECTION ( 'NONE',  ( 0.000000000000000000, 0.000000000000000000, 1.000000000000000000 ) ) ;
#40351=DIRECTION ( 'NONE',  ( -0.000000000000000000, -0.000000000000000000, -1.000000000000000000 ) ) ;
#40352=CIRCLE ( 'NONE', #4347, 17.50000000000000000 ) ;
#40354=EDGE_CURVE ( 'NONE', #62518, #69284, #24787, .T. ) ;
#40356=EDGE_CURVE ( 'NONE', #21253, #33323, #69223, .T. ) ;
#40357=CARTESIAN_POINT ( 'NONE',  ( 5.598654528085809545, 149.2549999999999955, -7.705886871421373741 ) ) ;
#40358=SURFACE_SIDE_STYLE ('',( #12910 ) ) ;
#40359=CARTESIAN_POINT ( 'NONE',  ( -34.99999999999999289, 99.99999999999998579, -4.000000000000000000 ) ) ;
#40362=CARTESIAN_POINT ( 'NONE',  ( -20.48276553341834827, 114.7646630323463057, -10.30680354032555712 ) ) ;
#40363=EDGE_CURVE ( 'NONE', #45776, #6348, #38987, .T. ) ;
#40365=CARTESIAN_POINT ( 'NONE',  ( -74.50000000000000000, 64.49137674618943095, 10.00000000000000000 ) ) ;
#40374=ORIENTED_EDGE ( 'NONE', *, *, #4149, .T. ) ;
#40375=AXIS2_PLACEMENT_3D ( 'NONE', #64837, #65178, #53930 ) ;
#40378=CIRCLE ( 'NONE', #964, 1.000000000000000888 ) ;
#40380=( NAMED_UNIT ( * ) SI_UNIT ( $, .STERADIAN. ) SOLID_ANGLE_UNIT ( ) );
#40383=ORIENTED_EDGE ( 'NONE', *, *, #50744, .T. ) ;
#40385=FILL_AREA_STYLE_COLOUR ( '', #38826 ) ;
#40388=DIRECTION ( 'NONE',  ( 0.000000000000000000, 1.000000000000000000, -0.000000000000000000 ) ) ;
#40389=ORIENTED_EDGE ( 'NONE', *, *, #11675, .T. ) ;
#40394=ORIENTED_EDGE ( 'NONE', *, *, #64645, .F. ) ;
#40395=CIRCLE ( 'NONE', #46035, 0.5000000000000004441 ) ;
#40397=SURFACE_STYLE_FILL_AREA ( #19248 ) ;
#40400=ORIENTED_EDGE ( 'NONE', *, *, #39587, .F. ) ;
#40401=CARTESIAN_POINT ( 'NONE',  ( -4.716976649647098618, 148.1429263765338078, 6.492361379858953008 ) ) ;
#40404=CARTESIAN_POINT ( 'NONE',  ( -71.50000000000000000, 35.92875272052971525, -10.00000000000000000 ) ) ;
#40406=ORIENTED_EDGE ( 'NONE', *, *, #40707, .F. ) ;
#40413=( NAMED_UNIT ( * ) SI_UNIT ( $, .STERADIAN. ) SOLID_ANGLE_UNIT ( ) );
#40416=CYLINDRICAL_SURFACE ( 'NONE', #36672, 8.025000000000000355 ) ;
#40420=SURFACE_STYLE_FILL_AREA ( #24212 ) ;
#40422=EDGE_LOOP ( 'NONE', ( #33512, #45946, #20825, #5723 ) ) ;
#40425=CIRCLE ( 'NONE', #28015, 13.00000000000000533 ) ;
#40426=DIRECTION ( 'NONE',  ( -1.000000000000000000, -0.000000000000000000, -0.000000000000000000 ) ) ;
#40427=CARTESIAN_POINT ( 'NONE',  ( 40.99999999999997868, 9.999999999999980460, -3.000000000000000444 ) ) ;
#40431=SURFACE_STYLE_FILL_AREA ( #2006 ) ;
#40433=AXIS2_PLACEMENT_3D ( 'NONE', #62778, #14617, #36082 ) ;
#40437=CARTESIAN_POINT ( 'NONE',  ( -74.54819447403424704, 36.40925622619634794, -10.00000000000000355 ) ) ;
#40440=VECTOR ( 'NONE', #7186, 1000.000000000000000 ) ;
#40448=EDGE_CURVE ( 'NONE', #34565, #15660, #53597, .T. ) ;
#40449=CARTESIAN_POINT ( 'NONE',  ( 10.01517768586949231, 118.8049999999999926, 1.839758294383810543E-15 ) ) ;
#40453=UNCERTAINTY_MEASURE_WITH_UNIT (LENGTH_MEASURE( 1.000000000000000082E-05 ), #22319, 'distance_accuracy_value', 'NONE');
#40454=AXIS2_PLACEMENT_3D ( 'NONE', #56251, #40813, #67875 ) ;
#40458=EDGE_CURVE ( 'NONE', #20280, #49901, #60321, .T. ) ;
#40461=FACE_OUTER_BOUND ( 'NONE', #32294, .T. ) ;
#40473=CARTESIAN_POINT ( 'NONE',  ( -74.99999999999998579, 118.4999999999999716, 7.500000000000000000 ) ) ;
#40474=FILL_AREA_STYLE_COLOUR ( '', #30341 ) ;
#40477=ORIENTED_EDGE ( 'NONE', *, *, #43855, .T. ) ;
#40480=CARTESIAN_POINT ( 'NONE',  ( -15.98999599679679839, 118.4999999999999716, -7.500000000000000000 ) ) ;
#40486=ORIENTED_EDGE ( 'NONE', *, *, #12634, .T. ) ;
#40487=AXIS2_PLACEMENT_3D ( 'NONE', #68225, #47864, #41866 ) ;
#40489=( NAMED_UNIT ( * ) SI_UNIT ( $, .STERADIAN. ) SOLID_ANGLE_UNIT ( ) );
#40490=ADVANCED_FACE ( 'NONE', ( #5670 ), #63693, .F. ) ;
#40492=CARTESIAN_POINT ( 'NONE',  ( 0.000000000000000000, 139.4449999999999932, -9.525000000000000355 ) ) ;
#40495=CARTESIAN_POINT ( 'NONE',  ( -5.598654528085806881, 143.8549999999999898, -7.705886871421374629 ) ) ;
#40496=SURFACE_SIDE_STYLE ('',( #40849 ) ) ;
#40497=STYLED_ITEM ( 'NONE', ( #3532 ), #32962 ) ;
#40499=CARTESIAN_POINT ( 'NONE',  ( -4.716976649647098618, 115.1429263765338078, 6.492361379858953008 ) ) ;
#40500=SURFACE_SIDE_STYLE ('',( #30588 ) ) ;
#40501=UNCERTAINTY_MEASURE_WITH_UNIT (LENGTH_MEASURE( 1.000000000000000082E-05 ), #1882, 'distance_accuracy_value', 'NONE');
#40504=FACE_OUTER_BOUND ( 'NONE', #22943, .T. ) ;
#40506=VERTEX_POINT ( 'NONE', #351 ) ;
#40514=UNCERTAINTY_MEASURE_WITH_UNIT (LENGTH_MEASURE( 1.000000000000000082E-05 ), #54079, 'distance_accuracy_value', 'NONE');
#40517=PRESENTATION_STYLE_ASSIGNMENT (( #45799 ) ) ;
#40519=CARTESIAN_POINT ( 'NONE',  ( 68.00000000000000000, 2.776762340297168394E-15, 12.00000000000000000 ) ) ;
#40523=DIRECTION ( 'NONE',  ( -0.000000000000000000, -0.000000000000000000, -1.000000000000000000 ) ) ;
#40527=PRESENTATION_STYLE_ASSIGNMENT (( #18002 ) ) ;
#40532=CIRCLE ( 'NONE', #9027, 16.00000000000000000 ) ;
#40534=CARTESIAN_POINT ( 'NONE',  ( -75.00000000000000000, 9.372809501821780742, -6.584099566153144067 ) ) ;
#40537=CARTESIAN_POINT ( 'NONE',  ( 48.00000000000000000, 99.99999999999992895, -7.000000000000000000 ) ) ;
#40538=EDGE_CURVE ( 'NONE', #32404, #61539, #50242, .T. ) ;
#40539=CARTESIAN_POINT ( 'NONE',  ( -3.094860106618432471, 139.5949999999999420, -9.525000000000000355 ) ) ;
#40544=UNCERTAINTY_MEASURE_WITH_UNIT (LENGTH_MEASURE( 1.000000000000000082E-05 ), #55353, 'distance_accuracy_value', 'NONE');
#40546=FILL_AREA_STYLE ('',( #7801 ) ) ;
#40554=ORIENTED_EDGE ( 'NONE', *, *, #48431, .F. ) ;
#40555=CARTESIAN_POINT ( 'NONE',  ( -72.00000000000000000, 14.49137674618942562, -9.500000000000000000 ) ) ;
#40557=CIRCLE ( 'NONE', #51791, 8.000000000000000000 ) ;
#40559=CARTESIAN_POINT ( 'NONE',  ( 0.000000000000000000, 131.5549999999999784, -9.525000000000000355 ) ) ;
#40560=( NAMED_UNIT ( * ) PLANE_ANGLE_UNIT ( ) SI_UNIT ( $, .RADIAN. ) );
#40561=CARTESIAN_POINT ( 'NONE',  ( 7.632228543268608334, 119.3429263765338249, -2.479861379858951942 ) ) ;
#40562=DIRECTION ( 'NONE',  ( 1.000000000000000000, 1.027984282060330356E-15, 0.000000000000000000 ) ) ;
#40570=FILL_AREA_STYLE_COLOUR ( '', #38284 ) ;
#40571=CARTESIAN_POINT ( 'NONE',  ( 5.598654528085809545, 112.1449999999999818, -7.705886871421373741 ) ) ;
#40574=FILL_AREA_STYLE ('',( #51118 ) ) ;
#40575=CARTESIAN_POINT ( 'NONE',  ( 9.058813317711337021, 115.6549999999999869, 2.943386871421375783 ) ) ;
#40578=( LENGTH_UNIT ( ) NAMED_UNIT ( * ) SI_UNIT ( .MILLI., .METRE. ) );
#40579=ORIENTED_EDGE ( 'NONE', *, *, #63648, .T. ) ;
#40580=CARTESIAN_POINT ( 'NONE',  ( 8.102448949553181734, 136.5049999999999386, 5.886773742842750679 ) ) ;
#40584=VECTOR ( 'NONE', #44398, 1000.000000000000000 ) ;
#40586=ORIENTED_EDGE ( 'NONE', *, *, #14288, .F. ) ;
#40587=FACE_OUTER_BOUND ( 'NONE', #14263, .T. ) ;
#40588=DIRECTION ( 'NONE',  ( 1.000000000000000000, 0.000000000000000000, 0.000000000000000000 ) ) ;
#40590=( GEOMETRIC_REPRESENTATION_CONTEXT ( 3 ) GLOBAL_UNCERTAINTY_ASSIGNED_CONTEXT ( ( #22927 ) ) GLOBAL_UNIT_ASSIGNED_CONTEXT ( ( #39450, #19593, #62500 ) ) REPRESENTATION_CONTEXT ( 'NONE', 'WORKASPACE' ) );
#40593=MECHANICAL_DESIGN_GEOMETRIC_PRESENTATION_REPRESENTATION('',(#58539),#51776);
#40594=CARTESIAN_POINT ( 'NONE',  ( 60.00000000000000000, 1.797044900979284448E-15, -11.50000000000001066 ) ) ;
#40598=EDGE_LOOP ( 'NONE', ( #35174, #29368, #37231, #46209 ) ) ;
#40599=CARTESIAN_POINT ( 'NONE',  ( 71.99999999999998579, 119.9999999999997868, -7.000000000000000000 ) ) ;
#40602=CARTESIAN_POINT ( 'NONE',  ( 15.48999599679679662, 147.4999999999999716, 9.500000000000000000 ) ) ;
#40603=EDGE_CURVE ( 'NONE', #2689, #28083, #5279, .T. ) ;
#40608=CARTESIAN_POINT ( 'NONE',  ( -5.598654528085808657, 143.6449999999999818, 7.705886871421373741 ) ) ;
#40617=CARTESIAN_POINT ( 'NONE',  ( -3.094860106618432471, 109.5949999999999847, -9.525000000000000355 ) ) ;
#40624=ORIENTED_EDGE ( 'NONE', *, *, #1855, .T. ) ;
#40626=CARTESIAN_POINT ( 'NONE',  ( 60.00000000000000000, -2.024042244987997205E-14, -7.000000000000000000 ) ) ;
#40631=STYLED_ITEM ( 'NONE', ( #59689 ), #11533 ) ;
#40632=EDGE_CURVE ( 'NONE', #5105, #41266, #54690, .T. ) ;
#40634=DIRECTION ( 'NONE',  ( 1.000000000000000000, 0.000000000000000000, 0.000000000000000000 ) ) ;
#40635=LINE ( 'NONE', #29711, #30498 ) ;
#40636=EDGE_LOOP ( 'NONE', ( #67140, #28477, #5680, #63708 ) ) ;
#40640=CARTESIAN_POINT ( 'NONE',  ( -72.00000000000000000, 35.92875272052971525, -9.500000000000000000 ) ) ;
#40646=( GEOMETRIC_REPRESENTATION_CONTEXT ( 3 ) GLOBAL_UNCERTAINTY_ASSIGNED_CONTEXT ( ( #55028 ) ) GLOBAL_UNIT_ASSIGNED_CONTEXT ( ( #32320, #27712, #44204 ) ) REPRESENTATION_CONTEXT ( 'NONE', 'WORKASPACE' ) );
#40648=ORIENTED_EDGE ( 'NONE', *, *, #29136, .T. ) ;
#40649=CIRCLE ( 'NONE', #128, 8.499999999999992895 ) ;
#40654=SURFACE_STYLE_USAGE ( .BOTH. , #31096 ) ;
#40655=CARTESIAN_POINT ( 'NONE',  ( -9.827790563157511022E-16, 134.5570736234661808, 8.025000000000000355 ) ) ;
#40659=CARTESIAN_POINT ( 'NONE',  ( 74.57962914963243861, 19.59826060529046288, -6.436893197989947524 ) ) ;
#40665=SURFACE_STYLE_USAGE ( .BOTH. , #55778 ) ;
#40666=CIRCLE ( 'NONE', #58614, 18.00000000000000355 ) ;
#40669=ORIENTED_EDGE ( 'NONE', *, *, #30038, .T. ) ;
#40672=AXIS2_PLACEMENT_3D ( 'NONE', #56081, #67687, #50138 ) ;
#40673=CARTESIAN_POINT ( 'NONE',  ( 0.000000000000000000, 154.9999999999999716, 0.000000000000000000 ) ) ;
#40675=CARTESIAN_POINT ( 'NONE',  ( -75.48275862068965125, 63.99167409976910648, -6.499999999999999112 ) ) ;
#40676=CIRCLE ( 'NONE', #58622, 23.00000000000000355 ) ;
#40677=DIRECTION ( 'NONE',  ( -1.000000000000000000, 0.000000000000000000, 0.000000000000000000 ) ) ;
#40682=EDGE_LOOP ( 'NONE', ( #9159, #65026, #32349, #63396 ) ) ;
#40684=( NAMED_UNIT ( * ) SI_UNIT ( $, .STERADIAN. ) SOLID_ANGLE_UNIT ( ) );
#40687=AXIS2_PLACEMENT_3D ( 'NONE', #48558, #11565, #33035 ) ;
#40694=EDGE_LOOP ( 'NONE', ( #52282, #64839, #14231, #50629 ) ) ;
#40697=EDGE_CURVE ( 'NONE', #7755, #33323, #28860, .T. ) ;
#40702=VECTOR ( 'NONE', #3049, 1000.000000000000000 ) ;
#40704=FILL_AREA_STYLE ('',( #46339 ) ) ;
#40707=EDGE_CURVE ( 'NONE', #30995, #16782, #35639, .T. ) ;
#40714=CARTESIAN_POINT ( 'NONE',  ( 71.99999999999998579, 64.07124727947029896, 9.500000000000000000 ) ) ;
#40720=CARTESIAN_POINT ( 'NONE',  ( 9.058813317711338797, 154.9549999999999841, -2.943386871421372675 ) ) ;
#40727=DIRECTION ( 'NONE',  ( 1.000000000000000000, 0.000000000000000000, 0.000000000000000000 ) ) ;
#40729=LINE ( 'NONE', #62829, #2275 ) ;
#40732=EDGE_LOOP ( 'NONE', ( #14218, #41818, #62598, #35454 ) ) ;
#40734=PRESENTATION_STYLE_ASSIGNMENT (( #8368 ) ) ;
#40735=VECTOR ( 'NONE', #61137, 1000.000000000000000 ) ;
#40737=EDGE_CURVE ( 'NONE', #53177, #36309, #45105, .T. ) ;
#40738=CARTESIAN_POINT ( 'NONE',  ( -45.00000000000000000, 9.520518382567219717, 6.450733387540871888 ) ) ;
#40741=CARTESIAN_POINT ( 'NONE',  ( -69.50000000000000000, 50.00000000000000000, -12.00000000000000000 ) ) ;
#40742=AXIS2_PLACEMENT_3D ( 'NONE', #49023, #16650, #10657 ) ;
#40744=SURFACE_STYLE_USAGE ( .BOTH. , #32656 ) ;
#40748=DIRECTION ( 'NONE',  ( 0.000000000000000000, 0.000000000000000000, -1.000000000000000000 ) ) ;
#40749=CARTESIAN_POINT ( 'NONE',  ( 21.02379604162864268, 110.4999999999999858, -10.00000000000000000 ) ) ;
#40751=ORIENTED_EDGE ( 'NONE', *, *, #23194, .T. ) ;
#40755=CARTESIAN_POINT ( 'NONE',  ( 7.632228543268607446, 149.0429263765338135, 2.479861379858954606 ) ) ;
#40756=SURFACE_SIDE_STYLE ('',( #61811 ) ) ;
#40758=CARTESIAN_POINT ( 'NONE',  ( 72.49999999999998579, 119.9999999999997868, 9.500000000000000000 ) ) ;
#40766=ORIENTED_EDGE ( 'NONE', *, *, #54300, .T. ) ;
#40768=DIRECTION ( 'NONE',  ( 1.000000000000000000, 0.000000000000000000, 0.000000000000000000 ) ) ;
#40769=CARTESIAN_POINT ( 'NONE',  ( -20.20529291564252361, 114.9650358309326634, 10.39743153126989128 ) ) ;
#40773=DIRECTION ( 'NONE',  ( 0.000000000000000000, 0.000000000000000000, 1.000000000000000000 ) ) ;
#40774=CARTESIAN_POINT ( 'NONE',  ( 4.716976649647096842, 140.8570736234661638, 6.492361379858953896 ) ) ;
#40778=CARTESIAN_POINT ( 'NONE',  ( -23.21231517720797655, 117.9999999999999716, -7.000000000000000000 ) ) ;
#40779=ORIENTED_EDGE ( 'NONE', *, *, #41024, .F. ) ;
#40781=CARTESIAN_POINT ( 'NONE',  ( -44.99154893936432842, 9.591540374752316467, 2.999999999999999556 ) ) ;
#40782=CARTESIAN_POINT ( 'NONE',  ( 45.65811388300841855, 10.21937129433612235, 6.000000000000000888 ) ) ;
#40785=VERTEX_POINT ( 'NONE', #12329 ) ;
#40790=EDGE_CURVE ( 'NONE', #2682, #10224, #35197, .T. ) ;
#40791=COLOUR_RGB ( '', 0.08235294, 0.09019608, 0.10196078) ;
#40793=DIRECTION ( 'NONE',  ( -1.387778780781444413E-14, 0.000000000000000000, -1.000000000000000000 ) ) ;
#40794=EDGE_LOOP ( 'NONE', ( #43123, #14800, #33650 ) ) ;
#40796=CARTESIAN_POINT ( 'NONE',  ( -75.00000000000000000, 35.50862325381056905, -9.500000000000000000 ) ) ;
#40797=FACE_OUTER_BOUND ( 'NONE', #6877, .T. ) ;
#40798=ADVANCED_FACE ( 'NONE', ( #19350 ), #41285, .T. ) ;
#40801=FILL_AREA_STYLE ('',( #68206 ) ) ;
#40806=CARTESIAN_POINT ( 'NONE',  ( -5.598654528085806881, 119.8549999999999898, -7.705886871421374629 ) ) ;
#40812=MECHANICAL_DESIGN_GEOMETRIC_PRESENTATION_REPRESENTATION('',(#16106),#57656);
#40813=DIRECTION ( 'NONE',  ( 0.000000000000000000, 0.000000000000000000, 1.000000000000000000 ) ) ;
#40822=ORIENTED_EDGE ( 'NONE', *, *, #20171, .T. ) ;
#40823=TOROIDAL_SURFACE ( 'NONE', #65543, 14.49999999999999822, 0.5000000000000000000 ) ;
#40826=EDGE_CURVE ( 'NONE', #2827, #2682, #59197, .T. ) ;
#40827=AXIS2_PLACEMENT_3D ( 'NONE', #39562, #48130, #2159 ) ;
#40831=ORIENTED_EDGE ( 'NONE', *, *, #30114, .T. ) ;
#40835=ORIENTED_EDGE ( 'NONE', *, *, #55908, .F. ) ;
#40837=CARTESIAN_POINT ( 'NONE',  ( -60.00000000000000000, -2.024042244987997205E-14, 11.50000000000003020 ) ) ;
#40841=CARTESIAN_POINT ( 'NONE',  ( -5.598654528085808657, 143.6449999999999818, 7.705886871421373741 ) ) ;
#40845=ORIENTED_EDGE ( 'NONE', *, *, #3352, .T. ) ;
#40848=CARTESIAN_POINT ( 'NONE',  ( -3.094860106618432471, 137.7049999999999841, -9.525000000000000355 ) ) ;
#40849=SURFACE_STYLE_FILL_AREA ( #13374 ) ;
#40850=EDGE_CURVE ( 'NONE', #25927, #2411, #29917, .T. ) ;
#40852=ORIENTED_EDGE ( 'NONE', *, *, #3371, .T. ) ;
#40853=CARTESIAN_POINT ( 'NONE',  ( 0.000000000000000000, 119.9429263765338050, -8.025000000000000355 ) ) ;
#40854=FILL_AREA_STYLE ('',( #14098 ) ) ;
#40856=MECHANICAL_DESIGN_GEOMETRIC_PRESENTATION_REPRESENTATION('',(#43086),#43132);
#40859=EDGE_CURVE ( 'NONE', #64235, #10212, #51400, .T. ) ;
#40864=CARTESIAN_POINT ( 'NONE',  ( 20.54889675933014814, 114.6603872790887095, 10.28544290717500509 ) ) ;
#40867=EDGE_LOOP ( 'NONE', ( #5882, #61783, #26753, #15400 ) ) ;
#40868=( LENGTH_UNIT ( ) NAMED_UNIT ( * ) SI_UNIT ( .MILLI., .METRE. ) );
#40870=MECHANICAL_DESIGN_GEOMETRIC_PRESENTATION_REPRESENTATION('',(#28446),#58810);
#40872=SURFACE_STYLE_FILL_AREA ( #55966 ) ;
#40873=CARTESIAN_POINT ( 'NONE',  ( -8.437984349512095861, 151.8070736234661524, -5.166775262442723748E-16 ) ) ;
#40874=CARTESIAN_POINT ( 'NONE',  ( 75.00000000000000000, 20.33294439366000006, 6.261747904192467296 ) ) ;
#40875=PRESENTATION_STYLE_ASSIGNMENT (( #9885 ) ) ;
#40877=SURFACE_STYLE_USAGE ( .BOTH. , #45801 ) ;
#40879=ADVANCED_FACE ( 'NONE', ( #40158 ), #45804, .T. ) ;
#40881=SURFACE_STYLE_FILL_AREA ( #20061 ) ;
#40883=VERTEX_POINT ( 'NONE', #8124 ) ;
#40891=CARTESIAN_POINT ( 'NONE',  ( 9.058813317711337021, 138.5449999999999875, 2.943386871421375783 ) ) ;
#40897=MECHANICAL_DESIGN_GEOMETRIC_PRESENTATION_REPRESENTATION('',(#66676),#10543);
#40898=CARTESIAN_POINT ( 'NONE',  ( -41.03386404901051776, 107.6974965691265140, -3.186685921634084817 ) ) ;
#40899=VERTEX_POINT ( 'NONE', #36967 ) ;
#40905=VECTOR ( 'NONE', #24881, 1000.000000000000000 ) ;
#40906=AXIS2_PLACEMENT_3D ( 'NONE', #25895, #19221, #47058 ) ;
#40907=PRESENTATION_STYLE_ASSIGNMENT (( #67606 ) ) ;
#40908=CARTESIAN_POINT ( 'NONE',  ( 49.12162162162162105, 13.70805908423323238, -10.00000000000000000 ) ) ;
#40909=VERTEX_POINT ( 'NONE', #11224 ) ;
#40911=AXIS2_PLACEMENT_3D ( 'NONE', #27465, #48991, #59136 ) ;
#40912=VERTEX_POINT ( 'NONE', #48212 ) ;
#40918=VERTEX_POINT ( 'NONE', #16197 ) ;
#40922=CARTESIAN_POINT ( 'NONE',  ( 60.00000000000000000, 1.797044900979284448E-15, 11.50000000000003730 ) ) ;
#40923=LINE ( 'NONE', #13809, #15235 ) ;
#40924=ORIENTED_EDGE ( 'NONE', *, *, #13251, .T. ) ;
#40928=CARTESIAN_POINT ( 'NONE',  ( -9.058813317711337021, 110.0449999999999875, -2.943386871421374895 ) ) ;
#40931=CARTESIAN_POINT ( 'NONE',  ( 48.00000000000000000, 99.99999999999992895, 7.500000000000000000 ) ) ;
#40932=CARTESIAN_POINT ( 'NONE',  ( 3.094860106618431583, 112.2049999999999841, 9.525000000000000355 ) ) ;
#40934=ORIENTED_EDGE ( 'NONE', *, *, #47742, .F. ) ;
#40935=CARTESIAN_POINT ( 'NONE',  ( -5.598654528085808657, 138.7549999999999955, 7.705886871421373741 ) ) ;
#40938=CARTESIAN_POINT ( 'NONE',  ( 19.89974874213239886, 114.9999999999999574, 10.50000000000000000 ) ) ;
#40939=MECHANICAL_DESIGN_GEOMETRIC_PRESENTATION_REPRESENTATION('',(#1526),#42063);
#40940=( NAMED_UNIT ( * ) SI_UNIT ( $, .STERADIAN. ) SOLID_ANGLE_UNIT ( ) );
#40944=FILL_AREA_STYLE_COLOUR ( '', #40791 ) ;
#40949=( GEOMETRIC_REPRESENTATION_CONTEXT ( 3 ) GLOBAL_UNCERTAINTY_ASSIGNED_CONTEXT ( ( #1707 ) ) GLOBAL_UNIT_ASSIGNED_CONTEXT ( ( #61396, #2248, #56842 ) ) REPRESENTATION_CONTEXT ( 'NONE', 'WORKASPACE' ) );
#40953=CIRCLE ( 'NONE', #45431, 0.5000000000000000000 ) ;
#40957=EDGE_LOOP ( 'NONE', ( #40383, #43909, #53713 ) ) ;
#40958=EDGE_CURVE ( 'NONE', #67110, #31971, #64889, .T. ) ;
#40960=DIRECTION ( 'NONE',  ( 1.000000000000000000, 0.000000000000000000, 0.000000000000000000 ) ) ;
#40962=ORIENTED_EDGE ( 'NONE', *, *, #52921, .T. ) ;
#40964=PRESENTATION_STYLE_ASSIGNMENT (( #35311 ) ) ;
#40968=CARTESIAN_POINT ( 'NONE',  ( 5.598654528085805993, 141.2449999999999761, 7.705886871421374629 ) ) ;
#40977=DIRECTION ( 'NONE',  ( 0.000000000000000000, 0.000000000000000000, 1.000000000000000000 ) ) ;
#40979=CARTESIAN_POINT ( 'NONE',  ( -5.598654528085806881, 109.7449999999999761, -7.705886871421374629 ) ) ;
#40981=COLOUR_RGB ( '', 0.66274510, 0.83137255, 0.94901961) ;
#40984=DIRECTION ( 'NONE',  ( 0.7071067811865549002, 0.000000000000000000, 0.7071067811865401342 ) ) ;
#40986=EDGE_LOOP ( 'NONE', ( #11742, #30572, #44814, #48277 ) ) ;
#40993=DIRECTION ( 'NONE',  ( -0.000000000000000000, 1.000000000000000000, 0.000000000000000000 ) ) ;
#40999=TOROIDAL_SURFACE ( 'NONE', #42130, 18.50000000000000355, 0.5000000000000000000 ) ;
#41004=EDGE_CURVE ( 'NONE', #9275, #45578, #13947, .T. ) ;
#41005=DIRECTION ( 'NONE',  ( 1.000000000000000000, 0.000000000000000000, 0.000000000000000000 ) ) ;
#41006=ORIENTED_EDGE ( 'NONE', *, *, #60125, .T. ) ;
#41008=DIRECTION ( 'NONE',  ( -0.000000000000000000, -0.000000000000000000, 1.000000000000000000 ) ) ;
#41009=CARTESIAN_POINT ( 'NONE',  ( 7.632228543268607446, 135.1570736234661467, 2.479861379858954606 ) ) ;
#41010=DIRECTION ( 'NONE',  ( -0.000000000000000000, -1.000000000000000000, 0.000000000000000000 ) ) ;
#41017=STYLED_ITEM ( 'NONE', ( #34442 ), #63755 ) ;
#41020=CARTESIAN_POINT ( 'NONE',  ( 8.437984349512095861, 150.3070736234661524, 1.550032578732816828E-15 ) ) ;
#41021=STYLED_ITEM ( 'NONE', ( #17389 ), #48750 ) ;
#41024=EDGE_CURVE ( 'NONE', #39381, #59067, #4553, .T. ) ;
#41028=( LENGTH_UNIT ( ) NAMED_UNIT ( * ) SI_UNIT ( .MILLI., .METRE. ) );
#41035=CARTESIAN_POINT ( 'NONE',  ( -65.99999999999998579, 50.00000000000000000, -11.50000000000000000 ) ) ;
#41038=SURFACE_STYLE_FILL_AREA ( #2625 ) ;
#41040=ORIENTED_EDGE ( 'NONE', *, *, #46482, .T. ) ;
#41044=CARTESIAN_POINT ( 'NONE',  ( 9.058813317711338797, 117.8449999999999847, -2.943386871421372675 ) ) ;
#41048=AXIS2_PLACEMENT_3D ( 'NONE', #57203, #47049, #36128 ) ;
#41049=ORIENTED_EDGE ( 'NONE', *, *, #25816, .T. ) ;
#41053=CARTESIAN_POINT ( 'NONE',  ( -75.00000000000000000, 9.680388875877742549, 6.198302543666472708 ) ) ;
#41054=CARTESIAN_POINT ( 'NONE',  ( -7.682360912638867667, 111.2596883495873925, -4.277065875361336644 ) ) ;
#41057=VERTEX_POINT ( 'NONE', #4908 ) ;
#41059=COLOUR_RGB ( '', 0.31764706, 0.68627451, 0.89019608) ;
#41060=CARTESIAN_POINT ( 'NONE',  ( -65.00000000000000000, -1.962809905030629631E-14, -11.50000000000000355 ) ) ;
#41066=AXIS2_PLACEMENT_3D ( 'NONE', #20973, #69166, #15706 ) ;
#41068=CARTESIAN_POINT ( 'NONE',  ( -5.598654528085808657, 159.7549999999999670, 7.705886871421373741 ) ) ;
#41069=CARTESIAN_POINT ( 'NONE',  ( -74.99999999999998579, 50.00000000000000000, -6.999999999999988454 ) ) ;
#41070=AXIS2_PLACEMENT_3D ( 'NONE', #46744, #19939, #50929 ) ;
#41071=( GEOMETRIC_REPRESENTATION_CONTEXT ( 3 ) GLOBAL_UNCERTAINTY_ASSIGNED_CONTEXT ( ( #14987 ) ) GLOBAL_UNIT_ASSIGNED_CONTEXT ( ( #62540, #47831, #62880 ) ) REPRESENTATION_CONTEXT ( 'NONE', 'WORKASPACE' ) );
#41073=UNCERTAINTY_MEASURE_WITH_UNIT (LENGTH_MEASURE( 1.000000000000000082E-05 ), #38916, 'distance_accuracy_value', 'NONE');
#41075=DIRECTION ( 'NONE',  ( 0.000000000000000000, -0.000000000000000000, 1.000000000000000000 ) ) ;
#41078=VECTOR ( 'NONE', #7086, 1000.000000000000000 ) ;
#41079=EDGE_CURVE ( 'NONE', #11506, #15151, #26359, .T. ) ;
#41081=VERTEX_POINT ( 'NONE', #37324 ) ;
#41083=DIRECTION ( 'NONE',  ( 0.000000000000000000, 0.000000000000000000, 1.000000000000000000 ) ) ;
#41085=AXIS2_PLACEMENT_3D ( 'NONE', #50676, #55604, #28496 ) ;
#41089=STYLED_ITEM ( 'NONE', ( #60655 ), #32465 ) ;
#41091=CARTESIAN_POINT ( 'NONE',  ( -45.00000000000000000, 7.967158085982124049, 7.000000000000001776 ) ) ;
#41093=FILL_AREA_STYLE_COLOUR ( '', #49894 ) ;
#41096=( NAMED_UNIT ( * ) PLANE_ANGLE_UNIT ( ) SI_UNIT ( $, .RADIAN. ) );
#41104=EDGE_CURVE ( 'NONE', #44405, #69362, #50297, .T. ) ;
#41112=ORIENTED_EDGE ( 'NONE', *, *, #12, .T. ) ;
#41113=CARTESIAN_POINT ( 'NONE',  ( -6.826472737025120807, 141.3929263765338078, -4.959722759717907437 ) ) ;
#41114=FACE_OUTER_BOUND ( 'NONE', #53634, .T. ) ;
#41123=DIRECTION ( 'NONE',  ( 0.000000000000000000, 0.000000000000000000, 1.000000000000000000 ) ) ;
#41127=FACE_OUTER_BOUND ( 'NONE', #65537, .T. ) ;
#41128=CARTESIAN_POINT ( 'NONE',  ( 74.99999999999998579, 50.00000000000000000, 9.500000000000000000 ) ) ;
#41133=ORIENTED_EDGE ( 'NONE', *, *, #59374, .T. ) ;
#41137=ORIENTED_EDGE ( 'NONE', *, *, #34461, .F. ) ;
#41147=COLOUR_RGB ( '', 0.08235294, 0.09019608, 0.10196078) ;
#41148=EDGE_LOOP ( 'NONE', ( #12584, #3187, #5743, #13844 ) ) ;
#41153=CARTESIAN_POINT ( 'NONE',  ( 8.752505052433008359, 154.4999999999998863, 3.782828924242557900 ) ) ;
#41154=CARTESIAN_POINT ( 'NONE',  ( 15.98999599679679839, 146.9999999999999716, 9.500000000000000000 ) ) ;
#41157=CARTESIAN_POINT ( 'NONE',  ( -8.102448949553181734, 132.0049999999999386, -5.886773742842749790 ) ) ;
#41162=UNCERTAINTY_MEASURE_WITH_UNIT (LENGTH_MEASURE( 1.000000000000000082E-05 ), #18197, 'distance_accuracy_value', 'NONE');
#41164=AXIS2_PLACEMENT_3D ( 'NONE', #9373, #4056, #68814 ) ;
#41165=ORIENTED_EDGE ( 'NONE', *, *, #5658, .T. ) ;
#41169=( NAMED_UNIT ( * ) SI_UNIT ( $, .STERADIAN. ) SOLID_ANGLE_UNIT ( ) );
#41172=DIRECTION ( 'NONE',  ( 0.000000000000000000, 0.000000000000000000, -1.000000000000000000 ) ) ;
#41173=CARTESIAN_POINT ( 'NONE',  ( -12.72792206135785698, 115.4999999999999574, -10.50000000000000000 ) ) ;
#41184=ORIENTED_EDGE ( 'NONE', *, *, #27339, .F. ) ;
#41188=VECTOR ( 'NONE', #34050, 1000.000000000000000 ) ;
#41192=SURFACE_STYLE_FILL_AREA ( #57324 ) ;
#41194=EDGE_CURVE ( 'NONE', #61072, #38783, #22134, .T. ) ;
#41196=CARTESIAN_POINT ( 'NONE',  ( 3.094860106618435136, 139.2949999999999591, -9.525000000000000355 ) ) ;
#41197=VERTEX_POINT ( 'NONE', #17575 ) ;
#41198=CARTESIAN_POINT ( 'NONE',  ( -48.00000000000000000, 14.49137674618942562, -9.500000000000000000 ) ) ;
#41199=CARTESIAN_POINT ( 'NONE',  ( -9.058813317711337021, 153.1549999999999727, -2.943386871421374895 ) ) ;
#41201=EDGE_CURVE ( 'NONE', #20191, #43736, #14323, .T. ) ;
#41202=VERTEX_POINT ( 'NONE', #927 ) ;
#41203=CARTESIAN_POINT ( 'NONE',  ( 2.607480562269076430, 119.7929263765337993, -8.025000000000000355 ) ) ;
#41204=( NAMED_UNIT ( * ) PLANE_ANGLE_UNIT ( ) SI_UNIT ( $, .RADIAN. ) );
#41205=UNCERTAINTY_MEASURE_WITH_UNIT (LENGTH_MEASURE( 1.000000000000000082E-05 ), #36626, 'distance_accuracy_value', 'NONE');
#41207=( NAMED_UNIT ( * ) SI_UNIT ( $, .STERADIAN. ) SOLID_ANGLE_UNIT ( ) );
#41209=( LENGTH_UNIT ( ) NAMED_UNIT ( * ) SI_UNIT ( .MILLI., .METRE. ) );
#41210=EDGE_LOOP ( 'NONE', ( #18566, #44267, #43968, #4992 ) ) ;
#41217=FACE_OUTER_BOUND ( 'NONE', #4666, .T. ) ;
#41218=UNCERTAINTY_MEASURE_WITH_UNIT (LENGTH_MEASURE( 1.000000000000000082E-05 ), #57272, 'distance_accuracy_value', 'NONE');
#41219=DIRECTION ( 'NONE',  ( 8.659560562354941486E-17, -0.7071067811865469066, 0.7071067811865482389 ) ) ;
#41221=DIRECTION ( 'NONE',  ( 1.000000000000000000, 0.000000000000000000, 0.000000000000000000 ) ) ;
#41222=CYLINDRICAL_SURFACE ( 'NONE', #35387, 10.00000000000000533 ) ;
#41227=ORIENTED_EDGE ( 'NONE', *, *, #33197, .T. ) ;
#41232=ADVANCED_FACE ( 'NONE', ( #39040 ), #11921, .F. ) ;
#41233=CARTESIAN_POINT ( 'NONE',  ( -75.00000000000000000, 9.291225313367323935, -6.640072787442762525 ) ) ;
#41234=CARTESIAN_POINT ( 'NONE',  ( -74.50000000000000000, -2.220952357103124925E-14, -6.500000000000000000 ) ) ;
#41239=CONICAL_SURFACE ( 'NONE', #67018, 5.000000000000004441, 0.7853981633974579379 ) ;
#41240=CARTESIAN_POINT ( 'NONE',  ( 8.102448949553183510, 144.9950000000000045, -5.886773742842746238 ) ) ;
#41242=PRESENTATION_STYLE_ASSIGNMENT (( #52138 ) ) ;
#41245=CARTESIAN_POINT ( 'NONE',  ( -6.826472737025120807, 144.3929263765338078, -4.959722759717907437 ) ) ;
#41249=( LENGTH_UNIT ( ) NAMED_UNIT ( * ) SI_UNIT ( .MILLI., .METRE. ) );
#41253=FILL_AREA_STYLE ('',( #57398 ) ) ;
#41255=FACE_OUTER_BOUND ( 'NONE', #65438, .T. ) ;
#41256=VERTEX_POINT ( 'NONE', #24884 ) ;
#41257=CARTESIAN_POINT ( 'NONE',  ( -8.437984349512095861, 129.6929263765338192, -5.166775262442723748E-16 ) ) ;
#41259=DIRECTION ( 'NONE',  ( -1.000000000000000000, 1.156482317317866302E-16, 0.000000000000000000 ) ) ;
#41260=UNCERTAINTY_MEASURE_WITH_UNIT (LENGTH_MEASURE( 1.000000000000000082E-05 ), #2355, 'distance_accuracy_value', 'NONE');
#41262=FACE_OUTER_BOUND ( 'NONE', #50741, .T. ) ;
#41263=CARTESIAN_POINT ( 'NONE',  ( -45.00000000000000000, 8.553059399042474809, 6.924772212933272719 ) ) ;
#41264=CARTESIAN_POINT ( 'NONE',  ( 44.70264083260470755, 9.999999999999978684, 3.296021741783508041 ) ) ;
#41266=VERTEX_POINT ( 'NONE', #19616 ) ;
#41270=FACE_OUTER_BOUND ( 'NONE', #22769, .T. ) ;
#41275=CARTESIAN_POINT ( 'NONE',  ( -8.102448949553181734, 110.4949999999999903, 5.886773742842747126 ) ) ;
#41276=VERTEX_POINT ( 'NONE', #29100 ) ;
#41278=CARTESIAN_POINT ( 'NONE',  ( -3.094860106618432471, 122.7049999999999699, -9.525000000000000355 ) ) ;
#41280=ADVANCED_FACE ( 'NONE', ( #41114 ), #67117, .F. ) ;
#41283=CARTESIAN_POINT ( 'NONE',  ( 5.598654528085805993, 142.3549999999999898, 7.705886871421374629 ) ) ;
#41285=TOROIDAL_SURFACE ( 'NONE', #19897, 27.49999999999999645, 0.5000000000000000000 ) ;
#41286=FILL_AREA_STYLE ('',( #57434 ) ) ;
#41287=SURFACE_STYLE_FILL_AREA ( #41998 ) ;
#41288=ORIENTED_EDGE ( 'NONE', *, *, #5055, .T. ) ;
#41289=CARTESIAN_POINT ( 'NONE',  ( -71.50000000000000000, 35.92875272052971525, -7.000000000000000000 ) ) ;
#41293=CARTESIAN_POINT ( 'NONE',  ( 8.487565887160195999, 111.4912942411369841, -0.9261705213944099180 ) ) ;
#41295=DIRECTION ( 'NONE',  ( 1.000000000000000000, 0.000000000000000000, 0.000000000000000000 ) ) ;
#41301=VERTEX_POINT ( 'NONE', #55759 ) ;
#41302=DIRECTION ( 'NONE',  ( -0.000000000000000000, -0.000000000000000000, -1.000000000000000000 ) ) ;
#41305=CARTESIAN_POINT ( 'NONE',  ( 9.058813317711337021, 150.5449999999999875, 2.943386871421375783 ) ) ;
#41309=VERTEX_POINT ( 'NONE', #45235 ) ;
#41312=AXIS2_PLACEMENT_3D ( 'NONE', #28415, #54810, #7671 ) ;
#41317=PRESENTATION_STYLE_ASSIGNMENT (( #14213 ) ) ;
#41318=CARTESIAN_POINT ( 'NONE',  ( 10.01517768586949231, 114.6949999999999932, 1.839758294383810543E-15 ) ) ;
#41322=( NAMED_UNIT ( * ) SI_UNIT ( $, .STERADIAN. ) SOLID_ANGLE_UNIT ( ) );
#41331=AXIS2_PLACEMENT_3D ( 'NONE', #5582, #41900, #16544 ) ;
#41333=ADVANCED_FACE ( 'NONE', ( #13172 ), #65957, .F. ) ;
#41334=CARTESIAN_POINT ( 'NONE',  ( -8.437984349512095861, 124.8070736234661382, -5.166775262442723748E-16 ) ) ;
#41342=CARTESIAN_POINT ( 'NONE',  ( -48.00000000000000000, 99.99999999999992895, -9.500000000000000000 ) ) ;
#41343=DIRECTION ( 'NONE',  ( -0.000000000000000000, 1.000000000000000000, -0.000000000000000000 ) ) ;
#41346=ORIENTED_EDGE ( 'NONE', *, *, #42790, .F. ) ;
#41349=EDGE_LOOP ( 'NONE', ( #30770, #61228, #63211, #36453 ) ) ;
#41351=CARTESIAN_POINT ( 'NONE',  ( -7.632228543268608334, 136.9570736234661581, 2.479861379858952830 ) ) ;
#41352=ORIENTED_EDGE ( 'NONE', *, *, #17278, .T. ) ;
#41355=CARTESIAN_POINT ( 'NONE',  ( 48.81081081081080697, 14.09971791521133255, 7.500000000000000000 ) ) ;
#41356=TOROIDAL_SURFACE ( 'NONE', #69407, 29.50000000000000000, 0.5000000000000000000 ) ;
#41359=SURFACE_STYLE_FILL_AREA ( #42767 ) ;
#41360=FILL_AREA_STYLE ('',( #67725 ) ) ;
#41361=ADVANCED_FACE ( 'NONE', ( #44207 ), #63154, .F. ) ;
#41373=CARTESIAN_POINT ( 'NONE',  ( 71.99999999999998579, 64.07124727947029896, -7.500000000000000000 ) ) ;
#41375=AXIS2_PLACEMENT_3D ( 'NONE', #7227, #65261, #18124 ) ;
#41377=CARTESIAN_POINT ( 'NONE',  ( -60.00000000000000000, -2.024042244987997205E-14, -6.500000000000000000 ) ) ;
#41383=CARTESIAN_POINT ( 'NONE',  ( -40.78947368421052744, 108.1536491499103647, 3.158024016299530334 ) ) ;
#41385=CARTESIAN_POINT ( 'NONE',  ( 8.102448949553179958, 126.3949999999999818, 5.886773742842750679 ) ) ;
#41387=CARTESIAN_POINT ( 'NONE',  ( -9.827790563157511022E-16, 112.4429263765338192, 8.025000000000000355 ) ) ;
#41389=EDGE_LOOP ( 'NONE', ( #9963, #48882, #56491, #37699 ) ) ;
#41392=CARTESIAN_POINT ( 'NONE',  ( -44.50000000000000000, 9.999999999999980460, -3.499999999999999112 ) ) ;
#41393=LINE ( 'NONE', #9372, #14465 ) ;
#41397=CARTESIAN_POINT ( 'NONE',  ( -5.805106041259629812, 111.0237597212471456, -6.890929992047162500 ) ) ;
#41399=ADVANCED_FACE ( 'NONE', ( #35390 ), #25504, .F. ) ;
#41405=FACE_OUTER_BOUND ( 'NONE', #27644, .T. ) ;
#41409=DIRECTION ( 'NONE',  ( 1.000000000000000000, -1.541976423090495436E-15, 0.000000000000000000 ) ) ;
#41411=VECTOR ( 'NONE', #56759, 1000.000000000000000 ) ;
#41412=STYLED_ITEM ( 'NONE', ( #26132 ), #66631 ) ;
#41415=CARTESIAN_POINT ( 'NONE',  ( -5.598654528085806881, 155.8549999999999898, -7.705886871421374629 ) ) ;
#41416=AXIS2_PLACEMENT_3D ( 'NONE', #35691, #57123, #8951 ) ;
#41418=AXIS2_PLACEMENT_3D ( 'NONE', #47448, #52687, #21700 ) ;
#41421=DIRECTION ( 'NONE',  ( 0.000000000000000000, -0.000000000000000000, -1.000000000000000000 ) ) ;
#41425=FILL_AREA_STYLE_COLOUR ( '', #23864 ) ;
#41426=ORIENTED_EDGE ( 'NONE', *, *, #7711, .T. ) ;
#41428=( NAMED_UNIT ( * ) SI_UNIT ( $, .STERADIAN. ) SOLID_ANGLE_UNIT ( ) );
#41433=AXIS2_PLACEMENT_3D ( 'NONE', #51063, #25937, #26288 ) ;
#41435=SURFACE_STYLE_USAGE ( .BOTH. , #67802 ) ;
#41436=ORIENTED_EDGE ( 'NONE', *, *, #57741, .F. ) ;
#41437=CARTESIAN_POINT ( 'NONE',  ( -9.058813317711338797, 123.4549999999999841, 2.943386871421373563 ) ) ;
#41438=CARTESIAN_POINT ( 'NONE',  ( -74.99999999999998579, 50.00000000000000000, 11.50000000000003730 ) ) ;
#41444=ORIENTED_EDGE ( 'NONE', *, *, #62409, .T. ) ;
#41446=SURFACE_SIDE_STYLE ('',( #20301 ) ) ;
#41448=ORIENTED_EDGE ( 'NONE', *, *, #52042, .F. ) ;
#41449=CARTESIAN_POINT ( 'NONE',  ( 0.000000000000000000, 155.9429263765338192, -8.025000000000000355 ) ) ;
#41451=CIRCLE ( 'NONE', #60485, 0.5000000000000004441 ) ;
#41454=CARTESIAN_POINT ( 'NONE',  ( 23.21231517720797655, 118.4999999999999716, 7.500000000000000000 ) ) ;
#41458=CARTESIAN_POINT ( 'NONE',  ( 20.99060317843563794, 114.7782486714346533, 10.00000000000000178 ) ) ;
#41459=FILL_AREA_STYLE ('',( #46769 ) ) ;
#41462=FILL_AREA_STYLE_COLOUR ( '', #63237 ) ;
#41463=CARTESIAN_POINT ( 'NONE',  ( -74.97963758645435917, 36.02033812954885406, 9.659135740435630169 ) ) ;
#41464=( NAMED_UNIT ( * ) SI_UNIT ( $, .STERADIAN. ) SOLID_ANGLE_UNIT ( ) );
#41467=VERTEX_POINT ( 'NONE', #19174 ) ;
#41476=DIRECTION ( 'NONE',  ( 0.000000000000000000, 0.000000000000000000, 1.000000000000000000 ) ) ;
#41477=VERTEX_POINT ( 'NONE', #35731 ) ;
#41478=( LENGTH_UNIT ( ) NAMED_UNIT ( * ) SI_UNIT ( .MILLI., .METRE. ) );
#41480=SURFACE_SIDE_STYLE ('',( #56237 ) ) ;
#41484=EDGE_CURVE ( 'NONE', #40244, #36166, #62664, .T. ) ;
#41485=MECHANICAL_DESIGN_GEOMETRIC_PRESENTATION_REPRESENTATION('',(#12207),#5468);
#41486=ADVANCED_FACE ( 'NONE', ( #51916 ), #790, .F. ) ;
#41488=CARTESIAN_POINT ( 'NONE',  ( -5.598654528085806881, 125.8549999999999898, -7.705886871421374629 ) ) ;
#41492=VECTOR ( 'NONE', #44876, 1000.000000000000000 ) ;
#41497=VECTOR ( 'NONE', #34382, 1000.000000000000000 ) ;
#41506=CARTESIAN_POINT ( 'NONE',  ( 44.99999999999977973, 147.4999999999999716, -9.500000000000000000 ) ) ;
#41510=MECHANICAL_DESIGN_GEOMETRIC_PRESENTATION_REPRESENTATION('',(#53825),#46030);
#41511=ORIENTED_EDGE ( 'NONE', *, *, #23598, .T. ) ;
#41512=CARTESIAN_POINT ( 'NONE',  ( -45.75852489800470835, 8.825811131586496217, -6.400570753484253750 ) ) ;
#41521=EDGE_LOOP ( 'NONE', ( #34521, #20024, #65662, #35656 ) ) ;
#41523=CARTESIAN_POINT ( 'NONE',  ( 60.00000000000000000, 1.797044900979284448E-15, -12.00000000000000000 ) ) ;
#41528=CARTESIAN_POINT ( 'NONE',  ( -3.094860106618434248, 152.7949999999999591, 9.525000000000000355 ) ) ;
#41530=CARTESIAN_POINT ( 'NONE',  ( -1.166476076187854022E-15, 154.0550000000000068, 9.525000000000000355 ) ) ;
#41531=CARTESIAN_POINT ( 'NONE',  ( 0.000000000000000000, 114.9999999999999574, 22.50000000000000000 ) ) ;
#41534=CARTESIAN_POINT ( 'NONE',  ( 2.607480562269071989, 112.5929263765338249, 8.025000000000002132 ) ) ;
#41535=CARTESIAN_POINT ( 'NONE',  ( -44.99999999999998579, 119.9999999999999716, 10.00000000000000000 ) ) ;
#41536=CIRCLE ( 'NONE', #39277, 0.5000000000000004441 ) ;
#41537=FILL_AREA_STYLE ('',( #36973 ) ) ;
#41545=FACE_OUTER_BOUND ( 'NONE', #30105, .T. ) ;
#41546=DIRECTION ( 'NONE',  ( -1.000000000000000000, 0.000000000000000000, 0.000000000000000000 ) ) ;
#41548=ORIENTED_EDGE ( 'NONE', *, *, #43660, .T. ) ;
#41549=AXIS2_PLACEMENT_3D ( 'NONE', #38512, #22274, #59905 ) ;
#41550=DIRECTION ( 'NONE',  ( 0.000000000000000000, 0.000000000000000000, 1.000000000000000000 ) ) ;
#41551=COLOUR_RGB ( '', 0.08235294, 0.09019608, 0.10196078) ;
#41554=( GEOMETRIC_REPRESENTATION_CONTEXT ( 3 ) GLOBAL_UNCERTAINTY_ASSIGNED_CONTEXT ( ( #9529 ) ) GLOBAL_UNIT_ASSIGNED_CONTEXT ( ( #15602, #31740, #9967 ) ) REPRESENTATION_CONTEXT ( 'NONE', 'WORKASPACE' ) );
#41556=CARTESIAN_POINT ( 'NONE',  ( 74.54138597727602189, 19.45803563998439856, 6.486986334521347430 ) ) ;
#41557=DIRECTION ( 'NONE',  ( -0.000000000000000000, -0.000000000000000000, -1.000000000000000000 ) ) ;
#41560=EDGE_LOOP ( 'NONE', ( #49660, #34138, #25717 ) ) ;
#41562=FACE_OUTER_BOUND ( 'NONE', #5575, .T. ) ;
#41565=EDGE_CURVE ( 'NONE', #67546, #20470, #15670, .T. ) ;
#41571=EDGE_CURVE ( 'NONE', #54956, #3572, #37860, .T. ) ;
#41572=CARTESIAN_POINT ( 'NONE',  ( -74.99999999999998579, 8.189963308881907267, -5.659193869481054406 ) ) ;
#41574=MECHANICAL_DESIGN_GEOMETRIC_PRESENTATION_REPRESENTATION('',(#7839),#29164);
#41575=CARTESIAN_POINT ( 'NONE',  ( 45.00000000000000000, 10.69371294336139222, 4.000000000000000000 ) ) ;
#41576=CARTESIAN_POINT ( 'NONE',  ( -5.598654528085806881, 151.7450000000000045, -7.705886871421374629 ) ) ;
#41578=ADVANCED_FACE ( 'NONE', ( #32877 ), #58395, .F. ) ;
#41581=STYLED_ITEM ( 'NONE', ( #64719 ), #59192 ) ;
#41590=( LENGTH_UNIT ( ) NAMED_UNIT ( * ) SI_UNIT ( .MILLI., .METRE. ) );
#41593=MECHANICAL_DESIGN_GEOMETRIC_PRESENTATION_REPRESENTATION('',(#5591),#60626);
#41594=SURFACE_STYLE_USAGE ( .BOTH. , #20818 ) ;
#41599=FACE_OUTER_BOUND ( 'NONE', #53225, .T. ) ;
#41600=( GEOMETRIC_REPRESENTATION_CONTEXT ( 3 ) GLOBAL_UNCERTAINTY_ASSIGNED_CONTEXT ( ( #15935 ) ) GLOBAL_UNIT_ASSIGNED_CONTEXT ( ( #41590, #61601, #29622 ) ) REPRESENTATION_CONTEXT ( 'NONE', 'WORKASPACE' ) );
#41601=LINE ( 'NONE', #15560, #22604 ) ;
#41603=CARTESIAN_POINT ( 'NONE',  ( 44.37560827694797183, 9.999999999999980460, 3.428805698905382560 ) ) ;
#41604=AXIS2_PLACEMENT_3D ( 'NONE', #51512, #34991, #3273 ) ;
#41608=CARTESIAN_POINT ( 'NONE',  ( -20.56323889998346388, 115.3189275942976337, -10.00000000000000000 ) ) ;
#41611=AXIS2_PLACEMENT_3D ( 'NONE', #64656, #38658, #60731 ) ;
#41614=CARTESIAN_POINT ( 'NONE',  ( 8.102448949553181734, 120.3949999999999960, 5.886773742842750679 ) ) ;
#41620=CARTESIAN_POINT ( 'NONE',  ( 0.000000000000000000, 119.5549999999999926, -9.525000000000000355 ) ) ;
#41622=CARTESIAN_POINT ( 'NONE',  ( -44.50000000000000000, 9.999999999999980460, 3.000000000000000000 ) ) ;
#41624=CARTESIAN_POINT ( 'NONE',  ( -8.102448949553181734, 141.6050000000000182, 5.886773742842747126 ) ) ;
#41628=CARTESIAN_POINT ( 'NONE',  ( 20.57648123434812959, 114.5706806360227290, 10.27659574044459667 ) ) ;
#41629=SURFACE_SIDE_STYLE ('',( #29996 ) ) ;
#41630=SURFACE_STYLE_USAGE ( .BOTH. , #51824 ) ;
#41631=ORIENTED_EDGE ( 'NONE', *, *, #39032, .T. ) ;
#41638=CARTESIAN_POINT ( 'NONE',  ( 6.257356667978436704, 111.7229373514514634, -5.482883996731869658 ) ) ;
#41640=ORIENTED_EDGE ( 'NONE', *, *, #63836, .T. ) ;
#41641=FILL_AREA_STYLE ('',( #30688 ) ) ;
#41642=DIRECTION ( 'NONE',  ( 1.000000000000000000, 0.000000000000000000, 0.000000000000000000 ) ) ;
#41643=ORIENTED_EDGE ( 'NONE', *, *, #25959, .T. ) ;
#41645=EDGE_CURVE ( 'NONE', #32302, #13670, #17068, .T. ) ;
#41646=PRESENTATION_STYLE_ASSIGNMENT (( #25090 ) ) ;
#41650=DIRECTION ( 'NONE',  ( 1.000000000000000000, 0.000000000000000000, -0.000000000000000000 ) ) ;
#41655=MECHANICAL_DESIGN_GEOMETRIC_PRESENTATION_REPRESENTATION('',(#1119),#29249);
#41656=( NAMED_UNIT ( * ) PLANE_ANGLE_UNIT ( ) SI_UNIT ( $, .RADIAN. ) );
#41657=CARTESIAN_POINT ( 'NONE',  ( -3.094860106618432471, 151.5949999999999704, -9.525000000000000355 ) ) ;
#41659=ADVANCED_FACE ( 'NONE', ( #58220 ), #21131, .T. ) ;
#41661=CARTESIAN_POINT ( 'NONE',  ( 0.000000000000000000, 140.9429263765338192, -8.025000000000000355 ) ) ;
#41664=STYLED_ITEM ( 'NONE', ( #31424 ), #52385 ) ;
#41665=CARTESIAN_POINT ( 'NONE',  ( 24.21231517720798010, 112.4999999999999858, -9.500000000000000000 ) ) ;
#41668=CARTESIAN_POINT ( 'NONE',  ( 9.058813317711337021, 117.5449999999999875, 2.943386871421375783 ) ) ;
#41670=AXIS2_PLACEMENT_3D ( 'NONE', #37681, #39385, #24532 ) ;
#41671=EDGE_CURVE ( 'NONE', #47273, #35967, #13437, .T. ) ;
#41673=FILL_AREA_STYLE ('',( #15293 ) ) ;
#41674=( GEOMETRIC_REPRESENTATION_CONTEXT ( 3 ) GLOBAL_UNCERTAINTY_ASSIGNED_CONTEXT ( ( #48188 ) ) GLOBAL_UNIT_ASSIGNED_CONTEXT ( ( #52735, #26316, #31952 ) ) REPRESENTATION_CONTEXT ( 'NONE', 'WORKASPACE' ) );
#41675=( NAMED_UNIT ( * ) PLANE_ANGLE_UNIT ( ) SI_UNIT ( $, .RADIAN. ) );
#41683=AXIS2_PLACEMENT_3D ( 'NONE', #58950, #20969, #32210 ) ;
#41685=CARTESIAN_POINT ( 'NONE',  ( -9.827790563157511022E-16, 125.5570736234661524, 8.025000000000000355 ) ) ;
#41690=PRESENTATION_STYLE_ASSIGNMENT (( #4329 ) ) ;
#41691=CARTESIAN_POINT ( 'NONE',  ( 7.632228543268608334, 152.3429263765338249, -2.479861379858951942 ) ) ;
#41694=VERTEX_POINT ( 'NONE', #1492 ) ;
#41700=CARTESIAN_POINT ( 'NONE',  ( -72.50000000000000000, 14.49137674618942562, 10.00000000000000000 ) ) ;
#41701=CARTESIAN_POINT ( 'NONE',  ( 8.437984349512095861, 135.3070736234661240, 1.550032578732817026E-15 ) ) ;
#41702=EDGE_CURVE ( 'NONE', #46073, #13670, #23020, .T. ) ;
#41704=ORIENTED_EDGE ( 'NONE', *, *, #29628, .T. ) ;
#41709=PRESENTATION_STYLE_ASSIGNMENT (( #68413 ) ) ;
#41710=CARTESIAN_POINT ( 'NONE',  ( 2.607480562269198554, 142.5929263765338533, 8.024999999999911537 ) ) ;
#41712=AXIS2_PLACEMENT_3D ( 'NONE', #530, #1223, #64950 ) ;
#41717=AXIS2_PLACEMENT_3D ( 'NONE', #65262, #38928, #59632 ) ;
#41719=DIRECTION ( 'NONE',  ( 0.000000000000000000, 0.000000000000000000, -1.000000000000000000 ) ) ;
#41721=DIRECTION ( 'NONE',  ( -0.000000000000000000, -0.000000000000000000, -1.000000000000000000 ) ) ;
#41722=DIRECTION ( 'NONE',  ( -0.000000000000000000, -0.000000000000000000, 1.000000000000000000 ) ) ;
#41723=UNCERTAINTY_MEASURE_WITH_UNIT (LENGTH_MEASURE( 1.000000000000000082E-05 ), #18517, 'distance_accuracy_value', 'NONE');
#41724=VERTEX_POINT ( 'NONE', #68023 ) ;
#41728=CARTESIAN_POINT ( 'NONE',  ( 0.000000000000000000, 149.9999999999999716, 0.000000000000000000 ) ) ;
#41733=ORIENTED_EDGE ( 'NONE', *, *, #3056, .F. ) ;
#41734=( LENGTH_UNIT ( ) NAMED_UNIT ( * ) SI_UNIT ( .MILLI., .METRE. ) );
#41739=CARTESIAN_POINT ( 'NONE',  ( -3.094860106618432471, 127.5949999999999847, -9.525000000000000355 ) ) ;
#41742=CARTESIAN_POINT ( 'NONE',  ( 7.632228543268608334, 113.3429263765338106, -2.479861379858951942 ) ) ;
#41743=EDGE_CURVE ( 'NONE', #61387, #29181, #10097, .T. ) ;
#41744=STYLED_ITEM ( 'NONE', ( #48778 ), #12804 ) ;
#41746=ORIENTED_EDGE ( 'NONE', *, *, #42648, .F. ) ;
#41747=DIRECTION ( 'NONE',  ( 0.000000000000000000, 1.000000000000000000, 0.000000000000000000 ) ) ;
#41758=CIRCLE ( 'NONE', #67524, 0.5000000000000004441 ) ;
#41767=CARTESIAN_POINT ( 'NONE',  ( 9.058813317711337021, 157.6550000000000011, 2.943386871421375783 ) ) ;
#41768=FILL_AREA_STYLE_COLOUR ( '', #63863 ) ;
#41772=EDGE_CURVE ( 'NONE', #41202, #13131, #19051, .T. ) ;
#41777=CARTESIAN_POINT ( 'NONE',  ( -41.49999999999997868, 10.49999999999998046, 3.000000000000000000 ) ) ;
#41779=FILL_AREA_STYLE_COLOUR ( '', #19202 ) ;
#41785=ORIENTED_EDGE ( 'NONE', *, *, #6372, .F. ) ;
#41786=STYLED_ITEM ( 'NONE', ( #51350 ), #60433 ) ;
#41788=STYLED_ITEM ( 'NONE', ( #19077 ), #45997 ) ;
#41790=CARTESIAN_POINT ( 'NONE',  ( -20.07572180596747913, 115.0406156812134952, 10.00000000000000000 ) ) ;
#41799=CARTESIAN_POINT ( 'NONE',  ( -5.598654528085808657, 120.7549999999999812, 7.705886871421373741 ) ) ;
#41801=( LENGTH_UNIT ( ) NAMED_UNIT ( * ) SI_UNIT ( .MILLI., .METRE. ) );
#41802=ADVANCED_FACE ( 'NONE', ( #30691 ), #19094, .T. ) ;
#41807=COLOUR_RGB ( '', 0.72549020, 0.75294118, 0.79215686) ;
#41809=( LENGTH_UNIT ( ) NAMED_UNIT ( * ) SI_UNIT ( .MILLI., .METRE. ) );
#41811=( LENGTH_UNIT ( ) NAMED_UNIT ( * ) SI_UNIT ( .MILLI., .METRE. ) );
#41813=CARTESIAN_POINT ( 'NONE',  ( 4.716976649647099507, 152.6429263765338078, -6.492361379858953008 ) ) ;
#41818=ORIENTED_EDGE ( 'NONE', *, *, #25841, .F. ) ;
#41819=AXIS2_PLACEMENT_3D ( 'NONE', #60540, #39488, #49326 ) ;
#41821=CARTESIAN_POINT ( 'NONE',  ( 21.02379604162863913, 114.4999999999999574, 10.00000000000000000 ) ) ;
#41822=CARTESIAN_POINT ( 'NONE',  ( 70.87837837837835764, 13.70805908423324482, -10.00000000000000000 ) ) ;
#41826=DIRECTION ( 'NONE',  ( 0.000000000000000000, 0.000000000000000000, 1.000000000000000000 ) ) ;
#41828=LINE ( 'NONE', #19965, #1282 ) ;
#41834=CARTESIAN_POINT ( 'NONE',  ( 60.00000000000000000, -2.024042244987997205E-14, 7.000000000000000000 ) ) ;
#41836=ADVANCED_FACE ( 'NONE', ( #53560 ), #53227, .F. ) ;
#41837=DIRECTION ( 'NONE',  ( -0.000000000000000000, -0.000000000000000000, -1.000000000000000000 ) ) ;
#41840=DIRECTION ( 'NONE',  ( 0.000000000000000000, 0.000000000000000000, 1.000000000000000000 ) ) ;
#41846=DIRECTION ( 'NONE',  ( -1.000000000000000000, 0.000000000000000000, 0.000000000000000000 ) ) ;
#41847=AXIS2_PLACEMENT_3D ( 'NONE', #55572, #17622, #33087 ) ;
#41852=CARTESIAN_POINT ( 'NONE',  ( -8.102448949553181734, 123.0049999999999955, -5.886773742842749790 ) ) ;
#41854=VECTOR ( 'NONE', #39276, 1000.000000000000000 ) ;
#41857=MECHANICAL_DESIGN_GEOMETRIC_PRESENTATION_REPRESENTATION('',(#5840),#47496);
#41858=ADVANCED_FACE ( 'NONE', ( #5689 ), #43415, .T. ) ;
#41860=DIRECTION ( 'NONE',  ( 0.000000000000000000, -1.000000000000000000, 0.000000000000000000 ) ) ;
#41864=SURFACE_SIDE_STYLE ('',( #19315 ) ) ;
#41865=COLOUR_RGB ( '', 0.72549020, 0.75294118, 0.79215686) ;
#41866=DIRECTION ( 'NONE',  ( 1.000000000000000000, 0.000000000000000000, 0.000000000000000000 ) ) ;
#41867=CARTESIAN_POINT ( 'NONE',  ( 7.632228543268607446, 135.1570736234661467, 2.479861379858954606 ) ) ;
#41869=PRESENTATION_STYLE_ASSIGNMENT (( #68571 ) ) ;
#41872=DIRECTION ( 'NONE',  ( 1.000000000000000000, 0.000000000000000000, 0.000000000000000000 ) ) ;
#41873=CARTESIAN_POINT ( 'NONE',  ( 7.632228543268607446, 131.0429263765338135, 2.479861379858954606 ) ) ;
#41874=UNCERTAINTY_MEASURE_WITH_UNIT (LENGTH_MEASURE( 1.000000000000000082E-05 ), #22624, 'distance_accuracy_value', 'NONE');
#41876=DIRECTION ( 'NONE',  ( -1.000000000000000000, 0.000000000000000000, 0.000000000000000000 ) ) ;
#41888=COLOUR_RGB ( '', 0.09019608, 0.27058824, 0.51372549) ;
#41890=CARTESIAN_POINT ( 'NONE',  ( -10.01517768586949231, 146.1949999999999648, -6.132527647946036459E-16 ) ) ;
#41891=DIRECTION ( 'NONE',  ( 1.000000000000000000, 0.000000000000000000, 0.000000000000000000 ) ) ;
#41894=CARTESIAN_POINT ( 'NONE',  ( 0.000000000000000000, 114.4999999999999574, 0.000000000000000000 ) ) ;
#41895=CARTESIAN_POINT ( 'NONE',  ( -1.166476076187854022E-15, 145.0549999999999784, 9.525000000000000355 ) ) ;
#41897=FILL_AREA_STYLE ('',( #67913 ) ) ;
#41899=CARTESIAN_POINT ( 'NONE',  ( 6.826472737025121695, 128.4929263765338305, -4.959722759717905660 ) ) ;
#41900=DIRECTION ( 'NONE',  ( -0.000000000000000000, -0.000000000000000000, -1.000000000000000000 ) ) ;
#41901=UNCERTAINTY_MEASURE_WITH_UNIT (LENGTH_MEASURE( 1.000000000000000082E-05 ), #38436, 'distance_accuracy_value', 'NONE');
#41908=ORIENTED_EDGE ( 'NONE', *, *, #10976, .T. ) ;
#41909=CARTESIAN_POINT ( 'NONE',  ( -41.72781494893835230, 107.4000720140338387, -4.000000000000000000 ) ) ;
#41913=CYLINDRICAL_SURFACE ( 'NONE', #34078, 0.5000000000000004441 ) ;
#41916=ORIENTED_EDGE ( 'NONE', *, *, #51785, .T. ) ;
#41917=SURFACE_SIDE_STYLE ('',( #36291 ) ) ;
#41919=TOROIDAL_SURFACE ( 'NONE', #37461, 1.000000000000000000, 0.5000000000000000000 ) ;
#41920=EDGE_CURVE ( 'NONE', #19597, #34517, #30129, .T. ) ;
#41922=CARTESIAN_POINT ( 'NONE',  ( -6.826472737025120807, 152.1070736234661354, 4.959722759717906548 ) ) ;
#41923=CARTESIAN_POINT ( 'NONE',  ( 75.00000000000000000, 19.46449454893559050, 6.525737028834527109 ) ) ;
#41924=CARTESIAN_POINT ( 'NONE',  ( 4.716976649647099507, 146.6429263765338078, -6.492361379858953008 ) ) ;
#41929=VECTOR ( 'NONE', #11602, 1000.000000000000000 ) ;
#41933=( NAMED_UNIT ( * ) SI_UNIT ( $, .STERADIAN. ) SOLID_ANGLE_UNIT ( ) );
#41934=AXIS2_PLACEMENT_3D ( 'NONE', #31920, #31212, #63592 ) ;
#41935=B_SPLINE_CURVE_WITH_KNOTS ( 'NONE', 3,
 ( #44765, #66163, #29925, #18689, #13389, #40864, #23952, #45110 ),
 .UNSPECIFIED., .F., .F.,
 ( 4, 2, 2, 4 ),
 ( 0.000000000000000000, 0.0004782788118992547534, 0.0007174182178488821031, 0.0009565576237985095069 ),
 .UNSPECIFIED. ) ;
#41938=EDGE_LOOP ( 'NONE', ( #29020, #64803, #43837, #34149 ) ) ;
#41940=VECTOR ( 'NONE', #50714, 1000.000000000000000 ) ;
#41944=CARTESIAN_POINT ( 'NONE',  ( 71.49999999999998579, 119.9999999999997868, -7.500000000000000000 ) ) ;
#41946=CARTESIAN_POINT ( 'NONE',  ( 5.598654528085805993, 147.2449999999999761, 7.705886871421374629 ) ) ;
#41952=CARTESIAN_POINT ( 'NONE',  ( -41.30869453359410670, 107.2693964154585871, -3.464738947915713574 ) ) ;
#41953=CIRCLE ( 'NONE', #26171, 16.50000000000000000 ) ;
#41960=CARTESIAN_POINT ( 'NONE',  ( 34.99999999999992895, 112.9999999999999858, 9.500000000000000000 ) ) ;
#41961=DIRECTION ( 'NONE',  ( 8.659560562354879857E-17, 0.7071067811865517916, -0.7071067811865431318 ) ) ;
#41963=ORIENTED_EDGE ( 'NONE', *, *, #52996, .F. ) ;
#41964=AXIS2_PLACEMENT_3D ( 'NONE', #52791, #10560, #41546 ) ;
#41969=CARTESIAN_POINT ( 'NONE',  ( -45.91547277936962246, 9.430195807687223208, 6.000000000000001776 ) ) ;
#41975=ORIENTED_EDGE ( 'NONE', *, *, #17022, .T. ) ;
#41979=EDGE_CURVE ( 'NONE', #58118, #53591, #28878, .T. ) ;
#41982=CARTESIAN_POINT ( 'NONE',  ( -10.01517768586949231, 119.1949999999999932, -6.132527647946036459E-16 ) ) ;
#41983=PRESENTATION_STYLE_ASSIGNMENT (( #56823 ) ) ;
#41985=( GEOMETRIC_REPRESENTATION_CONTEXT ( 3 ) GLOBAL_UNCERTAINTY_ASSIGNED_CONTEXT ( ( #46217 ) ) GLOBAL_UNIT_ASSIGNED_CONTEXT ( ( #8837, #62984, #41933 ) ) REPRESENTATION_CONTEXT ( 'NONE', 'WORKASPACE' ) );
#41988=SURFACE_STYLE_FILL_AREA ( #20481 ) ;
#41989=CARTESIAN_POINT ( 'NONE',  ( -8.102448949553179958, 123.6049999999999756, 5.886773742842747126 ) ) ;
#41993=CARTESIAN_POINT ( 'NONE',  ( -8.102448949553181734, 150.0049999999999386, -5.886773742842749790 ) ) ;
#41998=FILL_AREA_STYLE ('',( #8562 ) ) ;
#42000=ORIENTED_EDGE ( 'NONE', *, *, #2240, .T. ) ;
#42001=MECHANICAL_DESIGN_GEOMETRIC_PRESENTATION_REPRESENTATION('',(#21707),#304);
#42003=STYLED_ITEM ( 'NONE', ( #62272 ), #646 ) ;
#42005=DIRECTION ( 'NONE',  ( -0.000000000000000000, -0.000000000000000000, 1.000000000000000000 ) ) ;
#42008=CARTESIAN_POINT ( 'NONE',  ( 8.154247983011931211, 111.3129849151904978, 3.079081823141366581 ) ) ;
#42010=CIRCLE ( 'NONE', #63292, 8.025000000000000355 ) ;
#42011=EDGE_CURVE ( 'NONE', #47797, #25427, #22603, .T. ) ;
#42012=DIRECTION ( 'NONE',  ( 0.000000000000000000, -1.000000000000000000, 0.000000000000000000 ) ) ;
#42013=ORIENTED_EDGE ( 'NONE', *, *, #64121, .F. ) ;
#42014=DIRECTION ( 'NONE',  ( 1.000000000000000000, 0.000000000000000000, 0.000000000000000000 ) ) ;
#42017=DIRECTION ( 'NONE',  ( 1.000000000000000000, 0.000000000000000000, -0.000000000000000000 ) ) ;
#42021=FILL_AREA_STYLE ('',( #20513 ) ) ;
#42023=CIRCLE ( 'NONE', #21728, 0.5000000000000004441 ) ;
#42025=CARTESIAN_POINT ( 'NONE',  ( -5.598654528085806881, 148.7449999999999761, -7.705886871421374629 ) ) ;
#42029=STYLED_ITEM ( 'NONE', ( #31003 ), #31064 ) ;
#42030=ORIENTED_EDGE ( 'NONE', *, *, #16780, .T. ) ;
#42033=SURFACE_SIDE_STYLE ('',( #57464 ) ) ;
#42034=STYLED_ITEM ( 'NONE', ( #62602 ), #6571 ) ;
#42037=CARTESIAN_POINT ( 'NONE',  ( 8.102448949553181734, 117.3949999999999818, 5.886773742842750679 ) ) ;
#42042=( NAMED_UNIT ( * ) SI_UNIT ( $, .STERADIAN. ) SOLID_ANGLE_UNIT ( ) );
#42049=MECHANICAL_DESIGN_GEOMETRIC_PRESENTATION_REPRESENTATION('',(#46522),#13926);
#42050=CARTESIAN_POINT ( 'NONE',  ( -20.56347600517836938, 115.3187862480272372, -10.00000000000000000 ) ) ;
#42052=SURFACE_SIDE_STYLE ('',( #5050 ) ) ;
#42058=STYLED_ITEM ( 'NONE', ( #12704 ), #47145 ) ;
#42059=CARTESIAN_POINT ( 'NONE',  ( -15.98999599679679839, 117.4999999999999716, -10.00000000000000000 ) ) ;
#42063=( GEOMETRIC_REPRESENTATION_CONTEXT ( 3 ) GLOBAL_UNCERTAINTY_ASSIGNED_CONTEXT ( ( #50343 ) ) GLOBAL_UNIT_ASSIGNED_CONTEXT ( ( #22193, #17298, #17634 ) ) REPRESENTATION_CONTEXT ( 'NONE', 'WORKASPACE' ) );
#42072=FILL_AREA_STYLE ('',( #8627 ) ) ;
#42073=CARTESIAN_POINT ( 'NONE',  ( -8.437984349512095861, 139.8070736234661240, -5.166775262442723748E-16 ) ) ;
#42074=CARTESIAN_POINT ( 'NONE',  ( 15.98999599679679839, 117.9999999999999716, -7.500000000000000000 ) ) ;
#42076=VERTEX_POINT ( 'NONE', #29590 ) ;
#42077=LINE ( 'NONE', #63479, #44027 ) ;
#42081=CARTESIAN_POINT ( 'NONE',  ( -20.71231517720797655, 149.4999999999999716, -10.00000000000000000 ) ) ;
#42082=EDGE_LOOP ( 'NONE', ( #66172, #14685, #30598, #53230 ) ) ;
#42086=DIRECTION ( 'NONE',  ( 0.000000000000000000, -1.000000000000000000, 0.000000000000000000 ) ) ;
#42089=ORIENTED_EDGE ( 'NONE', *, *, #3257, .T. ) ;
#42090=AXIS2_PLACEMENT_3D ( 'NONE', #18054, #12762, #39539 ) ;
#42093=ORIENTED_EDGE ( 'NONE', *, *, #60557, .F. ) ;
#42094=CARTESIAN_POINT ( 'NONE',  ( 75.00000000000000000, -2.215169945516535778E-14, 9.500000000000000000 ) ) ;
#42095=AXIS2_PLACEMENT_3D ( 'NONE', #50204, #34360, #23125 ) ;
#42099=ORIENTED_EDGE ( 'NONE', *, *, #17046, .T. ) ;
#42106=VERTEX_POINT ( 'NONE', #4840 ) ;
#42107=DIRECTION ( 'NONE',  ( 0.000000000000000000, 0.000000000000000000, 1.000000000000000000 ) ) ;
#42108=TOROIDAL_SURFACE ( 'NONE', #11712, 13.50000000000000178, 0.5000000000000000000 ) ;
#42111=CARTESIAN_POINT ( 'NONE',  ( -5.598654528085806881, 118.7449999999999903, -7.705886871421374629 ) ) ;
#42113=SURFACE_STYLE_USAGE ( .BOTH. , #52291 ) ;
#42114=( NAMED_UNIT ( * ) PLANE_ANGLE_UNIT ( ) SI_UNIT ( $, .RADIAN. ) );
#42116=( NAMED_UNIT ( * ) SI_UNIT ( $, .STERADIAN. ) SOLID_ANGLE_UNIT ( ) );
#42118=( NAMED_UNIT ( * ) SI_UNIT ( $, .STERADIAN. ) SOLID_ANGLE_UNIT ( ) );
#42119=STYLED_ITEM ( 'NONE', ( #28479 ), #38249 ) ;
#42121=DIRECTION ( 'NONE',  ( -1.156482317317873451E-16, 1.000000000000000000, 0.000000000000000000 ) ) ;
#42126=COLOUR_RGB ( '', 0.66274510, 0.83137255, 0.94901961) ;
#42128=CARTESIAN_POINT ( 'NONE',  ( -45.00000000000000000, 99.99999999999992895, 10.00000000000000000 ) ) ;
#42129=CARTESIAN_POINT ( 'NONE',  ( -60.00000000000000000, -2.024042244987997205E-14, 10.50000000000000000 ) ) ;
#42130=AXIS2_PLACEMENT_3D ( 'NONE', #17282, #38746, #60153 ) ;
#42132=( NAMED_UNIT ( * ) PLANE_ANGLE_UNIT ( ) SI_UNIT ( $, .RADIAN. ) );
#42133=COLOUR_RGB ( '', 0.08235294, 0.09019608, 0.10196078) ;
#42134=CARTESIAN_POINT ( 'NONE',  ( 9.058813317711338797, 160.9549999999999841, -2.943386871421372675 ) ) ;
#42136=DIRECTION ( 'NONE',  ( 0.6842105263157866046, 0.7292845505553195995, 0.000000000000000000 ) ) ;
#42137=SURFACE_SIDE_STYLE ('',( #36505 ) ) ;
#42141=ADVANCED_FACE ( 'NONE', ( #15432 ), #56315, .F. ) ;
#42145=FILL_AREA_STYLE ('',( #20635 ) ) ;
#42146=EDGE_CURVE ( 'NONE', #15159, #37491, #22334, .T. ) ;
#42147=SURFACE_SIDE_STYLE ('',( #20636 ) ) ;
#42152=VERTEX_POINT ( 'NONE', #13403 ) ;
#42156=CARTESIAN_POINT ( 'NONE',  ( 2.607480562269071989, 116.7070736234661581, 8.025000000000002132 ) ) ;
#42158=CARTESIAN_POINT ( 'NONE',  ( -20.48327417467292832, 114.7638625681370002, 10.30663925914721268 ) ) ;
#42160=( GEOMETRIC_REPRESENTATION_CONTEXT ( 3 ) GLOBAL_UNCERTAINTY_ASSIGNED_CONTEXT ( ( #13553 ) ) GLOBAL_UNIT_ASSIGNED_CONTEXT ( ( #25679, #62974, #67574 ) ) REPRESENTATION_CONTEXT ( 'NONE', 'WORKASPACE' ) );
#42161=CYLINDRICAL_SURFACE ( 'NONE', #56608, 0.5000000000000004441 ) ;
#42164=ORIENTED_EDGE ( 'NONE', *, *, #58749, .F. ) ;
#42167=DIRECTION ( 'NONE',  ( -0.000000000000000000, -0.000000000000000000, -1.000000000000000000 ) ) ;
#42168=ORIENTED_EDGE ( 'NONE', *, *, #45629, .T. ) ;
#42169=CARTESIAN_POINT ( 'NONE',  ( 9.058813317711337021, 118.6549999999999869, 2.943386871421375783 ) ) ;
#42170=FILL_AREA_STYLE ('',( #58980 ) ) ;
#42171=SURFACE_STYLE_USAGE ( .BOTH. , #68503 ) ;
#42172=MECHANICAL_DESIGN_GEOMETRIC_PRESENTATION_REPRESENTATION('',(#33138),#56732);
#42182=CARTESIAN_POINT ( 'NONE',  ( 6.826472737025119919, 151.8929263765337794, 4.959722759717908325 ) ) ;
#42184=DIRECTION ( 'NONE',  ( -1.000000000000000000, -0.000000000000000000, -0.000000000000000000 ) ) ;
#42186=ORIENTED_EDGE ( 'NONE', *, *, #5961, .T. ) ;
#42187=CARTESIAN_POINT ( 'NONE',  ( -45.91025672304792948, 9.422403540771743025, 3.407313310066896417 ) ) ;
#42188=FILL_AREA_STYLE ('',( #46770 ) ) ;
#42194=( GEOMETRIC_REPRESENTATION_CONTEXT ( 3 ) GLOBAL_UNCERTAINTY_ASSIGNED_CONTEXT ( ( #28526 ) ) GLOBAL_UNIT_ASSIGNED_CONTEXT ( ( #3058, #60800, #3414 ) ) REPRESENTATION_CONTEXT ( 'NONE', 'WORKASPACE' ) );
#42196=CARTESIAN_POINT ( 'NONE',  ( 0.000000000000000000, 154.4999999999999432, 0.000000000000000000 ) ) ;
#42198=ORIENTED_EDGE ( 'NONE', *, *, #36259, .F. ) ;
#42200=CARTESIAN_POINT ( 'NONE',  ( 48.50000000000000000, 99.99999999999992895, -7.500000000000000000 ) ) ;
#42201=DIRECTION ( 'NONE',  ( 0.000000000000000000, 0.000000000000000000, -1.000000000000000000 ) ) ;
#42203=STYLED_ITEM ( 'NONE', ( #34969 ), #63938 ) ;
#42204=( NAMED_UNIT ( * ) PLANE_ANGLE_UNIT ( ) SI_UNIT ( $, .RADIAN. ) );
#42206=( NAMED_UNIT ( * ) SI_UNIT ( $, .STERADIAN. ) SOLID_ANGLE_UNIT ( ) );
#42219=CARTESIAN_POINT ( 'NONE',  ( 9.435716007889201506, 154.5000000000000000, -1.372719813851188686 ) ) ;
#42221=CARTESIAN_POINT ( 'NONE',  ( -75.04447465168979647, 36.22723619897207925, -9.923951063982375587 ) ) ;
#42224=CARTESIAN_POINT ( 'NONE',  ( -5.598654528085808657, 129.7549999999999955, 7.705886871421373741 ) ) ;
#42234=CIRCLE ( 'NONE', #10743, 8.500000000000000000 ) ;
#42235=CARTESIAN_POINT ( 'NONE',  ( -4.716976649647098618, 133.1429263765338362, 6.492361379858953008 ) ) ;
#42236=ADVANCED_FACE ( 'NONE', ( #15771 ), #34663, .F. ) ;
#42239=LINE ( 'NONE', #52059, #20634 ) ;
#42240=SURFACE_STYLE_FILL_AREA ( #31243 ) ;
#42243=CARTESIAN_POINT ( 'NONE',  ( 60.00000000000000000, -2.024042244987997205E-14, 7.000000000000000000 ) ) ;
#42245=AXIS2_PLACEMENT_3D ( 'NONE', #16977, #21899, #54584 ) ;
#42246=( GEOMETRIC_REPRESENTATION_CONTEXT ( 3 ) GLOBAL_UNCERTAINTY_ASSIGNED_CONTEXT ( ( #41218 ) ) GLOBAL_UNIT_ASSIGNED_CONTEXT ( ( #57272, #42204, #36902 ) ) REPRESENTATION_CONTEXT ( 'NONE', 'WORKASPACE' ) );
#42251=EDGE_LOOP ( 'NONE', ( #52389, #63050, #1247, #18439 ) ) ;
#42254=MECHANICAL_DESIGN_GEOMETRIC_PRESENTATION_REPRESENTATION('',(#15317),#19743);
#42256=FILL_AREA_STYLE_COLOUR ( '', #60168 ) ;
#42258=ORIENTED_EDGE ( 'NONE', *, *, #14145, .F. ) ;
#42260=( BOUNDED_CURVE ( )  B_SPLINE_CURVE ( 3, ( #31216, #4476, #9453, #56933 ),
 .UNSPECIFIED., .F., .T. ) 
 B_SPLINE_CURVE_WITH_KNOTS ( ( 4, 4 ),
 ( 4.712388980384695003, 6.283185307179586232 ),
 .UNSPECIFIED. ) 
 CURVE ( )  GEOMETRIC_REPRESENTATION_ITEM ( )  RATIONAL_B_SPLINE_CURVE ( ( 1.000000000000000000, 0.8047378541243662697, 0.8047378541243662697, 1.000000000000000000 ) ) 
 REPRESENTATION_ITEM ( '' )  );
#42261=CARTESIAN_POINT ( 'NONE',  ( -10.01517768586949231, 149.1950000000000216, -6.132527647946036459E-16 ) ) ;
#42265=CARTESIAN_POINT ( 'NONE',  ( 8.102448949553179958, 151.5049999999999955, 5.886773742842750679 ) ) ;
#42266=DIRECTION ( 'NONE',  ( 0.000000000000000000, 0.000000000000000000, 1.000000000000000000 ) ) ;
#42269=CARTESIAN_POINT ( 'NONE',  ( -2.607480562269073765, 126.0929263765338249, -8.025000000000000355 ) ) ;
#42270=CARTESIAN_POINT ( 'NONE',  ( -60.00000000000000000, -2.024042244987997205E-14, -9.500000000000000000 ) ) ;
#42272=CARTESIAN_POINT ( 'NONE',  ( 45.00000000000000000, 10.58011009419005433, 6.521986687992751719 ) ) ;
#42273=( GEOMETRIC_REPRESENTATION_CONTEXT ( 3 ) GLOBAL_UNCERTAINTY_ASSIGNED_CONTEXT ( ( #3846 ) ) GLOBAL_UNIT_ASSIGNED_CONTEXT ( ( #56279, #34485, #34824 ) ) REPRESENTATION_CONTEXT ( 'NONE', 'WORKASPACE' ) );
#42275=EDGE_CURVE ( 'NONE', #64972, #44684, #64273, .T. ) ;
#42276=ORIENTED_EDGE ( 'NONE', *, *, #52605, .T. ) ;
#42277=VECTOR ( 'NONE', #63998, 1000.000000000000000 ) ;
#42284=EDGE_CURVE ( 'NONE', #51627, #6348, #45175, .T. ) ;
#42285=CIRCLE ( 'NONE', #43391, 23.00000000000000000 ) ;
#42287=CARTESIAN_POINT ( 'NONE',  ( 60.00000000000000000, 149.4999999999999716, -10.00000000000000000 ) ) ;
#42289=CARTESIAN_POINT ( 'NONE',  ( 6.826472737025119919, 145.8929263765338078, 4.959722759717908325 ) ) ;
#42295=VERTEX_POINT ( 'NONE', #48143 ) ;
#42299=LINE ( 'NONE', #63686, #17369 ) ;
#42301=( LENGTH_UNIT ( ) NAMED_UNIT ( * ) SI_UNIT ( .MILLI., .METRE. ) );
#42304=CARTESIAN_POINT ( 'NONE',  ( -20.12916642283592950, 109.9999999999999858, -10.05319148936170137 ) ) ;
#42305=SURFACE_SIDE_STYLE ('',( #20799 ) ) ;
#42308=CARTESIAN_POINT ( 'NONE',  ( -3.094860106618434248, 146.7950000000000159, 9.525000000000000355 ) ) ;
#42312=CIRCLE ( 'NONE', #11909, 0.5000000000000004441 ) ;
#42315=ORIENTED_EDGE ( 'NONE', *, *, #11098, .T. ) ;
#42319=VECTOR ( 'NONE', #35456, 1000.000000000000000 ) ;
#42321=( GEOMETRIC_REPRESENTATION_CONTEXT ( 3 ) GLOBAL_UNCERTAINTY_ASSIGNED_CONTEXT ( ( #38463 ) ) GLOBAL_UNIT_ASSIGNED_CONTEXT ( ( #29674, #7520, #2886 ) ) REPRESENTATION_CONTEXT ( 'NONE', 'WORKASPACE' ) );
#42322=CARTESIAN_POINT ( 'NONE',  ( 15.98999599679679839, 146.4999999999999716, 9.500000000000000000 ) ) ;
#42323=PRESENTATION_STYLE_ASSIGNMENT (( #41594 ) ) ;
#42324=EDGE_LOOP ( 'NONE', ( #53257, #32496, #52631, #68704 ) ) ;
#42326=STYLED_ITEM ( 'NONE', ( #12075 ), #57568 ) ;
#42328=CARTESIAN_POINT ( 'NONE',  ( -45.86663432203000212, 9.244254510420724102, 6.241797924670663633 ) ) ;
#42330=PRESENTATION_STYLE_ASSIGNMENT (( #3919 ) ) ;
#42331=EDGE_CURVE ( 'NONE', #23279, #60866, #55090, .T. ) ;
#42337=CARTESIAN_POINT ( 'NONE',  ( -9.827790563157511022E-16, 113.5570736234661666, 8.025000000000000355 ) ) ;
#42338=CARTESIAN_POINT ( 'NONE',  ( -8.102448949553181734, 121.8949999999999818, -5.886773742842749790 ) ) ;
#42340=VERTEX_POINT ( 'NONE', #23435 ) ;
#42342=CARTESIAN_POINT ( 'NONE',  ( 5.598654528085805993, 118.3549999999999898, 7.705886871421374629 ) ) ;
#42346=ORIENTED_EDGE ( 'NONE', *, *, #68867, .F. ) ;
#42347=CARTESIAN_POINT ( 'NONE',  ( 3.094860106618431583, 151.2049999999999841, 9.525000000000000355 ) ) ;
#42350=FILL_AREA_STYLE ('',( #3212 ) ) ;
#42354=ORIENTED_EDGE ( 'NONE', *, *, #55098, .F. ) ;
#42356=( NAMED_UNIT ( * ) SI_UNIT ( $, .STERADIAN. ) SOLID_ANGLE_UNIT ( ) );
#42361=( BOUNDED_CURVE ( )  B_SPLINE_CURVE ( 2, ( #29003, #8285, #51522, #39972, #18814, #40296, #2595, #24773, #61374, #2938, #50495 ),
 .UNSPECIFIED., .F., .F. ) 
 B_SPLINE_CURVE_WITH_KNOTS ( ( 3, 2, 2, 2, 2, 3 ),
 ( 0.4705882352941177516, 0.4764705882352942012, 0.4823529411764707620, 0.4882352941176472116, 0.4941176470588237724, 0.5000000000000002220 ),
 .UNSPECIFIED. ) 
 CURVE ( )  GEOMETRIC_REPRESENTATION_ITEM ( )  RATIONAL_B_SPLINE_CURVE ( ( 0.9999999999999991118, 0.9510565162951544194, 1.000000000000000000, 0.9510565162951535312, 1.000000000000000000, 0.9510565162951535312, 1.000000000000000000, 0.9510565162951535312, 1.000000000000000000, 0.9510565162951516438, 1.000000000000001776 ) ) 
 REPRESENTATION_ITEM ( '' )  );
#42368=SURFACE_SIDE_STYLE ('',( #37785 ) ) ;
#42372=SURFACE_SIDE_STYLE ('',( #63429 ) ) ;
#42374=CARTESIAN_POINT ( 'NONE',  ( 9.058813317711338797, 150.8449999999999989, -2.943386871421372675 ) ) ;
#42377=VERTEX_POINT ( 'NONE', #55455 ) ;
#42379=VECTOR ( 'NONE', #54299, 1000.000000000000000 ) ;
#42381=SURFACE_STYLE_USAGE ( .BOTH. , #21198 ) ;
#42383=CARTESIAN_POINT ( 'NONE',  ( -5.598654528085806881, 118.7449999999999903, -7.705886871421374629 ) ) ;
#42386=FACE_OUTER_BOUND ( 'NONE', #33552, .T. ) ;
#42398=CARTESIAN_POINT ( 'NONE',  ( -20.26325459587049238, 115.0245731144845394, -10.00000000000000000 ) ) ;
#42399=CARTESIAN_POINT ( 'NONE',  ( 71.50000000000000000, 14.49137674618942562, 7.500000000000000000 ) ) ;
#42401=EDGE_CURVE ( 'NONE', #21177, #2846, #39652, .T. ) ;
#42404=DIRECTION ( 'NONE',  ( 1.000000000000000000, 0.000000000000000000, 0.000000000000000000 ) ) ;
#42408=DIRECTION ( 'NONE',  ( -1.000000000000000000, 0.000000000000000000, 0.000000000000000000 ) ) ;
#42409=CARTESIAN_POINT ( 'NONE',  ( 60.00000000000000000, 1.797044900979284448E-15, -12.00000000000000000 ) ) ;
#42410=AXIS2_PLACEMENT_3D ( 'NONE', #21521, #22221, #10633 ) ;
#42412=VERTEX_POINT ( 'NONE', #29038 ) ;
#42414=FACE_OUTER_BOUND ( 'NONE', #60421, .T. ) ;
#42416=CARTESIAN_POINT ( 'NONE',  ( 7.632228543268608334, 147.4570736234661581, -2.479861379858951942 ) ) ;
#42423=CARTESIAN_POINT ( 'NONE',  ( -54.49999999999999289, -2.024042244987997205E-14, -6.500000000000000000 ) ) ;
#42430=CARTESIAN_POINT ( 'NONE',  ( 15.98999599679679839, 146.4999999999999716, 7.000000000000000000 ) ) ;
#42433=CARTESIAN_POINT ( 'NONE',  ( -41.49999999999997868, 10.49999999999998046, -3.000000000000000444 ) ) ;
#42434=( GEOMETRIC_REPRESENTATION_CONTEXT ( 3 ) GLOBAL_UNCERTAINTY_ASSIGNED_CONTEXT ( ( #17195 ) ) GLOBAL_UNIT_ASSIGNED_CONTEXT ( ( #35580, #36301, #47206 ) ) REPRESENTATION_CONTEXT ( 'NONE', 'WORKASPACE' ) );
#42436=SURFACE_STYLE_USAGE ( .BOTH. , #42786 ) ;
#42437=ORIENTED_EDGE ( 'NONE', *, *, #11940, .T. ) ;
#42441=FILL_AREA_STYLE_COLOUR ( '', #6591 ) ;
#42443=DIRECTION ( 'NONE',  ( 0.000000000000000000, 1.000000000000000000, -0.000000000000000000 ) ) ;
#42445=CARTESIAN_POINT ( 'NONE',  ( -3.094860106618434248, 119.7949999999999733, 9.525000000000000355 ) ) ;
#42450=LINE ( 'NONE', #63512, #36899 ) ;
#42451=FILL_AREA_STYLE ('',( #59247 ) ) ;
#42463=FACE_OUTER_BOUND ( 'NONE', #49983, .T. ) ;
#42464=UNCERTAINTY_MEASURE_WITH_UNIT (LENGTH_MEASURE( 1.000000000000000082E-05 ), #39838, 'distance_accuracy_value', 'NONE');
#42468=EDGE_CURVE ( 'NONE', #30840, #35810, #67320, .T. ) ;
#42475=CIRCLE ( 'NONE', #3052, 0.5000000000000004441 ) ;
#42476=VECTOR ( 'NONE', #41837, 1000.000000000000000 ) ;
#42477=SURFACE_STYLE_USAGE ( .BOTH. , #52997 ) ;
#42478=CARTESIAN_POINT ( 'NONE',  ( -9.827790563157511022E-16, 139.4429263765338192, 8.025000000000000355 ) ) ;
#42480=FILL_AREA_STYLE ('',( #64595 ) ) ;
#42482=FILL_AREA_STYLE ('',( #16084 ) ) ;
#42484=CARTESIAN_POINT ( 'NONE',  ( -4.716976649647098618, 110.2570736234661695, 6.492361379858953008 ) ) ;
#42485=FACE_OUTER_BOUND ( 'NONE', #63974, .T. ) ;
#42487=( GEOMETRIC_REPRESENTATION_CONTEXT ( 3 ) GLOBAL_UNCERTAINTY_ASSIGNED_CONTEXT ( ( #63534 ) ) GLOBAL_UNIT_ASSIGNED_CONTEXT ( ( #53578, #62725, #42042 ) ) REPRESENTATION_CONTEXT ( 'NONE', 'WORKASPACE' ) );
#42488=DIRECTION ( 'NONE',  ( -1.000000000000000000, 0.000000000000000000, 0.000000000000000000 ) ) ;
#42489=ORIENTED_EDGE ( 'NONE', *, *, #37850, .T. ) ;
#42490=ORIENTED_EDGE ( 'NONE', *, *, #22347, .T. ) ;
#42491=DIRECTION ( 'NONE',  ( 1.000000000000000000, 0.000000000000000000, 0.000000000000000000 ) ) ;
#42492=( GEOMETRIC_REPRESENTATION_CONTEXT ( 3 ) GLOBAL_UNCERTAINTY_ASSIGNED_CONTEXT ( ( #25664 ) ) GLOBAL_UNIT_ASSIGNED_CONTEXT ( ( #46318, #30081, #29753 ) ) REPRESENTATION_CONTEXT ( 'NONE', 'WORKASPACE' ) );
#42495=ORIENTED_EDGE ( 'NONE', *, *, #16078, .F. ) ;
#42496=CARTESIAN_POINT ( 'NONE',  ( -3.094860106618432471, 122.7049999999999699, -9.525000000000000355 ) ) ;
#42497=( NAMED_UNIT ( * ) SI_UNIT ( $, .STERADIAN. ) SOLID_ANGLE_UNIT ( ) );
#42500=EDGE_CURVE ( 'NONE', #28999, #50847, #23114, .T. ) ;
#42503=CARTESIAN_POINT ( 'NONE',  ( 7.632228543268607446, 158.0429263765338419, 2.479861379858954606 ) ) ;
#42504=FILL_AREA_STYLE_COLOUR ( '', #25655 ) ;
#42506=SURFACE_STYLE_FILL_AREA ( #21701 ) ;
#42507=CARTESIAN_POINT ( 'NONE',  ( 21.02379604162863558, 114.4999999999999574, -10.00000000000000000 ) ) ;
#42510=FACE_OUTER_BOUND ( 'NONE', #55275, .T. ) ;
#42511=PRESENTATION_STYLE_ASSIGNMENT (( #4460 ) ) ;
#42512=DIRECTION ( 'NONE',  ( -0.000000000000000000, -0.000000000000000000, -1.000000000000000000 ) ) ;
#42513=SURFACE_SIDE_STYLE ('',( #54403 ) ) ;
#42516=CARTESIAN_POINT ( 'NONE',  ( 0.000000000000000000, 116.9429263765338192, -8.025000000000000355 ) ) ;
#42518=VERTEX_POINT ( 'NONE', #39310 ) ;
#42522=AXIS2_PLACEMENT_3D ( 'NONE', #6924, #5870, #23440 ) ;
#42523=DIRECTION ( 'NONE',  ( -0.000000000000000000, -0.000000000000000000, 1.000000000000000000 ) ) ;
#42524=DIRECTION ( 'NONE',  ( -0.000000000000000000, -1.000000000000000000, -0.000000000000000000 ) ) ;
#42525=EDGE_CURVE ( 'NONE', #37663, #53214, #60714, .T. ) ;
#42526=CARTESIAN_POINT ( 'NONE',  ( -9.827790563157511022E-16, 113.5570736234661666, 8.025000000000000355 ) ) ;
#42543=CIRCLE ( 'NONE', #22311, 0.5000000000000004441 ) ;
#42544=CARTESIAN_POINT ( 'NONE',  ( -74.66854778504175272, 36.33518165874313866, -9.980650098286423244 ) ) ;
#42546=CARTESIAN_POINT ( 'NONE',  ( 3.094860106618431583, 127.2049999999999841, 9.525000000000000355 ) ) ;
#42550=UNCERTAINTY_MEASURE_WITH_UNIT (LENGTH_MEASURE( 1.000000000000000082E-05 ), #56571, 'distance_accuracy_value', 'NONE');
#42551=FACE_OUTER_BOUND ( 'NONE', #52758, .T. ) ;
#42554=COLOUR_RGB ( '', 0.31764706, 0.68627451, 0.89019608) ;
#42555=ADVANCED_FACE ( 'NONE', ( #68809 ), #47751, .F. ) ;
#42557=DIRECTION ( 'NONE',  ( 1.000000000000000000, 1.665334536937734495E-14, 0.000000000000000000 ) ) ;
#42560=DIRECTION ( 'NONE',  ( 0.000000000000000000, 0.000000000000000000, 1.000000000000000000 ) ) ;
#42561=EDGE_LOOP ( 'NONE', ( #45848, #15174, #20288, #38722 ) ) ;
#42562=CIRCLE ( 'NONE', #12171, 8.025000000000000355 ) ;
#42566=UNCERTAINTY_MEASURE_WITH_UNIT (LENGTH_MEASURE( 1.000000000000000082E-05 ), #44030, 'distance_accuracy_value', 'NONE');
#42569=AXIS2_PLACEMENT_3D ( 'NONE', #50143, #17454, #44551 ) ;
#42573=ORIENTED_EDGE ( 'NONE', *, *, #47663, .T. ) ;
#42575=CARTESIAN_POINT ( 'NONE',  ( -74.50000000000000000, -2.220952357103124925E-14, -9.500000000000000000 ) ) ;
#42578=STYLED_ITEM ( 'NONE', ( #53982 ), #14812 ) ;
#42579=SURFACE_SIDE_STYLE ('',( #59380 ) ) ;
#42580=CARTESIAN_POINT ( 'NONE',  ( 8.102448949553181734, 153.3950000000000387, 5.886773742842750679 ) ) ;
#42581=CARTESIAN_POINT ( 'NONE',  ( -83.49999999999997158, 50.00000000000000000, 12.00000000000000000 ) ) ;
#42583=VERTEX_POINT ( 'NONE', #62462 ) ;
#42585=CARTESIAN_POINT ( 'NONE',  ( -10.01517768586949408, 153.3050000000000068, -6.132527647946036459E-16 ) ) ;
#42588=CARTESIAN_POINT ( 'NONE',  ( -8.437984349512095861, 129.6929263765338192, -5.166775262442723748E-16 ) ) ;
#42589=DIRECTION ( 'NONE',  ( -1.000000000000000000, 0.000000000000000000, 0.000000000000000000 ) ) ;
#42590=UNCERTAINTY_MEASURE_WITH_UNIT (LENGTH_MEASURE( 1.000000000000000082E-05 ), #7668, 'distance_accuracy_value', 'NONE');
#42591=CARTESIAN_POINT ( 'NONE',  ( -75.48275862068966546, 36.00832590023090063, -9.555431496530900404 ) ) ;
#42592=( NAMED_UNIT ( * ) PLANE_ANGLE_UNIT ( ) SI_UNIT ( $, .RADIAN. ) );
#42598=LINE ( 'NONE', #35903, #45787 ) ;
#42599=PRESENTATION_STYLE_ASSIGNMENT (( #57709 ) ) ;
#42602=UNCERTAINTY_MEASURE_WITH_UNIT (LENGTH_MEASURE( 1.000000000000000082E-05 ), #5705, 'distance_accuracy_value', 'NONE');
#42603=EDGE_CURVE ( 'NONE', #47060, #61874, #37036, .T. ) ;
#42606=FACE_OUTER_BOUND ( 'NONE', #2237, .T. ) ;
#42607=ORIENTED_EDGE ( 'NONE', *, *, #40826, .T. ) ;
#42620=AXIS2_PLACEMENT_3D ( 'NONE', #43292, #12230, #16531 ) ;
#42621=PRESENTATION_STYLE_ASSIGNMENT (( #33073 ) ) ;
#42623=ADVANCED_FACE ( 'NONE', ( #57541 ), #63883, .F. ) ;
#42624=CARTESIAN_POINT ( 'NONE',  ( 0.000000000000000000, 152.9999999999999716, 0.000000000000000000 ) ) ;
#42630=EDGE_CURVE ( 'NONE', #14819, #23416, #4385, .T. ) ;
#42632=CARTESIAN_POINT ( 'NONE',  ( -1.166476076187854022E-15, 149.9449999999999932, 9.525000000000000355 ) ) ;
#42635=FILL_AREA_STYLE_COLOUR ( '', #5578 ) ;
#42636=UNCERTAINTY_MEASURE_WITH_UNIT (LENGTH_MEASURE( 1.000000000000000082E-05 ), #14761, 'distance_accuracy_value', 'NONE');
#42643=VECTOR ( 'NONE', #27665, 1000.000000000000000 ) ;
#42646=VERTEX_POINT ( 'NONE', #64882 ) ;
#42648=EDGE_CURVE ( 'NONE', #32941, #10860, #38467, .T. ) ;
#42651=AXIS2_PLACEMENT_3D ( 'NONE', #21924, #11702, #10333 ) ;
#42653=CARTESIAN_POINT ( 'NONE',  ( -45.82474114033776402, 9.083251256839144361, 6.320036396439224546 ) ) ;
#42655=FILL_AREA_STYLE ('',( #15564 ) ) ;
#42657=ORIENTED_EDGE ( 'NONE', *, *, #38315, .F. ) ;
#42662=ORIENTED_EDGE ( 'NONE', *, *, #48485, .T. ) ;
#42663=CIRCLE ( 'NONE', #18996, 0.5000000000000006661 ) ;
#42668=CARTESIAN_POINT ( 'NONE',  ( 9.058813317711337021, 123.5449999999999875, 2.943386871421375783 ) ) ;
#42669=SURFACE_STYLE_FILL_AREA ( #10957 ) ;
#42671=STYLED_ITEM ( 'NONE', ( #13101 ), #9569 ) ;
#42672=EDGE_LOOP ( 'NONE', ( #35611, #32153, #49410, #67857 ) ) ;
#42673=PLANE ( 'NONE',  #59996 ) ;
#42674=CARTESIAN_POINT ( 'NONE',  ( 3.094860106618431583, 118.2049999999999699, 9.525000000000000355 ) ) ;
#42677=( GEOMETRIC_REPRESENTATION_CONTEXT ( 3 ) GLOBAL_UNCERTAINTY_ASSIGNED_CONTEXT ( ( #15167 ) ) GLOBAL_UNIT_ASSIGNED_CONTEXT ( ( #34951, #56397, #51144 ) ) REPRESENTATION_CONTEXT ( 'NONE', 'WORKASPACE' ) );
#42678=CARTESIAN_POINT ( 'NONE',  ( -41.00000002860135595, 108.0041655605167676, -3.103651540214122040 ) ) ;
#42680=CARTESIAN_POINT ( 'NONE',  ( 9.058813317711338797, 148.9550000000000125, -2.943386871421372675 ) ) ;
#42681=UNCERTAINTY_MEASURE_WITH_UNIT (LENGTH_MEASURE( 1.000000000000000082E-05 ), #12308, 'distance_accuracy_value', 'NONE');
#42682=MECHANICAL_DESIGN_GEOMETRIC_PRESENTATION_REPRESENTATION('',(#58401),#44929);
#42686=EDGE_CURVE ( 'NONE', #21155, #22693, #56062, .T. ) ;
#42689=ORIENTED_EDGE ( 'NONE', *, *, #65772, .F. ) ;
#42691=CARTESIAN_POINT ( 'NONE',  ( -44.99999999999998579, 119.9999999999999716, -9.500000000000000000 ) ) ;
#42692=PRESENTATION_STYLE_ASSIGNMENT (( #21175 ) ) ;
#42694=EDGE_LOOP ( 'NONE', ( #31308, #39454, #11574, #46377 ) ) ;
#42695=FACE_OUTER_BOUND ( 'NONE', #41148, .T. ) ;
#42697=( NAMED_UNIT ( * ) PLANE_ANGLE_UNIT ( ) SI_UNIT ( $, .RADIAN. ) );
#42699=DIRECTION ( 'NONE',  ( 0.000000000000000000, 0.000000000000000000, 1.000000000000000000 ) ) ;
#42700=CYLINDRICAL_SURFACE ( 'NONE', #12943, 0.5000000000000004441 ) ;
#42712=FILL_AREA_STYLE ('',( #1054 ) ) ;
#42713=CARTESIAN_POINT ( 'NONE',  ( -8.102448949553179958, 149.4949999999999761, 5.886773742842747126 ) ) ;
#42720=PRESENTATION_STYLE_ASSIGNMENT (( #42381 ) ) ;
#42724=CARTESIAN_POINT ( 'NONE',  ( -3.094860106618434248, 122.7949999999999875, 9.525000000000000355 ) ) ;
#42726=COLOUR_RGB ( '', 0.66274510, 0.83137255, 0.94901961) ;
#42727=FACE_OUTER_BOUND ( 'NONE', #16712, .T. ) ;
#42728=CIRCLE ( 'NONE', #23582, 0.4999999999999994449 ) ;
#42729=B_SPLINE_CURVE_WITH_KNOTS ( 'NONE', 3,
 ( #61461, #13280, #45695, #34736, #13635, #56190, #29469, #50940, #49563, #2697, #24190, #1294, #17569, #39034, #12239, #55153, #6983, #28406, #30145, #68167, #3383, #62167, #67813, #36544, #68508, #8384, #68865, #52681, #47081, #13998 ),
 .UNSPECIFIED., .F., .F.,
 ( 4, 2, 2, 2, 2, 2, 2, 2, 2, 2, 2, 2, 2, 2, 4 ),
 ( 0.000000000000000000, 0.001317596576228367410, 0.002635193152456734821, 0.005270386304913469641, 0.006587982881141837485, 0.007905579457370203594, 0.009223176033598571438, 0.01054077260982693928, 0.01185836918605530713, 0.01317596576228367497, 0.01449356233851204108, 0.01581115891474040719, 0.01712875549096877503, 0.01844635206719714288, 0.02108154521965387856 ),
 .UNSPECIFIED. ) ;
#42732=MECHANICAL_DESIGN_GEOMETRIC_PRESENTATION_REPRESENTATION('',(#5598),#26915);
#42735=MECHANICAL_DESIGN_GEOMETRIC_PRESENTATION_REPRESENTATION('',(#3311),#5545);
#42736=DIRECTION ( 'NONE',  ( 0.000000000000000000, 0.000000000000000000, 1.000000000000000000 ) ) ;
#42737=AXIS2_PLACEMENT_3D ( 'NONE', #33415, #34105, #17930 ) ;
#42739=( NAMED_UNIT ( * ) SI_UNIT ( $, .STERADIAN. ) SOLID_ANGLE_UNIT ( ) );
#42740=EDGE_LOOP ( 'NONE', ( #16307, #15969, #55666, #52080 ) ) ;
#42742=EDGE_CURVE ( 'NONE', #49636, #3770, #3184, .T. ) ;
#42744=STYLED_ITEM ( 'NONE', ( #49271 ), #16335 ) ;
#42751=ORIENTED_EDGE ( 'NONE', *, *, #13090, .F. ) ;
#42754=PRESENTATION_STYLE_ASSIGNMENT (( #64843 ) ) ;
#42758=CARTESIAN_POINT ( 'NONE',  ( -6.826472737025120807, 145.5070736234661410, -4.959722759717907437 ) ) ;
#42760=ORIENTED_EDGE ( 'NONE', *, *, #10360, .T. ) ;
#42764=UNCERTAINTY_MEASURE_WITH_UNIT (LENGTH_MEASURE( 1.000000000000000082E-05 ), #6882, 'distance_accuracy_value', 'NONE');
#42767=FILL_AREA_STYLE ('',( #36790 ) ) ;
#42771=EDGE_CURVE ( 'NONE', #14819, #3572, #59413, .T. ) ;
#42772=( GEOMETRIC_REPRESENTATION_CONTEXT ( 3 ) GLOBAL_UNCERTAINTY_ASSIGNED_CONTEXT ( ( #15330 ) ) GLOBAL_UNIT_ASSIGNED_CONTEXT ( ( #37642, #45239, #32299 ) ) REPRESENTATION_CONTEXT ( 'NONE', 'WORKASPACE' ) );
#42777=( GEOMETRIC_REPRESENTATION_CONTEXT ( 3 ) GLOBAL_UNCERTAINTY_ASSIGNED_CONTEXT ( ( #10969 ) ) GLOBAL_UNIT_ASSIGNED_CONTEXT ( ( #60412, #17550, #12928 ) ) REPRESENTATION_CONTEXT ( 'NONE', 'WORKASPACE' ) );
#42779=( LENGTH_UNIT ( ) NAMED_UNIT ( * ) SI_UNIT ( .MILLI., .METRE. ) );
#42781=AXIS2_PLACEMENT_3D ( 'NONE', #19755, #46898, #52150 ) ;
#42784=SURFACE_STYLE_USAGE ( .BOTH. , #68100 ) ;
#42786=SURFACE_SIDE_STYLE ('',( #32178 ) ) ;
#42787=EDGE_CURVE ( 'NONE', #16782, #49325, #59243, .T. ) ;
#42788=ORIENTED_EDGE ( 'NONE', *, *, #21851, .F. ) ;
#42790=EDGE_CURVE ( 'NONE', #60536, #33822, #11066, .T. ) ;
#42791=AXIS2_PLACEMENT_3D ( 'NONE', #4518, #10858, #59355 ) ;
#42793=( LENGTH_UNIT ( ) NAMED_UNIT ( * ) SI_UNIT ( .MILLI., .METRE. ) );
#42798=EDGE_CURVE ( 'NONE', #31700, #61072, #11772, .T. ) ;
#42799=COLOUR_RGB ( '', 0.31764706, 0.68627451, 0.89019608) ;
#42800=CARTESIAN_POINT ( 'NONE',  ( -10.01517768586949408, 122.1949999999999648, -6.132527647946036459E-16 ) ) ;
#42808=CARTESIAN_POINT ( 'NONE',  ( -9.827790563157511022E-16, 131.5570736234661524, 8.025000000000000355 ) ) ;
#42809=EDGE_CURVE ( 'NONE', #21436, #37680, #62780, .T. ) ;
#42821=CARTESIAN_POINT ( 'NONE',  ( -20.12916642283592950, 110.4999999999999858, -10.05319148936170137 ) ) ;
#42822=DIRECTION ( 'NONE',  ( 0.000000000000000000, 1.000000000000000000, -0.000000000000000000 ) ) ;
#42824=( LENGTH_UNIT ( ) NAMED_UNIT ( * ) SI_UNIT ( .MILLI., .METRE. ) );
#42836=CARTESIAN_POINT ( 'NONE',  ( -8.437984349512095861, 118.8070736234661666, -5.166775262442723748E-16 ) ) ;
#42838=( NAMED_UNIT ( * ) PLANE_ANGLE_UNIT ( ) SI_UNIT ( $, .RADIAN. ) );
#42840=AXIS2_PLACEMENT_3D ( 'NONE', #59977, #7217, #49786 ) ;
#42841=SURFACE_STYLE_USAGE ( .BOTH. , #38248 ) ;
#42844=DIRECTION ( 'NONE',  ( -0.000000000000000000, -0.000000000000000000, -1.000000000000000000 ) ) ;
#42848=CARTESIAN_POINT ( 'NONE',  ( -3.094860106618434248, 117.9049999999999727, 9.525000000000000355 ) ) ;
#42849=DIRECTION ( 'NONE',  ( 0.000000000000000000, 0.000000000000000000, 1.000000000000000000 ) ) ;
#42856=ADVANCED_FACE ( 'NONE', ( #39581 ), #39933, .F. ) ;
#42857=CARTESIAN_POINT ( 'NONE',  ( 7.398009814270800177, 153.1301383316707359, 3.525480039724990355 ) ) ;
#42858=DIRECTION ( 'NONE',  ( -1.000000000000000000, 0.000000000000000000, 0.000000000000000000 ) ) ;
#42860=( GEOMETRIC_REPRESENTATION_CONTEXT ( 3 ) GLOBAL_UNCERTAINTY_ASSIGNED_CONTEXT ( ( #29929 ) ) GLOBAL_UNIT_ASSIGNED_CONTEXT ( ( #47582, #26723, #26398 ) ) REPRESENTATION_CONTEXT ( 'NONE', 'WORKASPACE' ) );
#42861=ORIENTED_EDGE ( 'NONE', *, *, #50830, .F. ) ;
#42862=CARTESIAN_POINT ( 'NONE',  ( 2.607480562269071989, 151.5929263765337680, 8.025000000000002132 ) ) ;
#42863=( NAMED_UNIT ( * ) PLANE_ANGLE_UNIT ( ) SI_UNIT ( $, .RADIAN. ) );
#42867=AXIS2_PLACEMENT_3D ( 'NONE', #26422, #15909, #69014 ) ;
#42868=LINE ( 'NONE', #30864, #38651 ) ;
#42869=EDGE_CURVE ( 'NONE', #11358, #10407, #40425, .T. ) ;
#42872=CARTESIAN_POINT ( 'NONE',  ( 34.99999999999992895, 112.9999999999999858, 7.000000000000000000 ) ) ;
#42873=FILL_AREA_STYLE_COLOUR ( '', #49059 ) ;
#42880=DIRECTION ( 'NONE',  ( -1.156482317317873451E-16, 1.000000000000000000, 0.000000000000000000 ) ) ;
#42881=CARTESIAN_POINT ( 'NONE',  ( -5.237322049151774905, 153.2151860177439460, -6.367445604021556349 ) ) ;
#42882=ORIENTED_EDGE ( 'NONE', *, *, #5445, .F. ) ;
#42884=DIRECTION ( 'NONE',  ( 0.000000000000000000, 1.000000000000000000, -0.000000000000000000 ) ) ;
#42892=FACE_OUTER_BOUND ( 'NONE', #64710, .T. ) ;
#42901=CARTESIAN_POINT ( 'NONE',  ( 60.00000000000000000, 149.4999999999999716, -10.00000000000000000 ) ) ;
#42902=MECHANICAL_DESIGN_GEOMETRIC_PRESENTATION_REPRESENTATION('',(#51854),#68728);
#42903=CARTESIAN_POINT ( 'NONE',  ( -75.00000000000000000, 35.50862325381056905, -9.500000000000000000 ) ) ;
#42905=CARTESIAN_POINT ( 'NONE',  ( -8.102448949553181734, 132.6050000000000182, 5.886773742842747126 ) ) ;
#42910=CARTESIAN_POINT ( 'NONE',  ( -14.98999599679679662, 118.4999999999999716, 9.500000000000000000 ) ) ;
#42913=AXIS2_PLACEMENT_3D ( 'NONE', #6067, #69072, #63765 ) ;
#42917=CARTESIAN_POINT ( 'NONE',  ( 45.00000000000000000, 10.69371294336137979, -6.585786437626905077 ) ) ;
#42922=CARTESIAN_POINT ( 'NONE',  ( -9.827790563157511022E-16, 130.4429263765338192, 8.025000000000000355 ) ) ;
#42923=TOROIDAL_SURFACE ( 'NONE', #15995, 26.49999999999999645, 0.5000000000000000000 ) ;
#42924=LINE ( 'NONE', #31966, #45025 ) ;
#42925=STYLED_ITEM ( 'NONE', ( #7559 ), #52940 ) ;
#42930=ORIENTED_EDGE ( 'NONE', *, *, #39228, .T. ) ;
#42937=ORIENTED_EDGE ( 'NONE', *, *, #8602, .T. ) ;
#42938=CARTESIAN_POINT ( 'NONE',  ( 5.598654528085809545, 151.1449999999999818, -7.705886871421373741 ) ) ;
#42941=( GEOMETRIC_REPRESENTATION_CONTEXT ( 3 ) GLOBAL_UNCERTAINTY_ASSIGNED_CONTEXT ( ( #16698 ) ) GLOBAL_UNIT_ASSIGNED_CONTEXT ( ( #940, #33391, #54820 ) ) REPRESENTATION_CONTEXT ( 'NONE', 'WORKASPACE' ) );
#42945=CARTESIAN_POINT ( 'NONE',  ( 15.48999599679679662, 118.4999999999999716, -9.500000000000000000 ) ) ;
#42947=CARTESIAN_POINT ( 'NONE',  ( -9.827790563157511022E-16, 130.4429263765338192, 8.025000000000000355 ) ) ;
#42949=VECTOR ( 'NONE', #57079, 1000.000000000000000 ) ;
#42951=ORIENTED_EDGE ( 'NONE', *, *, #36353, .T. ) ;
#42956=CARTESIAN_POINT ( 'NONE',  ( -44.50000000000000000, 99.99999999999992895, 3.500000000000000000 ) ) ;
#42958=COLOUR_RGB ( '', 0.08235294, 0.09019608, 0.10196078) ;
#42960=CARTESIAN_POINT ( 'NONE',  ( 34.99999999999992895, 112.9999999999999858, 7.500000000000000000 ) ) ;
#42961=DIRECTION ( 'NONE',  ( -1.000000000000000000, 0.000000000000000000, 0.000000000000000000 ) ) ;
#42964=VECTOR ( 'NONE', #50815, 1000.000000000000000 ) ;
#42966=EDGE_CURVE ( 'NONE', #31846, #62231, #10084, .T. ) ;
#42969=ORIENTED_EDGE ( 'NONE', *, *, #61057, .F. ) ;
#42974=DIRECTION ( 'NONE',  ( 0.000000000000000000, 1.000000000000000000, -0.000000000000000000 ) ) ;
#42976=DIRECTION ( 'NONE',  ( 0.000000000000000000, 0.000000000000000000, -1.000000000000000000 ) ) ;
#42978=AXIS2_PLACEMENT_3D ( 'NONE', #66241, #21006, #22654 ) ;
#42979=DIRECTION ( 'NONE',  ( 0.000000000000000000, 0.000000000000000000, 1.000000000000000000 ) ) ;
#42981=VERTEX_POINT ( 'NONE', #41661 ) ;
#42987=CARTESIAN_POINT ( 'NONE',  ( -3.094860106618432471, 154.5949999999999704, -9.525000000000000355 ) ) ;
#42990=CARTESIAN_POINT ( 'NONE',  ( -4.716976649647098618, 113.2570736234661553, 6.492361379858953008 ) ) ;
#42992=DIRECTION ( 'NONE',  ( -0.000000000000000000, -0.000000000000000000, -1.000000000000000000 ) ) ;
#42993=EDGE_CURVE ( 'NONE', #8709, #20853, #41536, .T. ) ;
#42995=CARTESIAN_POINT ( 'NONE',  ( -74.50000000000000000, -2.220952357103124925E-14, 6.500000000000000000 ) ) ;
#43003=ORIENTED_EDGE ( 'NONE', *, *, #66733, .T. ) ;
#43010=DIRECTION ( 'NONE',  ( 1.000000000000000000, -1.156482317317873451E-16, 0.000000000000000000 ) ) ;
#43011=DIRECTION ( 'NONE',  ( -0.000000000000000000, 1.000000000000000000, 0.000000000000000000 ) ) ;
#43014=FACE_OUTER_BOUND ( 'NONE', #44947, .T. ) ;
#43021=( NAMED_UNIT ( * ) SI_UNIT ( $, .STERADIAN. ) SOLID_ANGLE_UNIT ( ) );
#43022=FILL_AREA_STYLE_COLOUR ( '', #38881 ) ;
#43024=ORIENTED_EDGE ( 'NONE', *, *, #4513, .F. ) ;
#43027=CARTESIAN_POINT ( 'NONE',  ( 3.094860106618431583, 117.0949999999999989, 9.525000000000000355 ) ) ;
#43028=( NAMED_UNIT ( * ) SI_UNIT ( $, .STERADIAN. ) SOLID_ANGLE_UNIT ( ) );
#43030=CARTESIAN_POINT ( 'NONE',  ( -40.99999999999998579, 107.7459666924148394, -3.000000000000000444 ) ) ;
#43031=CARTESIAN_POINT ( 'NONE',  ( -3.094860106618432471, 128.7049999999999841, -9.525000000000000355 ) ) ;
#43032=ADVANCED_FACE ( 'NONE', ( #38124 ), #15718, .T. ) ;
#43035=CARTESIAN_POINT ( 'NONE',  ( -41.21690152797611262, 107.8360404011451834, -3.444195824416889096 ) ) ;
#43037=CARTESIAN_POINT ( 'NONE',  ( -8.102448949553181734, 147.0049999999999955, -5.886773742842749790 ) ) ;
#43041=( NAMED_UNIT ( * ) PLANE_ANGLE_UNIT ( ) SI_UNIT ( $, .RADIAN. ) );
#43042=STYLED_ITEM ( 'NONE', ( #63170 ), #19408 ) ;
#43043=( NAMED_UNIT ( * ) SI_UNIT ( $, .STERADIAN. ) SOLID_ANGLE_UNIT ( ) );
#43050=STYLED_ITEM ( 'NONE', ( #66685 ), #252 ) ;
#43051=( NAMED_UNIT ( * ) SI_UNIT ( $, .STERADIAN. ) SOLID_ANGLE_UNIT ( ) );
#43052=FILL_AREA_STYLE ('',( #37779 ) ) ;
#43053=( BOUNDED_CURVE ( )  B_SPLINE_CURVE ( 2, ( #11110, #12147, #43872, #33614, #60001, #59281, #26916, #33281, #48806, #32229, #28308 ),
 .UNSPECIFIED., .F., .F. ) 
 B_SPLINE_CURVE_WITH_KNOTS ( ( 3, 2, 2, 2, 2, 3 ),
 ( 0.5588235294117649410, 0.5647058823529413907, 0.5705882352941178404, 0.5764705882352942901, 0.5823529411764708508, 0.5882352941176473005 ),
 .UNSPECIFIED. ) 
 CURVE ( )  GEOMETRIC_REPRESENTATION_ITEM ( )  RATIONAL_B_SPLINE_CURVE ( ( 0.9999999999999981126, 0.9510565162951554186, 1.000000000000000000, 0.9510565162951535312, 1.000000000000000000, 0.9510565162951535312, 1.000000000000000000, 0.9510565162951535312, 1.000000000000000000, 0.9510565162951516438, 1.000000000000001776 ) ) 
 REPRESENTATION_ITEM ( '' )  );
#43061=( NAMED_UNIT ( * ) SI_UNIT ( $, .STERADIAN. ) SOLID_ANGLE_UNIT ( ) );
#43065=CARTESIAN_POINT ( 'NONE',  ( 7.632228543268607446, 144.1570736234661751, 2.479861379858954606 ) ) ;
#43066=SURFACE_SIDE_STYLE ('',( #43421 ) ) ;
#43073=FILL_AREA_STYLE ('',( #37798 ) ) ;
#43075=CARTESIAN_POINT ( 'NONE',  ( -1.166476076187854022E-15, 122.9449999999999790, 9.525000000000000355 ) ) ;
#43079=CYLINDRICAL_SURFACE ( 'NONE', #943, 8.025000000000000355 ) ;
#43086=STYLED_ITEM ( 'NONE', ( #38419 ), #29449 ) ;
#43089=SURFACE_STYLE_USAGE ( .BOTH. , #42052 ) ;
#43090=ORIENTED_EDGE ( 'NONE', *, *, #36594, .T. ) ;
#43093=( NAMED_UNIT ( * ) PLANE_ANGLE_UNIT ( ) SI_UNIT ( $, .RADIAN. ) );
#43097=CARTESIAN_POINT ( 'NONE',  ( 0.000000000000000000, 125.9429263765338192, -8.025000000000000355 ) ) ;
#43099=EDGE_CURVE ( 'NONE', #52924, #43736, #27501, .T. ) ;
#43100=VERTEX_POINT ( 'NONE', #26795 ) ;
#43105=MECHANICAL_DESIGN_GEOMETRIC_PRESENTATION_REPRESENTATION('',(#54287),#26220);
#43106=FILL_AREA_STYLE ('',( #6445 ) ) ;
#43107=CARTESIAN_POINT ( 'NONE',  ( 4.716976649647099507, 147.7570736234661695, -6.492361379858953008 ) ) ;
#43109=ORIENTED_EDGE ( 'NONE', *, *, #68830, .T. ) ;
#43115=CIRCLE ( 'NONE', #53229, 1.000000000000000888 ) ;
#43116=DIRECTION ( 'NONE',  ( 1.000000000000000000, 0.000000000000000000, 0.000000000000000000 ) ) ;
#43117=FILL_AREA_STYLE_COLOUR ( '', #17638 ) ;
#43123=ORIENTED_EDGE ( 'NONE', *, *, #68968, .F. ) ;
#43125=PRESENTATION_STYLE_ASSIGNMENT (( #20579 ) ) ;
#43128=( NAMED_UNIT ( * ) SI_UNIT ( $, .STERADIAN. ) SOLID_ANGLE_UNIT ( ) );
#43129=SURFACE_STYLE_USAGE ( .BOTH. , #21613 ) ;
#43132=( GEOMETRIC_REPRESENTATION_CONTEXT ( 3 ) GLOBAL_UNCERTAINTY_ASSIGNED_CONTEXT ( ( #29288 ) ) GLOBAL_UNIT_ASSIGNED_CONTEXT ( ( #66486, #61884, #44726 ) ) REPRESENTATION_CONTEXT ( 'NONE', 'WORKASPACE' ) );
#43137=SURFACE_STYLE_USAGE ( .BOTH. , #43490 ) ;
#43140=DIRECTION ( 'NONE',  ( -0.000000000000000000, 1.000000000000000000, -0.000000000000000000 ) ) ;
#43141=CARTESIAN_POINT ( 'NONE',  ( -74.99999999999998579, 50.00000000000000000, -6.500000000000000000 ) ) ;
#43144=CARTESIAN_POINT ( 'NONE',  ( -1.166476076187854022E-15, 131.9449999999999932, 9.525000000000000355 ) ) ;
#43146=MECHANICAL_DESIGN_GEOMETRIC_PRESENTATION_REPRESENTATION('',(#58808),#27340);
#43148=FILL_AREA_STYLE ('',( #54674 ) ) ;
#43150=FILL_AREA_STYLE ('',( #16401 ) ) ;
#43157=CARTESIAN_POINT ( 'NONE',  ( -34.99999999999992184, 110.4999999999999858, -9.500000000000000000 ) ) ;
#43159=MECHANICAL_DESIGN_GEOMETRIC_PRESENTATION_REPRESENTATION('',(#361),#39775);
#43160=CIRCLE ( 'NONE', #30730, 0.5000000000000004441 ) ;
#43163=CARTESIAN_POINT ( 'NONE',  ( 45.65811388296465623, 10.21937129432153135, -3.824795692829479954 ) ) ;
#43164=AXIS2_PLACEMENT_3D ( 'NONE', #24303, #7775, #66533 ) ;
#43165=DIRECTION ( 'NONE',  ( 0.000000000000000000, -0.7071067811865469066, -0.7071067811865482389 ) ) ;
#43168=UNCERTAINTY_MEASURE_WITH_UNIT (LENGTH_MEASURE( 1.000000000000000082E-05 ), #37204, 'distance_accuracy_value', 'NONE');
#43170=( LENGTH_UNIT ( ) NAMED_UNIT ( * ) SI_UNIT ( .MILLI., .METRE. ) );
#43174=PRESENTATION_STYLE_ASSIGNMENT (( #64905 ) ) ;
#43179=( BOUNDED_CURVE ( )  B_SPLINE_CURVE ( 3, ( #4723, #5395, #26835, #48374 ),
 .UNSPECIFIED., .F., .F. ) 
 B_SPLINE_CURVE_WITH_KNOTS ( ( 4, 4 ),
 ( 0.000000000000000000, 1.570796326794896558 ),
 .UNSPECIFIED. ) 
 CURVE ( )  GEOMETRIC_REPRESENTATION_ITEM ( )  RATIONAL_B_SPLINE_CURVE ( ( 1.000000000000000000, 0.8047378541243649375, 0.8047378541243649375, 1.000000000000000000 ) ) 
 REPRESENTATION_ITEM ( '' )  );
#43180=STYLED_ITEM ( 'NONE', ( #41242 ), #31349 ) ;
#43184=AXIS2_PLACEMENT_3D ( 'NONE', #7994, #67089, #39348 ) ;
#43185=CARTESIAN_POINT ( 'NONE',  ( -71.50000000000000000, 14.49137674618942562, 9.500000000000000000 ) ) ;
#43187=LINE ( 'NONE', #37907, #46506 ) ;
#43189=VERTEX_POINT ( 'NONE', #1425 ) ;
#43190=AXIS2_PLACEMENT_3D ( 'NONE', #34833, #18333, #8477 ) ;
#43192=CARTESIAN_POINT ( 'NONE',  ( 8.437984349512095861, 117.3070736234661666, 1.550032578732817026E-15 ) ) ;
#43193=STYLED_ITEM ( 'NONE', ( #26880 ), #26973 ) ;
#43194=ADVANCED_FACE ( 'NONE', ( #39856 ), #61579, .T. ) ;
#43195=CARTESIAN_POINT ( 'NONE',  ( -19.98198699191933869, 115.0278726071232711, 9.999999999996266098 ) ) ;
#43196=CARTESIAN_POINT ( 'NONE',  ( 75.00000000000000000, 20.22733879051553885, -6.503618960537654203 ) ) ;
#43198=ORIENTED_EDGE ( 'NONE', *, *, #52814, .T. ) ;
#43202=CARTESIAN_POINT ( 'NONE',  ( 0.000000000000000000, 154.4999999999999432, 0.000000000000000000 ) ) ;
#43204=ORIENTED_EDGE ( 'NONE', *, *, #23461, .T. ) ;
#43205=CARTESIAN_POINT ( 'NONE',  ( -9.058813317711337021, 126.1549999999999869, -2.943386871421374895 ) ) ;
#43207=COLOUR_RGB ( '', 0.72549020, 0.75294118, 0.79215686) ;
#43210=ORIENTED_EDGE ( 'NONE', *, *, #47280, .T. ) ;
#43212=CYLINDRICAL_SURFACE ( 'NONE', #37468, 0.5000000000000004441 ) ;
#43216=( NAMED_UNIT ( * ) PLANE_ANGLE_UNIT ( ) SI_UNIT ( $, .RADIAN. ) );
#43217=AXIS2_PLACEMENT_3D ( 'NONE', #37648, #30921, #47511 ) ;
#43219=CARTESIAN_POINT ( 'NONE',  ( 20.30219483484659548, 114.9087424184428130, -10.36565267485733877 ) ) ;
#43225=CYLINDRICAL_SURFACE ( 'NONE', #67967, 15.00000000000000000 ) ;
#43228=CARTESIAN_POINT ( 'NONE',  ( -54.49999999999999289, -2.024042244987997205E-14, -6.500000000000000000 ) ) ;
#43230=CARTESIAN_POINT ( 'NONE',  ( -5.461490429277642278, 153.8976665511306692, 7.076668351203482032 ) ) ;
#43231=ORIENTED_EDGE ( 'NONE', *, *, #61166, .F. ) ;
#43232=ORIENTED_EDGE ( 'NONE', *, *, #35156, .F. ) ;
#43234=DIRECTION ( 'NONE',  ( -0.000000000000000000, -1.000000000000000000, 0.000000000000000000 ) ) ;
#43235=DIRECTION ( 'NONE',  ( -0.000000000000000000, -0.000000000000000000, 1.000000000000000000 ) ) ;
#43236=AXIS2_PLACEMENT_3D ( 'NONE', #61613, #13442, #2851 ) ;
#43239=CARTESIAN_POINT ( 'NONE',  ( 0.000000000000000000, 154.9999999999999716, -22.49999999999999645 ) ) ;
#43243=ORIENTED_EDGE ( 'NONE', *, *, #4942, .F. ) ;
#43244=PRESENTATION_STYLE_ASSIGNMENT (( #65676 ) ) ;
#43245=AXIS2_PLACEMENT_3D ( 'NONE', #57619, #24895, #18915 ) ;
#43247=CARTESIAN_POINT ( 'NONE',  ( -4.716976649647097730, 150.2429263765338021, -6.492361379858953896 ) ) ;
#43250=FILL_AREA_STYLE ('',( #37273 ) ) ;
#43251=CARTESIAN_POINT ( 'NONE',  ( -75.00000000000000000, 35.50862325239523898, -9.539713813943809129 ) ) ;
#43254=CARTESIAN_POINT ( 'NONE',  ( -5.598654528085808657, 135.7549999999999955, 7.705886871421373741 ) ) ;
#43259=UNCERTAINTY_MEASURE_WITH_UNIT (LENGTH_MEASURE( 1.000000000000000082E-05 ), #62247, 'distance_accuracy_value', 'NONE');
#43260=EDGE_CURVE ( 'NONE', #33694, #46319, #9564, .T. ) ;
#43261=SURFACE_STYLE_USAGE ( .BOTH. , #64305 ) ;
#43266=EDGE_CURVE ( 'NONE', #38501, #50095, #38085, .T. ) ;
#43269=EDGE_CURVE ( 'NONE', #631, #3378, #11065, .T. ) ;
#43270=EDGE_CURVE ( 'NONE', #46307, #34430, #16233, .T. ) ;
#43275=ORIENTED_EDGE ( 'NONE', *, *, #54397, .T. ) ;
#43276=FACE_OUTER_BOUND ( 'NONE', #34591, .T. ) ;
#43277=AXIS2_PLACEMENT_3D ( 'NONE', #38554, #49093, #65226 ) ;
#43279=CARTESIAN_POINT ( 'NONE',  ( -34.99999999999992895, 113.4999999999999858, -7.500000000000000000 ) ) ;
#43282=DIRECTION ( 'NONE',  ( 0.000000000000000000, 1.000000000000000000, -0.000000000000000000 ) ) ;
#43289=CARTESIAN_POINT ( 'NONE',  ( 0.000000000000000000, 152.9999999999999716, 8.025000000000000355 ) ) ;
#43290=CARTESIAN_POINT ( 'NONE',  ( -15.98999599679679839, 118.4999999999999716, -9.500000000000000000 ) ) ;
#43291=ORIENTED_EDGE ( 'NONE', *, *, #13330, .F. ) ;
#43292=CARTESIAN_POINT ( 'NONE',  ( 74.99999999999998579, 50.00000000000000000, 10.00000000000000000 ) ) ;
#43295=( LENGTH_UNIT ( ) NAMED_UNIT ( * ) SI_UNIT ( .MILLI., .METRE. ) );
#43296=CARTESIAN_POINT ( 'NONE',  ( 5.598654528085809545, 160.1449999999999818, -7.705886871421373741 ) ) ;
#43299=ORIENTED_EDGE ( 'NONE', *, *, #1916, .F. ) ;
#43300=STYLED_ITEM ( 'NONE', ( #8413 ), #8233 ) ;
#43302=SURFACE_SIDE_STYLE ('',( #5933 ) ) ;
#43303=CARTESIAN_POINT ( 'NONE',  ( 0.000000000000000000, 87.30187232391182306, 8.025000000000000355 ) ) ;
#43305=ORIENTED_EDGE ( 'NONE', *, *, #4913, .T. ) ;
#43306=CARTESIAN_POINT ( 'NONE',  ( -7.632228543268607446, 123.5429263765338135, -2.479861379858953718 ) ) ;
#43311=CARTESIAN_POINT ( 'NONE',  ( 4.716976649647096842, 124.7429263765338163, 6.492361379858953896 ) ) ;
#43316=( GEOMETRIC_REPRESENTATION_CONTEXT ( 3 ) GLOBAL_UNCERTAINTY_ASSIGNED_CONTEXT ( ( #17856 ) ) GLOBAL_UNIT_ASSIGNED_CONTEXT ( ( #56252, #67166, #28825 ) ) REPRESENTATION_CONTEXT ( 'NONE', 'WORKASPACE' ) );
#43318=DIRECTION ( 'NONE',  ( 1.000000000000000000, 0.000000000000000000, 0.000000000000000000 ) ) ;
#43321=CARTESIAN_POINT ( 'NONE',  ( -72.00000000000000000, 35.92875272052971525, -7.000000000000000000 ) ) ;
#43322=UNCERTAINTY_MEASURE_WITH_UNIT (LENGTH_MEASURE( 1.000000000000000082E-05 ), #26400, 'distance_accuracy_value', 'NONE');
#43323=ADVANCED_FACE ( 'NONE', ( #11260 ), #10921, .F. ) ;
#43324=CARTESIAN_POINT ( 'NONE',  ( -7.632228543268607446, 115.6570736234661467, -2.479861379858953718 ) ) ;
#43325=FILL_AREA_STYLE ('',( #54145 ) ) ;
#43326=ORIENTED_EDGE ( 'NONE', *, *, #16727, .T. ) ;
#43328=CARTESIAN_POINT ( 'NONE',  ( -45.00000000000000000, 8.062885781073935831, 3.611004237778676185 ) ) ;
#43332=DIRECTION ( 'NONE',  ( 0.000000000000000000, 1.000000000000000000, -0.000000000000000000 ) ) ;
#43343=CYLINDRICAL_SURFACE ( 'NONE', #32536, 5.000000000000004441 ) ;
#43344=CARTESIAN_POINT ( 'NONE',  ( -15.48999599679679662, 146.9999999999999716, -7.000000000000000000 ) ) ;
#43347=CARTESIAN_POINT ( 'NONE',  ( 3.094860106618431583, 159.0949999999999420, 9.525000000000000355 ) ) ;
#43352=UNCERTAINTY_MEASURE_WITH_UNIT (LENGTH_MEASURE( 1.000000000000000082E-05 ), #53743, 'distance_accuracy_value', 'NONE');
#43353=EDGE_CURVE ( 'NONE', #18998, #18360, #15876, .T. ) ;
#43354=STYLED_ITEM ( 'NONE', ( #53557 ), #27838 ) ;
#43356=SURFACE_STYLE_FILL_AREA ( #48957 ) ;
#43357=AXIS2_PLACEMENT_3D ( 'NONE', #35825, #57990, #26294 ) ;
#43363=ADVANCED_FACE ( 'NONE', ( #53816 ), #7705, .F. ) ;
#43371=DIRECTION ( 'NONE',  ( 1.000000000000000000, 0.000000000000000000, 0.000000000000000000 ) ) ;
#43372=CARTESIAN_POINT ( 'NONE',  ( -45.00000000000000000, 9.484039020261588959, 6.483595844450460888 ) ) ;
#43375=ORIENTED_EDGE ( 'NONE', *, *, #5219, .F. ) ;
#43378=AXIS2_PLACEMENT_3D ( 'NONE', #41523, #67538, #19695 ) ;
#43382=COLOUR_RGB ( '', 0.31764706, 0.68627451, 0.89019608) ;
#43384=CARTESIAN_POINT ( 'NONE',  ( 9.058813317711337021, 126.5449999999999875, 2.943386871421375783 ) ) ;
#43389=CARTESIAN_POINT ( 'NONE',  ( 0.000000000000000000, 134.5549999999999784, -9.525000000000000355 ) ) ;
#43391=AXIS2_PLACEMENT_3D ( 'NONE', #65522, #33510, #50061 ) ;
#43393=DIRECTION ( 'NONE',  ( 1.000000000000000000, -0.000000000000000000, 0.000000000000000000 ) ) ;
#43395=CARTESIAN_POINT ( 'NONE',  ( -8.102448949553181734, 144.0050000000000239, -5.886773742842749790 ) ) ;
#43398=FILL_AREA_STYLE_COLOUR ( '', #53548 ) ;
#43400=SURFACE_STYLE_FILL_AREA ( #5334 ) ;
#43408=CARTESIAN_POINT ( 'NONE',  ( 0.000000000000000000, 114.9999999999999574, 0.000000000000000000 ) ) ;
#43414=FILL_AREA_STYLE_COLOUR ( '', #13648 ) ;
#43415=CYLINDRICAL_SURFACE ( 'NONE', #16737, 0.5000000000000004441 ) ;
#43418=CARTESIAN_POINT ( 'NONE',  ( -34.99999999999992895, 112.4999999999999858, 10.00000000000000000 ) ) ;
#43419=CARTESIAN_POINT ( 'NONE',  ( -2.607480562269064439, 112.2929263765338135, 8.025000000000007461 ) ) ;
#43420=DIRECTION ( 'NONE',  ( -0.000000000000000000, -0.000000000000000000, -1.000000000000000000 ) ) ;
#43421=SURFACE_STYLE_FILL_AREA ( #38813 ) ;
#43426=FILL_AREA_STYLE_COLOUR ( '', #38123 ) ;
#43433=CARTESIAN_POINT ( 'NONE',  ( 9.058813317711338797, 132.8449999999999989, -2.943386871421372675 ) ) ;
#43439=ADVANCED_FACE ( 'NONE', ( #60145 ), #50291, .F. ) ;
#43443=CARTESIAN_POINT ( 'NONE',  ( -2.607480562269032021, 148.2070736234661581, -8.025000000000032330 ) ) ;
#43447=CARTESIAN_POINT ( 'NONE',  ( 71.49999999999998579, 64.07124727947029896, -7.500000000000000000 ) ) ;
#43448=EDGE_LOOP ( 'NONE', ( #26818, #22207, #6905, #55536 ) ) ;
#43451=CARTESIAN_POINT ( 'NONE',  ( 24.21231517720798010, 113.4999999999999858, 9.500000000000000000 ) ) ;
#43452=AXIS2_PLACEMENT_3D ( 'NONE', #44866, #38902, #66273 ) ;
#43454=CARTESIAN_POINT ( 'NONE',  ( -75.48275862068965125, 63.99167409976910648, -9.500000000000001776 ) ) ;
#43460=ORIENTED_EDGE ( 'NONE', *, *, #10823, .F. ) ;
#43461=CARTESIAN_POINT ( 'NONE',  ( 34.99999999999992895, 112.4999999999999858, 10.00000000000000000 ) ) ;
#43465=CARTESIAN_POINT ( 'NONE',  ( -2.607480562269075097, 143.4070736234661751, 8.025000000000000355 ) ) ;
#43466=ORIENTED_EDGE ( 'NONE', *, *, #29852, .T. ) ;
#43470=EDGE_LOOP ( 'NONE', ( #62688, #9705, #23860, #17447 ) ) ;
#43471=DIRECTION ( 'NONE',  ( 0.000000000000000000, 0.000000000000000000, 1.000000000000000000 ) ) ;
#43472=AXIS2_PLACEMENT_3D ( 'NONE', #23405, #45942, #18145 ) ;
#43473=SURFACE_SIDE_STYLE ('',( #28931 ) ) ;
#43480=CARTESIAN_POINT ( 'NONE',  ( 48.00000000000000000, 13.41640786499872284, -7.000000000000000000 ) ) ;
#43483=ORIENTED_EDGE ( 'NONE', *, *, #43801, .F. ) ;
#43490=SURFACE_SIDE_STYLE ('',( #5768 ) ) ;
#43491=SURFACE_STYLE_FILL_AREA ( #6143 ) ;
#43492=DIRECTION ( 'NONE',  ( -1.000000000000000000, 0.000000000000000000, 0.000000000000000000 ) ) ;
#43493=SURFACE_STYLE_FILL_AREA ( #38891 ) ;
#43495=CARTESIAN_POINT ( 'NONE',  ( 0.000000000000000000, 136.4449999999999932, -9.525000000000000355 ) ) ;
#43498=CARTESIAN_POINT ( 'NONE',  ( 23.71231517720798010, 117.9999999999999716, -9.500000000000000000 ) ) ;
#43501=EDGE_CURVE ( 'NONE', #48146, #68819, #21307, .T. ) ;
#43505=AXIS2_PLACEMENT_3D ( 'NONE', #2078, #40166, #61561 ) ;
#43510=CARTESIAN_POINT ( 'NONE',  ( 45.65811388300841855, 10.21937129433612057, -4.000000000000003553 ) ) ;
#43511=( NAMED_UNIT ( * ) PLANE_ANGLE_UNIT ( ) SI_UNIT ( $, .RADIAN. ) );
#43516=EDGE_CURVE ( 'NONE', #5028, #45388, #19292, .T. ) ;
#43520=SURFACE_SIDE_STYLE ('',( #6171 ) ) ;
#43524=SURFACE_STYLE_USAGE ( .BOTH. , #489 ) ;
#43529=EDGE_CURVE ( 'NONE', #26425, #18324, #14741, .T. ) ;
#43530=VERTEX_POINT ( 'NONE', #8760 ) ;
#43531=SURFACE_SIDE_STYLE ('',( #498 ) ) ;
#43534=ADVANCED_FACE ( 'NONE', ( #35841 ), #67151, .T. ) ;
#43535=CARTESIAN_POINT ( 'NONE',  ( 6.826472737025121695, 111.6070736234661354, -4.959722759717905660 ) ) ;
#43541=CARTESIAN_POINT ( 'NONE',  ( -34.99999999999999289, 99.99999999999998579, -7.500000000000000000 ) ) ;
#43542=CARTESIAN_POINT ( 'NONE',  ( -75.50000000000000000, 35.50862325381056905, -6.499999999999999112 ) ) ;
#43543=ORIENTED_EDGE ( 'NONE', *, *, #37320, .T. ) ;
#43550=CARTESIAN_POINT ( 'NONE',  ( 24.21231517720798010, 113.4999999999999858, -10.00000000000000000 ) ) ;
#43551=SURFACE_STYLE_FILL_AREA ( #520 ) ;
#43552=DIRECTION ( 'NONE',  ( 1.000000000000000000, 0.000000000000000000, 0.000000000000000000 ) ) ;
#43554=CARTESIAN_POINT ( 'NONE',  ( -6.826472737025120807, 159.9929263765338021, 4.959722759717906548 ) ) ;
#43555=B_SPLINE_CURVE_WITH_KNOTS ( 'NONE', 3,
 ( #32998, #890, #1618, #65689, #65343, #28371, #39680, #23459, #49188, #66374, #33675, #22434, #49530, #66029 ),
 .UNSPECIFIED., .F., .F.,
 ( 4, 2, 2, 2, 2, 2, 4 ),
 ( 1.226634733346699349E-18, 0.002172676916775652042, 0.003259015375163478497, 0.004345353833551304952, 0.005431692291939130973, 0.006518030750326958729, 0.008690707667102608169 ),
 .UNSPECIFIED. ) ;
#43556=CARTESIAN_POINT ( 'NONE',  ( -24.21231517720798010, 112.9999999999999858, -9.500000000000000000 ) ) ;
#43560=ADVANCED_FACE ( 'NONE', ( #40797 ), #27910, .T. ) ;
#43568=CARTESIAN_POINT ( 'NONE',  ( -3.648904307674157188, 153.9880311262221824, 8.259051035474737290 ) ) ;
#43570=SURFACE_SIDE_STYLE ('',( #1234 ) ) ;
#43572=ORIENTED_EDGE ( 'NONE', *, *, #68830, .F. ) ;
#43573=SURFACE_STYLE_FILL_AREA ( #546 ) ;
#43577=CARTESIAN_POINT ( 'NONE',  ( 0.000000000000000000, 87.30187232391182306, 0.000000000000000000 ) ) ;
#43580=ORIENTED_EDGE ( 'NONE', *, *, #33826, .F. ) ;
#43581=( NAMED_UNIT ( * ) SI_UNIT ( $, .STERADIAN. ) SOLID_ANGLE_UNIT ( ) );
#43582=CARTESIAN_POINT ( 'NONE',  ( 44.67254323996743182, 10.47540843667325383, 3.522617369932174558 ) ) ;
#43583=CARTESIAN_POINT ( 'NONE',  ( -49.12162162162162105, 13.70805908423323238, 10.00000000000000000 ) ) ;
#43584=FILL_AREA_STYLE ('',( #5887 ) ) ;
#43592=CARTESIAN_POINT ( 'NONE',  ( 0.000000000000000000, 137.5549999999999784, -9.525000000000000355 ) ) ;
#43596=DIRECTION ( 'NONE',  ( 1.000000000000000000, 0.000000000000000000, 0.000000000000000000 ) ) ;
#43598=CARTESIAN_POINT ( 'NONE',  ( -2.607480562269115509, 132.0929263765338249, -8.024999999999970157 ) ) ;
#43599=( NAMED_UNIT ( * ) SI_UNIT ( $, .STERADIAN. ) SOLID_ANGLE_UNIT ( ) );
#43601=COLOUR_RGB ( '', 0.31764706, 0.68627451, 0.89019608) ;
#43602=FILL_AREA_STYLE ('',( #64310 ) ) ;
#43604=VERTEX_POINT ( 'NONE', #25606 ) ;
#43606=CARTESIAN_POINT ( 'NONE',  ( -7.632228543268607446, 135.5429263765338135, -2.479861379858953718 ) ) ;
#43611=VERTEX_POINT ( 'NONE', #10499 ) ;
#43612=( NAMED_UNIT ( * ) PLANE_ANGLE_UNIT ( ) SI_UNIT ( $, .RADIAN. ) );
#43613=( NAMED_UNIT ( * ) SI_UNIT ( $, .STERADIAN. ) SOLID_ANGLE_UNIT ( ) );
#43616=CARTESIAN_POINT ( 'NONE',  ( -60.00000000000000000, -2.024042244987997205E-14, 11.50000000000000000 ) ) ;
#43617=ORIENTED_EDGE ( 'NONE', *, *, #37933, .F. ) ;
#43619=CARTESIAN_POINT ( 'NONE',  ( 8.102448949553181734, 156.3950000000000102, 5.886773742842750679 ) ) ;
#43626=ORIENTED_EDGE ( 'NONE', *, *, #64564, .F. ) ;
#43627=CARTESIAN_POINT ( 'NONE',  ( 7.632228543268608334, 140.3429263765338249, -2.479861379858951942 ) ) ;
#43630=VECTOR ( 'NONE', #26537, 1000.000000000000000 ) ;
#43640=COLOUR_RGB ( '', 0.66274510, 0.83137255, 0.94901961) ;
#43642=SURFACE_SIDE_STYLE ('',( #69631 ) ) ;
#43645=SURFACE_STYLE_FILL_AREA ( #629 ) ;
#43646=CARTESIAN_POINT ( 'NONE',  ( 41.05143861928668514, 107.9622656938502416, 3.673005875158968259 ) ) ;
#43651=LINE ( 'NONE', #7012, #47454 ) ;
#43652=AXIS2_PLACEMENT_3D ( 'NONE', #2332, #29475, #39611 ) ;
#43660=EDGE_CURVE ( 'NONE', #19239, #57600, #58269, .T. ) ;
#43664=EDGE_LOOP ( 'NONE', ( #62877, #62449, #33925, #57310 ) ) ;
#43665=EDGE_CURVE ( 'NONE', #26930, #6265, #48225, .T. ) ;
#43669=LINE ( 'NONE', #60818, #64067 ) ;
#43671=CARTESIAN_POINT ( 'NONE',  ( -3.094860106618434248, 111.9050000000000011, 9.525000000000000355 ) ) ;
#43674=VECTOR ( 'NONE', #28491, 1000.000000000000000 ) ;
#43678=DIRECTION ( 'NONE',  ( 1.224646799147353207E-16, 1.000000000000000000, -0.000000000000000000 ) ) ;
#43680=LINE ( 'NONE', #32042, #43838 ) ;
#43685=( GEOMETRIC_REPRESENTATION_CONTEXT ( 3 ) GLOBAL_UNCERTAINTY_ASSIGNED_CONTEXT ( ( #69172 ) ) GLOBAL_UNIT_ASSIGNED_CONTEXT ( ( #20524, #52557, #47667 ) ) REPRESENTATION_CONTEXT ( 'NONE', 'WORKASPACE' ) );
#43686=CYLINDRICAL_SURFACE ( 'NONE', #1438, 15.00000000000000000 ) ;
#43688=ORIENTED_EDGE ( 'NONE', *, *, #57582, .T. ) ;
#43689=TOROIDAL_SURFACE ( 'NONE', #59379, 1.000000000000000000, 0.5000000000000000000 ) ;
#43692=FILL_AREA_STYLE_COLOUR ( '', #28535 ) ;
#43693=MECHANICAL_DESIGN_GEOMETRIC_PRESENTATION_REPRESENTATION('',(#59337),#23398);
#43695=VECTOR ( 'NONE', #69324, 1000.000000000000000 ) ;
#43696=FILL_AREA_STYLE_COLOUR ( '', #8245 ) ;
#43701=EDGE_LOOP ( 'NONE', ( #3658, #5613, #41548, #8476 ) ) ;
#43703=DIRECTION ( 'NONE',  ( 0.000000000000000000, 0.000000000000000000, 1.000000000000000000 ) ) ;
#43706=CARTESIAN_POINT ( 'NONE',  ( -5.598654528085808657, 128.6449999999999818, 7.705886871421373741 ) ) ;
#43708=ORIENTED_EDGE ( 'NONE', *, *, #28814, .F. ) ;
#43710=CARTESIAN_POINT ( 'NONE',  ( -8.102448949553179958, 129.6049999999999613, 5.886773742842747126 ) ) ;
#43715=CARTESIAN_POINT ( 'NONE',  ( 0.000000000000000000, 158.5550000000000068, -9.525000000000000355 ) ) ;
#43716=LINE ( 'NONE', #33469, #49066 ) ;
#43718=DIRECTION ( 'NONE',  ( 0.6216216216216174928, 0.7833176619561892373, 0.000000000000000000 ) ) ;
#43720=TOROIDAL_SURFACE ( 'NONE', #6584, 14.49999999999999822, 0.5000000000000000000 ) ;
#43721=FILL_AREA_STYLE_COLOUR ( '', #17196 ) ;
#43729=CARTESIAN_POINT ( 'NONE',  ( 24.21231517720798010, 112.4999999999999858, -10.00000000000000000 ) ) ;
#43730=VERTEX_POINT ( 'NONE', #43583 ) ;
#43731=( GEOMETRIC_REPRESENTATION_CONTEXT ( 3 ) GLOBAL_UNCERTAINTY_ASSIGNED_CONTEXT ( ( #61593 ) ) GLOBAL_UNIT_ASSIGNED_CONTEXT ( ( #26895, #6859, #60323 ) ) REPRESENTATION_CONTEXT ( 'NONE', 'WORKASPACE' ) );
#43733=CARTESIAN_POINT ( 'NONE',  ( -45.91547277936962246, 9.430195807687217879, -3.611004237778682402 ) ) ;
#43736=VERTEX_POINT ( 'NONE', #7545 ) ;
#43738=ADVANCED_FACE ( 'NONE', ( #16829 ), #50813, .T. ) ;
#43739=CARTESIAN_POINT ( 'NONE',  ( -21.02379604162863913, 110.4999999999999858, -9.500000000000000000 ) ) ;
#43740=COLOUR_RGB ( '', 0.40784314, 0.44705882, 0.49803922) ;
#43741=CARTESIAN_POINT ( 'NONE',  ( -60.00000000000000000, -2.024042244987997205E-14, 12.00000000000000000 ) ) ;
#43742=( NAMED_UNIT ( * ) PLANE_ANGLE_UNIT ( ) SI_UNIT ( $, .RADIAN. ) );
#43747=EDGE_LOOP ( 'NONE', ( #36116, #34008, #37030, #66571 ) ) ;
#43748=( NAMED_UNIT ( * ) PLANE_ANGLE_UNIT ( ) SI_UNIT ( $, .RADIAN. ) );
#43751=CARTESIAN_POINT ( 'NONE',  ( 8.102448949553183510, 132.9949999999999477, -5.886773742842746238 ) ) ;
#43754=PRESENTATION_STYLE_ASSIGNMENT (( #33837 ) ) ;
#43759=AXIS2_PLACEMENT_3D ( 'NONE', #49423, #16399, #27226 ) ;
#43765=( NAMED_UNIT ( * ) PLANE_ANGLE_UNIT ( ) SI_UNIT ( $, .RADIAN. ) );
#43770=( BOUNDED_CURVE ( )  B_SPLINE_CURVE ( 2, ( #62028, #39936, #34602, #24063, #57106, #35323, #2905, #8248, #13493, #14211, #61338 ),
 .UNSPECIFIED., .F., .F. ) 
 B_SPLINE_CURVE_WITH_KNOTS ( ( 3, 2, 2, 2, 2, 3 ),
 ( 0.2058823529411763498, 0.2117647058823528272, 0.2176470588235293047, 0.2235294117647058099, 0.2294117647058822596, 0.2352941176470587370 ),
 .UNSPECIFIED. ) 
 CURVE ( )  GEOMETRIC_REPRESENTATION_ITEM ( )  RATIONAL_B_SPLINE_CURVE ( ( 1.000000000000000888, 0.9510565162951526430, 1.000000000000000000, 0.9510565162951535312, 1.000000000000000000, 0.9510565162951535312, 1.000000000000000000, 0.9510565162951535312, 1.000000000000000000, 0.9510565162951541973, 0.9999999999999993339 ) ) 
 REPRESENTATION_ITEM ( '' )  );
#43776=CARTESIAN_POINT ( 'NONE',  ( 75.15811388300841145, 19.52565835097472302, 6.000000000000000888 ) ) ;
#43780=( NAMED_UNIT ( * ) PLANE_ANGLE_UNIT ( ) SI_UNIT ( $, .RADIAN. ) );
#43781=CARTESIAN_POINT ( 'NONE',  ( -60.00000000000000000, -2.024042244987997205E-14, -12.00000000000000000 ) ) ;
#43787=CARTESIAN_POINT ( 'NONE',  ( -2.607480562269073765, 157.2070736234661297, -8.025000000000000355 ) ) ;
#43788=ORIENTED_EDGE ( 'NONE', *, *, #59447, .F. ) ;
#43789=SURFACE_STYLE_USAGE ( .BOTH. , #27545 ) ;
#43791=DIRECTION ( 'NONE',  ( -0.000000000000000000, -0.000000000000000000, 1.000000000000000000 ) ) ;
#43799=ORIENTED_EDGE ( 'NONE', *, *, #41743, .F. ) ;
#43800=DIRECTION ( 'NONE',  ( -1.000000000000000000, 0.000000000000000000, 0.000000000000000000 ) ) ;
#43801=EDGE_CURVE ( 'NONE', #49707, #34861, #23722, .T. ) ;
#43802=CARTESIAN_POINT ( 'NONE',  ( -45.00000000000000000, 9.609158271987121580, -6.330303435919273802 ) ) ;
#43807=STYLED_ITEM ( 'NONE', ( #28958 ), #42856 ) ;
#43808=CARTESIAN_POINT ( 'NONE',  ( 45.00000000000000000, 9.916356254361716083, -6.999999999944073181 ) ) ;
#43809=CARTESIAN_POINT ( 'NONE',  ( -44.99999999999998579, 119.9999999999999716, 7.500000000000000000 ) ) ;
#43816=FILL_AREA_STYLE ('',( #22673 ) ) ;
#43817=DIRECTION ( 'NONE',  ( 0.000000000000000000, 0.000000000000000000, 1.000000000000000000 ) ) ;
#43821=CARTESIAN_POINT ( 'NONE',  ( 5.598654528085809545, 133.1449999999999818, -7.705886871421373741 ) ) ;
#43824=( GEOMETRIC_REPRESENTATION_CONTEXT ( 3 ) GLOBAL_UNCERTAINTY_ASSIGNED_CONTEXT ( ( #48213 ) ) GLOBAL_UNIT_ASSIGNED_CONTEXT ( ( #86, #48396, #58563 ) ) REPRESENTATION_CONTEXT ( 'NONE', 'WORKASPACE' ) );
#43825=EDGE_CURVE ( 'NONE', #26176, #16496, #39944, .T. ) ;
#43826=( LENGTH_UNIT ( ) NAMED_UNIT ( * ) SI_UNIT ( .MILLI., .METRE. ) );
#43829=LINE ( 'NONE', #11776, #13287 ) ;
#43830=LINE ( 'NONE', #5431, #63567 ) ;
#43837=ORIENTED_EDGE ( 'NONE', *, *, #31759, .F. ) ;
#43838=VECTOR ( 'NONE', #53506, 1000.000000000000000 ) ;
#43839=PLANE ( 'NONE',  #61668 ) ;
#43840=FILL_AREA_STYLE_COLOUR ( '', #28913 ) ;
#43843=FILL_AREA_STYLE ('',( #39603 ) ) ;
#43847=PRESENTATION_STYLE_ASSIGNMENT (( #27602 ) ) ;
#43848=PRESENTATION_STYLE_ASSIGNMENT (( #38586 ) ) ;
#43854=CARTESIAN_POINT ( 'NONE',  ( 0.000000000000000000, 111.9999999999999858, 0.000000000000000000 ) ) ;
#43855=EDGE_CURVE ( 'NONE', #32455, #4040, #557, .T. ) ;
#43857=DIRECTION ( 'NONE',  ( 1.000000000000000000, 0.000000000000000000, 0.000000000000000000 ) ) ;
#43858=FACE_OUTER_BOUND ( 'NONE', #30501, .T. ) ;
#43865=CARTESIAN_POINT ( 'NONE',  ( -45.50000000000000711, 9.708372675170615196, 6.000000000000000888 ) ) ;
#43867=CARTESIAN_POINT ( 'NONE',  ( 6.826472737025121695, 126.6070736234661638, -4.959722759717905660 ) ) ;
#43869=EDGE_CURVE ( 'NONE', #32404, #60894, #69512, .T. ) ;
#43872=CARTESIAN_POINT ( 'NONE',  ( 4.716976649647096842, 137.8570736234661638, 6.492361379858953896 ) ) ;
#43875=ORIENTED_EDGE ( 'NONE', *, *, #68314, .T. ) ;
#43876=CARTESIAN_POINT ( 'NONE',  ( 71.49999999999998579, 119.9999999999997868, 7.000000000000000000 ) ) ;
#43879=ORIENTED_EDGE ( 'NONE', *, *, #48241, .F. ) ;
#43882=DIRECTION ( 'NONE',  ( 1.000000000000000000, -0.000000000000000000, 0.000000000000000000 ) ) ;
#43883=VECTOR ( 'NONE', #67172, 1000.000000000000000 ) ;
#43884=CARTESIAN_POINT ( 'NONE',  ( 7.632228543268608334, 149.3429263765338249, -2.479861379858951942 ) ) ;
#43889=CARTESIAN_POINT ( 'NONE',  ( 45.00000000000000000, 9.801220280675936536, 6.455927277201578107 ) ) ;
#43890=EDGE_CURVE ( 'NONE', #25427, #45842, #11169, .T. ) ;
#43895=EDGE_CURVE ( 'NONE', #60834, #5568, #66645, .T. ) ;
#43900=DIRECTION ( 'NONE',  ( 0.000000000000000000, 0.000000000000000000, 1.000000000000000000 ) ) ;
#43902=LINE ( 'NONE', #69543, #15086 ) ;
#43904=CARTESIAN_POINT ( 'NONE',  ( 60.00000000000000000, 1.797044900979284448E-15, 10.00000000000000000 ) ) ;
#43907=PRESENTATION_STYLE_ASSIGNMENT (( #54738 ) ) ;
#43909=ORIENTED_EDGE ( 'NONE', *, *, #58232, .F. ) ;
#43910=CARTESIAN_POINT ( 'NONE',  ( 48.50000000000000000, 14.49137674618942562, 7.500000000000000000 ) ) ;
#43911=FILL_AREA_STYLE ('',( #11854 ) ) ;
#43912=FILL_AREA_STYLE_COLOUR ( '', #41059 ) ;
#43913=ORIENTED_EDGE ( 'NONE', *, *, #39982, .T. ) ;
#43917=MECHANICAL_DESIGN_GEOMETRIC_PRESENTATION_REPRESENTATION('',(#29294),#4540);
#43922=CYLINDRICAL_SURFACE ( 'NONE', #30192, 8.025000000000000355 ) ;
#43923=FACE_OUTER_BOUND ( 'NONE', #42740, .T. ) ;
#43924=( LENGTH_UNIT ( ) NAMED_UNIT ( * ) SI_UNIT ( .MILLI., .METRE. ) );
#43930=CARTESIAN_POINT ( 'NONE',  ( 8.102448949553183510, 140.1049999999999898, -5.886773742842746238 ) ) ;
#43932=UNCERTAINTY_MEASURE_WITH_UNIT (LENGTH_MEASURE( 1.000000000000000082E-05 ), #17754, 'distance_accuracy_value', 'NONE');
#43935=CARTESIAN_POINT ( 'NONE',  ( -24.21231517720798010, 112.4999999999999858, 9.500000000000000000 ) ) ;
#43940=ADVANCED_FACE ( 'NONE', ( #66995 ), #29119, .T. ) ;
#43941=DIRECTION ( 'NONE',  ( 1.000000000000000000, 0.000000000000000000, 0.000000000000000000 ) ) ;
#43942=CARTESIAN_POINT ( 'NONE',  ( -6.826472737025120807, 136.5070736234661410, -4.959722759717907437 ) ) ;
#43945=CARTESIAN_POINT ( 'NONE',  ( -2.607480562268991608, 136.2929263765338135, 8.025000000000060751 ) ) ;
#43950=( LENGTH_UNIT ( ) NAMED_UNIT ( * ) SI_UNIT ( .MILLI., .METRE. ) );
#43951=PRESENTATION_STYLE_ASSIGNMENT (( #65709 ) ) ;
#43957=ORIENTED_EDGE ( 'NONE', *, *, #36890, .F. ) ;
#43958=( LENGTH_UNIT ( ) NAMED_UNIT ( * ) SI_UNIT ( .MILLI., .METRE. ) );
#43959=EDGE_CURVE ( 'NONE', #69341, #41724, #20531, .T. ) ;
#43960=VERTEX_POINT ( 'NONE', #47309 ) ;
#43963=ORIENTED_EDGE ( 'NONE', *, *, #64526, .F. ) ;
#43966=CARTESIAN_POINT ( 'NONE',  ( 3.094860106618435136, 157.2949999999999591, -9.525000000000000355 ) ) ;
#43968=ORIENTED_EDGE ( 'NONE', *, *, #53556, .T. ) ;
#43969=AXIS2_PLACEMENT_3D ( 'NONE', #28740, #29439, #66035 ) ;
#43973=DIRECTION ( 'NONE',  ( -0.000000000000000000, -0.000000000000000000, -1.000000000000000000 ) ) ;
#43974=EDGE_LOOP ( 'NONE', ( #39692, #59738, #21717, #9786 ) ) ;
#43975=CARTESIAN_POINT ( 'NONE',  ( -6.826472737025120807, 135.3929263765338362, -4.959722759717907437 ) ) ;
#43982=VECTOR ( 'NONE', #22058, 1000.000000000000000 ) ;
#43985=CARTESIAN_POINT ( 'NONE',  ( 15.48999599679679662, 146.4999999999999716, -9.500000000000000000 ) ) ;
#43989=LINE ( 'NONE', #11936, #23806 ) ;
#43990=UNCERTAINTY_MEASURE_WITH_UNIT (LENGTH_MEASURE( 1.000000000000000082E-05 ), #58330, 'distance_accuracy_value', 'NONE');
#43993=CARTESIAN_POINT ( 'NONE',  ( -6.826472737025120807, 115.5070736234661553, -4.959722759717907437 ) ) ;
#44000=VERTEX_POINT ( 'NONE', #52900 ) ;
#44001=CARTESIAN_POINT ( 'NONE',  ( -45.91409082377983708, 9.428132016590232922, 3.509142856994616810 ) ) ;
#44004=ORIENTED_EDGE ( 'NONE', *, *, #57916, .T. ) ;
#44005=SURFACE_SIDE_STYLE ('',( #28084 ) ) ;
#44009=CARTESIAN_POINT ( 'NONE',  ( 15.98999599679679839, 118.4999999999999716, 7.500000000000000000 ) ) ;
#44012=ORIENTED_EDGE ( 'NONE', *, *, #36605, .T. ) ;
#44013=VECTOR ( 'NONE', #34650, 1000.000000000000000 ) ;
#44017=DIRECTION ( 'NONE',  ( -0.000000000000000000, -1.000000000000000000, -0.000000000000000000 ) ) ;
#44018=CARTESIAN_POINT ( 'NONE',  ( -9.827790563157511022E-16, 112.4429263765338192, 8.025000000000000355 ) ) ;
#44021=CARTESIAN_POINT ( 'NONE',  ( 8.102448949553183510, 159.9950000000000330, -5.886773742842746238 ) ) ;
#44023=CIRCLE ( 'NONE', #60825, 0.5000000000000004441 ) ;
#44025=CARTESIAN_POINT ( 'NONE',  ( 0.000000000000000000, 140.9429263765338192, -8.025000000000000355 ) ) ;
#44026=DIRECTION ( 'NONE',  ( -0.000000000000000000, 1.000000000000000000, -0.000000000000000000 ) ) ;
#44027=VECTOR ( 'NONE', #15328, 1000.000000000000000 ) ;
#44030=( LENGTH_UNIT ( ) NAMED_UNIT ( * ) SI_UNIT ( .MILLI., .METRE. ) );
#44037=CYLINDRICAL_SURFACE ( 'NONE', #67786, 8.025000000000000355 ) ;
#44038=FILL_AREA_STYLE ('',( #22536 ) ) ;
#44039=VERTEX_POINT ( 'NONE', #52565 ) ;
#44041=DIRECTION ( 'NONE',  ( -1.000000000000000000, 0.000000000000000000, 0.000000000000000000 ) ) ;
#44043=DIRECTION ( 'NONE',  ( -0.000000000000000000, -0.000000000000000000, 1.000000000000000000 ) ) ;
#44056=AXIS2_PLACEMENT_3D ( 'NONE', #24256, #28832, #8088 ) ;
#44058=ADVANCED_FACE ( 'NONE', ( #42386 ), #3982, .F. ) ;
#44059=CARTESIAN_POINT ( 'NONE',  ( -3.094860106618432471, 127.5949999999999847, -9.525000000000000355 ) ) ;
#44062=CIRCLE ( 'NONE', #19289, 0.5000000000000004441 ) ;
#44063=CARTESIAN_POINT ( 'NONE',  ( -21.02379604162863913, 114.4999999999999574, 10.50000000000000000 ) ) ;
#44064=CARTESIAN_POINT ( 'NONE',  ( -8.102448949553179958, 132.0049999999999670, -5.886773742842749790 ) ) ;
#44065=ADVANCED_FACE ( 'NONE', ( #42727 ), #43079, .F. ) ;
#44067=CARTESIAN_POINT ( 'NONE',  ( -41.13967244528112133, 107.8968002066633431, -3.376844662570002598 ) ) ;
#44069=CARTESIAN_POINT ( 'NONE',  ( -5.598654528085808657, 153.7549999999999670, 7.705886871421373741 ) ) ;
#44071=UNCERTAINTY_MEASURE_WITH_UNIT (LENGTH_MEASURE( 1.000000000000000082E-05 ), #62098, 'distance_accuracy_value', 'NONE');
#44074=EDGE_CURVE ( 'NONE', #68774, #23185, #48268, .T. ) ;
#44075=FILL_AREA_STYLE_COLOUR ( '', #7005 ) ;
#44076=ORIENTED_EDGE ( 'NONE', *, *, #28569, .T. ) ;
#44078=DIRECTION ( 'NONE',  ( 1.000000000000000000, 0.000000000000000000, 0.000000000000000000 ) ) ;
#44080=DIRECTION ( 'NONE',  ( 0.000000000000000000, 1.000000000000000000, -0.000000000000000000 ) ) ;
#44082=AXIS2_PLACEMENT_3D ( 'NONE', #55154, #55861, #6984 ) ;
#44083=ORIENTED_EDGE ( 'NONE', *, *, #54774, .T. ) ;
#44084=DIRECTION ( 'NONE',  ( 0.000000000000000000, 1.000000000000000000, -0.000000000000000000 ) ) ;
#44085=UNCERTAINTY_MEASURE_WITH_UNIT (LENGTH_MEASURE( 1.000000000000000082E-05 ), #48135, 'distance_accuracy_value', 'NONE');
#44087=DIRECTION ( 'NONE',  ( 0.000000000000000000, 1.000000000000000000, 0.000000000000000000 ) ) ;
#44088=SURFACE_SIDE_STYLE ('',( #6389 ) ) ;
#44093=PLANE ( 'NONE',  #52988 ) ;
#44096=ORIENTED_EDGE ( 'NONE', *, *, #26932, .F. ) ;
#44098=COLOUR_RGB ( '', 0.31764706, 0.68627451, 0.89019608) ;
#44100=( NAMED_UNIT ( * ) PLANE_ANGLE_UNIT ( ) SI_UNIT ( $, .RADIAN. ) );
#44101=SPHERICAL_SURFACE ( 'NONE', #25210, 0.5000000000000000000 ) ;
#44106=DIRECTION ( 'NONE',  ( 0.000000000000000000, 0.000000000000000000, 1.000000000000000000 ) ) ;
#44110=CARTESIAN_POINT ( 'NONE',  ( 8.102448949553181734, 126.3949999999999818, 5.886773742842750679 ) ) ;
#44119=STYLED_ITEM ( 'NONE', ( #47621 ), #22638 ) ;
#44141=( NAMED_UNIT ( * ) PLANE_ANGLE_UNIT ( ) SI_UNIT ( $, .RADIAN. ) );
#44144=( NAMED_UNIT ( * ) SI_UNIT ( $, .STERADIAN. ) SOLID_ANGLE_UNIT ( ) );
#44145=CARTESIAN_POINT ( 'NONE',  ( -6.826472737025120807, 151.5070736234661979, -4.959722759717907437 ) ) ;
#44146=AXIS2_PLACEMENT_3D ( 'NONE', #53892, #49331, #37441 ) ;
#44154=CYLINDRICAL_SURFACE ( 'NONE', #9187, 0.5000000000000000000 ) ;
#44155=CARTESIAN_POINT ( 'NONE',  ( -14.98999599679679662, 118.4999999999999716, 10.00000000000000000 ) ) ;
#44159=AXIS2_PLACEMENT_3D ( 'NONE', #44218, #44567, #56100 ) ;
#44163=B_SPLINE_CURVE_WITH_KNOTS ( 'NONE', 3,
 ( #22629, #28207, #12395, #56350, #34218, #28568, #12056, #6779 ),
 .UNSPECIFIED., .F., .F.,
 ( 4, 2, 2, 4 ),
 ( 0.000000000000000000, 0.0003517464476818396276, 0.0005276196715227495209, 0.0007034928953636595227 ),
 .UNSPECIFIED. ) ;
#44165=CARTESIAN_POINT ( 'NONE',  ( -45.00000000000000000, -2.024042244987997205E-14, 9.500000000000000000 ) ) ;
#44166=CARTESIAN_POINT ( 'NONE',  ( -45.00000000000000000, 9.581012678897851131, -6.371410634540580098 ) ) ;
#44170=CARTESIAN_POINT ( 'NONE',  ( -74.29271480430246299, 8.623151806617508797, 6.441684343570472926 ) ) ;
#44172=ORIENTED_EDGE ( 'NONE', *, *, #56645, .F. ) ;
#44174=PRESENTATION_STYLE_ASSIGNMENT (( #61328 ) ) ;
#44178=( GEOMETRIC_REPRESENTATION_CONTEXT ( 3 ) GLOBAL_UNCERTAINTY_ASSIGNED_CONTEXT ( ( #11662 ) ) GLOBAL_UNIT_ASSIGNED_CONTEXT ( ( #11321, #65836, #32781 ) ) REPRESENTATION_CONTEXT ( 'NONE', 'WORKASPACE' ) );
#44179=CARTESIAN_POINT ( 'NONE',  ( 9.058813317711337021, 135.5449999999999875, 2.943386871421375783 ) ) ;
#44182=STYLED_ITEM ( 'NONE', ( #16295 ), #54983 ) ;
#44184=ORIENTED_EDGE ( 'NONE', *, *, #50791, .F. ) ;
#44190=LINE ( 'NONE', #38906, #12297 ) ;
#44194=EDGE_LOOP ( 'NONE', ( #2429, #45010, #13412, #52620 ) ) ;
#44196=( BOUNDED_CURVE ( )  B_SPLINE_CURVE ( 2, ( #62655, #19761, #45831, #2116, #67978, #41257, #2489, #3536, #13433, #13087, #45150 ),
 .UNSPECIFIED., .F., .F. ) 
 B_SPLINE_CURVE_WITH_KNOTS ( ( 3, 2, 2, 2, 2, 3 ),
 ( 0.3529411764705882582, 0.3588235294117647078, 0.3647058823529411575, 0.3705882352941177182, 0.3764705882352941679, 0.3823529411764706176 ),
 .UNSPECIFIED. ) 
 CURVE ( )  GEOMETRIC_REPRESENTATION_ITEM ( )  RATIONAL_B_SPLINE_CURVE ( ( 1.000000000000000000, 0.9510565162951535312, 1.000000000000000000, 0.9510565162951535312, 1.000000000000000000, 0.9510565162951535312, 1.000000000000000000, 0.9510565162951535312, 1.000000000000000000, 0.9510565162951530871, 1.000000000000000444 ) ) 
 REPRESENTATION_ITEM ( '' )  );
#44201=CYLINDRICAL_SURFACE ( 'NONE', #35448, 0.5000000000000004441 ) ;
#44204=( NAMED_UNIT ( * ) SI_UNIT ( $, .STERADIAN. ) SOLID_ANGLE_UNIT ( ) );
#44207=FACE_OUTER_BOUND ( 'NONE', #9329, .T. ) ;
#44208=EDGE_CURVE ( 'NONE', #9417, #31048, #30277, .T. ) ;
#44214=CIRCLE ( 'NONE', #50749, 0.5000000000000004441 ) ;
#44215=ORIENTED_EDGE ( 'NONE', *, *, #31735, .T. ) ;
#44218=CARTESIAN_POINT ( 'NONE',  ( -23.21231517720797655, 117.4999999999999716, 7.500000000000000000 ) ) ;
#44219=ORIENTED_EDGE ( 'NONE', *, *, #19814, .F. ) ;
#44220=CARTESIAN_POINT ( 'NONE',  ( -34.99999999999992184, 112.9999999999999858, -9.500000000000000000 ) ) ;
#44221=AXIS2_PLACEMENT_3D ( 'NONE', #27729, #37684, #59082 ) ;
#44222=CARTESIAN_POINT ( 'NONE',  ( -7.632228543268608334, 127.9570736234661439, 2.479861379858952830 ) ) ;
#44227=( NAMED_UNIT ( * ) PLANE_ANGLE_UNIT ( ) SI_UNIT ( $, .RADIAN. ) );
#44228=ORIENTED_EDGE ( 'NONE', *, *, #3789, .F. ) ;
#44229=STYLED_ITEM ( 'NONE', ( #22923 ), #6402 ) ;
#44231=CIRCLE ( 'NONE', #13859, 0.5000000000000004441 ) ;
#44233=ORIENTED_EDGE ( 'NONE', *, *, #66319, .T. ) ;
#44236=DIRECTION ( 'NONE',  ( 0.000000000000000000, 1.000000000000000000, 0.000000000000000000 ) ) ;
#44240=CARTESIAN_POINT ( 'NONE',  ( -20.57648123223228964, 114.5812418126072174, -10.27659574468084891 ) ) ;
#44242=CARTESIAN_POINT ( 'NONE',  ( 44.99999999999999289, 9.905302582397009559, 6.348323522273335406 ) ) ;
#44246=LINE ( 'NONE', #33635, #67246 ) ;
#44251=PLANE ( 'NONE',  #51006 ) ;
#44257=EDGE_CURVE ( 'NONE', #20808, #15660, #51650, .T. ) ;
#44258=AXIS2_PLACEMENT_3D ( 'NONE', #4284, #47646, #69053 ) ;
#44261=CARTESIAN_POINT ( 'NONE',  ( -6.050614363280173436, 153.8633571366135584, 6.516612769276303396 ) ) ;
#44264=DIRECTION ( 'NONE',  ( 0.000000000000000000, 0.000000000000000000, 1.000000000000000000 ) ) ;
#44265=SURFACE_STYLE_FILL_AREA ( #43911 ) ;
#44267=ORIENTED_EDGE ( 'NONE', *, *, #43260, .T. ) ;
#44273=STYLED_ITEM ( 'NONE', ( #15426 ), #36673 ) ;
#44277=CARTESIAN_POINT ( 'NONE',  ( 44.40987964080542127, 10.30029937056511713, 3.500456542365121937 ) ) ;
#44278=CARTESIAN_POINT ( 'NONE',  ( -9.827790563157511022E-16, 151.4429263765338192, 8.025000000000000355 ) ) ;
#44279=( GEOMETRIC_REPRESENTATION_CONTEXT ( 3 ) GLOBAL_UNCERTAINTY_ASSIGNED_CONTEXT ( ( #24360 ) ) GLOBAL_UNIT_ASSIGNED_CONTEXT ( ( #62928, #21770, #48540 ) ) REPRESENTATION_CONTEXT ( 'NONE', 'WORKASPACE' ) );
#44284=EDGE_CURVE ( 'NONE', #13679, #17136, #34814, .T. ) ;
#44288=CARTESIAN_POINT ( 'NONE',  ( 9.058813317711337021, 133.6550000000000011, 2.943386871421375783 ) ) ;
#44289=CARTESIAN_POINT ( 'NONE',  ( -8.437984349512095861, 126.6929263765338192, -5.166775262442723748E-16 ) ) ;
#44292=MECHANICAL_DESIGN_GEOMETRIC_PRESENTATION_REPRESENTATION('',(#38717),#36460);
#44294=CIRCLE ( 'NONE', #13915, 0.5000000000000004441 ) ;
#44295=ORIENTED_EDGE ( 'NONE', *, *, #22574, .F. ) ;
#44298=EDGE_CURVE ( 'NONE', #37840, #10308, #39163, .T. ) ;
#44299=CIRCLE ( 'NONE', #50983, 0.5000000000000004441 ) ;
#44301=DIRECTION ( 'NONE',  ( 0.000000000000000000, 1.000000000000000000, -0.000000000000000000 ) ) ;
#44304=ORIENTED_EDGE ( 'NONE', *, *, #55663, .T. ) ;
#44305=COLOUR_RGB ( '', 0.72549020, 0.75294118, 0.79215686) ;
#44307=STYLED_ITEM ( 'NONE', ( #27267 ), #61927 ) ;
#44308=FACE_OUTER_BOUND ( 'NONE', #32396, .T. ) ;
#44310=SURFACE_SIDE_STYLE ('',( #34042 ) ) ;
#44312=EDGE_LOOP ( 'NONE', ( #23343, #6363, #13179, #54586 ) ) ;
#44316=FILL_AREA_STYLE ('',( #6602 ) ) ;
#44317=ORIENTED_EDGE ( 'NONE', *, *, #25012, .F. ) ;
#44318=FILL_AREA_STYLE_COLOUR ( '', #60526 ) ;
#44320=ORIENTED_EDGE ( 'NONE', *, *, #49675, .T. ) ;
#44322=FILL_AREA_STYLE ('',( #39028 ) ) ;
#44323=CARTESIAN_POINT ( 'NONE',  ( 9.058813317711338797, 156.8449999999999704, -2.943386871421372675 ) ) ;
#44325=EDGE_LOOP ( 'NONE', ( #14316, #27982, #62375, #677 ) ) ;
#44328=PRESENTATION_STYLE_ASSIGNMENT (( #37669 ) ) ;
#44332=CARTESIAN_POINT ( 'NONE',  ( -7.632228543268607446, 138.5429263765338135, -2.479861379858953718 ) ) ;
#44336=CARTESIAN_POINT ( 'NONE',  ( -48.81081081081080697, 14.09971791521133255, 7.500000000000000000 ) ) ;
#44344=( NAMED_UNIT ( * ) PLANE_ANGLE_UNIT ( ) SI_UNIT ( $, .RADIAN. ) );
#44348=CARTESIAN_POINT ( 'NONE',  ( -9.827790563157511022E-16, 140.5570736234661524, 8.025000000000000355 ) ) ;
#44352=VERTEX_POINT ( 'NONE', #52489 ) ;
#44353=CARTESIAN_POINT ( 'NONE',  ( -44.99310538600512643, 9.606306540395133098, 3.226244738077002072 ) ) ;
#44354=MECHANICAL_DESIGN_GEOMETRIC_PRESENTATION_REPRESENTATION('',(#51040),#15116);
#44358=CARTESIAN_POINT ( 'NONE',  ( 60.00000000000000000, 147.4999999999999716, -9.500000000000000000 ) ) ;
#44359=SURFACE_STYLE_USAGE ( .BOTH. , #22863 ) ;
#44362=CARTESIAN_POINT ( 'NONE',  ( 54.99999999999999289, 2.409368300552961372E-15, 11.50000000000003730 ) ) ;
#44371=EDGE_CURVE ( 'NONE', #24181, #13131, #54986, .T. ) ;
#44372=AXIS2_PLACEMENT_3D ( 'NONE', #2401, #34813, #35866 ) ;
#44374=CARTESIAN_POINT ( 'NONE',  ( 9.058813317711338797, 153.8449999999999704, -2.943386871421372675 ) ) ;
#44377=FILL_AREA_STYLE ('',( #48952 ) ) ;
#44378=CARTESIAN_POINT ( 'NONE',  ( -34.99999999999992895, 110.4999999999999858, 10.00000000000000000 ) ) ;
#44379=AXIS2_PLACEMENT_3D ( 'NONE', #28953, #34262, #28249 ) ;
#44380=SURFACE_STYLE_USAGE ( .BOTH. , #66469 ) ;
#44383=CARTESIAN_POINT ( 'NONE',  ( 40.82991390394946052, 108.1252238755516970, -3.311222316328668480 ) ) ;
#44389=FACE_OUTER_BOUND ( 'NONE', #45018, .T. ) ;
#44396=DIRECTION ( 'NONE',  ( -0.000000000000000000, 1.000000000000000000, -0.000000000000000000 ) ) ;
#44398=DIRECTION ( 'NONE',  ( -1.000000000000000000, 0.000000000000000000, 0.000000000000000000 ) ) ;
#44403=ORIENTED_EDGE ( 'NONE', *, *, #48539, .F. ) ;
#44405=VERTEX_POINT ( 'NONE', #29955 ) ;
#44409=( NAMED_UNIT ( * ) PLANE_ANGLE_UNIT ( ) SI_UNIT ( $, .RADIAN. ) );
#44410=ORIENTED_EDGE ( 'NONE', *, *, #42686, .T. ) ;
#44411=VECTOR ( 'NONE', #9847, 1000.000000000000114 ) ;
#44412=COLOUR_RGB ( '', 0.66274510, 0.83137255, 0.94901961) ;
#44413=AXIS2_PLACEMENT_3D ( 'NONE', #43541, #55334, #13819 ) ;
#44416=CARTESIAN_POINT ( 'NONE',  ( 9.058813317711338797, 129.8449999999999989, -2.943386871421372675 ) ) ;
#44417=CARTESIAN_POINT ( 'NONE',  ( 47.50000000000000000, 13.41640786499872284, 9.500000000000000000 ) ) ;
#44420=CARTESIAN_POINT ( 'NONE',  ( 5.598654528085805993, 127.3549999999999898, 7.705886871421374629 ) ) ;
#44422=CARTESIAN_POINT ( 'NONE',  ( 41.36364127011594150, 107.7184400395433386, -3.928466540244119454 ) ) ;
#44423=VERTEX_POINT ( 'NONE', #3894 ) ;
#44424=CARTESIAN_POINT ( 'NONE',  ( -8.102448949553181734, 153.6049999999999898, 5.886773742842747126 ) ) ;
#44429=COLOUR_RGB ( '', 0.72549020, 0.75294118, 0.79215686) ;
#44430=DIRECTION ( 'NONE',  ( 0.000000000000000000, 0.000000000000000000, 1.000000000000000000 ) ) ;
#44431=VERTEX_POINT ( 'NONE', #46537 ) ;
#44432=AXIS2_PLACEMENT_3D ( 'NONE', #2691, #61456, #8014 ) ;
#44439=SURFACE_STYLE_FILL_AREA ( #11677 ) ;
#44442=CARTESIAN_POINT ( 'NONE',  ( -45.00000000000000000, 9.696030919201687581, -3.569498281159027453 ) ) ;
#44445=ORIENTED_EDGE ( 'NONE', *, *, #57027, .F. ) ;
#44449=MECHANICAL_DESIGN_GEOMETRIC_PRESENTATION_REPRESENTATION('',(#5065),#63517);
#44451=EDGE_CURVE ( 'NONE', #64475, #49204, #67962, .T. ) ;
#44453=ORIENTED_EDGE ( 'NONE', *, *, #67935, .F. ) ;
#44455=SURFACE_SIDE_STYLE ('',( #22954 ) ) ;
#44458=EDGE_CURVE ( 'NONE', #7834, #12513, #11220, .T. ) ;
#44459=CARTESIAN_POINT ( 'NONE',  ( 9.058813317711337021, 129.5449999999999875, 2.943386871421375783 ) ) ;
#44461=CIRCLE ( 'NONE', #56768, 13.50000000000000533 ) ;
#44462=CIRCLE ( 'NONE', #36628, 13.99999999999999822 ) ;
#44471=CARTESIAN_POINT ( 'NONE',  ( -21.02379604162863913, 114.4999999999999574, 10.00000000000000000 ) ) ;
#44472=EDGE_LOOP ( 'NONE', ( #74, #20181 ) ) ;
#44473=DIRECTION ( 'NONE',  ( 1.000000000000000000, 0.000000000000000000, 0.000000000000000000 ) ) ;
#44477=AXIS2_PLACEMENT_3D ( 'NONE', #15708, #10428, #11794 ) ;
#44480=FILL_AREA_STYLE_COLOUR ( '', #60570 ) ;
#44481=CYLINDRICAL_SURFACE ( 'NONE', #3828, 0.4999999999999995004 ) ;
#44486=DIRECTION ( 'NONE',  ( -0.000000000000000000, -0.000000000000000000, 1.000000000000000000 ) ) ;
#44489=CARTESIAN_POINT ( 'NONE',  ( 60.00000000000000000, 1.797044900979284448E-15, 10.00000000000000000 ) ) ;
#44490=CARTESIAN_POINT ( 'NONE',  ( -6.826472737025120807, 149.1070736234661354, 4.959722759717906548 ) ) ;
#44491=( GEOMETRIC_REPRESENTATION_CONTEXT ( 3 ) GLOBAL_UNCERTAINTY_ASSIGNED_CONTEXT ( ( #14433 ) ) GLOBAL_UNIT_ASSIGNED_CONTEXT ( ( #48150, #5871, #33321 ) ) REPRESENTATION_CONTEXT ( 'NONE', 'WORKASPACE' ) );
#44492=ORIENTED_EDGE ( 'NONE', *, *, #41079, .F. ) ;
#44493=( NAMED_UNIT ( * ) SI_UNIT ( $, .STERADIAN. ) SOLID_ANGLE_UNIT ( ) );
#44495=CARTESIAN_POINT ( 'NONE',  ( -9.058813317711338797, 126.4549999999999841, 2.943386871421373563 ) ) ;
#44500=DIRECTION ( 'NONE',  ( 0.000000000000000000, 0.000000000000000000, 1.000000000000000000 ) ) ;
#44502=ORIENTED_EDGE ( 'NONE', *, *, #29118, .F. ) ;
#44503=CIRCLE ( 'NONE', #9687, 13.00000000000000178 ) ;
#44504=DIRECTION ( 'NONE',  ( 1.000000000000000000, 0.000000000000000000, 0.000000000000000000 ) ) ;
#44507=( BOUNDED_SURFACE ( )  B_SPLINE_SURFACE ( 3, 2, ( 
 ( #33463, #18677, #28856 ),
 ( #29564, #12683, #33799 ),
 ( #44422, #44754, #17979 ),
 ( #13042, #65824, #56289 ),
 ( #65471, #34154, #51034 ),
 ( #7076, #7754, #39124 ),
 ( #66514, #2793, #55612 ),
 ( #60514, #28507, #17322 ) ),
 .UNSPECIFIED., .F., .F., .F. ) 
 B_SPLINE_SURFACE_WITH_KNOTS ( ( 4, 2, 2, 4 ),
 ( 3, 3 ),
 ( 0.0006464147718099828898, 0.001546301970866985689, 0.001996245570395487143, 0.002446189169923988597 ),
 ( 0.000000000000000000, 1.000000000000000000 ),
 .UNSPECIFIED. ) 
 GEOMETRIC_REPRESENTATION_ITEM ( )  RATIONAL_B_SPLINE_SURFACE ( (
 ( 1.000000000000000000, 0.7071067811865475727, 1.000000000000000000),
 ( 1.000000000000000000, 0.7604340084997890381, 1.000000000000000000),
 ( 1.000000000000000000, 0.8048286378023303822, 1.000000000000000000),
 ( 1.000000000000000000, 0.8534265415375306141, 1.000000000000000000),
 ( 1.000000000000000000, 0.8663147087829253801, 1.000000000000000000),
 ( 1.000000000000000000, 0.8838688826992951997, 1.000000000000000000),
 ( 1.000000000000000000, 0.8885266032451287765, 1.000000000000000000),
 ( 1.000000000000000000, 0.8885233166386380388, 1.000000000000000000) ) ) 
 REPRESENTATION_ITEM ( '' )  SURFACE ( )  );
#44509=DIRECTION ( 'NONE',  ( 1.000000000000000000, 0.000000000000000000, 0.000000000000000000 ) ) ;
#44510=CARTESIAN_POINT ( 'NONE',  ( 45.00000000000000000, 10.69371294336137801, -6.000000000000000000 ) ) ;
#44511=ORIENTED_EDGE ( 'NONE', *, *, #53472, .T. ) ;
#44513=FACE_OUTER_BOUND ( 'NONE', #60898, .T. ) ;
#44514=VERTEX_POINT ( 'NONE', #4227 ) ;
#44518=ORIENTED_EDGE ( 'NONE', *, *, #57762, .F. ) ;
#44522=STYLED_ITEM ( 'NONE', ( #50359 ), #1783 ) ;
#44524=LINE ( 'NONE', #65928, #59743 ) ;
#44525=CARTESIAN_POINT ( 'NONE',  ( 9.058813317711338797, 132.8449999999999989, -2.943386871421372675 ) ) ;
#44526=VECTOR ( 'NONE', #58046, 1000.000000000000000 ) ;
#44532=SURFACE_SIDE_STYLE ('',( #23035 ) ) ;
#44533=SURFACE_SIDE_STYLE ('',( #60637 ) ) ;
#44542=ORIENTED_EDGE ( 'NONE', *, *, #40826, .F. ) ;
#44544=VECTOR ( 'NONE', #45975, 1000.000000000000000 ) ;
#44545=( LENGTH_UNIT ( ) NAMED_UNIT ( * ) SI_UNIT ( .MILLI., .METRE. ) );
#44548=UNCERTAINTY_MEASURE_WITH_UNIT (LENGTH_MEASURE( 1.000000000000000082E-05 ), #10763, 'distance_accuracy_value', 'NONE');
#44551=DIRECTION ( 'NONE',  ( 1.000000000000000000, 0.000000000000000000, 0.000000000000000000 ) ) ;
#44552=CARTESIAN_POINT ( 'NONE',  ( 23.71231517720798010, 117.9999999999999716, 9.500000000000000000 ) ) ;
#44553=( GEOMETRIC_REPRESENTATION_CONTEXT ( 3 ) GLOBAL_UNCERTAINTY_ASSIGNED_CONTEXT ( ( #3895 ) ) GLOBAL_UNIT_ASSIGNED_CONTEXT ( ( #29993, #67638, #40230 ) ) REPRESENTATION_CONTEXT ( 'NONE', 'WORKASPACE' ) );
#44554=AXIS2_PLACEMENT_3D ( 'NONE', #44671, #33382, #54478 ) ;
#44555=DIRECTION ( 'NONE',  ( -1.000000000000000000, 0.000000000000000000, 0.000000000000000000 ) ) ;
#44560=( NAMED_UNIT ( * ) PLANE_ANGLE_UNIT ( ) SI_UNIT ( $, .RADIAN. ) );
#44567=DIRECTION ( 'NONE',  ( 0.000000000000000000, 0.000000000000000000, 1.000000000000000000 ) ) ;
#44568=MECHANICAL_DESIGN_GEOMETRIC_PRESENTATION_REPRESENTATION('',(#60239),#28782);
#44569=ORIENTED_EDGE ( 'NONE', *, *, #50069, .T. ) ;
#44571=CARTESIAN_POINT ( 'NONE',  ( 7.632228543268608334, 120.4570736234661723, -2.479861379858951942 ) ) ;
#44572=CARTESIAN_POINT ( 'NONE',  ( 20.74185979783655043, 149.7721295005298714, 9.939118314201632387 ) ) ;
#44573=FILL_AREA_STYLE_COLOUR ( '', #5839 ) ;
#44577=ORIENTED_EDGE ( 'NONE', *, *, #53058, .F. ) ;
#44578=( LENGTH_UNIT ( ) NAMED_UNIT ( * ) SI_UNIT ( .MILLI., .METRE. ) );
#44580=CARTESIAN_POINT ( 'NONE',  ( 40.99999999999998579, 107.7459666924148252, -3.000000000000000444 ) ) ;
#44582=VERTEX_POINT ( 'NONE', #5624 ) ;
#44583=CARTESIAN_POINT ( 'NONE',  ( 0.000000000000000000, 122.9429263765338192, -8.025000000000000355 ) ) ;
#44584=SURFACE_SIDE_STYLE ('',( #43551 ) ) ;
#44585=UNCERTAINTY_MEASURE_WITH_UNIT (LENGTH_MEASURE( 1.000000000000000082E-05 ), #41801, 'distance_accuracy_value', 'NONE');
#44586=EDGE_LOOP ( 'NONE', ( #43957, #49942, #62656, #19413 ) ) ;
#44587=CARTESIAN_POINT ( 'NONE',  ( -2.607480562269075097, 160.2929263765337851, 8.025000000000000355 ) ) ;
#44588=DIRECTION ( 'NONE',  ( -0.000000000000000000, 1.000000000000000000, -0.000000000000000000 ) ) ;
#44595=VERTEX_POINT ( 'NONE', #37369 ) ;
#44602=FILL_AREA_STYLE_COLOUR ( '', #11775 ) ;
#44607=FILL_AREA_STYLE ('',( #8663 ) ) ;
#44608=CARTESIAN_POINT ( 'NONE',  ( 9.827790563157511022E-16, 87.30187232391182306, -8.025000000000000355 ) ) ;
#44609=VERTEX_POINT ( 'NONE', #16588 ) ;
#44620=EDGE_LOOP ( 'NONE', ( #53767, #17070, #65642, #61981 ) ) ;
#44621=( NAMED_UNIT ( * ) PLANE_ANGLE_UNIT ( ) SI_UNIT ( $, .RADIAN. ) );
#44624=CARTESIAN_POINT ( 'NONE',  ( -7.632228543268608334, 150.8429263765338249, 2.479861379858952830 ) ) ;
#44627=AXIS2_PLACEMENT_3D ( 'NONE', #49387, #1113, #27885 ) ;
#44629=CARTESIAN_POINT ( 'NONE',  ( 5.598654528085805993, 151.3549999999999898, 7.705886871421374629 ) ) ;
#44634=SURFACE_STYLE_FILL_AREA ( #22442 ) ;
#44642=VERTEX_POINT ( 'NONE', #27076 ) ;
#44643=ORIENTED_EDGE ( 'NONE', *, *, #58678, .F. ) ;
#44646=DIRECTION ( 'NONE',  ( 0.000000000000000000, 0.000000000000000000, 1.000000000000000000 ) ) ;
#44649=( LENGTH_UNIT ( ) NAMED_UNIT ( * ) SI_UNIT ( .MILLI., .METRE. ) );
#44650=ORIENTED_EDGE ( 'NONE', *, *, #28585, .T. ) ;
#44653=SURFACE_STYLE_USAGE ( .BOTH. , #54110 ) ;
#44656=ORIENTED_EDGE ( 'NONE', *, *, #23360, .T. ) ;
#44658=DIRECTION ( 'NONE',  ( 0.000000000000000000, 1.000000000000000000, -0.000000000000000000 ) ) ;
#44662=ORIENTED_EDGE ( 'NONE', *, *, #67032, .T. ) ;
#44663=ORIENTED_EDGE ( 'NONE', *, *, #29598, .F. ) ;
#44664=CARTESIAN_POINT ( 'NONE',  ( -74.35456378092618479, 8.376853334107019933, -6.482973932537273498 ) ) ;
#44669=CARTESIAN_POINT ( 'NONE',  ( 2.607480562269071989, 139.5929263765337964, 8.025000000000002132 ) ) ;
#44671=CARTESIAN_POINT ( 'NONE',  ( 12.72792206135785698, 115.4999999999999574, 10.50000000000000000 ) ) ;
#44674=CARTESIAN_POINT ( 'NONE',  ( -9.827790563157511022E-16, 115.4429263765338192, 8.025000000000000355 ) ) ;
#44677=ORIENTED_EDGE ( 'NONE', *, *, #59269, .F. ) ;
#44679=( NAMED_UNIT ( * ) PLANE_ANGLE_UNIT ( ) SI_UNIT ( $, .RADIAN. ) );
#44684=VERTEX_POINT ( 'NONE', #48612 ) ;
#44686=ADVANCED_FACE ( 'NONE', ( #53165 ), #307, .T. ) ;
#44689=( LENGTH_UNIT ( ) NAMED_UNIT ( * ) SI_UNIT ( .MILLI., .METRE. ) );
#44691=EDGE_LOOP ( 'NONE', ( #62844, #53831, #68894, #37667 ) ) ;
#44693=AXIS2_PLACEMENT_3D ( 'NONE', #26957, #36901, #4475 ) ;
#44697=CARTESIAN_POINT ( 'NONE',  ( 51.49999999999998579, 2.837994680254535968E-15, -10.49999999999999822 ) ) ;
#44699=CARTESIAN_POINT ( 'NONE',  ( 71.18918918918917882, 14.09971791521133255, 9.500000000000000000 ) ) ;
#44700=COLOUR_RGB ( '', 0.08235294, 0.09019608, 0.10196078) ;
#44701=DIRECTION ( 'NONE',  ( 0.000000000000000000, 0.000000000000000000, -1.000000000000000000 ) ) ;
#44707=CARTESIAN_POINT ( 'NONE',  ( 2.607480562269113733, 116.7070736234661723, 8.024999999999973710 ) ) ;
#44708=CARTESIAN_POINT ( 'NONE',  ( -34.99999999999992895, 112.9999999999999858, 7.500000000000000000 ) ) ;
#44709=AXIS2_PLACEMENT_3D ( 'NONE', #40626, #25113, #34287 ) ;
#44713=CARTESIAN_POINT ( 'NONE',  ( 9.058813317711338797, 115.9549999999999841, -2.943386871421372675 ) ) ;
#44716=CARTESIAN_POINT ( 'NONE',  ( -8.437984349512095861, 141.6929263765338192, -5.166775262442723748E-16 ) ) ;
#44718=UNCERTAINTY_MEASURE_WITH_UNIT (LENGTH_MEASURE( 1.000000000000000082E-05 ), #9193, 'distance_accuracy_value', 'NONE');
#44726=( NAMED_UNIT ( * ) SI_UNIT ( $, .STERADIAN. ) SOLID_ANGLE_UNIT ( ) );
#44731=FACE_OUTER_BOUND ( 'NONE', #58995, .T. ) ;
#44734=CYLINDRICAL_SURFACE ( 'NONE', #30437, 8.025000000000000355 ) ;
#44735=COLOUR_RGB ( '', 0.40784314, 0.44705882, 0.49803922) ;
#44738=VERTEX_POINT ( 'NONE', #39085 ) ;
#44741=ORIENTED_EDGE ( 'NONE', *, *, #21562, .T. ) ;
#44742=CARTESIAN_POINT ( 'NONE',  ( 34.99999999999992895, 110.4999999999999858, -9.500000000000000000 ) ) ;
#44743=FACE_BOUND ( 'NONE', #36062, .T. ) ;
#44748=CARTESIAN_POINT ( 'NONE',  ( 0.000000000000000000, 133.4449999999999932, -9.525000000000000355 ) ) ;
#44751=EDGE_CURVE ( 'NONE', #57062, #27715, #54851, .T. ) ;
#44752=CARTESIAN_POINT ( 'NONE',  ( 5.598654528085805993, 139.3549999999999898, 7.705886871421374629 ) ) ;
#44754=CARTESIAN_POINT ( 'NONE',  ( 41.47640344042797977, 107.6239624391513132, -3.580003982101955806 ) ) ;
#44756=CARTESIAN_POINT ( 'NONE',  ( -6.826472737025120807, 111.3929263765337936, -4.959722759717907437 ) ) ;
#44759=VECTOR ( 'NONE', #24329, 1000.000000000000000 ) ;
#44762=ADVANCED_FACE ( 'NONE', ( #27764 ), #60478, .F. ) ;
#44765=CARTESIAN_POINT ( 'NONE',  ( 19.89974874213239886, 114.9999999999999574, 10.49999999999999645 ) ) ;
#44766=CARTESIAN_POINT ( 'NONE',  ( -34.99999999999992895, 113.4999999999999858, 7.000000000000000000 ) ) ;
#44770=UNCERTAINTY_MEASURE_WITH_UNIT (LENGTH_MEASURE( 1.000000000000000082E-05 ), #20334, 'distance_accuracy_value', 'NONE');
#44771=EDGE_CURVE ( 'NONE', #12385, #38874, #40532, .T. ) ;
#44772=( NAMED_UNIT ( * ) SI_UNIT ( $, .STERADIAN. ) SOLID_ANGLE_UNIT ( ) );
#44773=DIRECTION ( 'NONE',  ( 0.000000000000000000, 0.000000000000000000, 1.000000000000000000 ) ) ;
#44775=EDGE_LOOP ( 'NONE', ( #9115, #9923, #29841, #60269 ) ) ;
#44776=EDGE_CURVE ( 'NONE', #53321, #36102, #10130, .T. ) ;
#44777=CARTESIAN_POINT ( 'NONE',  ( -45.13108574187265987, 8.257324008952721783, -3.517130741219093526 ) ) ;
#44781=DIRECTION ( 'NONE',  ( 0.000000000000000000, 0.000000000000000000, 1.000000000000000000 ) ) ;
#44782=( GEOMETRIC_REPRESENTATION_CONTEXT ( 3 ) GLOBAL_UNCERTAINTY_ASSIGNED_CONTEXT ( ( #39142 ) ) GLOBAL_UNIT_ASSIGNED_CONTEXT ( ( #22990, #43780, #34225 ) ) REPRESENTATION_CONTEXT ( 'NONE', 'WORKASPACE' ) );
#44785=DIRECTION ( 'NONE',  ( -1.000000000000000000, 0.000000000000000000, 0.000000000000000000 ) ) ;
#44791=CARTESIAN_POINT ( 'NONE',  ( 8.102448949553181734, 135.3950000000000102, 5.886773742842750679 ) ) ;
#44796=( GEOMETRIC_REPRESENTATION_CONTEXT ( 3 ) GLOBAL_UNCERTAINTY_ASSIGNED_CONTEXT ( ( #63570 ) ) GLOBAL_UNIT_ASSIGNED_CONTEXT ( ( #29101, #3390, #34742 ) ) REPRESENTATION_CONTEXT ( 'NONE', 'WORKASPACE' ) );
#44804=ORIENTED_EDGE ( 'NONE', *, *, #2739, .T. ) ;
#44812=ORIENTED_EDGE ( 'NONE', *, *, #101, .T. ) ;
#44814=ORIENTED_EDGE ( 'NONE', *, *, #30321, .T. ) ;
#44816=CARTESIAN_POINT ( 'NONE',  ( 23.21231517720797655, 117.4999999999999716, -9.500000000000000000 ) ) ;
#44817=EDGE_CURVE ( 'NONE', #36852, #31700, #29238, .T. ) ;
#44820=CARTESIAN_POINT ( 'NONE',  ( 4.716976649647096842, 152.8570736234661638, 6.492361379858953896 ) ) ;
#44825=CARTESIAN_POINT ( 'NONE',  ( -9.827790563157511022E-16, 136.4429263765338192, 8.025000000000000355 ) ) ;
#44827=FACE_OUTER_BOUND ( 'NONE', #61638, .T. ) ;
#44828=CARTESIAN_POINT ( 'NONE',  ( 5.598654528085809545, 131.2549999999999955, -7.705886871421373741 ) ) ;
#44829=UNCERTAINTY_MEASURE_WITH_UNIT (LENGTH_MEASURE( 1.000000000000000082E-05 ), #25654, 'distance_accuracy_value', 'NONE');
#44831=DIRECTION ( 'NONE',  ( 1.000000000000000000, 0.000000000000000000, 0.000000000000000000 ) ) ;
#44834=DIRECTION ( 'NONE',  ( 0.000000000000000000, 0.000000000000000000, -1.000000000000000000 ) ) ;
#44837=MECHANICAL_DESIGN_GEOMETRIC_PRESENTATION_REPRESENTATION('',(#37016),#56029);
#44838=( NAMED_UNIT ( * ) PLANE_ANGLE_UNIT ( ) SI_UNIT ( $, .RADIAN. ) );
#44844=( NAMED_UNIT ( * ) PLANE_ANGLE_UNIT ( ) SI_UNIT ( $, .RADIAN. ) );
#44848=( NAMED_UNIT ( * ) SI_UNIT ( $, .STERADIAN. ) SOLID_ANGLE_UNIT ( ) );
#44852=CARTESIAN_POINT ( 'NONE',  ( -75.00000000000000000, 8.092690183933195058, 5.807220890438696159 ) ) ;
#44855=CARTESIAN_POINT ( 'NONE',  ( -9.827790563157511022E-16, 119.5570736234661524, 8.025000000000000355 ) ) ;
#44859=CARTESIAN_POINT ( 'NONE',  ( -9.058813317711337021, 146.0449999999999875, -2.943386871421374895 ) ) ;
#44861=AXIS2_PLACEMENT_3D ( 'NONE', #34784, #8061, #2741 ) ;
#44862=DIRECTION ( 'NONE',  ( 0.000000000000000000, 0.000000000000000000, -1.000000000000000000 ) ) ;
#44863=ORIENTED_EDGE ( 'NONE', *, *, #23980, .F. ) ;
#44866=CARTESIAN_POINT ( 'NONE',  ( -34.99999999999999289, 99.99999999999998579, 3.500000000000000000 ) ) ;
#44876=DIRECTION ( 'NONE',  ( 0.000000000000000000, 1.000000000000000000, -0.000000000000000000 ) ) ;
#44877=DIRECTION ( 'NONE',  ( 0.000000000000000000, 0.000000000000000000, 1.000000000000000000 ) ) ;
#44883=COLOUR_RGB ( '', 0.31764706, 0.68627451, 0.89019608) ;
#44886=SURFACE_SIDE_STYLE ('',( #60324 ) ) ;
#44887=CARTESIAN_POINT ( 'NONE',  ( 0.000000000000000000, 110.4999999999999858, 23.00000000000000000 ) ) ;
#44888=SURFACE_SIDE_STYLE ('',( #27939 ) ) ;
#44895=CARTESIAN_POINT ( 'NONE',  ( -41.84210526315788314, 107.2928455055531600, 3.500000000000000444 ) ) ;
#44896=CIRCLE ( 'NONE', #14524, 0.5000000000000004441 ) ;
#44898=ORIENTED_EDGE ( 'NONE', *, *, #21949, .T. ) ;
#44904=( GEOMETRIC_REPRESENTATION_CONTEXT ( 3 ) GLOBAL_UNCERTAINTY_ASSIGNED_CONTEXT ( ( #16590 ) ) GLOBAL_UNIT_ASSIGNED_CONTEXT ( ( #4741, #26196, #25503 ) ) REPRESENTATION_CONTEXT ( 'NONE', 'WORKASPACE' ) );
#44905=CARTESIAN_POINT ( 'NONE',  ( -7.632228543268608334, 121.9570736234661723, 2.479861379858952830 ) ) ;
#44907=SURFACE_STYLE_FILL_AREA ( #45936 ) ;
#44912=EDGE_CURVE ( 'NONE', #35108, #16524, #62926, .T. ) ;
#44914=DIRECTION ( 'NONE',  ( 1.000000000000000000, 0.000000000000000000, 0.000000000000000000 ) ) ;
#44918=LINE ( 'NONE', #13912, #33958 ) ;
#44921=ORIENTED_EDGE ( 'NONE', *, *, #53058, .T. ) ;
#44927=VERTEX_POINT ( 'NONE', #15123 ) ;
#44929=( GEOMETRIC_REPRESENTATION_CONTEXT ( 3 ) GLOBAL_UNCERTAINTY_ASSIGNED_CONTEXT ( ( #42636 ) ) GLOBAL_UNIT_ASSIGNED_CONTEXT ( ( #14761, #61880, #36236 ) ) REPRESENTATION_CONTEXT ( 'NONE', 'WORKASPACE' ) );
#44932=CARTESIAN_POINT ( 'NONE',  ( -15.98999599679679839, 118.4999999999999716, 9.500000000000000000 ) ) ;
#44934=CARTESIAN_POINT ( 'NONE',  ( 60.00000000000000000, 110.4999999999999858, 9.500000000000000000 ) ) ;
#44942=CARTESIAN_POINT ( 'NONE',  ( 44.91886116991580735, 9.999999999999980460, 3.500000000000000000 ) ) ;
#44946=DIRECTION ( 'NONE',  ( -1.000000000000000000, 0.000000000000000000, 0.000000000000000000 ) ) ;
#44947=EDGE_LOOP ( 'NONE', ( #6452, #36517, #2247, #34486 ) ) ;
#44950=DIRECTION ( 'NONE',  ( 0.000000000000000000, 0.000000000000000000, 1.000000000000000000 ) ) ;
#44953=AXIS2_PLACEMENT_3D ( 'NONE', #19455, #18433, #13476 ) ;
#44954=VECTOR ( 'NONE', #51057, 1000.000000000000000 ) ;
#44957=STYLED_ITEM ( 'NONE', ( #59437 ), #44686 ) ;
#44961=CARTESIAN_POINT ( 'NONE',  ( 24.21231517720798010, 112.9999999999999858, 10.00000000000000000 ) ) ;
#44963=CARTESIAN_POINT ( 'NONE',  ( 8.102448949553183510, 146.1049999999999898, -5.886773742842746238 ) ) ;
#44965=( GEOMETRIC_REPRESENTATION_CONTEXT ( 3 ) GLOBAL_UNCERTAINTY_ASSIGNED_CONTEXT ( ( #68771 ) ) GLOBAL_UNIT_ASSIGNED_CONTEXT ( ( #14219, #47311, #35682 ) ) REPRESENTATION_CONTEXT ( 'NONE', 'WORKASPACE' ) );
#44966=( GEOMETRIC_REPRESENTATION_CONTEXT ( 3 ) GLOBAL_UNCERTAINTY_ASSIGNED_CONTEXT ( ( #36981 ) ) GLOBAL_UNIT_ASSIGNED_CONTEXT ( ( #11403, #32872, #58917 ) ) REPRESENTATION_CONTEXT ( 'NONE', 'WORKASPACE' ) );
#44968=CIRCLE ( 'NONE', #51675, 0.5000000000000004441 ) ;
#44971=CARTESIAN_POINT ( 'NONE',  ( 47.50000000000000000, 99.99999999999992895, 10.00000000000000000 ) ) ;
#44973=ORIENTED_EDGE ( 'NONE', *, *, #22101, .F. ) ;
#44981=CARTESIAN_POINT ( 'NONE',  ( -45.00000000000001421, 8.163938725409353836, 6.987118804072284028 ) ) ;
#44995=CARTESIAN_POINT ( 'NONE',  ( 60.00000000000000000, 1.797044900979284448E-15, -12.00000000000000000 ) ) ;
#45004=EDGE_LOOP ( 'NONE', ( #41040, #58688, #52656, #23073 ) ) ;
#45009=( NAMED_UNIT ( * ) PLANE_ANGLE_UNIT ( ) SI_UNIT ( $, .RADIAN. ) );
#45010=ORIENTED_EDGE ( 'NONE', *, *, #8836, .F. ) ;
#45011=CARTESIAN_POINT ( 'NONE',  ( -4.716976649647098618, 139.1429263765338078, 6.492361379858953008 ) ) ;
#45013=CARTESIAN_POINT ( 'NONE',  ( 68.50000000000000000, 1.797044900979284448E-15, 10.50000000000000000 ) ) ;
#45014=DIRECTION ( 'NONE',  ( -1.000000000000000000, 0.000000000000000000, 0.000000000000000000 ) ) ;
#45018=EDGE_LOOP ( 'NONE', ( #49214, #16686, #38277, #41137 ) ) ;
#45019=FILL_AREA_STYLE_COLOUR ( '', #4560 ) ;
#45021=SURFACE_STYLE_USAGE ( .BOTH. , #39049 ) ;
#45022=CARTESIAN_POINT ( 'NONE',  ( -83.99999999999997158, 50.00000000000000000, 12.00000000000000000 ) ) ;
#45024=CARTESIAN_POINT ( 'NONE',  ( -34.99999999999999289, 99.99999999999998579, 9.500000000000000000 ) ) ;
#45025=VECTOR ( 'NONE', #27356, 1000.000000000000000 ) ;
#45026=DIRECTION ( 'NONE',  ( -0.000000000000000000, -0.000000000000000000, 1.000000000000000000 ) ) ;
#45027=VERTEX_POINT ( 'NONE', #67273 ) ;
#45036=ORIENTED_EDGE ( 'NONE', *, *, #23912, .T. ) ;
#45038=PRESENTATION_STYLE_ASSIGNMENT (( #44359 ) ) ;
#45043=DIRECTION ( 'NONE',  ( 0.000000000000000000, -1.000000000000000000, -0.000000000000000000 ) ) ;
#45044=STYLED_ITEM ( 'NONE', ( #59037 ), #16578 ) ;
#45045=ORIENTED_EDGE ( 'NONE', *, *, #38101, .F. ) ;
#45047=CARTESIAN_POINT ( 'NONE',  ( -74.88079918414226199, 35.74057955362109595, -9.832742485723521497 ) ) ;
#45050=CARTESIAN_POINT ( 'NONE',  ( 4.237300235311910690, 154.5000000000000568, -8.541910993906817851 ) ) ;
#45053=CARTESIAN_POINT ( 'NONE',  ( -9.058813317711338797, 114.4549999999999841, 2.943386871421373563 ) ) ;
#45060=CARTESIAN_POINT ( 'NONE',  ( 41.61282686761438043, 107.5028968421555930, -3.982829320873341850 ) ) ;
#45074=ORIENTED_EDGE ( 'NONE', *, *, #6854, .T. ) ;
#45079=AXIS2_PLACEMENT_3D ( 'NONE', #24166, #45673, #7314 ) ;
#45088=ORIENTED_EDGE ( 'NONE', *, *, #15131, .F. ) ;
#45091=EDGE_LOOP ( 'NONE', ( #22190, #56385, #16205, #43708 ) ) ;
#45092=ADVANCED_FACE ( 'NONE', ( #18738 ), #45167, .F. ) ;
#45093=FILL_AREA_STYLE_COLOUR ( '', #56787 ) ;
#45094=CARTESIAN_POINT ( 'NONE',  ( 5.598654528085809545, 139.1449999999999818, -7.705886871421373741 ) ) ;
#45095=CARTESIAN_POINT ( 'NONE',  ( 0.000000000000000000, 154.9999999999999716, 0.000000000000000000 ) ) ;
#45096=COLOUR_RGB ( '', 0.66274510, 0.83137255, 0.94901961) ;
#45098=DIRECTION ( 'NONE',  ( 1.000000000000000000, 3.469446951953611033E-15, 0.000000000000000000 ) ) ;
#45099=CARTESIAN_POINT ( 'NONE',  ( -9.058813317711337021, 144.1549999999999727, -2.943386871421374895 ) ) ;
#45101=EDGE_CURVE ( 'NONE', #42646, #54470, #50647, .T. ) ;
#45102=( LENGTH_UNIT ( ) NAMED_UNIT ( * ) SI_UNIT ( .MILLI., .METRE. ) );
#45104=CARTESIAN_POINT ( 'NONE',  ( 9.058813317711338797, 154.9549999999999841, -2.943386871421372675 ) ) ;
#45105=LINE ( 'NONE', #59852, #21012 ) ;
#45107=DIRECTION ( 'NONE',  ( 1.000000000000000000, 0.000000000000000000, 0.000000000000000000 ) ) ;
#45108=EDGE_LOOP ( 'NONE', ( #22054, #68321 ) ) ;
#45110=CARTESIAN_POINT ( 'NONE',  ( 20.57648123223228254, 114.4999999999999574, 10.27659574468085069 ) ) ;
#45115=MECHANICAL_DESIGN_GEOMETRIC_PRESENTATION_REPRESENTATION('',(#55086),#17023);
#45116=( GEOMETRIC_REPRESENTATION_CONTEXT ( 3 ) GLOBAL_UNCERTAINTY_ASSIGNED_CONTEXT ( ( #40514 ) ) GLOBAL_UNIT_ASSIGNED_CONTEXT ( ( #54079, #16830, #59703 ) ) REPRESENTATION_CONTEXT ( 'NONE', 'WORKASPACE' ) );
#45118=SURFACE_STYLE_FILL_AREA ( #60892 ) ;
#45119=ORIENTED_EDGE ( 'NONE', *, *, #27682, .T. ) ;
#45123=CARTESIAN_POINT ( 'NONE',  ( -45.89905495956738690, 9.405628579031727554, -3.102072197697239631 ) ) ;
#45125=EDGE_LOOP ( 'NONE', ( #25785, #39148, #62424, #25316 ) ) ;
#45126=CARTESIAN_POINT ( 'NONE',  ( -52.00000000000000000, -1.926070501056209087E-14, -10.49999999999999822 ) ) ;
#45127=AXIS2_PLACEMENT_3D ( 'NONE', #49285, #44043, #28123 ) ;
#45128=LINE ( 'NONE', #1422, #2502 ) ;
#45129=SURFACE_SIDE_STYLE ('',( #13771 ) ) ;
#45132=VERTEX_POINT ( 'NONE', #39890 ) ;
#45133=FILL_AREA_STYLE_COLOUR ( '', #28113 ) ;
#45135=SURFACE_STYLE_FILL_AREA ( #45492 ) ;
#45136=CARTESIAN_POINT ( 'NONE',  ( 9.058813317711338797, 141.8449999999999989, -2.943386871421372675 ) ) ;
#45141=CARTESIAN_POINT ( 'NONE',  ( -71.49999999999998579, 64.07124727947029896, 9.500000000000000000 ) ) ;
#45145=EDGE_CURVE ( 'NONE', #29357, #20853, #52171, .T. ) ;
#45150=CARTESIAN_POINT ( 'NONE',  ( -9.827790563157511022E-16, 130.4429263765338192, 8.025000000000000355 ) ) ;
#45152=DIRECTION ( 'NONE',  ( -0.7833176619561879050, 0.6216216216216192691, -2.156683240403591475E-15 ) ) ;
#45153=AXIS2_PLACEMENT_3D ( 'NONE', #67366, #7928, #13194 ) ;
#45155=( GEOMETRIC_REPRESENTATION_CONTEXT ( 3 ) GLOBAL_UNCERTAINTY_ASSIGNED_CONTEXT ( ( #26377 ) ) GLOBAL_UNIT_ASSIGNED_CONTEXT ( ( #55393, #2916, #12822 ) ) REPRESENTATION_CONTEXT ( 'NONE', 'WORKASPACE' ) );
#45156=DIRECTION ( 'NONE',  ( 1.000000000000000000, 0.000000000000000000, -0.000000000000000000 ) ) ;
#45158=DIRECTION ( 'NONE',  ( 1.000000000000000000, 0.000000000000000000, -0.000000000000000000 ) ) ;
#45160=ORIENTED_EDGE ( 'NONE', *, *, #43260, .F. ) ;
#45163=FACE_OUTER_BOUND ( 'NONE', #54482, .T. ) ;
#45164=AXIS2_PLACEMENT_3D ( 'NONE', #46376, #35081, #56175 ) ;
#45167=CYLINDRICAL_SURFACE ( 'NONE', #10239, 0.5000000000000004441 ) ;
#45168=VECTOR ( 'NONE', #34566, 1000.000000000000000 ) ;
#45169=DIRECTION ( 'NONE',  ( 0.000000000000000000, 1.000000000000000000, 0.000000000000000000 ) ) ;
#45170=CARTESIAN_POINT ( 'NONE',  ( 6.826472737025121695, 153.6070736234661638, -4.959722759717905660 ) ) ;
#45175=B_SPLINE_CURVE_WITH_KNOTS ( 'NONE', 3,
 ( #16126, #22404, #48490, #37603, #189, #43568, #53396, #59004, #43230, #44261, #64957, #59319, #21354, #10818, #54060, #38286, #27995, #26621, #59681, #1231, #33316, #11500, #69550, #32596, #32264, #32973, #53712, #5866, #54409, #38634, #27309, #6228, #27655, #16812, #22762, #42881, #60038, #65317, #22067, #11149, #49164, #17507, #6546, #65661 ),
 .UNSPECIFIED., .F., .F.,
 ( 4, 2, 2, 2, 2, 2, 2, 2, 2, 2, 2, 2, 2, 2, 2, 2, 2, 2, 2, 2, 2, 4 ),
 ( 0.008690707667102608169, 0.01030713786529175932, 0.01192356806348091047, 0.01353999826167006162, 0.01515642845985921278, 0.01596464355895379009, 0.01677285865804836393, 0.01838928885623751855, 0.01919750395533209586, 0.02000571905442666970, 0.02162214925261582432, 0.02323857945080497547, 0.02404679454989955278, 0.02485500964899412663, 0.02647143984718328125, 0.02727965494627785509, 0.02808787004537243240, 0.02970430024356158355, 0.03051251534265616433, 0.03132073044175073817, 0.03293716063993989973, 0.03455359083812905435 ),
 .UNSPECIFIED. ) ;
#45176=CARTESIAN_POINT ( 'NONE',  ( 3.094860106618431583, 133.2049999999999841, 9.525000000000000355 ) ) ;
#45180=SURFACE_SIDE_STYLE ('',( #24702 ) ) ;
#45181=DIRECTION ( 'NONE',  ( 0.000000000000000000, -1.000000000000000000, 0.000000000000000000 ) ) ;
#45183=FILL_AREA_STYLE_COLOUR ( '', #56421 ) ;
#45186=ORIENTED_EDGE ( 'NONE', *, *, #59465, .T. ) ;
#45189=CARTESIAN_POINT ( 'NONE',  ( -23.71231517720798010, 117.9999999999999716, -7.500000000000000000 ) ) ;
#45191=SURFACE_STYLE_FILL_AREA ( #23691 ) ;
#45192=ORIENTED_EDGE ( 'NONE', *, *, #44298, .T. ) ;
#45195=SURFACE_STYLE_USAGE ( .BOTH. , #39566 ) ;
#45198=CARTESIAN_POINT ( 'NONE',  ( -75.00000000000000000, 8.552062714373263930, 6.929199553059595118 ) ) ;
#45202=FILL_AREA_STYLE_COLOUR ( '', #41551 ) ;
#45207=CARTESIAN_POINT ( 'NONE',  ( 3.094860106618431583, 147.0949999999999704, 9.525000000000000355 ) ) ;
#45213=FILL_AREA_STYLE_COLOUR ( '', #60491 ) ;
#45216=CARTESIAN_POINT ( 'NONE',  ( 8.102448949553181734, 114.3949999999999676, 5.886773742842750679 ) ) ;
#45217=AXIS2_PLACEMENT_3D ( 'NONE', #38246, #1194, #11811 ) ;
#45220=AXIS2_PLACEMENT_3D ( 'NONE', #8718, #47082, #25237 ) ;
#45225=CARTESIAN_POINT ( 'NONE',  ( 45.50000000000000000, 99.99999999999992895, 10.00000000000000000 ) ) ;
#45235=CARTESIAN_POINT ( 'NONE',  ( -15.98999599679679839, 117.9999999999999716, -9.500000000000000000 ) ) ;
#45236=FACE_BOUND ( 'NONE', #22561, .T. ) ;
#45237=STYLED_ITEM ( 'NONE', ( #28614 ), #25627 ) ;
#45239=( NAMED_UNIT ( * ) PLANE_ANGLE_UNIT ( ) SI_UNIT ( $, .RADIAN. ) );
#45243=ORIENTED_EDGE ( 'NONE', *, *, #17011, .F. ) ;
#45245=SURFACE_SIDE_STYLE ('',( #18134 ) ) ;
#45246=CARTESIAN_POINT ( 'NONE',  ( -48.00000000000000000, 99.99999999999992895, 9.500000000000000000 ) ) ;
#45248=FILL_AREA_STYLE ('',( #18137 ) ) ;
#45251=CARTESIAN_POINT ( 'NONE',  ( 4.716976649647096842, 119.8570736234661638, 6.492361379858953896 ) ) ;
#45252=VECTOR ( 'NONE', #26691, 1000.000000000000000 ) ;
#45254=CARTESIAN_POINT ( 'NONE',  ( 75.00000000000000000, 19.30628705663858469, -6.500000000000000888 ) ) ;
#45255=B_SPLINE_CURVE_WITH_KNOTS ( 'NONE', 3,
 ( #40796, #3069, #50289, #55901, #23534, #45047, #51673, #66452, #67491, #13320, #40437, #3424 ),
 .UNSPECIFIED., .F., .F.,
 ( 4, 2, 2, 2, 2, 4 ),
 ( 0.000000000000000000, 0.0001665198070560709623, 0.0003330396141121419245, 0.0006660792282242990279, 0.0009991188423364562397, 0.001332158456448613235 ),
 .UNSPECIFIED. ) ;
#45258=ORIENTED_EDGE ( 'NONE', *, *, #35571, .T. ) ;
#45259=FACE_OUTER_BOUND ( 'NONE', #16608, .T. ) ;
#45261=CARTESIAN_POINT ( 'NONE',  ( 20.71231517720798010, 115.4999999999999574, 10.00000000000000000 ) ) ;
#45262=CARTESIAN_POINT ( 'NONE',  ( 2.607480562269030688, 149.7070736234661581, 8.025000000000034106 ) ) ;
#45269=ORIENTED_EDGE ( 'NONE', *, *, #17635, .T. ) ;
#45270=( GEOMETRIC_REPRESENTATION_CONTEXT ( 3 ) GLOBAL_UNCERTAINTY_ASSIGNED_CONTEXT ( ( #17285 ) ) GLOBAL_UNIT_ASSIGNED_CONTEXT ( ( #37060, #32778, #22226 ) ) REPRESENTATION_CONTEXT ( 'NONE', 'WORKASPACE' ) );
#45273=UNCERTAINTY_MEASURE_WITH_UNIT (LENGTH_MEASURE( 1.000000000000000082E-05 ), #26609, 'distance_accuracy_value', 'NONE');
#45274=ORIENTED_EDGE ( 'NONE', *, *, #66902, .T. ) ;
#45275=SURFACE_SIDE_STYLE ('',( #23770 ) ) ;
#45277=DIRECTION ( 'NONE',  ( 1.000000000000000000, 2.055968564120660634E-14, 0.000000000000000000 ) ) ;
#45278=ORIENTED_EDGE ( 'NONE', *, *, #42603, .F. ) ;
#45280=CARTESIAN_POINT ( 'NONE',  ( -74.49999999999998579, 119.9999999999997726, -9.500000000000000000 ) ) ;
#45283=DIRECTION ( 'NONE',  ( 0.000000000000000000, 0.000000000000000000, 1.000000000000000000 ) ) ;
#45284=PLANE ( 'NONE',  #34190 ) ;
#45288=CARTESIAN_POINT ( 'NONE',  ( 9.058813317711338797, 111.8449999999999847, -2.943386871421372675 ) ) ;
#45293=( BOUNDED_CURVE ( )  B_SPLINE_CURVE ( 2, ( #66257, #61653, #1841, #46241, #50113, #30014, #66622, #12436, #23352, #39572, #44855 ),
 .UNSPECIFIED., .F., .F. ) 
 B_SPLINE_CURVE_WITH_KNOTS ( ( 3, 2, 2, 2, 2, 3 ),
 ( 0.1764705882352939903, 0.1823529411764704400, 0.1882352941176469174, 0.1941176470588234226, 0.1999999999999999001, 0.2058823529411763498 ),
 .UNSPECIFIED. ) 
 CURVE ( )  GEOMETRIC_REPRESENTATION_ITEM ( )  RATIONAL_B_SPLINE_CURVE ( ( 1.000000000000001110, 0.9510565162951523099, 1.000000000000000000, 0.9510565162951535312, 1.000000000000000000, 0.9510565162951535312, 1.000000000000000000, 0.9510565162951535312, 1.000000000000000000, 0.9510565162951544194, 0.9999999999999991118 ) ) 
 REPRESENTATION_ITEM ( '' )  );
#45294=MECHANICAL_DESIGN_GEOMETRIC_PRESENTATION_REPRESENTATION('',(#5914),#12656);
#45302=COLOUR_RGB ( '', 0.09019608, 0.27058824, 0.51372549) ;
#45306=CIRCLE ( 'NONE', #47595, 0.5000000000000004441 ) ;
#45307=CARTESIAN_POINT ( 'NONE',  ( 72.50000000000000000, 35.92875272052971525, 10.00000000000000000 ) ) ;
#45312=EDGE_CURVE ( 'NONE', #38501, #37491, #64428, .T. ) ;
#45314=CARTESIAN_POINT ( 'NONE',  ( 8.102448949553183510, 143.1049999999999329, -5.886773742842746238 ) ) ;
#45315=COLOUR_RGB ( '', 0.40784314, 0.44705882, 0.49803922) ;
#45316=SURFACE_STYLE_USAGE ( .BOTH. , #40358 ) ;
#45323=CARTESIAN_POINT ( 'NONE',  ( -19.89974874213239886, 114.9999999999999574, -10.00000000000001421 ) ) ;
#45324=( GEOMETRIC_REPRESENTATION_CONTEXT ( 3 ) GLOBAL_UNCERTAINTY_ASSIGNED_CONTEXT ( ( #8210 ) ) GLOBAL_UNIT_ASSIGNED_CONTEXT ( ( #25308, #52422, #36252 ) ) REPRESENTATION_CONTEXT ( 'NONE', 'WORKASPACE' ) );
#45325=( NAMED_UNIT ( * ) SI_UNIT ( $, .STERADIAN. ) SOLID_ANGLE_UNIT ( ) );
#45334=ORIENTED_EDGE ( 'NONE', *, *, #40538, .F. ) ;
#45335=CARTESIAN_POINT ( 'NONE',  ( -74.50000000000001421, 1.735173206890468129E-14, -10.00000000000000000 ) ) ;
#45337=COLOUR_RGB ( '', 0.09019608, 0.27058824, 0.51372549) ;
#45338=CARTESIAN_POINT ( 'NONE',  ( -45.00000000000000000, 7.768687147774684831, 6.999999999999999112 ) ) ;
#45339=CARTESIAN_POINT ( 'NONE',  ( 47.50000000000000000, 13.41640786499872462, -10.00000000000000000 ) ) ;
#45342=ORIENTED_EDGE ( 'NONE', *, *, #55183, .T. ) ;
#45344=ORIENTED_EDGE ( 'NONE', *, *, #3357, .T. ) ;
#45353=AXIS2_PLACEMENT_3D ( 'NONE', #7178, #37931, #59306 ) ;
#45358=ORIENTED_EDGE ( 'NONE', *, *, #6854, .F. ) ;
#45359=CARTESIAN_POINT ( 'NONE',  ( 4.716976649647099507, 149.6429263765338078, -6.492361379858953008 ) ) ;
#45363=CARTESIAN_POINT ( 'NONE',  ( -4.716976649647098618, 115.1429263765338078, 6.492361379858953008 ) ) ;
#45366=CARTESIAN_POINT ( 'NONE',  ( -69.99999999999998579, 50.00000000000000000, -6.999999999999988454 ) ) ;
#45369=CARTESIAN_POINT ( 'NONE',  ( -2.607480562269157254, 139.2070736234662149, -8.024999999999939959 ) ) ;
#45370=CARTESIAN_POINT ( 'NONE',  ( -20.05205915161432628, 114.9999999999999574, 10.44837816993549318 ) ) ;
#45373=AXIS2_PLACEMENT_3D ( 'NONE', #31200, #67829, #4829 ) ;
#45376=STYLED_ITEM ( 'NONE', ( #29755 ), #55842 ) ;
#45382=PRESENTATION_STYLE_ASSIGNMENT (( #12619 ) ) ;
#45387=CARTESIAN_POINT ( 'NONE',  ( 44.99999999999998579, 119.9999999999999716, 9.500000000000000000 ) ) ;
#45388=VERTEX_POINT ( 'NONE', #36161 ) ;
#45389=( NAMED_UNIT ( * ) SI_UNIT ( $, .STERADIAN. ) SOLID_ANGLE_UNIT ( ) );
#45391=EDGE_CURVE ( 'NONE', #41301, #16804, #1740, .T. ) ;
#45404=FACE_OUTER_BOUND ( 'NONE', #26081, .T. ) ;
#45407=ADVANCED_FACE ( 'NONE', ( #28494 ), #68500, .F. ) ;
#45409=CARTESIAN_POINT ( 'NONE',  ( -5.598654528085808657, 120.7549999999999812, 7.705886871421373741 ) ) ;
#45416=UNCERTAINTY_MEASURE_WITH_UNIT (LENGTH_MEASURE( 1.000000000000000082E-05 ), #19173, 'distance_accuracy_value', 'NONE');
#45424=( LENGTH_UNIT ( ) NAMED_UNIT ( * ) SI_UNIT ( .MILLI., .METRE. ) );
#45425=ORIENTED_EDGE ( 'NONE', *, *, #27221, .T. ) ;
#45429=( GEOMETRIC_REPRESENTATION_CONTEXT ( 3 ) GLOBAL_UNCERTAINTY_ASSIGNED_CONTEXT ( ( #30547 ) ) GLOBAL_UNIT_ASSIGNED_CONTEXT ( ( #20589, #52956, #68432 ) ) REPRESENTATION_CONTEXT ( 'NONE', 'WORKASPACE' ) );
#45430=( BOUNDED_CURVE ( )  B_SPLINE_CURVE ( 2, ( #41387, #57900, #30425, #30790, #31132, #3682, #41742, #47373, #19889, #25514, #47028 ),
 .UNSPECIFIED., .F., .F. ) 
 B_SPLINE_CURVE_WITH_KNOTS ( ( 3, 2, 2, 2, 2, 3 ),
 ( 0.02941176470588238029, 0.03529411764705885773, 0.04117647058823532824, 0.04705882352941180569, 0.05294117647058828313, 0.05882352941176476058 ),
 .UNSPECIFIED. ) 
 CURVE ( )  GEOMETRIC_REPRESENTATION_ITEM ( )  RATIONAL_B_SPLINE_CURVE ( ( 0.9999999999999997780, 0.9510565162951538642, 1.000000000000000000, 0.9510565162951535312, 1.000000000000000000, 0.9510565162951535312, 1.000000000000000000, 0.9510565162951535312, 1.000000000000000000, 0.9510565162951530871, 1.000000000000000444 ) ) 
 REPRESENTATION_ITEM ( '' )  );
#45431=AXIS2_PLACEMENT_3D ( 'NONE', #4956, #9213, #47935 ) ;
#45433=DIRECTION ( 'NONE',  ( 0.000000000000000000, 0.000000000000000000, 1.000000000000000000 ) ) ;
#45435=DIRECTION ( 'NONE',  ( -0.000000000000000000, 1.000000000000000000, -0.000000000000000000 ) ) ;
#45436=EDGE_LOOP ( 'NONE', ( #26775, #21356, #46190, #2135 ) ) ;
#45439=VECTOR ( 'NONE', #32837, 1000.000000000000000 ) ;
#45443=EDGE_LOOP ( 'NONE', ( #18876, #50838, #40648, #61911 ) ) ;
#45445=SURFACE_STYLE_FILL_AREA ( #38776 ) ;
#45446=CARTESIAN_POINT ( 'NONE',  ( -9.058813317711338797, 140.3449999999999989, 2.943386871421373563 ) ) ;
#45449=ORIENTED_EDGE ( 'NONE', *, *, #33894, .F. ) ;
#45450=CARTESIAN_POINT ( 'NONE',  ( -60.49999999999998579, 50.00000000000000000, 6.999999999999999112 ) ) ;
#45451=CARTESIAN_POINT ( 'NONE',  ( 8.102448949553179958, 142.5049999999999955, 5.886773742842750679 ) ) ;
#45454=CARTESIAN_POINT ( 'NONE',  ( -7.632228543268607446, 117.5429263765338135, -2.479861379858953718 ) ) ;
#45456=UNCERTAINTY_MEASURE_WITH_UNIT (LENGTH_MEASURE( 1.000000000000000082E-05 ), #56003, 'distance_accuracy_value', 'NONE');
#45458=STYLED_ITEM ( 'NONE', ( #55978 ), #63145 ) ;
#45459=( NAMED_UNIT ( * ) PLANE_ANGLE_UNIT ( ) SI_UNIT ( $, .RADIAN. ) );
#45461=ORIENTED_EDGE ( 'NONE', *, *, #23830, .T. ) ;
#45462=CARTESIAN_POINT ( 'NONE',  ( 24.21231517720798010, 99.99999999999998579, 7.500000000000000000 ) ) ;
#45472=LINE ( 'NONE', #65843, #22614 ) ;
#45474=EDGE_LOOP ( 'NONE', ( #11458, #59728, #2506, #33386 ) ) ;
#45475=ORIENTED_EDGE ( 'NONE', *, *, #2394, .F. ) ;
#45479=VECTOR ( 'NONE', #61889, 1000.000000000000000 ) ;
#45482=DIRECTION ( 'NONE',  ( 1.000000000000000000, 0.000000000000000000, 0.000000000000000000 ) ) ;
#45483=EDGE_CURVE ( 'NONE', #52933, #12157, #9130, .T. ) ;
#45488=CARTESIAN_POINT ( 'NONE',  ( -75.00000000000000000, 8.164117261306888196, -6.987107442241105026 ) ) ;
#45492=FILL_AREA_STYLE ('',( #7464 ) ) ;
#45495=CARTESIAN_POINT ( 'NONE',  ( -5.598654528085808657, 143.6449999999999818, 7.705886871421373741 ) ) ;
#45503=COLOUR_RGB ( '', 0.31764706, 0.68627451, 0.89019608) ;
#45504=EDGE_CURVE ( 'NONE', #13063, #53683, #23725, .T. ) ;
#45507=AXIS2_PLACEMENT_3D ( 'NONE', #34779, #45733, #50974 ) ;
#45510=VECTOR ( 'NONE', #25484, 1000.000000000000000 ) ;
#45511=DIRECTION ( 'NONE',  ( 0.000000000000000000, 0.000000000000000000, 1.000000000000000000 ) ) ;
#45512=EDGE_LOOP ( 'NONE', ( #31247, #58362, #35127, #53549 ) ) ;
#45515=PRESENTATION_STYLE_ASSIGNMENT (( #62334 ) ) ;
#45521=( GEOMETRIC_REPRESENTATION_CONTEXT ( 3 ) GLOBAL_UNCERTAINTY_ASSIGNED_CONTEXT ( ( #61553 ) ) GLOBAL_UNIT_ASSIGNED_CONTEXT ( ( #11541, #16520, #18812 ) ) REPRESENTATION_CONTEXT ( 'NONE', 'WORKASPACE' ) );
#45522=ORIENTED_EDGE ( 'NONE', *, *, #50131, .F. ) ;
#45523=SURFACE_STYLE_USAGE ( .BOTH. , #29273 ) ;
#45525=ORIENTED_EDGE ( 'NONE', *, *, #36763, .F. ) ;
#45526=CARTESIAN_POINT ( 'NONE',  ( 9.058813317711337021, 114.5449999999999733, 2.943386871421375783 ) ) ;
#45530=CARTESIAN_POINT ( 'NONE',  ( -9.058813317711338797, 114.4549999999999841, 2.943386871421373563 ) ) ;
#45534=CARTESIAN_POINT ( 'NONE',  ( 0.000000000000000000, 128.5549999999999784, -9.525000000000000355 ) ) ;
#45535=UNCERTAINTY_MEASURE_WITH_UNIT (LENGTH_MEASURE( 1.000000000000000082E-05 ), #64110, 'distance_accuracy_value', 'NONE');
#45536=CARTESIAN_POINT ( 'NONE',  ( 20.48276553341834827, 114.7646630323463057, 10.30680354032555712 ) ) ;
#45539=ORIENTED_EDGE ( 'NONE', *, *, #57344, .T. ) ;
#45540=SURFACE_STYLE_USAGE ( .BOTH. , #55703 ) ;
#45544=( GEOMETRIC_REPRESENTATION_CONTEXT ( 3 ) GLOBAL_UNCERTAINTY_ASSIGNED_CONTEXT ( ( #24997 ) ) GLOBAL_UNIT_ASSIGNED_CONTEXT ( ( #64629, #37599, #4833 ) ) REPRESENTATION_CONTEXT ( 'NONE', 'WORKASPACE' ) );
#45546=DIRECTION ( 'NONE',  ( 1.224646799147353207E-16, 1.000000000000000000, -0.000000000000000000 ) ) ;
#45554=CARTESIAN_POINT ( 'NONE',  ( -75.00000000000000000, 8.443649368548715728, 5.542175914092815958 ) ) ;
#45557=EDGE_CURVE ( 'NONE', #10312, #56046, #50080, .T. ) ;
#45562=CARTESIAN_POINT ( 'NONE',  ( 12.72792206135785698, 115.4999999999999574, -10.50000000000000000 ) ) ;
#45563=CARTESIAN_POINT ( 'NONE',  ( -5.598654528085808657, 137.6449999999999818, 7.705886871421373741 ) ) ;
#45566=( LENGTH_UNIT ( ) NAMED_UNIT ( * ) SI_UNIT ( .MILLI., .METRE. ) );
#45572=CARTESIAN_POINT ( 'NONE',  ( 0.000000000000000000, 109.4449999999999932, -9.525000000000000355 ) ) ;
#45574=TOROIDAL_SURFACE ( 'NONE', #10733, 1.000000000000000000, 0.5000000000000000000 ) ;
#45578=VERTEX_POINT ( 'NONE', #32237 ) ;
#45580=LINE ( 'NONE', #23377, #30532 ) ;
#45581=VECTOR ( 'NONE', #34295, 1000.000000000000000 ) ;
#45586=FILL_AREA_STYLE_COLOUR ( '', #30152 ) ;
#45588=SURFACE_SIDE_STYLE ('',( #61688 ) ) ;
#45590=ORIENTED_EDGE ( 'NONE', *, *, #20850, .T. ) ;
#45594=COLOUR_RGB ( '', 0.40784314, 0.44705882, 0.49803922) ;
#45601=( NAMED_UNIT ( * ) PLANE_ANGLE_UNIT ( ) SI_UNIT ( $, .RADIAN. ) );
#45602=ORIENTED_EDGE ( 'NONE', *, *, #21374, .T. ) ;
#45608=CARTESIAN_POINT ( 'NONE',  ( -4.716976649647098618, 137.2570736234661695, 6.492361379858953008 ) ) ;
#45609=EDGE_CURVE ( 'NONE', #36166, #45027, #39280, .T. ) ;
#45610=CARTESIAN_POINT ( 'NONE',  ( 75.00000000000000000, 19.30628705663858469, -7.000000000000000000 ) ) ;
#45615=CARTESIAN_POINT ( 'NONE',  ( 6.826472737025121695, 150.6070736234661069, -4.959722759717905660 ) ) ;
#45618=CARTESIAN_POINT ( 'NONE',  ( -48.50000000000000000, 14.49137674618942562, -10.00000000000000000 ) ) ;
#45620=ORIENTED_EDGE ( 'NONE', *, *, #3337, .T. ) ;
#45622=( BOUNDED_SURFACE ( )  B_SPLINE_SURFACE ( 3, 2, ( 
 ( #41575, #25698, #12546 ),
 ( #16827, #6934, #22780 ),
 ( #29055, #55815, #12192 ),
 ( #33665, #1605, #17181 ),
 ( #49521, #49179, #11518 ),
 ( #43582, #1249, #33331 ),
 ( #17846, #28359, #54752 ),
 ( #44277, #22421, #32987 ),
 ( #65678, #39669, #34011 ),
 ( #49867, #17524, #60727 ) ),
 .UNSPECIFIED., .F., .F., .F. ) 
 B_SPLINE_SURFACE_WITH_KNOTS ( ( 4, 2, 2, 2, 4 ),
 ( 3, 3 ),
 ( 3.141592653589793116, 3.666904475503235616, 4.192216297416678117, 4.717528119330120617, 5.242839941243563118 ),
 ( 0.000000000000000000, 1.000000000000000000 ),
 .UNSPECIFIED. ) 
 GEOMETRIC_REPRESENTATION_ITEM ( )  RATIONAL_B_SPLINE_SURFACE ( (
 ( 1.000000000000000000, 0.5847102846637711737, 1.000000000000000000),
 ( 1.000000000000000000, 0.5846320934540470970, 1.000000000000000000),
 ( 1.000000000000000000, 0.5911458751171370096, 1.000000000000000000),
 ( 1.000000000000000000, 0.6141839381259066588, 1.000000000000000000),
 ( 1.000000000000000000, 0.6306589281296752780, 1.000000000000000000),
 ( 1.000000000000000000, 0.6676671612970677128, 1.000000000000000000),
 ( 1.000000000000000000, 0.6881200523218607978, 1.000000000000000000),
 ( 1.000000000000000000, 0.7272421848983147141, 1.000000000000000000),
 ( 1.000000000000000000, 0.7459210345857979485, 1.000000000000000000),
 ( 1.000000000000000000, 0.7615729461579521242, 1.000000000000000000) ) ) 
 REPRESENTATION_ITEM ( '' )  SURFACE ( )  );
#45626=( GEOMETRIC_REPRESENTATION_CONTEXT ( 3 ) GLOBAL_UNCERTAINTY_ASSIGNED_CONTEXT ( ( #26447 ) ) GLOBAL_UNIT_ASSIGNED_CONTEXT ( ( #59536, #11356, #21213 ) ) REPRESENTATION_CONTEXT ( 'NONE', 'WORKASPACE' ) );
#45627=ORIENTED_EDGE ( 'NONE', *, *, #18872, .T. ) ;
#45628=CARTESIAN_POINT ( 'NONE',  ( -74.99999999999998579, 50.00000000000000000, 9.500000000000000000 ) ) ;
#45629=EDGE_CURVE ( 'NONE', #56046, #4654, #12498, .T. ) ;
#45631=EDGE_LOOP ( 'NONE', ( #19588, #59669, #57451, #25566, #62092, #43963, #30529, #29124 ) ) ;
#45634=ORIENTED_EDGE ( 'NONE', *, *, #2647, .F. ) ;
#45635=FILL_AREA_STYLE_COLOUR ( '', #65608 ) ;
#45636=SURFACE_SIDE_STYLE ('',( #40326 ) ) ;
#45639=CARTESIAN_POINT ( 'NONE',  ( 9.058813317711337021, 117.5449999999999875, 2.943386871421375783 ) ) ;
#45648=DIRECTION ( 'NONE',  ( -0.000000000000000000, -0.000000000000000000, -1.000000000000000000 ) ) ;
#45650=CARTESIAN_POINT ( 'NONE',  ( -75.00000000000000000, 9.117000356772813063, 6.738247770644825607 ) ) ;
#45651=CARTESIAN_POINT ( 'NONE',  ( -8.208819650266621082, 111.3781065788698896, -2.747382571411663754 ) ) ;
#45662=CARTESIAN_POINT ( 'NONE',  ( 3.094860106618435136, 149.4049999999999443, -9.525000000000000355 ) ) ;
#45666=DIRECTION ( 'NONE',  ( 1.000000000000000000, 0.000000000000000000, 0.000000000000000000 ) ) ;
#45673=DIRECTION ( 'NONE',  ( 0.000000000000000000, 0.000000000000000000, 1.000000000000000000 ) ) ;
#45675=FILL_AREA_STYLE ('',( #28743 ) ) ;
#45679=CARTESIAN_POINT ( 'NONE',  ( 45.50000000000000000, 9.639620389971918613, -6.500000000000000000 ) ) ;
#45680=SURFACE_SIDE_STYLE ('',( #23158 ) ) ;
#45682=ORIENTED_EDGE ( 'NONE', *, *, #17123, .T. ) ;
#45688=EDGE_LOOP ( 'NONE', ( #45627, #62038, #4061, #48084 ) ) ;
#45689=EDGE_CURVE ( 'NONE', #1660, #37997, #8638, .T. ) ;
#45690=CIRCLE ( 'NONE', #9739, 0.5000000000000004441 ) ;
#45695=CARTESIAN_POINT ( 'NONE',  ( -0.8808868071890268991, 110.4999999999999574, -9.494348005351133324 ) ) ;
#45698=ADVANCED_FACE ( 'NONE', ( #24436 ), #2607, .T. ) ;
#45701=CARTESIAN_POINT ( 'NONE',  ( 0.000000000000000000, 146.9429263765338192, -8.025000000000000355 ) ) ;
#45703=CYLINDRICAL_SURFACE ( 'NONE', #34010, 13.00000000000000533 ) ;
#45705=EDGE_CURVE ( 'NONE', #3488, #67189, #22678, .T. ) ;
#45706=( NAMED_UNIT ( * ) SI_UNIT ( $, .STERADIAN. ) SOLID_ANGLE_UNIT ( ) );
#45709=ORIENTED_EDGE ( 'NONE', *, *, #52669, .T. ) ;
#45712=LINE ( 'NONE', #7675, #55466 ) ;
#45715=DIRECTION ( 'NONE',  ( -0.000000000000000000, 1.000000000000000000, 0.000000000000000000 ) ) ;
#45718=DIRECTION ( 'NONE',  ( -1.000000000000000000, 0.000000000000000000, 0.000000000000000000 ) ) ;
#45720=ORIENTED_EDGE ( 'NONE', *, *, #35673, .F. ) ;
#45722=CYLINDRICAL_SURFACE ( 'NONE', #9262, 0.5000000000000004441 ) ;
#45733=DIRECTION ( 'NONE',  ( 0.000000000000000000, 0.000000000000000000, 1.000000000000000000 ) ) ;
#45734=ORIENTED_EDGE ( 'NONE', *, *, #69082, .F. ) ;
#45736=FILL_AREA_STYLE ('',( #62896 ) ) ;
#45741=AXIS2_PLACEMENT_3D ( 'NONE', #15356, #69471, #9006 ) ;
#45743=CARTESIAN_POINT ( 'NONE',  ( -8.102448949553181734, 114.6049999999999756, 5.886773742842747126 ) ) ;
#45754=CARTESIAN_POINT ( 'NONE',  ( 0.000000000000000000, 87.30187232391182306, 8.025000000000000355 ) ) ;
#45757=FILL_AREA_STYLE_COLOUR ( '', #42958 ) ;
#45759=ORIENTED_EDGE ( 'NONE', *, *, #22043, .T. ) ;
#45764=ORIENTED_EDGE ( 'NONE', *, *, #13245, .F. ) ;
#45772=EDGE_CURVE ( 'NONE', #11926, #13586, #29379, .T. ) ;
#45774=CARTESIAN_POINT ( 'NONE',  ( 9.058813317711338797, 144.8449999999999989, -2.943386871421372675 ) ) ;
#45776=VERTEX_POINT ( 'NONE', #3656 ) ;
#45778=CARTESIAN_POINT ( 'NONE',  ( -5.598654528085808657, 144.7549999999999955, 7.705886871421373741 ) ) ;
#45779=CYLINDRICAL_SURFACE ( 'NONE', #47441, 13.00000000000000178 ) ;
#45781=CARTESIAN_POINT ( 'NONE',  ( 6.826472737025119919, 118.8929263765337936, 4.959722759717908325 ) ) ;
#45782=FILL_AREA_STYLE ('',( #2796 ) ) ;
#45783=COLOUR_RGB ( '', 0.72549020, 0.75294118, 0.79215686) ;
#45787=VECTOR ( 'NONE', #9182, 1000.000000000000000 ) ;
#45789=EDGE_CURVE ( 'NONE', #29357, #7058, #23765, .T. ) ;
#45799=SURFACE_STYLE_USAGE ( .BOTH. , #62290 ) ;
#45801=SURFACE_SIDE_STYLE ('',( #25003 ) ) ;
#45804=TOROIDAL_SURFACE ( 'NONE', #31139, 14.49999999999999822, 0.5000000000000000000 ) ;
#45806=( NAMED_UNIT ( * ) SI_UNIT ( $, .STERADIAN. ) SOLID_ANGLE_UNIT ( ) );
#45807=DIRECTION ( 'NONE',  ( -0.000000000000000000, -0.000000000000000000, 1.000000000000000000 ) ) ;
#45809=VERTEX_POINT ( 'NONE', #68776 ) ;
#45810=CYLINDRICAL_SURFACE ( 'NONE', #38524, 0.5000000000000004441 ) ;
#45811=DIRECTION ( 'NONE',  ( -0.000000000000000000, -1.000000000000000000, -0.000000000000000000 ) ) ;
#45812=CARTESIAN_POINT ( 'NONE',  ( -75.00000000000000000, 8.062885798616331812, -5.903555993539113089 ) ) ;
#45817=CARTESIAN_POINT ( 'NONE',  ( -9.058813317711338797, 137.3449999999999989, 2.943386871421373563 ) ) ;
#45821=DIRECTION ( 'NONE',  ( 1.156482317317873451E-16, 1.000000000000000000, -0.000000000000000000 ) ) ;
#45823=AXIS2_PLACEMENT_3D ( 'NONE', #55472, #1931, #54423 ) ;
#45827=AXIS2_PLACEMENT_3D ( 'NONE', #31666, #53143, #26386 ) ;
#45828=CYLINDRICAL_SURFACE ( 'NONE', #53911, 0.5000000000000004441 ) ;
#45830=CIRCLE ( 'NONE', #14364, 0.5000000000000004441 ) ;
#45831=CARTESIAN_POINT ( 'NONE',  ( -4.716976649647097730, 129.2429263765338021, -6.492361379858953896 ) ) ;
#45836=DIRECTION ( 'NONE',  ( 0.000000000000000000, -1.000000000000000000, -0.000000000000000000 ) ) ;
#45837=AXIS2_PLACEMENT_3D ( 'NONE', #63182, #20616, #4774 ) ;
#45838=CARTESIAN_POINT ( 'NONE',  ( -74.99999999999998579, 50.00000000000000000, -7.500000000000000000 ) ) ;
#45842=VERTEX_POINT ( 'NONE', #16020 ) ;
#45843=EDGE_CURVE ( 'NONE', #29016, #3957, #44062, .T. ) ;
#45846=CARTESIAN_POINT ( 'NONE',  ( 3.094860106618435136, 115.2949999999999733, -9.525000000000000355 ) ) ;
#45847=EDGE_CURVE ( 'NONE', #46203, #27439, #34979, .T. ) ;
#45848=ORIENTED_EDGE ( 'NONE', *, *, #34707, .T. ) ;
#45850=CARTESIAN_POINT ( 'NONE',  ( 0.000000000000000000, 113.5549999999999926, -9.525000000000000355 ) ) ;
#45852=FILL_AREA_STYLE ('',( #24025 ) ) ;
#45854=CARTESIAN_POINT ( 'NONE',  ( -5.598654528085808657, 135.7549999999999955, 7.705886871421373741 ) ) ;
#45855=FILL_AREA_STYLE ('',( #51125 ) ) ;
#45857=CARTESIAN_POINT ( 'NONE',  ( -48.00000000000000000, 13.41640786499872284, 7.500000000000000000 ) ) ;
#45859=EDGE_CURVE ( 'NONE', #31646, #52813, #47423, .T. ) ;
#45862=DIRECTION ( 'NONE',  ( 1.000000000000000000, 0.000000000000000000, 0.000000000000000000 ) ) ;
#45867=DIRECTION ( 'NONE',  ( -1.000000000000000000, 1.224646799147349509E-16, 0.000000000000000000 ) ) ;
#45872=CYLINDRICAL_SURFACE ( 'NONE', #14201, 0.5000000000000004441 ) ;
#45873=ORIENTED_EDGE ( 'NONE', *, *, #25876, .F. ) ;
#45874=VECTOR ( 'NONE', #55706, 1000.000000000000000 ) ;
#45884=CARTESIAN_POINT ( 'NONE',  ( 9.058813317711338797, 141.8449999999999989, -2.943386871421372675 ) ) ;
#45887=FILL_AREA_STYLE_COLOUR ( '', #33856 ) ;
#45890=CARTESIAN_POINT ( 'NONE',  ( -74.99999999999998579, 50.00000000000000000, -7.000000000000000000 ) ) ;
#45894=CARTESIAN_POINT ( 'NONE',  ( -5.598654528085808657, 113.6449999999999818, 7.705886871421373741 ) ) ;
#45900=FACE_OUTER_BOUND ( 'NONE', #20058, .T. ) ;
#45902=SURFACE_SIDE_STYLE ('',( #2198 ) ) ;
#45909=( NAMED_UNIT ( * ) PLANE_ANGLE_UNIT ( ) SI_UNIT ( $, .RADIAN. ) );
#45911=VERTEX_POINT ( 'NONE', #42423 ) ;
#45918=PRESENTATION_STYLE_ASSIGNMENT (( #56442 ) ) ;
#45921=AXIS2_PLACEMENT_3D ( 'NONE', #15284, #14545, #19824 ) ;
#45924=EDGE_CURVE ( 'NONE', #3912, #51799, #22647, .T. ) ;
#45927=CARTESIAN_POINT ( 'NONE',  ( 34.99999999999999289, 99.99999999999998579, 3.500000000000000000 ) ) ;
#45932=CARTESIAN_POINT ( 'NONE',  ( -7.632228543268608334, 133.9570736234661581, 2.479861379858952830 ) ) ;
#45935=ORIENTED_EDGE ( 'NONE', *, *, #47130, .T. ) ;
#45936=FILL_AREA_STYLE ('',( #50845 ) ) ;
#45937=( GEOMETRIC_REPRESENTATION_CONTEXT ( 3 ) GLOBAL_UNCERTAINTY_ASSIGNED_CONTEXT ( ( #7307 ) ) GLOBAL_UNIT_ASSIGNED_CONTEXT ( ( #37353, #64728, #47924 ) ) REPRESENTATION_CONTEXT ( 'NONE', 'WORKASPACE' ) );
#45939=ORIENTED_EDGE ( 'NONE', *, *, #55524, .T. ) ;
#45941=CARTESIAN_POINT ( 'NONE',  ( -74.99999999999998579, 50.00000000000000000, 10.00000000000000000 ) ) ;
#45942=DIRECTION ( 'NONE',  ( 0.000000000000000000, 1.000000000000000000, 0.000000000000000000 ) ) ;
#45946=ORIENTED_EDGE ( 'NONE', *, *, #34556, .F. ) ;
#45950=ADVANCED_FACE ( 'NONE', ( #23004 ), #44154, .F. ) ;
#45951=UNCERTAINTY_MEASURE_WITH_UNIT (LENGTH_MEASURE( 1.000000000000000082E-05 ), #61472, 'distance_accuracy_value', 'NONE');
#45952=ORIENTED_EDGE ( 'NONE', *, *, #66218, .F. ) ;
#45957=ORIENTED_EDGE ( 'NONE', *, *, #24928, .T. ) ;
#45958=SURFACE_STYLE_FILL_AREA ( #56122 ) ;
#45964=CARTESIAN_POINT ( 'NONE',  ( 9.058813317711337021, 111.5449999999999875, 2.943386871421375783 ) ) ;
#45965=MECHANICAL_DESIGN_GEOMETRIC_PRESENTATION_REPRESENTATION('',(#61627),#39290);
#45971=CARTESIAN_POINT ( 'NONE',  ( 0.000000000000000000, 122.9429263765338192, -8.025000000000000355 ) ) ;
#45972=COLOUR_RGB ( '', 0.08235294, 0.09019608, 0.10196078) ;
#45973=DIRECTION ( 'NONE',  ( -0.9704308468600219006, -0.2413793103448194921, 0.000000000000000000 ) ) ;
#45975=DIRECTION ( 'NONE',  ( -0.000000000000000000, -0.000000000000000000, 1.000000000000000000 ) ) ;
#45980=ORIENTED_EDGE ( 'NONE', *, *, #14623, .F. ) ;
#45984=DIRECTION ( 'NONE',  ( 1.000000000000000000, 4.336808689941999001E-16, 0.000000000000000000 ) ) ;
#45985=SURFACE_SIDE_STYLE ('',( #51245 ) ) ;
#45990=CARTESIAN_POINT ( 'NONE',  ( 5.598654528085809545, 155.2549999999999670, -7.705886871421373741 ) ) ;
#45997=ADVANCED_FACE ( 'NONE', ( #27883 ), #20734, .F. ) ;
#46003=LINE ( 'NONE', #3005, #25986 ) ;
#46004=EDGE_CURVE ( 'NONE', #7942, #49243, #21171, .T. ) ;
#46009=MECHANICAL_DESIGN_GEOMETRIC_PRESENTATION_REPRESENTATION('',(#49356),#63949);
#46010=ORIENTED_EDGE ( 'NONE', *, *, #21284, .F. ) ;
#46012=VECTOR ( 'NONE', #7140, 1000.000000000000000 ) ;
#46017=CARTESIAN_POINT ( 'NONE',  ( 48.50000000000000000, 14.49137674618942562, -7.500000000000000000 ) ) ;
#46018=DIRECTION ( 'NONE',  ( -1.000000000000000000, 0.000000000000000000, 0.000000000000000000 ) ) ;
#46024=DIRECTION ( 'NONE',  ( 0.000000000000000000, 0.000000000000000000, -1.000000000000000000 ) ) ;
#46030=( GEOMETRIC_REPRESENTATION_CONTEXT ( 3 ) GLOBAL_UNCERTAINTY_ASSIGNED_CONTEXT ( ( #22146 ) ) GLOBAL_UNIT_ASSIGNED_CONTEXT ( ( #24735, #56414, #30707 ) ) REPRESENTATION_CONTEXT ( 'NONE', 'WORKASPACE' ) );
#46032=DIRECTION ( 'NONE',  ( 0.000000000000000000, 0.000000000000000000, 1.000000000000000000 ) ) ;
#46034=ORIENTED_EDGE ( 'NONE', *, *, #27629, .F. ) ;
#46035=AXIS2_PLACEMENT_3D ( 'NONE', #14141, #19035, #61959 ) ;
#46036=DIRECTION ( 'NONE',  ( -1.156482317317873451E-16, 1.000000000000000000, 0.000000000000000000 ) ) ;
#46039=CARTESIAN_POINT ( 'NONE',  ( -9.827790563157511022E-16, 148.4429263765338476, 8.025000000000000355 ) ) ;
#46042=AXIS2_PLACEMENT_3D ( 'NONE', #17440, #1514, #49108 ) ;
#46058=CARTESIAN_POINT ( 'NONE',  ( -7.632228543268607446, 120.5429263765338135, -2.479861379858953718 ) ) ;
#46059=VERTEX_POINT ( 'NONE', #10634 ) ;
#46060=VERTEX_POINT ( 'NONE', #47632 ) ;
#46067=CARTESIAN_POINT ( 'NONE',  ( 44.99999999999998579, 119.9999999999999716, 9.500000000000000000 ) ) ;
#46072=DIRECTION ( 'NONE',  ( 1.000000000000000000, -1.387778780781444256E-14, -1.387778780781444256E-14 ) ) ;
#46073=VERTEX_POINT ( 'NONE', #26450 ) ;
#46077=CARTESIAN_POINT ( 'NONE',  ( 9.534962109133534369, 154.5000000000000284, -0.05439801238995608385 ) ) ;
#46078=DIRECTION ( 'NONE',  ( 0.000000000000000000, 1.000000000000000000, 0.000000000000000000 ) ) ;
#46079=AXIS2_PLACEMENT_3D ( 'NONE', #40043, #65350, #12558 ) ;
#46080=DIRECTION ( 'NONE',  ( 1.000000000000000000, -0.000000000000000000, 0.000000000000000000 ) ) ;
#46082=CARTESIAN_POINT ( 'NONE',  ( 9.058813317711337021, 121.6549999999999869, 2.943386871421375783 ) ) ;
#46085=VECTOR ( 'NONE', #67958, 1000.000000000000000 ) ;
#46090=ORIENTED_EDGE ( 'NONE', *, *, #51549, .T. ) ;
#46097=CARTESIAN_POINT ( 'NONE',  ( -23.21231517720797655, 113.4999999999999858, -9.500000000000000000 ) ) ;
#46099=LINE ( 'NONE', #67520, #43883 ) ;
#46100=( LENGTH_UNIT ( ) NAMED_UNIT ( * ) SI_UNIT ( .MILLI., .METRE. ) );
#46101=VERTEX_POINT ( 'NONE', #32087 ) ;
#46103=STYLED_ITEM ( 'NONE', ( #2451 ), #59098 ) ;
#46107=CARTESIAN_POINT ( 'NONE',  ( -72.49999999999998579, 119.9999999999997868, -9.500000000000000000 ) ) ;
#46109=EDGE_CURVE ( 'NONE', #50108, #16746, #12556, .T. ) ;
#46110=ORIENTED_EDGE ( 'NONE', *, *, #21047, .F. ) ;
#46112=ORIENTED_EDGE ( 'NONE', *, *, #22167, .T. ) ;
#46113=DIRECTION ( 'NONE',  ( -1.000000000000000000, 0.000000000000000000, 0.000000000000000000 ) ) ;
#46119=VECTOR ( 'NONE', #42974, 1000.000000000000000 ) ;
#46120=CIRCLE ( 'NONE', #31506, 0.5000000000000004441 ) ;
#46121=CARTESIAN_POINT ( 'NONE',  ( -5.598654528085806881, 142.7449999999999761, -7.705886871421374629 ) ) ;
#46124=DIRECTION ( 'NONE',  ( 0.000000000000000000, 0.000000000000000000, 1.000000000000000000 ) ) ;
#46125=CARTESIAN_POINT ( 'NONE',  ( 3.094860106618431583, 136.2049999999999557, 9.525000000000000355 ) ) ;
#46126=CARTESIAN_POINT ( 'NONE',  ( 0.000000000000000000, 109.9999999999999858, -9.525000000000000355 ) ) ;
#46127=TOROIDAL_SURFACE ( 'NONE', #7871, 17.50000000000000000, 0.5000000000000000000 ) ;
#46128=DIRECTION ( 'NONE',  ( 0.6363636363636357984, 0.000000000000000000, 0.7713892158398705234 ) ) ;
#46129=EDGE_LOOP ( 'NONE', ( #42788, #24306, #58365, #31663 ) ) ;
#46130=CARTESIAN_POINT ( 'NONE',  ( 8.437984349512095861, 119.1929263765338050, 1.550032578732817026E-15 ) ) ;
#46134=FILL_AREA_STYLE_COLOUR ( '', #8116 ) ;
#46138=EDGE_LOOP ( 'NONE', ( #26417, #3410, #45461, #31446 ) ) ;
#46139=STYLED_ITEM ( 'NONE', ( #52396 ), #15603 ) ;
#46144=EDGE_CURVE ( 'NONE', #15724, #49424, #64229, .T. ) ;
#46145=UNCERTAINTY_MEASURE_WITH_UNIT (LENGTH_MEASURE( 1.000000000000000082E-05 ), #5873, 'distance_accuracy_value', 'NONE');
#46146=CIRCLE ( 'NONE', #20284, 0.5000000000000004441 ) ;
#46148=DIRECTION ( 'NONE',  ( 1.000000000000000000, 0.000000000000000000, 0.000000000000000000 ) ) ;
#46149=CARTESIAN_POINT ( 'NONE',  ( -4.716976649647097730, 151.3570736234661638, -6.492361379858953896 ) ) ;
#46150=DIRECTION ( 'NONE',  ( -0.000000000000000000, -1.000000000000000000, 0.000000000000000000 ) ) ;
#46151=ORIENTED_EDGE ( 'NONE', *, *, #14663, .F. ) ;
#46152=AXIS2_PLACEMENT_3D ( 'NONE', #31940, #37624, #54082 ) ;
#46154=ORIENTED_EDGE ( 'NONE', *, *, #11200, .F. ) ;
#46157=ORIENTED_EDGE ( 'NONE', *, *, #24338, .T. ) ;
#46159=AXIS2_PLACEMENT_3D ( 'NONE', #62911, #67876, #14754 ) ;
#46164=CARTESIAN_POINT ( 'NONE',  ( -74.08599351457367277, 9.424643574460649376, -6.049632038801590284 ) ) ;
#46169=CARTESIAN_POINT ( 'NONE',  ( 5.598654528085805993, 141.2449999999999761, 7.705886871421374629 ) ) ;
#46176=AXIS2_PLACEMENT_3D ( 'NONE', #50913, #1947, #29070 ) ;
#46178=CARTESIAN_POINT ( 'NONE',  ( -41.40606286463610530, 107.1009606408073580, -3.493716402184703806 ) ) ;
#46183=CIRCLE ( 'NONE', #58502, 13.99999999999999822 ) ;
#46184=EDGE_CURVE ( 'NONE', #18963, #9977, #22572, .T. ) ;
#46185=SURFACE_SIDE_STYLE ('',( #13792 ) ) ;
#46189=CARTESIAN_POINT ( 'NONE',  ( -2.607480562269073321, 127.2070736234661723, -8.025000000000000355 ) ) ;
#46190=ORIENTED_EDGE ( 'NONE', *, *, #60513, .F. ) ;
#46191=ADVANCED_FACE ( 'NONE', ( #23262 ), #56407, .T. ) ;
#46193=CYLINDRICAL_SURFACE ( 'NONE', #30743, 0.5000000000000004441 ) ;
#46196=CARTESIAN_POINT ( 'NONE',  ( -44.99999999999999289, 8.340816515359847472, 6.279506003890324983 ) ) ;
#46201=ORIENTED_EDGE ( 'NONE', *, *, #169, .F. ) ;
#46203=VERTEX_POINT ( 'NONE', #49313 ) ;
#46205=LINE ( 'NONE', #35969, #3922 ) ;
#46208=CARTESIAN_POINT ( 'NONE',  ( -2.607480562269075097, 158.4070736234661751, 8.025000000000000355 ) ) ;
#46209=ORIENTED_EDGE ( 'NONE', *, *, #35648, .F. ) ;
#46212=CARTESIAN_POINT ( 'NONE',  ( -5.598654528085808657, 111.7549999999999955, 7.705886871421373741 ) ) ;
#46216=CARTESIAN_POINT ( 'NONE',  ( -3.094860106618432471, 134.7050000000000125, -9.525000000000000355 ) ) ;
#46217=UNCERTAINTY_MEASURE_WITH_UNIT (LENGTH_MEASURE( 1.000000000000000082E-05 ), #8837, 'distance_accuracy_value', 'NONE');
#46218=PRESENTATION_STYLE_ASSIGNMENT (( #61996 ) ) ;
#46219=DIRECTION ( 'NONE',  ( 0.000000000000000000, -1.000000000000000000, 0.000000000000000000 ) ) ;
#46221=CARTESIAN_POINT ( 'NONE',  ( -41.49999999999998579, 106.9282032302754999, 3.500000000000000000 ) ) ;
#46222=AXIS2_PLACEMENT_3D ( 'NONE', #51011, #18313, #2773 ) ;
#46226=FILL_AREA_STYLE_COLOUR ( '', #3652 ) ;
#46230=DIRECTION ( 'NONE',  ( -1.387778780781444413E-14, -1.000000000000000000, 0.000000000000000000 ) ) ;
#46231=COLOUR_RGB ( '', 0.72549020, 0.75294118, 0.79215686) ;
#46236=STYLED_ITEM ( 'NONE', ( #39882 ), #52528 ) ;
#46241=CARTESIAN_POINT ( 'NONE',  ( -6.826472737025120807, 118.5070736234661553, -4.959722759717907437 ) ) ;
#46245=CARTESIAN_POINT ( 'NONE',  ( -1.166476076187854022E-15, 140.9449999999999932, 9.525000000000000355 ) ) ;
#46248=( NAMED_UNIT ( * ) SI_UNIT ( $, .STERADIAN. ) SOLID_ANGLE_UNIT ( ) );
#46251=FILL_AREA_STYLE_COLOUR ( '', #54862 ) ;
#46254=CARTESIAN_POINT ( 'NONE',  ( 15.98999599679679839, 147.4999999999999716, 10.00000000000000000 ) ) ;
#46256=ADVANCED_FACE ( 'NONE', ( #40504 ), #62275, .F. ) ;
#46259=( NAMED_UNIT ( * ) PLANE_ANGLE_UNIT ( ) SI_UNIT ( $, .RADIAN. ) );
#46260=ORIENTED_EDGE ( 'NONE', *, *, #42993, .F. ) ;
#46262=SURFACE_STYLE_USAGE ( .BOTH. , #19832 ) ;
#46264=ADVANCED_FACE ( 'NONE', ( #24616 ), #67718, .T. ) ;
#46265=( GEOMETRIC_REPRESENTATION_CONTEXT ( 3 ) GLOBAL_UNCERTAINTY_ASSIGNED_CONTEXT ( ( #62811 ) ) GLOBAL_UNIT_ASSIGNED_CONTEXT ( ( #51900, #35719, #62765 ) ) REPRESENTATION_CONTEXT ( 'NONE', 'WORKASPACE' ) );
#46274=TOROIDAL_SURFACE ( 'NONE', #55206, 1.000000000000000000, 0.5000000000000000000 ) ;
#46278=EDGE_LOOP ( 'NONE', ( #59298, #60956, #37435, #67590 ) ) ;
#46281=SHAPE_DEFINITION_REPRESENTATION ( #36716, #6947 ) ;
#46282=COLOUR_RGB ( '', 0.40784314, 0.44705882, 0.49803922) ;
#46284=COLOUR_RGB ( '', 0.72549020, 0.75294118, 0.79215686) ;
#46285=DIRECTION ( 'NONE',  ( -0.000000000000000000, -0.000000000000000000, -1.000000000000000000 ) ) ;
#46294=CARTESIAN_POINT ( 'NONE',  ( 6.826472737025119919, 135.0070736234661126, 4.959722759717908325 ) ) ;
#46295=VECTOR ( 'NONE', #62871, 1000.000000000000000 ) ;
#46296=ORIENTED_EDGE ( 'NONE', *, *, #69358, .T. ) ;
#46302=DIRECTION ( 'NONE',  ( -1.000000000000000000, -0.000000000000000000, 0.000000000000000000 ) ) ;
#46303=FACE_OUTER_BOUND ( 'NONE', #26953, .T. ) ;
#46307=VERTEX_POINT ( 'NONE', #20040 ) ;
#46308=ADVANCED_FACE ( 'NONE', ( #63319 ), #68958, .F. ) ;
#46309=STYLED_ITEM ( 'NONE', ( #67207 ), #46264 ) ;
#46311=AXIS2_PLACEMENT_3D ( 'NONE', #59438, #9663, #57116 ) ;
#46313=DIRECTION ( 'NONE',  ( 1.000000000000000000, 0.000000000000000000, 0.000000000000000000 ) ) ;
#46314=( LENGTH_UNIT ( ) NAMED_UNIT ( * ) SI_UNIT ( .MILLI., .METRE. ) );
#46317=SPHERICAL_SURFACE ( 'NONE', #6688, 0.5000000000000000000 ) ;
#46318=( LENGTH_UNIT ( ) NAMED_UNIT ( * ) SI_UNIT ( .MILLI., .METRE. ) );
#46319=VERTEX_POINT ( 'NONE', #68606 ) ;
#46320=COLOUR_RGB ( '', 0.09019608, 0.27058824, 0.51372549) ;
#46326=CIRCLE ( 'NONE', #59792, 0.5000000000000004441 ) ;
#46328=CARTESIAN_POINT ( 'NONE',  ( 5.598654528085805993, 117.2449999999999903, 7.705886871421374629 ) ) ;
#46330=AXIS2_PLACEMENT_3D ( 'NONE', #4184, #42266, #52440 ) ;
#46331=( NAMED_UNIT ( * ) SI_UNIT ( $, .STERADIAN. ) SOLID_ANGLE_UNIT ( ) );
#46332=FILL_AREA_STYLE_COLOUR ( '', #39237 ) ;
#46339=FILL_AREA_STYLE_COLOUR ( '', #7197 ) ;
#46352=( GEOMETRIC_REPRESENTATION_CONTEXT ( 3 ) GLOBAL_UNCERTAINTY_ASSIGNED_CONTEXT ( ( #5398 ) ) GLOBAL_UNIT_ASSIGNED_CONTEXT ( ( #27204, #64535, #17060 ) ) REPRESENTATION_CONTEXT ( 'NONE', 'WORKASPACE' ) );
#46355=CARTESIAN_POINT ( 'NONE',  ( -3.094860106618432471, 158.7049999999999557, -9.525000000000000355 ) ) ;
#46356=CYLINDRICAL_SURFACE ( 'NONE', #11789, 4.999999999999997335 ) ;
#46357=EDGE_CURVE ( 'NONE', #3932, #12107, #5248, .T. ) ;
#46363=DIRECTION ( 'NONE',  ( 0.000000000000000000, 1.000000000000000000, 0.000000000000000000 ) ) ;
#46364=AXIS2_PLACEMENT_3D ( 'NONE', #24790, #47007, #57879 ) ;
#46370=DIRECTION ( 'NONE',  ( 1.000000000000000000, 0.000000000000000000, 0.000000000000000000 ) ) ;
#46373=COLOUR_RGB ( '', 0.66274510, 0.83137255, 0.94901961) ;
#46374=( GEOMETRIC_REPRESENTATION_CONTEXT ( 3 ) GLOBAL_UNCERTAINTY_ASSIGNED_CONTEXT ( ( #10984 ) ) GLOBAL_UNIT_ASSIGNED_CONTEXT ( ( #41811, #57244, #3386 ) ) REPRESENTATION_CONTEXT ( 'NONE', 'WORKASPACE' ) );
#46376=CARTESIAN_POINT ( 'NONE',  ( -74.99999999999998579, 50.00000000000000000, -7.000000000000000000 ) ) ;
#46377=ORIENTED_EDGE ( 'NONE', *, *, #14870, .T. ) ;
#46379=DIRECTION ( 'NONE',  ( 0.7071067811865345831, 8.659560562354775086E-17, -0.7071067811865603403 ) ) ;
#46381=CIRCLE ( 'NONE', #9260, 5.499999999999976907 ) ;
#46383=CARTESIAN_POINT ( 'NONE',  ( 10.01517768586949231, 112.8049999999999784, 1.839758294383810543E-15 ) ) ;
#46384=DIRECTION ( 'NONE',  ( 1.000000000000000000, 0.000000000000000000, 0.000000000000000000 ) ) ;
#46391=FILL_AREA_STYLE ('',( #51991 ) ) ;
#46395=CARTESIAN_POINT ( 'NONE',  ( 2.607480562269076430, 149.7929263765338135, -8.025000000000000355 ) ) ;
#46398=MECHANICAL_DESIGN_GEOMETRIC_PRESENTATION_REPRESENTATION('',(#39654),#27246);
#46400=DIRECTION ( 'NONE',  ( 0.000000000000000000, 0.000000000000000000, 1.000000000000000000 ) ) ;
#46402=EDGE_LOOP ( 'NONE', ( #50609, #38515, #9680, #17997 ) ) ;
#46408=CARTESIAN_POINT ( 'NONE',  ( -52.00000000000000000, -1.926070501056209087E-14, 11.50000000000000000 ) ) ;
#46410=SURFACE_STYLE_FILL_AREA ( #14015 ) ;
#46411=( GEOMETRIC_REPRESENTATION_CONTEXT ( 3 ) GLOBAL_UNCERTAINTY_ASSIGNED_CONTEXT ( ( #38217 ) ) GLOBAL_UNIT_ASSIGNED_CONTEXT ( ( #8485, #45459, #13742 ) ) REPRESENTATION_CONTEXT ( 'NONE', 'WORKASPACE' ) );
#46415=ORIENTED_EDGE ( 'NONE', *, *, #56725, .F. ) ;
#46416=STYLED_ITEM ( 'NONE', ( #67646 ), #23814 ) ;
#46420=EDGE_CURVE ( 'NONE', #4040, #13709, #32868, .T. ) ;
#46421=CARTESIAN_POINT ( 'NONE',  ( -71.49999999999998579, 119.9999999999997868, 7.500000000000000000 ) ) ;
#46422=ORIENTED_EDGE ( 'NONE', *, *, #25841, .T. ) ;
#46425=EDGE_CURVE ( 'NONE', #2160, #68013, #66560, .T. ) ;
#46428=DIRECTION ( 'NONE',  ( -0.000000000000000000, -0.000000000000000000, -1.000000000000000000 ) ) ;
#46430=AXIS2_PLACEMENT_3D ( 'NONE', #9620, #36724, #48305 ) ;
#46435=EDGE_CURVE ( 'NONE', #19491, #4798, #12247, .T. ) ;
#46439=EDGE_CURVE ( 'NONE', #44000, #33694, #1775, .T. ) ;
#46440=STYLED_ITEM ( 'NONE', ( #23768 ), #7097 ) ;
#46441=AXIS2_PLACEMENT_3D ( 'NONE', #39493, #45811, #18707 ) ;
#46443=CARTESIAN_POINT ( 'NONE',  ( -5.598654528085808657, 123.7549999999999955, 7.705886871421373741 ) ) ;
#46447=DIRECTION ( 'NONE',  ( 0.000000000000000000, 0.000000000000000000, -1.000000000000000000 ) ) ;
#46450=CIRCLE ( 'NONE', #53153, 0.5000000000000004441 ) ;
#46451=SURFACE_STYLE_FILL_AREA ( #3435 ) ;
#46462=( GEOMETRIC_REPRESENTATION_CONTEXT ( 3 ) GLOBAL_UNCERTAINTY_ASSIGNED_CONTEXT ( ( #64304 ) ) GLOBAL_UNIT_ASSIGNED_CONTEXT ( ( #68400, #52590, #67354 ) ) REPRESENTATION_CONTEXT ( 'NONE', 'WORKASPACE' ) );
#46464=CARTESIAN_POINT ( 'NONE',  ( -23.21231517720797655, 118.4999999999999716, 7.500000000000000000 ) ) ;
#46465=( LENGTH_UNIT ( ) NAMED_UNIT ( * ) SI_UNIT ( .MILLI., .METRE. ) );
#46466=DIRECTION ( 'NONE',  ( 0.000000000000000000, 0.000000000000000000, 1.000000000000000000 ) ) ;
#46473=( GEOMETRIC_REPRESENTATION_CONTEXT ( 3 ) GLOBAL_UNCERTAINTY_ASSIGNED_CONTEXT ( ( #1751 ) ) GLOBAL_UNIT_ASSIGNED_CONTEXT ( ( #36044, #30371, #3629 ) ) REPRESENTATION_CONTEXT ( 'NONE', 'WORKASPACE' ) );
#46479=CARTESIAN_POINT ( 'NONE',  ( -79.99999999999998579, 50.00000000000000000, -6.999999999999988454 ) ) ;
#46480=CARTESIAN_POINT ( 'NONE',  ( -10.01517768586949231, 137.1949999999999363, -6.132527647946036459E-16 ) ) ;
#46482=EDGE_CURVE ( 'NONE', #6975, #45132, #29493, .T. ) ;
#46485=CARTESIAN_POINT ( 'NONE',  ( -5.598654528085806881, 149.8549999999999898, -7.705886871421374629 ) ) ;
#46486=DIRECTION ( 'NONE',  ( -0.000000000000000000, -0.000000000000000000, -1.000000000000000000 ) ) ;
#46487=( NAMED_UNIT ( * ) PLANE_ANGLE_UNIT ( ) SI_UNIT ( $, .RADIAN. ) );
#46488=MECHANICAL_DESIGN_GEOMETRIC_PRESENTATION_REPRESENTATION('',(#20630),#44279);
#46490=CARTESIAN_POINT ( 'NONE',  ( -8.437984349512095861, 120.6929263765338050, -5.166775262442723748E-16 ) ) ;
#46492=CIRCLE ( 'NONE', #48699, 0.5000000000000004441 ) ;
#46495=DIRECTION ( 'NONE',  ( 0.6216216216216174928, -0.7833176619561892373, 0.000000000000000000 ) ) ;
#46497=DIRECTION ( 'NONE',  ( -0.000000000000000000, -1.000000000000000000, -0.000000000000000000 ) ) ;
#46504=( NAMED_UNIT ( * ) PLANE_ANGLE_UNIT ( ) SI_UNIT ( $, .RADIAN. ) );
#46505=MECHANICAL_DESIGN_GEOMETRIC_PRESENTATION_REPRESENTATION('',(#65531),#35214);
#46506=VECTOR ( 'NONE', #32929, 1000.000000000000000 ) ;
#46509=CARTESIAN_POINT ( 'NONE',  ( 75.00000000000000000, 20.36037961002804053, 5.999999999999999112 ) ) ;
#46510=DIRECTION ( 'NONE',  ( 1.000000000000000000, 0.000000000000000000, 0.000000000000000000 ) ) ;
#46512=( NAMED_UNIT ( * ) PLANE_ANGLE_UNIT ( ) SI_UNIT ( $, .RADIAN. ) );
#46513=ADVANCED_FACE ( 'NONE', ( #23182 ), #45703, .T. ) ;
#46514=ORIENTED_EDGE ( 'NONE', *, *, #58011, .F. ) ;
#46521=DIRECTION ( 'NONE',  ( 0.000000000000000000, -1.000000000000000000, 0.000000000000000000 ) ) ;
#46522=STYLED_ITEM ( 'NONE', ( #40734 ), #48203 ) ;
#46523=DIRECTION ( 'NONE',  ( 0.000000000000000000, 0.000000000000000000, -1.000000000000000000 ) ) ;
#46527=AXIS2_PLACEMENT_3D ( 'NONE', #18047, #12402, #49722 ) ;
#46528=CARTESIAN_POINT ( 'NONE',  ( -74.21272224914370952, 8.937790484661849888, -6.368793980437817304 ) ) ;
#46530=CARTESIAN_POINT ( 'NONE',  ( -74.99999999999998579, 50.00000000000000000, 6.500000000000000000 ) ) ;
#46531=LINE ( 'NONE', #40537, #46085 ) ;
#46532=EDGE_CURVE ( 'NONE', #13679, #42412, #53168, .T. ) ;
#46534=CARTESIAN_POINT ( 'NONE',  ( 8.102448949553183510, 147.9949999999999761, -5.886773742842746238 ) ) ;
#46537=CARTESIAN_POINT ( 'NONE',  ( 41.84210526315788314, 107.2928455055531600, -4.000000000000000000 ) ) ;
#46539=CARTESIAN_POINT ( 'NONE',  ( -4.716976649647098618, 145.1429263765338078, 6.492361379858953008 ) ) ;
#46542=TOROIDAL_SURFACE ( 'NONE', #21791, 1.000000000000000000, 0.5000000000000000000 ) ;
#46544=LINE ( 'NONE', #25035, #29789 ) ;
#46546=STYLED_ITEM ( 'NONE', ( #39374 ), #6816 ) ;
#46547=VECTOR ( 'NONE', #26997, 1000.000000000000000 ) ;
#46548=EDGE_CURVE ( 'NONE', #26070, #23836, #18312, .T. ) ;
#46550=CARTESIAN_POINT ( 'NONE',  ( 0.000000000000000000, 87.30187232391182306, 0.000000000000000000 ) ) ;
#46553=AXIS2_PLACEMENT_3D ( 'NONE', #39464, #7073, #45098 ) ;
#46554=ORIENTED_EDGE ( 'NONE', *, *, #45609, .F. ) ;
#46555=EDGE_CURVE ( 'NONE', #46101, #12948, #67767, .T. ) ;
#46556=FILL_AREA_STYLE ('',( #40203 ) ) ;
#46562=ORIENTED_EDGE ( 'NONE', *, *, #68867, .T. ) ;
#46564=CIRCLE ( 'NONE', #11663, 1.000000000000000888 ) ;
#46567=ORIENTED_EDGE ( 'NONE', *, *, #50534, .T. ) ;
#46568=VECTOR ( 'NONE', #38943, 1000.000000000000000 ) ;
#46569=SURFACE_STYLE_FILL_AREA ( #8879 ) ;
#46570=DIRECTION ( 'NONE',  ( 0.000000000000000000, 0.000000000000000000, 1.000000000000000000 ) ) ;
#46571=CARTESIAN_POINT ( 'NONE',  ( -6.826472737025120807, 157.5070736234661126, -4.959722759717907437 ) ) ;
#46573=CARTESIAN_POINT ( 'NONE',  ( -34.99999999999992895, 112.9999999999999858, 7.000000000000000000 ) ) ;
#46576=SURFACE_STYLE_FILL_AREA ( #63401 ) ;
#46578=CARTESIAN_POINT ( 'NONE',  ( -1.166476076187854022E-15, 142.0549999999999784, 9.525000000000000355 ) ) ;
#46580=CARTESIAN_POINT ( 'NONE',  ( 20.07516809221520404, 115.0406803144924766, 9.999999999999998224 ) ) ;
#46581=COLOUR_RGB ( '', 0.08235294, 0.09019608, 0.10196078) ;
#46582=PRESENTATION_STYLE_ASSIGNMENT (( #30677 ) ) ;
#46584=PRESENTATION_STYLE_ASSIGNMENT (( #41630 ) ) ;
#46586=MECHANICAL_DESIGN_GEOMETRIC_PRESENTATION_REPRESENTATION('',(#17350),#380);
#46587=FACE_OUTER_BOUND ( 'NONE', #35222, .T. ) ;
#46592=AXIS2_PLACEMENT_3D ( 'NONE', #45280, #66699, #40001 ) ;
#46593=MECHANICAL_DESIGN_GEOMETRIC_PRESENTATION_REPRESENTATION('',(#3820),#21842);
#46594=CARTESIAN_POINT ( 'NONE',  ( -45.00000000000000000, 8.119648659858167861, -6.397056658262325612 ) ) ;
#46595=EDGE_CURVE ( 'NONE', #46073, #15243, #57623, .T. ) ;
#46599=( NAMED_UNIT ( * ) PLANE_ANGLE_UNIT ( ) SI_UNIT ( $, .RADIAN. ) );
#46601=ORIENTED_EDGE ( 'NONE', *, *, #31533, .F. ) ;
#46604=CARTESIAN_POINT ( 'NONE',  ( -74.99999999999998579, 50.00000000000000000, -10.00000000000000000 ) ) ;
#46611=CARTESIAN_POINT ( 'NONE',  ( 9.058813317711338797, 147.8449999999999989, -2.943386871421372675 ) ) ;
#46613=CIRCLE ( 'NONE', #17410, 5.000000000000004441 ) ;
#46614=CARTESIAN_POINT ( 'NONE',  ( 60.00000000000000000, -2.024042244987997205E-14, 7.500000000000000000 ) ) ;
#46618=FILL_AREA_STYLE_COLOUR ( '', #4287 ) ;
#46621=VECTOR ( 'NONE', #24644, 1000.000000000000000 ) ;
#46623=DIRECTION ( 'NONE',  ( 0.000000000000000000, 0.000000000000000000, -1.000000000000000000 ) ) ;
#46624=CARTESIAN_POINT ( 'NONE',  ( -5.598654528085806881, 112.7449999999999903, -7.705886871421374629 ) ) ;
#46630=CARTESIAN_POINT ( 'NONE',  ( -71.49999999999998579, 64.07124727947029896, -10.00000000000000000 ) ) ;
#46634=CARTESIAN_POINT ( 'NONE',  ( -7.632228543268607446, 124.6570736234661609, -2.479861379858953718 ) ) ;
#46636=CARTESIAN_POINT ( 'NONE',  ( -80.49999999999998579, 50.00000000000000000, -6.500000000000000000 ) ) ;
#46638=ORIENTED_EDGE ( 'NONE', *, *, #48162, .F. ) ;
#46640=VECTOR ( 'NONE', #25824, 1000.000000000000000 ) ;
#46642=CARTESIAN_POINT ( 'NONE',  ( 0.000000000000000000, 110.4999999999999858, 0.000000000000000000 ) ) ;
#46643=AXIS2_PLACEMENT_3D ( 'NONE', #61426, #13596, #2284 ) ;
#46645=CARTESIAN_POINT ( 'NONE',  ( 8.437984349512095861, 123.3070736234661524, 1.550032578732816828E-15 ) ) ;
#46648=B_SPLINE_CURVE_WITH_KNOTS ( 'NONE', 3,
 ( #47452, #68874, #10806, #21013, #36878, #58296 ),
 .UNSPECIFIED., .F., .F.,
 ( 4, 2, 4 ),
 ( 0.000000000000000000, 0.0004110251708232767233, 0.0008220503416465534466 ),
 .UNSPECIFIED. ) ;
#46649=ORIENTED_EDGE ( 'NONE', *, *, #29173, .T. ) ;
#46652=DIRECTION ( 'NONE',  ( 0.000000000000000000, -1.000000000000000000, 0.000000000000000000 ) ) ;
#46653=VERTEX_POINT ( 'NONE', #15078 ) ;
#46655=SURFACE_STYLE_FILL_AREA ( #42072 ) ;
#46656=CARTESIAN_POINT ( 'NONE',  ( 8.437984349512095861, 132.3070736234661524, 1.550032578732817026E-15 ) ) ;
#46658=ORIENTED_EDGE ( 'NONE', *, *, #64017, .T. ) ;
#46663=FACE_OUTER_BOUND ( 'NONE', #29026, .T. ) ;
#46664=CIRCLE ( 'NONE', #12907, 16.00000000000000000 ) ;
#46666=( NAMED_UNIT ( * ) SI_UNIT ( $, .STERADIAN. ) SOLID_ANGLE_UNIT ( ) );
#46667=EDGE_CURVE ( 'NONE', #38669, #46059, #27257, .T. ) ;
#46668=COLOUR_RGB ( '', 0.40784314, 0.44705882, 0.49803922) ;
#46672=ORIENTED_EDGE ( 'NONE', *, *, #6896, .F. ) ;
#46676=UNCERTAINTY_MEASURE_WITH_UNIT (LENGTH_MEASURE( 1.000000000000000082E-05 ), #8, 'distance_accuracy_value', 'NONE');
#46683=EDGE_LOOP ( 'NONE', ( #21361, #44577, #31315, #54511 ) ) ;
#46686=VECTOR ( 'NONE', #32411, 1000.000000000000000 ) ;
#46690=PRESENTATION_STYLE_ASSIGNMENT (( #9716 ) ) ;
#46693=CARTESIAN_POINT ( 'NONE',  ( -5.598654528085806881, 112.7449999999999903, -7.705886871421374629 ) ) ;
#46697=CARTESIAN_POINT ( 'NONE',  ( -74.99999999999998579, 50.00000000000000000, -10.49999999999999822 ) ) ;
#46701=CARTESIAN_POINT ( 'NONE',  ( -45.00000000000000000, -2.024042244987997205E-14, 9.500000000000000000 ) ) ;
#46705=CYLINDRICAL_SURFACE ( 'NONE', #4923, 0.5000000000000004441 ) ;
#46706=CARTESIAN_POINT ( 'NONE',  ( -7.896567696116268742, 111.7770433562488108, 2.415862565091794867 ) ) ;
#46710=STYLED_ITEM ( 'NONE', ( #66170 ), #27846 ) ;
#46712=FILL_AREA_STYLE ('',( #25196 ) ) ;
#46713=CARTESIAN_POINT ( 'NONE',  ( 0.000000000000000000, 114.9999999999999574, -10.50000000000000000 ) ) ;
#46714=UNCERTAINTY_MEASURE_WITH_UNIT (LENGTH_MEASURE( 1.000000000000000082E-05 ), #14101, 'distance_accuracy_value', 'NONE');
#46720=CARTESIAN_POINT ( 'NONE',  ( -9.058813317711338797, 159.4549999999999841, 2.943386871421373563 ) ) ;
#46730=( NAMED_UNIT ( * ) SI_UNIT ( $, .STERADIAN. ) SOLID_ANGLE_UNIT ( ) );
#46732=AXIS2_PLACEMENT_3D ( 'NONE', #31726, #27476, #64446 ) ;
#46734=ORIENTED_EDGE ( 'NONE', *, *, #48426, .F. ) ;
#46737=TOROIDAL_SURFACE ( 'NONE', #1690, 8.499999999999994671, 0.5000000000000000000 ) ;
#46738=DIRECTION ( 'NONE',  ( 0.000000000000000000, 0.000000000000000000, 1.000000000000000000 ) ) ;
#46740=CARTESIAN_POINT ( 'NONE',  ( -21.02379604162863558, 114.4999999999999574, 10.00000000000000000 ) ) ;
#46742=VERTEX_POINT ( 'NONE', #3752 ) ;
#46744=CARTESIAN_POINT ( 'NONE',  ( 47.50000000000000000, 99.99999999999992895, -9.500000000000000000 ) ) ;
#46745=SURFACE_SIDE_STYLE ('',( #9061 ) ) ;
#46747=CARTESIAN_POINT ( 'NONE',  ( -1.166476076187854022E-15, 118.0549999999999926, 9.525000000000000355 ) ) ;
#46750=EDGE_CURVE ( 'NONE', #7249, #68346, #37490, .T. ) ;
#46754=EDGE_CURVE ( 'NONE', #13202, #60808, #30635, .T. ) ;
#46757=SURFACE_SIDE_STYLE ('',( #15073 ) ) ;
#46758=ORIENTED_EDGE ( 'NONE', *, *, #8825, .T. ) ;
#46759=CARTESIAN_POINT ( 'NONE',  ( 7.632228543268608334, 146.3429263765338249, -2.479861379858951942 ) ) ;
#46764=EDGE_CURVE ( 'NONE', #62297, #47153, #5487, .T. ) ;
#46765=ORIENTED_EDGE ( 'NONE', *, *, #13301, .T. ) ;
#46769=FILL_AREA_STYLE_COLOUR ( '', #34631 ) ;
#46770=FILL_AREA_STYLE_COLOUR ( '', #26236 ) ;
#46772=COLOUR_RGB ( '', 0.08235294, 0.09019608, 0.10196078) ;
#46777=SURFACE_SIDE_STYLE ('',( #29492 ) ) ;
#46783=ORIENTED_EDGE ( 'NONE', *, *, #34901, .T. ) ;
#46785=SURFACE_SIDE_STYLE ('',( #25941 ) ) ;
#46786=( LENGTH_UNIT ( ) NAMED_UNIT ( * ) SI_UNIT ( .MILLI., .METRE. ) );
#46788=COLOUR_RGB ( '', 0.31764706, 0.68627451, 0.89019608) ;
#46789=VERTEX_POINT ( 'NONE', #43556 ) ;
#46791=FILL_AREA_STYLE ('',( #8416 ) ) ;
#46794=COLOUR_RGB ( '', 0.09019608, 0.27058824, 0.51372549) ;
#46797=AXIS2_PLACEMENT_3D ( 'NONE', #29464, #23843, #35458 ) ;
#46800=CARTESIAN_POINT ( 'NONE',  ( 45.65811388300841855, 10.21937129433612057, -6.500000000000000000 ) ) ;
#46802=LINE ( 'NONE', #19983, #47218 ) ;
#46806=CARTESIAN_POINT ( 'NONE',  ( 5.598654528085805993, 127.3549999999999898, 7.705886871421374629 ) ) ;
#46811=UNCERTAINTY_MEASURE_WITH_UNIT (LENGTH_MEASURE( 1.000000000000000082E-05 ), #27617, 'distance_accuracy_value', 'NONE');
#46813=CARTESIAN_POINT ( 'NONE',  ( 0.000000000000000000, 110.4999999999999858, 0.000000000000000000 ) ) ;
#46815=SURFACE_SIDE_STYLE ('',( #46451 ) ) ;
#46819=SURFACE_STYLE_USAGE ( .BOTH. , #1714 ) ;
#46820=VECTOR ( 'NONE', #11577, 1000.000000000000000 ) ;
#46823=DIRECTION ( 'NONE',  ( -0.000000000000000000, -0.000000000000000000, -1.000000000000000000 ) ) ;
#46824=( GEOMETRIC_REPRESENTATION_CONTEXT ( 3 ) GLOBAL_UNCERTAINTY_ASSIGNED_CONTEXT ( ( #26405 ) ) GLOBAL_UNIT_ASSIGNED_CONTEXT ( ( #27549, #758, #38531 ) ) REPRESENTATION_CONTEXT ( 'NONE', 'WORKASPACE' ) );
#46825=CARTESIAN_POINT ( 'NONE',  ( -12.72792206135785698, 115.4999999999999574, 10.50000000000000000 ) ) ;
#46827=EDGE_LOOP ( 'NONE', ( #27203, #9334, #45952, #43109 ) ) ;
#46828=CARTESIAN_POINT ( 'NONE',  ( 4.716976649647099507, 131.6429263765338362, -6.492361379858953008 ) ) ;
#46837=EDGE_CURVE ( 'NONE', #36852, #49243, #45306, .T. ) ;
#46839=CARTESIAN_POINT ( 'NONE',  ( -23.71231517720798365, 112.4999999999999858, -10.00000000000000000 ) ) ;
#46842=CARTESIAN_POINT ( 'NONE',  ( 5.598654528085809545, 145.1450000000000102, -7.705886871421373741 ) ) ;
#46846=CARTESIAN_POINT ( 'NONE',  ( -5.598654528085806881, 146.8549999999999898, -7.705886871421374629 ) ) ;
#46847=EDGE_CURVE ( 'NONE', #40244, #47977, #41953, .T. ) ;
#46850=CARTESIAN_POINT ( 'NONE',  ( 6.826472737025121695, 113.4929263765337879, -4.959722759717905660 ) ) ;
#46851=CARTESIAN_POINT ( 'NONE',  ( 44.99999999999977973, 146.4999999999999716, 7.500000000000000000 ) ) ;
#46853=( NAMED_UNIT ( * ) PLANE_ANGLE_UNIT ( ) SI_UNIT ( $, .RADIAN. ) );
#46855=CARTESIAN_POINT ( 'NONE',  ( 48.50000000000000000, 99.99999999999992895, 7.000000000000000000 ) ) ;
#46856=ORIENTED_EDGE ( 'NONE', *, *, #722, .T. ) ;
#46858=ADVANCED_FACE ( 'NONE', ( #53381 ), #16801, .T. ) ;
#46861=SURFACE_STYLE_USAGE ( .BOTH. , #15179 ) ;
#46862=FILL_AREA_STYLE ('',( #15180 ) ) ;
#46865=CARTESIAN_POINT ( 'NONE',  ( 12.72792206135785698, 149.9999999999999716, -10.00000000000000000 ) ) ;
#46875=CARTESIAN_POINT ( 'NONE',  ( 21.02379604162864268, 1.797044900979284448E-15, 10.00000000000000000 ) ) ;
#46877=ORIENTED_EDGE ( 'NONE', *, *, #47317, .F. ) ;
#46879=CYLINDRICAL_SURFACE ( 'NONE', #52048, 0.5000000000000004441 ) ;
#46880=AXIS2_PLACEMENT_3D ( 'NONE', #60200, #20343, #33133 ) ;
#46881=DIRECTION ( 'NONE',  ( -1.000000000000000000, 0.000000000000000000, 0.000000000000000000 ) ) ;
#46885=CARTESIAN_POINT ( 'NONE',  ( -75.00000000000000000, 8.701466902705684348, -5.869459488308679695 ) ) ;
#46889=CARTESIAN_POINT ( 'NONE',  ( 3.094860106618435136, 151.2949999999999875, -9.525000000000000355 ) ) ;
#46892=UNCERTAINTY_MEASURE_WITH_UNIT (LENGTH_MEASURE( 1.000000000000000082E-05 ), #57520, 'distance_accuracy_value', 'NONE');
#46895=ORIENTED_EDGE ( 'NONE', *, *, #38980, .F. ) ;
#46898=DIRECTION ( 'NONE',  ( -0.7833176619561906806, -0.6216216216216158275, 0.000000000000000000 ) ) ;
#46900=ORIENTED_EDGE ( 'NONE', *, *, #32634, .F. ) ;
#46905=DIRECTION ( 'NONE',  ( 1.156482317317873451E-16, 1.000000000000000000, 0.000000000000000000 ) ) ;
#46906=CARTESIAN_POINT ( 'NONE',  ( -61.49999999999998579, 50.00000000000000000, 10.00000000000000000 ) ) ;
#46908=DIRECTION ( 'NONE',  ( 0.000000000000000000, -1.000000000000000000, 0.000000000000000000 ) ) ;
#46915=ORIENTED_EDGE ( 'NONE', *, *, #66192, .T. ) ;
#46918=CARTESIAN_POINT ( 'NONE',  ( 3.094860106618431583, 114.0949999999999704, 9.525000000000000355 ) ) ;
#46919=ORIENTED_EDGE ( 'NONE', *, *, #60557, .T. ) ;
#46921=CARTESIAN_POINT ( 'NONE',  ( -3.094860106618432471, 116.7049999999999841, -9.525000000000000355 ) ) ;
#46925=ORIENTED_EDGE ( 'NONE', *, *, #18816, .F. ) ;
#46926=CARTESIAN_POINT ( 'NONE',  ( 9.058813317711337021, 139.6550000000000011, 2.943386871421375783 ) ) ;
#46927=UNCERTAINTY_MEASURE_WITH_UNIT (LENGTH_MEASURE( 1.000000000000000082E-05 ), #53646, 'distance_accuracy_value', 'NONE');
#46935=CARTESIAN_POINT ( 'NONE',  ( -34.99999999999992895, 112.4999999999999858, -9.500000000000000000 ) ) ;
#46939=CARTESIAN_POINT ( 'NONE',  ( 6.946753979098149401, 111.6727723711330071, -4.645043913640917843 ) ) ;
#46942=ORIENTED_EDGE ( 'NONE', *, *, #16630, .F. ) ;
#46943=SURFACE_STYLE_USAGE ( .BOTH. , #35652 ) ;
#46948=ORIENTED_EDGE ( 'NONE', *, *, #60648, .F. ) ;
#46949=FILL_AREA_STYLE_COLOUR ( '', #38196 ) ;
#46951=EDGE_CURVE ( 'NONE', #50261, #41081, #25130, .T. ) ;
#46952=CARTESIAN_POINT ( 'NONE',  ( 74.50000000000000000, -2.220952357103124925E-14, 6.500000000000000000 ) ) ;
#46953=PRESENTATION_STYLE_ASSIGNMENT (( #10658 ) ) ;
#46955=DIRECTION ( 'NONE',  ( 0.000000000000000000, 0.000000000000000000, 1.000000000000000000 ) ) ;
#46957=CARTESIAN_POINT ( 'NONE',  ( -69.99999999999998579, 50.00000000000000000, -12.00000000000000000 ) ) ;
#46963=DIRECTION ( 'NONE',  ( -0.000000000000000000, -0.000000000000000000, 1.000000000000000000 ) ) ;
#46964=CARTESIAN_POINT ( 'NONE',  ( 3.094860106618435136, 121.2949999999999733, -9.525000000000000355 ) ) ;
#46966=SURFACE_STYLE_USAGE ( .BOTH. , #30034 ) ;
#46969=DIRECTION ( 'NONE',  ( 1.000000000000000000, 0.000000000000000000, 0.000000000000000000 ) ) ;
#46973=MECHANICAL_DESIGN_GEOMETRIC_PRESENTATION_REPRESENTATION('',(#53642),#13208);
#46976=EDGE_CURVE ( 'NONE', #37991, #47273, #42010, .T. ) ;
#46978=ORIENTED_EDGE ( 'NONE', *, *, #29613, .F. ) ;
#46981=DIRECTION ( 'NONE',  ( -0.000000000000000000, -0.000000000000000000, -1.000000000000000000 ) ) ;
#46986=EDGE_CURVE ( 'NONE', #2072, #17063, #65547, .T. ) ;
#46987=EDGE_LOOP ( 'NONE', ( #8269, #25924, #11750, #9562 ) ) ;
#46989=PLANE ( 'NONE',  #36532 ) ;
#46990=( LENGTH_UNIT ( ) NAMED_UNIT ( * ) SI_UNIT ( .MILLI., .METRE. ) );
#46993=CARTESIAN_POINT ( 'NONE',  ( -2.607480562269073765, 136.2070736234661581, -8.025000000000000355 ) ) ;
#46999=VECTOR ( 'NONE', #1483, 1000.000000000000000 ) ;
#47001=( GEOMETRIC_REPRESENTATION_CONTEXT ( 3 ) GLOBAL_UNCERTAINTY_ASSIGNED_CONTEXT ( ( #49532 ) ) GLOBAL_UNIT_ASSIGNED_CONTEXT ( ( #22071, #11155, #49508 ) ) REPRESENTATION_CONTEXT ( 'NONE', 'WORKASPACE' ) );
#47003=ADVANCED_FACE ( 'NONE', ( #21180 ), #50939, .T. ) ;
#47004=SURFACE_STYLE_USAGE ( .BOTH. , #62439 ) ;
#47005=DIRECTION ( 'NONE',  ( 0.000000000000000000, 0.000000000000000000, 1.000000000000000000 ) ) ;
#47006=EDGE_LOOP ( 'NONE', ( #18615, #8537, #53770, #7417 ) ) ;
#47007=DIRECTION ( 'NONE',  ( 0.000000000000000000, 0.000000000000000000, -1.000000000000000000 ) ) ;
#47009=ORIENTED_EDGE ( 'NONE', *, *, #25626, .T. ) ;
#47015=DIRECTION ( 'NONE',  ( 0.000000000000000000, 0.000000000000000000, 1.000000000000000000 ) ) ;
#47018=PRESENTATION_STYLE_ASSIGNMENT (( #47737 ) ) ;
#47022=CYLINDRICAL_SURFACE ( 'NONE', #55510, 0.5000000000000004441 ) ;
#47025=ADVANCED_FACE ( 'NONE', ( #10648 ), #48312, .T. ) ;
#47026=CARTESIAN_POINT ( 'NONE',  ( 0.000000000000000000, 127.4449999999999790, -9.525000000000000355 ) ) ;
#47028=CARTESIAN_POINT ( 'NONE',  ( 0.000000000000000000, 113.9429263765338192, -8.025000000000000355 ) ) ;
#47030=EDGE_LOOP ( 'NONE', ( #48206, #44863, #13516, #66529 ) ) ;
#47032=DIRECTION ( 'NONE',  ( 0.000000000000000000, 0.000000000000000000, -1.000000000000000000 ) ) ;
#47034=CARTESIAN_POINT ( 'NONE',  ( -47.50000000000000000, 99.99999999999992895, 10.00000000000000000 ) ) ;
#47036=CARTESIAN_POINT ( 'NONE',  ( -3.869190034097910402, 110.8545876537711621, -8.353339643030292194 ) ) ;
#47038=CONICAL_SURFACE ( 'NONE', #51503, 5.000000000000004441, 0.7853981633974587151 ) ;
#47047=CARTESIAN_POINT ( 'NONE',  ( -8.102448949553181734, 156.0050000000000239, -5.886773742842749790 ) ) ;
#47048=CARTESIAN_POINT ( 'NONE',  ( 48.50000000000000000, 14.49137674618942562, 7.500000000000000000 ) ) ;
#47049=DIRECTION ( 'NONE',  ( 0.000000000000000000, 0.000000000000000000, 1.000000000000000000 ) ) ;
#47051=MECHANICAL_DESIGN_GEOMETRIC_PRESENTATION_REPRESENTATION('',(#38057),#15556);
#47052=LINE ( 'NONE', #10431, #31222 ) ;
#47053=AXIS2_PLACEMENT_3D ( 'NONE', #40758, #35803, #62173 ) ;
#47054=CARTESIAN_POINT ( 'NONE',  ( -7.186760109405158303, 110.5296962873079707, 6.248938465618036453 ) ) ;
#47055=CARTESIAN_POINT ( 'NONE',  ( 72.00000000000000000, 14.49137674618942917, 7.500000000000000000 ) ) ;
#47057=ADVANCED_FACE ( 'NONE', ( #25765 ), #27136, .T. ) ;
#47058=DIRECTION ( 'NONE',  ( 8.881784197001252323E-16, 0.000000000000000000, 1.000000000000000000 ) ) ;
#47059=DIRECTION ( 'NONE',  ( 1.000000000000000000, 0.000000000000000000, 0.000000000000000000 ) ) ;
#47060=VERTEX_POINT ( 'NONE', #34180 ) ;
#47061=VERTEX_POINT ( 'NONE', #65131 ) ;
#47062=SURFACE_STYLE_FILL_AREA ( #42482 ) ;
#47066=DIRECTION ( 'NONE',  ( 0.000000000000000000, 1.000000000000000000, 0.000000000000000000 ) ) ;
#47069=ORIENTED_EDGE ( 'NONE', *, *, #5086, .F. ) ;
#47074=CARTESIAN_POINT ( 'NONE',  ( -5.598654528085806881, 119.8549999999999898, -7.705886871421374629 ) ) ;
#47077=DIRECTION ( 'NONE',  ( 0.000000000000000000, 0.000000000000000000, 1.000000000000000000 ) ) ;
#47080=( GEOMETRIC_REPRESENTATION_CONTEXT ( 3 ) GLOBAL_UNCERTAINTY_ASSIGNED_CONTEXT ( ( #36080 ) ) GLOBAL_UNIT_ASSIGNED_CONTEXT ( ( #61400, #49838, #7600 ) ) REPRESENTATION_CONTEXT ( 'NONE', 'WORKASPACE' ) );
#47081=CARTESIAN_POINT ( 'NONE',  ( -8.175053251830410872, 110.5000000000000000, 4.967543156751275113 ) ) ;
#47082=DIRECTION ( 'NONE',  ( 0.000000000000000000, 1.000000000000000000, 0.000000000000000000 ) ) ;
#47085=CARTESIAN_POINT ( 'NONE',  ( -7.632228543268607446, 156.5429263765338419, -2.479861379858953718 ) ) ;
#47089=( LENGTH_UNIT ( ) NAMED_UNIT ( * ) SI_UNIT ( .MILLI., .METRE. ) );
#47092=ORIENTED_EDGE ( 'NONE', *, *, #1954, .F. ) ;
#47093=CARTESIAN_POINT ( 'NONE',  ( 20.86636340060661610, 115.0297054428233707, 10.00000000000000000 ) ) ;
#47099=LINE ( 'NONE', #36193, #46295 ) ;
#47102=( LENGTH_UNIT ( ) NAMED_UNIT ( * ) SI_UNIT ( .MILLI., .METRE. ) );
#47103=FACE_OUTER_BOUND ( 'NONE', #24370, .T. ) ;
#47107=ORIENTED_EDGE ( 'NONE', *, *, #11100, .T. ) ;
#47109=CARTESIAN_POINT ( 'NONE',  ( -75.50000000000000000, 64.49137674618943095, 10.00000000000000000 ) ) ;
#47111=CARTESIAN_POINT ( 'NONE',  ( 6.826472737025121695, 114.6070736234661496, -4.959722759717905660 ) ) ;
#47113=DIRECTION ( 'NONE',  ( 1.000000000000000000, -0.000000000000000000, 0.000000000000000000 ) ) ;
#47120=DIRECTION ( 'NONE',  ( 1.000000000000000000, 0.000000000000000000, 0.000000000000000000 ) ) ;
#47124=SURFACE_STYLE_USAGE ( .BOTH. , #36919 ) ;
#47125=COLOUR_RGB ( '', 0.08235294, 0.09019608, 0.10196078) ;
#47127=CARTESIAN_POINT ( 'NONE',  ( 3.094860106618431583, 130.2049999999999841, 9.525000000000000355 ) ) ;
#47129=CARTESIAN_POINT ( 'NONE',  ( 20.57648123223228254, 114.5810881445910070, -10.27659574468084891 ) ) ;
#47130=EDGE_CURVE ( 'NONE', #66131, #32455, #68988, .T. ) ;
#47131=STYLED_ITEM ( 'NONE', ( #16061 ), #20490 ) ;
#47136=ADVANCED_FACE ( 'NONE', ( #38107 ), #2085, .F. ) ;
#47137=LINE ( 'NONE', #69254, #7936 ) ;
#47140=ORIENTED_EDGE ( 'NONE', *, *, #63480, .T. ) ;
#47144=CIRCLE ( 'NONE', #33636, 14.49999999999999822 ) ;
#47145=ADVANCED_FACE ( 'NONE', ( #6052 ), #17675, .F. ) ;
#47146=EDGE_CURVE ( 'NONE', #5542, #56654, #3139, .T. ) ;
#47148=ADVANCED_FACE ( 'NONE', ( #51753 ), #29649, .T. ) ;
#47151=ORIENTED_EDGE ( 'NONE', *, *, #4023, .F. ) ;
#47152=COLOUR_RGB ( '', 0.08235294, 0.09019608, 0.10196078) ;
#47153=VERTEX_POINT ( 'NONE', #23959 ) ;
#47154=CARTESIAN_POINT ( 'NONE',  ( 2.607480562269034241, 131.7929263765337851, -8.025000000000032330 ) ) ;
#47156=EDGE_CURVE ( 'NONE', #34517, #38501, #51392, .T. ) ;
#47157=CARTESIAN_POINT ( 'NONE',  ( -6.826472737025120807, 147.9929263765338305, 4.959722759717906548 ) ) ;
#47158=DIRECTION ( 'NONE',  ( -1.000000000000000000, -0.000000000000000000, -0.000000000000000000 ) ) ;
#47159=STYLED_ITEM ( 'NONE', ( #49775 ), #68785 ) ;
#47160=FILL_AREA_STYLE_COLOUR ( '', #42133 ) ;
#47168=SURFACE_SIDE_STYLE ('',( #26344 ) ) ;
#47171=COLOUR_RGB ( '', 0.66274510, 0.83137255, 0.94901961) ;
#47173=CARTESIAN_POINT ( 'NONE',  ( 5.598654528085805993, 153.2450000000000045, 7.705886871421374629 ) ) ;
#47174=PRESENTATION_STYLE_ASSIGNMENT (( #9520 ) ) ;
#47175=ORIENTED_EDGE ( 'NONE', *, *, #6042, .F. ) ;
#47176=CARTESIAN_POINT ( 'NONE',  ( 5.598654528085805993, 151.3549999999999898, 7.705886871421374629 ) ) ;
#47181=CARTESIAN_POINT ( 'NONE',  ( -9.827790563157511022E-16, 127.4429263765338192, 8.025000000000000355 ) ) ;
#47184=DIRECTION ( 'NONE',  ( -0.000000000000000000, 0.000000000000000000, -1.000000000000000000 ) ) ;
#47188=DIRECTION ( 'NONE',  ( 0.000000000000000000, 0.000000000000000000, 1.000000000000000000 ) ) ;
#47189=ORIENTED_EDGE ( 'NONE', *, *, #1638, .T. ) ;
#47191=CIRCLE ( 'NONE', #59470, 0.5000000000000004441 ) ;
#47196=CIRCLE ( 'NONE', #66915, 1.000000000000000888 ) ;
#47197=EDGE_CURVE ( 'NONE', #2776, #4654, #47694, .T. ) ;
#47198=MECHANICAL_DESIGN_GEOMETRIC_PRESENTATION_REPRESENTATION('',(#42671),#44782);
#47206=( NAMED_UNIT ( * ) SI_UNIT ( $, .STERADIAN. ) SOLID_ANGLE_UNIT ( ) );
#47210=CARTESIAN_POINT ( 'NONE',  ( 34.99999999999992895, 113.4999999999999858, 7.000000000000000000 ) ) ;
#47211=AXIS2_PLACEMENT_3D ( 'NONE', #18375, #11695, #33832 ) ;
#47215=CARTESIAN_POINT ( 'NONE',  ( -74.09163092349538715, 9.403269179647930187, -6.097839204891418063 ) ) ;
#47218=VECTOR ( 'NONE', #57645, 1000.000000000000000 ) ;
#47219=DIRECTION ( 'NONE',  ( 0.000000000000000000, -0.000000000000000000, -1.000000000000000000 ) ) ;
#47220=ADVANCED_FACE ( 'NONE', ( #61567 ), #35572, .F. ) ;
#47221=CARTESIAN_POINT ( 'NONE',  ( 3.094860106618435136, 145.2949999999999875, -9.525000000000000355 ) ) ;
#47223=FILL_AREA_STYLE ('',( #25702 ) ) ;
#47234=DIRECTION ( 'NONE',  ( 1.000000000000000000, 0.000000000000000000, 0.000000000000000000 ) ) ;
#47236=EDGE_CURVE ( 'NONE', #64181, #35564, #61068, .T. ) ;
#47246=CARTESIAN_POINT ( 'NONE',  ( -45.00000000000000000, 9.657020704707438341, 6.241538579429709799 ) ) ;
#47248=CIRCLE ( 'NONE', #32562, 13.99999999999999822 ) ;
#47249=SURFACE_STYLE_FILL_AREA ( #42655 ) ;
#47252=EDGE_LOOP ( 'NONE', ( #48398, #44662, #40852, #12351, #20100, #46296, #27523, #24146, #43326, #6014, #38088, #440, #39188 ) ) ;
#47254=ORIENTED_EDGE ( 'NONE', *, *, #64121, .T. ) ;
#47255=MECHANICAL_DESIGN_GEOMETRIC_PRESENTATION_REPRESENTATION('',(#22511),#21383);
#47256=( GEOMETRIC_REPRESENTATION_CONTEXT ( 3 ) GLOBAL_UNCERTAINTY_ASSIGNED_CONTEXT ( ( #54491 ) ) GLOBAL_UNIT_ASSIGNED_CONTEXT ( ( #15115, #47487, #4494 ) ) REPRESENTATION_CONTEXT ( 'NONE', 'WORKASPACE' ) );
#47259=CARTESIAN_POINT ( 'NONE',  ( 0.000000000000000000, 121.4449999999999790, -9.525000000000000355 ) ) ;
#47262=CARTESIAN_POINT ( 'NONE',  ( 0.000000000000000000, 122.5549999999999784, -9.525000000000000355 ) ) ;
#47264=DIRECTION ( 'NONE',  ( 0.9704308468600219006, -0.2413793103448194366, 0.000000000000000000 ) ) ;
#47266=CARTESIAN_POINT ( 'NONE',  ( 10.01517768586949231, 148.8050000000000068, 1.839758294383810543E-15 ) ) ;
#47267=CIRCLE ( 'NONE', #58469, 9.499999999999998224 ) ;
#47270=SURFACE_STYLE_USAGE ( .BOTH. , #41629 ) ;
#47272=DIRECTION ( 'NONE',  ( 0.000000000000000000, -1.000000000000000000, 0.000000000000000000 ) ) ;
#47273=VERTEX_POINT ( 'NONE', #57715 ) ;
#47277=ORIENTED_EDGE ( 'NONE', *, *, #39354, .T. ) ;
#47278=CARTESIAN_POINT ( 'NONE',  ( 4.559337023122163046, 111.8214503647300688, -6.825287955804331119 ) ) ;
#47280=EDGE_CURVE ( 'NONE', #12316, #9058, #36651, .T. ) ;
#47281=SURFACE_STYLE_FILL_AREA ( #37433 ) ;
#47286=ORIENTED_EDGE ( 'NONE', *, *, #45847, .F. ) ;
#47288=CIRCLE ( 'NONE', #49514, 0.5000000000000003331 ) ;
#47290=STYLED_ITEM ( 'NONE', ( #4887 ), #34548 ) ;
#47292=CARTESIAN_POINT ( 'NONE',  ( -9.058813317711338797, 152.3449999999999704, 2.943386871421373563 ) ) ;
#47301=SURFACE_STYLE_USAGE ( .BOTH. , #51488 ) ;
#47306=CARTESIAN_POINT ( 'NONE',  ( 3.094860106618435136, 118.2949999999999875, -9.525000000000000355 ) ) ;
#47308=AXIS2_PLACEMENT_3D ( 'NONE', #18244, #35112, #19260 ) ;
#47309=CARTESIAN_POINT ( 'NONE',  ( 15.98999599679679839, 146.4999999999999716, -7.000000000000000000 ) ) ;
#47310=MECHANICAL_DESIGN_GEOMETRIC_PRESENTATION_REPRESENTATION('',(#13503),#25859);
#47311=( NAMED_UNIT ( * ) PLANE_ANGLE_UNIT ( ) SI_UNIT ( $, .RADIAN. ) );
#47317=EDGE_CURVE ( 'NONE', #2677, #10181, #32862, .T. ) ;
#47332=PRESENTATION_STYLE_ASSIGNMENT (( #51519 ) ) ;
#47337=CARTESIAN_POINT ( 'NONE',  ( -4.716976649647098618, 143.2570736234661410, 6.492361379858953008 ) ) ;
#47338=FACE_OUTER_BOUND ( 'NONE', #25247, .T. ) ;
#47339=AXIS2_PLACEMENT_3D ( 'NONE', #57759, #5904, #22102 ) ;
#47343=( GEOMETRIC_REPRESENTATION_CONTEXT ( 3 ) GLOBAL_UNCERTAINTY_ASSIGNED_CONTEXT ( ( #25029 ) ) GLOBAL_UNIT_ASSIGNED_CONTEXT ( ( #51102, #66576, #24006 ) ) REPRESENTATION_CONTEXT ( 'NONE', 'WORKASPACE' ) );
#47347=FACE_OUTER_BOUND ( 'NONE', #1796, .T. ) ;
#47350=DIRECTION ( 'NONE',  ( 0.000000000000000000, 0.000000000000000000, -1.000000000000000000 ) ) ;
#47353=B_SPLINE_CURVE_WITH_KNOTS ( 'NONE', 3,
 ( #21401, #58030, #37293, #41512, #47510, #47870, #63965, #4883, #62921, #68928, #5217, #9837 ),
 .UNSPECIFIED., .F., .F.,
 ( 4, 2, 2, 2, 2, 4 ),
 ( 0.000000000000000000, 0.0009390420820170817780, 0.001408563123025622721, 0.001643323643529895524, 0.001760703903782034853, 0.001878084164034174398 ),
 .UNSPECIFIED. ) ;
#47362=ORIENTED_EDGE ( 'NONE', *, *, #14068, .T. ) ;
#47364=EDGE_LOOP ( 'NONE', ( #47362, #30636, #26278, #40406 ) ) ;
#47369=CARTESIAN_POINT ( 'NONE',  ( 8.102448949553181734, 120.9949999999999761, -5.886773742842746238 ) ) ;
#47372=EDGE_CURVE ( 'NONE', #373, #20601, #59819, .T. ) ;
#47373=CARTESIAN_POINT ( 'NONE',  ( 6.826472737025121695, 113.4929263765338021, -4.959722759717905660 ) ) ;
#47374=DIRECTION ( 'NONE',  ( -1.156482317317873451E-16, -1.000000000000000000, 0.000000000000000000 ) ) ;
#47375=PRODUCT ( '2. Support', '2. Support', '', ( #62049 ) ) ;
#47379=DIRECTION ( 'NONE',  ( 0.000000000000000000, -1.000000000000000000, 0.000000000000000000 ) ) ;
#47380=SURFACE_SIDE_STYLE ('',( #36106 ) ) ;
#47381=( GEOMETRIC_REPRESENTATION_CONTEXT ( 3 ) GLOBAL_UNCERTAINTY_ASSIGNED_CONTEXT ( ( #46145 ) ) GLOBAL_UNIT_ASSIGNED_CONTEXT ( ( #5873, #870, #24061 ) ) REPRESENTATION_CONTEXT ( 'NONE', 'WORKASPACE' ) );
#47382=CARTESIAN_POINT ( 'NONE',  ( -60.00000000000000000, -2.024042244987997205E-14, 6.500000000000000000 ) ) ;
#47385=CARTESIAN_POINT ( 'NONE',  ( 71.99999999999998579, 119.9999999999997868, -7.000000000000000000 ) ) ;
#47390=CONICAL_SURFACE ( 'NONE', #2320, 5.000000000000004441, 0.7853981633974587151 ) ;
#47392=MECHANICAL_DESIGN_GEOMETRIC_PRESENTATION_REPRESENTATION('',(#50718),#17043);
#47399=CARTESIAN_POINT ( 'NONE',  ( -1.166476076187854022E-15, 157.0550000000000068, 9.525000000000000355 ) ) ;
#47404=( NAMED_UNIT ( * ) PLANE_ANGLE_UNIT ( ) SI_UNIT ( $, .RADIAN. ) );
#47412=FACE_OUTER_BOUND ( 'NONE', #2149, .T. ) ;
#47415=DIRECTION ( 'NONE',  ( 1.000000000000000000, 0.000000000000000000, 0.000000000000000000 ) ) ;
#47419=DIRECTION ( 'NONE',  ( -0.000000000000000000, 1.000000000000000000, 0.000000000000000000 ) ) ;
#47422=CARTESIAN_POINT ( 'NONE',  ( 2.607480562269076430, 114.9070736234661325, -8.025000000000000355 ) ) ;
#47423=CIRCLE ( 'NONE', #28255, 0.5000000000000006661 ) ;
#47425=CARTESIAN_POINT ( 'NONE',  ( -20.44134218812435932, 115.3860596766049440, 10.00000000000000000 ) ) ;
#47428=MECHANICAL_DESIGN_GEOMETRIC_PRESENTATION_REPRESENTATION('',(#65353),#28263);
#47434=CARTESIAN_POINT ( 'NONE',  ( -8.102448949553181734, 114.6049999999999756, 5.886773742842747126 ) ) ;
#47436=DIRECTION ( 'NONE',  ( 0.000000000000000000, 0.000000000000000000, -1.000000000000000000 ) ) ;
#47440=EDGE_LOOP ( 'NONE', ( #67801, #6696 ) ) ;
#47441=AXIS2_PLACEMENT_3D ( 'NONE', #24976, #46486, #19705 ) ;
#47444=FILL_AREA_STYLE_COLOUR ( '', #25050 ) ;
#47445=UNCERTAINTY_MEASURE_WITH_UNIT (LENGTH_MEASURE( 1.000000000000000082E-05 ), #46314, 'distance_accuracy_value', 'NONE');
#47447=CARTESIAN_POINT ( 'NONE',  ( 6.826472737025121695, 155.4929263765338305, -4.959722759717905660 ) ) ;
#47448=CARTESIAN_POINT ( 'NONE',  ( 14.98999599679679662, 1.797044900979284448E-15, -9.500000000000000000 ) ) ;
#47452=CARTESIAN_POINT ( 'NONE',  ( -20.71231517720797655, 149.4999999999999716, -10.00000000000000000 ) ) ;
#47454=VECTOR ( 'NONE', #49594, 1000.000000000000000 ) ;
#47456=CARTESIAN_POINT ( 'NONE',  ( 20.07572180596747913, 115.0406156812134952, -10.00000000000000000 ) ) ;
#47458=CARTESIAN_POINT ( 'NONE',  ( 20.77867704735745136, 115.1383905251040716, 10.00000000000000000 ) ) ;
#47463=CARTESIAN_POINT ( 'NONE',  ( -72.00000000000000000, 14.49137674618942562, 7.500000000000000000 ) ) ;
#47467=AXIS2_PLACEMENT_3D ( 'NONE', #63492, #63821, #19872 ) ;
#47468=VERTEX_POINT ( 'NONE', #39393 ) ;
#47487=( NAMED_UNIT ( * ) PLANE_ANGLE_UNIT ( ) SI_UNIT ( $, .RADIAN. ) );
#47488=EDGE_CURVE ( 'NONE', #50847, #29858, #20602, .T. ) ;
#47490=CARTESIAN_POINT ( 'NONE',  ( 5.598654528085805993, 124.3549999999999898, 7.705886871421374629 ) ) ;
#47493=CARTESIAN_POINT ( 'NONE',  ( -75.00000000000000000, 9.520518382567221494, -6.450733387540871000 ) ) ;
#47496=( GEOMETRIC_REPRESENTATION_CONTEXT ( 3 ) GLOBAL_UNCERTAINTY_ASSIGNED_CONTEXT ( ( #38453 ) ) GLOBAL_UNIT_ASSIGNED_CONTEXT ( ( #57078, #19798, #9265 ) ) REPRESENTATION_CONTEXT ( 'NONE', 'WORKASPACE' ) );
#47500=VERTEX_POINT ( 'NONE', #44348 ) ;
#47501=DIRECTION ( 'NONE',  ( -0.000000000000000000, -0.000000000000000000, -1.000000000000000000 ) ) ;
#47502=STYLED_ITEM ( 'NONE', ( #33158 ), #28849 ) ;
#47505=( NAMED_UNIT ( * ) PLANE_ANGLE_UNIT ( ) SI_UNIT ( $, .RADIAN. ) );
#47509=ORIENTED_EDGE ( 'NONE', *, *, #23676, .F. ) ;
#47510=CARTESIAN_POINT ( 'NONE',  ( -45.79646929189460280, 8.974048487541155694, -6.364280603494541388 ) ) ;
#47511=DIRECTION ( 'NONE',  ( 0.000000000000000000, 0.000000000000000000, -1.000000000000000000 ) ) ;
#47513=CIRCLE ( 'NONE', #55329, 15.00000000000000000 ) ;
#47515=DIRECTION ( 'NONE',  ( 0.000000000000000000, 0.000000000000000000, 1.000000000000000000 ) ) ;
#47521=ORIENTED_EDGE ( 'NONE', *, *, #47372, .T. ) ;
#47523=CARTESIAN_POINT ( 'NONE',  ( 2.607480562269034241, 129.9070736234661467, -8.025000000000032330 ) ) ;
#47529=CARTESIAN_POINT ( 'NONE',  ( -5.598654528085808657, 152.6449999999999818, 7.705886871421373741 ) ) ;
#47532=STYLED_ITEM ( 'NONE', ( #66782 ), #46513 ) ;
#47533=CARTESIAN_POINT ( 'NONE',  ( 0.000000000000000000, 154.9999999999999716, 10.02499999999997904 ) ) ;
#47534=CARTESIAN_POINT ( 'NONE',  ( 8.102448949553181734, 152.1049999999999613, -5.886773742842746238 ) ) ;
#47537=ORIENTED_EDGE ( 'NONE', *, *, #67414, .T. ) ;
#47538=CARTESIAN_POINT ( 'NONE',  ( 7.632228543268608334, 125.3429263765338249, -2.479861379858951942 ) ) ;
#47542=( GEOMETRIC_REPRESENTATION_CONTEXT ( 3 ) GLOBAL_UNCERTAINTY_ASSIGNED_CONTEXT ( ( #32156 ) ) GLOBAL_UNIT_ASSIGNED_CONTEXT ( ( #29999, #67296, #29297 ) ) REPRESENTATION_CONTEXT ( 'NONE', 'WORKASPACE' ) );
#47543=CARTESIAN_POINT ( 'NONE',  ( 45.65811388298785545, 10.21937129432926916, 6.131267346259030582 ) ) ;
#47544=SURFACE_STYLE_FILL_AREA ( #41537 ) ;
#47546=AXIS2_PLACEMENT_3D ( 'NONE', #44417, #27796, #1388 ) ;
#47551=PRESENTATION_STYLE_ASSIGNMENT (( #20046 ) ) ;
#47554=COLOUR_RGB ( '', 0.31764706, 0.68627451, 0.89019608) ;
#47555=ORIENTED_EDGE ( 'NONE', *, *, #6833, .F. ) ;
#47556=FILL_AREA_STYLE ('',( #52794 ) ) ;
#47563=DIRECTION ( 'NONE',  ( 0.000000000000000000, 1.000000000000000000, 0.000000000000000000 ) ) ;
#47565=EDGE_LOOP ( 'NONE', ( #13392, #13448, #14988, #61745 ) ) ;
#47570=TOROIDAL_SURFACE ( 'NONE', #7083, 16.44999999999999574, 0.5000000000000000000 ) ;
#47572=EDGE_LOOP ( 'NONE', ( #42751, #55970, #64498, #36403 ) ) ;
#47573=CARTESIAN_POINT ( 'NONE',  ( 60.00000000000000000, 1.797044900979284448E-15, 6.999999999999988454 ) ) ;
#47577=EDGE_CURVE ( 'NONE', #61826, #27592, #1365, .T. ) ;
#47579=DIRECTION ( 'NONE',  ( 0.000000000000000000, 0.000000000000000000, -1.000000000000000000 ) ) ;
#47582=( LENGTH_UNIT ( ) NAMED_UNIT ( * ) SI_UNIT ( .MILLI., .METRE. ) );
#47584=( BOUNDED_CURVE ( )  B_SPLINE_CURVE ( 2, ( #14716, #67470, #40774, #25582, #68522, #35477, #63241, #15088, #52009, #51648, #19629 ),
 .UNSPECIFIED., .F., .F. ) 
 B_SPLINE_CURVE_WITH_KNOTS ( ( 3, 2, 2, 2, 2, 3 ),
 ( 0.6176470588235291048, 0.6235294117647055545, 0.6294117647058820042, 0.6352941176470585649, 0.6411764705882351256, 0.6470588235294115753 ),
 .UNSPECIFIED. ) 
 CURVE ( )  GEOMETRIC_REPRESENTATION_ITEM ( )  RATIONAL_B_SPLINE_CURVE ( ( 1.000000000000002665, 0.9510565162951507556, 1.000000000000000000, 0.9510565162951535312, 1.000000000000000000, 0.9510565162951535312, 1.000000000000000000, 0.9510565162951535312, 1.000000000000000000, 0.9510565162951554186, 0.9999999999999981126 ) ) 
 REPRESENTATION_ITEM ( '' )  );
#47585=AXIS2_PLACEMENT_3D ( 'NONE', #50026, #60887, #41550 ) ;
#47588=CARTESIAN_POINT ( 'NONE',  ( -3.094860106618434248, 149.7949999999999875, 9.525000000000000355 ) ) ;
#47593=UNCERTAINTY_MEASURE_WITH_UNIT (LENGTH_MEASURE( 1.000000000000000082E-05 ), #41028, 'distance_accuracy_value', 'NONE');
#47594=DIRECTION ( 'NONE',  ( 0.000000000000000000, -1.000000000000000000, 0.000000000000000000 ) ) ;
#47595=AXIS2_PLACEMENT_3D ( 'NONE', #28940, #32958, #10804 ) ;
#47602=( NAMED_UNIT ( * ) PLANE_ANGLE_UNIT ( ) SI_UNIT ( $, .RADIAN. ) );
#47615=ORIENTED_EDGE ( 'NONE', *, *, #10269, .T. ) ;
#47617=( NAMED_UNIT ( * ) PLANE_ANGLE_UNIT ( ) SI_UNIT ( $, .RADIAN. ) );
#47618=EDGE_LOOP ( 'NONE', ( #47277, #28834, #53442, #67800 ) ) ;
#47620=CARTESIAN_POINT ( 'NONE',  ( 5.598654528085809545, 118.1449999999999818, -7.705886871421373741 ) ) ;
#47621=PRESENTATION_STYLE_ASSIGNMENT (( #32395 ) ) ;
#47624=LINE ( 'NONE', #4636, #17360 ) ;
#47625=CARTESIAN_POINT ( 'NONE',  ( 3.094860106618431583, 121.2049999999999841, 9.525000000000000355 ) ) ;
#47627=DIRECTION ( 'NONE',  ( -1.156482317317873451E-16, -1.000000000000000000, 0.000000000000000000 ) ) ;
#47628=EDGE_LOOP ( 'NONE', ( #46978, #39272, #43879, #68229 ) ) ;
#47629=CARTESIAN_POINT ( 'NONE',  ( -9.058813317711338797, 150.4550000000000125, 2.943386871421373563 ) ) ;
#47630=UNCERTAINTY_MEASURE_WITH_UNIT (LENGTH_MEASURE( 1.000000000000000082E-05 ), #7221, 'distance_accuracy_value', 'NONE');
#47632=CARTESIAN_POINT ( 'NONE',  ( -15.98999599679679839, 117.9999999999999716, 9.500000000000000000 ) ) ;
#47633=CARTESIAN_POINT ( 'NONE',  ( -41.03154609328242941, 107.7014457728230781, 3.191672614837958388 ) ) ;
#47635=DIRECTION ( 'NONE',  ( 0.000000000000000000, 1.000000000000000000, 0.000000000000000000 ) ) ;
#47638=CARTESIAN_POINT ( 'NONE',  ( -74.49999999999998579, 119.9999999999997726, -10.00000000000000000 ) ) ;
#47640=ORIENTED_EDGE ( 'NONE', *, *, #31735, .F. ) ;
#47641=CARTESIAN_POINT ( 'NONE',  ( 8.234833373661283318, 111.3243718155183899, 2.821501943811244750 ) ) ;
#47644=CARTESIAN_POINT ( 'NONE',  ( -72.00000000000000000, 36.32520566882265456, -9.500000000000000000 ) ) ;
#47646=DIRECTION ( 'NONE',  ( -1.156482317317873451E-16, -1.000000000000000000, 0.000000000000000000 ) ) ;
#47650=ORIENTED_EDGE ( 'NONE', *, *, #13920, .T. ) ;
#47657=DIRECTION ( 'NONE',  ( -0.000000000000000000, -0.000000000000000000, -1.000000000000000000 ) ) ;
#47661=CARTESIAN_POINT ( 'NONE',  ( 8.102448949553181734, 150.9950000000000045, -5.886773742842746238 ) ) ;
#47663=EDGE_CURVE ( 'NONE', #7643, #41467, #29535, .T. ) ;
#47664=CARTESIAN_POINT ( 'NONE',  ( 45.00000000000000000, -1.469576158976824618E-14, -9.500000000000000000 ) ) ;
#47666=VERTEX_POINT ( 'NONE', #68525 ) ;
#47667=( NAMED_UNIT ( * ) SI_UNIT ( $, .STERADIAN. ) SOLID_ANGLE_UNIT ( ) );
#47668=( NAMED_UNIT ( * ) SI_UNIT ( $, .STERADIAN. ) SOLID_ANGLE_UNIT ( ) );
#47669=AXIS2_PLACEMENT_3D ( 'NONE', #22475, #50594, #1297 ) ;
#47672=B_SPLINE_CURVE_WITH_KNOTS ( 'NONE', 3,
 ( #62959, #36283, #57705, #9535, #30953, #56662, #3128, #52452, #18997, #18686, #13385, #13745 ),
 .UNSPECIFIED., .F., .F.,
 ( 4, 2, 2, 2, 2, 4 ),
 ( 0.000000000000000000, 0.0001470450322352820696, 0.0002940900644705641393, 0.0005881801289411533237, 0.0008822701934117425622, 0.001176360257882331801 ),
 .UNSPECIFIED. ) ;
#47673=CARTESIAN_POINT ( 'NONE',  ( 0.000000000000000000, 118.4449999999999932, -9.525000000000000355 ) ) ;
#47676=SURFACE_STYLE_USAGE ( .BOTH. , #3255 ) ;
#47677=SURFACE_STYLE_FILL_AREA ( #26142 ) ;
#47678=COLOUR_RGB ( '', 0.08235294, 0.09019608, 0.10196078) ;
#47684=PRESENTATION_STYLE_ASSIGNMENT (( #53916 ) ) ;
#47687=PRESENTATION_STYLE_ASSIGNMENT (( #43089 ) ) ;
#47693=ADVANCED_FACE ( 'NONE', ( #4467 ), #53109, .T. ) ;
#47694=CIRCLE ( 'NONE', #48777, 0.5000000000000004441 ) ;
#47695=CARTESIAN_POINT ( 'NONE',  ( 7.632228543268608334, 147.4570736234661581, -2.479861379858951942 ) ) ;
#47701=SURFACE_STYLE_FILL_AREA ( #56 ) ;
#47702=CARTESIAN_POINT ( 'NONE',  ( -23.71231517720798010, 113.4999999999999858, -7.000000000000000000 ) ) ;
#47705=PRESENTATION_STYLE_ASSIGNMENT (( #40654 ) ) ;
#47706=CARTESIAN_POINT ( 'NONE',  ( -6.826472737025120807, 140.1070736234661354, 4.959722759717906548 ) ) ;
#47707=AXIS2_PLACEMENT_3D ( 'NONE', #17421, #64874, #12437 ) ;
#47708=( BOUNDED_SURFACE ( )  B_SPLINE_SURFACE ( 3, 2, ( 
 ( #46740, #68147, #19933 ),
 ( #62840, #14681, #36151 ),
 ( #57583, #9413, #30835 ),
 ( #25550, #21675, #42158 ),
 ( #53358, #32558, #69188 ),
 ( #58621, #52662, #47786 ),
 ( #47425, #63880, #37910 ),
 ( #31528, #41790, #57947 ),
 ( #68492, #43195, #21317 ),
 ( #27266, #59280, #64231 ) ),
 .UNSPECIFIED., .F., .F., .F. ) 
 B_SPLINE_SURFACE_WITH_KNOTS ( ( 4, 2, 2, 2, 4 ),
 ( 3, 3 ),
 ( 0.0006185862396527136518, 0.001034390655347180218, 0.001450195071041647001, 0.001865999486736113783, 0.002281803902430580566 ),
 ( 0.000000000000000000, 1.000000000000000000 ),
 .UNSPECIFIED. ) 
 GEOMETRIC_REPRESENTATION_ITEM ( )  RATIONAL_B_SPLINE_SURFACE ( (
 ( 1.000000000000000000, 0.8505317485662434729, 1.000000000000000000),
 ( 1.000000000000000000, 0.8505807179912472371, 1.000000000000000000),
 ( 1.000000000000000000, 0.8467906168084839980, 1.000000000000000000),
 ( 1.000000000000000000, 0.8327126069847174961, 1.000000000000000000),
 ( 1.000000000000000000, 0.8223235278808177506, 1.000000000000000000),
 ( 1.000000000000000000, 0.7965633808504525293, 1.000000000000000000),
 ( 1.000000000000000000, 0.7811310880225481590, 1.000000000000000000),
 ( 1.000000000000000000, 0.7464785550193693275, 1.000000000000000000),
 ( 1.000000000000000000, 0.7273804381889640291, 1.000000000000000000),
 ( 1.000000000000000000, 0.7071067811865585639, 1.000000000000000000) ) ) 
 REPRESENTATION_ITEM ( '' )  SURFACE ( )  );
#47712=UNCERTAINTY_MEASURE_WITH_UNIT (LENGTH_MEASURE( 1.000000000000000082E-05 ), #1639, 'distance_accuracy_value', 'NONE');
#47713=LINE ( 'NONE', #64852, #16277 ) ;
#47718=CARTESIAN_POINT ( 'NONE',  ( -9.827790563157511022E-16, 142.4429263765338192, 8.025000000000000355 ) ) ;
#47720=CYLINDRICAL_SURFACE ( 'NONE', #57842, 0.5000000000000004441 ) ;
#47721=( LENGTH_UNIT ( ) NAMED_UNIT ( * ) SI_UNIT ( .MILLI., .METRE. ) );
#47724=CARTESIAN_POINT ( 'NONE',  ( -74.99999999999998579, 50.00000000000000000, -6.500000000000000000 ) ) ;
#47726=VERTEX_POINT ( 'NONE', #63244 ) ;
#47729=CARTESIAN_POINT ( 'NONE',  ( 71.99999999999998579, 64.07124727947029896, 10.00000000000000000 ) ) ;
#47730=EDGE_CURVE ( 'NONE', #5568, #26425, #31562, .T. ) ;
#47732=ORIENTED_EDGE ( 'NONE', *, *, #38801, .T. ) ;
#47737=SURFACE_STYLE_USAGE ( .BOTH. , #9708 ) ;
#47742=EDGE_CURVE ( 'NONE', #52352, #69681, #39006, .T. ) ;
#47743=FACE_OUTER_BOUND ( 'NONE', #20572, .T. ) ;
#47745=FILL_AREA_STYLE ('',( #48067 ) ) ;
#47746=VECTOR ( 'NONE', #6187, 1000.000000000000000 ) ;
#47748=CARTESIAN_POINT ( 'NONE',  ( 9.058813317711337021, 123.5449999999999875, 2.943386871421375783 ) ) ;
#47751=SPHERICAL_SURFACE ( 'NONE', #24567, 0.5000000000000000000 ) ;
#47755=( LENGTH_UNIT ( ) NAMED_UNIT ( * ) SI_UNIT ( .MILLI., .METRE. ) );
#47756=AXIS2_PLACEMENT_3D ( 'NONE', #35531, #61525, #62243 ) ;
#47763=STYLED_ITEM ( 'NONE', ( #27541 ), #56306 ) ;
#47764=CARTESIAN_POINT ( 'NONE',  ( 44.32257855570050253, 10.24209864716914531, -3.524404701560114539 ) ) ;
#47766=DIRECTION ( 'NONE',  ( 1.224646799147353207E-16, 1.000000000000000000, -0.000000000000000000 ) ) ;
#47769=SPHERICAL_SURFACE ( 'NONE', #64999, 0.5000000000000000000 ) ;
#47774=LINE ( 'NONE', #8692, #68598 ) ;
#47781=STYLED_ITEM ( 'NONE', ( #34459 ), #62618 ) ;
#47784=CARTESIAN_POINT ( 'NONE',  ( 0.000000000000000000, 112.0570736234661666, -8.025000000000000355 ) ) ;
#47786=CARTESIAN_POINT ( 'NONE',  ( -20.30219483484659548, 114.9087424184428130, 10.36565267485733877 ) ) ;
#47789=DIRECTION ( 'NONE',  ( 0.000000000000000000, 0.000000000000000000, -1.000000000000000000 ) ) ;
#47790=EDGE_LOOP ( 'NONE', ( #9596, #28079, #61163, #21412 ) ) ;
#47791=ORIENTED_EDGE ( 'NONE', *, *, #11228, .F. ) ;
#47797=VERTEX_POINT ( 'NONE', #6917 ) ;
#47799=CARTESIAN_POINT ( 'NONE',  ( 0.000000000000000000, 122.5549999999999784, -9.525000000000000355 ) ) ;
#47800=DIRECTION ( 'NONE',  ( -1.000000000000000000, 0.000000000000000000, 0.000000000000000000 ) ) ;
#47806=PRESENTATION_STYLE_ASSIGNMENT (( #31545 ) ) ;
#47808=( LENGTH_UNIT ( ) NAMED_UNIT ( * ) SI_UNIT ( .MILLI., .METRE. ) );
#47809=ORIENTED_EDGE ( 'NONE', *, *, #33683, .F. ) ;
#47810=CARTESIAN_POINT ( 'NONE',  ( 2.607480562269076430, 158.7929263765338135, -8.025000000000000355 ) ) ;
#47812=ADVANCED_FACE ( 'NONE', ( #59002 ), #40823, .F. ) ;
#47815=CARTESIAN_POINT ( 'NONE',  ( 20.71462254620879762, 114.5909367637873402, -9.999999999998797406 ) ) ;
#47817=CARTESIAN_POINT ( 'NONE',  ( 8.437984349512095861, 128.1929263765338192, 1.550032578732816828E-15 ) ) ;
#47821=DIRECTION ( 'NONE',  ( 0.000000000000000000, 0.000000000000000000, -1.000000000000000000 ) ) ;
#47824=PRESENTATION_STYLE_ASSIGNMENT (( #10478 ) ) ;
#47826=DIRECTION ( 'NONE',  ( 0.000000000000000000, 1.000000000000000000, 0.000000000000000000 ) ) ;
#47831=( NAMED_UNIT ( * ) PLANE_ANGLE_UNIT ( ) SI_UNIT ( $, .RADIAN. ) );
#47833=MECHANICAL_DESIGN_GEOMETRIC_PRESENTATION_REPRESENTATION('',(#544),#5073);
#47835=ORIENTED_EDGE ( 'NONE', *, *, #10422, .F. ) ;
#47836=( NAMED_UNIT ( * ) PLANE_ANGLE_UNIT ( ) SI_UNIT ( $, .RADIAN. ) );
#47838=FILL_AREA_STYLE_COLOUR ( '', #34098 ) ;
#47840=CARTESIAN_POINT ( 'NONE',  ( -60.00000000000000000, -2.024042244987997205E-14, -10.00000000000000000 ) ) ;
#47842=COLOUR_RGB ( '', 0.72549020, 0.75294118, 0.79215686) ;
#47843=COLOUR_RGB ( '', 0.08235294, 0.09019608, 0.10196078) ;
#47845=ADVANCED_FACE ( 'NONE', ( #23787 ), #61743, .T. ) ;
#47852=CARTESIAN_POINT ( 'NONE',  ( -74.49999999999998579, 36.50926243676796190, -10.00000000000000000 ) ) ;
#47853=AXIS2_PLACEMENT_3D ( 'NONE', #11298, #48636, #37397 ) ;
#47855=CARTESIAN_POINT ( 'NONE',  ( 8.102448949553183510, 131.1049999999999898, -5.886773742842746238 ) ) ;
#47856=CARTESIAN_POINT ( 'NONE',  ( -75.00000000000000000, 9.680295737756338781, -6.198572516085027573 ) ) ;
#47857=( GEOMETRIC_REPRESENTATION_CONTEXT ( 3 ) GLOBAL_UNCERTAINTY_ASSIGNED_CONTEXT ( ( #23549 ) ) GLOBAL_UNIT_ASSIGNED_CONTEXT ( ( #10636, #43041, #5674 ) ) REPRESENTATION_CONTEXT ( 'NONE', 'WORKASPACE' ) );
#47858=DIRECTION ( 'NONE',  ( -1.000000000000000000, 0.000000000000000000, 0.000000000000000000 ) ) ;
#47863=LINE ( 'NONE', #69258, #49425 ) ;
#47864=DIRECTION ( 'NONE',  ( -0.000000000000000000, -0.000000000000000000, -1.000000000000000000 ) ) ;
#47867=CARTESIAN_POINT ( 'NONE',  ( 0.000000000000000000, 136.0570736234661808, -8.025000000000000355 ) ) ;
#47869=ORIENTED_EDGE ( 'NONE', *, *, #51896, .F. ) ;
#47870=CARTESIAN_POINT ( 'NONE',  ( -45.85105955898281138, 9.184648417642959473, -6.276141209865980564 ) ) ;
#47871=( NAMED_UNIT ( * ) PLANE_ANGLE_UNIT ( ) SI_UNIT ( $, .RADIAN. ) );
#47877=CARTESIAN_POINT ( 'NONE',  ( 9.827790563157511022E-16, 87.30187232391182306, -8.025000000000000355 ) ) ;
#47881=AXIS2_PLACEMENT_3D ( 'NONE', #12253, #65742, #60787 ) ;
#47884=EDGE_LOOP ( 'NONE', ( #37131, #67979, #27668, #21078 ) ) ;
#47885=FILL_AREA_STYLE_COLOUR ( '', #17578 ) ;
#47887=DIRECTION ( 'NONE',  ( 0.000000000000000000, 0.000000000000000000, 1.000000000000000000 ) ) ;
#47888=CARTESIAN_POINT ( 'NONE',  ( 5.598654528085809545, 154.1449999999999818, -7.705886871421373741 ) ) ;
#47892=CARTESIAN_POINT ( 'NONE',  ( -10.01517768586949408, 150.3050000000000068, -6.132527647946036459E-16 ) ) ;
#47896=CARTESIAN_POINT ( 'NONE',  ( -2.607480562269075097, 121.2929263765337993, 8.025000000000000355 ) ) ;
#47897=CARTESIAN_POINT ( 'NONE',  ( 20.71231517720798010, 149.9999999999999716, 10.00000000000000000 ) ) ;
#47898=EDGE_CURVE ( 'NONE', #64306, #3150, #66346, .T. ) ;
#47901=LINE ( 'NONE', #38008, #57940 ) ;
#47903=MECHANICAL_DESIGN_GEOMETRIC_PRESENTATION_REPRESENTATION('',(#33229),#27574);
#47904=CARTESIAN_POINT ( 'NONE',  ( -41.06069799967657730, 107.9552192246431730, -3.682425535826299612 ) ) ;
#47907=TOROIDAL_SURFACE ( 'NONE', #1739, 1.000000000000000000, 0.5000000000000000000 ) ;
#47910=CIRCLE ( 'NONE', #20884, 0.5000000000000000000 ) ;
#47914=PRESENTATION_STYLE_ASSIGNMENT (( #28341 ) ) ;
#47924=( NAMED_UNIT ( * ) SI_UNIT ( $, .STERADIAN. ) SOLID_ANGLE_UNIT ( ) );
#47927=AXIS2_PLACEMENT_3D ( 'NONE', #54334, #64888, #33241 ) ;
#47928=CARTESIAN_POINT ( 'NONE',  ( -20.57648123223228254, 110.4999999999999858, 10.27659574468085069 ) ) ;
#47930=CARTESIAN_POINT ( 'NONE',  ( 2.607480562269071989, 125.7070736234661723, 8.025000000000002132 ) ) ;
#47931=AXIS2_PLACEMENT_3D ( 'NONE', #3041, #24205, #34751 ) ;
#47933=CARTESIAN_POINT ( 'NONE',  ( -9.058813317711338797, 152.3449999999999704, 2.943386871421373563 ) ) ;
#47935=DIRECTION ( 'NONE',  ( 0.000000000000000000, 0.000000000000000000, 1.000000000000000000 ) ) ;
#47940=FACE_OUTER_BOUND ( 'NONE', #55740, .T. ) ;
#47941=ORIENTED_EDGE ( 'NONE', *, *, #56530, .F. ) ;
#47944=CARTESIAN_POINT ( 'NONE',  ( 0.000000000000000000, 114.9999999999999574, 16.00000000000000000 ) ) ;
#47946=CARTESIAN_POINT ( 'NONE',  ( -60.00000000000000000, -2.024042244987997205E-14, 10.00000000000000000 ) ) ;
#47947=AXIS2_PLACEMENT_3D ( 'NONE', #43616, #28047, #1965 ) ;
#47953=FILL_AREA_STYLE ('',( #31339 ) ) ;
#47954=CARTESIAN_POINT ( 'NONE',  ( -7.632228543268608334, 117.8429263765338249, 2.479861379858952830 ) ) ;
#47960=ORIENTED_EDGE ( 'NONE', *, *, #35897, .T. ) ;
#47961=SURFACE_STYLE_FILL_AREA ( #53854 ) ;
#47968=CARTESIAN_POINT ( 'NONE',  ( -1.166476076187854022E-15, 116.9449999999999932, 9.525000000000000355 ) ) ;
#47972=CARTESIAN_POINT ( 'NONE',  ( 3.094860106618435136, 125.4049999999999869, -9.525000000000000355 ) ) ;
#47977=VERTEX_POINT ( 'NONE', #36098 ) ;
#47978=CARTESIAN_POINT ( 'NONE',  ( -3.094860106618434248, 150.9050000000000011, 9.525000000000000355 ) ) ;
#47991=( NAMED_UNIT ( * ) PLANE_ANGLE_UNIT ( ) SI_UNIT ( $, .RADIAN. ) );
#47993=ORIENTED_EDGE ( 'NONE', *, *, #24615, .F. ) ;
#47995=MECHANICAL_DESIGN_GEOMETRIC_PRESENTATION_REPRESENTATION('',(#26569),#1819);
#47996=FILL_AREA_STYLE ('',( #26116 ) ) ;
#48001=CARTESIAN_POINT ( 'NONE',  ( -0.5586952923285121164, 154.4720785402125500, -9.525000000000002132 ) ) ;
#48006=( NAMED_UNIT ( * ) PLANE_ANGLE_UNIT ( ) SI_UNIT ( $, .RADIAN. ) );
#48008=DIRECTION ( 'NONE',  ( 1.000000000000000000, 0.000000000000000000, 0.000000000000000000 ) ) ;
#48010=CARTESIAN_POINT ( 'NONE',  ( -10.01517768586949231, 122.1949999999999648, -6.132527647946036459E-16 ) ) ;
#48017=AXIS2_PLACEMENT_3D ( 'NONE', #14121, #51761, #14444 ) ;
#48018=CIRCLE ( 'NONE', #49107, 0.5000000000000004441 ) ;
#48019=EDGE_CURVE ( 'NONE', #15417, #28999, #45430, .T. ) ;
#48023=ORIENTED_EDGE ( 'NONE', *, *, #56594, .F. ) ;
#48026=DIRECTION ( 'NONE',  ( -0.2413793103448194644, 0.9704308468600220117, 0.000000000000000000 ) ) ;
#48029=ADVANCED_FACE ( 'NONE', ( #68443 ), #31612, .T. ) ;
#48034=FILL_AREA_STYLE_COLOUR ( '', #56728 ) ;
#48035=EDGE_CURVE ( 'NONE', #55705, #15297, #52063, .T. ) ;
#48037=CARTESIAN_POINT ( 'NONE',  ( 34.99999999999999289, 99.99999999999998579, 7.500000000000000000 ) ) ;
#48039=CARTESIAN_POINT ( 'NONE',  ( 2.607480562269071989, 143.7070736234661297, 8.025000000000002132 ) ) ;
#48040=EDGE_LOOP ( 'NONE', ( #60443, #51219, #18434, #30959 ) ) ;
#48046=DIRECTION ( 'NONE',  ( -1.000000000000000000, 0.000000000000000000, 0.000000000000000000 ) ) ;
#48048=SURFACE_STYLE_USAGE ( .BOTH. , #11040 ) ;
#48054=DIRECTION ( 'NONE',  ( 1.000000000000000000, 0.000000000000000000, 0.000000000000000000 ) ) ;
#48057=CARTESIAN_POINT ( 'NONE',  ( 12.72792206135785698, 149.9999999999999716, 10.50000000000000000 ) ) ;
#48063=DIRECTION ( 'NONE',  ( -0.000000000000000000, -0.000000000000000000, 1.000000000000000000 ) ) ;
#48066=SURFACE_SIDE_STYLE ('',( #11763 ) ) ;
#48067=FILL_AREA_STYLE_COLOUR ( '', #690 ) ;
#48070=CARTESIAN_POINT ( 'NONE',  ( 5.598654528085809545, 121.1449999999999818, -7.705886871421373741 ) ) ;
#48072=ADVANCED_FACE ( 'NONE', ( #69270 ), #10862, .T. ) ;
#48073=SURFACE_SIDE_STYLE ('',( #11419 ) ) ;
#48081=CARTESIAN_POINT ( 'NONE',  ( 75.00000000000000000, 19.30628705663858469, 6.999999999999999112 ) ) ;
#48084=ORIENTED_EDGE ( 'NONE', *, *, #55554, .T. ) ;
#48085=CARTESIAN_POINT ( 'NONE',  ( 44.99999999999999289, 9.999999999999992895, -4.000000000000000888 ) ) ;
#48086=DIRECTION ( 'NONE',  ( 0.000000000000000000, -1.000000000000000000, 0.000000000000000000 ) ) ;
#48087=CARTESIAN_POINT ( 'NONE',  ( 20.88896767935282739, 150.0000000000000284, -9.626543325103073201 ) ) ;
#48088=UNCERTAINTY_MEASURE_WITH_UNIT (LENGTH_MEASURE( 1.000000000000000082E-05 ), #1634, 'distance_accuracy_value', 'NONE');
#48090=DIRECTION ( 'NONE',  ( 0.000000000000000000, 0.000000000000000000, -1.000000000000000000 ) ) ;
#48092=EDGE_CURVE ( 'NONE', #29444, #8875, #15475, .T. ) ;
#48094=CYLINDRICAL_SURFACE ( 'NONE', #33540, 0.5000000000000004441 ) ;
#48095=DIRECTION ( 'NONE',  ( -7.080503983578803083E-17, -1.000000000000000000, 0.000000000000000000 ) ) ;
#48098=EDGE_CURVE ( 'NONE', #19597, #19879, #47353, .T. ) ;
#48099=VECTOR ( 'NONE', #57383, 1000.000000000000000 ) ;
#48101=VECTOR ( 'NONE', #13836, 999.9999999999998863 ) ;
#48102=AXIS2_PLACEMENT_3D ( 'NONE', #5428, #26554, #58579 ) ;
#48103=DIRECTION ( 'NONE',  ( -0.000000000000000000, -0.000000000000000000, -1.000000000000000000 ) ) ;
#48104=ADVANCED_FACE ( 'NONE', ( #14768 ), #50934, .F. ) ;
#48106=SURFACE_STYLE_USAGE ( .BOTH. , #68843 ) ;
#48108=CARTESIAN_POINT ( 'NONE',  ( 4.716976649647099507, 111.7570736234661553, -6.492361379858953008 ) ) ;
#48112=FILL_AREA_STYLE ('',( #16774 ) ) ;
#48118=EDGE_LOOP ( 'NONE', ( #64987, #47140, #67009 ) ) ;
#48119=CARTESIAN_POINT ( 'NONE',  ( -5.598654528085808657, 123.7549999999999955, 7.705886871421373741 ) ) ;
#48125=CARTESIAN_POINT ( 'NONE',  ( 4.879427070620491413, 154.0600444928449804, -7.674131026540870870 ) ) ;
#48127=DIRECTION ( 'NONE',  ( 0.000000000000000000, 0.000000000000000000, 1.000000000000000000 ) ) ;
#48128=ORIENTED_EDGE ( 'NONE', *, *, #66120, .F. ) ;
#48129=CARTESIAN_POINT ( 'NONE',  ( -7.632228543268607446, 159.5429263765338419, -2.479861379858953718 ) ) ;
#48130=DIRECTION ( 'NONE',  ( 0.000000000000000000, 0.000000000000000000, -1.000000000000000000 ) ) ;
#48131=SURFACE_SIDE_STYLE ('',( #42506 ) ) ;
#48132=CARTESIAN_POINT ( 'NONE',  ( 20.48327417467292832, 114.7638625681370002, -10.30663925914721268 ) ) ;
#48135=( LENGTH_UNIT ( ) NAMED_UNIT ( * ) SI_UNIT ( .MILLI., .METRE. ) );
#48140=EDGE_CURVE ( 'NONE', #12229, #53126, #59751, .T. ) ;
#48143=CARTESIAN_POINT ( 'NONE',  ( 71.62068965517238439, 63.58603185604027885, 7.500000000000000000 ) ) ;
#48146=VERTEX_POINT ( 'NONE', #17547 ) ;
#48150=( LENGTH_UNIT ( ) NAMED_UNIT ( * ) SI_UNIT ( .MILLI., .METRE. ) );
#48153=SURFACE_SIDE_STYLE ('',( #5186 ) ) ;
#48157=ORIENTED_EDGE ( 'NONE', *, *, #52356, .F. ) ;
#48160=EDGE_CURVE ( 'NONE', #62390, #58089, #18366, .T. ) ;
#48161=FACE_OUTER_BOUND ( 'NONE', #62148, .T. ) ;
#48162=EDGE_CURVE ( 'NONE', #55582, #36075, #38323, .T. ) ;
#48166=CARTESIAN_POINT ( 'NONE',  ( -75.00479156420786353, 35.98735966460310465, -9.505900230725330857 ) ) ;
#48170=CARTESIAN_POINT ( 'NONE',  ( -8.102448949553181734, 138.0049999999999670, -5.886773742842749790 ) ) ;
#48173=DIRECTION ( 'NONE',  ( -0.000000000000000000, -1.000000000000000000, 0.000000000000000000 ) ) ;
#48174=UNCERTAINTY_MEASURE_WITH_UNIT (LENGTH_MEASURE( 1.000000000000000082E-05 ), #55580, 'distance_accuracy_value', 'NONE');
#48176=EDGE_LOOP ( 'NONE', ( #3576, #21632, #32053, #41227 ) ) ;
#48177=ADVANCED_FACE ( 'NONE', ( #37987 ), #1463, .T. ) ;
#48179=CARTESIAN_POINT ( 'NONE',  ( -6.826472737025120807, 132.3929263765338362, -4.959722759717907437 ) ) ;
#48180=ADVANCED_FACE ( 'NONE', ( #43276 ), #901, .F. ) ;
#48181=VECTOR ( 'NONE', #7104, 1000.000000000000000 ) ;
#48188=UNCERTAINTY_MEASURE_WITH_UNIT (LENGTH_MEASURE( 1.000000000000000082E-05 ), #52735, 'distance_accuracy_value', 'NONE');
#48190=CARTESIAN_POINT ( 'NONE',  ( -45.00000000000000000, 7.768687147774684831, -6.999999999999999112 ) ) ;
#48194=CARTESIAN_POINT ( 'NONE',  ( 4.716976649647096842, 139.7429263765338305, 6.492361379858953896 ) ) ;
#48195=VERTEX_POINT ( 'NONE', #60079 ) ;
#48199=CARTESIAN_POINT ( 'NONE',  ( 19.89974874213240597, 115.4999999999999574, -10.00000000000000000 ) ) ;
#48200=VERTEX_POINT ( 'NONE', #54780 ) ;
#48202=AXIS2_PLACEMENT_3D ( 'NONE', #48704, #6426, #49047 ) ;
#48203=ADVANCED_FACE ( 'NONE', ( #44308 ), #37539, .T. ) ;
#48204=CARTESIAN_POINT ( 'NONE',  ( 3.094860106618431583, 153.0949999999999989, 9.525000000000000355 ) ) ;
#48205=FILL_AREA_STYLE_COLOUR ( '', #45315 ) ;
#48206=ORIENTED_EDGE ( 'NONE', *, *, #45843, .T. ) ;
#48211=CARTESIAN_POINT ( 'NONE',  ( -2.607480562269073765, 123.0929263765338106, -8.025000000000000355 ) ) ;
#48212=CARTESIAN_POINT ( 'NONE',  ( -9.827790563157511022E-16, 139.4429263765338192, 8.025000000000000355 ) ) ;
#48213=UNCERTAINTY_MEASURE_WITH_UNIT (LENGTH_MEASURE( 1.000000000000000082E-05 ), #86, 'distance_accuracy_value', 'NONE');
#48214=AXIS2_PLACEMENT_3D ( 'NONE', #15105, #56937, #4133 ) ;
#48225=CIRCLE ( 'NONE', #63879, 0.5000000000000004441 ) ;
#48227=CARTESIAN_POINT ( 'NONE',  ( 41.84210526315787604, 107.2928455055531458, 3.500000000000011102 ) ) ;
#48228=( NAMED_UNIT ( * ) SI_UNIT ( $, .STERADIAN. ) SOLID_ANGLE_UNIT ( ) );
#48231=DIRECTION ( 'NONE',  ( -1.000000000000000000, -1.387778780781444256E-14, 0.000000000000000000 ) ) ;
#48234=ORIENTED_EDGE ( 'NONE', *, *, #31777, .T. ) ;
#48238=CARTESIAN_POINT ( 'NONE',  ( -15.98999599679679839, 117.9999999999999716, -7.000000000000000000 ) ) ;
#48239=STYLED_ITEM ( 'NONE', ( #2251 ), #4435 ) ;
#48241=EDGE_CURVE ( 'NONE', #15321, #61387, #67430, .T. ) ;
#48242=CARTESIAN_POINT ( 'NONE',  ( -34.99999999999999289, 99.99999999999998579, 10.00000000000000000 ) ) ;
#48244=AXIS2_PLACEMENT_3D ( 'NONE', #66844, #55219, #29163 ) ;
#48245=AXIS2_PLACEMENT_3D ( 'NONE', #55648, #19391, #67593 ) ;
#48248=CARTESIAN_POINT ( 'NONE',  ( 9.058813317711338797, 156.8449999999999704, -2.943386871421372675 ) ) ;
#48253=DIRECTION ( 'NONE',  ( 1.000000000000000000, 0.000000000000000000, 0.000000000000000000 ) ) ;
#48260=CARTESIAN_POINT ( 'NONE',  ( -72.49999999999998579, 119.9999999999997868, -10.00000000000000000 ) ) ;
#48261=EDGE_CURVE ( 'NONE', #20470, #22693, #64449, .T. ) ;
#48265=ORIENTED_EDGE ( 'NONE', *, *, #41743, .T. ) ;
#48268=CIRCLE ( 'NONE', #42651, 0.5000000000000004441 ) ;
#48269=CARTESIAN_POINT ( 'NONE',  ( -45.88781401545035266, 9.325134922070681398, 6.185423913763131942 ) ) ;
#48277=ORIENTED_EDGE ( 'NONE', *, *, #54620, .F. ) ;
#48284=CARTESIAN_POINT ( 'NONE',  ( 5.598654528085809545, 124.1449999999999960, -7.705886871421373741 ) ) ;
#48285=LINE ( 'NONE', #59475, #9292 ) ;
#48286=( GEOMETRIC_REPRESENTATION_CONTEXT ( 3 ) GLOBAL_UNCERTAINTY_ASSIGNED_CONTEXT ( ( #67732 ) ) GLOBAL_UNIT_ASSIGNED_CONTEXT ( ( #9636, #62381, #25775 ) ) REPRESENTATION_CONTEXT ( 'NONE', 'WORKASPACE' ) );
#48289=ORIENTED_EDGE ( 'NONE', *, *, #31423, .F. ) ;
#48290=CARTESIAN_POINT ( 'NONE',  ( 9.058813317711337021, 118.6549999999999869, 2.943386871421375783 ) ) ;
#48294=DIRECTION ( 'NONE',  ( -0.000000000000000000, 1.000000000000000000, -0.000000000000000000 ) ) ;
#48296=CARTESIAN_POINT ( 'NONE',  ( 3.094860106618435136, 143.4049999999999443, -9.525000000000000355 ) ) ;
#48297=SURFACE_SIDE_STYLE ('',( #30397 ) ) ;
#48299=AXIS2_PLACEMENT_3D ( 'NONE', #23148, #12205, #66032 ) ;
#48300=DIRECTION ( 'NONE',  ( -0.000000000000000000, -0.000000000000000000, 1.000000000000000000 ) ) ;
#48301=CARTESIAN_POINT ( 'NONE',  ( 20.57648123223239622, 114.4999999999999574, 10.27659574468085246 ) ) ;
#48305=DIRECTION ( 'NONE',  ( 0.000000000000000000, -0.000000000000000000, 1.000000000000000000 ) ) ;
#48311=FACE_OUTER_BOUND ( 'NONE', #25681, .T. ) ;
#48312=CYLINDRICAL_SURFACE ( 'NONE', #44258, 0.5000000000000004441 ) ;
#48326=FACE_OUTER_BOUND ( 'NONE', #38011, .T. ) ;
#48329=EDGE_LOOP ( 'NONE', ( #5325, #63487, #58371, #10472 ) ) ;
#48332=FILL_AREA_STYLE ('',( #11341 ) ) ;
#48333=DIRECTION ( 'NONE',  ( 0.000000000000000000, 0.000000000000000000, 1.000000000000000000 ) ) ;
#48335=ADVANCED_FACE ( 'NONE', ( #25218 ), #51969, .F. ) ;
#48336=CARTESIAN_POINT ( 'NONE',  ( -9.058813317711338797, 116.3449999999999847, 2.943386871421373563 ) ) ;
#48349=CARTESIAN_POINT ( 'NONE',  ( 0.000000000000000000, 87.30187232391182306, 0.000000000000000000 ) ) ;
#48351=DIRECTION ( 'NONE',  ( 0.000000000000000000, 0.000000000000000000, 1.000000000000000000 ) ) ;
#48352=DIRECTION ( 'NONE',  ( -0.2413793103448194644, -0.9704308468600220117, 0.000000000000000000 ) ) ;
#48353=CYLINDRICAL_SURFACE ( 'NONE', #49519, 0.5000000000000004441 ) ;
#48357=CARTESIAN_POINT ( 'NONE',  ( -75.00000000000000000, 67.00000000000000000, 6.500000000000000000 ) ) ;
#48361=( LENGTH_UNIT ( ) NAMED_UNIT ( * ) SI_UNIT ( .MILLI., .METRE. ) );
#48362=CARTESIAN_POINT ( 'NONE',  ( -44.99999999999977263, 147.4999999999999716, 9.500000000000000000 ) ) ;
#48368=( LENGTH_UNIT ( ) NAMED_UNIT ( * ) SI_UNIT ( .MILLI., .METRE. ) );
#48369=( GEOMETRIC_REPRESENTATION_CONTEXT ( 3 ) GLOBAL_UNCERTAINTY_ASSIGNED_CONTEXT ( ( #56610 ) ) GLOBAL_UNIT_ASSIGNED_CONTEXT ( ( #54495, #37691, #48581 ) ) REPRESENTATION_CONTEXT ( 'NONE', 'WORKASPACE' ) );
#48370=( NAMED_UNIT ( * ) SI_UNIT ( $, .STERADIAN. ) SOLID_ANGLE_UNIT ( ) );
#48371=CARTESIAN_POINT ( 'NONE',  ( -7.632228543268608334, 142.9570736234661581, 2.479861379858952830 ) ) ;
#48372=VERTEX_POINT ( 'NONE', #65273 ) ;
#48374=CARTESIAN_POINT ( 'NONE',  ( 44.50000000000000000, 10.36037961002804408, -3.500000000000000000 ) ) ;
#48376=UNCERTAINTY_MEASURE_WITH_UNIT (LENGTH_MEASURE( 1.000000000000000082E-05 ), #64071, 'distance_accuracy_value', 'NONE');
#48385=ORIENTED_EDGE ( 'NONE', *, *, #33742, .F. ) ;
#48387=VECTOR ( 'NONE', #62583, 1000.000000000000000 ) ;
#48388=EDGE_LOOP ( 'NONE', ( #7183, #67382, #12153, #17150 ) ) ;
#48389=DIRECTION ( 'NONE',  ( -1.000000000000000000, 0.000000000000000000, -0.000000000000000000 ) ) ;
#48390=DIRECTION ( 'NONE',  ( -1.000000000000000000, 0.000000000000000000, 0.000000000000000000 ) ) ;
#48394=SURFACE_STYLE_FILL_AREA ( #39215 ) ;
#48395=FILL_AREA_STYLE_COLOUR ( '', #47171 ) ;
#48396=( NAMED_UNIT ( * ) PLANE_ANGLE_UNIT ( ) SI_UNIT ( $, .RADIAN. ) );
#48398=ORIENTED_EDGE ( 'NONE', *, *, #5614, .F. ) ;
#48403=CARTESIAN_POINT ( 'NONE',  ( -45.00000000000000000, -1.469576158976824302E-14, -9.500000000000000000 ) ) ;
#48407=CARTESIAN_POINT ( 'NONE',  ( -1.166476076187854022E-15, 125.9449999999999790, 9.525000000000000355 ) ) ;
#48413=MECHANICAL_DESIGN_GEOMETRIC_PRESENTATION_REPRESENTATION('',(#57366),#15863);
#48415=EDGE_CURVE ( 'NONE', #44000, #6894, #6510, .T. ) ;
#48417=FILL_AREA_STYLE_COLOUR ( '', #40345 ) ;
#48419=EDGE_CURVE ( 'NONE', #26152, #320, #13970, .T. ) ;
#48420=( NAMED_UNIT ( * ) SI_UNIT ( $, .STERADIAN. ) SOLID_ANGLE_UNIT ( ) );
#48421=FACE_OUTER_BOUND ( 'NONE', #33365, .T. ) ;
#48426=EDGE_CURVE ( 'NONE', #27627, #65906, #59643, .T. ) ;
#48428=CARTESIAN_POINT ( 'NONE',  ( 45.00050070149897152, 10.00016690049880630, -3.905286714425280969 ) ) ;
#48431=EDGE_CURVE ( 'NONE', #46789, #40883, #16769, .T. ) ;
#48432=DIRECTION ( 'NONE',  ( 0.000000000000000000, -1.000000000000000000, 0.000000000000000000 ) ) ;
#48435=( LENGTH_UNIT ( ) NAMED_UNIT ( * ) SI_UNIT ( .MILLI., .METRE. ) );
#48436=FILL_AREA_STYLE ('',( #41768 ) ) ;
#48437=CARTESIAN_POINT ( 'NONE',  ( 5.696827471326748160, 152.9267479045095968, 5.780458086807691132 ) ) ;
#48439=DIRECTION ( 'NONE',  ( 0.000000000000000000, 0.000000000000000000, 1.000000000000000000 ) ) ;
#48448=CARTESIAN_POINT ( 'NONE',  ( -6.826472737025120807, 138.3929263765338078, -4.959722759717907437 ) ) ;
#48450=ORIENTED_EDGE ( 'NONE', *, *, #41004, .T. ) ;
#48452=CARTESIAN_POINT ( 'NONE',  ( -9.827790563157511022E-16, 113.5570736234661666, 8.025000000000000355 ) ) ;
#48455=CARTESIAN_POINT ( 'NONE',  ( 74.99999999999998579, 19.99999999996227018, -6.081205180447406100 ) ) ;
#48462=CARTESIAN_POINT ( 'NONE',  ( 8.102448949553181734, 127.5049999999999812, 5.886773742842750679 ) ) ;
#48466=VERTEX_POINT ( 'NONE', #66673 ) ;
#48467=CARTESIAN_POINT ( 'NONE',  ( 8.336895043469018773, 153.3467911821693690, 0.8633023660745396954 ) ) ;
#48469=STYLED_ITEM ( 'NONE', ( #16580 ), #12139 ) ;
#48471=ORIENTED_EDGE ( 'NONE', *, *, #27479, .T. ) ;
#48472=DIRECTION ( 'NONE',  ( -1.596582957076307996E-15, -1.000000000000000000, -0.000000000000000000 ) ) ;
#48476=FILL_AREA_STYLE_COLOUR ( '', #45783 ) ;
#48479=ORIENTED_EDGE ( 'NONE', *, *, #43895, .T. ) ;
#48483=FILL_AREA_STYLE_COLOUR ( '', #60098 ) ;
#48485=EDGE_CURVE ( 'NONE', #62454, #45809, #42361, .T. ) ;
#48490=CARTESIAN_POINT ( 'NONE',  ( -1.085428990800084259, 154.1022378970840236, 9.078527738363963095 ) ) ;
#48494=( LENGTH_UNIT ( ) NAMED_UNIT ( * ) SI_UNIT ( .MILLI., .METRE. ) );
#48501=DIRECTION ( 'NONE',  ( 0.000000000000000000, -0.7071067811865647812, -0.7071067811865302533 ) ) ;
#48507=FILL_AREA_STYLE ('',( #27326 ) ) ;
#48512=SURFACE_SIDE_STYLE ('',( #64655 ) ) ;
#48513=CARTESIAN_POINT ( 'NONE',  ( -75.01967246898638564, 35.97479162478882131, -9.552766844405001123 ) ) ;
#48515=CARTESIAN_POINT ( 'NONE',  ( -3.094860106618434248, 141.9050000000000011, 9.525000000000000355 ) ) ;
#48516=B_SPLINE_CURVE_WITH_KNOTS ( 'NONE', 3,
 ( #64002, #41909, #21437, #15849, #15506, #47904, #31647, #31287, #63322, #58062 ),
 .UNSPECIFIED., .F., .F.,
 ( 4, 2, 2, 2, 4 ),
 ( 0.000000000000000000, 0.0004658606356703480804, 0.0009317212713406961607, 0.001397581907011044133, 0.001863442542681392321 ),
 .UNSPECIFIED. ) ;
#48519=MECHANICAL_DESIGN_GEOMETRIC_PRESENTATION_REPRESENTATION('',(#9184),#49600);
#48524=AXIS2_PLACEMENT_3D ( 'NONE', #11171, #1606, #32616 ) ;
#48527=AXIS2_PLACEMENT_3D ( 'NONE', #68036, #52210, #31060 ) ;
#48528=MECHANICAL_DESIGN_GEOMETRIC_PRESENTATION_REPRESENTATION('',(#39531),#5790);
#48529=PRESENTATION_STYLE_ASSIGNMENT (( #17208 ) ) ;
#48534=CYLINDRICAL_SURFACE ( 'NONE', #23038, 18.00000000000000355 ) ;
#48536=( GEOMETRIC_REPRESENTATION_CONTEXT ( 3 ) GLOBAL_UNCERTAINTY_ASSIGNED_CONTEXT ( ( #11622 ) ) GLOBAL_UNIT_ASSIGNED_CONTEXT ( ( #21426, #68948, #36963 ) ) REPRESENTATION_CONTEXT ( 'NONE', 'WORKASPACE' ) );
#48537=( NAMED_UNIT ( * ) PLANE_ANGLE_UNIT ( ) SI_UNIT ( $, .RADIAN. ) );
#48538=CYLINDRICAL_SURFACE ( 'NONE', #33721, 0.5000000000000004441 ) ;
#48539=EDGE_CURVE ( 'NONE', #41467, #7942, #57777, .T. ) ;
#48540=( NAMED_UNIT ( * ) SI_UNIT ( $, .STERADIAN. ) SOLID_ANGLE_UNIT ( ) );
#48547=CARTESIAN_POINT ( 'NONE',  ( 7.632228543268607446, 129.1570736234661467, 2.479861379858954606 ) ) ;
#48550=DIRECTION ( 'NONE',  ( 1.000000000000000000, 0.000000000000000000, 0.000000000000000000 ) ) ;
#48554=CARTESIAN_POINT ( 'NONE',  ( 3.094860106618435136, 160.2949999999999875, -9.525000000000000355 ) ) ;
#48557=DIRECTION ( 'NONE',  ( -0.6363636363636377968, -0.000000000000000000, -0.7713892158398687471 ) ) ;
#48558=CARTESIAN_POINT ( 'NONE',  ( -74.99999999999998579, 50.00000000000000000, 11.50000000000000000 ) ) ;
#48561=ORIENTED_EDGE ( 'NONE', *, *, #21284, .T. ) ;
#48562=CARTESIAN_POINT ( 'NONE',  ( 6.826472737025119919, 121.8929263765338220, 4.959722759717908325 ) ) ;
#48564=VECTOR ( 'NONE', #48389, 1000.000000000000000 ) ;
#48566=CARTESIAN_POINT ( 'NONE',  ( -65.00000000000000000, -1.962809905030629631E-14, -12.00000000000000000 ) ) ;
#48567=ADVANCED_FACE ( 'NONE', ( #56450 ), #42108, .F. ) ;
#48570=VERTEX_POINT ( 'NONE', #19507 ) ;
#48572=SURFACE_STYLE_FILL_AREA ( #33051 ) ;
#48574=( GEOMETRIC_REPRESENTATION_CONTEXT ( 3 ) GLOBAL_UNCERTAINTY_ASSIGNED_CONTEXT ( ( #48174 ) ) GLOBAL_UNIT_ASSIGNED_CONTEXT ( ( #55580, #39788, #29167 ) ) REPRESENTATION_CONTEXT ( 'NONE', 'WORKASPACE' ) );
#48576=( LENGTH_UNIT ( ) NAMED_UNIT ( * ) SI_UNIT ( .MILLI., .METRE. ) );
#48577=CARTESIAN_POINT ( 'NONE',  ( -74.99999999999998579, 50.00000000000000000, -10.00000000000000000 ) ) ;
#48579=CARTESIAN_POINT ( 'NONE',  ( -6.826472737025120807, 116.1070736234661496, 4.959722759717906548 ) ) ;
#48580=SURFACE_SIDE_STYLE ('',( #43645 ) ) ;
#48581=( NAMED_UNIT ( * ) SI_UNIT ( $, .STERADIAN. ) SOLID_ANGLE_UNIT ( ) );
#48582=ORIENTED_EDGE ( 'NONE', *, *, #28707, .F. ) ;
#48586=DIRECTION ( 'NONE',  ( 1.000000000000000000, -0.000000000000000000, -0.000000000000000000 ) ) ;
#48590=CARTESIAN_POINT ( 'NONE',  ( 12.72792206135785875, 1.797044900979284448E-15, 10.00000000000000000 ) ) ;
#48595=COLOUR_RGB ( '', 0.08235294, 0.09019608, 0.10196078) ;
#48596=CARTESIAN_POINT ( 'NONE',  ( -45.00000000000000000, -1.469576158976824302E-14, 6.999999999999999112 ) ) ;
#48599=STYLED_ITEM ( 'NONE', ( #9263 ), #54849 ) ;
#48600=DIRECTION ( 'NONE',  ( 1.000000000000000000, 0.000000000000000000, 0.000000000000000000 ) ) ;
#48602=CARTESIAN_POINT ( 'NONE',  ( -34.99999999999992895, 112.4999999999999858, 9.500000000000000000 ) ) ;
#48608=CARTESIAN_POINT ( 'NONE',  ( 3.094860106618431583, 112.2049999999999841, 9.525000000000000355 ) ) ;
#48610=VECTOR ( 'NONE', #61164, 1000.000000000000000 ) ;
#48611=( NAMED_UNIT ( * ) PLANE_ANGLE_UNIT ( ) SI_UNIT ( $, .RADIAN. ) );
#48612=CARTESIAN_POINT ( 'NONE',  ( -23.21231517720797655, 117.9999999999999716, 9.500000000000000000 ) ) ;
#48620=( NAMED_UNIT ( * ) SI_UNIT ( $, .STERADIAN. ) SOLID_ANGLE_UNIT ( ) );
#48625=ORIENTED_EDGE ( 'NONE', *, *, #65434, .F. ) ;
#48627=DIRECTION ( 'NONE',  ( -0.000000000000000000, -0.000000000000000000, -1.000000000000000000 ) ) ;
#48629=CARTESIAN_POINT ( 'NONE',  ( -45.00000000000000000, 8.841134989786979759, 6.848475133234977363 ) ) ;
#48630=AXIS2_PLACEMENT_3D ( 'NONE', #55066, #32573, #64612 ) ;
#48635=CARTESIAN_POINT ( 'NONE',  ( 60.00000000000000000, 1.797044900979284448E-15, 9.500000000000000000 ) ) ;
#48636=DIRECTION ( 'NONE',  ( -0.000000000000000000, 1.000000000000000000, -0.000000000000000000 ) ) ;
#48641=CARTESIAN_POINT ( 'NONE',  ( -3.094860106618434248, 134.7949999999999875, 9.525000000000000355 ) ) ;
#48643=ORIENTED_EDGE ( 'NONE', *, *, #67258, .F. ) ;
#48646=CARTESIAN_POINT ( 'NONE',  ( 8.102448949553181734, 134.1049999999999329, -5.886773742842746238 ) ) ;
#48649=LINE ( 'NONE', #348, #16147 ) ;
#48650=ORIENTED_EDGE ( 'NONE', *, *, #62836, .T. ) ;
#48651=CARTESIAN_POINT ( 'NONE',  ( -3.094860106618432471, 152.7049999999999841, -9.525000000000000355 ) ) ;
#48652=ADVANCED_FACE ( 'NONE', ( #42414 ), #63802, .F. ) ;
#48653=CARTESIAN_POINT ( 'NONE',  ( -75.00000000000000000, -2.215169945516535778E-14, -7.000000000000000888 ) ) ;
#48654=ADVANCED_FACE ( 'NONE', ( #35706 ), #33199, .T. ) ;
#48668=CARTESIAN_POINT ( 'NONE',  ( 0.000000000000000000, 114.9999999999999574, 0.000000000000000000 ) ) ;
#48669=SURFACE_STYLE_FILL_AREA ( #64798 ) ;
#48671=VERTEX_POINT ( 'NONE', #21592 ) ;
#48673=CARTESIAN_POINT ( 'NONE',  ( -45.91547274654412547, 9.430195758660492089, -3.559962078525838347 ) ) ;
#48674=( NAMED_UNIT ( * ) SI_UNIT ( $, .STERADIAN. ) SOLID_ANGLE_UNIT ( ) );
#48677=CARTESIAN_POINT ( 'NONE',  ( 45.50000000000000000, 1.797044900979284448E-15, -10.00000000000000000 ) ) ;
#48678=CARTESIAN_POINT ( 'NONE',  ( -4.716976649647098618, 112.1429263765338220, 6.492361379858953008 ) ) ;
#48679=CARTESIAN_POINT ( 'NONE',  ( 6.826472737025121695, 144.6070736234661354, -4.959722759717905660 ) ) ;
#48680=DIRECTION ( 'NONE',  ( 1.000000000000000000, 0.000000000000000000, 0.000000000000000000 ) ) ;
#48682=FILL_AREA_STYLE_COLOUR ( '', #19039 ) ;
#48683=ORIENTED_EDGE ( 'NONE', *, *, #26464, .F. ) ;
#48687=CARTESIAN_POINT ( 'NONE',  ( -3.094860106618432471, 130.5949999999999989, -9.525000000000000355 ) ) ;
#48699=AXIS2_PLACEMENT_3D ( 'NONE', #11311, #32081, #21883 ) ;
#48700=CARTESIAN_POINT ( 'NONE',  ( 0.000000000000000000, 109.9999999999999858, 0.000000000000000000 ) ) ;
#48701=STYLED_ITEM ( 'NONE', ( #20244 ), #19473 ) ;
#48704=CARTESIAN_POINT ( 'NONE',  ( -71.49999999999998579, 64.07124727947029896, -7.500000000000000000 ) ) ;
#48706=ORIENTED_EDGE ( 'NONE', *, *, #20186, .T. ) ;
#48713=DIRECTION ( 'NONE',  ( 0.000000000000000000, 0.000000000000000000, 1.000000000000000000 ) ) ;
#48715=ORIENTED_EDGE ( 'NONE', *, *, #25876, .T. ) ;
#48720=EDGE_CURVE ( 'NONE', #65093, #7834, #1615, .T. ) ;
#48723=AXIS2_PLACEMENT_3D ( 'NONE', #16170, #28383, #6590 ) ;
#48725=CARTESIAN_POINT ( 'NONE',  ( 7.632228543268608334, 138.4570736234661581, -2.479861379858951942 ) ) ;
#48737=PRESENTATION_STYLE_ASSIGNMENT (( #32167 ) ) ;
#48744=CARTESIAN_POINT ( 'NONE',  ( -45.00000000000000000, 9.371995676438096723, -6.584629826274035480 ) ) ;
#48746=VERTEX_POINT ( 'NONE', #37487 ) ;
#48747=SURFACE_STYLE_FILL_AREA ( #54657 ) ;
#48750=ADVANCED_FACE ( 'NONE', ( #21956 ), #24113, .F. ) ;
#48751=VECTOR ( 'NONE', #44301, 1000.000000000000000 ) ;
#48752=CARTESIAN_POINT ( 'NONE',  ( -23.71231517720798010, 113.4999999999999858, 10.00000000000000000 ) ) ;
#48760=CARTESIAN_POINT ( 'NONE',  ( -3.094860106618434248, 131.7949999999999875, 9.525000000000000355 ) ) ;
#48762=AXIS2_PLACEMENT_3D ( 'NONE', #33405, #33733, #13314 ) ;
#48766=FACE_OUTER_BOUND ( 'NONE', #15353, .T. ) ;
#48769=CARTESIAN_POINT ( 'NONE',  ( -47.50000000000000000, 13.41640786499872284, 10.00000000000000000 ) ) ;
#48776=CARTESIAN_POINT ( 'NONE',  ( 72.00000000000000000, 35.92875272052971525, -9.500000000000000000 ) ) ;
#48777=AXIS2_PLACEMENT_3D ( 'NONE', #61251, #46148, #34858 ) ;
#48778=PRESENTATION_STYLE_ASSIGNMENT (( #21291 ) ) ;
#48782=SURFACE_SIDE_STYLE ('',( #5447 ) ) ;
#48783=FILL_AREA_STYLE_COLOUR ( '', #60146 ) ;
#48789=FILL_AREA_STYLE_COLOUR ( '', #28137 ) ;
#48791=SURFACE_STYLE_FILL_AREA ( #5816 ) ;
#48792=AXIS2_PLACEMENT_3D ( 'NONE', #31277, #25660, #36271 ) ;
#48797=CARTESIAN_POINT ( 'NONE',  ( 0.000000000000000000, 137.9429263765338192, -8.025000000000000355 ) ) ;
#48799=FILL_AREA_STYLE ('',( #27261 ) ) ;
#48801=TOROIDAL_SURFACE ( 'NONE', #54324, 22.50000000000000000, 0.5000000000000000000 ) ;
#48802=CARTESIAN_POINT ( 'NONE',  ( -7.632228543268607446, 112.6570736234661609, -2.479861379858953718 ) ) ;
#48805=CARTESIAN_POINT ( 'NONE',  ( 20.71231517720797655, 149.4999999999999716, 10.00000000000000000 ) ) ;
#48806=CARTESIAN_POINT ( 'NONE',  ( 4.716976649647099507, 138.7570736234661695, -6.492361379858953008 ) ) ;
#48809=EDGE_LOOP ( 'NONE', ( #25374, #42099, #14189, #19310 ) ) ;
#48815=CARTESIAN_POINT ( 'NONE',  ( -9.058813317711338797, 129.4549999999999841, 2.943386871421373563 ) ) ;
#48819=MECHANICAL_DESIGN_GEOMETRIC_PRESENTATION_REPRESENTATION('',(#44307),#55493);
#48821=CARTESIAN_POINT ( 'NONE',  ( -9.827790563157511022E-16, 133.4429263765338192, 8.025000000000000355 ) ) ;
#48824=CARTESIAN_POINT ( 'NONE',  ( 8.443840259832290585, 153.4094599605764984, 0.06244066176116176009 ) ) ;
#48825=PLANE ( 'NONE',  #18737 ) ;
#48826=EDGE_CURVE ( 'NONE', #49243, #31700, #56712, .T. ) ;
#48827=( NAMED_UNIT ( * ) SI_UNIT ( $, .STERADIAN. ) SOLID_ANGLE_UNIT ( ) );
#48829=CARTESIAN_POINT ( 'NONE',  ( 4.716976649647096842, 160.7429263765338021, 6.492361379858953896 ) ) ;
#48838=CARTESIAN_POINT ( 'NONE',  ( 45.02564408151554431, 10.00854802717183389, 3.127379285698622446 ) ) ;
#48840=( GEOMETRIC_REPRESENTATION_CONTEXT ( 3 ) GLOBAL_UNCERTAINTY_ASSIGNED_CONTEXT ( ( #58134 ) ) GLOBAL_UNIT_ASSIGNED_CONTEXT ( ( #5623, #48611, #38405 ) ) REPRESENTATION_CONTEXT ( 'NONE', 'WORKASPACE' ) );
#48844=FILL_AREA_STYLE_COLOUR ( '', #47843 ) ;
#48845=SURFACE_STYLE_FILL_AREA ( #33999 ) ;
#48846=AXIS2_PLACEMENT_3D ( 'NONE', #2044, #62246, #35535 ) ;
#48851=CARTESIAN_POINT ( 'NONE',  ( 60.00000000000000000, 1.797044900979284448E-15, 10.00000000000000000 ) ) ;
#48857=( GEOMETRIC_REPRESENTATION_CONTEXT ( 3 ) GLOBAL_UNCERTAINTY_ASSIGNED_CONTEXT ( ( #51053 ) ) GLOBAL_UNIT_ASSIGNED_CONTEXT ( ( #52365, #30508, #40413 ) ) REPRESENTATION_CONTEXT ( 'NONE', 'WORKASPACE' ) );
#48859=DIRECTION ( 'NONE',  ( -0.000000000000000000, -0.000000000000000000, 1.000000000000000000 ) ) ;
#48864=CIRCLE ( 'NONE', #19585, 18.50000000000000355 ) ;
#48866=CARTESIAN_POINT ( 'NONE',  ( 10.01517768586949231, 139.8050000000000068, 1.839758294383810543E-15 ) ) ;
#48870=DIRECTION ( 'NONE',  ( -0.7071067811865352493, 8.659560562354782482E-17, 0.7071067811865597852 ) ) ;
#48871=UNCERTAINTY_MEASURE_WITH_UNIT (LENGTH_MEASURE( 1.000000000000000082E-05 ), #21677, 'distance_accuracy_value', 'NONE');
#48873=SURFACE_STYLE_USAGE ( .BOTH. , #69586 ) ;
#48878=PRESENTATION_STYLE_ASSIGNMENT (( #9226 ) ) ;
#48880=DIRECTION ( 'NONE',  ( 0.000000000000000000, 0.000000000000000000, 1.000000000000000000 ) ) ;
#48882=ORIENTED_EDGE ( 'NONE', *, *, #13321, .T. ) ;
#48884=AXIS2_PLACEMENT_3D ( 'NONE', #58522, #53269, #48026 ) ;
#48885=CARTESIAN_POINT ( 'NONE',  ( 41.84210526315788314, 107.2928455055531600, 4.000000000000000000 ) ) ;
#48887=EDGE_CURVE ( 'NONE', #30297, #29473, #57681, .T. ) ;
#48888=STYLED_ITEM ( 'NONE', ( #66737 ), #32089 ) ;
#48889=DIRECTION ( 'NONE',  ( 1.000000000000000000, 0.000000000000000000, 0.000000000000000000 ) ) ;
#48890=LINE ( 'NONE', #33016, #57696 ) ;
#48891=CARTESIAN_POINT ( 'NONE',  ( 4.716976649647099507, 140.6429263765338078, -6.492361379858953008 ) ) ;
#48895=DIRECTION ( 'NONE',  ( -1.000000000000000000, -0.000000000000000000, -0.000000000000000000 ) ) ;
#48902=CARTESIAN_POINT ( 'NONE',  ( -9.058813317711338797, 158.3449999999999989, 2.943386871421373563 ) ) ;
#48903=CARTESIAN_POINT ( 'NONE',  ( -72.00000000000000000, 14.49137674618942562, 9.500000000000000000 ) ) ;
#48904=VERTEX_POINT ( 'NONE', #35540 ) ;
#48905=VECTOR ( 'NONE', #32711, 1000.000000000000000 ) ;
#48906=ORIENTED_EDGE ( 'NONE', *, *, #34335, .F. ) ;
#48913=CARTESIAN_POINT ( 'NONE',  ( 7.632228543268607446, 137.0429263765338135, 2.479861379858954606 ) ) ;
#48916=SURFACE_STYLE_USAGE ( .BOTH. , #27385 ) ;
#48919=ORIENTED_EDGE ( 'NONE', *, *, #62081, .F. ) ;
#48923=DIRECTION ( 'NONE',  ( 1.596582957076308193E-15, 1.000000000000000000, -1.712231188808098028E-15 ) ) ;
#48924=DIRECTION ( 'NONE',  ( -0.000000000000000000, 1.000000000000000000, -0.000000000000000000 ) ) ;
#48930=( NAMED_UNIT ( * ) PLANE_ANGLE_UNIT ( ) SI_UNIT ( $, .RADIAN. ) );
#48932=ORIENTED_EDGE ( 'NONE', *, *, #32613, .T. ) ;
#48933=LINE ( 'NONE', #64722, #68760 ) ;
#48934=CYLINDRICAL_SURFACE ( 'NONE', #69357, 10.00000000000000178 ) ;
#48936=( GEOMETRIC_REPRESENTATION_CONTEXT ( 3 ) GLOBAL_UNCERTAINTY_ASSIGNED_CONTEXT ( ( #58056 ) ) GLOBAL_UNIT_ASSIGNED_CONTEXT ( ( #8196, #67269, #29979 ) ) REPRESENTATION_CONTEXT ( 'NONE', 'WORKASPACE' ) );
#48937=ORIENTED_EDGE ( 'NONE', *, *, #62690, .T. ) ;
#48941=CARTESIAN_POINT ( 'NONE',  ( -74.99999999999998579, 50.00000000000000000, 12.00000000000000000 ) ) ;
#48945=EDGE_CURVE ( 'NONE', #2052, #12977, #35376, .T. ) ;
#48950=CARTESIAN_POINT ( 'NONE',  ( 0.000000000000000000, 110.5549999999999926, -9.525000000000000355 ) ) ;
#48952=FILL_AREA_STYLE_COLOUR ( '', #67890 ) ;
#48953=SURFACE_STYLE_FILL_AREA ( #21838 ) ;
#48955=UNCERTAINTY_MEASURE_WITH_UNIT (LENGTH_MEASURE( 1.000000000000000082E-05 ), #51460, 'distance_accuracy_value', 'NONE');
#48957=FILL_AREA_STYLE ('',( #26407 ) ) ;
#48962=DIRECTION ( 'NONE',  ( 0.000000000000000000, 0.000000000000000000, 1.000000000000000000 ) ) ;
#48963=EDGE_CURVE ( 'NONE', #51627, #2848, #21774, .T. ) ;
#48964=MECHANICAL_DESIGN_GEOMETRIC_PRESENTATION_REPRESENTATION('',(#39966),#65732);
#48966=CARTESIAN_POINT ( 'NONE',  ( -79.99999999999998579, 50.00000000000000000, 6.999999999999988454 ) ) ;
#48981=MECHANICAL_DESIGN_GEOMETRIC_PRESENTATION_REPRESENTATION('',(#16384),#42273);
#48983=SURFACE_SIDE_STYLE ('',( #23248 ) ) ;
#48984=ORIENTED_EDGE ( 'NONE', *, *, #47197, .F. ) ;
#48985=EDGE_CURVE ( 'NONE', #38290, #16746, #5227, .T. ) ;
#48988=CARTESIAN_POINT ( 'NONE',  ( 9.058813317711338797, 126.8449999999999847, -2.943386871421372675 ) ) ;
#48989=DIRECTION ( 'NONE',  ( 0.000000000000000000, 1.000000000000000000, 0.000000000000000000 ) ) ;
#48991=DIRECTION ( 'NONE',  ( -0.000000000000000000, -0.000000000000000000, -1.000000000000000000 ) ) ;
#48992=CARTESIAN_POINT ( 'NONE',  ( -9.058813317711337021, 132.1550000000000011, -2.943386871421374895 ) ) ;
#48996=EDGE_CURVE ( 'NONE', #68077, #32017, #44461, .T. ) ;
#48997=FACE_OUTER_BOUND ( 'NONE', #67490, .T. ) ;
#48999=CARTESIAN_POINT ( 'NONE',  ( -3.094860106618434248, 156.9050000000000011, 9.525000000000000355 ) ) ;
#49001=UNCERTAINTY_MEASURE_WITH_UNIT (LENGTH_MEASURE( 1.000000000000000082E-05 ), #26256, 'distance_accuracy_value', 'NONE');
#49007=AXIS2_PLACEMENT_3D ( 'NONE', #26878, #15690, #4761 ) ;
#49008=( LENGTH_UNIT ( ) NAMED_UNIT ( * ) SI_UNIT ( .MILLI., .METRE. ) );
#49009=FILL_AREA_STYLE_COLOUR ( '', #52307 ) ;
#49010=PRESENTATION_STYLE_ASSIGNMENT (( #53886 ) ) ;
#49013=CIRCLE ( 'NONE', #53445, 12.50000000000000355 ) ;
#49014=CARTESIAN_POINT ( 'NONE',  ( -45.89905495956738690, 9.405628579031731107, -3.000000000000000444 ) ) ;
#49016=ORIENTED_EDGE ( 'NONE', *, *, #39445, .T. ) ;
#49018=CARTESIAN_POINT ( 'NONE',  ( -21.02379604162863913, 114.4999999999999574, 10.00000000000000000 ) ) ;
#49019=COLOUR_RGB ( '', 0.72549020, 0.75294118, 0.79215686) ;
#49021=MECHANICAL_DESIGN_GEOMETRIC_PRESENTATION_REPRESENTATION('',(#36679),#16429);
#49023=CARTESIAN_POINT ( 'NONE',  ( -60.00000000000000000, -2.024042244987997205E-14, -12.00000000000000000 ) ) ;
#49026=EDGE_CURVE ( 'NONE', #18324, #25577, #7303, .T. ) ;
#49029=CARTESIAN_POINT ( 'NONE',  ( 0.000000000000000000, 149.9999999999999716, 0.000000000000000000 ) ) ;
#49030=DIRECTION ( 'NONE',  ( -0.000000000000000000, 1.000000000000000000, -0.000000000000000000 ) ) ;
#49032=VECTOR ( 'NONE', #68158, 1000.000000000000000 ) ;
#49034=CARTESIAN_POINT ( 'NONE',  ( 10.01517768586949231, 129.6949999999999648, 1.839758294383810543E-15 ) ) ;
#49037=CARTESIAN_POINT ( 'NONE',  ( 23.21231517720797655, 117.9999999999999716, -9.500000000000000000 ) ) ;
#49043=EDGE_CURVE ( 'NONE', #8109, #4457, #23484, .T. ) ;
#49044=CARTESIAN_POINT ( 'NONE',  ( -4.716976649647097730, 148.3570736234661638, -6.492361379858953896 ) ) ;
#49047=DIRECTION ( 'NONE',  ( -1.000000000000000000, 0.000000000000000000, 0.000000000000000000 ) ) ;
#49056=DIRECTION ( 'NONE',  ( 1.000000000000000000, 0.000000000000000000, 0.000000000000000000 ) ) ;
#49059=COLOUR_RGB ( '', 0.66274510, 0.83137255, 0.94901961) ;
#49060=ORIENTED_EDGE ( 'NONE', *, *, #46667, .F. ) ;
#49065=CARTESIAN_POINT ( 'NONE',  ( -34.99999999999992895, 112.4999999999999858, -10.00000000000000000 ) ) ;
#49066=VECTOR ( 'NONE', #48300, 1000.000000000000000 ) ;
#49068=CARTESIAN_POINT ( 'NONE',  ( 6.826472737025119919, 150.0070736234661695, 4.959722759717908325 ) ) ;
#49069=EDGE_LOOP ( 'NONE', ( #44804, #41133, #43003, #15773, #51200, #51352, #4805, #25403, #46758, #18320, #12407, #19686, #54240 ) ) ;
#49075=DIRECTION ( 'NONE',  ( -1.000000000000000000, 0.000000000000000000, 0.000000000000000000 ) ) ;
#49076=ORIENTED_EDGE ( 'NONE', *, *, #32109, .T. ) ;
#49078=ADVANCED_FACE ( 'NONE', ( #49904 ), #65374, .F. ) ;
#49080=ORIENTED_EDGE ( 'NONE', *, *, #53794, .F. ) ;
#49081=DIRECTION ( 'NONE',  ( 0.000000000000000000, 0.000000000000000000, 1.000000000000000000 ) ) ;
#49082=CARTESIAN_POINT ( 'NONE',  ( -45.00000000000000000, 9.701542612659405762, -6.099661992412403144 ) ) ;
#49084=FACE_OUTER_BOUND ( 'NONE', #27090, .T. ) ;
#49086=ORIENTED_EDGE ( 'NONE', *, *, #41979, .T. ) ;
#49087=CARTESIAN_POINT ( 'NONE',  ( 45.65811388298785545, 10.21937129432926916, -6.131267346259138940 ) ) ;
#49090=CARTESIAN_POINT ( 'NONE',  ( 45.00000000000000000, 99.99999999999992895, 9.500000000000000000 ) ) ;
#49093=DIRECTION ( 'NONE',  ( 0.000000000000000000, 0.000000000000000000, 1.000000000000000000 ) ) ;
#49096=CARTESIAN_POINT ( 'NONE',  ( 3.094860106618431583, 132.0949999999999989, 9.525000000000000355 ) ) ;
#49098=CARTESIAN_POINT ( 'NONE',  ( -0.3706977682293637888, 154.4502386517839341, -9.475238651784067656 ) ) ;
#49104=SURFACE_SIDE_STYLE ('',( #11424 ) ) ;
#49107=AXIS2_PLACEMENT_3D ( 'NONE', #22935, #54226, #53880 ) ;
#49108=DIRECTION ( 'NONE',  ( -1.000000000000000000, 2.055968564120660634E-14, 0.000000000000000000 ) ) ;
#49113=ORIENTED_EDGE ( 'NONE', *, *, #54155, .T. ) ;
#49114=( BOUNDED_CURVE ( )  B_SPLINE_CURVE ( 2, ( #15770, #37602, #21714, #21023, #5174, #37944, #59318, #32595, #32263, #26620, #42516 ),
 .UNSPECIFIED., .F., .F. ) 
 B_SPLINE_CURVE_WITH_KNOTS ( ( 3, 2, 2, 2, 2, 3 ),
 ( 0.08823529411764713393, 0.09411764705882361137, 0.1000000000000000888, 0.1058823529411765663, 0.1117647058823530437, 0.1176470588235295212 ),
 .UNSPECIFIED. ) 
 CURVE ( )  GEOMETRIC_REPRESENTATION_ITEM ( )  RATIONAL_B_SPLINE_CURVE ( ( 0.9999999999999994449, 0.9510565162951540863, 1.000000000000000000, 0.9510565162951535312, 1.000000000000000000, 0.9510565162951535312, 1.000000000000000000, 0.9510565162951535312, 1.000000000000000000, 0.9510565162951526430, 1.000000000000000888 ) ) 
 REPRESENTATION_ITEM ( '' )  );
#49115=CARTESIAN_POINT ( 'NONE',  ( 45.00000000011532109, 10.00000000003076295, -3.953713388244109339 ) ) ;
#49121=ADVANCED_FACE ( 'NONE', ( #66400 ), #1668, .F. ) ;
#49123=CARTESIAN_POINT ( 'NONE',  ( -74.99999999999998579, 36.00000000000000711, 6.499999999999999112 ) ) ;
#49127=FACE_OUTER_BOUND ( 'NONE', #26383, .T. ) ;
#49130=ADVANCED_FACE ( 'NONE', ( #38337 ), #18886, .F. ) ;
#49132=VERTEX_POINT ( 'NONE', #24866 ) ;
#49135=CARTESIAN_POINT ( 'NONE',  ( -9.827790563157511022E-16, 122.5570736234661524, 8.025000000000000355 ) ) ;
#49136=SURFACE_STYLE_FILL_AREA ( #5830 ) ;
#49146=ORIENTED_EDGE ( 'NONE', *, *, #4171, .T. ) ;
#49148=CARTESIAN_POINT ( 'NONE',  ( 44.50000000000000000, 99.99999999999992895, -4.000000000000000000 ) ) ;
#49150=ORIENTED_EDGE ( 'NONE', *, *, #6372, .T. ) ;
#49151=CARTESIAN_POINT ( 'NONE',  ( -8.437984349512095861, 159.6929263765338192, -5.166775262442723748E-16 ) ) ;
#49164=CARTESIAN_POINT ( 'NONE',  ( -3.105708046185574389, 153.1036296714643754, -7.531667776144036708 ) ) ;
#49165=ORIENTED_EDGE ( 'NONE', *, *, #50529, .F. ) ;
#49168=SURFACE_STYLE_USAGE ( .BOTH. , #12182 ) ;
#49169=ORIENTED_EDGE ( 'NONE', *, *, #62001, .T. ) ;
#49170=( NAMED_UNIT ( * ) PLANE_ANGLE_UNIT ( ) SI_UNIT ( $, .RADIAN. ) );
#49177=EDGE_LOOP ( 'NONE', ( #20474, #57472, #8748, #41640 ) ) ;
#49178=DIRECTION ( 'NONE',  ( 0.000000000000000000, 0.000000000000000000, -1.000000000000000000 ) ) ;
#49179=CARTESIAN_POINT ( 'NONE',  ( 44.94709371290443300, 9.982364570967702022, 3.713690726390154850 ) ) ;
#49182=MECHANICAL_DESIGN_GEOMETRIC_PRESENTATION_REPRESENTATION('',(#58164),#37968);
#49184=EDGE_CURVE ( 'NONE', #6631, #67791, #25272, .T. ) ;
#49186=CARTESIAN_POINT ( 'NONE',  ( -9.058813317711338797, 132.4549999999999841, 2.943386871421373563 ) ) ;
#49187=EDGE_CURVE ( 'NONE', #21071, #50108, #29084, .T. ) ;
#49188=CARTESIAN_POINT ( 'NONE',  ( 3.569376287083594779, 154.2959099316039726, 8.618005638701651705 ) ) ;
#49191=ADVANCED_FACE ( 'NONE', ( #35452 ), #2310, .T. ) ;
#49193=( NAMED_UNIT ( * ) PLANE_ANGLE_UNIT ( ) SI_UNIT ( $, .RADIAN. ) );
#49194=STYLED_ITEM ( 'NONE', ( #28276 ), #67472 ) ;
#49201=LINE ( 'NONE', #12571, #63099 ) ;
#49204=VERTEX_POINT ( 'NONE', #9767 ) ;
#49206=ORIENTED_EDGE ( 'NONE', *, *, #16078, .T. ) ;
#49207=PRESENTATION_STYLE_ASSIGNMENT (( #44653 ) ) ;
#49212=( LENGTH_UNIT ( ) NAMED_UNIT ( * ) SI_UNIT ( .MILLI., .METRE. ) );
#49214=ORIENTED_EDGE ( 'NONE', *, *, #56594, .T. ) ;
#49215=CARTESIAN_POINT ( 'NONE',  ( 72.50000000000000000, 35.92875272052971525, -10.00000000000000000 ) ) ;
#49216=PRESENTATION_STYLE_ASSIGNMENT (( #12592 ) ) ;
#49219=CARTESIAN_POINT ( 'NONE',  ( -2.607480562269075097, 136.2929263765337851, 8.025000000000000355 ) ) ;
#49220=CARTESIAN_POINT ( 'NONE',  ( -15.48999599679679662, 146.4999999999999716, -10.00000000000000000 ) ) ;
#49224=DIRECTION ( 'NONE',  ( 1.000000000000000000, -0.000000000000000000, -0.000000000000000000 ) ) ;
#49230=DIRECTION ( 'NONE',  ( 1.000000000000000000, 0.000000000000000000, 0.000000000000000000 ) ) ;
#49235=( NAMED_UNIT ( * ) SI_UNIT ( $, .STERADIAN. ) SOLID_ANGLE_UNIT ( ) );
#49241=VERTEX_POINT ( 'NONE', #5470 ) ;
#49243=VERTEX_POINT ( 'NONE', #58627 ) ;
#49244=CARTESIAN_POINT ( 'NONE',  ( -45.91547277936962246, 9.430195807687219656, 3.611004237778676185 ) ) ;
#49247=EDGE_LOOP ( 'NONE', ( #64731, #499, #20533 ) ) ;
#49248=CARTESIAN_POINT ( 'NONE',  ( -60.49999999999998579, 50.00000000000000000, 7.500000000000000000 ) ) ;
#49249=SURFACE_STYLE_USAGE ( .BOTH. , #27748 ) ;
#49252=DIRECTION ( 'NONE',  ( 0.000000000000000000, -1.000000000000000000, 3.469446951953611033E-15 ) ) ;
#49262=EDGE_CURVE ( 'NONE', #61842, #62248, #63532, .T. ) ;
#49264=CARTESIAN_POINT ( 'NONE',  ( 9.058813317711338797, 159.8449999999999989, -2.943386871421372675 ) ) ;
#49267=AXIS2_PLACEMENT_3D ( 'NONE', #57413, #9239, #31711 ) ;
#49269=( LENGTH_UNIT ( ) NAMED_UNIT ( * ) SI_UNIT ( .MILLI., .METRE. ) );
#49270=DIRECTION ( 'NONE',  ( 0.000000000000000000, 0.000000000000000000, -1.000000000000000000 ) ) ;
#49271=PRESENTATION_STYLE_ASSIGNMENT (( #33089 ) ) ;
#49277=STYLED_ITEM ( 'NONE', ( #2183 ), #66610 ) ;
#49280=VERTEX_POINT ( 'NONE', #52667 ) ;
#49282=ORIENTED_EDGE ( 'NONE', *, *, #8673, .T. ) ;
#49283=DIRECTION ( 'NONE',  ( 0.000000000000000000, 0.000000000000000000, -1.000000000000000000 ) ) ;
#49285=CARTESIAN_POINT ( 'NONE',  ( -44.99999999999998579, 119.9999999999999716, 7.000000000000000000 ) ) ;
#49287=CIRCLE ( 'NONE', #32381, 0.5000000000000004441 ) ;
#49289=CARTESIAN_POINT ( 'NONE',  ( 45.50000000000000000, 9.639620389971920389, 6.999999999999999112 ) ) ;
#49295=EDGE_LOOP ( 'NONE', ( #29780, #29624, #59783, #21073 ) ) ;
#49297=( LENGTH_UNIT ( ) NAMED_UNIT ( * ) SI_UNIT ( .MILLI., .METRE. ) );
#49298=CARTESIAN_POINT ( 'NONE',  ( 10.01517768586949231, 126.6949999999999932, 1.839758294383810543E-15 ) ) ;
#49301=EDGE_LOOP ( 'NONE', ( #59045, #6676, #52337, #28139 ) ) ;
#49303=CARTESIAN_POINT ( 'NONE',  ( -5.598654528085808657, 129.7549999999999955, 7.705886871421373741 ) ) ;
#49308=ORIENTED_EDGE ( 'NONE', *, *, #57582, .F. ) ;
#49309=CARTESIAN_POINT ( 'NONE',  ( -8.102448949553181734, 156.6049999999999329, 5.886773742842747126 ) ) ;
#49313=CARTESIAN_POINT ( 'NONE',  ( -9.827790563157511022E-16, 142.4429263765338192, 8.025000000000000355 ) ) ;
#49314=DIRECTION ( 'NONE',  ( 0.000000000000000000, 0.000000000000000000, 1.000000000000000000 ) ) ;
#49316=ORIENTED_EDGE ( 'NONE', *, *, #3357, .F. ) ;
#49318=DIRECTION ( 'NONE',  ( -0.000000000000000000, -1.000000000000000000, 0.000000000000000000 ) ) ;
#49323=PRESENTATION_STYLE_ASSIGNMENT (( #16975 ) ) ;
#49324=CARTESIAN_POINT ( 'NONE',  ( -44.99154893936433552, 9.591540374752312914, 3.000000000000000000 ) ) ;
#49325=VERTEX_POINT ( 'NONE', #26921 ) ;
#49326=DIRECTION ( 'NONE',  ( 0.000000000000000000, 0.000000000000000000, 1.000000000000000000 ) ) ;
#49331=DIRECTION ( 'NONE',  ( 1.000000000000000000, 0.000000000000000000, -0.000000000000000000 ) ) ;
#49332=VECTOR ( 'NONE', #24469, 1000.000000000000000 ) ;
#49333=SURFACE_STYLE_USAGE ( .BOTH. , #43066 ) ;
#49335=AXIS2_PLACEMENT_3D ( 'NONE', #51158, #55730, #55009 ) ;
#49337=CARTESIAN_POINT ( 'NONE',  ( -75.00000000000000000, 9.027119726910738606, -6.778758691516489243 ) ) ;
#49340=PLANE ( 'NONE',  #23438 ) ;
#49343=CARTESIAN_POINT ( 'NONE',  ( 8.102448949553181734, 132.3949999999999534, 5.886773742842750679 ) ) ;
#49353=VECTOR ( 'NONE', #59957, 1000.000000000000000 ) ;
#49356=STYLED_ITEM ( 'NONE', ( #24121 ), #10590 ) ;
#49357=CARTESIAN_POINT ( 'NONE',  ( 15.98999599679679839, 146.4999999999999716, 9.500000000000000000 ) ) ;
#49361=VERTEX_POINT ( 'NONE', #20651 ) ;
#49370=COLOUR_RGB ( '', 0.08235294, 0.09019608, 0.10196078) ;
#49372=ORIENTED_EDGE ( 'NONE', *, *, #47130, .F. ) ;
#49374=ORIENTED_EDGE ( 'NONE', *, *, #29870, .F. ) ;
#49375=( LENGTH_UNIT ( ) NAMED_UNIT ( * ) SI_UNIT ( .MILLI., .METRE. ) );
#49378=CARTESIAN_POINT ( 'NONE',  ( 4.716976649647099507, 153.7570736234661695, -6.492361379858953008 ) ) ;
#49379=VECTOR ( 'NONE', #64749, 1000.000000000000000 ) ;
#49385=CARTESIAN_POINT ( 'NONE',  ( -24.21231517720798010, 113.4999999999999858, -7.500000000000000000 ) ) ;
#49387=CARTESIAN_POINT ( 'NONE',  ( -60.00000000000000000, -2.024042244987997205E-14, -10.00000000000000000 ) ) ;
#49388=DIRECTION ( 'NONE',  ( 0.9704308468600219006, -0.2413793103448194921, -0.000000000000000000 ) ) ;
#49392=MECHANICAL_DESIGN_GEOMETRIC_PRESENTATION_REPRESENTATION('',(#53727),#66242);
#49396=FILL_AREA_STYLE_COLOUR ( '', #51898 ) ;
#49398=LINE ( 'NONE', #23339, #23346 ) ;
#49399=CARTESIAN_POINT ( 'NONE',  ( -45.91547277936962246, 9.430195807687216103, -6.000000000000000000 ) ) ;
#49402=SURFACE_SIDE_STYLE ('',( #16718 ) ) ;
#49404=VERTEX_POINT ( 'NONE', #43876 ) ;
#49405=( GEOMETRIC_REPRESENTATION_CONTEXT ( 3 ) GLOBAL_UNCERTAINTY_ASSIGNED_CONTEXT ( ( #10205 ) ) GLOBAL_UNIT_ASSIGNED_CONTEXT ( ( #8244, #33910, #18778 ) ) REPRESENTATION_CONTEXT ( 'NONE', 'WORKASPACE' ) );
#49408=CARTESIAN_POINT ( 'NONE',  ( -74.21332857261049298, 8.935426707107593458, 6.369485321263598010 ) ) ;
#49410=ORIENTED_EDGE ( 'NONE', *, *, #8369, .F. ) ;
#49413=SURFACE_STYLE_FILL_AREA ( #6469 ) ;
#49415=SURFACE_STYLE_USAGE ( .BOTH. , #66623 ) ;
#49416=( LENGTH_UNIT ( ) NAMED_UNIT ( * ) SI_UNIT ( .MILLI., .METRE. ) );
#49417=AXIS2_PLACEMENT_3D ( 'NONE', #29305, #8226, #39917 ) ;
#49419=CARTESIAN_POINT ( 'NONE',  ( 0.000000000000000000, 130.4449999999999648, -9.525000000000000355 ) ) ;
#49422=STYLED_ITEM ( 'NONE', ( #41646 ), #41802 ) ;
#49423=CARTESIAN_POINT ( 'NONE',  ( 74.99999999999998579, 50.00000000000000000, -9.500000000000000000 ) ) ;
#49424=VERTEX_POINT ( 'NONE', #836 ) ;
#49425=VECTOR ( 'NONE', #37286, 1000.000000000000000 ) ;
#49431=DIRECTION ( 'NONE',  ( -1.000000000000000000, 0.000000000000000000, 0.000000000000000000 ) ) ;
#49432=DIRECTION ( 'NONE',  ( 0.000000000000000000, 1.000000000000000000, 0.000000000000000000 ) ) ;
#49436=ORIENTED_EDGE ( 'NONE', *, *, #63219, .F. ) ;
#49439=CARTESIAN_POINT ( 'NONE',  ( 44.40987964080542838, 10.30029937056526990, -3.500456542365120605 ) ) ;
#49441=DIRECTION ( 'NONE',  ( 1.000000000000000000, 0.000000000000000000, 0.000000000000000000 ) ) ;
#49445=SURFACE_SIDE_STYLE ('',( #6856 ) ) ;
#49448=DIRECTION ( 'NONE',  ( -1.000000000000000000, 0.000000000000000000, 0.000000000000000000 ) ) ;
#49449=DIRECTION ( 'NONE',  ( 1.000000000000000000, 0.000000000000000000, 0.000000000000000000 ) ) ;
#49457=ORIENTED_EDGE ( 'NONE', *, *, #29706, .F. ) ;
#49458=CARTESIAN_POINT ( 'NONE',  ( -41.49999999999997868, 10.49999999999998046, -3.500000000000000000 ) ) ;
#49462=MECHANICAL_DESIGN_GEOMETRIC_PRESENTATION_REPRESENTATION('',(#32609),#9037);
#49463=CARTESIAN_POINT ( 'NONE',  ( -8.437984349512095861, 121.8070736234661666, -5.166775262442723748E-16 ) ) ;
#49464=CARTESIAN_POINT ( 'NONE',  ( 34.99999999999992895, 110.4999999999999858, -9.500000000000000000 ) ) ;
#49466=CARTESIAN_POINT ( 'NONE',  ( 74.59716837049624871, 19.66257108179103241, -6.399833413891735212 ) ) ;
#49471=ORIENTED_EDGE ( 'NONE', *, *, #7322, .T. ) ;
#49479=AXIS2_PLACEMENT_3D ( 'NONE', #8079, #62229, #19669 ) ;
#49480=CARTESIAN_POINT ( 'NONE',  ( -4.716976649647098618, 124.1429263765338220, 6.492361379858953008 ) ) ;
#49487=( NAMED_UNIT ( * ) PLANE_ANGLE_UNIT ( ) SI_UNIT ( $, .RADIAN. ) );
#49497=DIRECTION ( 'NONE',  ( 0.000000000000000000, 0.000000000000000000, -1.000000000000000000 ) ) ;
#49502=AXIS2_PLACEMENT_3D ( 'NONE', #62634, #3158, #61582 ) ;
#49503=CARTESIAN_POINT ( 'NONE',  ( -23.21231517720797655, 117.9999999999999716, 7.000000000000000000 ) ) ;
#49505=DIRECTION ( 'NONE',  ( 0.2413793103448194644, 0.9704308468600220117, 0.000000000000000000 ) ) ;
#49508=( NAMED_UNIT ( * ) SI_UNIT ( $, .STERADIAN. ) SOLID_ANGLE_UNIT ( ) );
#49509=SURFACE_STYLE_FILL_AREA ( #53404 ) ;
#49512=DIRECTION ( 'NONE',  ( 1.000000000000000000, 0.000000000000000000, 0.000000000000000000 ) ) ;
#49514=AXIS2_PLACEMENT_3D ( 'NONE', #59904, #18038, #12055 ) ;
#49516=AXIS2_PLACEMENT_3D ( 'NONE', #14731, #47113, #36205 ) ;
#49518=ORIENTED_EDGE ( 'NONE', *, *, #43269, .T. ) ;
#49519=AXIS2_PLACEMENT_3D ( 'NONE', #42, #36427, #59187 ) ;
#49520=SURFACE_SIDE_STYLE ('',( #59338 ) ) ;
#49521=CARTESIAN_POINT ( 'NONE',  ( 44.82448674805887379, 10.57670410873373079, 3.609649266065623863 ) ) ;
#49527=CARTESIAN_POINT ( 'NONE',  ( 5.598654528085805993, 133.3549999999999898, 7.705886871421374629 ) ) ;
#49529=CARTESIAN_POINT ( 'NONE',  ( -9.827790563157511022E-16, 127.4429263765338192, 8.025000000000000355 ) ) ;
#49530=CARTESIAN_POINT ( 'NONE',  ( 0.7252983342190405525, 154.1754443422797465, 9.200444342279759269 ) ) ;
#49532=UNCERTAINTY_MEASURE_WITH_UNIT (LENGTH_MEASURE( 1.000000000000000082E-05 ), #22071, 'distance_accuracy_value', 'NONE');
#49535=SURFACE_SIDE_STYLE ('',( #28024 ) ) ;
#49537=FACE_OUTER_BOUND ( 'NONE', #66896, .T. ) ;
#49539=ORIENTED_EDGE ( 'NONE', *, *, #21849, .T. ) ;
#49541=DIRECTION ( 'NONE',  ( 1.000000000000000000, 0.000000000000000000, 0.000000000000000000 ) ) ;
#49542=MECHANICAL_DESIGN_GEOMETRIC_PRESENTATION_REPRESENTATION('',(#2255),#51806);
#49545=SURFACE_STYLE_FILL_AREA ( #34041 ) ;
#49550=ORIENTED_EDGE ( 'NONE', *, *, #43501, .T. ) ;
#49552=ORIENTED_EDGE ( 'NONE', *, *, #63585, .F. ) ;
#49553=DIRECTION ( 'NONE',  ( 1.000000000000000000, 0.000000000000000000, 0.000000000000000000 ) ) ;
#49559=FACE_OUTER_BOUND ( 'NONE', #8189, .T. ) ;
#49563=CARTESIAN_POINT ( 'NONE',  ( -5.735626173591136023, 110.4999999999999858, -7.617005373172553995 ) ) ;
#49565=CARTESIAN_POINT ( 'NONE',  ( 44.99999999999999289, 10.69371294336139400, 3.707106781186544353 ) ) ;
#49566=ORIENTED_EDGE ( 'NONE', *, *, #63256, .F. ) ;
#49567=CARTESIAN_POINT ( 'NONE',  ( 8.437984349512095861, 134.1929263765338192, 1.550032578732817026E-15 ) ) ;
#49570=( GEOMETRIC_REPRESENTATION_CONTEXT ( 3 ) GLOBAL_UNCERTAINTY_ASSIGNED_CONTEXT ( ( #27079 ) ) GLOBAL_UNIT_ASSIGNED_CONTEXT ( ( #36697, #58114, #36339 ) ) REPRESENTATION_CONTEXT ( 'NONE', 'WORKASPACE' ) );
#49571=CARTESIAN_POINT ( 'NONE',  ( -9.827790563157511022E-16, 124.4429263765338192, 8.025000000000000355 ) ) ;
#49572=ADVANCED_FACE ( 'NONE', ( #45259 ), #66681, .T. ) ;
#49580=SURFACE_SIDE_STYLE ('',( #33718 ) ) ;
#49582=CARTESIAN_POINT ( 'NONE',  ( -74.50000000000000000, -2.220952357103124925E-14, 6.999999999999999112 ) ) ;
#49589=FACE_OUTER_BOUND ( 'NONE', #62277, .T. ) ;
#49590=CARTESIAN_POINT ( 'NONE',  ( -45.00000000000000000, 9.708372675170616972, -6.100915009778865361 ) ) ;
#49591=ORIENTED_EDGE ( 'NONE', *, *, #45312, .T. ) ;
#49593=VERTEX_POINT ( 'NONE', #35008 ) ;
#49594=DIRECTION ( 'NONE',  ( 0.000000000000000000, 0.000000000000000000, -1.000000000000000000 ) ) ;
#49595=EDGE_CURVE ( 'NONE', #21468, #67711, #26473, .T. ) ;
#49598=CARTESIAN_POINT ( 'NONE',  ( 21.02379604162863913, 110.4999999999999858, -10.50000000000000000 ) ) ;
#49599=( LENGTH_UNIT ( ) NAMED_UNIT ( * ) SI_UNIT ( .MILLI., .METRE. ) );
#49600=( GEOMETRIC_REPRESENTATION_CONTEXT ( 3 ) GLOBAL_UNCERTAINTY_ASSIGNED_CONTEXT ( ( #3805 ) ) GLOBAL_UNIT_ASSIGNED_CONTEXT ( ( #63707, #15554, #67976 ) ) REPRESENTATION_CONTEXT ( 'NONE', 'WORKASPACE' ) );
#49601=DIRECTION ( 'NONE',  ( 1.224646799147353207E-16, 1.000000000000000000, -0.000000000000000000 ) ) ;
#49602=EDGE_LOOP ( 'NONE', ( #37451, #35139, #31729, #4445 ) ) ;
#49605=DIRECTION ( 'NONE',  ( -0.000000000000000000, -1.000000000000000000, -0.000000000000000000 ) ) ;
#49610=CARTESIAN_POINT ( 'NONE',  ( 3.094860106618435136, 160.2949999999999875, -9.525000000000000355 ) ) ;
#49612=MECHANICAL_DESIGN_GEOMETRIC_PRESENTATION_REPRESENTATION('',(#64201),#51870);
#49618=FILL_AREA_STYLE ('',( #34113 ) ) ;
#49622=AXIS2_PLACEMENT_3D ( 'NONE', #64497, #20540, #16342 ) ;
#49628=ORIENTED_EDGE ( 'NONE', *, *, #35040, .F. ) ;
#49630=DIRECTION ( 'NONE',  ( -1.000000000000000000, 0.000000000000000000, 0.000000000000000000 ) ) ;
#49631=DIRECTION ( 'NONE',  ( 0.000000000000000000, 0.000000000000000000, -1.000000000000000000 ) ) ;
#49636=VERTEX_POINT ( 'NONE', #37137 ) ;
#49641=EDGE_CURVE ( 'NONE', #42412, #24967, #66914, .T. ) ;
#49642=AXIS2_PLACEMENT_3D ( 'NONE', #29533, #51003, #2768 ) ;
#49644=CARTESIAN_POINT ( 'NONE',  ( -1.166476076187854022E-15, 125.9449999999999790, 9.525000000000000355 ) ) ;
#49645=CYLINDRICAL_SURFACE ( 'NONE', #47546, 0.5000000000000004441 ) ;
#49646=EDGE_LOOP ( 'NONE', ( #41963, #34051, #5843, #63557 ) ) ;
#49647=CYLINDRICAL_SURFACE ( 'NONE', #29626, 0.5000000000000004441 ) ;
#49648=CARTESIAN_POINT ( 'NONE',  ( -8.102448949553179958, 126.0049999999999812, -5.886773742842749790 ) ) ;
#49649=AXIS2_PLACEMENT_3D ( 'NONE', #46630, #19834, #48253 ) ;
#49652=CARTESIAN_POINT ( 'NONE',  ( -9.058813317711337021, 153.1549999999999727, -2.943386871421374895 ) ) ;
#49653=DIRECTION ( 'NONE',  ( 1.000000000000000000, -0.000000000000000000, -0.000000000000000000 ) ) ;
#49654=UNCERTAINTY_MEASURE_WITH_UNIT (LENGTH_MEASURE( 1.000000000000000082E-05 ), #46465, 'distance_accuracy_value', 'NONE');
#49655=AXIS2_PLACEMENT_3D ( 'NONE', #67809, #14329, #9070 ) ;
#49658=SURFACE_STYLE_USAGE ( .BOTH. , #28515 ) ;
#49660=ORIENTED_EDGE ( 'NONE', *, *, #29654, .F. ) ;
#49665=SURFACE_STYLE_USAGE ( .BOTH. , #64793 ) ;
#49668=EDGE_CURVE ( 'NONE', #7860, #29261, #18603, .T. ) ;
#49669=ORIENTED_EDGE ( 'NONE', *, *, #5658, .F. ) ;
#49671=UNCERTAINTY_MEASURE_WITH_UNIT (LENGTH_MEASURE( 1.000000000000000082E-05 ), #14794, 'distance_accuracy_value', 'NONE');
#49672=COLOUR_RGB ( '', 0.40784314, 0.44705882, 0.49803922) ;
#49674=PLANE ( 'NONE',  #67237 ) ;
#49675=EDGE_CURVE ( 'NONE', #48195, #35027, #24809, .T. ) ;
#49676=SURFACE_STYLE_USAGE ( .BOTH. , #27489 ) ;
#49681=CARTESIAN_POINT ( 'NONE',  ( -44.99154893906889896, 9.591540376338688390, -3.113676943954755139 ) ) ;
#49683=AXIS2_PLACEMENT_3D ( 'NONE', #50612, #66083, #33394 ) ;
#49687=STYLED_ITEM ( 'NONE', ( #55543 ), #18880 ) ;
#49688=( NAMED_UNIT ( * ) SI_UNIT ( $, .STERADIAN. ) SOLID_ANGLE_UNIT ( ) );
#49690=CARTESIAN_POINT ( 'NONE',  ( -75.00000000000000000, 8.411230060884987481, -6.233452521073311381 ) ) ;
#49692=FILL_AREA_STYLE ('',( #7463 ) ) ;
#49694=CARTESIAN_POINT ( 'NONE',  ( 5.598654528085805993, 126.2449999999999903, 7.705886871421374629 ) ) ;
#49703=AXIS2_PLACEMENT_3D ( 'NONE', #10284, #5660, #63395 ) ;
#49704=CARTESIAN_POINT ( 'NONE',  ( -41.49999999999997868, 10.49999999999998401, 3.500000000000000000 ) ) ;
#49707=VERTEX_POINT ( 'NONE', #52604 ) ;
#49713=( NAMED_UNIT ( * ) PLANE_ANGLE_UNIT ( ) SI_UNIT ( $, .RADIAN. ) );
#49715=ORIENTED_EDGE ( 'NONE', *, *, #23823, .T. ) ;
#49717=MECHANICAL_DESIGN_GEOMETRIC_PRESENTATION_REPRESENTATION('',(#39606),#17148);
#49720=SURFACE_SIDE_STYLE ('',( #33860 ) ) ;
#49722=DIRECTION ( 'NONE',  ( 0.000000000000000000, 0.000000000000000000, 1.000000000000000000 ) ) ;
#49725=FACE_BOUND ( 'NONE', #711, .T. ) ;
#49726=CARTESIAN_POINT ( 'NONE',  ( 8.437984349512095861, 150.3070736234661240, 1.550032578732817026E-15 ) ) ;
#49727=EDGE_CURVE ( 'NONE', #54121, #599, #58204, .T. ) ;
#49732=CIRCLE ( 'NONE', #59867, 0.5000000000000004441 ) ;
#49736=SURFACE_SIDE_STYLE ('',( #65905 ) ) ;
#49739=CIRCLE ( 'NONE', #54288, 0.5000000000000004441 ) ;
#49746=CARTESIAN_POINT ( 'NONE',  ( -45.00000000000000711, 8.554981036081898083, -6.127545679190936845 ) ) ;
#49751=ORIENTED_EDGE ( 'NONE', *, *, #29739, .F. ) ;
#49753=CARTESIAN_POINT ( 'NONE',  ( -75.00000000000000000, 7.951225523245171622, 6.457238017240461758 ) ) ;
#49755=EDGE_LOOP ( 'NONE', ( #20503, #28395, #18693, #19437 ) ) ;
#49759=DIRECTION ( 'NONE',  ( 1.000000000000000000, 0.000000000000000000, 0.000000000000000000 ) ) ;
#49763=( NAMED_UNIT ( * ) PLANE_ANGLE_UNIT ( ) SI_UNIT ( $, .RADIAN. ) );
#49764=CARTESIAN_POINT ( 'NONE',  ( 9.058813317711338797, 135.8449999999999989, -2.943386871421372675 ) ) ;
#49766=MECHANICAL_DESIGN_GEOMETRIC_PRESENTATION_REPRESENTATION('',(#48599),#58750);
#49767=DIRECTION ( 'NONE',  ( 0.000000000000000000, -1.000000000000000000, 0.000000000000000000 ) ) ;
#49775=PRESENTATION_STYLE_ASSIGNMENT (( #54680 ) ) ;
#49780=ADVANCED_FACE ( 'NONE', ( #46663 ), #26525, .T. ) ;
#49782=SPHERICAL_SURFACE ( 'NONE', #32296, 0.5000000000000000000 ) ;
#49786=DIRECTION ( 'NONE',  ( 1.000000000000000000, 0.000000000000000000, 0.000000000000000000 ) ) ;
#49790=DIRECTION ( 'NONE',  ( 0.000000000000000000, 0.000000000000000000, 1.000000000000000000 ) ) ;
#49791=( NAMED_UNIT ( * ) SI_UNIT ( $, .STERADIAN. ) SOLID_ANGLE_UNIT ( ) );
#49795=DIRECTION ( 'NONE',  ( 0.000000000000000000, 0.000000000000000000, 1.000000000000000000 ) ) ;
#49799=CARTESIAN_POINT ( 'NONE',  ( -41.84210526315788314, 107.2928455055531600, 4.000000000000000000 ) ) ;
#49800=EDGE_CURVE ( 'NONE', #68674, #15666, #16427, .T. ) ;
#49801=DIRECTION ( 'NONE',  ( 1.000000000000000000, 0.000000000000000000, 0.000000000000000000 ) ) ;
#49810=CARTESIAN_POINT ( 'NONE',  ( -2.607480562269073765, 121.2070736234661581, -8.025000000000000355 ) ) ;
#49815=FACE_OUTER_BOUND ( 'NONE', #44472, .T. ) ;
#49816=DIRECTION ( 'NONE',  ( 1.000000000000000000, 0.000000000000000000, 0.000000000000000000 ) ) ;
#49821=SURFACE_SIDE_STYLE ('',( #38609 ) ) ;
#49822=ADVANCED_FACE ( 'NONE', ( #12414 ), #27194, .T. ) ;
#49829=DIRECTION ( 'NONE',  ( 0.000000000000000000, -1.000000000000000000, 0.000000000000000000 ) ) ;
#49832=CARTESIAN_POINT ( 'NONE',  ( 7.632228543268607446, 161.0429263765338419, 2.479861379858954606 ) ) ;
#49833=CARTESIAN_POINT ( 'NONE',  ( -23.21231517720797655, 117.4999999999999716, -9.500000000000000000 ) ) ;
#49836=ORIENTED_EDGE ( 'NONE', *, *, #38583, .T. ) ;
#49838=( NAMED_UNIT ( * ) PLANE_ANGLE_UNIT ( ) SI_UNIT ( $, .RADIAN. ) );
#49841=VECTOR ( 'NONE', #2679, 1000.000000000000000 ) ;
#49842=MECHANICAL_DESIGN_GEOMETRIC_PRESENTATION_REPRESENTATION('',(#19488),#6086);
#49852=ORIENTED_EDGE ( 'NONE', *, *, #19749, .F. ) ;
#49854=CARTESIAN_POINT ( 'NONE',  ( 74.49999999999998579, 119.9999999999997584, 9.500000000000000000 ) ) ;
#49862=TOROIDAL_SURFACE ( 'NONE', #2596, 1.000000000000000000, 0.5000000000000000000 ) ;
#49867=CARTESIAN_POINT ( 'NONE',  ( 44.24703880899742359, 10.19173881602634246, 3.568710496479965411 ) ) ;
#49868=SURFACE_STYLE_USAGE ( .BOTH. , #27671 ) ;
#49872=CIRCLE ( 'NONE', #28488, 10.02499999999997904 ) ;
#49874=CARTESIAN_POINT ( 'NONE',  ( 3.094860106618435136, 146.4050000000000011, -9.525000000000000355 ) ) ;
#49880=FILL_AREA_STYLE_COLOUR ( '', #3432 ) ;
#49883=ADVANCED_FACE ( 'NONE', ( #2871 ), #66598, .T. ) ;
#49884=FILL_AREA_STYLE_COLOUR ( '', #10099 ) ;
#49885=DIRECTION ( 'NONE',  ( 0.000000000000000000, 0.000000000000000000, 1.000000000000000000 ) ) ;
#49886=EDGE_CURVE ( 'NONE', #17642, #6589, #23675, .T. ) ;
#49887=AXIS2_PLACEMENT_3D ( 'NONE', #52699, #31910, #68882 ) ;
#49891=EDGE_LOOP ( 'NONE', ( #12060, #8878, #18271, #46112 ) ) ;
#49892=AXIS2_PLACEMENT_3D ( 'NONE', #37128, #58535, #14244 ) ;
#49894=COLOUR_RGB ( '', 0.31764706, 0.68627451, 0.89019608) ;
#49895=CARTESIAN_POINT ( 'NONE',  ( 0.000000000000000000, 134.9429263765338192, -8.025000000000000355 ) ) ;
#49897=ADVANCED_FACE ( 'NONE', ( #7840 ), #19076, .T. ) ;
#49899=FACE_OUTER_BOUND ( 'NONE', #36554, .T. ) ;
#49901=VERTEX_POINT ( 'NONE', #63044 ) ;
#49904=FACE_OUTER_BOUND ( 'NONE', #49602, .T. ) ;
#49908=CARTESIAN_POINT ( 'NONE',  ( 9.827790563157511022E-16, 87.30187232391182306, -8.025000000000000355 ) ) ;
#49915=ORIENTED_EDGE ( 'NONE', *, *, #51406, .F. ) ;
#49921=EDGE_LOOP ( 'NONE', ( #24600, #31023, #57678, #54551 ) ) ;
#49922=CARTESIAN_POINT ( 'NONE',  ( -6.826472737025120807, 132.9929263765338305, 4.959722759717906548 ) ) ;
#49925=DIRECTION ( 'NONE',  ( -0.000000000000000000, 1.000000000000000000, -0.000000000000000000 ) ) ;
#49931=CARTESIAN_POINT ( 'NONE',  ( -44.50000000000000000, 99.99999999999992895, 4.000000000000000000 ) ) ;
#49934=FACE_OUTER_BOUND ( 'NONE', #43664, .T. ) ;
#49936=ORIENTED_EDGE ( 'NONE', *, *, #59547, .F. ) ;
#49938=STYLED_ITEM ( 'NONE', ( #51303 ), #7858 ) ;
#49941=SURFACE_STYLE_USAGE ( .BOTH. , #50962 ) ;
#49942=ORIENTED_EDGE ( 'NONE', *, *, #13815, .T. ) ;
#49944=CARTESIAN_POINT ( 'NONE',  ( -45.00000000000000000, 9.708372675170618749, 3.611004237778676185 ) ) ;
#49946=AXIS2_PLACEMENT_3D ( 'NONE', #36663, #26041, #47579 ) ;
#49949=SURFACE_SIDE_STYLE ('',( #22862 ) ) ;
#49950=DIRECTION ( 'NONE',  ( 0.000000000000000000, 1.000000000000000000, 0.000000000000000000 ) ) ;
#49951=DIRECTION ( 'NONE',  ( 0.000000000000000000, 0.000000000000000000, 1.000000000000000000 ) ) ;
#49954=CARTESIAN_POINT ( 'NONE',  ( -71.74137931034479720, 63.10081643261027295, -9.500000000000000000 ) ) ;
#49957=FILL_AREA_STYLE ('',( #43426 ) ) ;
#49960=DIRECTION ( 'NONE',  ( 1.000000000000000000, 0.000000000000000000, 0.000000000000000000 ) ) ;
#49963=CIRCLE ( 'NONE', #47756, 0.5000000000000004441 ) ;
#49965=CARTESIAN_POINT ( 'NONE',  ( -3.094860106618432471, 113.7049999999999699, -9.525000000000000355 ) ) ;
#49967=EDGE_CURVE ( 'NONE', #45388, #42340, #14184, .T. ) ;
#49972=MECHANICAL_DESIGN_GEOMETRIC_PRESENTATION_REPRESENTATION('',(#47763),#22996);
#49980=SURFACE_STYLE_FILL_AREA ( #28472 ) ;
#49982=DIRECTION ( 'NONE',  ( 0.000000000000000000, 1.000000000000000000, -0.000000000000000000 ) ) ;
#49983=EDGE_LOOP ( 'NONE', ( #37979, #15182, #44304, #44215 ) ) ;
#49985=CARTESIAN_POINT ( 'NONE',  ( -74.99999999999998579, 50.00000000000000000, -12.00000000000000000 ) ) ;
#49986=AXIS2_PLACEMENT_3D ( 'NONE', #57286, #35843, #53068 ) ;
#49990=LINE ( 'NONE', #24592, #27436 ) ;
#49998=ORIENTED_EDGE ( 'NONE', *, *, #18019, .T. ) ;
#50000=( GEOMETRIC_REPRESENTATION_CONTEXT ( 3 ) GLOBAL_UNCERTAINTY_ASSIGNED_CONTEXT ( ( #19993 ) ) GLOBAL_UNIT_ASSIGNED_CONTEXT ( ( #3942, #35284, #30316 ) ) REPRESENTATION_CONTEXT ( 'NONE', 'WORKASPACE' ) );
#50002=DIRECTION ( 'NONE',  ( -1.000000000000000000, 0.000000000000000000, 0.000000000000000000 ) ) ;
#50003=SURFACE_STYLE_USAGE ( .BOTH. , #7427 ) ;
#50004=CARTESIAN_POINT ( 'NONE',  ( 8.102448949553181734, 129.3949999999999818, 5.886773742842750679 ) ) ;
#50005=ORIENTED_EDGE ( 'NONE', *, *, #16780, .F. ) ;
#50007=CARTESIAN_POINT ( 'NONE',  ( 5.598654528085809545, 137.2549999999999955, -7.705886871421373741 ) ) ;
#50009=FACE_OUTER_BOUND ( 'NONE', #64101, .T. ) ;
#50011=CARTESIAN_POINT ( 'NONE',  ( 5.598654528085809545, 161.2549999999999955, -7.705886871421373741 ) ) ;
#50013=VECTOR ( 'NONE', #52463, 1000.000000000000000 ) ;
#50014=DIRECTION ( 'NONE',  ( 0.000000000000000000, -0.000000000000000000, -1.000000000000000000 ) ) ;
#50016=STYLED_ITEM ( 'NONE', ( #47332 ), #38742 ) ;
#50020=ORIENTED_EDGE ( 'NONE', *, *, #28580, .T. ) ;
#50021=FACE_OUTER_BOUND ( 'NONE', #33477, .T. ) ;
#50022=SURFACE_STYLE_FILL_AREA ( #60528 ) ;
#50026=CARTESIAN_POINT ( 'NONE',  ( -71.49999999999998579, 64.07124727947029896, -7.500000000000000000 ) ) ;
#50027=AXIS2_PLACEMENT_3D ( 'NONE', #18405, #34917, #61625 ) ;
#50029=CARTESIAN_POINT ( 'NONE',  ( -9.827790563157511022E-16, 130.4429263765338192, 8.025000000000000355 ) ) ;
#50033=SURFACE_STYLE_USAGE ( .BOTH. , #1047 ) ;
#50041=STYLED_ITEM ( 'NONE', ( #29045 ), #8448 ) ;
#50042=CARTESIAN_POINT ( 'NONE',  ( -75.00000000000000000, 8.592356338113649628, -6.069948737346060774 ) ) ;
#50045=CARTESIAN_POINT ( 'NONE',  ( 75.00000000000000000, -2.215169945516535778E-14, 10.00000000000000000 ) ) ;
#50048=CARTESIAN_POINT ( 'NONE',  ( 3.094860106618431583, 126.0949999999999847, 9.525000000000000355 ) ) ;
#50050=EDGE_CURVE ( 'NONE', #48372, #43611, #37886, .T. ) ;
#50052=AXIS2_PLACEMENT_3D ( 'NONE', #55503, #50241, #65005 ) ;
#50054=CARTESIAN_POINT ( 'NONE',  ( 45.65811388300841855, 10.21937129433612235, 3.999999999999999112 ) ) ;
#50059=( GEOMETRIC_REPRESENTATION_CONTEXT ( 3 ) GLOBAL_UNCERTAINTY_ASSIGNED_CONTEXT ( ( #51732 ) ) GLOBAL_UNIT_ASSIGNED_CONTEXT ( ( #49375, #44141, #28920 ) ) REPRESENTATION_CONTEXT ( 'NONE', 'WORKASPACE' ) );
#50061=DIRECTION ( 'NONE',  ( 0.000000000000000000, 0.000000000000000000, 1.000000000000000000 ) ) ;
#50067=AXIS2_PLACEMENT_3D ( 'NONE', #32393, #4631, #32757 ) ;
#50069=EDGE_CURVE ( 'NONE', #14677, #51230, #59149, .T. ) ;
#50070=SURFACE_STYLE_FILL_AREA ( #1451 ) ;
#50072=FACE_OUTER_BOUND ( 'NONE', #55509, .T. ) ;
#50074=ADVANCED_FACE ( 'NONE', ( #26771 ), #7493, .T. ) ;
#50078=FILL_AREA_STYLE ('',( #33530 ) ) ;
#50079=CARTESIAN_POINT ( 'NONE',  ( 4.716976649647099507, 150.7570736234661695, -6.492361379858953008 ) ) ;
#50080=B_SPLINE_CURVE_WITH_KNOTS ( 'NONE', 3,
 ( #68854, #31885, #36864, #58977, #58277, #20654, #52670, #15404 ),
 .UNSPECIFIED., .F., .F.,
 ( 4, 2, 2, 4 ),
 ( 0.000000000000000000, 0.0004110476197876519158, 0.0006165714296814797440, 0.0008220952395753075180 ),
 .UNSPECIFIED. ) ;
#50082=EDGE_LOOP ( 'NONE', ( #39369, #26830 ) ) ;
#50086=CARTESIAN_POINT ( 'NONE',  ( 19.89974874213240597, 115.4999999999999574, -10.00000000000000000 ) ) ;
#50087=CARTESIAN_POINT ( 'NONE',  ( -3.094860106618434248, 129.9050000000000011, 9.525000000000000355 ) ) ;
#50089=CARTESIAN_POINT ( 'NONE',  ( -47.50000000000000000, 1.797044900979284448E-15, -9.500000000000000000 ) ) ;
#50092=( NAMED_UNIT ( * ) PLANE_ANGLE_UNIT ( ) SI_UNIT ( $, .RADIAN. ) );
#50095=VERTEX_POINT ( 'NONE', #48653 ) ;
#50097=SURFACE_STYLE_FILL_AREA ( #60603 ) ;
#50099=ORIENTED_EDGE ( 'NONE', *, *, #43801, .T. ) ;
#50104=ORIENTED_EDGE ( 'NONE', *, *, #8275, .F. ) ;
#50108=VERTEX_POINT ( 'NONE', #353 ) ;
#50109=VECTOR ( 'NONE', #8797, 1000.000000000000000 ) ;
#50110=CARTESIAN_POINT ( 'NONE',  ( -75.00000000000000000, 8.254931070086577449, 5.606557580296888332 ) ) ;
#50113=CARTESIAN_POINT ( 'NONE',  ( -7.632228543268607446, 118.6570736234661609, -2.479861379858953718 ) ) ;
#50114=( NAMED_UNIT ( * ) SI_UNIT ( $, .STERADIAN. ) SOLID_ANGLE_UNIT ( ) );
#50115=VECTOR ( 'NONE', #38708, 1000.000000000000000 ) ;
#50117=STYLED_ITEM ( 'NONE', ( #49010 ), #1741 ) ;
#50120=CARTESIAN_POINT ( 'NONE',  ( 3.094860106618435136, 130.2949999999999591, -9.525000000000000355 ) ) ;
#50124=CYLINDRICAL_SURFACE ( 'NONE', #49335, 0.5000000000000004441 ) ;
#50128=SURFACE_STYLE_FILL_AREA ( #59965 ) ;
#50129=FACE_OUTER_BOUND ( 'NONE', #27962, .T. ) ;
#50131=EDGE_CURVE ( 'NONE', #38290, #19166, #43716, .T. ) ;
#50133=DIRECTION ( 'NONE',  ( 0.000000000000000000, 0.000000000000000000, 1.000000000000000000 ) ) ;
#50134=ORIENTED_EDGE ( 'NONE', *, *, #27445, .F. ) ;
#50135=EDGE_CURVE ( 'NONE', #20601, #47060, #18706, .T. ) ;
#50136=CARTESIAN_POINT ( 'NONE',  ( 47.50000000000000000, 99.99999999999992895, 10.00000000000000000 ) ) ;
#50137=MECHANICAL_DESIGN_GEOMETRIC_PRESENTATION_REPRESENTATION('',(#61349),#64733);
#50138=DIRECTION ( 'NONE',  ( 0.000000000000000000, 0.000000000000000000, -1.000000000000000000 ) ) ;
#50141=EDGE_CURVE ( 'NONE', #61874, #47060, #54634, .T. ) ;
#50142=CARTESIAN_POINT ( 'NONE',  ( -34.99999999999999289, 99.99999999999998579, -4.000000000000000000 ) ) ;
#50143=CARTESIAN_POINT ( 'NONE',  ( 71.49999999999998579, 64.07124727947029896, 10.00000000000000000 ) ) ;
#50145=( GEOMETRIC_REPRESENTATION_CONTEXT ( 3 ) GLOBAL_UNCERTAINTY_ASSIGNED_CONTEXT ( ( #3166 ) ) GLOBAL_UNIT_ASSIGNED_CONTEXT ( ( #64161, #26177, #69 ) ) REPRESENTATION_CONTEXT ( 'NONE', 'WORKASPACE' ) );
#50147=CARTESIAN_POINT ( 'NONE',  ( -15.98999599679679839, 146.4999999999999716, 7.500000000000000000 ) ) ;
#50156=CARTESIAN_POINT ( 'NONE',  ( -41.27272961514525917, 107.3325180337009215, 3.464233254638040549 ) ) ;
#50164=CARTESIAN_POINT ( 'NONE',  ( 7.632228543268608334, 123.4570736234661581, -2.479861379858951942 ) ) ;
#50172=CARTESIAN_POINT ( 'NONE',  ( 71.49999999999998579, 64.07124727947029896, -9.500000000000000000 ) ) ;
#50173=DIRECTION ( 'NONE',  ( 0.000000000000000000, 0.000000000000000000, 1.000000000000000000 ) ) ;
#50179=( LENGTH_UNIT ( ) NAMED_UNIT ( * ) SI_UNIT ( .MILLI., .METRE. ) );
#50180=DIRECTION ( 'NONE',  ( 0.000000000000000000, 0.000000000000000000, -1.000000000000000000 ) ) ;
#50184=CARTESIAN_POINT ( 'NONE',  ( 45.50000000000000000, -1.414600137340999687E-14, -7.000000000000000888 ) ) ;
#50192=SURFACE_SIDE_STYLE ('',( #34679 ) ) ;
#50195=( BOUNDED_CURVE ( )  B_SPLINE_CURVE ( 2, ( #27250, #5448, #809, #48437, #16426 ),
 .UNSPECIFIED., .F., .F. ) 
 B_SPLINE_CURVE_WITH_KNOTS ( ( 3, 2, 3 ),
 ( 0.8529411764705880916, 0.8588235294117646523, 0.8616293943929277388 ),
 .UNSPECIFIED. ) 
 CURVE ( )  GEOMETRIC_REPRESENTATION_ITEM ( )  RATIONAL_B_SPLINE_CURVE ( ( 1.000000000000000888, 0.9510565162951526430, 1.000000000000000000, 0.9766541028127959656, 0.9755800536518708377 ) ) 
 REPRESENTATION_ITEM ( '' )  );
#50197=DIRECTION ( 'NONE',  ( -1.156482317317873451E-16, -1.000000000000000000, 0.000000000000000000 ) ) ;
#50199=CARTESIAN_POINT ( 'NONE',  ( 44.99999999999977973, 149.4999999999999716, -9.500000000000000000 ) ) ;
#50200=MECHANICAL_DESIGN_GEOMETRIC_PRESENTATION_REPRESENTATION('',(#4067),#60275);
#50204=CARTESIAN_POINT ( 'NONE',  ( 34.99999999999992895, 112.4999999999999858, -9.500000000000000000 ) ) ;
#50205=LINE ( 'NONE', #1925, #51530 ) ;
#50209=EDGE_CURVE ( 'NONE', #25180, #19879, #45690, .T. ) ;
#50210=CARTESIAN_POINT ( 'NONE',  ( 60.00000000000000000, -2.024042244987997205E-14, 9.500000000000000000 ) ) ;
#50211=AXIS2_PLACEMENT_3D ( 'NONE', #9773, #31182, #47436 ) ;
#50212=CYLINDRICAL_SURFACE ( 'NONE', #66019, 0.5000000000000004441 ) ;
#50218=CARTESIAN_POINT ( 'NONE',  ( 8.102448949553181734, 142.5049999999999955, 5.886773742842750679 ) ) ;
#50221=UNCERTAINTY_MEASURE_WITH_UNIT (LENGTH_MEASURE( 1.000000000000000082E-05 ), #55025, 'distance_accuracy_value', 'NONE');
#50223=ADVANCED_FACE ( 'NONE', ( #65829 ), #33804, .T. ) ;
#50225=FILL_AREA_STYLE_COLOUR ( '', #55057 ) ;
#50230=MECHANICAL_DESIGN_GEOMETRIC_PRESENTATION_REPRESENTATION('',(#51337),#40120);
#50232=EDGE_LOOP ( 'NONE', ( #27790, #10820, #51440, #64615 ) ) ;
#50233=CARTESIAN_POINT ( 'NONE',  ( -15.98999599679679839, 146.4999999999999716, -9.500000000000000000 ) ) ;
#50234=FILL_AREA_STYLE_COLOUR ( '', #111 ) ;
#50235=FILL_AREA_STYLE ('',( #29079 ) ) ;
#50237=DIRECTION ( 'NONE',  ( -1.000000000000000000, 0.000000000000000000, 0.000000000000000000 ) ) ;
#50240=ORIENTED_EDGE ( 'NONE', *, *, #62228, .T. ) ;
#50241=DIRECTION ( 'NONE',  ( 0.000000000000000000, 1.000000000000000000, -0.000000000000000000 ) ) ;
#50242=CIRCLE ( 'NONE', #15421, 27.49999999999999645 ) ;
#50243=FACE_OUTER_BOUND ( 'NONE', #43974, .T. ) ;
#50253=PRESENTATION_STYLE_ASSIGNMENT (( #66415 ) ) ;
#50254=CYLINDRICAL_SURFACE ( 'NONE', #47669, 0.5000000000000004441 ) ;
#50256=CARTESIAN_POINT ( 'NONE',  ( -2.607480562269075097, 133.2929263765338135, 8.025000000000000355 ) ) ;
#50259=DIRECTION ( 'NONE',  ( -0.000000000000000000, -0.000000000000000000, -1.000000000000000000 ) ) ;
#50261=VERTEX_POINT ( 'NONE', #35560 ) ;
#50265=CARTESIAN_POINT ( 'NONE',  ( -12.72792206135785698, 149.9999999999999716, 10.50000000000000000 ) ) ;
#50266=PRESENTATION_STYLE_ASSIGNMENT (( #17249 ) ) ;
#50270=ORIENTED_EDGE ( 'NONE', *, *, #14223, .F. ) ;
#50272=DIRECTION ( 'NONE',  ( 0.000000000000000000, 0.000000000000000000, -1.000000000000000000 ) ) ;
#50276=MECHANICAL_DESIGN_GEOMETRIC_PRESENTATION_REPRESENTATION('',(#33397),#30023);
#50277=ORIENTED_EDGE ( 'NONE', *, *, #69176, .F. ) ;
#50279=ADVANCED_FACE ( 'NONE', ( #52781 ), #57342, .T. ) ;
#50284=ADVANCED_FACE ( 'NONE', ( #25331 ), #51766, .T. ) ;
#50285=AXIS2_PLACEMENT_3D ( 'NONE', #58742, #54134, #22489 ) ;
#50289=CARTESIAN_POINT ( 'NONE',  ( -74.99027199483633410, 35.52740363875328455, -9.609103569194060057 ) ) ;
#50291=CYLINDRICAL_SURFACE ( 'NONE', #69475, 16.94999999999999218 ) ;
#50292=CARTESIAN_POINT ( 'NONE',  ( -48.00000000000000000, 14.49137674618942562, 10.00000000000000000 ) ) ;
#50294=MECHANICAL_DESIGN_GEOMETRIC_PRESENTATION_REPRESENTATION('',(#49194),#35688);
#50296=EDGE_CURVE ( 'NONE', #62390, #64972, #18153, .T. ) ;
#50297=CIRCLE ( 'NONE', #13209, 8.999999999999994671 ) ;
#50299=CARTESIAN_POINT ( 'NONE',  ( 5.598654528085809545, 122.2549999999999955, -7.705886871421373741 ) ) ;
#50303=CARTESIAN_POINT ( 'NONE',  ( -74.99999999999998579, 50.00000000000000000, -41.30495168499704306 ) ) ;
#50305=UNCERTAINTY_MEASURE_WITH_UNIT (LENGTH_MEASURE( 1.000000000000000082E-05 ), #9617, 'distance_accuracy_value', 'NONE');
#50306=DIRECTION ( 'NONE',  ( 1.000000000000000000, 0.000000000000000000, 0.000000000000000000 ) ) ;
#50307=CARTESIAN_POINT ( 'NONE',  ( -71.49999999999998579, 64.07124727947029896, -7.000000000000000000 ) ) ;
#50313=DIRECTION ( 'NONE',  ( 0.000000000000000000, 0.000000000000000000, 1.000000000000000000 ) ) ;
#50316=EDGE_CURVE ( 'NONE', #8462, #5088, #68215, .T. ) ;
#50319=( BOUNDED_CURVE ( )  B_SPLINE_CURVE ( 2, ( #44825, #11031, #38163, #59565, #54640, #32478, #11385, #6793, #27876, #1103, #53940 ),
 .UNSPECIFIED., .F., .F. ) 
 B_SPLINE_CURVE_WITH_KNOTS ( ( 3, 2, 2, 2, 2, 3 ),
 ( 0.5000000000000002220, 0.5058823529411766717, 0.5117647058823531214, 0.5176470588235296821, 0.5235294117647061318, 0.5294117647058825815 ),
 .UNSPECIFIED. ) 
 CURVE ( )  GEOMETRIC_REPRESENTATION_ITEM ( )  RATIONAL_B_SPLINE_CURVE ( ( 0.9999999999999981126, 0.9510565162951554186, 1.000000000000000000, 0.9510565162951535312, 1.000000000000000000, 0.9510565162951535312, 1.000000000000000000, 0.9510565162951535312, 1.000000000000000000, 0.9510565162951516438, 1.000000000000001776 ) ) 
 REPRESENTATION_ITEM ( '' )  );
#50320=( GEOMETRIC_REPRESENTATION_CONTEXT ( 3 ) GLOBAL_UNCERTAINTY_ASSIGNED_CONTEXT ( ( #34025 ) ) GLOBAL_UNIT_ASSIGNED_CONTEXT ( ( #30271, #52132, #15206 ) ) REPRESENTATION_CONTEXT ( 'NONE', 'WORKASPACE' ) );
#50321=LINE ( 'NONE', #28124, #4486 ) ;
#50325=( NAMED_UNIT ( * ) SI_UNIT ( $, .STERADIAN. ) SOLID_ANGLE_UNIT ( ) );
#50326=ORIENTED_EDGE ( 'NONE', *, *, #33983, .T. ) ;
#50330=PRESENTATION_STYLE_ASSIGNMENT (( #28846 ) ) ;
#50332=STYLED_ITEM ( 'NONE', ( #30820 ), #13999 ) ;
#50334=CARTESIAN_POINT ( 'NONE',  ( 9.058813317711337021, 141.5449999999999875, 2.943386871421375783 ) ) ;
#50337=CARTESIAN_POINT ( 'NONE',  ( -10.01517768586949408, 138.3049999999999500, -6.132527647946036459E-16 ) ) ;
#50340=EDGE_LOOP ( 'NONE', ( #1291, #19979, #45278, #6392 ) ) ;
#50341=CARTESIAN_POINT ( 'NONE',  ( -3.094860106618432471, 155.7049999999999841, -9.525000000000000355 ) ) ;
#50343=UNCERTAINTY_MEASURE_WITH_UNIT (LENGTH_MEASURE( 1.000000000000000082E-05 ), #22193, 'distance_accuracy_value', 'NONE');
#50348=LINE ( 'NONE', #1028, #57581 ) ;
#50350=CARTESIAN_POINT ( 'NONE',  ( 0.000000000000000000, 87.30187232391182306, 8.025000000000000355 ) ) ;
#50351=FILL_AREA_STYLE ('',( #23269 ) ) ;
#50354=ORIENTED_EDGE ( 'NONE', *, *, #23912, .F. ) ;
#50356=UNCERTAINTY_MEASURE_WITH_UNIT (LENGTH_MEASURE( 1.000000000000000082E-05 ), #50179, 'distance_accuracy_value', 'NONE');
#50358=CARTESIAN_POINT ( 'NONE',  ( 60.00000000000000000, 1.797044900979284448E-15, -10.49999999999999822 ) ) ;
#50359=PRESENTATION_STYLE_ASSIGNMENT (( #13759 ) ) ;
#50360=VERTEX_POINT ( 'NONE', #59662 ) ;
#50366=EDGE_LOOP ( 'NONE', ( #24202, #61176, #16979, #23512 ) ) ;
#50367=LINE ( 'NONE', #9200, #57601 ) ;
#50369=( NAMED_UNIT ( * ) PLANE_ANGLE_UNIT ( ) SI_UNIT ( $, .RADIAN. ) );
#50372=SURFACE_SIDE_STYLE ('',( #12035 ) ) ;
#50373=( GEOMETRIC_REPRESENTATION_CONTEXT ( 3 ) GLOBAL_UNCERTAINTY_ASSIGNED_CONTEXT ( ( #37018 ) ) GLOBAL_UNIT_ASSIGNED_CONTEXT ( ( #49008, #22582, #27820 ) ) REPRESENTATION_CONTEXT ( 'NONE', 'WORKASPACE' ) );
#50377=CARTESIAN_POINT ( 'NONE',  ( 5.598654528085809545, 142.1449999999999818, -7.705886871421373741 ) ) ;
#50382=VECTOR ( 'NONE', #30497, 1000.000000000000000 ) ;
#50391=CARTESIAN_POINT ( 'NONE',  ( -4.716976649647097730, 127.3570736234661496, -6.492361379858953896 ) ) ;
#50394=ADVANCED_FACE ( 'NONE', ( #1569 ), #48825, .F. ) ;
#50395=DIRECTION ( 'NONE',  ( -0.000000000000000000, 1.000000000000000000, 0.000000000000000000 ) ) ;
#50397=CARTESIAN_POINT ( 'NONE',  ( -48.81081081081080697, 14.09971791521133255, 7.000000000000000000 ) ) ;
#50398=PRESENTATION_STYLE_ASSIGNMENT (( #18039 ) ) ;
#50407=STYLED_ITEM ( 'NONE', ( #32315 ), #10177 ) ;
#50409=CARTESIAN_POINT ( 'NONE',  ( 4.716976649647096842, 155.8570736234661638, 6.492361379858953896 ) ) ;
#50410=STYLED_ITEM ( 'NONE', ( #35031 ), #4408 ) ;
#50412=( NAMED_UNIT ( * ) PLANE_ANGLE_UNIT ( ) SI_UNIT ( $, .RADIAN. ) );
#50413=CARTESIAN_POINT ( 'NONE',  ( 8.102448949553179958, 115.5049999999999812, 5.886773742842750679 ) ) ;
#50416=CARTESIAN_POINT ( 'NONE',  ( -8.102448949553181734, 132.0049999999999386, -5.886773742842749790 ) ) ;
#50417=UNCERTAINTY_MEASURE_WITH_UNIT (LENGTH_MEASURE( 1.000000000000000082E-05 ), #52037, 'distance_accuracy_value', 'NONE');
#50418=CARTESIAN_POINT ( 'NONE',  ( 8.437984349512095861, 132.3070736234661524, 1.550032578732816828E-15 ) ) ;
#50421=CARTESIAN_POINT ( 'NONE',  ( 20.22843684326250369, 114.9428328902810676, 10.38991920486588327 ) ) ;
#50423=DIRECTION ( 'NONE',  ( -1.000000000000000000, 0.000000000000000000, 0.000000000000000000 ) ) ;
#50432=CARTESIAN_POINT ( 'NONE',  ( 34.99999999999999289, 118.4999999999999716, -7.000000000000000000 ) ) ;
#50437=CARTESIAN_POINT ( 'NONE',  ( -74.99999999999998579, 8.554981036082050849, 6.127545679190784078 ) ) ;
#50441=FACE_OUTER_BOUND ( 'NONE', #50708, .T. ) ;
#50442=CARTESIAN_POINT ( 'NONE',  ( 15.98999599679679839, 118.4999999999999716, -7.500000000000000000 ) ) ;
#50445=ADVANCED_FACE ( 'NONE', ( #67040 ), #26690, .F. ) ;
#50447=CARTESIAN_POINT ( 'NONE',  ( -3.094860106618434248, 146.7949999999999875, 9.525000000000000355 ) ) ;
#50449=VECTOR ( 'NONE', #30183, 1000.000000000000000 ) ;
#50450=SURFACE_SIDE_STYLE ('',( #55727 ) ) ;
#50451=CARTESIAN_POINT ( 'NONE',  ( 23.71231517720798010, 117.9999999999999716, 7.000000000000000000 ) ) ;
#50454=SURFACE_STYLE_USAGE ( .BOTH. , #7535 ) ;
#50460=CARTESIAN_POINT ( 'NONE',  ( -3.094860106618432471, 112.5949999999999989, -9.525000000000000355 ) ) ;
#50462=CIRCLE ( 'NONE', #20104, 15.00000000000000000 ) ;
#50463=MECHANICAL_DESIGN_GEOMETRIC_PRESENTATION_REPRESENTATION('',(#57218),#7765);
#50465=DIRECTION ( 'NONE',  ( 1.000000000000000000, 0.000000000000000000, 0.000000000000000000 ) ) ;
#50467=AXIS2_PLACEMENT_3D ( 'NONE', #13561, #39301, #25171 ) ;
#50471=( NAMED_UNIT ( * ) SI_UNIT ( $, .STERADIAN. ) SOLID_ANGLE_UNIT ( ) );
#50475=LINE ( 'NONE', #50821, #1695 ) ;
#50482=CARTESIAN_POINT ( 'NONE',  ( 12.72792206135785698, 149.9999999999999716, -10.50000000000000000 ) ) ;
#50485=SURFACE_STYLE_FILL_AREA ( #7566 ) ;
#50487=VECTOR ( 'NONE', #644, 1000.000000000000000 ) ;
#50494=EDGE_LOOP ( 'NONE', ( #3326, #66397, #23472, #13767 ) ) ;
#50495=CARTESIAN_POINT ( 'NONE',  ( -9.827790563157511022E-16, 134.5570736234661808, 8.025000000000000355 ) ) ;
#50497=CARTESIAN_POINT ( 'NONE',  ( 6.826472737025121695, 120.6070736234661496, -4.959722759717905660 ) ) ;
#50498=STYLED_ITEM ( 'NONE', ( #36028 ), #43940 ) ;
#50501=STYLED_ITEM ( 'NONE', ( #59518 ), #43032 ) ;
#50505=( NAMED_UNIT ( * ) SI_UNIT ( $, .STERADIAN. ) SOLID_ANGLE_UNIT ( ) );
#50506=ADVANCED_FACE ( 'NONE', ( #10720 ), #50518, .T. ) ;
#50507=CIRCLE ( 'NONE', #3299, 0.5000000000000004441 ) ;
#50511=EDGE_LOOP ( 'NONE', ( #27001, #10873, #49146, #21438 ) ) ;
#50516=CARTESIAN_POINT ( 'NONE',  ( -6.826472737025120807, 123.9929263765338163, 4.959722759717906548 ) ) ;
#50517=EDGE_CURVE ( 'NONE', #60543, #12588, #36799, .T. ) ;
#50518=CYLINDRICAL_SURFACE ( 'NONE', #35715, 15.00000000000000000 ) ;
#50519=COLOUR_RGB ( '', 0.09019608, 0.27058824, 0.51372549) ;
#50521=DIRECTION ( 'NONE',  ( 0.000000000000000000, 1.000000000000000000, 0.000000000000000000 ) ) ;
#50523=AXIS2_PLACEMENT_3D ( 'NONE', #29882, #51345, #24580 ) ;
#50525=CARTESIAN_POINT ( 'NONE',  ( -65.50000000000000000, -2.024042244987997205E-14, 6.500000000000000000 ) ) ;
#50526=EDGE_CURVE ( 'NONE', #61802, #43189, #80, .T. ) ;
#50528=DIRECTION ( 'NONE',  ( 0.000000000000000000, 0.000000000000000000, -1.000000000000000000 ) ) ;
#50529=EDGE_CURVE ( 'NONE', #10363, #26930, #36078, .T. ) ;
#50531=SURFACE_SIDE_STYLE ('',( #56126 ) ) ;
#50532=CARTESIAN_POINT ( 'NONE',  ( -67.99999999999998579, -2.024042244987997205E-14, 11.50000000000000000 ) ) ;
#50534=EDGE_CURVE ( 'NONE', #6975, #59919, #33440, .T. ) ;
#50535=CARTESIAN_POINT ( 'NONE',  ( -10.01517768586949408, 113.1949999999999790, -6.132527647946036459E-16 ) ) ;
#50539=ORIENTED_EDGE ( 'NONE', *, *, #27452, .F. ) ;
#50541=( NAMED_UNIT ( * ) PLANE_ANGLE_UNIT ( ) SI_UNIT ( $, .RADIAN. ) );
#50542=CARTESIAN_POINT ( 'NONE',  ( -60.00000000000000000, -2.024042244987997205E-14, -6.500000000000000000 ) ) ;
#50543=DIRECTION ( 'NONE',  ( -0.000000000000000000, -0.000000000000000000, -1.000000000000000000 ) ) ;
#50544=EDGE_LOOP ( 'NONE', ( #29998, #47640, #30287, #24194 ) ) ;
#50546=CARTESIAN_POINT ( 'NONE',  ( -45.00000000000000000, 9.999999999999978684, -4.000000000000000000 ) ) ;
#50553=( NAMED_UNIT ( * ) SI_UNIT ( $, .STERADIAN. ) SOLID_ANGLE_UNIT ( ) );
#50560=CARTESIAN_POINT ( 'NONE',  ( 5.598654528085809545, 146.2549999999999955, -7.705886871421373741 ) ) ;
#50562=VECTOR ( 'NONE', #45836, 1000.000000000000000 ) ;
#50570=DIRECTION ( 'NONE',  ( -1.000000000000000000, 0.000000000000000000, 0.000000000000000000 ) ) ;
#50571=VERTEX_POINT ( 'NONE', #69460 ) ;
#50580=EDGE_CURVE ( 'NONE', #67023, #25443, #12090, .T. ) ;
#50581=ORIENTED_EDGE ( 'NONE', *, *, #28625, .T. ) ;
#50583=ORIENTED_EDGE ( 'NONE', *, *, #68550, .T. ) ;
#50584=EDGE_CURVE ( 'NONE', #27560, #60303, #5756, .T. ) ;
#50591=CARTESIAN_POINT ( 'NONE',  ( -71.49999999999998579, 64.07124727947029896, 7.500000000000000000 ) ) ;
#50594=DIRECTION ( 'NONE',  ( -0.000000000000000000, -1.000000000000000000, -0.000000000000000000 ) ) ;
#50595=ORIENTED_EDGE ( 'NONE', *, *, #3337, .F. ) ;
#50596=CARTESIAN_POINT ( 'NONE',  ( -9.827790563157511022E-16, 145.4429263765338192, 8.025000000000000355 ) ) ;
#50597=CARTESIAN_POINT ( 'NONE',  ( -6.826472737025120807, 114.9929263765338163, 4.959722759717906548 ) ) ;
#50600=EDGE_LOOP ( 'NONE', ( #50665, #37816, #6440, #58838 ) ) ;
#50601=SURFACE_SIDE_STYLE ('',( #60784 ) ) ;
#50602=CARTESIAN_POINT ( 'NONE',  ( -6.826472737025120807, 139.5070736234661126, -4.959722759717907437 ) ) ;
#50603=CARTESIAN_POINT ( 'NONE',  ( -20.40217977176332553, 114.8427411095148472, 10.33293932795019643 ) ) ;
#50607=AXIS2_PLACEMENT_3D ( 'NONE', #16522, #36942, #48889 ) ;
#50608=CARTESIAN_POINT ( 'NONE',  ( 60.00000000000000000, 1.797044900979284448E-15, -12.00000000000000000 ) ) ;
#50609=ORIENTED_EDGE ( 'NONE', *, *, #18692, .T. ) ;
#50611=EDGE_CURVE ( 'NONE', #52417, #65027, #57045, .T. ) ;
#50612=CARTESIAN_POINT ( 'NONE',  ( -60.00000000000000000, -2.024042244987997205E-14, 6.999999999999995559 ) ) ;
#50614=ORIENTED_EDGE ( 'NONE', *, *, #65365, .F. ) ;
#50617=CARTESIAN_POINT ( 'NONE',  ( -24.21231517720798010, 113.4999999999999858, 7.000000000000000000 ) ) ;
#50618=( NAMED_UNIT ( * ) PLANE_ANGLE_UNIT ( ) SI_UNIT ( $, .RADIAN. ) );
#50619=DIRECTION ( 'NONE',  ( -0.000000000000000000, -0.000000000000000000, -1.000000000000000000 ) ) ;
#50627=DIRECTION ( 'NONE',  ( 0.9704308468600219006, -0.2413793103448194366, -0.000000000000000000 ) ) ;
#50629=ORIENTED_EDGE ( 'NONE', *, *, #66575, .T. ) ;
#50634=CARTESIAN_POINT ( 'NONE',  ( 8.111916646337986592, 154.4999999999999147, -5.069419100131139722 ) ) ;
#50638=CARTESIAN_POINT ( 'NONE',  ( -8.102448949553181734, 120.0049999999999955, -5.886773742842749790 ) ) ;
#50640=LINE ( 'NONE', #61867, #7228 ) ;
#50641=CARTESIAN_POINT ( 'NONE',  ( -4.716976649647098618, 142.1429263765338078, 6.492361379858953008 ) ) ;
#50646=LINE ( 'NONE', #12293, #34264 ) ;
#50647=CIRCLE ( 'NONE', #62991, 0.5000000000000004441 ) ;
#50648=ORIENTED_EDGE ( 'NONE', *, *, #12218, .T. ) ;
#50651=EDGE_CURVE ( 'NONE', #3770, #1012, #49398, .T. ) ;
#50653=CARTESIAN_POINT ( 'NONE',  ( -34.99999999999999289, 99.99999999999998579, 4.000000000000000000 ) ) ;
#50655=PRESENTATION_STYLE_ASSIGNMENT (( #2034 ) ) ;
#50656=ORIENTED_EDGE ( 'NONE', *, *, #59090, .F. ) ;
#50658=CIRCLE ( 'NONE', #58536, 0.5000000000000006661 ) ;
#50661=COLOUR_RGB ( '', 0.40784314, 0.44705882, 0.49803922) ;
#50665=ORIENTED_EDGE ( 'NONE', *, *, #63648, .F. ) ;
#50668=EDGE_CURVE ( 'NONE', #57165, #49424, #42475, .T. ) ;
#50671=CARTESIAN_POINT ( 'NONE',  ( -60.99999999999998579, 50.00000000000000000, -9.500000000000000000 ) ) ;
#50673=ORIENTED_EDGE ( 'NONE', *, *, #63528, .F. ) ;
#50676=CARTESIAN_POINT ( 'NONE',  ( 0.000000000000000000, 87.30187232391182306, 0.000000000000000000 ) ) ;
#50677=CARTESIAN_POINT ( 'NONE',  ( 3.094860106618431583, 144.0949999999999704, 9.525000000000000355 ) ) ;
#50679=AXIS2_PLACEMENT_3D ( 'NONE', #36134, #56879, #30118 ) ;
#50682=CARTESIAN_POINT ( 'NONE',  ( -9.058813317711338797, 135.4549999999999841, 2.943386871421373563 ) ) ;
#50683=EDGE_CURVE ( 'NONE', #5601, #66072, #767, .T. ) ;
#50685=CARTESIAN_POINT ( 'NONE',  ( -55.00000000000000000, -2.024042244987997205E-14, -7.000000000000024869 ) ) ;
#50686=ORIENTED_EDGE ( 'NONE', *, *, #28625, .F. ) ;
#50687=CARTESIAN_POINT ( 'NONE',  ( 8.437984349512095861, 116.1929263765338192, 1.550032578732817026E-15 ) ) ;
#50689=( LENGTH_UNIT ( ) NAMED_UNIT ( * ) SI_UNIT ( .MILLI., .METRE. ) );
#50694=ORIENTED_EDGE ( 'NONE', *, *, #40697, .F. ) ;
#50698=CONICAL_SURFACE ( 'NONE', #65290, 22.49999999999999645, 0.7853981633974239651 ) ;
#50700=ORIENTED_EDGE ( 'NONE', *, *, #37388, .T. ) ;
#50702=COLOUR_RGB ( '', 0.40784314, 0.44705882, 0.49803922) ;
#50703=( LENGTH_UNIT ( ) NAMED_UNIT ( * ) SI_UNIT ( .MILLI., .METRE. ) );
#50706=SURFACE_STYLE_FILL_AREA ( #39840 ) ;
#50708=EDGE_LOOP ( 'NONE', ( #39349, #2794, #34586, #25167 ) ) ;
#50714=DIRECTION ( 'NONE',  ( 0.000000000000000000, 0.000000000000000000, 1.000000000000000000 ) ) ;
#50717=( NAMED_UNIT ( * ) PLANE_ANGLE_UNIT ( ) SI_UNIT ( $, .RADIAN. ) );
#50718=STYLED_ITEM ( 'NONE', ( #4791 ), #54120 ) ;
#50721=CARTESIAN_POINT ( 'NONE',  ( -60.00000000000000000, -2.024042244987997205E-14, -11.50000000000000355 ) ) ;
#50725=CARTESIAN_POINT ( 'NONE',  ( -3.094860106618434248, 140.7950000000000159, 9.525000000000000355 ) ) ;
#50729=DIRECTION ( 'NONE',  ( 0.000000000000000000, 0.000000000000000000, 1.000000000000000000 ) ) ;
#50731=ADVANCED_FACE ( 'NONE', ( #39210 ), #41356, .T. ) ;
#50733=SURFACE_SIDE_STYLE ('',( #61958 ) ) ;
#50740=CARTESIAN_POINT ( 'NONE',  ( -8.437984349512095861, 127.8070736234661666, -5.166775262442723748E-16 ) ) ;
#50741=EDGE_LOOP ( 'NONE', ( #19348, #29948, #35920, #6803 ) ) ;
#50742=CIRCLE ( 'NONE', #49642, 16.44999999999999218 ) ;
#50744=EDGE_CURVE ( 'NONE', #37946, #61027, #38876, .T. ) ;
#50749=AXIS2_PLACEMENT_3D ( 'NONE', #62513, #56904, #24185 ) ;
#50750=COLOUR_RGB ( '', 0.72549020, 0.75294118, 0.79215686) ;
#50756=DIRECTION ( 'NONE',  ( -0.000000000000000000, -0.000000000000000000, -1.000000000000000000 ) ) ;
#50761=CARTESIAN_POINT ( 'NONE',  ( -9.827790563157511022E-16, 158.5570736234661524, 8.025000000000000355 ) ) ;
#50764=CARTESIAN_POINT ( 'NONE',  ( -9.058813317711337021, 114.1549999999999869, -2.943386871421374895 ) ) ;
#50768=CARTESIAN_POINT ( 'NONE',  ( -1.166476076187854022E-15, 127.0549999999999784, 9.525000000000000355 ) ) ;
#50772=CIRCLE ( 'NONE', #28282, 10.00000000000000533 ) ;
#50773=CARTESIAN_POINT ( 'NONE',  ( 20.44241585271047867, 115.3856657692246444, 10.00000000000000000 ) ) ;
#50774=AXIS2_PLACEMENT_3D ( 'NONE', #63336, #58754, #5263 ) ;
#50776=ORIENTED_EDGE ( 'NONE', *, *, #43516, .T. ) ;
#50779=DIRECTION ( 'NONE',  ( -0.2413793103448194644, 0.9704308468600220117, 0.000000000000000000 ) ) ;
#50782=ORIENTED_EDGE ( 'NONE', *, *, #48426, .T. ) ;
#50786=ORIENTED_EDGE ( 'NONE', *, *, #3952, .F. ) ;
#50787=STYLED_ITEM ( 'NONE', ( #12082 ), #24315 ) ;
#50788=CARTESIAN_POINT ( 'NONE',  ( -75.00000000000000000, 9.701542612659364906, 6.099661992412386269 ) ) ;
#50790=ORIENTED_EDGE ( 'NONE', *, *, #46425, .T. ) ;
#50791=EDGE_CURVE ( 'NONE', #60808, #22472, #56035, .T. ) ;
#50797=CARTESIAN_POINT ( 'NONE',  ( -60.00000000000000000, -2.024042244987997205E-14, 6.999999999999995559 ) ) ;
#50798=CARTESIAN_POINT ( 'NONE',  ( -10.01517768586949408, 143.1949999999999932, -6.132527647946036459E-16 ) ) ;
#50802=FILL_AREA_STYLE ('',( #33571 ) ) ;
#50803=FILL_AREA_STYLE_COLOUR ( '', #23772 ) ;
#50804=CIRCLE ( 'NONE', #63151, 5.500000000000005329 ) ;
#50809=CARTESIAN_POINT ( 'NONE',  ( 5.598654528085809545, 115.1449999999999818, -7.705886871421373741 ) ) ;
#50813=CYLINDRICAL_SURFACE ( 'NONE', #3179, 0.5000000000000004441 ) ;
#50815=DIRECTION ( 'NONE',  ( 0.000000000000000000, 1.000000000000000000, 0.000000000000000000 ) ) ;
#50820=CARTESIAN_POINT ( 'NONE',  ( -71.99999999999998579, 119.9999999999997868, -7.500000000000000000 ) ) ;
#50821=CARTESIAN_POINT ( 'NONE',  ( -45.00000000000000000, -2.024042244987997205E-14, 10.00000000000000000 ) ) ;
#50822=VECTOR ( 'NONE', #27739, 1000.000000000000000 ) ;
#50824=DIRECTION ( 'NONE',  ( -0.000000000000000000, 1.000000000000000000, 0.000000000000000000 ) ) ;
#50828=DIRECTION ( 'NONE',  ( 1.000000000000000000, 0.000000000000000000, 0.000000000000000000 ) ) ;
#50829=CIRCLE ( 'NONE', #44146, 0.5000000000000004441 ) ;
#50830=EDGE_CURVE ( 'NONE', #15666, #49707, #35299, .T. ) ;
#50831=CARTESIAN_POINT ( 'NONE',  ( 2.607480562269030688, 151.5929263765338249, 8.025000000000034106 ) ) ;
#50832=CIRCLE ( 'NONE', #68826, 0.4999999999999991118 ) ;
#50838=ORIENTED_EDGE ( 'NONE', *, *, #35241, .T. ) ;
#50840=VECTOR ( 'NONE', #35215, 1000.000000000000000 ) ;
#50842=CARTESIAN_POINT ( 'NONE',  ( 0.000000000000000000, 133.0570736234661524, -8.025000000000000355 ) ) ;
#50843=( GEOMETRIC_REPRESENTATION_CONTEXT ( 3 ) GLOBAL_UNCERTAINTY_ASSIGNED_CONTEXT ( ( #24832 ) ) GLOBAL_UNIT_ASSIGNED_CONTEXT ( ( #9868, #42592, #15171 ) ) REPRESENTATION_CONTEXT ( 'NONE', 'WORKASPACE' ) );
#50845=FILL_AREA_STYLE_COLOUR ( '', #46320 ) ;
#50847=VERTEX_POINT ( 'NONE', #24711 ) ;
#50850=CIRCLE ( 'NONE', #54202, 0.5000000000000004441 ) ;
#50852=DIRECTION ( 'NONE',  ( -1.156482317317873451E-16, -1.000000000000000000, 0.000000000000000000 ) ) ;
#50854=STYLED_ITEM ( 'NONE', ( #39138 ), #35927 ) ;
#50860=UNCERTAINTY_MEASURE_WITH_UNIT (LENGTH_MEASURE( 1.000000000000000082E-05 ), #27904, 'distance_accuracy_value', 'NONE');
#50862=AXIS2_PLACEMENT_3D ( 'NONE', #23414, #49829, #23095 ) ;
#50863=CIRCLE ( 'NONE', #20537, 18.00000000000000355 ) ;
#50864=SURFACE_STYLE_FILL_AREA ( #67380 ) ;
#50870=( NAMED_UNIT ( * ) SI_UNIT ( $, .STERADIAN. ) SOLID_ANGLE_UNIT ( ) );
#50871=CARTESIAN_POINT ( 'NONE',  ( -44.50000000000000000, 10.49999999999998224, -3.000000000000000444 ) ) ;
#50875=CARTESIAN_POINT ( 'NONE',  ( -9.058813317711337021, 116.0449999999999875, -2.943386871421374895 ) ) ;
#50877=CIRCLE ( 'NONE', #1352, 8.999999999999994671 ) ;
#50880=ORIENTED_EDGE ( 'NONE', *, *, #67258, .T. ) ;
#50882=DIRECTION ( 'NONE',  ( -0.000000000000000000, -0.000000000000000000, -1.000000000000000000 ) ) ;
#50889=( GEOMETRIC_REPRESENTATION_CONTEXT ( 3 ) GLOBAL_UNCERTAINTY_ASSIGNED_CONTEXT ( ( #12201 ) ) GLOBAL_UNIT_ASSIGNED_CONTEXT ( ( #15648, #63471, #58 ) ) REPRESENTATION_CONTEXT ( 'NONE', 'WORKASPACE' ) );
#50891=ORIENTED_EDGE ( 'NONE', *, *, #56962, .T. ) ;
#50892=CARTESIAN_POINT ( 'NONE',  ( 45.50000000000000000, -1.469576158976824618E-14, -10.00000000000000000 ) ) ;
#50894=CARTESIAN_POINT ( 'NONE',  ( 14.98999599679679662, 118.4999999999999716, -9.500000000000000000 ) ) ;
#50899=CARTESIAN_POINT ( 'NONE',  ( -1.166476076187854022E-15, 148.0549999999999784, 9.525000000000000355 ) ) ;
#50901=CARTESIAN_POINT ( 'NONE',  ( 0.000000000000000000, 110.4999999999999858, 22.50000000000000000 ) ) ;
#50902=ADVANCED_FACE ( 'NONE', ( #4658 ), #14397, .T. ) ;
#50910=CARTESIAN_POINT ( 'NONE',  ( -7.647808743681030030, 110.5000000000002984, 5.677732506914710875 ) ) ;
#50911=SURFACE_SIDE_STYLE ('',( #8357 ) ) ;
#50912=MECHANICAL_DESIGN_GEOMETRIC_PRESENTATION_REPRESENTATION('',(#58970),#9350);
#50913=CARTESIAN_POINT ( 'NONE',  ( 71.74137931034481142, 36.89918356738973415, -9.500000000000000000 ) ) ;
#50915=EDGE_CURVE ( 'NONE', #53532, #17136, #53221, .T. ) ;
#50916=SURFACE_STYLE_USAGE ( .BOTH. , #1948 ) ;
#50917=DIRECTION ( 'NONE',  ( 0.000000000000000000, 1.000000000000000000, 0.000000000000000000 ) ) ;
#50918=ORIENTED_EDGE ( 'NONE', *, *, #28257, .F. ) ;
#50929=DIRECTION ( 'NONE',  ( 0.000000000000000000, 0.000000000000000000, 1.000000000000000000 ) ) ;
#50930=ORIENTED_EDGE ( 'NONE', *, *, #956, .T. ) ;
#50931=DIRECTION ( 'NONE',  ( 0.000000000000000000, 0.000000000000000000, 1.000000000000000000 ) ) ;
#50932=CARTESIAN_POINT ( 'NONE',  ( -19.89974874213240597, 115.4999999999999574, -10.00000000000000000 ) ) ;
#50934=TOROIDAL_SURFACE ( 'NONE', #48723, 18.50000000000000355, 0.5000000000000000000 ) ;
#50935=( GEOMETRIC_REPRESENTATION_CONTEXT ( 3 ) GLOBAL_UNCERTAINTY_ASSIGNED_CONTEXT ( ( #31238 ) ) GLOBAL_UNIT_ASSIGNED_CONTEXT ( ( #46990, #25137, #36055 ) ) REPRESENTATION_CONTEXT ( 'NONE', 'WORKASPACE' ) );
#50936=( LENGTH_UNIT ( ) NAMED_UNIT ( * ) SI_UNIT ( .MILLI., .METRE. ) );
#50939=TOROIDAL_SURFACE ( 'NONE', #67812, 7.499999999999998224, 0.5000000000000000000 ) ;
#50940=CARTESIAN_POINT ( 'NONE',  ( -5.377101922857332461, 110.5000000000000000, -7.874436908571754934 ) ) ;
#50942=FACE_OUTER_BOUND ( 'NONE', #65397, .T. ) ;
#50944=CARTESIAN_POINT ( 'NONE',  ( 8.437984349512095861, 143.1929263765338192, 1.550032578732817026E-15 ) ) ;
#50946=FILL_AREA_STYLE ('',( #18239 ) ) ;
#50947=( NAMED_UNIT ( * ) PLANE_ANGLE_UNIT ( ) SI_UNIT ( $, .RADIAN. ) );
#50952=VERTEX_POINT ( 'NONE', #57799 ) ;
#50953=( NAMED_UNIT ( * ) SI_UNIT ( $, .STERADIAN. ) SOLID_ANGLE_UNIT ( ) );
#50954=CARTESIAN_POINT ( 'NONE',  ( 40.99999999999998579, 107.7459666924148252, -3.000000000000000444 ) ) ;
#50956=MECHANICAL_DESIGN_GEOMETRIC_PRESENTATION_REPRESENTATION('',(#25140),#68941);
#50959=( NAMED_UNIT ( * ) SI_UNIT ( $, .STERADIAN. ) SOLID_ANGLE_UNIT ( ) );
#50960=MECHANICAL_DESIGN_GEOMETRIC_PRESENTATION_REPRESENTATION('',(#45376),#40949);
#50961=FILL_AREA_STYLE_COLOUR ( '', #36181 ) ;
#50962=SURFACE_SIDE_STYLE ('',( #60454 ) ) ;
#50966=PRESENTATION_STYLE_ASSIGNMENT (( #29128 ) ) ;
#50968=ORIENTED_EDGE ( 'NONE', *, *, #32756, .T. ) ;
#50970=DIRECTION ( 'NONE',  ( 1.000000000000000000, 0.000000000000000000, -0.000000000000000000 ) ) ;
#50974=DIRECTION ( 'NONE',  ( 1.000000000000000000, 0.000000000000000000, 0.000000000000000000 ) ) ;
#50975=EDGE_LOOP ( 'NONE', ( #8504, #1002, #7824, #52073 ) ) ;
#50976=VECTOR ( 'NONE', #48501, 1000.000000000000114 ) ;
#50983=AXIS2_PLACEMENT_3D ( 'NONE', #57457, #31395, #69402 ) ;
#50985=CARTESIAN_POINT ( 'NONE',  ( 8.102448949553181734, 118.5049999999999955, 5.886773742842750679 ) ) ;
#50987=EDGE_CURVE ( 'NONE', #57704, #44431, #11035, .T. ) ;
#50992=UNCERTAINTY_MEASURE_WITH_UNIT (LENGTH_MEASURE( 1.000000000000000082E-05 ), #43295, 'distance_accuracy_value', 'NONE');
#50993=ADVANCED_FACE ( 'NONE', ( #1040 ), #8786, .T. ) ;
#50994=CARTESIAN_POINT ( 'NONE',  ( -75.00000000000000000, 9.708372675170620525, -6.000000000000000000 ) ) ;
#50995=COLOUR_RGB ( '', 0.40784314, 0.44705882, 0.49803922) ;
#50999=ADVANCED_FACE ( 'NONE', ( #59502 ), #49674, .T. ) ;
#51000=CARTESIAN_POINT ( 'NONE',  ( 68.00000000000000000, 2.776762340297169183E-15, 11.50000000000000000 ) ) ;
#51001=ADVANCED_FACE ( 'NONE', ( #48311 ), #39158, .F. ) ;
#51003=DIRECTION ( 'NONE',  ( 0.000000000000000000, 0.000000000000000000, 1.000000000000000000 ) ) ;
#51006=AXIS2_PLACEMENT_3D ( 'NONE', #6222, #59312, #5169 ) ;
#51007=CARTESIAN_POINT ( 'NONE',  ( 34.99999999999992895, 112.9999999999999858, -9.500000000000000000 ) ) ;
#51011=CARTESIAN_POINT ( 'NONE',  ( -74.99999999999998579, 50.00000000000000000, -10.00000000000000000 ) ) ;
#51013=DIRECTION ( 'NONE',  ( 0.000000000000000000, -1.000000000000000000, 0.000000000000000000 ) ) ;
#51017=ORIENTED_EDGE ( 'NONE', *, *, #5007, .F. ) ;
#51018=VECTOR ( 'NONE', #13094, 1000.000000000000000 ) ;
#51021=ORIENTED_EDGE ( 'NONE', *, *, #501, .T. ) ;
#51024=ORIENTED_EDGE ( 'NONE', *, *, #50580, .T. ) ;
#51025=MECHANICAL_DESIGN_GEOMETRIC_PRESENTATION_REPRESENTATION('',(#65626),#54367);
#51026=FILL_AREA_STYLE_COLOUR ( '', #32647 ) ;
#51027=CARTESIAN_POINT ( 'NONE',  ( 9.058813317711338797, 138.8449999999999989, -2.943386871421372675 ) ) ;
#51030=COLOUR_RGB ( '', 0.09019608, 0.27058824, 0.51372549) ;
#51031=FACE_OUTER_BOUND ( 'NONE', #69391, .T. ) ;
#51032=CARTESIAN_POINT ( 'NONE',  ( -5.598654528085808657, 138.7549999999999955, 7.705886871421373741 ) ) ;
#51033=( NAMED_UNIT ( * ) SI_UNIT ( $, .STERADIAN. ) SOLID_ANGLE_UNIT ( ) );
#51034=CARTESIAN_POINT ( 'NONE',  ( 41.08002123031661768, 107.6301924976394702, -3.280722492564373205 ) ) ;
#51035=EDGE_LOOP ( 'NONE', ( #57588, #13266, #65852 ) ) ;
#51036=CARTESIAN_POINT ( 'NONE',  ( -8.437984349512095861, 114.6929263765338050, -5.166775262442723748E-16 ) ) ;
#51038=UNCERTAINTY_MEASURE_WITH_UNIT (LENGTH_MEASURE( 1.000000000000000082E-05 ), #55225, 'distance_accuracy_value', 'NONE');
#51040=STYLED_ITEM ( 'NONE', ( #37792 ), #63109 ) ;
#51041=( NAMED_UNIT ( * ) SI_UNIT ( $, .STERADIAN. ) SOLID_ANGLE_UNIT ( ) );
#51049=CARTESIAN_POINT ( 'NONE',  ( 14.98999599679679662, 118.4999999999999716, -10.00000000000000000 ) ) ;
#51053=UNCERTAINTY_MEASURE_WITH_UNIT (LENGTH_MEASURE( 1.000000000000000082E-05 ), #52365, 'distance_accuracy_value', 'NONE');
#51054=EDGE_CURVE ( 'NONE', #20368, #31194, #11091, .T. ) ;
#51055=SURFACE_STYLE_USAGE ( .BOTH. , #14435 ) ;
#51057=DIRECTION ( 'NONE',  ( -0.000000000000000000, 0.000000000000000000, 1.000000000000000000 ) ) ;
#51059=ORIENTED_EDGE ( 'NONE', *, *, #13188, .T. ) ;
#51060=ORIENTED_EDGE ( 'NONE', *, *, #41565, .T. ) ;
#51062=CARTESIAN_POINT ( 'NONE',  ( 48.50000000000000000, 14.49137674618942384, -7.500000000000000000 ) ) ;
#51063=CARTESIAN_POINT ( 'NONE',  ( -60.00000000000000000, -2.024042244987997205E-14, -9.500000000000000000 ) ) ;
#51071=CARTESIAN_POINT ( 'NONE',  ( -75.00000000000000000, 8.588294701370022821, -5.575869277511084299 ) ) ;
#51073=ORIENTED_EDGE ( 'NONE', *, *, #23310, .F. ) ;
#51074=( NAMED_UNIT ( * ) SI_UNIT ( $, .STERADIAN. ) SOLID_ANGLE_UNIT ( ) );
#51077=AXIS2_PLACEMENT_3D ( 'NONE', #61894, #39449, #61211 ) ;
#51078=ADVANCED_FACE ( 'NONE', ( #68828 ), #47769, .F. ) ;
#51079=CARTESIAN_POINT ( 'NONE',  ( -1.166476076187854022E-15, 137.9449999999999932, 9.525000000000000355 ) ) ;
#51091=VECTOR ( 'NONE', #39411, 1000.000000000000000 ) ;
#51092=ADVANCED_FACE ( 'NONE', ( #53341 ), #48094, .F. ) ;
#51102=( LENGTH_UNIT ( ) NAMED_UNIT ( * ) SI_UNIT ( .MILLI., .METRE. ) );
#51104=CARTESIAN_POINT ( 'NONE',  ( 0.000000000000000000, 154.9999999999999716, -22.49999999999999645 ) ) ;
#51105=CIRCLE ( 'NONE', #16291, 0.5000000000000004441 ) ;
#51107=ORIENTED_EDGE ( 'NONE', *, *, #28655, .T. ) ;
#51110=CARTESIAN_POINT ( 'NONE',  ( -21.02379604162863913, 114.4999999999999574, -10.00000000000000000 ) ) ;
#51113=B_SPLINE_CURVE_WITH_KNOTS ( 'NONE', 3,
 ( #20677, #67464, #9088, #42187, #14009, #63579 ),
 .UNSPECIFIED., .F., .F.,
 ( 4, 2, 4 ),
 ( 0.000000000000000000, 0.0003058591473678551830, 0.0006117182947357103660 ),
 .UNSPECIFIED. ) ;
#51116=CARTESIAN_POINT ( 'NONE',  ( 0.000000000000000000, 115.4449999999999932, -9.525000000000000355 ) ) ;
#51118=FILL_AREA_STYLE_COLOUR ( '', #4885 ) ;
#51119=CARTESIAN_POINT ( 'NONE',  ( -9.058813317711338797, 111.4549999999999841, 2.943386871421373563 ) ) ;
#51122=CARTESIAN_POINT ( 'NONE',  ( -6.826472737025120807, 121.5070736234661410, -4.959722759717907437 ) ) ;
#51123=CARTESIAN_POINT ( 'NONE',  ( -5.598654528085808657, 141.7549999999999955, 7.705886871421373741 ) ) ;
#51125=FILL_AREA_STYLE_COLOUR ( '', #44412 ) ;
#51126=( NAMED_UNIT ( * ) SI_UNIT ( $, .STERADIAN. ) SOLID_ANGLE_UNIT ( ) );
#51127=CARTESIAN_POINT ( 'NONE',  ( 21.02379605245189964, 114.6413612702713465, 10.00000000000000000 ) ) ;
#51130=DIRECTION ( 'NONE',  ( -1.000000000000000000, 1.047380211910525101E-15, 0.000000000000000000 ) ) ;
#51131=CARTESIAN_POINT ( 'NONE',  ( -71.49999999999998579, 64.07124727947029896, -7.500000000000000000 ) ) ;
#51133=ORIENTED_EDGE ( 'NONE', *, *, #62836, .F. ) ;
#51135=CIRCLE ( 'NONE', #10661, 13.00000000000000533 ) ;
#51137=CIRCLE ( 'NONE', #1604, 30.00000000000000000 ) ;
#51142=ORIENTED_EDGE ( 'NONE', *, *, #65532, .T. ) ;
#51143=STYLED_ITEM ( 'NONE', ( #483 ), #64083 ) ;
#51144=( NAMED_UNIT ( * ) SI_UNIT ( $, .STERADIAN. ) SOLID_ANGLE_UNIT ( ) );
#51147=CYLINDRICAL_SURFACE ( 'NONE', #60903, 0.5000000000000004441 ) ;
#51148=COLOUR_RGB ( '', 0.72549020, 0.75294118, 0.79215686) ;
#51152=CARTESIAN_POINT ( 'NONE',  ( 9.058813317711337021, 138.5449999999999875, 2.943386871421375783 ) ) ;
#51155=EDGE_CURVE ( 'NONE', #15634, #59936, #69497, .T. ) ;
#51157=PRESENTATION_STYLE_ASSIGNMENT (( #14918 ) ) ;
#51158=CARTESIAN_POINT ( 'NONE',  ( 15.98999599679679839, 99.99999999999998579, 7.500000000000000000 ) ) ;
#51161=CIRCLE ( 'NONE', #56778, 0.5000000000000004441 ) ;
#51171=FILL_AREA_STYLE_COLOUR ( '', #60869 ) ;
#51172=AXIS2_PLACEMENT_3D ( 'NONE', #58597, #58954, #10764 ) ;
#51175=EDGE_CURVE ( 'NONE', #47726, #53938, #41451, .T. ) ;
#51176=CYLINDRICAL_SURFACE ( 'NONE', #26744, 0.5000000000000004441 ) ;
#51185=CARTESIAN_POINT ( 'NONE',  ( 24.21231517720798010, 113.4999999999999858, -7.500000000000000000 ) ) ;
#51187=CARTESIAN_POINT ( 'NONE',  ( 23.21231517720797655, 118.4999999999999716, 7.000000000000000000 ) ) ;
#51188=FILL_AREA_STYLE_COLOUR ( '', #28633 ) ;
#51191=ORIENTED_EDGE ( 'NONE', *, *, #46435, .T. ) ;
#51192=SURFACE_STYLE_USAGE ( .BOTH. , #12847 ) ;
#51195=CARTESIAN_POINT ( 'NONE',  ( 6.826472737025119919, 138.0070736234661695, 4.959722759717908325 ) ) ;
#51200=ORIENTED_EDGE ( 'NONE', *, *, #8102, .T. ) ;
#51205=FILL_AREA_STYLE_COLOUR ( '', #28345 ) ;
#51207=MECHANICAL_DESIGN_GEOMETRIC_PRESENTATION_REPRESENTATION('',(#50117),#36644);
#51216=LINE ( 'NONE', #52278, #68471 ) ;
#51219=ORIENTED_EDGE ( 'NONE', *, *, #20599, .T. ) ;
#51221=SURFACE_SIDE_STYLE ('',( #29030 ) ) ;
#51222=SURFACE_STYLE_USAGE ( .BOTH. , #45636 ) ;
#51225=CARTESIAN_POINT ( 'NONE',  ( -7.647808743681030030, 110.5000000000002984, 5.677732506914710875 ) ) ;
#51228=ADVANCED_FACE ( 'NONE', ( #55751 ), #20074, .T. ) ;
#51230=VERTEX_POINT ( 'NONE', #31333 ) ;
#51231=CARTESIAN_POINT ( 'NONE',  ( 2.607480562269030688, 121.5929263765338249, 8.025000000000034106 ) ) ;
#51233=CIRCLE ( 'NONE', #53496, 18.00000000000000355 ) ;
#51238=CARTESIAN_POINT ( 'NONE',  ( -6.087059439501893543, 111.0522570712095103, -6.604466948054985131 ) ) ;
#51245=SURFACE_STYLE_FILL_AREA ( #3341 ) ;
#51247=CARTESIAN_POINT ( 'NONE',  ( 71.74137931034479720, 63.10081643261027295, 9.500000000000000000 ) ) ;
#51252=CARTESIAN_POINT ( 'NONE',  ( -5.598654528085806881, 149.8549999999999898, -7.705886871421374629 ) ) ;
#51254=CIRCLE ( 'NONE', #5190, 1.000000000000000888 ) ;
#51258=CARTESIAN_POINT ( 'NONE',  ( -20.43039690318515156, 114.8190495831791793, -10.32375696423105360 ) ) ;
#51259=CARTESIAN_POINT ( 'NONE',  ( -5.812336001415696174, 110.6020537967688284, 7.425621158969065938 ) ) ;
#51261=DIRECTION ( 'NONE',  ( 0.000000000000000000, 1.000000000000000000, -0.000000000000000000 ) ) ;
#51264=ORIENTED_EDGE ( 'NONE', *, *, #33292, .F. ) ;
#51269=DIRECTION ( 'NONE',  ( -1.156482317317873451E-16, 1.000000000000000000, 0.000000000000000000 ) ) ;
#51270=CARTESIAN_POINT ( 'NONE',  ( 60.00000000000000000, 117.4999999999999716, -9.500000000000000000 ) ) ;
#51271=VERTEX_POINT ( 'NONE', #50820 ) ;
#51272=ORIENTED_EDGE ( 'NONE', *, *, #48826, .F. ) ;
#51276=CARTESIAN_POINT ( 'NONE',  ( 8.102448949553181734, 112.5049999999999670, 5.886773742842750679 ) ) ;
#51284=FACE_OUTER_BOUND ( 'NONE', #63805, .T. ) ;
#51286=CARTESIAN_POINT ( 'NONE',  ( -40.99999999999998579, 108.0000000000000000, 3.500000000000000000 ) ) ;
#51288=CARTESIAN_POINT ( 'NONE',  ( -6.826472737025120807, 144.3929263765338078, -4.959722759717907437 ) ) ;
#51290=SURFACE_STYLE_USAGE ( .BOTH. , #19617 ) ;
#51298=DIRECTION ( 'NONE',  ( 0.000000000000000000, 0.000000000000000000, -1.000000000000000000 ) ) ;
#51299=CARTESIAN_POINT ( 'NONE',  ( 0.000000000000000000, 139.0570736234661808, -8.025000000000000355 ) ) ;
#51300=DIRECTION ( 'NONE',  ( 1.000000000000000000, 0.000000000000000000, 0.000000000000000000 ) ) ;
#51303=PRESENTATION_STYLE_ASSIGNMENT (( #15087 ) ) ;
#51306=CARTESIAN_POINT ( 'NONE',  ( -75.00000000000000000, 36.00000000000000711, 9.581200359586295789 ) ) ;
#51315=EDGE_CURVE ( 'NONE', #8903, #54396, #11277, .T. ) ;
#51318=CYLINDRICAL_SURFACE ( 'NONE', #53782, 0.5000000000000004441 ) ;
#51322=LINE ( 'NONE', #44362, #24110 ) ;
#51325=CARTESIAN_POINT ( 'NONE',  ( 0.000000000000000000, 118.0570736234661524, -8.025000000000000355 ) ) ;
#51327=CARTESIAN_POINT ( 'NONE',  ( 2.182090618630762702, 154.5000000000000284, -9.281935407964393647 ) ) ;
#51328=FILL_AREA_STYLE ('',( #52038 ) ) ;
#51333=CARTESIAN_POINT ( 'NONE',  ( 3.094860106618431583, 121.2049999999999841, 9.525000000000000355 ) ) ;
#51337=STYLED_ITEM ( 'NONE', ( #58381 ), #50279 ) ;
#51341=( NAMED_UNIT ( * ) PLANE_ANGLE_UNIT ( ) SI_UNIT ( $, .RADIAN. ) );
#51342=ORIENTED_EDGE ( 'NONE', *, *, #16304, .T. ) ;
#51345=DIRECTION ( 'NONE',  ( 0.000000000000000000, 0.000000000000000000, -1.000000000000000000 ) ) ;
#51350=PRESENTATION_STYLE_ASSIGNMENT (( #39097 ) ) ;
#51351=VERTEX_POINT ( 'NONE', #48260 ) ;
#51352=ORIENTED_EDGE ( 'NONE', *, *, #46754, .T. ) ;
#51354=PRESENTATION_STYLE_ASSIGNMENT (( #29895 ) ) ;
#51359=ORIENTED_EDGE ( 'NONE', *, *, #45504, .F. ) ;
#51366=CARTESIAN_POINT ( 'NONE',  ( -9.058813317711337021, 137.0449999999999875, -2.943386871421374895 ) ) ;
#51370=CARTESIAN_POINT ( 'NONE',  ( -8.102448949553179958, 141.6049999999999613, 5.886773742842747126 ) ) ;
#51372=SURFACE_SIDE_STYLE ('',( #19706 ) ) ;
#51375=CARTESIAN_POINT ( 'NONE',  ( 0.000000000000000000, 113.9429263765338192, -8.025000000000000355 ) ) ;
#51376=AXIS2_PLACEMENT_3D ( 'NONE', #43141, #58925, #64550 ) ;
#51379=( GEOMETRIC_REPRESENTATION_CONTEXT ( 3 ) GLOBAL_UNCERTAINTY_ASSIGNED_CONTEXT ( ( #29748 ) ) GLOBAL_UNIT_ASSIGNED_CONTEXT ( ( #19720, #57352, #30956 ) ) REPRESENTATION_CONTEXT ( 'NONE', 'WORKASPACE' ) );
#51381=EDGE_CURVE ( 'NONE', #53103, #67023, #29080, .T. ) ;
#51388=ORIENTED_EDGE ( 'NONE', *, *, #8361, .F. ) ;
#51389=DIRECTION ( 'NONE',  ( 0.000000000000000000, 0.000000000000000000, 1.000000000000000000 ) ) ;
#51390=ADVANCED_FACE ( 'NONE', ( #315 ), #27435, .F. ) ;
#51392=LINE ( 'NONE', #9188, #50840 ) ;
#51394=CARTESIAN_POINT ( 'NONE',  ( 75.00000000000000000, 19.90218225813096353, 6.307374275523923934 ) ) ;
#51400=CIRCLE ( 'NONE', #23316, 0.5000000000000004441 ) ;
#51404=EDGE_CURVE ( 'NONE', #1721, #7517, #27980, .T. ) ;
#51405=( NAMED_UNIT ( * ) PLANE_ANGLE_UNIT ( ) SI_UNIT ( $, .RADIAN. ) );
#51406=EDGE_CURVE ( 'NONE', #15243, #39399, #47144, .T. ) ;
#51408=DIRECTION ( 'NONE',  ( 0.000000000000000000, 0.000000000000000000, -1.000000000000000000 ) ) ;
#51409=CARTESIAN_POINT ( 'NONE',  ( 34.99999999999992895, 112.9999999999999858, 7.000000000000000000 ) ) ;
#51412=CARTESIAN_POINT ( 'NONE',  ( -74.12583008533032114, 9.273068908601683091, -6.223864456579094373 ) ) ;
#51417=CARTESIAN_POINT ( 'NONE',  ( 3.094860106618431583, 138.0949999999999989, 9.525000000000000355 ) ) ;
#51420=CARTESIAN_POINT ( 'NONE',  ( -40.99999999999998579, 107.7459666924148394, -3.000000000000000444 ) ) ;
#51424=PRESENTATION_STYLE_ASSIGNMENT (( #18117 ) ) ;
#51435=SURFACE_SIDE_STYLE ('',( #34904 ) ) ;
#51436=CARTESIAN_POINT ( 'NONE',  ( -45.00000000000000000, 8.121151660575840481, 6.396433738441380079 ) ) ;
#51440=ORIENTED_EDGE ( 'NONE', *, *, #26651, .F. ) ;
#51448=CARTESIAN_POINT ( 'NONE',  ( -10.01517768586949231, 116.1949999999999932, -6.132527647946036459E-16 ) ) ;
#51449=VERTEX_POINT ( 'NONE', #22892 ) ;
#51450=( LENGTH_UNIT ( ) NAMED_UNIT ( * ) SI_UNIT ( .MILLI., .METRE. ) );
#51454=ORIENTED_EDGE ( 'NONE', *, *, #34335, .T. ) ;
#51455=CARTESIAN_POINT ( 'NONE',  ( -9.058813317711337021, 141.1549999999999727, -2.943386871421374895 ) ) ;
#51456=CARTESIAN_POINT ( 'NONE',  ( -41.49999999999997868, 10.49999999999998224, 3.500000000000000000 ) ) ;
#51457=SURFACE_STYLE_USAGE ( .BOTH. , #7503 ) ;
#51458=CARTESIAN_POINT ( 'NONE',  ( 20.04014546381213435, 115.4999999869038163, 10.00000000000000000 ) ) ;
#51459=ADVANCED_FACE ( 'NONE', ( #55921 ), #2392, .F. ) ;
#51460=( LENGTH_UNIT ( ) NAMED_UNIT ( * ) SI_UNIT ( .MILLI., .METRE. ) );
#51464=ORIENTED_EDGE ( 'NONE', *, *, #33913, .T. ) ;
#51465=CARTESIAN_POINT ( 'NONE',  ( 2.652578976365602692, 110.9659062983237732, 8.678865135533694541 ) ) ;
#51466=ADVANCED_FACE ( 'NONE', ( #44389 ), #17627, .T. ) ;
#51473=VECTOR ( 'NONE', #9371, 1000.000000000000000 ) ;
#51476=ORIENTED_EDGE ( 'NONE', *, *, #55194, .T. ) ;
#51481=CARTESIAN_POINT ( 'NONE',  ( -3.094860106618434248, 143.7949999999999875, 9.525000000000000355 ) ) ;
#51482=COLOUR_RGB ( '', 0.31764706, 0.68627451, 0.89019608) ;
#51484=EDGE_CURVE ( 'NONE', #16813, #41256, #56250, .T. ) ;
#51488=SURFACE_SIDE_STYLE ('',( #30025 ) ) ;
#51490=CARTESIAN_POINT ( 'NONE',  ( -71.49999999999998579, 64.07124727947029896, 7.500000000000000000 ) ) ;
#51491=SURFACE_STYLE_USAGE ( .BOTH. , #2560 ) ;
#51494=PRESENTATION_STYLE_ASSIGNMENT (( #46966 ) ) ;
#51498=VECTOR ( 'NONE', #53154, 1000.000000000000000 ) ;
#51503=AXIS2_PLACEMENT_3D ( 'NONE', #40922, #29978, #63025 ) ;
#51508=COLOUR_RGB ( '', 0.66274510, 0.83137255, 0.94901961) ;
#51509=PRESENTATION_STYLE_ASSIGNMENT (( #24757 ) ) ;
#51511=ADVANCED_FACE ( 'NONE', ( #40461 ), #56617, .F. ) ;
#51512=CARTESIAN_POINT ( 'NONE',  ( 71.49999999999998579, 119.9999999999997868, 7.500000000000000000 ) ) ;
#51516=SPHERICAL_SURFACE ( 'NONE', #59733, 0.5000000000000000000 ) ;
#51519=SURFACE_STYLE_USAGE ( .BOTH. , #56813 ) ;
#51520=DIRECTION ( 'NONE',  ( 0.000000000000000000, 0.000000000000000000, 1.000000000000000000 ) ) ;
#51522=CARTESIAN_POINT ( 'NONE',  ( -4.716976649647097730, 133.3570736234661638, -6.492361379858953896 ) ) ;
#51523=CIRCLE ( 'NONE', #21189, 0.5000000000000004441 ) ;
#51525=CARTESIAN_POINT ( 'NONE',  ( 2.607480562269071989, 128.7070736234661865, 8.025000000000002132 ) ) ;
#51529=CARTESIAN_POINT ( 'NONE',  ( 34.99999999999992895, 112.9999999999999858, -7.000000000000000000 ) ) ;
#51530=VECTOR ( 'NONE', #23444, 1000.000000000000000 ) ;
#51532=ORIENTED_EDGE ( 'NONE', *, *, #68968, .T. ) ;
#51536=EDGE_CURVE ( 'NONE', #36186, #35924, #22444, .T. ) ;
#51538=CARTESIAN_POINT ( 'NONE',  ( 75.00000000000000000, -2.215169945516535778E-14, 10.00000000000000000 ) ) ;
#51540=VERTEX_POINT ( 'NONE', #21393 ) ;
#51541=( NAMED_UNIT ( * ) PLANE_ANGLE_UNIT ( ) SI_UNIT ( $, .RADIAN. ) );
#51547=FILL_AREA_STYLE_COLOUR ( '', #3253 ) ;
#51548=DIRECTION ( 'NONE',  ( 1.000000000000000000, -0.000000000000000000, 0.000000000000000000 ) ) ;
#51549=EDGE_CURVE ( 'NONE', #60674, #42583, #37004, .T. ) ;
#51551=( NAMED_UNIT ( * ) PLANE_ANGLE_UNIT ( ) SI_UNIT ( $, .RADIAN. ) );
#51553=PRESENTATION_STYLE_ASSIGNMENT (( #18514 ) ) ;
#51555=( GEOMETRIC_REPRESENTATION_CONTEXT ( 3 ) GLOBAL_UNCERTAINTY_ASSIGNED_CONTEXT ( ( #16985 ) ) GLOBAL_UNIT_ASSIGNED_CONTEXT ( ( #41478, #21037, #58003 ) ) REPRESENTATION_CONTEXT ( 'NONE', 'WORKASPACE' ) );
#51561=DIRECTION ( 'NONE',  ( 0.000000000000000000, 0.000000000000000000, 1.000000000000000000 ) ) ;
#51562=CARTESIAN_POINT ( 'NONE',  ( -8.102448949553179958, 113.4949999999999761, 5.886773742842747126 ) ) ;
#51563=MECHANICAL_DESIGN_GEOMETRIC_PRESENTATION_REPRESENTATION('',(#48239),#69530);
#51566=EDGE_CURVE ( 'NONE', #2689, #28436, #68920, .T. ) ;
#51569=( GEOMETRIC_REPRESENTATION_CONTEXT ( 3 ) GLOBAL_UNCERTAINTY_ASSIGNED_CONTEXT ( ( #35599 ) ) GLOBAL_UNIT_ASSIGNED_CONTEXT ( ( #3811, #52410, #41169 ) ) REPRESENTATION_CONTEXT ( 'NONE', 'WORKASPACE' ) );
#51570=FILL_AREA_STYLE_COLOUR ( '', #9355 ) ;
#51573=CARTESIAN_POINT ( 'NONE',  ( 0.000000000000000000, 149.9999999999999716, 0.000000000000000000 ) ) ;
#51574=( NAMED_UNIT ( * ) SI_UNIT ( $, .STERADIAN. ) SOLID_ANGLE_UNIT ( ) );
#51578=STYLED_ITEM ( 'NONE', ( #31400 ), #15038 ) ;
#51581=COLOUR_RGB ( '', 0.09019608, 0.27058824, 0.51372549) ;
#51582=( LENGTH_UNIT ( ) NAMED_UNIT ( * ) SI_UNIT ( .MILLI., .METRE. ) );
#51584=FILL_AREA_STYLE_COLOUR ( '', #50702 ) ;
#51588=CIRCLE ( 'NONE', #59393, 8.999999999999994671 ) ;
#51591=CARTESIAN_POINT ( 'NONE',  ( -9.058813317711338797, 153.4549999999999841, 2.943386871421373563 ) ) ;
#51593=UNCERTAINTY_MEASURE_WITH_UNIT (LENGTH_MEASURE( 1.000000000000000082E-05 ), #5704, 'distance_accuracy_value', 'NONE');
#51594=CARTESIAN_POINT ( 'NONE',  ( 45.00000000000000000, -1.469576158976824618E-14, -7.000000000000000888 ) ) ;
#51596=DIRECTION ( 'NONE',  ( -0.000000000000000000, -0.000000000000000000, 1.000000000000000000 ) ) ;
#51599=AXIS2_PLACEMENT_3D ( 'NONE', #39667, #23805, #7976 ) ;
#51602=AXIS2_PLACEMENT_3D ( 'NONE', #66693, #50521, #13919 ) ;
#51603=ORIENTED_EDGE ( 'NONE', *, *, #55771, .F. ) ;
#51606=UNCERTAINTY_MEASURE_WITH_UNIT (LENGTH_MEASURE( 1.000000000000000082E-05 ), #11068, 'distance_accuracy_value', 'NONE');
#51611=AXIS2_PLACEMENT_3D ( 'NONE', #40599, #62013, #30010 ) ;
#51612=SURFACE_SIDE_STYLE ('',( #23242 ) ) ;
#51613=CARTESIAN_POINT ( 'NONE',  ( -45.00000000000000711, 9.680295737756338781, 6.198572516085028461 ) ) ;
#51616=EDGE_CURVE ( 'NONE', #49241, #10695, #53085, .T. ) ;
#51619=EDGE_CURVE ( 'NONE', #50261, #8395, #47863, .T. ) ;
#51621=ADVANCED_FACE ( 'NONE', ( #58690 ), #31955, .T. ) ;
#51624=ORIENTED_EDGE ( 'NONE', *, *, #17278, .F. ) ;
#51627=VERTEX_POINT ( 'NONE', #2289 ) ;
#51628=CARTESIAN_POINT ( 'NONE',  ( 74.49999999999998579, 119.9999999999997584, 10.00000000000000000 ) ) ;
#51631=CARTESIAN_POINT ( 'NONE',  ( 2.607480562269076430, 146.7929263765338135, -8.025000000000000355 ) ) ;
#51633=FACE_OUTER_BOUND ( 'NONE', #35587, .T. ) ;
#51634=COLOUR_RGB ( '', 0.40784314, 0.44705882, 0.49803922) ;
#51635=EDGE_CURVE ( 'NONE', #22849, #51540, #69591, .T. ) ;
#51637=SURFACE_SIDE_STYLE ('',( #57250 ) ) ;
#51640=EDGE_LOOP ( 'NONE', ( #26590, #43210, #34064, #24293 ) ) ;
#51642=DIRECTION ( 'NONE',  ( 0.000000000000000000, 0.000000000000000000, -1.000000000000000000 ) ) ;
#51643=SURFACE_SIDE_STYLE ('',( #18605 ) ) ;
#51644=CARTESIAN_POINT ( 'NONE',  ( 41.30888752411017606, 107.2690689356287663, -3.464811251346369581 ) ) ;
#51646=( NAMED_UNIT ( * ) SI_UNIT ( $, .STERADIAN. ) SOLID_ANGLE_UNIT ( ) );
#51648=CARTESIAN_POINT ( 'NONE',  ( 2.607480562269160362, 141.9070736234661467, -8.024999999999939959 ) ) ;
#51650=CIRCLE ( 'NONE', #53897, 0.5000000000000004441 ) ;
#51655=( NAMED_UNIT ( * ) SI_UNIT ( $, .STERADIAN. ) SOLID_ANGLE_UNIT ( ) );
#51657=PLANE ( 'NONE',  #53411 ) ;
#51659=CARTESIAN_POINT ( 'NONE',  ( 8.437984349512095861, 114.3070736234661666, 1.550032578732816828E-15 ) ) ;
#51667=MECHANICAL_DESIGN_GEOMETRIC_PRESENTATION_REPRESENTATION('',(#13430),#44966);
#51671=PLANE ( 'NONE',  #57924 ) ;
#51673=CARTESIAN_POINT ( 'NONE',  ( -74.83430136428034984, 35.83209040110467214, -9.876238371507287894 ) ) ;
#51674=( NAMED_UNIT ( * ) SI_UNIT ( $, .STERADIAN. ) SOLID_ANGLE_UNIT ( ) );
#51675=AXIS2_PLACEMENT_3D ( 'NONE', #68657, #33682, #6582 ) ;
#51682=CARTESIAN_POINT ( 'NONE',  ( 8.102448949553183510, 125.1049999999999756, -5.886773742842746238 ) ) ;
#51684=DIRECTION ( 'NONE',  ( -0.000000000000000000, -0.000000000000000000, -1.000000000000000000 ) ) ;
#51688=UNCERTAINTY_MEASURE_WITH_UNIT (LENGTH_MEASURE( 1.000000000000000082E-05 ), #62567, 'distance_accuracy_value', 'NONE');
#51689=AXIS2_PLACEMENT_3D ( 'NONE', #58100, #47594, #69669 ) ;
#51697=EDGE_CURVE ( 'NONE', #43730, #18512, #65113, .T. ) ;
#51698=DIRECTION ( 'NONE',  ( 1.000000000000000000, -4.336808689941999001E-16, 0.000000000000000000 ) ) ;
#51701=EDGE_LOOP ( 'NONE', ( #5275, #4339, #31628, #18989 ) ) ;
#51702=VERTEX_POINT ( 'NONE', #66378 ) ;
#51706=CARTESIAN_POINT ( 'NONE',  ( -4.716976649647097730, 147.2429263765338305, -6.492361379858953896 ) ) ;
#51708=FILL_AREA_STYLE_COLOUR ( '', #26243 ) ;
#51716=CARTESIAN_POINT ( 'NONE',  ( 44.43085292287471333, 10.23783787917596122, -3.500000000000000000 ) ) ;
#51722=AXIS2_PLACEMENT_3D ( 'NONE', #26666, #41876, #21769 ) ;
#51723=CARTESIAN_POINT ( 'NONE',  ( -8.102448949553181734, 142.8949999999999818, -5.886773742842749790 ) ) ;
#51726=CARTESIAN_POINT ( 'NONE',  ( 9.058813317711337021, 148.6549999999999727, 2.943386871421375783 ) ) ;
#51727=CIRCLE ( 'NONE', #16789, 23.00000000000000000 ) ;
#51730=CARTESIAN_POINT ( 'NONE',  ( -6.826472737025120807, 120.3929263765338220, -4.959722759717907437 ) ) ;
#51731=DIRECTION ( 'NONE',  ( 1.000000000000000000, 0.000000000000000000, 0.000000000000000000 ) ) ;
#51732=UNCERTAINTY_MEASURE_WITH_UNIT (LENGTH_MEASURE( 1.000000000000000082E-05 ), #49375, 'distance_accuracy_value', 'NONE');
#51733=FILL_AREA_STYLE ('',( #25330 ) ) ;
#51735=( NAMED_UNIT ( * ) SI_UNIT ( $, .STERADIAN. ) SOLID_ANGLE_UNIT ( ) );
#51737=SURFACE_SIDE_STYLE ('',( #2069 ) ) ;
#51738=( NAMED_UNIT ( * ) SI_UNIT ( $, .STERADIAN. ) SOLID_ANGLE_UNIT ( ) );
#51739=ORIENTED_EDGE ( 'NONE', *, *, #15514, .T. ) ;
#51741=LINE ( 'NONE', #24292, #4856 ) ;
#51742=ORIENTED_EDGE ( 'NONE', *, *, #14068, .F. ) ;
#51745=CARTESIAN_POINT ( 'NONE',  ( -72.49999999999998579, 119.9999999999997868, 10.00000000000000000 ) ) ;
#51746=CARTESIAN_POINT ( 'NONE',  ( -45.50000000000000000, 9.708372675170618749, -6.500000000000000000 ) ) ;
#51749=SPHERICAL_SURFACE ( 'NONE', #3637, 0.5000000000000000000 ) ;
#51750=UNCERTAINTY_MEASURE_WITH_UNIT (LENGTH_MEASURE( 1.000000000000000082E-05 ), #28277, 'distance_accuracy_value', 'NONE');
#51753=FACE_OUTER_BOUND ( 'NONE', #26251, .T. ) ;
#51755=CARTESIAN_POINT ( 'NONE',  ( 75.00000000000000000, 19.99999999999997868, 6.000000000000000000 ) ) ;
#51761=DIRECTION ( 'NONE',  ( 0.000000000000000000, 0.000000000000000000, 1.000000000000000000 ) ) ;
#51763=ORIENTED_EDGE ( 'NONE', *, *, #59289, .F. ) ;
#51766=( BOUNDED_SURFACE ( )  B_SPLINE_SURFACE ( 3, 2, ( 
 ( #58058, #68257, #36278 ),
 ( #47543, #57699, #4190 ),
 ( #25667, #20765, #42272 ),
 ( #17812, #44242, #66330 ),
 ( #28685, #43889, #39292 ),
 ( #33974, #12158, #11827 ) ),
 .UNSPECIFIED., .F., .F., .F. ) 
 B_SPLINE_SURFACE_WITH_KNOTS ( ( 4, 2, 4 ),
 ( 3, 3 ),
 ( 0.000000000000000000, 0.7853981633974482790, 1.570796326794896558 ),
 ( 0.000000000000000000, 1.000000000000000000 ),
 .UNSPECIFIED. ) 
 GEOMETRIC_REPRESENTATION_ITEM ( )  RATIONAL_B_SPLINE_SURFACE ( (
 ( 1.000000000000000000, 0.5847102846637692863, 1.000000000000000000),
 ( 1.000000000000000000, 0.5843845446924222919, 1.000000000000000000),
 ( 1.000000000000000000, 0.5995650817083321149, 1.000000000000000000),
 ( 1.000000000000000000, 0.6465434225961957937, 1.000000000000000000),
 ( 1.000000000000000000, 0.6778979487210353705, 1.000000000000000000),
 ( 1.000000000000000000, 0.7071067811865530128, 1.000000000000000000) ) ) 
 REPRESENTATION_ITEM ( '' )  SURFACE ( )  );
#51768=VECTOR ( 'NONE', #8512, 1000.000000000000000 ) ;
#51770=CARTESIAN_POINT ( 'NONE',  ( -8.102448949553181734, 136.8949999999999534, -5.886773742842749790 ) ) ;
#51776=( GEOMETRIC_REPRESENTATION_CONTEXT ( 3 ) GLOBAL_UNCERTAINTY_ASSIGNED_CONTEXT ( ( #24328 ) ) GLOBAL_UNIT_ASSIGNED_CONTEXT ( ( #16512, #16848, #33005 ) ) REPRESENTATION_CONTEXT ( 'NONE', 'WORKASPACE' ) );
#51777=CARTESIAN_POINT ( 'NONE',  ( -41.00754902350323050, 107.7352920524769786, -3.098114188008660896 ) ) ;
#51783=SURFACE_STYLE_FILL_AREA ( #41253 ) ;
#51784=( GEOMETRIC_REPRESENTATION_CONTEXT ( 3 ) GLOBAL_UNCERTAINTY_ASSIGNED_CONTEXT ( ( #36338 ) ) GLOBAL_UNIT_ASSIGNED_CONTEXT ( ( #39730, #29482, #23861 ) ) REPRESENTATION_CONTEXT ( 'NONE', 'WORKASPACE' ) );
#51785=EDGE_CURVE ( 'NONE', #66402, #5542, #22622, .T. ) ;
#51786=DIRECTION ( 'NONE',  ( 0.000000000000000000, 0.000000000000000000, 1.000000000000000000 ) ) ;
#51787=CYLINDRICAL_SURFACE ( 'NONE', #1206, 8.025000000000000355 ) ;
#51789=CYLINDRICAL_SURFACE ( 'NONE', #47339, 0.5000000000000004441 ) ;
#51791=AXIS2_PLACEMENT_3D ( 'NONE', #13522, #19139, #50828 ) ;
#51794=SURFACE_STYLE_FILL_AREA ( #35615 ) ;
#51796=CARTESIAN_POINT ( 'NONE',  ( 44.91886116991580735, 9.999999999999980460, 3.201362207699192997 ) ) ;
#51798=CARTESIAN_POINT ( 'NONE',  ( -7.632228543268607446, 142.6570736234661751, -2.479861379858953718 ) ) ;
#51799=VERTEX_POINT ( 'NONE', #40365 ) ;
#51802=ORIENTED_EDGE ( 'NONE', *, *, #67045, .F. ) ;
#51806=( GEOMETRIC_REPRESENTATION_CONTEXT ( 3 ) GLOBAL_UNCERTAINTY_ASSIGNED_CONTEXT ( ( #41162 ) ) GLOBAL_UNIT_ASSIGNED_CONTEXT ( ( #18197, #66741, #34706 ) ) REPRESENTATION_CONTEXT ( 'NONE', 'WORKASPACE' ) );
#51808=ADVANCED_FACE ( 'NONE', ( #24847 ), #29436, .T. ) ;
#51809=CARTESIAN_POINT ( 'NONE',  ( -5.598654528085808657, 110.6449999999999960, 7.705886871421373741 ) ) ;
#51811=CARTESIAN_POINT ( 'NONE',  ( 8.102448949553181734, 113.1049999999999898, -5.886773742842746238 ) ) ;
#51813=CIRCLE ( 'NONE', #5684, 0.5000000000000004441 ) ;
#51818=CARTESIAN_POINT ( 'NONE',  ( -8.102448949553181734, 135.0050000000000239, -5.886773742842749790 ) ) ;
#51820=SURFACE_SIDE_STYLE ('',( #24700 ) ) ;
#51824=SURFACE_SIDE_STYLE ('',( #30322 ) ) ;
#51830=CARTESIAN_POINT ( 'NONE',  ( 8.527945164174102644, 111.3821367850715376, 1.507062088730521499 ) ) ;
#51832=DIRECTION ( 'NONE',  ( 1.000000000000000000, 0.000000000000000000, 0.000000000000000000 ) ) ;
#51842=CARTESIAN_POINT ( 'NONE',  ( 44.28021770739999852, 9.999999999999980460, -3.500000000000000000 ) ) ;
#51847=CARTESIAN_POINT ( 'NONE',  ( -9.058813317711337021, 152.0449999999999875, -2.943386871421374895 ) ) ;
#51854=STYLED_ITEM ( 'NONE', ( #65038 ), #28085 ) ;
#51855=FACE_OUTER_BOUND ( 'NONE', #51035, .T. ) ;
#51857=( NAMED_UNIT ( * ) SI_UNIT ( $, .STERADIAN. ) SOLID_ANGLE_UNIT ( ) );
#51858=FACE_OUTER_BOUND ( 'NONE', #53280, .T. ) ;
#51860=( GEOMETRIC_REPRESENTATION_CONTEXT ( 3 ) GLOBAL_UNCERTAINTY_ASSIGNED_CONTEXT ( ( #55118 ) ) GLOBAL_UNIT_ASSIGNED_CONTEXT ( ( #28558, #61280, #34212 ) ) REPRESENTATION_CONTEXT ( 'NONE', 'WORKASPACE' ) );
#51863=FILL_AREA_STYLE_COLOUR ( '', #29071 ) ;
#51866=MECHANICAL_DESIGN_GEOMETRIC_PRESENTATION_REPRESENTATION('',(#7999),#61928);
#51870=( GEOMETRIC_REPRESENTATION_CONTEXT ( 3 ) GLOBAL_UNCERTAINTY_ASSIGNED_CONTEXT ( ( #22290 ) ) GLOBAL_UNIT_ASSIGNED_CONTEXT ( ( #43950, #48537, #27355 ) ) REPRESENTATION_CONTEXT ( 'NONE', 'WORKASPACE' ) );
#51872=CARTESIAN_POINT ( 'NONE',  ( 71.49999999999998579, 64.07124727947029896, -10.00000000000000000 ) ) ;
#51873=DIRECTION ( 'NONE',  ( 0.000000000000000000, 0.000000000000000000, 1.000000000000000000 ) ) ;
#51877=MECHANICAL_DESIGN_GEOMETRIC_PRESENTATION_REPRESENTATION('',(#55212),#37406);
#51879=CARTESIAN_POINT ( 'NONE',  ( 45.65811388300841855, 10.21937129433612235, -6.000000000000000000 ) ) ;
#51881=CIRCLE ( 'NONE', #21542, 0.5000000000000004441 ) ;
#51890=DIRECTION ( 'NONE',  ( 0.000000000000000000, 0.000000000000000000, 1.000000000000000000 ) ) ;
#51891=CARTESIAN_POINT ( 'NONE',  ( -4.716976649647097730, 130.3570736234661638, -6.492361379858953896 ) ) ;
#51892=SURFACE_SIDE_STYLE ('',( #8972 ) ) ;
#51895=LINE ( 'NONE', #56454, #37245 ) ;
#51896=EDGE_CURVE ( 'NONE', #8139, #44039, #47248, .T. ) ;
#51898=COLOUR_RGB ( '', 0.09019608, 0.27058824, 0.51372549) ;
#51900=( LENGTH_UNIT ( ) NAMED_UNIT ( * ) SI_UNIT ( .MILLI., .METRE. ) );
#51906=ORIENTED_EDGE ( 'NONE', *, *, #42869, .T. ) ;
#51908=B_SPLINE_CURVE_WITH_KNOTS ( 'NONE', 3,
 ( #27285, #53694, #42857, #26933, #64936, #37226, #48467, #48824, #15415, #10799, #16461, #16792, #843, #26604, #22384, #38264, #32952, #32246, #36872, #58289, #10117, #48125, #53026, #58638, #31544, #7257, #1900 ),
 .UNSPECIFIED., .F., .F.,
 ( 4, 2, 2, 2, 2, 2, 2, 1, 2, 2, 2, 2, 2, 4 ),
 ( 5.946939743265090950E-16, 0.002417576611438273116, 0.003626364917157114988, 0.004835153222875957293, 0.006043941528594800466, 0.007252729834313642772, 0.008461518140032485077, 0.009670306445751328250, 0.01087909475147017142, 0.01208788305718901633, 0.01329667136290785777, 0.01450545966862670268, 0.01692303628006438729, 0.01934061289150207363 ),
 .UNSPECIFIED. ) ;
#51909=VECTOR ( 'NONE', #59144, 1000.000000000000000 ) ;
#51914=STYLED_ITEM ( 'NONE', ( #16103 ), #23274 ) ;
#51916=FACE_OUTER_BOUND ( 'NONE', #50600, .T. ) ;
#51918=MECHANICAL_DESIGN_GEOMETRIC_PRESENTATION_REPRESENTATION('',(#64245),#65421);
#51921=CARTESIAN_POINT ( 'NONE',  ( -41.61282686761437333, 107.5028968421555930, 3.982829320873340073 ) ) ;
#51923=DIRECTION ( 'NONE',  ( -1.000000000000000000, 0.000000000000000000, 0.000000000000000000 ) ) ;
#51924=CARTESIAN_POINT ( 'NONE',  ( 3.094860106618435136, 112.2949999999999733, -9.525000000000000355 ) ) ;
#51926=EDGE_CURVE ( 'NONE', #69362, #11926, #59535, .T. ) ;
#51927=MECHANICAL_DESIGN_GEOMETRIC_PRESENTATION_REPRESENTATION('',(#31718),#54163);
#51930=ORIENTED_EDGE ( 'NONE', *, *, #32538, .T. ) ;
#51931=CARTESIAN_POINT ( 'NONE',  ( -23.21231517720797655, 112.9999999999999858, 9.500000000000000000 ) ) ;
#51935=( GEOMETRIC_REPRESENTATION_CONTEXT ( 3 ) GLOBAL_UNCERTAINTY_ASSIGNED_CONTEXT ( ( #2518 ) ) GLOBAL_UNIT_ASSIGNED_CONTEXT ( ( #25440, #41656, #57456 ) ) REPRESENTATION_CONTEXT ( 'NONE', 'WORKASPACE' ) );
#51937=( NAMED_UNIT ( * ) SI_UNIT ( $, .STERADIAN. ) SOLID_ANGLE_UNIT ( ) );
#51938=CARTESIAN_POINT ( 'NONE',  ( -0.4067914857153943076, 110.6009882518928720, -9.424011748107126607 ) ) ;
#51939=MECHANICAL_DESIGN_GEOMETRIC_PRESENTATION_REPRESENTATION('',(#49687),#18226);
#51948=VECTOR ( 'NONE', #60609, 1000.000000000000000 ) ;
#51952=CARTESIAN_POINT ( 'NONE',  ( 5.598654528085809545, 152.2549999999999670, -7.705886871421373741 ) ) ;
#51954=MECHANICAL_DESIGN_GEOMETRIC_PRESENTATION_REPRESENTATION('',(#59771),#39620);
#51962=CARTESIAN_POINT ( 'NONE',  ( -71.49999999999998579, 64.07124727947029896, 7.500000000000000000 ) ) ;
#51966=CYLINDRICAL_SURFACE ( 'NONE', #2474, 13.99999999999999822 ) ;
#51967=EDGE_LOOP ( 'NONE', ( #69534, #15847, #34577, #21510 ) ) ;
#51969=PLANE ( 'NONE',  #11667 ) ;
#51970=AXIS2_PLACEMENT_3D ( 'NONE', #21533, #52532, #68343 ) ;
#51972=STYLED_ITEM ( 'NONE', ( #46584 ), #54871 ) ;
#51975=( LENGTH_UNIT ( ) NAMED_UNIT ( * ) SI_UNIT ( .MILLI., .METRE. ) );
#51976=ORIENTED_EDGE ( 'NONE', *, *, #62409, .F. ) ;
#51979=CIRCLE ( 'NONE', #66583, 8.999999999999994671 ) ;
#51980=VERTEX_POINT ( 'NONE', #22022 ) ;
#51981=CARTESIAN_POINT ( 'NONE',  ( -9.058813317711338797, 117.4549999999999841, 2.943386871421373563 ) ) ;
#51984=CIRCLE ( 'NONE', #21641, 0.4999999999999994449 ) ;
#51989=FILL_AREA_STYLE ('',( #21604 ) ) ;
#51991=FILL_AREA_STYLE_COLOUR ( '', #48595 ) ;
#51992=AXIS2_PLACEMENT_3D ( 'NONE', #19520, #61715, #13198 ) ;
#51995=CARTESIAN_POINT ( 'NONE',  ( 6.826472737025121695, 140.4929263765338021, -4.959722759717905660 ) ) ;
#51996=CYLINDRICAL_SURFACE ( 'NONE', #47053, 0.5000000000000004441 ) ;
#52001=( NAMED_UNIT ( * ) SI_UNIT ( $, .STERADIAN. ) SOLID_ANGLE_UNIT ( ) );
#52005=MECHANICAL_DESIGN_GEOMETRIC_PRESENTATION_REPRESENTATION('',(#32921),#68879);
#52006=VECTOR ( 'NONE', #18487, 1000.000000000000114 ) ;
#52008=( NAMED_UNIT ( * ) PLANE_ANGLE_UNIT ( ) SI_UNIT ( $, .RADIAN. ) );
#52009=CARTESIAN_POINT ( 'NONE',  ( 4.716976649647099507, 141.7570736234661410, -6.492361379858953008 ) ) ;
#52012=AXIS2_PLACEMENT_3D ( 'NONE', #32583, #61319, #59667 ) ;
#52014=PLANE ( 'NONE',  #4713 ) ;
#52020=CARTESIAN_POINT ( 'NONE',  ( 4.716976649647099507, 114.7570736234661553, -6.492361379858953008 ) ) ;
#52030=CARTESIAN_POINT ( 'NONE',  ( 41.61274205743404053, 107.5029750606318402, 3.982828305957055726 ) ) ;
#52031=EDGE_LOOP ( 'NONE', ( #29827, #20937, #3609, #23525, #41746, #38056, #15127, #56892, #38462, #46900, #46010, #62848, #55785, #68627, #66488, #47151, #26941, #5231, #62350, #62609, #51976, #28467, #31179, #68178, #64556, #55870, #5822, #47175, #238, #25485, #32940, #52710, #38102, #18243 ) ) ;
#52034=SURFACE_SIDE_STYLE ('',( #29515 ) ) ;
#52035=CARTESIAN_POINT ( 'NONE',  ( 7.632228543268607446, 117.1570736234661609, 2.479861379858954606 ) ) ;
#52037=( LENGTH_UNIT ( ) NAMED_UNIT ( * ) SI_UNIT ( .MILLI., .METRE. ) );
#52038=FILL_AREA_STYLE_COLOUR ( '', #64034 ) ;
#52039=EDGE_CURVE ( 'NONE', #32455, #66131, #12380, .T. ) ;
#52042=EDGE_CURVE ( 'NONE', #62231, #3129, #26917, .T. ) ;
#52043=CARTESIAN_POINT ( 'NONE',  ( -10.01517768586949231, 132.3049999999999500, -6.132527647946036459E-16 ) ) ;
#52045=CARTESIAN_POINT ( 'NONE',  ( -75.00000000000000000, 9.708372675170620525, -6.000000000000000000 ) ) ;
#52048=AXIS2_PLACEMENT_3D ( 'NONE', #58084, #9895, #31310 ) ;
#52056=PRESENTATION_STYLE_ASSIGNMENT (( #18958 ) ) ;
#52057=EDGE_CURVE ( 'NONE', #51702, #43100, #22500, .T. ) ;
#52059=CARTESIAN_POINT ( 'NONE',  ( -75.00000000000000000, -2.215169945516535778E-14, -9.500000000000000000 ) ) ;
#52060=DIRECTION ( 'NONE',  ( -0.000000000000000000, -1.000000000000000000, 0.000000000000000000 ) ) ;
#52062=ORIENTED_EDGE ( 'NONE', *, *, #11634, .F. ) ;
#52063=CIRCLE ( 'NONE', #62118, 0.5000000000000004441 ) ;
#52065=STYLED_ITEM ( 'NONE', ( #67530 ), #61447 ) ;
#52066=MECHANICAL_DESIGN_GEOMETRIC_PRESENTATION_REPRESENTATION('',(#20615),#29599);
#52073=ORIENTED_EDGE ( 'NONE', *, *, #52669, .F. ) ;
#52077=ORIENTED_EDGE ( 'NONE', *, *, #39445, .F. ) ;
#52079=CARTESIAN_POINT ( 'NONE',  ( -45.50000000000000000, -2.024042244987997205E-14, 10.00000000000000000 ) ) ;
#52080=ORIENTED_EDGE ( 'NONE', *, *, #66895, .F. ) ;
#52084=( BOUNDED_CURVE ( )  B_SPLINE_CURVE ( 2, ( #14438, #57364, #20780, #42289, #20420, #68274, #9549, #30966, #41924, #36297, #20056 ),
 .UNSPECIFIED., .F., .F. ) 
 B_SPLINE_CURVE_WITH_KNOTS ( ( 3, 2, 2, 2, 2, 3 ),
 ( 0.6764705882352943789, 0.6823529411764708286, 0.6882352941176472783, 0.6941176470588237279, 0.7000000000000001776, 0.7058823529411767383 ),
 .UNSPECIFIED. ) 
 CURVE ( )  GEOMETRIC_REPRESENTATION_ITEM ( )  RATIONAL_B_SPLINE_CURVE ( ( 0.9999999999999981126, 0.9510565162951554186, 1.000000000000000000, 0.9510565162951535312, 1.000000000000000000, 0.9510565162951535312, 1.000000000000000000, 0.9510565162951535312, 1.000000000000000000, 0.9510565162951516438, 1.000000000000001776 ) ) 
 REPRESENTATION_ITEM ( '' )  );
#52085=CARTESIAN_POINT ( 'NONE',  ( 3.094860106618431583, 147.0949999999999704, 9.525000000000000355 ) ) ;
#52089=SURFACE_STYLE_FILL_AREA ( #35885 ) ;
#52090=CARTESIAN_POINT ( 'NONE',  ( 9.058813317711337021, 151.6549999999999727, 2.943386871421375783 ) ) ;
#52093=ORIENTED_EDGE ( 'NONE', *, *, #16069, .T. ) ;
#52094=CARTESIAN_POINT ( 'NONE',  ( 4.716976649647099507, 113.6429263765338078, -6.492361379858953008 ) ) ;
#52095=DIRECTION ( 'NONE',  ( 0.000000000000000000, -1.000000000000000000, 0.000000000000000000 ) ) ;
#52096=FACE_OUTER_BOUND ( 'NONE', #22998, .T. ) ;
#52098=AXIS2_PLACEMENT_3D ( 'NONE', #58466, #10290, #5667 ) ;
#52099=AXIS2_PLACEMENT_3D ( 'NONE', #56967, #4517, #24585 ) ;
#52101=CARTESIAN_POINT ( 'NONE',  ( 45.59262096826685706, 9.979230606950402205, -6.500000000000001776 ) ) ;
#52110=FILL_AREA_STYLE_COLOUR ( '', #10425 ) ;
#52111=( NAMED_UNIT ( * ) PLANE_ANGLE_UNIT ( ) SI_UNIT ( $, .RADIAN. ) );
#52113=CARTESIAN_POINT ( 'NONE',  ( 74.62643842725375976, 19.76989462323618341, 6.307273367294704336 ) ) ;
#52114=CARTESIAN_POINT ( 'NONE',  ( 9.827790563157511022E-16, 87.30187232391182306, -8.025000000000000355 ) ) ;
#52132=( NAMED_UNIT ( * ) PLANE_ANGLE_UNIT ( ) SI_UNIT ( $, .RADIAN. ) );
#52135=VECTOR ( 'NONE', #53845, 1000.000000000000000 ) ;
#52136=CARTESIAN_POINT ( 'NONE',  ( 9.058813317711337021, 147.5449999999999875, 2.943386871421375783 ) ) ;
#52138=SURFACE_STYLE_USAGE ( .BOTH. , #68643 ) ;
#52139=CIRCLE ( 'NONE', #57743, 27.49999999999999645 ) ;
#52150=DIRECTION ( 'NONE',  ( 0.6216216216216174928, -0.7833176619561892373, 0.000000000000000000 ) ) ;
#52156=( NAMED_UNIT ( * ) SI_UNIT ( $, .STERADIAN. ) SOLID_ANGLE_UNIT ( ) );
#52160=CARTESIAN_POINT ( 'NONE',  ( 2.607480562269113733, 118.5929263765338391, 8.024999999999973710 ) ) ;
#52165=VECTOR ( 'NONE', #1354, 1000.000000000000000 ) ;
#52169=VERTEX_POINT ( 'NONE', #39614 ) ;
#52170=VECTOR ( 'NONE', #27620, 1000.000000000000000 ) ;
#52171=LINE ( 'NONE', #68675, #7958 ) ;
#52172=EDGE_CURVE ( 'NONE', #15394, #35956, #62901, .T. ) ;
#52173=LINE ( 'NONE', #69367, #55631 ) ;
#52174=CARTESIAN_POINT ( 'NONE',  ( -7.632228543268608334, 157.9570736234661581, 2.479861379858952830 ) ) ;
#52175=VERTEX_POINT ( 'NONE', #54361 ) ;
#52177=CARTESIAN_POINT ( 'NONE',  ( 10.01517768586949408, 124.8049999999999784, 1.839758294383810543E-15 ) ) ;
#52179=( LENGTH_UNIT ( ) NAMED_UNIT ( * ) SI_UNIT ( .MILLI., .METRE. ) );
#52181=CARTESIAN_POINT ( 'NONE',  ( 10.01517768586949231, 136.8049999999999500, 1.839758294383810543E-15 ) ) ;
#52185=ORIENTED_EDGE ( 'NONE', *, *, #52288, .F. ) ;
#52190=( BOUNDED_CURVE ( )  B_SPLINE_CURVE ( 2, ( #2514, #24023, #8205, #55688, #56019, #56740, #51119, #24693, #46212, #29987, #67633, #40932, #24355, #7497, #8884, #62352, #35633, #51811, #39895, #28926, #45850, #35278, #57069, #13817, #50764, #19070, #45530, #61302, #3563, #40224, #13113, #67999, #7836, #50413, #40575, #2138, #61990, #18411, #9939, #3934, #68682, #46921, #68331, #15245, #58812, #20112, #37049, #58129, #31361, #10627, #19784, #42674, #42342, #4263, #48290, #32077, #15574, #15927, #4637, #36713, #41620, #52860, #62676, #63036, #52519, #53535, #26093, #20482, #30670, #14880, #63398, #47625, #37409, #35979, #69032, #5320, #20841, #36362, #26763, #25744, #47262, #41278, #14503, #58463, #9608, #57423, #63727, #41989, #64076, #10287, #31720, #53204, #9252, #4989, #31025, #52177, #26442, #25406, #57783, #47972, #69372, #21162, #22562, #49648, #38781, #1392, #64780, #7074, #5664, #683, #28504, #33460, #44420, #22921, #65821, #55247, #27798, #59480, #28140, #39121, #6712, #43031, #16618, #11655, #60510, #10962, #27111, #43710, #49303, #17654, #16284, #1014, #12324, #33125, #344, #33797, #32763, #27466, #59846, #38445, #40559, #11308, #21513, #44064, #48992, #64436, #22215, #65105, #16958, #37760, #60192, #54214, #59137, #54560, #32398, #53865, #6030, #48646, #38083, #21879, #43389, #11999, #6369, #65469, #17320, #54886, #50682, #56991, #13732, #24608, #3115, #46125, #35553, #8117, #39814, #8478, #19345, #56650, #50007, #29194, #35191, #40848, #2424, #61913, #34152, #50337, #29913, #67197, #51032, #18675, #23936, #24282, #44752, #14092, #66870, #55609, #62266, #17976, #60868, #8803, #55947, #13373, #61230, #1745, #18986, #34834, #23255, #51370, #7433, #66145, #2792, #34493, #56287, #45451, #12681, #67548, #28854, #39465, #40153, #2061, #23587, #61547, #40495, #29561, #45099, #66511, #18334, #13040, #45778, #7751, #41895, #25658, #14414, #57693, #58726, #15162, #63988, #37318, #35886, #10198, #30230, #9168, #46846, #63313, #3474, #30583, #62946, #15838, #36633, #9525, #31636, #68947, #53115, #25324, #51726, #57333, #30942, #24975, #63654, #4903, #26354, #58051, #46485, #68596, #4182, #47892, #67911, #52439, #19703, #68250, #9858, #21084, #47176, #42265, #52090, #3841, #69291, #47534, #31274, #20394, #52772, #15495, #20757, #4547, #41199, #42585, #36962, #58373, #62600, #20033, #41530, #26005, #14792, #36269, #27717 ),
 .UNSPECIFIED., .F., .T. ) 
 B_SPLINE_CURVE_WITH_KNOTS ( ( 3, 2, 2, 2, 2, 2, 2, 2, 2, 2, 2, 2, 2, 2, 2, 2, 2, 2, 2, 2, 2, 2, 2, 2, 2, 2, 2, 2, 2, 2, 2, 2, 2, 2, 2, 2, 2, 2, 2, 2, 2, 2, 2, 2, 2, 2, 2, 2, 2, 2, 2, 2, 2, 2, 2, 2, 2, 2, 2, 2, 2, 2, 2, 2, 2, 2, 2, 2, 2, 2, 2, 2, 2, 2, 2, 2, 2, 2, 2, 2, 2, 2, 2, 2, 2, 2, 2, 2, 2, 2, 2, 2, 2, 2, 2, 2, 2, 2, 2, 2, 2, 2, 2, 2, 2, 2, 2, 2, 2, 2, 2, 2, 2, 2, 2, 2, 2, 2, 2, 2, 2, 2, 2, 2, 2, 2, 2, 2, 2, 2, 2, 2, 2, 2, 2, 2, 2, 2, 2, 2, 2, 2, 2, 2, 2, 2, 2, 3 ),
 ( 0.000000000000000000, 0.005882352941176470507, 0.01176470588235294101, 0.01764705882352941152, 0.02352941176470588203, 0.02941176470588234906, 0.03529411764705882304, 0.04117647058823529355, 0.04705882352941176405, 0.05294117647058823456, 0.05882352941176469813, 0.06470588235294118251, 0.07058823529411764608, 0.07647058823529412352, 0.08235294117647058709, 0.08823529411764706454, 0.09411764705882352811, 0.1000000000000000194, 0.1058823529411764691, 0.1117647058823529466, 0.1176470588235293963, 0.1235294117647058876, 0.1294117647058823650, 0.1352941176470588147, 0.1411764705882352922, 0.1470588235294117696, 0.1529411764705882470, 0.1588235294117646967, 0.1647058823529411742, 0.1705882352941176794, 0.1764705882352941291, 0.1823529411764705788, 0.1882352941176470562, 0.1941176470588235337, 0.2000000000000000389, 0.2058823529411764330, 0.2117647058823529382, 0.2176470588235294157, 0.2235294117647058931, 0.2294117647058823428, 0.2352941176470587925, 0.2411764705882352977, 0.2470588235294117752, 0.2529411764705882248, 0.2588235294117647300, 0.2647058823529411797, 0.2705882352941176294, 0.2764705882352941346, 0.2823529411764705843, 0.2882352941176470340, 0.2941176470588235392, 0.2999999999999999889, 0.3058823529411764941, 0.3117647058823529438, 0.3176470588235293935, 0.3235294117647058987, 0.3294117647058823484, 0.3352941176470587981, 0.3411764705882353588, 0.3470588235294116974, 0.3529411764705882582, 0.3588235294117647078, 0.3647058823529411575, 0.3705882352941176627, 0.3764705882352941124, 0.3823529411764705621, 0.3882352941176470673, 0.3941176470588235170, 0.4000000000000000777, 0.4058823529411765274, 0.4117647058823528661, 0.4176470588235294268, 0.4235294117647058765, 0.4294117647058823262, 0.4352941176470588314, 0.4411764705882352811, 0.4470588235294117863, 0.4529411764705882359, 0.4588235294117646856, 0.4647058823529412463, 0.4705882352941175850, 0.4764705882352940347, 0.4823529411764705954, 0.4882352941176470451, 0.4941176470588235503, 0.5000000000000000000, 0.5058823529411764497, 0.5117647058823528994, 0.5176470588235294601, 0.5235294117647059098, 0.5294117647058823595, 0.5352941176470588092, 0.5411764705882352589, 0.5470588235294118196, 0.5529411764705882693, 0.5588235294117647189, 0.5647058823529411686, 0.5705882352941176183, 0.5764705882352940680, 0.5823529411764706287, 0.5882352941176470784, 0.5941176470588235281, 0.5999999999999999778, 0.6058823529411764275, 0.6117647058823529882, 0.6176470588235294379, 0.6235294117647058876, 0.6294117647058823373, 0.6352941176470587870, 0.6411764705882353477, 0.6470588235294117974, 0.6529411764705882470, 0.6588235294117646967, 0.6647058823529411464, 0.6705882352941175961, 0.6764705882352942679, 0.6823529411764707175, 0.6882352941176469452, 0.6941176470588233949, 0.6999999999999998446, 0.7058823529411765163, 0.7117647058823529660, 0.7176470588235294157, 0.7235294117647058654, 0.7294117647058823151, 0.7352941176470588758, 0.7411764705882353255, 0.7470588235294117752, 0.7529411764705882248, 0.7588235294117646745, 0.7647058823529411242, 0.7705882352941176849, 0.7764705882352941346, 0.7823529411764705843, 0.7882352941176470340, 0.7941176470588234837, 0.8000000000000001554, 0.8058823529411766051, 0.8117647058823530548, 0.8176470588235292825, 0.8235294117647057321, 0.8294117647058824039, 0.8352941176470588536, 0.8411764705882353033, 0.8470588235294117530, 0.8529411764705882026, 0.8588235294117646523, 0.8616690633200179139 ),
 .UNSPECIFIED. ) 
 CURVE ( )  GEOMETRIC_REPRESENTATION_ITEM ( )  RATIONAL_B_SPLINE_CURVE ( ( 1.000000000000000000, 0.9510565162951535312, 1.000000000000000000, 0.9510565162951535312, 1.000000000000000000, 0.9510565162951535312, 1.000000000000000000, 0.9510565162951535312, 1.000000000000000000, 0.9510565162951535312, 1.000000000000000000, 0.9510565162951535312, 1.000000000000000000, 0.9510565162951535312, 1.000000000000000000, 0.9510565162951535312, 1.000000000000000000, 0.9510565162951535312, 1.000000000000000000, 0.9510565162951535312, 1.000000000000000000, 0.9510565162951535312, 1.000000000000000000, 0.9510565162951535312, 1.000000000000000000, 0.9510565162951535312, 1.000000000000000000, 0.9510565162951535312, 1.000000000000000000, 0.9510565162951535312, 1.000000000000000000, 0.9510565162951535312, 1.000000000000000000, 0.9510565162951535312, 1.000000000000000000, 0.9510565162951535312, 1.000000000000000000, 0.9510565162951535312, 1.000000000000000000, 0.9510565162951535312, 1.000000000000000000, 0.9510565162951535312, 1.000000000000000000, 0.9510565162951535312, 1.000000000000000000, 0.9510565162951535312, 1.000000000000000000, 0.9510565162951535312, 1.000000000000000000, 0.9510565162951535312, 1.000000000000000000, 0.9510565162951535312, 1.000000000000000000, 0.9510565162951535312, 1.000000000000000000, 0.9510565162951535312, 1.000000000000000000, 0.9510565162951535312, 1.000000000000000000, 0.9510565162951535312, 1.000000000000000000, 0.9510565162951535312, 1.000000000000000000, 0.9510565162951535312, 1.000000000000000000, 0.9510565162951535312, 1.000000000000000000, 0.9510565162951535312, 1.000000000000000000, 0.9510565162951535312, 1.000000000000000000, 0.9510565162951535312, 1.000000000000000000, 0.9510565162951535312, 1.000000000000000000, 0.9510565162951535312, 1.000000000000000000, 0.9510565162951535312, 1.000000000000000000, 0.9510565162951535312, 1.000000000000000000, 0.9510565162951535312, 1.000000000000000000, 0.9510565162951535312, 1.000000000000000000, 0.9510565162951535312, 1.000000000000000000, 0.9510565162951535312, 1.000000000000000000, 0.9510565162951535312, 1.000000000000000000, 0.9510565162951535312, 1.000000000000000000, 0.9510565162951535312, 1.000000000000000000, 0.9510565162951535312, 1.000000000000000000, 0.9510565162951535312, 1.000000000000000000, 0.9510565162951535312, 1.000000000000000000, 0.9510565162951535312, 1.000000000000000000, 0.9510565162951535312, 1.000000000000000000, 0.9510565162951535312, 1.000000000000000000, 0.9510565162951535312, 1.000000000000000000, 0.9510565162951535312, 1.000000000000000000, 0.9510565162951535312, 1.000000000000000000, 0.9510565162951535312, 1.000000000000000000, 0.9510565162951535312, 1.000000000000000000, 0.9510565162951535312, 1.000000000000000000, 0.9510565162951535312, 1.000000000000000000, 0.9510565162951535312, 1.000000000000000000, 0.9510565162951535312, 1.000000000000000000, 0.9510565162951535312, 1.000000000000000000, 0.9510565162951535312, 1.000000000000000000, 0.9510565162951535312, 1.000000000000000000, 0.9510565162951535312, 1.000000000000000000, 0.9510565162951535312, 1.000000000000000000, 0.9510565162951535312, 1.000000000000000000, 0.9510565162951535312, 1.000000000000000000, 0.9510565162951535312, 1.000000000000000000, 0.9510565162951535312, 1.000000000000000000, 0.9510565162951535312, 1.000000000000000000, 0.9510565162951535312, 1.000000000000000000, 0.9510565162951535312, 1.000000000000000000, 0.9510565162951535312, 1.000000000000000000, 0.9510565162951535312, 1.000000000000000000, 0.9510565162951535312, 1.000000000000000000, 0.9510565162951535312, 1.000000000000000000, 0.9510565162951535312, 1.000000000000000000, 0.9510565162951535312, 1.000000000000000000, 0.9510565162951535312, 1.000000000000000000, 0.9510565162951535312, 1.000000000000000000, 0.9510565162951535312, 1.000000000000000000, 0.9510565162951535312, 1.000000000000000000, 0.9510565162951535312, 1.000000000000000000, 0.9510565162951535312, 1.000000000000000000, 0.9510565162951535312, 1.000000000000000000, 0.9510565162951535312, 1.000000000000000000, 0.9510565162951535312, 1.000000000000000000, 0.9510565162951535312, 1.000000000000000000, 0.9510565162951535312, 1.000000000000000000, 0.9510565162951535312, 1.000000000000000000, 0.9510565162951535312, 1.000000000000000000, 0.9510565162951535312, 1.000000000000000000, 0.9510565162951535312, 1.000000000000000000, 0.9510565162951535312, 1.000000000000000000, 0.9510565162951535312, 1.000000000000000000, 0.9510565162951535312, 1.000000000000000000, 0.9510565162951535312, 1.000000000000000000, 0.9510565162951535312, 1.000000000000000000, 0.9510565162951535312, 1.000000000000000000, 0.9510565162951535312, 1.000000000000000000, 0.9510565162951535312, 1.000000000000000000, 0.9510565162951535312, 1.000000000000000000, 0.9510565162951535312, 1.000000000000000000, 0.9510565162951535312, 1.000000000000000000, 0.9510565162951535312, 1.000000000000000000, 0.9510565162951535312, 1.000000000000000000, 0.9510565162951535312, 1.000000000000000000, 0.9510565162951535312, 1.000000000000000000, 0.9510565162951535312, 1.000000000000000000, 0.9510565162951535312, 1.000000000000000000, 0.9510565162951535312, 1.000000000000000000, 0.9510565162951535312, 1.000000000000000000, 0.9510565162951535312, 1.000000000000000000, 0.9510565162951535312, 1.000000000000000000, 0.9510565162951535312, 1.000000000000000000, 0.9510565162951535312, 1.000000000000000000, 0.9510565162951535312, 1.000000000000000000, 0.9510565162951535312, 1.000000000000000000, 0.9510565162951535312, 1.000000000000000000, 0.9510565162951535312, 1.000000000000000000, 0.9510565162951535312, 1.000000000000000000, 0.9510565162951535312, 1.000000000000000000, 0.9510565162951535312, 1.000000000000000000, 0.9510565162951535312, 1.000000000000000000, 0.9510565162951535312, 1.000000000000000000, 0.9510565162951535312, 1.000000000000000000, 0.9510565162951535312, 1.000000000000000000, 0.9510565162951535312, 1.000000000000000000, 0.9510565162951535312, 1.000000000000000000, 0.9510565162951535312, 1.000000000000000000, 0.9510565162951535312, 1.000000000000000000, 0.9510565162951535312, 1.000000000000000000, 0.9510565162951535312, 1.000000000000000000, 0.9510565162951535312, 1.000000000000000000, 0.9510565162951535312, 1.000000000000000000, 0.9510565162951535312, 1.000000000000000000, 0.9510565162951535312, 1.000000000000000000, 0.9510565162951535312, 1.000000000000000000, 0.9510565162951535312, 1.000000000000000000, 0.9510565162951535312, 1.000000000000000000, 0.9510565162951535312, 1.000000000000000000, 0.9510565162951535312, 1.000000000000000000, 0.9510565162951535312, 1.000000000000000000, 0.9510565162951535312, 1.000000000000000000, 0.9763240417800694848, 0.9755541358147066244 ) ) 
 REPRESENTATION_ITEM ( '' )  );
#52191=COLOUR_RGB ( '', 0.08235294, 0.09019608, 0.10196078) ;
#52195=CARTESIAN_POINT ( 'NONE',  ( 0.000000000000000000, 121.0570736234661524, -8.025000000000000355 ) ) ;
#52197=( GEOMETRIC_REPRESENTATION_CONTEXT ( 3 ) GLOBAL_UNCERTAINTY_ASSIGNED_CONTEXT ( ( #61634 ) ) GLOBAL_UNIT_ASSIGNED_CONTEXT ( ( #31344, #62663, #14863 ) ) REPRESENTATION_CONTEXT ( 'NONE', 'WORKASPACE' ) );
#52198=FILL_AREA_STYLE ('',( #19811 ) ) ;
#52202=ADVANCED_FACE ( 'NONE', ( #27610 ), #817, .F. ) ;
#52206=CARTESIAN_POINT ( 'NONE',  ( 3.094860106618435136, 151.2949999999999875, -9.525000000000000355 ) ) ;
#52210=DIRECTION ( 'NONE',  ( -0.000000000000000000, -1.000000000000000000, -0.000000000000000000 ) ) ;
#52218=CARTESIAN_POINT ( 'NONE',  ( 9.058813317711338797, 120.8449999999999847, -2.943386871421372675 ) ) ;
#52222=EDGE_CURVE ( 'NONE', #10363, #2682, #55059, .T. ) ;
#52224=SURFACE_STYLE_FILL_AREA ( #9296 ) ;
#52225=DIRECTION ( 'NONE',  ( -1.000000000000000000, 0.000000000000000000, 0.000000000000000000 ) ) ;
#52235=FACE_OUTER_BOUND ( 'NONE', #61727, .T. ) ;
#52236=CARTESIAN_POINT ( 'NONE',  ( 0.000000000000000000, 136.0570736234661808, -8.025000000000000355 ) ) ;
#52240=AXIS2_PLACEMENT_3D ( 'NONE', #16008, #5063, #17041 ) ;
#52241=CYLINDRICAL_SURFACE ( 'NONE', #56557, 0.5000000000000004441 ) ;
#52250=SURFACE_SIDE_STYLE ('',( #35704 ) ) ;
#52254=CARTESIAN_POINT ( 'NONE',  ( 0.000000000000000000, 130.0570736234661524, -8.025000000000000355 ) ) ;
#52260=ORIENTED_EDGE ( 'NONE', *, *, #18809, .T. ) ;
#52264=( LENGTH_UNIT ( ) NAMED_UNIT ( * ) SI_UNIT ( .MILLI., .METRE. ) );
#52266=( GEOMETRIC_REPRESENTATION_CONTEXT ( 3 ) GLOBAL_UNCERTAINTY_ASSIGNED_CONTEXT ( ( #32040 ) ) GLOBAL_UNIT_ASSIGNED_CONTEXT ( ( #12933, #8005, #9060 ) ) REPRESENTATION_CONTEXT ( 'NONE', 'WORKASPACE' ) );
#52273=DIRECTION ( 'NONE',  ( 0.000000000000000000, 1.000000000000000000, 0.000000000000000000 ) ) ;
#52274=UNCERTAINTY_MEASURE_WITH_UNIT (LENGTH_MEASURE( 1.000000000000000082E-05 ), #4181, 'distance_accuracy_value', 'NONE');
#52276=CARTESIAN_POINT ( 'NONE',  ( 34.99999999999992895, 110.4999999999999858, 10.00000000000000000 ) ) ;
#52277=CARTESIAN_POINT ( 'NONE',  ( -72.50000000000000000, 35.92875272052971525, 10.00000000000000000 ) ) ;
#52278=CARTESIAN_POINT ( 'NONE',  ( -75.00000000000000000, -2.215169945516535778E-14, 6.500000000000000000 ) ) ;
#52282=ORIENTED_EDGE ( 'NONE', *, *, #44751, .F. ) ;
#52283=FILL_AREA_STYLE_COLOUR ( '', #903 ) ;
#52285=CARTESIAN_POINT ( 'NONE',  ( 15.98999599679679839, 146.9999999999999716, 7.000000000000000000 ) ) ;
#52287=CARTESIAN_POINT ( 'NONE',  ( 3.094860106618435136, 121.2949999999999733, -9.525000000000000355 ) ) ;
#52288=EDGE_CURVE ( 'NONE', #26176, #49404, #35963, .T. ) ;
#52291=SURFACE_SIDE_STYLE ('',( #20598 ) ) ;
#52292=COLOUR_RGB ( '', 0.40784314, 0.44705882, 0.49803922) ;
#52295=CYLINDRICAL_SURFACE ( 'NONE', #10457, 0.5000000000000004441 ) ;
#52301=DIRECTION ( 'NONE',  ( 0.000000000000000000, 0.000000000000000000, -1.000000000000000000 ) ) ;
#52302=CARTESIAN_POINT ( 'NONE',  ( -4.877232780471185691, 110.9397655174076078, -7.675753971875499460 ) ) ;
#52304=EDGE_CURVE ( 'NONE', #18998, #42152, #8616, .T. ) ;
#52306=ORIENTED_EDGE ( 'NONE', *, *, #61045, .F. ) ;
#52307=COLOUR_RGB ( '', 0.66274510, 0.83137255, 0.94901961) ;
#52309=AXIS2_PLACEMENT_3D ( 'NONE', #30520, #53052, #4846 ) ;
#52314=VECTOR ( 'NONE', #40263, 1000.000000000000000 ) ;
#52316=CARTESIAN_POINT ( 'NONE',  ( 8.102448949553181734, 154.5049999999999670, 5.886773742842750679 ) ) ;
#52317=DIRECTION ( 'NONE',  ( 1.000000000000000000, 0.000000000000000000, 0.000000000000000000 ) ) ;
#52318=AXIS2_PLACEMENT_3D ( 'NONE', #43739, #40426, #34433 ) ;
#52319=DIRECTION ( 'NONE',  ( 0.000000000000000000, 0.000000000000000000, -1.000000000000000000 ) ) ;
#52322=CARTESIAN_POINT ( 'NONE',  ( -5.512442546754645178, 110.6161587570711191, 7.633710229764736788 ) ) ;
#52324=CIRCLE ( 'NONE', #30950, 8.000000000000007105 ) ;
#52325=LINE ( 'NONE', #25211, #32665 ) ;
#52334=FACE_OUTER_BOUND ( 'NONE', #31493, .T. ) ;
#52337=ORIENTED_EDGE ( 'NONE', *, *, #32910, .F. ) ;
#52341=DIRECTION ( 'NONE',  ( -0.000000000000000000, -0.000000000000000000, -1.000000000000000000 ) ) ;
#52342=VERTEX_POINT ( 'NONE', #42059 ) ;
#52343=CARTESIAN_POINT ( 'NONE',  ( -5.598654528085808657, 114.7549999999999812, 7.705886871421373741 ) ) ;
#52344=DIRECTION ( 'NONE',  ( -0.000000000000000000, -0.000000000000000000, 1.000000000000000000 ) ) ;
#52345=CARTESIAN_POINT ( 'NONE',  ( 0.000000000000000000, 154.9999999999999716, 0.000000000000000000 ) ) ;
#52350=( NAMED_UNIT ( * ) SI_UNIT ( $, .STERADIAN. ) SOLID_ANGLE_UNIT ( ) );
#52351=CARTESIAN_POINT ( 'NONE',  ( -65.49999999999997158, -2.024042244987997205E-14, -12.00000000000000000 ) ) ;
#52352=VERTEX_POINT ( 'NONE', #58185 ) ;
#52353=CARTESIAN_POINT ( 'NONE',  ( 6.826472737025121695, 158.4929263765337737, -4.959722759717905660 ) ) ;
#52354=COLOUR_RGB ( '', 0.72549020, 0.75294118, 0.79215686) ;
#52356=EDGE_CURVE ( 'NONE', #19997, #42076, #46183, .T. ) ;
#52358=CARTESIAN_POINT ( 'NONE',  ( 19.89974874213240597, 114.9999999999999574, -10.00000000000001421 ) ) ;
#52359=ORIENTED_EDGE ( 'NONE', *, *, #59547, .T. ) ;
#52360=CARTESIAN_POINT ( 'NONE',  ( 7.632228543268608334, 128.3429263765338249, -2.479861379858951942 ) ) ;
#52361=AXIS2_PLACEMENT_3D ( 'NONE', #50089, #46219, #24701 ) ;
#52362=COLOUR_RGB ( '', 0.08235294, 0.09019608, 0.10196078) ;
#52363=( LENGTH_UNIT ( ) NAMED_UNIT ( * ) SI_UNIT ( .MILLI., .METRE. ) );
#52365=( LENGTH_UNIT ( ) NAMED_UNIT ( * ) SI_UNIT ( .MILLI., .METRE. ) );
#52369=CARTESIAN_POINT ( 'NONE',  ( 0.000000000000000000, 115.4999999999999574, 16.00000000000000000 ) ) ;
#52372=ORIENTED_EDGE ( 'NONE', *, *, #13188, .F. ) ;
#52375=CARTESIAN_POINT ( 'NONE',  ( 44.99999999999998579, 119.9999999999999716, -7.500000000000000000 ) ) ;
#52377=DIRECTION ( 'NONE',  ( -1.000000000000000000, -4.336808689941999001E-16, 0.000000000000000000 ) ) ;
#52379=ORIENTED_EDGE ( 'NONE', *, *, #57297, .T. ) ;
#52383=FACE_OUTER_BOUND ( 'NONE', #68632, .T. ) ;
#52385=ADVANCED_FACE ( 'NONE', ( #68393 ), #19159, .T. ) ;
#52386=( GEOMETRIC_REPRESENTATION_CONTEXT ( 3 ) GLOBAL_UNCERTAINTY_ASSIGNED_CONTEXT ( ( #9346 ) ) GLOBAL_UNIT_ASSIGNED_CONTEXT ( ( #18697, #61570, #24305 ) ) REPRESENTATION_CONTEXT ( 'NONE', 'WORKASPACE' ) );
#52389=ORIENTED_EDGE ( 'NONE', *, *, #63228, .F. ) ;
#52390=DIRECTION ( 'NONE',  ( 0.000000000000000000, 0.000000000000000000, 1.000000000000000000 ) ) ;
#52395=SURFACE_SIDE_STYLE ('',( #4492 ) ) ;
#52396=PRESENTATION_STYLE_ASSIGNMENT (( #9821 ) ) ;
#52398=CARTESIAN_POINT ( 'NONE',  ( -3.094860106618434248, 126.9049999999999869, 9.525000000000000355 ) ) ;
#52400=DIRECTION ( 'NONE',  ( -0.000000000000000000, 1.000000000000000000, -0.000000000000000000 ) ) ;
#52402=DIRECTION ( 'NONE',  ( -1.000000000000000000, 0.000000000000000000, 0.000000000000000000 ) ) ;
#52405=AXIS2_PLACEMENT_3D ( 'NONE', #36513, #2039, #34126 ) ;
#52410=( NAMED_UNIT ( * ) PLANE_ANGLE_UNIT ( ) SI_UNIT ( $, .RADIAN. ) );
#52414=CARTESIAN_POINT ( 'NONE',  ( 2.607480562268992941, 135.9070736234661751, -8.025000000000060751 ) ) ;
#52417=VERTEX_POINT ( 'NONE', #43454 ) ;
#52422=( NAMED_UNIT ( * ) PLANE_ANGLE_UNIT ( ) SI_UNIT ( $, .RADIAN. ) );
#52423=ORIENTED_EDGE ( 'NONE', *, *, #56530, .T. ) ;
#52429=VERTEX_POINT ( 'NONE', #7138 ) ;
#52430=DIRECTION ( 'NONE',  ( 0.000000000000000000, 0.000000000000000000, 1.000000000000000000 ) ) ;
#52432=ORIENTED_EDGE ( 'NONE', *, *, #67061, .F. ) ;
#52434=CARTESIAN_POINT ( 'NONE',  ( -8.102448949553181734, 145.8949999999999534, -5.886773742842749790 ) ) ;
#52439=CARTESIAN_POINT ( 'NONE',  ( -8.102448949553179958, 150.6049999999999898, 5.886773742842747126 ) ) ;
#52440=DIRECTION ( 'NONE',  ( 1.000000000000000000, 0.000000000000000000, 0.000000000000000000 ) ) ;
#52441=DIRECTION ( 'NONE',  ( 0.000000000000000000, 1.000000000000000000, 0.000000000000000000 ) ) ;
#52442=ORIENTED_EDGE ( 'NONE', *, *, #1046, .F. ) ;
#52443=CARTESIAN_POINT ( 'NONE',  ( -6.826472737025120807, 126.9929263765338163, 4.959722759717906548 ) ) ;
#52445=UNCERTAINTY_MEASURE_WITH_UNIT (LENGTH_MEASURE( 1.000000000000000082E-05 ), #68711, 'distance_accuracy_value', 'NONE');
#52449=FILL_AREA_STYLE ('',( #9869 ) ) ;
#52450=ADVANCED_FACE ( 'NONE', ( #39179 ), #34895, .T. ) ;
#52452=CARTESIAN_POINT ( 'NONE',  ( 41.25890975875731215, 107.3519676386824813, 3.442113426143906807 ) ) ;
#52453=EDGE_LOOP ( 'NONE', ( #24283, #20944, #1426, #15991 ) ) ;
#52455=DIRECTION ( 'NONE',  ( 0.000000000000000000, 0.000000000000000000, 1.000000000000000000 ) ) ;
#52463=DIRECTION ( 'NONE',  ( -1.000000000000000000, -0.000000000000000000, -0.000000000000000000 ) ) ;
#52464=ORIENTED_EDGE ( 'NONE', *, *, #1933, .F. ) ;
#52473=VECTOR ( 'NONE', #65645, 1000.000000000000000 ) ;
#52475=CARTESIAN_POINT ( 'NONE',  ( -60.00000000000000000, -2.024042244987997205E-14, -7.500000000000000000 ) ) ;
#52481=( BOUNDED_CURVE ( )  B_SPLINE_CURVE ( 2, ( #56007, #35262, #8188, #34555, #51798, #34220, #18728, #55674, #7823, #29637, #7486 ),
 .UNSPECIFIED., .F., .F. ) 
 B_SPLINE_CURVE_WITH_KNOTS ( ( 3, 2, 2, 2, 2, 3 ),
 ( 0.6470588235294115753, 0.6529411764705880250, 0.6588235294117644747, 0.6647058823529409244, 0.6705882352941173741, 0.6764705882352939348 ),
 .UNSPECIFIED. ) 
 CURVE ( )  GEOMETRIC_REPRESENTATION_ITEM ( )  RATIONAL_B_SPLINE_CURVE ( ( 1.000000000000001776, 0.9510565162951516438, 1.000000000000000000, 0.9510565162951535312, 1.000000000000000000, 0.9510565162951535312, 1.000000000000000000, 0.9510565162951535312, 1.000000000000000000, 0.9510565162951554186, 0.9999999999999981126 ) ) 
 REPRESENTATION_ITEM ( '' )  );
#52485=STYLED_ITEM ( 'NONE', ( #37417 ), #40490 ) ;
#52486=CARTESIAN_POINT ( 'NONE',  ( 8.102448949553181734, 147.3950000000000102, 5.886773742842750679 ) ) ;
#52489=CARTESIAN_POINT ( 'NONE',  ( 20.71231517720798010, 149.9999999999999716, -10.00000000000000000 ) ) ;
#52490=UNCERTAINTY_MEASURE_WITH_UNIT (LENGTH_MEASURE( 1.000000000000000082E-05 ), #61780, 'distance_accuracy_value', 'NONE');
#52493=ORIENTED_EDGE ( 'NONE', *, *, #68539, .T. ) ;
#52497=( LENGTH_UNIT ( ) NAMED_UNIT ( * ) SI_UNIT ( .MILLI., .METRE. ) );
#52502=DIRECTION ( 'NONE',  ( 0.000000000000000000, -1.000000000000000000, 0.000000000000000000 ) ) ;
#52503=CARTESIAN_POINT ( 'NONE',  ( -45.00000000000000000, 8.545765431912348831, 5.556277950132127330 ) ) ;
#52506=CIRCLE ( 'NONE', #4142, 0.5000000000000004441 ) ;
#52507=ORIENTED_EDGE ( 'NONE', *, *, #21290, .F. ) ;
#52511=FILL_AREA_STYLE ('',( #9601 ) ) ;
#52515=CARTESIAN_POINT ( 'NONE',  ( -9.058813317711337021, 125.0449999999999875, -2.943386871421374895 ) ) ;
#52518=PRESENTATION_STYLE_ASSIGNMENT (( #9251 ) ) ;
#52519=CARTESIAN_POINT ( 'NONE',  ( -9.058813317711337021, 120.1549999999999869, -2.943386871421374895 ) ) ;
#52521=CARTESIAN_POINT ( 'NONE',  ( 71.74137931034481142, 36.89918356738973415, 9.500000000000000000 ) ) ;
#52522=EDGE_LOOP ( 'NONE', ( #16606, #55678, #10275, #6278 ) ) ;
#52523=CARTESIAN_POINT ( 'NONE',  ( -8.102448949553181734, 138.0049999999999670, -5.886773742842749790 ) ) ;
#52525=ADVANCED_FACE ( 'NONE', ( #62659 ), #29265, .F. ) ;
#52528=ADVANCED_FACE ( 'NONE', ( #41262 ), #13438, .T. ) ;
#52532=DIRECTION ( 'NONE',  ( 7.080503983578803083E-17, 1.000000000000000000, 0.000000000000000000 ) ) ;
#52536=CARTESIAN_POINT ( 'NONE',  ( 7.789749869348521649, 111.5987935625219052, -3.257487185497865312 ) ) ;
#52537=CARTESIAN_POINT ( 'NONE',  ( 41.49999999999998579, 106.9282032302754999, -4.000000000000000000 ) ) ;
#52538=( NAMED_UNIT ( * ) PLANE_ANGLE_UNIT ( ) SI_UNIT ( $, .RADIAN. ) );
#52539=VERTEX_POINT ( 'NONE', #7819 ) ;
#52548=CARTESIAN_POINT ( 'NONE',  ( -15.98999599679679839, 146.9999999999999716, 7.500000000000000000 ) ) ;
#52551=CARTESIAN_POINT ( 'NONE',  ( 5.598654528085809545, 148.1450000000000102, -7.705886871421373741 ) ) ;
#52553=EDGE_LOOP ( 'NONE', ( #65896, #67284, #68649, #22681 ) ) ;
#52554=CARTESIAN_POINT ( 'NONE',  ( 75.00000000000000000, -2.215169945516535778E-14, 6.999999999999999112 ) ) ;
#52557=( NAMED_UNIT ( * ) PLANE_ANGLE_UNIT ( ) SI_UNIT ( $, .RADIAN. ) );
#52563=CARTESIAN_POINT ( 'NONE',  ( -3.094860106618432471, 124.5949999999999704, -9.525000000000000355 ) ) ;
#52565=CARTESIAN_POINT ( 'NONE',  ( -60.99999999999998579, 50.00000000000000000, 7.500000000000000000 ) ) ;
#52566=ADVANCED_FACE ( 'NONE', ( #56721 ), #18725, .F. ) ;
#52567=FACE_OUTER_BOUND ( 'NONE', #15341, .T. ) ;
#52573=VECTOR ( 'NONE', #43165, 999.9999999999998863 ) ;
#52577=CARTESIAN_POINT ( 'NONE',  ( -48.50000000000000000, 13.41640786499872284, -7.500000000000000000 ) ) ;
#52578=EDGE_LOOP ( 'NONE', ( #64192, #34545, #44643, #43198 ) ) ;
#52590=( NAMED_UNIT ( * ) PLANE_ANGLE_UNIT ( ) SI_UNIT ( $, .RADIAN. ) );
#52591=EDGE_LOOP ( 'NONE', ( #56474, #49436, #17199, #31053 ) ) ;
#52593=( NAMED_UNIT ( * ) PLANE_ANGLE_UNIT ( ) SI_UNIT ( $, .RADIAN. ) );
#52594=CARTESIAN_POINT ( 'NONE',  ( 4.716976649647099507, 144.7570736234661410, -6.492361379858953008 ) ) ;
#52600=UNCERTAINTY_MEASURE_WITH_UNIT (LENGTH_MEASURE( 1.000000000000000082E-05 ), #22081, 'distance_accuracy_value', 'NONE');
#52602=VERTEX_POINT ( 'NONE', #10270 ) ;
#52603=MECHANICAL_DESIGN_GEOMETRIC_PRESENTATION_REPRESENTATION('',(#5359),#47001);
#52604=CARTESIAN_POINT ( 'NONE',  ( -23.71231517720798010, 117.4999999999999716, -7.500000000000000000 ) ) ;
#52605=EDGE_CURVE ( 'NONE', #50571, #59291, #63856, .T. ) ;
#52608=VERTEX_POINT ( 'NONE', #57406 ) ;
#52611=ORIENTED_EDGE ( 'NONE', *, *, #22161, .F. ) ;
#52612=CARTESIAN_POINT ( 'NONE',  ( 44.99999999999977973, 149.9999999999999716, 9.500000000000000000 ) ) ;
#52616=SURFACE_STYLE_FILL_AREA ( #9707 ) ;
#52617=VECTOR ( 'NONE', #6412, 1000.000000000000000 ) ;
#52618=EDGE_CURVE ( 'NONE', #67222, #7479, #41601, .T. ) ;
#52620=ORIENTED_EDGE ( 'NONE', *, *, #30377, .F. ) ;
#52621=FILL_AREA_STYLE ('',( #26544 ) ) ;
#52623=DIRECTION ( 'NONE',  ( 1.224646799147353207E-16, 1.000000000000000000, -0.000000000000000000 ) ) ;
#52624=FILL_AREA_STYLE_COLOUR ( '', #68998 ) ;
#52625=DIRECTION ( 'NONE',  ( 0.000000000000000000, 0.000000000000000000, 1.000000000000000000 ) ) ;
#52627=CARTESIAN_POINT ( 'NONE',  ( 8.102448949553179958, 123.3949999999999818, 5.886773742842750679 ) ) ;
#52629=( LENGTH_UNIT ( ) NAMED_UNIT ( * ) SI_UNIT ( .MILLI., .METRE. ) );
#52631=ORIENTED_EDGE ( 'NONE', *, *, #17446, .F. ) ;
#52632=SURFACE_SIDE_STYLE ('',( #36481 ) ) ;
#52641=ORIENTED_EDGE ( 'NONE', *, *, #59558, .T. ) ;
#52644=DIRECTION ( 'NONE',  ( 1.000000000000000000, 0.000000000000000000, 0.000000000000000000 ) ) ;
#52646=DIRECTION ( 'NONE',  ( -0.2413793103448194644, 0.9704308468600220117, 0.000000000000000000 ) ) ;
#52647=CARTESIAN_POINT ( 'NONE',  ( -10.01517768586949231, 156.3049999999999500, -6.132527647946036459E-16 ) ) ;
#52649=CIRCLE ( 'NONE', #63869, 0.5000000000000004441 ) ;
#52650=DIRECTION ( 'NONE',  ( 0.000000000000000000, 0.000000000000000000, -1.000000000000000000 ) ) ;
#52655=EDGE_LOOP ( 'NONE', ( #44320, #19096, #11823, #38097 ) ) ;
#52656=ORIENTED_EDGE ( 'NONE', *, *, #61139, .F. ) ;
#52660=EDGE_CURVE ( 'NONE', #69671, #5028, #24835, .T. ) ;
#52662=CARTESIAN_POINT ( 'NONE',  ( -20.35573775503900151, 114.9974703310426634, 9.999999999999998224 ) ) ;
#52664=ORIENTED_EDGE ( 'NONE', *, *, #60106, .T. ) ;
#52667=CARTESIAN_POINT ( 'NONE',  ( -65.50000000000000000, -1.956686671034892874E-14, -6.500000000000000000 ) ) ;
#52669=EDGE_CURVE ( 'NONE', #23306, #25927, #19207, .T. ) ;
#52670=CARTESIAN_POINT ( 'NONE',  ( -20.71231517720798365, 149.5697028012963301, 10.00000000000000000 ) ) ;
#52672=CARTESIAN_POINT ( 'NONE',  ( 3.094860106618431583, 118.2049999999999699, 9.525000000000000355 ) ) ;
#52675=VECTOR ( 'NONE', #52430, 1000.000000000000000 ) ;
#52681=CARTESIAN_POINT ( 'NONE',  ( -8.594831491281922808, 110.4999999999999858, 4.199347284499536315 ) ) ;
#52685=EDGE_LOOP ( 'NONE', ( #4214, #10134, #7442, #14401 ) ) ;
#52686=CARTESIAN_POINT ( 'NONE',  ( -9.827790563157511022E-16, 157.4429263765338192, 8.025000000000000355 ) ) ;
#52687=DIRECTION ( 'NONE',  ( 0.000000000000000000, 1.000000000000000000, -0.000000000000000000 ) ) ;
#52690=DIRECTION ( 'NONE',  ( 0.000000000000000000, 0.000000000000000000, -1.000000000000000000 ) ) ;
#52692=CARTESIAN_POINT ( 'NONE',  ( 20.86748625714523087, 115.0277251398784273, -10.00000000000000000 ) ) ;
#52693=ORIENTED_EDGE ( 'NONE', *, *, #6261, .T. ) ;
#52694=CARTESIAN_POINT ( 'NONE',  ( -60.00000000000000000, -2.024042244987997205E-14, -12.00000000000000000 ) ) ;
#52695=SURFACE_SIDE_STYLE ('',( #19625 ) ) ;
#52699=CARTESIAN_POINT ( 'NONE',  ( 71.50000000000000000, 35.92875272052971525, 10.00000000000000000 ) ) ;
#52700=CARTESIAN_POINT ( 'NONE',  ( -74.10730706101928433, 9.343722028457024820, 6.169771923672650260 ) ) ;
#52702=CARTESIAN_POINT ( 'NONE',  ( 0.000000000000000000, 119.9429263765338050, -8.025000000000000355 ) ) ;
#52704=ORIENTED_EDGE ( 'NONE', *, *, #52222, .T. ) ;
#52706=DIRECTION ( 'NONE',  ( -0.000000000000000000, -0.000000000000000000, -1.000000000000000000 ) ) ;
#52707=FACE_OUTER_BOUND ( 'NONE', #60177, .T. ) ;
#52709=SURFACE_STYLE_USAGE ( .BOTH. , #36573 ) ;
#52710=ORIENTED_EDGE ( 'NONE', *, *, #47488, .F. ) ;
#52713=CARTESIAN_POINT ( 'NONE',  ( 15.98999599679679839, 117.9999999999999716, 7.500000000000000000 ) ) ;
#52717=ORIENTED_EDGE ( 'NONE', *, *, #37853, .F. ) ;
#52720=DIRECTION ( 'NONE',  ( 1.000000000000000000, 0.000000000000000000, 0.000000000000000000 ) ) ;
#52721=FILL_AREA_STYLE ('',( #69570 ) ) ;
#52724=DIRECTION ( 'NONE',  ( 0.000000000000000000, 0.000000000000000000, 1.000000000000000000 ) ) ;
#52725=FACE_OUTER_BOUND ( 'NONE', #11501, .T. ) ;
#52726=AXIS2_PLACEMENT_3D ( 'NONE', #37167, #31831, #54330 ) ;
#52728=CARTESIAN_POINT ( 'NONE',  ( 8.102448949553181734, 127.5049999999999812, 5.886773742842750679 ) ) ;
#52730=CARTESIAN_POINT ( 'NONE',  ( -75.00000000000000000, 8.553246373267512581, -6.928940927505454539 ) ) ;
#52734=MECHANICAL_DESIGN_GEOMETRIC_PRESENTATION_REPRESENTATION('',(#4382),#48286);
#52735=( LENGTH_UNIT ( ) NAMED_UNIT ( * ) SI_UNIT ( .MILLI., .METRE. ) );
#52739=FILL_AREA_STYLE ('',( #9135 ) ) ;
#52744=DIRECTION ( 'NONE',  ( -1.000000000000000000, -0.000000000000000000, -0.000000000000000000 ) ) ;
#52745=LINE ( 'NONE', #26323, #5655 ) ;
#52755=DIRECTION ( 'NONE',  ( -0.000000000000000000, -1.000000000000000000, -0.000000000000000000 ) ) ;
#52756=EDGE_LOOP ( 'NONE', ( #11666, #52849, #26519, #6636 ) ) ;
#52758=EDGE_LOOP ( 'NONE', ( #56381, #15874, #49372, #43460 ) ) ;
#52759=CARTESIAN_POINT ( 'NONE',  ( 45.50000000000000000, 10.69371294336137801, 3.999999999999999112 ) ) ;
#52760=CARTESIAN_POINT ( 'NONE',  ( 8.437984349512095861, 129.3070736234661524, 1.550032578732816828E-15 ) ) ;
#52761=ORIENTED_EDGE ( 'NONE', *, *, #35340, .T. ) ;
#52765=EDGE_CURVE ( 'NONE', #60632, #66255, #23155, .T. ) ;
#52768=CARTESIAN_POINT ( 'NONE',  ( 5.598654528085805993, 150.2449999999999761, 7.705886871421374629 ) ) ;
#52769=DIRECTION ( 'NONE',  ( 0.000000000000000000, -1.000000000000000000, 0.000000000000000000 ) ) ;
#52770=ORIENTED_EDGE ( 'NONE', *, *, #52814, .F. ) ;
#52772=CARTESIAN_POINT ( 'NONE',  ( 0.000000000000000000, 152.5550000000000068, -9.525000000000000355 ) ) ;
#52774=STYLED_ITEM ( 'NONE', ( #51494 ), #44058 ) ;
#52776=CARTESIAN_POINT ( 'NONE',  ( 12.72792206135785698, 115.4999999999999574, -10.50000000000000000 ) ) ;
#52778=CARTESIAN_POINT ( 'NONE',  ( -6.826472737025120807, 123.9929263765338163, 4.959722759717906548 ) ) ;
#52781=FACE_OUTER_BOUND ( 'NONE', #18965, .T. ) ;
#52783=CARTESIAN_POINT ( 'NONE',  ( 45.50000000000000000, 9.639620389971918613, -6.500000000000000000 ) ) ;
#52786=FACE_OUTER_BOUND ( 'NONE', #37292, .T. ) ;
#52787=EDGE_LOOP ( 'NONE', ( #6536, #5746, #57219, #32238 ) ) ;
#52789=CONICAL_SURFACE ( 'NONE', #65095, 5.499999999999976907, 0.7853981633974300713 ) ;
#52790=( NAMED_UNIT ( * ) PLANE_ANGLE_UNIT ( ) SI_UNIT ( $, .RADIAN. ) );
#52791=CARTESIAN_POINT ( 'NONE',  ( -24.21231517720798010, 113.4999999999999858, 7.500000000000000000 ) ) ;
#52794=FILL_AREA_STYLE_COLOUR ( '', #67705 ) ;
#52802=ORIENTED_EDGE ( 'NONE', *, *, #38505, .T. ) ;
#52804=DIRECTION ( 'NONE',  ( 1.000000000000000000, 0.000000000000000000, 0.000000000000000000 ) ) ;
#52812=COLOUR_RGB ( '', 0.72549020, 0.75294118, 0.79215686) ;
#52813=VERTEX_POINT ( 'NONE', #13262 ) ;
#52814=EDGE_CURVE ( 'NONE', #38619, #57494, #56271, .T. ) ;
#52818=CARTESIAN_POINT ( 'NONE',  ( 7.632228543268607446, 126.1570736234661467, 2.479861379858954606 ) ) ;
#52820=CARTESIAN_POINT ( 'NONE',  ( 3.094860106618431583, 144.0949999999999704, 9.525000000000000355 ) ) ;
#52823=DIRECTION ( 'NONE',  ( 0.000000000000000000, -1.000000000000000000, 0.000000000000000000 ) ) ;
#52827=ORIENTED_EDGE ( 'NONE', *, *, #47577, .F. ) ;
#52834=SURFACE_STYLE_USAGE ( .BOTH. , #38671 ) ;
#52839=ORIENTED_EDGE ( 'NONE', *, *, #32218, .F. ) ;
#52840=AXIS2_PLACEMENT_3D ( 'NONE', #3918, #2850, #40562 ) ;
#52843=CARTESIAN_POINT ( 'NONE',  ( -45.00000000000000000, 8.745397170020954292, 6.877347455810014054 ) ) ;
#52849=ORIENTED_EDGE ( 'NONE', *, *, #18407, .F. ) ;
#52851=( LENGTH_UNIT ( ) NAMED_UNIT ( * ) SI_UNIT ( .MILLI., .METRE. ) );
#52853=COLOUR_RGB ( '', 0.31764706, 0.68627451, 0.89019608) ;
#52854=EDGE_CURVE ( 'NONE', #29473, #42106, #4609, .T. ) ;
#52856=CARTESIAN_POINT ( 'NONE',  ( 65.49999999999997158, 2.470600640510325396E-15, -12.00000000000000000 ) ) ;
#52857=CARTESIAN_POINT ( 'NONE',  ( -8.102448949553181734, 119.4949999999999903, 5.886773742842747126 ) ) ;
#52858=FACE_OUTER_BOUND ( 'NONE', #21008, .T. ) ;
#52860=CARTESIAN_POINT ( 'NONE',  ( -3.094860106618432471, 119.7049999999999983, -9.525000000000000355 ) ) ;
#52864=CARTESIAN_POINT ( 'NONE',  ( -9.058813317711337021, 150.1549999999999727, -2.943386871421374895 ) ) ;
#52865=AXIS2_PLACEMENT_3D ( 'NONE', #25282, #52724, #25957 ) ;
#52869=ORIENTED_EDGE ( 'NONE', *, *, #35919, .T. ) ;
#52877=MECHANICAL_DESIGN_GEOMETRIC_PRESENTATION_REPRESENTATION('',(#39373),#13523);
#52879=FACE_OUTER_BOUND ( 'NONE', #60261, .T. ) ;
#52880=DIRECTION ( 'NONE',  ( 1.000000000000000000, 0.000000000000000000, 0.000000000000000000 ) ) ;
#52885=ORIENTED_EDGE ( 'NONE', *, *, #60826, .T. ) ;
#52889=CARTESIAN_POINT ( 'NONE',  ( 0.000000000000000000, 151.4449999999999932, -9.525000000000000355 ) ) ;
#52892=ORIENTED_EDGE ( 'NONE', *, *, #38156, .T. ) ;
#52897=LINE ( 'NONE', #65060, #34804 ) ;
#52898=CARTESIAN_POINT ( 'NONE',  ( 5.598654528085805993, 120.2449999999999903, 7.705886871421374629 ) ) ;
#52900=CARTESIAN_POINT ( 'NONE',  ( -9.827790563157511022E-16, 124.4429263765338192, 8.025000000000000355 ) ) ;
#52901=VECTOR ( 'NONE', #23064, 1000.000000000000000 ) ;
#52907=ADVANCED_FACE ( 'NONE', ( #56889 ), #53594, .T. ) ;
#52908=CARTESIAN_POINT ( 'NONE',  ( -8.437984349512095861, 148.8070736234661240, -5.166775262442723748E-16 ) ) ;
#52909=CARTESIAN_POINT ( 'NONE',  ( -21.02379604162874926, 114.4999999999999574, -10.00000000000000000 ) ) ;
#52910=CYLINDRICAL_SURFACE ( 'NONE', #6964, 0.5000000000000004441 ) ;
#52911=ORIENTED_EDGE ( 'NONE', *, *, #24077, .F. ) ;
#52916=ADVANCED_FACE ( 'NONE', ( #49559 ), #61015, .F. ) ;
#52918=CARTESIAN_POINT ( 'NONE',  ( 0.000000000000000000, 152.9429263765338192, -8.025000000000000355 ) ) ;
#52919=CARTESIAN_POINT ( 'NONE',  ( 8.437984349512095861, 147.3070736234662093, 1.550032578732816828E-15 ) ) ;
#52920=CARTESIAN_POINT ( 'NONE',  ( 45.00000000000000000, -1.469576158976824618E-14, 6.999999999999999112 ) ) ;
#52921=EDGE_CURVE ( 'NONE', #12616, #69397, #8026, .T. ) ;
#52924=VERTEX_POINT ( 'NONE', #7224 ) ;
#52929=ORIENTED_EDGE ( 'NONE', *, *, #8102, .F. ) ;
#52931=AXIS2_PLACEMENT_3D ( 'NONE', #46017, #47066, #3369 ) ;
#52932=CARTESIAN_POINT ( 'NONE',  ( -6.826472737025120807, 139.5070736234661126, -4.959722759717907437 ) ) ;
#52933=VERTEX_POINT ( 'NONE', #22707 ) ;
#52936=( GEOMETRIC_REPRESENTATION_CONTEXT ( 3 ) GLOBAL_UNCERTAINTY_ASSIGNED_CONTEXT ( ( #15212 ) ) GLOBAL_UNIT_ASSIGNED_CONTEXT ( ( #29633, #40560, #13799 ) ) REPRESENTATION_CONTEXT ( 'NONE', 'WORKASPACE' ) );
#52940=ADVANCED_FACE ( 'NONE', ( #54355 ), #38225, .T. ) ;
#52943=ORIENTED_EDGE ( 'NONE', *, *, #2660, .T. ) ;
#52948=SURFACE_SIDE_STYLE ('',( #58213 ) ) ;
#52953=VECTOR ( 'NONE', #33817, 1000.000000000000000 ) ;
#52954=CARTESIAN_POINT ( 'NONE',  ( -75.00000000000000000, 9.708372675170616972, 6.000000000000000888 ) ) ;
#52955=EDGE_LOOP ( 'NONE', ( #46649, #22296, #64183, #46601 ) ) ;
#52956=( NAMED_UNIT ( * ) PLANE_ANGLE_UNIT ( ) SI_UNIT ( $, .RADIAN. ) );
#52957=ORIENTED_EDGE ( 'NONE', *, *, #57598, .F. ) ;
#52960=CARTESIAN_POINT ( 'NONE',  ( -41.72783051798697329, 107.4000574072428833, 3.999999999999999112 ) ) ;
#52962=CIRCLE ( 'NONE', #30473, 13.99999999999999822 ) ;
#52963=CARTESIAN_POINT ( 'NONE',  ( 8.102448949553181734, 123.9949999999999903, -5.886773742842746238 ) ) ;
#52972=EDGE_CURVE ( 'NONE', #64724, #12513, #1233, .T. ) ;
#52978=DIRECTION ( 'NONE',  ( -0.000000000000000000, -0.000000000000000000, -1.000000000000000000 ) ) ;
#52981=UNCERTAINTY_MEASURE_WITH_UNIT (LENGTH_MEASURE( 1.000000000000000082E-05 ), #22403, 'distance_accuracy_value', 'NONE');
#52983=( NAMED_UNIT ( * ) SI_UNIT ( $, .STERADIAN. ) SOLID_ANGLE_UNIT ( ) );
#52984=MECHANICAL_DESIGN_GEOMETRIC_PRESENTATION_REPRESENTATION('',(#9150),#40646);
#52986=CARTESIAN_POINT ( 'NONE',  ( 5.598654528085805993, 160.3549999999999898, 7.705886871421374629 ) ) ;
#52987=SURFACE_STYLE_FILL_AREA ( #36838 ) ;
#52988=AXIS2_PLACEMENT_3D ( 'NONE', #32794, #17998, #21902 ) ;
#52989=UNCERTAINTY_MEASURE_WITH_UNIT (LENGTH_MEASURE( 1.000000000000000082E-05 ), #64024, 'distance_accuracy_value', 'NONE');
#52992=VECTOR ( 'NONE', #31561, 1000.000000000000000 ) ;
#52993=DIRECTION ( 'NONE',  ( 0.000000000000000000, -1.000000000000000000, 0.000000000000000000 ) ) ;
#52995=CIRCLE ( 'NONE', #27154, 0.5000000000000004441 ) ;
#52996=EDGE_CURVE ( 'NONE', #46653, #29207, #12129, .T. ) ;
#52997=SURFACE_SIDE_STYLE ('',( #31514 ) ) ;
#53004=STYLED_ITEM ( 'NONE', ( #65447 ), #60410 ) ;
#53005=CARTESIAN_POINT ( 'NONE',  ( 4.716976649647099507, 114.7570736234661553, -6.492361379858953008 ) ) ;
#53006=AXIS2_PLACEMENT_3D ( 'NONE', #45941, #39984, #56461 ) ;
#53007=AXIS2_PLACEMENT_3D ( 'NONE', #10759, #53655, #49441 ) ;
#53008=PRESENTATION_STYLE_ASSIGNMENT (( #10098 ) ) ;
#53012=COLOUR_RGB ( '', 0.09019608, 0.27058824, 0.51372549) ;
#53018=CARTESIAN_POINT ( 'NONE',  ( -9.058813317711338797, 120.4549999999999983, 2.943386871421373563 ) ) ;
#53020=( GEOMETRIC_REPRESENTATION_CONTEXT ( 3 ) GLOBAL_UNCERTAINTY_ASSIGNED_CONTEXT ( ( #42764 ) ) GLOBAL_UNIT_ASSIGNED_CONTEXT ( ( #6882, #44227, #6191 ) ) REPRESENTATION_CONTEXT ( 'NONE', 'WORKASPACE' ) );
#53021=( GEOMETRIC_REPRESENTATION_CONTEXT ( 3 ) GLOBAL_UNCERTAINTY_ASSIGNED_CONTEXT ( ( #66518 ) ) GLOBAL_UNIT_ASSIGNED_CONTEXT ( ( #38352, #1295, #17234 ) ) REPRESENTATION_CONTEXT ( 'NONE', 'WORKASPACE' ) );
#53025=MECHANICAL_DESIGN_GEOMETRIC_PRESENTATION_REPRESENTATION('',(#32787),#1273);
#53026=CARTESIAN_POINT ( 'NONE',  ( 3.871746768188337740, 154.1452054115613350, -8.351915511153046978 ) ) ;
#53029=ORIENTED_EDGE ( 'NONE', *, *, #18036, .F. ) ;
#53030=CARTESIAN_POINT ( 'NONE',  ( 2.607480562269076430, 155.7929263765337566, -8.025000000000000355 ) ) ;
#53031=SURFACE_STYLE_USAGE ( .BOTH. , #31191 ) ;
#53037=CARTESIAN_POINT ( 'NONE',  ( 7.632228543268607446, 128.0429263765338135, 2.479861379858954606 ) ) ;
#53052=DIRECTION ( 'NONE',  ( 0.000000000000000000, 0.000000000000000000, 1.000000000000000000 ) ) ;
#53054=SURFACE_STYLE_USAGE ( .BOTH. , #5184 ) ;
#53058=EDGE_CURVE ( 'NONE', #4457, #11295, #33873, .T. ) ;
#53068=DIRECTION ( 'NONE',  ( 1.000000000000000000, 0.000000000000000000, 0.000000000000000000 ) ) ;
#53070=CIRCLE ( 'NONE', #10394, 5.500000000000005329 ) ;
#53071=EDGE_CURVE ( 'NONE', #57942, #12184, #2334, .T. ) ;
#53073=CARTESIAN_POINT ( 'NONE',  ( 3.094860106618431583, 124.2049999999999841, 9.525000000000000355 ) ) ;
#53075=CARTESIAN_POINT ( 'NONE',  ( 20.05205915161432628, 114.9999999999999858, -10.44837816993549495 ) ) ;
#53077=COLOUR_RGB ( '', 0.40784314, 0.44705882, 0.49803922) ;
#53080=UNCERTAINTY_MEASURE_WITH_UNIT (LENGTH_MEASURE( 1.000000000000000082E-05 ), #16989, 'distance_accuracy_value', 'NONE');
#53085=LINE ( 'NONE', #4876, #32516 ) ;
#53090=ORIENTED_EDGE ( 'NONE', *, *, #55402, .T. ) ;
#53091=EDGE_LOOP ( 'NONE', ( #54109, #6932, #46895, #36284 ) ) ;
#53097=SURFACE_SIDE_STYLE ('',( #11202 ) ) ;
#53098=CIRCLE ( 'NONE', #32917, 0.5000000000000006661 ) ;
#53099=CARTESIAN_POINT ( 'NONE',  ( 51.99999999999998579, 1.797044900979284448E-15, 10.50000000000000000 ) ) ;
#53103=VERTEX_POINT ( 'NONE', #39955 ) ;
#53106=ORIENTED_EDGE ( 'NONE', *, *, #64017, .F. ) ;
#53108=ORIENTED_EDGE ( 'NONE', *, *, #20171, .F. ) ;
#53109=TOROIDAL_SURFACE ( 'NONE', #17225, 13.49999999999999822, 0.5000000000000000000 ) ;
#53112=CARTESIAN_POINT ( 'NONE',  ( 8.102448949553183510, 153.9950000000000045, -5.886773742842746238 ) ) ;
#53114=MECHANICAL_DESIGN_GEOMETRIC_PRESENTATION_REPRESENTATION('',(#47532),#13788);
#53115=CARTESIAN_POINT ( 'NONE',  ( 5.598654528085805993, 148.3549999999999898, 7.705886871421374629 ) ) ;
#53116=PRESENTATION_STYLE_ASSIGNMENT (( #53776 ) ) ;
#53118=VERTEX_POINT ( 'NONE', #52236 ) ;
#53119=CARTESIAN_POINT ( 'NONE',  ( 7.632228543268608334, 122.3429263765338249, -2.479861379858951942 ) ) ;
#53121=UNCERTAINTY_MEASURE_WITH_UNIT (LENGTH_MEASURE( 1.000000000000000082E-05 ), #67493, 'distance_accuracy_value', 'NONE');
#53125=LINE ( 'NONE', #48566, #42277 ) ;
#53126=VERTEX_POINT ( 'NONE', #13515 ) ;
#53134=STYLED_ITEM ( 'NONE', ( #16299 ), #35839 ) ;
#53135=UNCERTAINTY_MEASURE_WITH_UNIT (LENGTH_MEASURE( 1.000000000000000082E-05 ), #36484, 'distance_accuracy_value', 'NONE');
#53137=CARTESIAN_POINT ( 'NONE',  ( 44.99999999999998579, 119.9999999999999716, 10.00000000000000000 ) ) ;
#53138=DIRECTION ( 'NONE',  ( 0.000000000000000000, 0.000000000000000000, -1.000000000000000000 ) ) ;
#53140=ORIENTED_EDGE ( 'NONE', *, *, #53690, .T. ) ;
#53141=ORIENTED_EDGE ( 'NONE', *, *, #45557, .T. ) ;
#53143=DIRECTION ( 'NONE',  ( -1.000000000000000000, 0.000000000000000000, 0.000000000000000000 ) ) ;
#53144=COLOUR_RGB ( '', 0.08235294, 0.09019608, 0.10196078) ;
#53149=CARTESIAN_POINT ( 'NONE',  ( -55.00000000000000000, -2.024042244987997205E-14, 11.50000000000003020 ) ) ;
#53150=DIRECTION ( 'NONE',  ( 0.000000000000000000, 0.000000000000000000, -1.000000000000000000 ) ) ;
#53153=AXIS2_PLACEMENT_3D ( 'NONE', #49248, #64727, #42976 ) ;
#53154=DIRECTION ( 'NONE',  ( -0.000000000000000000, -1.000000000000000000, -0.000000000000000000 ) ) ;
#53155=SURFACE_STYLE_FILL_AREA ( #37360 ) ;
#53160=CARTESIAN_POINT ( 'NONE',  ( -3.094860106618432471, 151.5949999999999989, -9.525000000000000355 ) ) ;
#53163=CARTESIAN_POINT ( 'NONE',  ( 12.34222745343792127, 115.4999999999999574, 10.18181818181818166 ) ) ;
#53165=FACE_OUTER_BOUND ( 'NONE', #63212, .T. ) ;
#53166=UNCERTAINTY_MEASURE_WITH_UNIT (LENGTH_MEASURE( 1.000000000000000082E-05 ), #69092, 'distance_accuracy_value', 'NONE');
#53167=FACE_OUTER_BOUND ( 'NONE', #38287, .T. ) ;
#53168=CIRCLE ( 'NONE', #16123, 1.000000000000000888 ) ;
#53170=EDGE_CURVE ( 'NONE', #6589, #26613, #51881, .T. ) ;
#53175=COLOUR_RGB ( '', 0.40784314, 0.44705882, 0.49803922) ;
#53176=FACE_OUTER_BOUND ( 'NONE', #68326, .T. ) ;
#53177=VERTEX_POINT ( 'NONE', #8612 ) ;
#53180=CARTESIAN_POINT ( 'NONE',  ( 60.99999999999998579, 50.00000000000000000, -7.000000000000000000 ) ) ;
#53183=CARTESIAN_POINT ( 'NONE',  ( -4.716976649647097730, 117.2429263765338163, -6.492361379858953896 ) ) ;
#53187=TOROIDAL_SURFACE ( 'NONE', #11593, 14.49999999999999822, 0.5000000000000000000 ) ;
#53190=CIRCLE ( 'NONE', #52099, 0.5000000000000004441 ) ;
#53193=FILL_AREA_STYLE ('',( #43022 ) ) ;
#53197=CARTESIAN_POINT ( 'NONE',  ( -9.058813317711337021, 119.0449999999999875, -2.943386871421374895 ) ) ;
#53199=EDGE_CURVE ( 'NONE', #1408, #49241, #40635, .T. ) ;
#53203=( NAMED_UNIT ( * ) SI_UNIT ( $, .STERADIAN. ) SOLID_ANGLE_UNIT ( ) );
#53204=CARTESIAN_POINT ( 'NONE',  ( 3.094860106618431583, 124.2049999999999841, 9.525000000000000355 ) ) ;
#53206=LINE ( 'NONE', #69375, #23944 ) ;
#53208=CARTESIAN_POINT ( 'NONE',  ( 3.094860106618435136, 146.4050000000000011, -9.525000000000000355 ) ) ;
#53210=DIRECTION ( 'NONE',  ( -1.000000000000000000, 0.000000000000000000, 0.000000000000000000 ) ) ;
#53213=DIRECTION ( 'NONE',  ( -0.000000000000000000, -0.000000000000000000, -1.000000000000000000 ) ) ;
#53214=VERTEX_POINT ( 'NONE', #62045 ) ;
#53216=LINE ( 'NONE', #26457, #68844 ) ;
#53218=ORIENTED_EDGE ( 'NONE', *, *, #37853, .T. ) ;
#53221=LINE ( 'NONE', #47644, #66065 ) ;
#53222=SURFACE_STYLE_FILL_AREA ( #57801 ) ;
#53223=ORIENTED_EDGE ( 'NONE', *, *, #577, .F. ) ;
#53224=( LENGTH_UNIT ( ) NAMED_UNIT ( * ) SI_UNIT ( .MILLI., .METRE. ) );
#53225=EDGE_LOOP ( 'NONE', ( #14123, #15505, #45939, #47509 ) ) ;
#53227=CYLINDRICAL_SURFACE ( 'NONE', #68491, 0.5000000000000004441 ) ;
#53229=AXIS2_PLACEMENT_3D ( 'NONE', #5727, #16346, #32458 ) ;
#53230=ORIENTED_EDGE ( 'NONE', *, *, #15492, .T. ) ;
#53235=CARTESIAN_POINT ( 'NONE',  ( 5.598654528085809545, 151.1449999999999818, -7.705886871421373741 ) ) ;
#53239=FILL_AREA_STYLE ('',( #48682 ) ) ;
#53241=VERTEX_POINT ( 'NONE', #4701 ) ;
#53244=CYLINDRICAL_SURFACE ( 'NONE', #58294, 5.000000000000004441 ) ;
#53246=CIRCLE ( 'NONE', #16048, 0.5000000000000004441 ) ;
#53249=CARTESIAN_POINT ( 'NONE',  ( 10.01517768586949231, 120.6949999999999790, 1.839758294383810543E-15 ) ) ;
#53255=CYLINDRICAL_SURFACE ( 'NONE', #17763, 0.5000000000000004441 ) ;
#53256=AXIS2_PLACEMENT_3D ( 'NONE', #59773, #38371, #58746 ) ;
#53257=ORIENTED_EDGE ( 'NONE', *, *, #50517, .F. ) ;
#53262=DIRECTION ( 'NONE',  ( 0.000000000000000000, 1.000000000000000000, 0.000000000000000000 ) ) ;
#53266=FILL_AREA_STYLE_COLOUR ( '', #28280 ) ;
#53267=ORIENTED_EDGE ( 'NONE', *, *, #33357, .T. ) ;
#53269=DIRECTION ( 'NONE',  ( 0.9704308468600219006, 0.2413793103448194921, 0.000000000000000000 ) ) ;
#53270=CARTESIAN_POINT ( 'NONE',  ( 48.81081081081080697, 14.09971791521132900, 9.500000000000000000 ) ) ;
#53274=ORIENTED_EDGE ( 'NONE', *, *, #12713, .F. ) ;
#53275=CARTESIAN_POINT ( 'NONE',  ( -74.50000000000000000, 36.50926243676796190, -10.00000000000000000 ) ) ;
#53277=CARTESIAN_POINT ( 'NONE',  ( -7.632228543268608334, 145.9570736234661581, 2.479861379858952830 ) ) ;
#53279=EDGE_CURVE ( 'NONE', #11259, #62586, #123, .T. ) ;
#53280=EDGE_LOOP ( 'NONE', ( #21877, #24952, #43275, #33960, #55282, #764 ) ) ;
#53281=CARTESIAN_POINT ( 'NONE',  ( 34.99999999999992895, 109.9999999999999858, 10.00000000000000000 ) ) ;
#53284=UNCERTAINTY_MEASURE_WITH_UNIT (LENGTH_MEASURE( 1.000000000000000082E-05 ), #23336, 'distance_accuracy_value', 'NONE');
#53286=CARTESIAN_POINT ( 'NONE',  ( 23.21231517720797655, 117.4999999999999716, 7.500000000000000000 ) ) ;
#53293=ORIENTED_EDGE ( 'NONE', *, *, #50050, .T. ) ;
#53297=AXIS2_PLACEMENT_3D ( 'NONE', #45024, #38715, #60449 ) ;
#53301=ADVANCED_FACE ( 'NONE', ( #64136 ), #48353, .T. ) ;
#53302=ORIENTED_EDGE ( 'NONE', *, *, #1303, .F. ) ;
#53304=PRESENTATION_STYLE_ASSIGNMENT (( #42784 ) ) ;
#53305=ADVANCED_FACE ( 'NONE', ( #15633 ), #52910, .F. ) ;
#53306=TOROIDAL_SURFACE ( 'NONE', #7247, 13.49999999999999822, 0.5000000000000000000 ) ;
#53317=CARTESIAN_POINT ( 'NONE',  ( 9.058813317711337021, 120.5449999999999875, 2.943386871421375783 ) ) ;
#53320=CARTESIAN_POINT ( 'NONE',  ( 40.99999999999998579, 107.7459666924148252, -3.499999999999999556 ) ) ;
#53321=VERTEX_POINT ( 'NONE', #34214 ) ;
#53322=CARTESIAN_POINT ( 'NONE',  ( -44.99999999999977973, 146.9999999999999716, 7.500000000000000000 ) ) ;
#53330=DIRECTION ( 'NONE',  ( -0.000000000000000000, 1.000000000000000000, -0.000000000000000000 ) ) ;
#53336=DIRECTION ( 'NONE',  ( -0.000000000000000000, -0.000000000000000000, 1.000000000000000000 ) ) ;
#53337=FILL_AREA_STYLE ('',( #4402 ) ) ;
#53338=MECHANICAL_DESIGN_GEOMETRIC_PRESENTATION_REPRESENTATION('',(#31964),#48840);
#53340=SURFACE_STYLE_USAGE ( .BOTH. , #48782 ) ;
#53341=FACE_OUTER_BOUND ( 'NONE', #5908, .T. ) ;
#53342=CYLINDRICAL_SURFACE ( 'NONE', #33188, 8.000000000000014211 ) ;
#53344=EDGE_CURVE ( 'NONE', #38783, #20552, #29407, .T. ) ;
#53346=AXIS2_PLACEMENT_3D ( 'NONE', #67154, #18942, #55906 ) ;
#53350=MECHANICAL_DESIGN_GEOMETRIC_PRESENTATION_REPRESENTATION('',(#41017),#15170);
#53352=CYLINDRICAL_SURFACE ( 'NONE', #16071, 8.000000000000014211 ) ;
#53357=CARTESIAN_POINT ( 'NONE',  ( -7.632228543268608334, 112.9570736234661581, 2.479861379858952830 ) ) ;
#53358=CARTESIAN_POINT ( 'NONE',  ( -20.77797364267480518, 115.1388508835393907, 10.00000000000000000 ) ) ;
#53360=( LENGTH_UNIT ( ) NAMED_UNIT ( * ) SI_UNIT ( .MILLI., .METRE. ) );
#53366=CARTESIAN_POINT ( 'NONE',  ( 5.598654528085809545, 122.2549999999999955, -7.705886871421373741 ) ) ;
#53369=TOROIDAL_SURFACE ( 'NONE', #62345, 13.50000000000000178, 0.5000000000000000000 ) ;
#53372=ORIENTED_EDGE ( 'NONE', *, *, #65370, .F. ) ;
#53376=EDGE_CURVE ( 'NONE', #20808, #19090, #57491, .T. ) ;
#53378=EDGE_LOOP ( 'NONE', ( #14957, #2266, #42662, #61220 ) ) ;
#53379=CARTESIAN_POINT ( 'NONE',  ( 0.000000000000000000, 158.9429263765338192, -8.025000000000000355 ) ) ;
#53380=( NAMED_UNIT ( * ) SI_UNIT ( $, .STERADIAN. ) SOLID_ANGLE_UNIT ( ) );
#53381=FACE_OUTER_BOUND ( 'NONE', #59992, .T. ) ;
#53382=EDGE_CURVE ( 'NONE', #60182, #4086, #11439, .T. ) ;
#53384=CARTESIAN_POINT ( 'NONE',  ( 19.98198699191933869, 115.0278726071232711, -9.999999999996266098 ) ) ;
#53387=CYLINDRICAL_SURFACE ( 'NONE', #8843, 0.4999999999999995004 ) ;
#53390=CARTESIAN_POINT ( 'NONE',  ( 45.07697505292422591, 10.02565835097472480, -6.500000000000000000 ) ) ;
#53391=STYLED_ITEM ( 'NONE', ( #3583 ), #27767 ) ;
#53395=LINE ( 'NONE', #20687, #10175 ) ;
#53396=CARTESIAN_POINT ( 'NONE',  ( -4.134715136431658777, 153.9646786816057045, 8.000580966448437081 ) ) ;
#53401=EDGE_CURVE ( 'NONE', #20703, #52602, #10359, .T. ) ;
#53402=CARTESIAN_POINT ( 'NONE',  ( 0.000000000000000000, 110.5549999999999926, -9.525000000000000355 ) ) ;
#53404=FILL_AREA_STYLE ('',( #65323 ) ) ;
#53407=DIRECTION ( 'NONE',  ( 0.000000000000000000, 0.000000000000000000, -1.000000000000000000 ) ) ;
#53410=AXIS2_PLACEMENT_3D ( 'NONE', #25225, #8374, #46024 ) ;
#53411=AXIS2_PLACEMENT_3D ( 'NONE', #63593, #68532, #10136 ) ;
#53414=FILL_AREA_STYLE_COLOUR ( '', #40325 ) ;
#53419=CARTESIAN_POINT ( 'NONE',  ( -74.98971658424945019, 36.00805210434474901, -9.715834439412292411 ) ) ;
#53422=CARTESIAN_POINT ( 'NONE',  ( -8.102448949553181734, 135.6049999999999613, 5.886773742842747126 ) ) ;
#53430=CARTESIAN_POINT ( 'NONE',  ( -9.827790563157511022E-16, 133.4429263765338192, 8.025000000000000355 ) ) ;
#53432=SURFACE_SIDE_STYLE ('',( #22446 ) ) ;
#53433=DIRECTION ( 'NONE',  ( -1.040834085586083310E-14, 0.000000000000000000, -1.000000000000000000 ) ) ;
#53437=DIRECTION ( 'NONE',  ( 1.000000000000000000, 0.000000000000000000, 0.000000000000000000 ) ) ;
#53439=FILL_AREA_STYLE_COLOUR ( '', #18016 ) ;
#53442=ORIENTED_EDGE ( 'NONE', *, *, #61615, .T. ) ;
#53444=ORIENTED_EDGE ( 'NONE', *, *, #48035, .F. ) ;
#53445=AXIS2_PLACEMENT_3D ( 'NONE', #9579, #3901, #9219 ) ;
#53446=CARTESIAN_POINT ( 'NONE',  ( -2.451748578458123784E-13, 110.8535625161535592, 9.171437483846442973 ) ) ;
#53448=DIRECTION ( 'NONE',  ( 0.000000000000000000, 2.430666987508117145E-16, -1.000000000000000000 ) ) ;
#53451=AXIS2_PLACEMENT_3D ( 'NONE', #24817, #9370, #3686 ) ;
#53453=CARTESIAN_POINT ( 'NONE',  ( -1.166476076187854022E-15, 152.9449999999999932, 9.525000000000000355 ) ) ;
#53456=( NAMED_UNIT ( * ) PLANE_ANGLE_UNIT ( ) SI_UNIT ( $, .RADIAN. ) );
#53457=DIRECTION ( 'NONE',  ( -0.000000000000000000, -0.000000000000000000, 1.000000000000000000 ) ) ;
#53458=EDGE_LOOP ( 'NONE', ( #27776, #56218 ) ) ;
#53459=CARTESIAN_POINT ( 'NONE',  ( 2.607480562269071989, 121.5929263765338249, 8.025000000000002132 ) ) ;
#53460=CARTESIAN_POINT ( 'NONE',  ( 45.44163888576682808, 10.14721296192225886, -3.260160134650228247 ) ) ;
#53464=ORIENTED_EDGE ( 'NONE', *, *, #46667, .T. ) ;
#53465=CIRCLE ( 'NONE', #15291, 0.5000000000000004441 ) ;
#53467=ORIENTED_EDGE ( 'NONE', *, *, #26138, .F. ) ;
#53469=( GEOMETRIC_REPRESENTATION_CONTEXT ( 3 ) GLOBAL_UNCERTAINTY_ASSIGNED_CONTEXT ( ( #67043 ) ) GLOBAL_UNIT_ASSIGNED_CONTEXT ( ( #13061, #66893, #39841 ) ) REPRESENTATION_CONTEXT ( 'NONE', 'WORKASPACE' ) );
#53472=EDGE_CURVE ( 'NONE', #46653, #27901, #44196, .T. ) ;
#53477=DIRECTION ( 'NONE',  ( -0.000000000000000000, -0.000000000000000000, -1.000000000000000000 ) ) ;
#53478=( NAMED_UNIT ( * ) PLANE_ANGLE_UNIT ( ) SI_UNIT ( $, .RADIAN. ) );
#53486=ORIENTED_EDGE ( 'NONE', *, *, #19610, .T. ) ;
#53489=DIRECTION ( 'NONE',  ( 0.000000000000000000, 0.000000000000000000, 1.000000000000000000 ) ) ;
#53492=CARTESIAN_POINT ( 'NONE',  ( -60.00000000000000000, -2.024042244987997205E-14, -7.000000000000000888 ) ) ;
#53496=AXIS2_PLACEMENT_3D ( 'NONE', #67466, #40084, #30161 ) ;
#53498=CARTESIAN_POINT ( 'NONE',  ( 8.102448949553181734, 153.3950000000000387, 5.886773742842750679 ) ) ;
#53506=DIRECTION ( 'NONE',  ( 0.000000000000000000, 1.000000000000000000, 0.000000000000000000 ) ) ;
#53507=ORIENTED_EDGE ( 'NONE', *, *, #8981, .F. ) ;
#53510=COLOUR_RGB ( '', 0.08235294, 0.09019608, 0.10196078) ;
#53511=COLOUR_RGB ( '', 0.09019608, 0.27058824, 0.51372549) ;
#53514=ORIENTED_EDGE ( 'NONE', *, *, #56720, .F. ) ;
#53516=DIRECTION ( 'NONE',  ( 0.000000000000000000, 0.000000000000000000, 1.000000000000000000 ) ) ;
#53517=CARTESIAN_POINT ( 'NONE',  ( -8.437984349512095861, 117.6929263765338050, -5.166775262442723748E-16 ) ) ;
#53518=CARTESIAN_POINT ( 'NONE',  ( -45.87416991466958649, 9.273068908601562299, 6.223864456579077498 ) ) ;
#53525=FACE_OUTER_BOUND ( 'NONE', #54042, .T. ) ;
#53529=CARTESIAN_POINT ( 'NONE',  ( 8.102448949553183510, 123.9949999999999903, -5.886773742842746238 ) ) ;
#53530=DIRECTION ( 'NONE',  ( 0.000000000000000000, -1.000000000000000000, 0.000000000000000000 ) ) ;
#53532=VERTEX_POINT ( 'NONE', #40555 ) ;
#53535=CARTESIAN_POINT ( 'NONE',  ( -10.01517768586949408, 120.3049999999999784, -6.132527647946036459E-16 ) ) ;
#53540=CARTESIAN_POINT ( 'NONE',  ( 5.598654528085809545, 152.2549999999999670, -7.705886871421373741 ) ) ;
#53542=DIRECTION ( 'NONE',  ( 1.000000000000000000, 0.000000000000000000, 0.000000000000000000 ) ) ;
#53548=COLOUR_RGB ( '', 0.72549020, 0.75294118, 0.79215686) ;
#53549=ORIENTED_EDGE ( 'NONE', *, *, #23830, .F. ) ;
#53552=EDGE_CURVE ( 'NONE', #26603, #4250, #2847, .T. ) ;
#53554=CARTESIAN_POINT ( 'NONE',  ( 2.056319983864932865, 111.9482313798679769, -7.829595205988900908 ) ) ;
#53555=( NAMED_UNIT ( * ) SI_UNIT ( $, .STERADIAN. ) SOLID_ANGLE_UNIT ( ) );
#53556=EDGE_CURVE ( 'NONE', #46319, #20411, #39247, .T. ) ;
#53557=PRESENTATION_STYLE_ASSIGNMENT (( #38108 ) ) ;
#53558=EDGE_LOOP ( 'NONE', ( #18151, #20828, #68961, #35232 ) ) ;
#53560=FACE_OUTER_BOUND ( 'NONE', #40682, .T. ) ;
#53565=SURFACE_STYLE_FILL_AREA ( #42712 ) ;
#53566=DIRECTION ( 'NONE',  ( 1.000000000000000000, 0.000000000000000000, 0.000000000000000000 ) ) ;
#53568=DIRECTION ( 'NONE',  ( 0.000000000000000000, -1.000000000000000000, 0.000000000000000000 ) ) ;
#53569=ORIENTED_EDGE ( 'NONE', *, *, #39985, .F. ) ;
#53570=( LENGTH_UNIT ( ) NAMED_UNIT ( * ) SI_UNIT ( .MILLI., .METRE. ) );
#53572=( LENGTH_UNIT ( ) NAMED_UNIT ( * ) SI_UNIT ( .MILLI., .METRE. ) );
#53574=CARTESIAN_POINT ( 'NONE',  ( 9.058813317711337021, 123.5449999999999875, 2.943386871421375783 ) ) ;
#53578=( LENGTH_UNIT ( ) NAMED_UNIT ( * ) SI_UNIT ( .MILLI., .METRE. ) );
#53580=ORIENTED_EDGE ( 'NONE', *, *, #32459, .T. ) ;
#53584=CIRCLE ( 'NONE', #23261, 13.99999999999999822 ) ;
#53586=AXIS2_PLACEMENT_3D ( 'NONE', #37771, #12015, #16297 ) ;
#53587=FACE_OUTER_BOUND ( 'NONE', #40986, .T. ) ;
#53589=DIRECTION ( 'NONE',  ( 1.000000000000000000, 0.000000000000000000, 0.000000000000000000 ) ) ;
#53591=VERTEX_POINT ( 'NONE', #35610 ) ;
#53593=LINE ( 'NONE', #59546, #16134 ) ;
#53594=( BOUNDED_SURFACE ( )  B_SPLINE_SURFACE ( 1, 2, ( 
 ( #8703, #24858, #14319, #5824, #58972, #143, #27264, #10443, #42484, #59645, #31525, #5462, #37206, #54368, #26252, #26583, #59278, #43535, #48108, #54023, #47784, #69186, #64228, #10783, #48802, #26914, #53357, #64920, #69511, #6189, #48452, #37909, #11462, #36854, #32934, #502, #37572, #20643, #53005, #47422, #4802, #16770, #32227, #11106, #16086, #38243, #22032, #68845, #15726, #32557, #63550, #42156, #15396, #21673, #64600, #43192, #58268, #10094, #20986, #63877, #58617, #31874, #5138, #16446, #21314, #42836, #53676, #23397, #28302, #55056, #6512, #7238, #45251, #2223, #28669, #1887, #44571, #50497, #34316, #23753, #17798, #49810, #12146, #55769, #38600, #49463, #44905, #12848, #66311, #27622, #49135, #18138, #17471, #830, #17128, #22368, #50164, #39274, #23076, #65627, #13186, #7575, #59997, #60339, #33611, #39974, #65966, #33279, #66675, #12493, #39622, #60676, #18490, #29005, #61375, #38940, #61030, #43867, #34644, #65275, #56103, #11809, #54707, #27955, #1189, #22723, #44222, #6880, #1552, #33953, #55413, #51525, #35363, #24427, #3646, #8628, #56819, #56453, #57139, #25479, #52254, #8971, #51891, #24775, #30751, #14592, #4011, #67716, #30058, #62067, #36059, #18815, #29729, #25143, #62756, #46656, #7920, #29363, #68075, #67358, #50842, #67025, #2597, #30389, #19510, #3287, #45932, #63122, #57501, #40298, #40655, #13897, #20200, #46294, #41009, #41701, #14962, #8287, #9327, #19858, #24102, #46993, #62430, #14245, #35709, #36445, #41351, #68405, #45608, #61705, #13536, #35004, #19154, #51195, #2939, #31438, #48725, #64153, #16357, #69442, #10699, #37832, #20917, #52932, #428, #42073, #16009, #47706, #64846, #36784, #37130, #61, #53937, #58538, #64513, #58195, #10018, #5064, #21231, #59205, #37489, #63804, #5742, #10371, #16694, #58893, #48371, #21958, #47337, #43465, #11028, #48039, #31097, #63475, #57865, #9689, #32152, #27186, #52594, #31797, #53606, #4341, #25825, #42758, #68766, #21594, #53277, #26517, #5393, #4720, #20558, #32475, #15326, #26169, #26833, #69109, #42416, #15650, #43107, #55684, #65546, #65190, #27542, #22285, #12406, #33864, #66225, #44490, #55328, #65895, #1100, #17722, #12758, #49068, #7153, #49726, #60268, #7495, #50079, #17392, #6108, #752, #60588, #44145, #28923, #22995, #11733, #38857, #22641, #17042, #59562, #27872, #44820, #12069, #11383, #23664, #54964, #45170, #49378, #28581, #66589, #38523, #33533, #32847, #6789, #28217, #18050, #59916, #1466, #39536, #54638, #1809, #50409, #39193, #23324, #60939, #34230, #2133, #38159, #54290, #6446, #43787, #33200, #46571, #67993, #29279, #52174, #24688, #8200, #46208, #50761, #19430, #62348, #35274, #29648, #13109, #19066, #18740, #61297, #3930, #67630 ),
 ( #40222, #62673, #3559, #19780, #40928, #35974, #14171, #41275, #51809, #9248, #2510, #35630, #24019, #57065, #18406, #8881, #57420, #25401, #40571, #30305, #34564, #30667, #29983, #56016, #25061, #67276, #61988, #3196, #13452, #7832, #14498, #46918, #39891, #8550, #45526, #66946, #61626, #34918, #56365, #45846, #51116, #2860, #24352, #13813, #56736, #51448, #4985, #64070, #26435, #31355, #47968, #43027, #57780, #15923, #10283, #20836, #16280, #10622, #47620, #36358, #9605, #21158, #4632, #59133, #53197, #41982, #69027, #52857, #25740, #20109, #58125, #5316, #26087, #41614, #53862, #15571, #5659, #9935, #37404, #27107, #47259, #63724, #63031, #42338, #37043, #26761, #68677, #31716, #55171, #15241, #58806, #10956, #58460, #69368, #42668, #32073, #32394, #53529, #48284, #36709, #31021, #21509, #64430, #37754, #52515, #68328, #14874, #4260, #20477, #63394, #49644, #22916, #65465, #59842, #43384, #49298, #48988, #21875, #34146, #6707, #28136, #44059, #32758, #33455, #11650, #1011, #22210, #54209, #43706, #17315, #679, #23251, #33790, #50004, #1387, #66142, #44416, #28497, #12320, #39460, #65817, #60863, #54556, #17649, #39118, #60187, #12677, #27795, #60507, #16953, #16614, #33120, #7069, #1743, #59474, #55605, #54883, #38440, #55242, #11303, #44748, #17972, #38777, #6366, #64775, #22556, #65099, #38077, #7428, #48641, #340, #11995, #6025, #27463, #40149, #29558, #2419, #13036, #23932, #67193, #29190, #3470, #14088, #30227, #51366, #46480, #8474, #8801, #62260, #19699, #39808, #56647, #28851, #29908, #67905, #35883, #51027, #3112, #45094, #41196, #40492, #66507, #35549, #8113, #2788, #13727, #45446, #23583, #56987, #57329, #62596, #18982, #18328, #14410, #50334, #66866, #2056, #56283, #55944, #61226, #34489, #24605, #46121, #51723, #35187, #67542, #19341, #61543, #40841, #24971, #7749, #50677, #61908, #24277, #18671, #13370, #45774, #34830, #46842, #31631, #15156, #69611, #63650, #52434, #58047, #41890, #36265, #30580, #68593, #15834, #36630, #52085, #64339, #26000, #16187, #20388, #26348, #37665, #57690, #4543, #3836, #63308, #9853, #37313, #9519, #42261, #10542, #25653, #58721, #58368, #31268, #26679, #52768, #9165, #36957, #69287, #21420, #68248, #42938, #31979, #68943, #25320, #62942, #20029, #14787, #5235, #15490, #21081, #47529, #41528, #53453, #48204, #47173, #42580, #30938, #4179, #20751, #53112, #47888, #4899, #10193, #63984, #250, #59381, #11215, #53772, #59062, #38693, #16872, #22125, #32662, #65380, #65014, #43619, #16535, #919, #44323, #1289, #22470, #43966, #59748, #22825, #54797, #65721, #33029, #38346, #48902, #6606, #21783, #54118, #17228, #33371, #60094, #10879, #5573, #11911, #27371, #27019, #43296, #48554, #28050 ) ),
 .UNSPECIFIED., .F., .F., .F. ) 
 B_SPLINE_SURFACE_WITH_KNOTS ( ( 2, 2 ),
 ( 3, 2, 2, 2, 2, 2, 2, 2, 2, 2, 2, 2, 2, 2, 2, 2, 2, 2, 2, 2, 2, 2, 2, 2, 2, 2, 2, 2, 2, 2, 2, 2, 2, 2, 2, 2, 2, 2, 2, 2, 2, 2, 2, 2, 2, 2, 2, 2, 2, 2, 2, 2, 2, 2, 2, 2, 2, 2, 2, 2, 2, 2, 2, 2, 2, 2, 2, 2, 2, 2, 2, 2, 2, 2, 2, 2, 2, 2, 2, 2, 2, 2, 2, 2, 2, 2, 2, 2, 2, 2, 2, 2, 2, 2, 2, 2, 2, 2, 2, 2, 2, 2, 2, 2, 2, 2, 2, 2, 2, 2, 2, 2, 2, 2, 2, 2, 2, 2, 2, 2, 2, 2, 2, 2, 2, 2, 2, 2, 2, 2, 2, 2, 2, 2, 2, 2, 2, 2, 2, 2, 2, 2, 2, 2, 2, 2, 2, 2, 2, 2, 2, 2, 2, 2, 2, 2, 2, 2, 2, 2, 2, 2, 2, 2, 2, 2, 2, 2, 2, 2, 3 ),
 ( 0.000000000000000000, 1.000000000000000000 ),
 ( 0.000000000000000000, 0.005882352941176470507, 0.01176470588235294101, 0.01764705882352941152, 0.02352941176470588203, 0.02941176470588235253, 0.03529411764705882304, 0.04117647058823529355, 0.04705882352941176405, 0.05294117647058823456, 0.05882352941176470507, 0.06470588235294118251, 0.07058823529411764608, 0.07647058823529412352, 0.08235294117647058709, 0.08823529411764706454, 0.09411764705882352811, 0.1000000000000000056, 0.1058823529411764691, 0.1117647058823529466, 0.1176470588235294101, 0.1235294117647058876, 0.1294117647058823650, 0.1352941176470588147, 0.1411764705882352922, 0.1470588235294117696, 0.1529411764705882470, 0.1588235294117646967, 0.1647058823529411742, 0.1705882352941176516, 0.1764705882352941291, 0.1823529411764705788, 0.1882352941176470562, 0.1941176470588235337, 0.2000000000000000111, 0.2058823529411764608, 0.2117647058823529382, 0.2176470588235294157, 0.2235294117647058931, 0.2294117647058823428, 0.2352941176470588203, 0.2411764705882352977, 0.2470588235294117752, 0.2529411764705882248, 0.2588235294117647300, 0.2647058823529411797, 0.2705882352941176294, 0.2764705882352941346, 0.2823529411764705843, 0.2882352941176470340, 0.2941176470588235392, 0.2999999999999999889, 0.3058823529411764941, 0.3117647058823529438, 0.3176470588235293935, 0.3235294117647058987, 0.3294117647058823484, 0.3352941176470587981, 0.3411764705882353033, 0.3470588235294117530, 0.3529411764705882582, 0.3588235294117647078, 0.3647058823529411575, 0.3705882352941176627, 0.3764705882352941124, 0.3823529411764705621, 0.3882352941176470673, 0.3941176470588235170, 0.4000000000000000222, 0.4058823529411764719, 0.4117647058823529216, 0.4176470588235294268, 0.4235294117647058765, 0.4294117647058823262, 0.4352941176470588314, 0.4411764705882352811, 0.4470588235294117863, 0.4529411764705882359, 0.4588235294117646856, 0.4647058823529411908, 0.4705882352941176405, 0.4764705882352940902, 0.4823529411764705954, 0.4882352941176470451, 0.4941176470588235503, 0.5000000000000000000, 0.5058823529411764497, 0.5117647058823528994, 0.5176470588235294601, 0.5235294117647059098, 0.5294117647058823595, 0.5352941176470588092, 0.5411764705882352589, 0.5470588235294118196, 0.5529411764705882693, 0.5588235294117647189, 0.5647058823529411686, 0.5705882352941176183, 0.5764705882352940680, 0.5823529411764706287, 0.5882352941176470784, 0.5941176470588235281, 0.5999999999999999778, 0.6058823529411764275, 0.6117647058823529882, 0.6176470588235294379, 0.6235294117647058876, 0.6294117647058823373, 0.6352941176470587870, 0.6411764705882353477, 0.6470588235294117974, 0.6529411764705882470, 0.6588235294117646967, 0.6647058823529411464, 0.6705882352941175961, 0.6764705882352941568, 0.6823529411764706065, 0.6882352941176470562, 0.6941176470588235059, 0.6999999999999999556, 0.7058823529411765163, 0.7117647058823529660, 0.7176470588235294157, 0.7235294117647058654, 0.7294117647058823151, 0.7352941176470588758, 0.7411764705882353255, 0.7470588235294117752, 0.7529411764705882248, 0.7588235294117646745, 0.7647058823529411242, 0.7705882352941176849, 0.7764705882352941346, 0.7823529411764705843, 0.7882352941176470340, 0.7941176470588234837, 0.8000000000000000444, 0.8058823529411764941, 0.8117647058823529438, 0.8176470588235293935, 0.8235294117647058432, 0.8294117647058824039, 0.8352941176470588536, 0.8411764705882353033, 0.8470588235294117530, 0.8529411764705882026, 0.8588235294117646523, 0.8647058823529412130, 0.8705882352941176627, 0.8764705882352941124, 0.8823529411764705621, 0.8882352941176470118, 0.8941176470588235725, 0.9000000000000000222, 0.9058823529411764719, 0.9117647058823529216, 0.9176470588235293713, 0.9235294117647059320, 0.9294117647058823817, 0.9352941176470588314, 0.9411764705882352811, 0.9470588235294117307, 0.9529411764705881804, 0.9588235294117647411, 0.9647058823529411908, 0.9705882352941176405, 0.9764705882352940902, 0.9823529411764705399, 0.9882352941176471006, 0.9941176470588235503, 1.000000000000000000 ),
 .UNSPECIFIED. ) 
 GEOMETRIC_REPRESENTATION_ITEM ( )  RATIONAL_B_SPLINE_SURFACE ( (
 ( 1.000000000000000000, 0.9510565162951535312, 1.000000000000000000, 0.9510565162951535312, 1.000000000000000000, 0.9510565162951535312, 1.000000000000000000, 0.9510565162951535312, 1.000000000000000000, 0.9510565162951535312, 1.000000000000000000, 0.9510565162951535312, 1.000000000000000000, 0.9510565162951535312, 1.000000000000000000, 0.9510565162951535312, 1.000000000000000000, 0.9510565162951535312, 1.000000000000000000, 0.9510565162951535312, 1.000000000000000000, 0.9510565162951535312, 1.000000000000000000, 0.9510565162951535312, 1.000000000000000000, 0.9510565162951535312, 1.000000000000000000, 0.9510565162951535312, 1.000000000000000000, 0.9510565162951535312, 1.000000000000000000, 0.9510565162951535312, 1.000000000000000000, 0.9510565162951535312, 1.000000000000000000, 0.9510565162951535312, 1.000000000000000000, 0.9510565162951535312, 1.000000000000000000, 0.9510565162951535312, 1.000000000000000000, 0.9510565162951535312, 1.000000000000000000, 0.9510565162951535312, 1.000000000000000000, 0.9510565162951535312, 1.000000000000000000, 0.9510565162951535312, 1.000000000000000000, 0.9510565162951535312, 1.000000000000000000, 0.9510565162951535312, 1.000000000000000000, 0.9510565162951535312, 1.000000000000000000, 0.9510565162951535312, 1.000000000000000000, 0.9510565162951535312, 1.000000000000000000, 0.9510565162951535312, 1.000000000000000000, 0.9510565162951535312, 1.000000000000000000, 0.9510565162951535312, 1.000000000000000000, 0.9510565162951535312, 1.000000000000000000, 0.9510565162951535312, 1.000000000000000000, 0.9510565162951535312, 1.000000000000000000, 0.9510565162951535312, 1.000000000000000000, 0.9510565162951535312, 1.000000000000000000, 0.9510565162951535312, 1.000000000000000000, 0.9510565162951535312, 1.000000000000000000, 0.9510565162951535312, 1.000000000000000000, 0.9510565162951535312, 1.000000000000000000, 0.9510565162951535312, 1.000000000000000000, 0.9510565162951535312, 1.000000000000000000, 0.9510565162951535312, 1.000000000000000000, 0.9510565162951535312, 1.000000000000000000, 0.9510565162951535312, 1.000000000000000000, 0.9510565162951535312, 1.000000000000000000, 0.9510565162951535312, 1.000000000000000000, 0.9510565162951535312, 1.000000000000000000, 0.9510565162951535312, 1.000000000000000000, 0.9510565162951535312, 1.000000000000000000, 0.9510565162951535312, 1.000000000000000000, 0.9510565162951535312, 1.000000000000000000, 0.9510565162951535312, 1.000000000000000000, 0.9510565162951535312, 1.000000000000000000, 0.9510565162951535312, 1.000000000000000000, 0.9510565162951535312, 1.000000000000000000, 0.9510565162951535312, 1.000000000000000000, 0.9510565162951535312, 1.000000000000000000, 0.9510565162951535312, 1.000000000000000000, 0.9510565162951535312, 1.000000000000000000, 0.9510565162951535312, 1.000000000000000000, 0.9510565162951535312, 1.000000000000000000, 0.9510565162951535312, 1.000000000000000000, 0.9510565162951535312, 1.000000000000000000, 0.9510565162951535312, 1.000000000000000000, 0.9510565162951535312, 1.000000000000000000, 0.9510565162951535312, 1.000000000000000000, 0.9510565162951535312, 1.000000000000000000, 0.9510565162951535312, 1.000000000000000000, 0.9510565162951535312, 1.000000000000000000, 0.9510565162951535312, 1.000000000000000000, 0.9510565162951535312, 1.000000000000000000, 0.9510565162951535312, 1.000000000000000000, 0.9510565162951535312, 1.000000000000000000, 0.9510565162951535312, 1.000000000000000000, 0.9510565162951535312, 1.000000000000000000, 0.9510565162951535312, 1.000000000000000000, 0.9510565162951535312, 1.000000000000000000, 0.9510565162951535312, 1.000000000000000000, 0.9510565162951535312, 1.000000000000000000, 0.9510565162951535312, 1.000000000000000000, 0.9510565162951535312, 1.000000000000000000, 0.9510565162951535312, 1.000000000000000000, 0.9510565162951535312, 1.000000000000000000, 0.9510565162951535312, 1.000000000000000000, 0.9510565162951535312, 1.000000000000000000, 0.9510565162951535312, 1.000000000000000000, 0.9510565162951535312, 1.000000000000000000, 0.9510565162951535312, 1.000000000000000000, 0.9510565162951535312, 1.000000000000000000, 0.9510565162951535312, 1.000000000000000000, 0.9510565162951535312, 1.000000000000000000, 0.9510565162951535312, 1.000000000000000000, 0.9510565162951535312, 1.000000000000000000, 0.9510565162951535312, 1.000000000000000000, 0.9510565162951535312, 1.000000000000000000, 0.9510565162951535312, 1.000000000000000000, 0.9510565162951535312, 1.000000000000000000, 0.9510565162951535312, 1.000000000000000000, 0.9510565162951535312, 1.000000000000000000, 0.9510565162951535312, 1.000000000000000000, 0.9510565162951535312, 1.000000000000000000, 0.9510565162951535312, 1.000000000000000000, 0.9510565162951535312, 1.000000000000000000, 0.9510565162951535312, 1.000000000000000000, 0.9510565162951535312, 1.000000000000000000, 0.9510565162951535312, 1.000000000000000000, 0.9510565162951535312, 1.000000000000000000, 0.9510565162951535312, 1.000000000000000000, 0.9510565162951535312, 1.000000000000000000, 0.9510565162951535312, 1.000000000000000000, 0.9510565162951535312, 1.000000000000000000, 0.9510565162951535312, 1.000000000000000000, 0.9510565162951535312, 1.000000000000000000, 0.9510565162951535312, 1.000000000000000000, 0.9510565162951535312, 1.000000000000000000, 0.9510565162951535312, 1.000000000000000000, 0.9510565162951535312, 1.000000000000000000, 0.9510565162951535312, 1.000000000000000000, 0.9510565162951535312, 1.000000000000000000, 0.9510565162951535312, 1.000000000000000000, 0.9510565162951535312, 1.000000000000000000, 0.9510565162951535312, 1.000000000000000000, 0.9510565162951535312, 1.000000000000000000, 0.9510565162951535312, 1.000000000000000000, 0.9510565162951535312, 1.000000000000000000, 0.9510565162951535312, 1.000000000000000000, 0.9510565162951535312, 1.000000000000000000, 0.9510565162951535312, 1.000000000000000000, 0.9510565162951535312, 1.000000000000000000, 0.9510565162951535312, 1.000000000000000000, 0.9510565162951535312, 1.000000000000000000, 0.9510565162951535312, 1.000000000000000000, 0.9510565162951535312, 1.000000000000000000, 0.9510565162951535312, 1.000000000000000000, 0.9510565162951535312, 1.000000000000000000, 0.9510565162951535312, 1.000000000000000000, 0.9510565162951535312, 1.000000000000000000, 0.9510565162951535312, 1.000000000000000000, 0.9510565162951535312, 1.000000000000000000, 0.9510565162951535312, 1.000000000000000000, 0.9510565162951535312, 1.000000000000000000, 0.9510565162951535312, 1.000000000000000000, 0.9510565162951535312, 1.000000000000000000, 0.9510565162951535312, 1.000000000000000000, 0.9510565162951535312, 1.000000000000000000, 0.9510565162951535312, 1.000000000000000000, 0.9510565162951535312, 1.000000000000000000, 0.9510565162951535312, 1.000000000000000000, 0.9510565162951535312, 1.000000000000000000, 0.9510565162951535312, 1.000000000000000000, 0.9510565162951535312, 1.000000000000000000, 0.9510565162951535312, 1.000000000000000000, 0.9510565162951535312, 1.000000000000000000, 0.9510565162951535312, 1.000000000000000000, 0.9510565162951535312, 1.000000000000000000, 0.9510565162951535312, 1.000000000000000000, 0.9510565162951535312, 1.000000000000000000, 0.9510565162951535312, 1.000000000000000000, 0.9510565162951535312, 1.000000000000000000, 0.9510565162951535312, 1.000000000000000000, 0.9510565162951535312, 1.000000000000000000, 0.9510565162951535312, 1.000000000000000000, 0.9510565162951535312, 1.000000000000000000, 0.9510565162951535312, 1.000000000000000000, 0.9510565162951535312, 1.000000000000000000, 0.9510565162951535312, 1.000000000000000000, 0.9510565162951535312, 1.000000000000000000, 0.9510565162951535312, 1.000000000000000000),
 ( 1.000000000000000000, 0.9510565162951535312, 1.000000000000000000, 0.9510565162951535312, 1.000000000000000000, 0.9510565162951535312, 1.000000000000000000, 0.9510565162951535312, 1.000000000000000000, 0.9510565162951535312, 1.000000000000000000, 0.9510565162951535312, 1.000000000000000000, 0.9510565162951535312, 1.000000000000000000, 0.9510565162951535312, 1.000000000000000000, 0.9510565162951535312, 1.000000000000000000, 0.9510565162951535312, 1.000000000000000000, 0.9510565162951535312, 1.000000000000000000, 0.9510565162951535312, 1.000000000000000000, 0.9510565162951535312, 1.000000000000000000, 0.9510565162951535312, 1.000000000000000000, 0.9510565162951535312, 1.000000000000000000, 0.9510565162951535312, 1.000000000000000000, 0.9510565162951535312, 1.000000000000000000, 0.9510565162951535312, 1.000000000000000000, 0.9510565162951535312, 1.000000000000000000, 0.9510565162951535312, 1.000000000000000000, 0.9510565162951535312, 1.000000000000000000, 0.9510565162951535312, 1.000000000000000000, 0.9510565162951535312, 1.000000000000000000, 0.9510565162951535312, 1.000000000000000000, 0.9510565162951535312, 1.000000000000000000, 0.9510565162951535312, 1.000000000000000000, 0.9510565162951535312, 1.000000000000000000, 0.9510565162951535312, 1.000000000000000000, 0.9510565162951535312, 1.000000000000000000, 0.9510565162951535312, 1.000000000000000000, 0.9510565162951535312, 1.000000000000000000, 0.9510565162951535312, 1.000000000000000000, 0.9510565162951535312, 1.000000000000000000, 0.9510565162951535312, 1.000000000000000000, 0.9510565162951535312, 1.000000000000000000, 0.9510565162951535312, 1.000000000000000000, 0.9510565162951535312, 1.000000000000000000, 0.9510565162951535312, 1.000000000000000000, 0.9510565162951535312, 1.000000000000000000, 0.9510565162951535312, 1.000000000000000000, 0.9510565162951535312, 1.000000000000000000, 0.9510565162951535312, 1.000000000000000000, 0.9510565162951535312, 1.000000000000000000, 0.9510565162951535312, 1.000000000000000000, 0.9510565162951535312, 1.000000000000000000, 0.9510565162951535312, 1.000000000000000000, 0.9510565162951535312, 1.000000000000000000, 0.9510565162951535312, 1.000000000000000000, 0.9510565162951535312, 1.000000000000000000, 0.9510565162951535312, 1.000000000000000000, 0.9510565162951535312, 1.000000000000000000, 0.9510565162951535312, 1.000000000000000000, 0.9510565162951535312, 1.000000000000000000, 0.9510565162951535312, 1.000000000000000000, 0.9510565162951535312, 1.000000000000000000, 0.9510565162951535312, 1.000000000000000000, 0.9510565162951535312, 1.000000000000000000, 0.9510565162951535312, 1.000000000000000000, 0.9510565162951535312, 1.000000000000000000, 0.9510565162951535312, 1.000000000000000000, 0.9510565162951535312, 1.000000000000000000, 0.9510565162951535312, 1.000000000000000000, 0.9510565162951535312, 1.000000000000000000, 0.9510565162951535312, 1.000000000000000000, 0.9510565162951535312, 1.000000000000000000, 0.9510565162951535312, 1.000000000000000000, 0.9510565162951535312, 1.000000000000000000, 0.9510565162951535312, 1.000000000000000000, 0.9510565162951535312, 1.000000000000000000, 0.9510565162951535312, 1.000000000000000000, 0.9510565162951535312, 1.000000000000000000, 0.9510565162951535312, 1.000000000000000000, 0.9510565162951535312, 1.000000000000000000, 0.9510565162951535312, 1.000000000000000000, 0.9510565162951535312, 1.000000000000000000, 0.9510565162951535312, 1.000000000000000000, 0.9510565162951535312, 1.000000000000000000, 0.9510565162951535312, 1.000000000000000000, 0.9510565162951535312, 1.000000000000000000, 0.9510565162951535312, 1.000000000000000000, 0.9510565162951535312, 1.000000000000000000, 0.9510565162951535312, 1.000000000000000000, 0.9510565162951535312, 1.000000000000000000, 0.9510565162951535312, 1.000000000000000000, 0.9510565162951535312, 1.000000000000000000, 0.9510565162951535312, 1.000000000000000000, 0.9510565162951535312, 1.000000000000000000, 0.9510565162951535312, 1.000000000000000000, 0.9510565162951535312, 1.000000000000000000, 0.9510565162951535312, 1.000000000000000000, 0.9510565162951535312, 1.000000000000000000, 0.9510565162951535312, 1.000000000000000000, 0.9510565162951535312, 1.000000000000000000, 0.9510565162951535312, 1.000000000000000000, 0.9510565162951535312, 1.000000000000000000, 0.9510565162951535312, 1.000000000000000000, 0.9510565162951535312, 1.000000000000000000, 0.9510565162951535312, 1.000000000000000000, 0.9510565162951535312, 1.000000000000000000, 0.9510565162951535312, 1.000000000000000000, 0.9510565162951535312, 1.000000000000000000, 0.9510565162951535312, 1.000000000000000000, 0.9510565162951535312, 1.000000000000000000, 0.9510565162951535312, 1.000000000000000000, 0.9510565162951535312, 1.000000000000000000, 0.9510565162951535312, 1.000000000000000000, 0.9510565162951535312, 1.000000000000000000, 0.9510565162951535312, 1.000000000000000000, 0.9510565162951535312, 1.000000000000000000, 0.9510565162951535312, 1.000000000000000000, 0.9510565162951535312, 1.000000000000000000, 0.9510565162951535312, 1.000000000000000000, 0.9510565162951535312, 1.000000000000000000, 0.9510565162951535312, 1.000000000000000000, 0.9510565162951535312, 1.000000000000000000, 0.9510565162951535312, 1.000000000000000000, 0.9510565162951535312, 1.000000000000000000, 0.9510565162951535312, 1.000000000000000000, 0.9510565162951535312, 1.000000000000000000, 0.9510565162951535312, 1.000000000000000000, 0.9510565162951535312, 1.000000000000000000, 0.9510565162951535312, 1.000000000000000000, 0.9510565162951535312, 1.000000000000000000, 0.9510565162951535312, 1.000000000000000000, 0.9510565162951535312, 1.000000000000000000, 0.9510565162951535312, 1.000000000000000000, 0.9510565162951535312, 1.000000000000000000, 0.9510565162951535312, 1.000000000000000000, 0.9510565162951535312, 1.000000000000000000, 0.9510565162951535312, 1.000000000000000000, 0.9510565162951535312, 1.000000000000000000, 0.9510565162951535312, 1.000000000000000000, 0.9510565162951535312, 1.000000000000000000, 0.9510565162951535312, 1.000000000000000000, 0.9510565162951535312, 1.000000000000000000, 0.9510565162951535312, 1.000000000000000000, 0.9510565162951535312, 1.000000000000000000, 0.9510565162951535312, 1.000000000000000000, 0.9510565162951535312, 1.000000000000000000, 0.9510565162951535312, 1.000000000000000000, 0.9510565162951535312, 1.000000000000000000, 0.9510565162951535312, 1.000000000000000000, 0.9510565162951535312, 1.000000000000000000, 0.9510565162951535312, 1.000000000000000000, 0.9510565162951535312, 1.000000000000000000, 0.9510565162951535312, 1.000000000000000000, 0.9510565162951535312, 1.000000000000000000, 0.9510565162951535312, 1.000000000000000000, 0.9510565162951535312, 1.000000000000000000, 0.9510565162951535312, 1.000000000000000000, 0.9510565162951535312, 1.000000000000000000, 0.9510565162951535312, 1.000000000000000000, 0.9510565162951535312, 1.000000000000000000, 0.9510565162951535312, 1.000000000000000000, 0.9510565162951535312, 1.000000000000000000, 0.9510565162951535312, 1.000000000000000000, 0.9510565162951535312, 1.000000000000000000, 0.9510565162951535312, 1.000000000000000000, 0.9510565162951535312, 1.000000000000000000, 0.9510565162951535312, 1.000000000000000000, 0.9510565162951535312, 1.000000000000000000, 0.9510565162951535312, 1.000000000000000000, 0.9510565162951535312, 1.000000000000000000, 0.9510565162951535312, 1.000000000000000000, 0.9510565162951535312, 1.000000000000000000, 0.9510565162951535312, 1.000000000000000000, 0.9510565162951535312, 1.000000000000000000, 0.9510565162951535312, 1.000000000000000000, 0.9510565162951535312, 1.000000000000000000, 0.9510565162951535312, 1.000000000000000000) ) ) 
 REPRESENTATION_ITEM ( '' )  SURFACE ( )  );
#53595=( NAMED_UNIT ( * ) SI_UNIT ( $, .STERADIAN. ) SOLID_ANGLE_UNIT ( ) );
#53596=CARTESIAN_POINT ( 'NONE',  ( 23.71231517720798010, 117.4999999999999716, -9.500000000000000000 ) ) ;
#53597=CIRCLE ( 'NONE', #42410, 1.000000000000000888 ) ;
#53599=ADVANCED_FACE ( 'NONE', ( #57049 ), #51789, .F. ) ;
#53604=SURFACE_STYLE_USAGE ( .BOTH. , #26832 ) ;
#53605=FACE_OUTER_BOUND ( 'NONE', #20933, .T. ) ;
#53606=CARTESIAN_POINT ( 'NONE',  ( 0.000000000000000000, 145.0570736234661524, -8.025000000000000355 ) ) ;
#53613=FILL_AREA_STYLE ('',( #65199 ) ) ;
#53615=CARTESIAN_POINT ( 'NONE',  ( -71.50000000000000000, 35.92875272052971525, 7.500000000000000000 ) ) ;
#53616=ADVANCED_FACE ( 'NONE', ( #16161 ), #65355, .F. ) ;
#53629=DIRECTION ( 'NONE',  ( -0.000000000000000000, -0.000000000000000000, 1.000000000000000000 ) ) ;
#53632=MECHANICAL_DESIGN_GEOMETRIC_PRESENTATION_REPRESENTATION('',(#16609),#4145);
#53634=EDGE_LOOP ( 'NONE', ( #27856, #45539, #7132, #6100 ) ) ;
#53638=CARTESIAN_POINT ( 'NONE',  ( -9.058813317711338797, 125.3449999999999847, 2.943386871421373563 ) ) ;
#53640=ORIENTED_EDGE ( 'NONE', *, *, #34901, .F. ) ;
#53642=STYLED_ITEM ( 'NONE', ( #33927 ), #67425 ) ;
#53643=CARTESIAN_POINT ( 'NONE',  ( -52.00000000000000000, -1.926070501056209087E-14, 12.00000000000000000 ) ) ;
#53644=LINE ( 'NONE', #48769, #11894 ) ;
#53646=( LENGTH_UNIT ( ) NAMED_UNIT ( * ) SI_UNIT ( .MILLI., .METRE. ) );
#53648=CARTESIAN_POINT ( 'NONE',  ( 40.78947368421051323, 108.1536491499103363, 3.000000000000000000 ) ) ;
#53655=DIRECTION ( 'NONE',  ( -0.000000000000000000, -0.000000000000000000, 1.000000000000000000 ) ) ;
#53656=UNCERTAINTY_MEASURE_WITH_UNIT (LENGTH_MEASURE( 1.000000000000000082E-05 ), #15595, 'distance_accuracy_value', 'NONE');
#53658=FILL_AREA_STYLE_COLOUR ( '', #22569 ) ;
#53660=CARTESIAN_POINT ( 'NONE',  ( 0.000000000000000000, 161.5550000000000068, -9.525000000000000355 ) ) ;
#53672=EDGE_CURVE ( 'NONE', #40899, #3817, #34032, .T. ) ;
#53674=DIRECTION ( 'NONE',  ( -0.000000000000000000, 1.000000000000000000, -0.000000000000000000 ) ) ;
#53675=COLOUR_RGB ( '', 0.08235294, 0.09019608, 0.10196078) ;
#53676=CARTESIAN_POINT ( 'NONE',  ( -7.632228543268608334, 118.9570736234661581, 2.479861379858952830 ) ) ;
#53677=EDGE_CURVE ( 'NONE', #40049, #12184, #59633, .T. ) ;
#53678=( NAMED_UNIT ( * ) SI_UNIT ( $, .STERADIAN. ) SOLID_ANGLE_UNIT ( ) );
#53681=PLANE ( 'NONE',  #7209 ) ;
#53682=EDGE_CURVE ( 'NONE', #44352, #44514, #13255, .T. ) ;
#53683=VERTEX_POINT ( 'NONE', #23149 ) ;
#53688=CARTESIAN_POINT ( 'NONE',  ( -5.598654528085806881, 131.8549999999999898, -7.705886871421374629 ) ) ;
#53690=EDGE_CURVE ( 'NONE', #26112, #41724, #5699, .T. ) ;
#53691=SURFACE_STYLE_FILL_AREA ( #37223 ) ;
#53694=CARTESIAN_POINT ( 'NONE',  ( 6.962805267914501606, 153.0662478080784012, 4.200845087328706207 ) ) ;
#53695=EDGE_CURVE ( 'NONE', #61842, #22693, #3404, .T. ) ;
#53697=CARTESIAN_POINT ( 'NONE',  ( 8.437984349512095861, 152.1929263765338192, 1.550032578732817026E-15 ) ) ;
#53700=( LENGTH_UNIT ( ) NAMED_UNIT ( * ) SI_UNIT ( .MILLI., .METRE. ) );
#53706=CIRCLE ( 'NONE', #53756, 15.00000000000000000 ) ;
#53710=CARTESIAN_POINT ( 'NONE',  ( -54.49999999999999289, -1.956686671034893189E-14, 6.500000000000000000 ) ) ;
#53712=CARTESIAN_POINT ( 'NONE',  ( -8.253986449296890626, 153.4602809114455511, -1.986321737243838648 ) ) ;
#53713=ORIENTED_EDGE ( 'NONE', *, *, #54397, .F. ) ;
#53714=MECHANICAL_DESIGN_GEOMETRIC_PRESENTATION_REPRESENTATION('',(#3097),#24480);
#53716=PLANE ( 'NONE',  #1346 ) ;
#53719=SURFACE_STYLE_USAGE ( .BOTH. , #63926 ) ;
#53727=STYLED_ITEM ( 'NONE', ( #55075 ), #1109 ) ;
#53736=PLANE ( 'NONE',  #41611 ) ;
#53738=CARTESIAN_POINT ( 'NONE',  ( -9.058813317711338797, 141.4549999999999841, 2.943386871421373563 ) ) ;
#53741=CARTESIAN_POINT ( 'NONE',  ( -72.50000000000001421, 35.92875272052971525, -10.00000000000000000 ) ) ;
#53743=( LENGTH_UNIT ( ) NAMED_UNIT ( * ) SI_UNIT ( .MILLI., .METRE. ) );
#53747=EDGE_CURVE ( 'NONE', #27816, #20613, #2292, .T. ) ;
#53751=DIRECTION ( 'NONE',  ( -0.000000000000000000, -0.000000000000000000, -1.000000000000000000 ) ) ;
#53752=ADVANCED_FACE ( 'NONE', ( #49537 ), #61890, .F. ) ;
#53755=ORIENTED_EDGE ( 'NONE', *, *, #22327, .F. ) ;
#53756=AXIS2_PLACEMENT_3D ( 'NONE', #48635, #15568, #21868 ) ;
#53760=VECTOR ( 'NONE', #26614, 1000.000000000000000 ) ;
#53762=DIRECTION ( 'NONE',  ( 0.000000000000000000, 0.000000000000000000, 1.000000000000000000 ) ) ;
#53765=ORIENTED_EDGE ( 'NONE', *, *, #47730, .T. ) ;
#53767=ORIENTED_EDGE ( 'NONE', *, *, #45101, .F. ) ;
#53770=ORIENTED_EDGE ( 'NONE', *, *, #8349, .F. ) ;
#53772=CARTESIAN_POINT ( 'NONE',  ( -10.01517768586949231, 155.1949999999999648, -6.132527647946036459E-16 ) ) ;
#53773=FILL_AREA_STYLE ('',( #48205 ) ) ;
#53774=VERTEX_POINT ( 'NONE', #12208 ) ;
#53776=SURFACE_STYLE_USAGE ( .BOTH. , #10546 ) ;
#53777=DIRECTION ( 'NONE',  ( 0.000000000000000000, 0.000000000000000000, -1.000000000000000000 ) ) ;
#53779=CARTESIAN_POINT ( 'NONE',  ( -2.607480562269075097, 124.2929263765337993, 8.025000000000000355 ) ) ;
#53781=CARTESIAN_POINT ( 'NONE',  ( -75.46465235827693618, 36.01723441224693545, -9.608246556350810152 ) ) ;
#53782=AXIS2_PLACEMENT_3D ( 'NONE', #24554, #46428, #57997 ) ;
#53783=CARTESIAN_POINT ( 'NONE',  ( 2.607480562269051116, 124.5929263765338106, 8.025000000000016342 ) ) ;
#53788=ORIENTED_EDGE ( 'NONE', *, *, #60487, .T. ) ;
#53791=CARTESIAN_POINT ( 'NONE',  ( 74.50000000000000000, -2.135340797662720349E-14, 6.999999999999999112 ) ) ;
#53793=PRESENTATION_STYLE_ASSIGNMENT (( #65032 ) ) ;
#53794=EDGE_CURVE ( 'NONE', #2846, #43100, #40729, .T. ) ;
#53795=UNCERTAINTY_MEASURE_WITH_UNIT (LENGTH_MEASURE( 1.000000000000000082E-05 ), #32214, 'distance_accuracy_value', 'NONE');
#53798=CARTESIAN_POINT ( 'NONE',  ( 40.78947371891847240, 108.1536491252660568, 3.151596837137058404 ) ) ;
#53808=CARTESIAN_POINT ( 'NONE',  ( 0.000000000000000000, 154.9999999999999716, 0.000000000000000000 ) ) ;
#53811=VECTOR ( 'NONE', #54462, 1000.000000000000000 ) ;
#53812=CARTESIAN_POINT ( 'NONE',  ( -75.46551724137930250, 63.49197145334878201, -10.00000000000000000 ) ) ;
#53814=MECHANICAL_DESIGN_GEOMETRIC_PRESENTATION_REPRESENTATION('',(#67277),#62792);
#53815=EDGE_LOOP ( 'NONE', ( #56098, #60333, #41426, #11405 ) ) ;
#53816=FACE_OUTER_BOUND ( 'NONE', #8470, .T. ) ;
#53817=DIRECTION ( 'NONE',  ( 0.000000000000000000, 0.000000000000000000, 1.000000000000000000 ) ) ;
#53822=CARTESIAN_POINT ( 'NONE',  ( -5.598654528085808657, 111.7549999999999955, 7.705886871421373741 ) ) ;
#53825=STYLED_ITEM ( 'NONE', ( #68729 ), #14964 ) ;
#53829=CIRCLE ( 'NONE', #11145, 0.5000000000000004441 ) ;
#53831=ORIENTED_EDGE ( 'NONE', *, *, #67769, .T. ) ;
#53837=EDGE_CURVE ( 'NONE', #8600, #49132, #63002, .T. ) ;
#53838=FILL_AREA_STYLE_COLOUR ( '', #66637 ) ;
#53839=( NAMED_UNIT ( * ) PLANE_ANGLE_UNIT ( ) SI_UNIT ( $, .RADIAN. ) );
#53843=STYLED_ITEM ( 'NONE', ( #67047 ), #58874 ) ;
#53845=DIRECTION ( 'NONE',  ( -0.000000000000000000, 1.000000000000000000, -0.000000000000000000 ) ) ;
#53847=CARTESIAN_POINT ( 'NONE',  ( 9.827790563157511022E-16, 87.30187232391182306, -8.025000000000000355 ) ) ;
#53848=CARTESIAN_POINT ( 'NONE',  ( -45.00000000000000000, 8.380821545698690755, 5.549835146672248420 ) ) ;
#53850=EDGE_CURVE ( 'NONE', #16782, #43736, #52325, .T. ) ;
#53854=FILL_AREA_STYLE ('',( #59128 ) ) ;
#53858=VECTOR ( 'NONE', #33301, 1000.000000000000000 ) ;
#53859=DIRECTION ( 'NONE',  ( -0.000000000000000000, -0.000000000000000000, -1.000000000000000000 ) ) ;
#53862=CARTESIAN_POINT ( 'NONE',  ( 9.058813317711337021, 120.5449999999999875, 2.943386871421375783 ) ) ;
#53865=CARTESIAN_POINT ( 'NONE',  ( 10.01517768586949408, 133.8049999999999784, 1.839758294383810543E-15 ) ) ;
#53872=CARTESIAN_POINT ( 'NONE',  ( 3.094860106618431583, 148.2050000000000125, 9.525000000000000355 ) ) ;
#53874=UNCERTAINTY_MEASURE_WITH_UNIT (LENGTH_MEASURE( 1.000000000000000082E-05 ), #15944, 'distance_accuracy_value', 'NONE');
#53875=SURFACE_STYLE_FILL_AREA ( #691 ) ;
#53880=DIRECTION ( 'NONE',  ( -1.000000000000000000, 1.224646799147349509E-16, 0.000000000000000000 ) ) ;
#53885=COLOUR_RGB ( '', 0.72549020, 0.75294118, 0.79215686) ;
#53886=SURFACE_STYLE_USAGE ( .BOTH. , #58833 ) ;
#53889=SURFACE_STYLE_USAGE ( .BOTH. , #42368 ) ;
#53892=CARTESIAN_POINT ( 'NONE',  ( 24.21231517720798010, 113.4999999999999858, -7.500000000000000000 ) ) ;
#53897=AXIS2_PLACEMENT_3D ( 'NONE', #18015, #55655, #39865 ) ;
#53900=FACE_OUTER_BOUND ( 'NONE', #51967, .T. ) ;
#53902=CARTESIAN_POINT ( 'NONE',  ( -1.166476076187854022E-15, 131.9449999999999932, 9.525000000000000355 ) ) ;
#53906=VECTOR ( 'NONE', #49283, 1000.000000000000000 ) ;
#53911=AXIS2_PLACEMENT_3D ( 'NONE', #65696, #63367, #27685 ) ;
#53916=SURFACE_STYLE_USAGE ( .BOTH. , #4696 ) ;
#53920=EDGE_LOOP ( 'NONE', ( #57885, #17031, #24379, #63882 ) ) ;
#53922=DIRECTION ( 'NONE',  ( 0.000000000000000000, -1.000000000000000000, 0.000000000000000000 ) ) ;
#53923=ORIENTED_EDGE ( 'NONE', *, *, #56829, .F. ) ;
#53924=ADVANCED_FACE ( 'NONE', ( #31161 ), #19220, .F. ) ;
#53929=EDGE_CURVE ( 'NONE', #54030, #11506, #46003, .T. ) ;
#53930=DIRECTION ( 'NONE',  ( 0.000000000000000000, 0.000000000000000000, -1.000000000000000000 ) ) ;
#53936=SURFACE_STYLE_USAGE ( .BOTH. , #11382 ) ;
#53937=CARTESIAN_POINT ( 'NONE',  ( 4.716976649647096842, 140.8570736234661638, 6.492361379858953896 ) ) ;
#53938=VERTEX_POINT ( 'NONE', #62140 ) ;
#53940=CARTESIAN_POINT ( 'NONE',  ( 0.000000000000000000, 137.9429263765338192, -8.025000000000000355 ) ) ;
#53942=UNCERTAINTY_MEASURE_WITH_UNIT (LENGTH_MEASURE( 1.000000000000000082E-05 ), #29352, 'distance_accuracy_value', 'NONE');
#53944=ORIENTED_EDGE ( 'NONE', *, *, #16630, .T. ) ;
#53948=PRESENTATION_STYLE_ASSIGNMENT (( #10711 ) ) ;
#53949=MECHANICAL_DESIGN_GEOMETRIC_PRESENTATION_REPRESENTATION('',(#64050),#2219);
#53952=COLOUR_RGB ( '', 0.31764706, 0.68627451, 0.89019608) ;
#53954=LINE ( 'NONE', #21976, #16015 ) ;
#53957=AXIS2_PLACEMENT_3D ( 'NONE', #16436, #37904, #59635 ) ;
#53958=ORIENTED_EDGE ( 'NONE', *, *, #45924, .T. ) ;
#53963=CARTESIAN_POINT ( 'NONE',  ( -74.99999999999998579, 36.00000000000000711, -41.30495168499704306 ) ) ;
#53966=FILL_AREA_STYLE ('',( #27573 ) ) ;
#53973=AXIS2_PLACEMENT_3D ( 'NONE', #43935, #65344, #17197 ) ;
#53974=CARTESIAN_POINT ( 'NONE',  ( 8.102448949553181734, 135.9949999999999477, -5.886773742842746238 ) ) ;
#53977=DIRECTION ( 'NONE',  ( 0.000000000000000000, 0.000000000000000000, 1.000000000000000000 ) ) ;
#53978=ORIENTED_EDGE ( 'NONE', *, *, #17080, .F. ) ;
#53980=DIRECTION ( 'NONE',  ( 0.000000000000000000, 0.000000000000000000, -1.000000000000000000 ) ) ;
#53981=FILL_AREA_STYLE ('',( #28630 ) ) ;
#53982=PRESENTATION_STYLE_ASSIGNMENT (( #106 ) ) ;
#53983=CARTESIAN_POINT ( 'NONE',  ( 72.50000000000000000, 14.49137674618942562, 9.500000000000000000 ) ) ;
#53986=LINE ( 'NONE', #47385, #55483 ) ;
#53987=( NAMED_UNIT ( * ) PLANE_ANGLE_UNIT ( ) SI_UNIT ( $, .RADIAN. ) );
#53992=ORIENTED_EDGE ( 'NONE', *, *, #43869, .F. ) ;
#53993=EDGE_CURVE ( 'NONE', #27227, #22912, #9146, .T. ) ;
#53994=( BOUNDED_CURVE ( )  B_SPLINE_CURVE ( 2, ( #23857, #17579, #60779, #18240, #22836, #23184, #29104, #50597, #45363, #28777, #44674 ),
 .UNSPECIFIED., .F., .F. ) 
 B_SPLINE_CURVE_WITH_KNOTS ( ( 3, 2, 2, 2, 2, 3 ),
 ( 0.05882352941176476058, 0.06470588235294123802, 0.07058823529411770159, 0.07647058823529419291, 0.08235294117647065648, 0.08823529411764713393 ),
 .UNSPECIFIED. ) 
 CURVE ( )  GEOMETRIC_REPRESENTATION_ITEM ( )  RATIONAL_B_SPLINE_CURVE ( ( 0.9999999999999995559, 0.9510565162951539753, 1.000000000000000000, 0.9510565162951535312, 1.000000000000000000, 0.9510565162951535312, 1.000000000000000000, 0.9510565162951535312, 1.000000000000000000, 0.9510565162951529761, 1.000000000000000666 ) ) 
 REPRESENTATION_ITEM ( '' )  );
#53995=SURFACE_STYLE_FILL_AREA ( #11787 ) ;
#53996=DIRECTION ( 'NONE',  ( 1.000000000000000000, 0.000000000000000000, 0.000000000000000000 ) ) ;
#54006=VECTOR ( 'NONE', #11722, 1000.000000000000000 ) ;
#54010=CARTESIAN_POINT ( 'NONE',  ( -41.49999999999997868, 9.999999999999978684, 3.500000000000000000 ) ) ;
#54014=FILL_AREA_STYLE_COLOUR ( '', #23637 ) ;
#54020=ORIENTED_EDGE ( 'NONE', *, *, #50131, .T. ) ;
#54023=CARTESIAN_POINT ( 'NONE',  ( 2.607480562269076430, 111.9070736234661751, -8.025000000000000355 ) ) ;
#54025=FACE_OUTER_BOUND ( 'NONE', #52655, .T. ) ;
#54026=( NAMED_UNIT ( * ) SI_UNIT ( $, .STERADIAN. ) SOLID_ANGLE_UNIT ( ) );
#54028=ORIENTED_EDGE ( 'NONE', *, *, #69580, .F. ) ;
#54030=VERTEX_POINT ( 'NONE', #69506 ) ;
#54031=CARTESIAN_POINT ( 'NONE',  ( -10.01517768586949231, 129.3050000000000068, -6.132527647946036459E-16 ) ) ;
#54035=CARTESIAN_POINT ( 'NONE',  ( 45.50000000000000000, -1.469576158976824618E-14, 10.00000000000000000 ) ) ;
#54041=CARTESIAN_POINT ( 'NONE',  ( -71.50000000000000000, 35.92875272052971525, -7.500000000000000000 ) ) ;
#54042=EDGE_LOOP ( 'NONE', ( #25002, #64105, #54921, #20342 ) ) ;
#54044=PLANE ( 'NONE',  #37082 ) ;
#54059=CARTESIAN_POINT ( 'NONE',  ( -72.49999999999998579, 63.67479433117734544, -10.00000000000000000 ) ) ;
#54060=CARTESIAN_POINT ( 'NONE',  ( -7.514523004098856873, 153.7576610836294151, 4.578433682763812129 ) ) ;
#54063=CARTESIAN_POINT ( 'NONE',  ( 74.99999999999998579, 50.00000000000000000, -7.500000000000000000 ) ) ;
#54074=( GEOMETRIC_REPRESENTATION_CONTEXT ( 3 ) GLOBAL_UNCERTAINTY_ASSIGNED_CONTEXT ( ( #41874 ) ) GLOBAL_UNIT_ASSIGNED_CONTEXT ( ( #22624, #43093, #59901 ) ) REPRESENTATION_CONTEXT ( 'NONE', 'WORKASPACE' ) );
#54079=( LENGTH_UNIT ( ) NAMED_UNIT ( * ) SI_UNIT ( .MILLI., .METRE. ) );
#54082=DIRECTION ( 'NONE',  ( 0.000000000000000000, 0.000000000000000000, -1.000000000000000000 ) ) ;
#54085=CARTESIAN_POINT ( 'NONE',  ( -9.058813317711337021, 135.1550000000000011, -2.943386871421374895 ) ) ;
#54086=CARTESIAN_POINT ( 'NONE',  ( -4.716976649647097730, 126.2429263765338163, -6.492361379858953896 ) ) ;
#54089=CARTESIAN_POINT ( 'NONE',  ( 0.000000000000000000, 110.4999999999999858, 0.000000000000000000 ) ) ;
#54093=ADVANCED_FACE ( 'NONE', ( #47412 ), #68836, .T. ) ;
#54096=MECHANICAL_DESIGN_GEOMETRIC_PRESENTATION_REPRESENTATION('',(#29342),#47381);
#54097=( LENGTH_UNIT ( ) NAMED_UNIT ( * ) SI_UNIT ( .MILLI., .METRE. ) );
#54101=ORIENTED_EDGE ( 'NONE', *, *, #23551, .F. ) ;
#54103=SURFACE_SIDE_STYLE ('',( #16521 ) ) ;
#54104=( NAMED_UNIT ( * ) SI_UNIT ( $, .STERADIAN. ) SOLID_ANGLE_UNIT ( ) );
#54107=ORIENTED_EDGE ( 'NONE', *, *, #10262, .F. ) ;
#54109=ORIENTED_EDGE ( 'NONE', *, *, #29056, .T. ) ;
#54110=SURFACE_SIDE_STYLE ('',( #39021 ) ) ;
#54111=CARTESIAN_POINT ( 'NONE',  ( 20.03990113061529144, 115.4999999999999574, -9.999999999999998224 ) ) ;
#54118=CARTESIAN_POINT ( 'NONE',  ( -3.094860106618434248, 158.7949999999999875, 9.525000000000000355 ) ) ;
#54120=ADVANCED_FACE ( 'NONE', ( #10437 ), #12480, .F. ) ;
#54121=VERTEX_POINT ( 'NONE', #31867 ) ;
#54126=CARTESIAN_POINT ( 'NONE',  ( -9.827790563157511022E-16, 136.4429263765338192, 8.025000000000000355 ) ) ;
#54134=DIRECTION ( 'NONE',  ( 0.000000000000000000, 0.000000000000000000, 1.000000000000000000 ) ) ;
#54135=CARTESIAN_POINT ( 'NONE',  ( 74.50000000000000000, 3.473944261090200865E-15, 6.500000000000000000 ) ) ;
#54138=FACE_OUTER_BOUND ( 'NONE', #9498, .T. ) ;
#54144=DIRECTION ( 'NONE',  ( 1.000000000000000000, -0.000000000000000000, -0.000000000000000000 ) ) ;
#54145=FILL_AREA_STYLE_COLOUR ( '', #1053 ) ;
#54146=EDGE_LOOP ( 'NONE', ( #61559, #27404, #45980, #22538 ) ) ;
#54147=MECHANICAL_DESIGN_GEOMETRIC_PRESENTATION_REPRESENTATION('',(#21615),#35071);
#54149=CARTESIAN_POINT ( 'NONE',  ( -45.07457192895288500, 8.173863537799691770, 3.593626512517976934 ) ) ;
#54153=ORIENTED_EDGE ( 'NONE', *, *, #33980, .T. ) ;
#54155=EDGE_CURVE ( 'NONE', #13586, #11926, #28218, .T. ) ;
#54156=FILL_AREA_STYLE_COLOUR ( '', #62105 ) ;
#54161=DIRECTION ( 'NONE',  ( -0.000000000000000000, 1.000000000000000000, -0.000000000000000000 ) ) ;
#54163=( GEOMETRIC_REPRESENTATION_CONTEXT ( 3 ) GLOBAL_UNCERTAINTY_ASSIGNED_CONTEXT ( ( #29157 ) ) GLOBAL_UNIT_ASSIGNED_CONTEXT ( ( #64529, #54301, #38172 ) ) REPRESENTATION_CONTEXT ( 'NONE', 'WORKASPACE' ) );
#54165=CARTESIAN_POINT ( 'NONE',  ( -23.71231517720798010, 112.9999999999999858, 7.500000000000000000 ) ) ;
#54173=CARTESIAN_POINT ( 'NONE',  ( 8.102448949553181734, 112.5049999999999670, 5.886773742842750679 ) ) ;
#54175=STYLED_ITEM ( 'NONE', ( #45382 ), #18831 ) ;
#54176=SURFACE_STYLE_USAGE ( .BOTH. , #32363 ) ;
#54179=DIRECTION ( 'NONE',  ( -0.000000000000000000, 1.000000000000000000, 0.000000000000000000 ) ) ;
#54184=AXIS2_PLACEMENT_3D ( 'NONE', #43480, #37849, #60284 ) ;
#54185=DIRECTION ( 'NONE',  ( -0.000000000000000000, 1.000000000000000000, -0.000000000000000000 ) ) ;
#54190=CARTESIAN_POINT ( 'NONE',  ( 60.00000000000000000, 1.797044900979284448E-15, -6.500000000000000000 ) ) ;
#54198=FILL_AREA_STYLE_COLOUR ( '', #69044 ) ;
#54202=AXIS2_PLACEMENT_3D ( 'NONE', #57596, #25230, #37220 ) ;
#54204=FACE_BOUND ( 'NONE', #2316, .T. ) ;
#54207=TOROIDAL_SURFACE ( 'NONE', #30602, 1.000000000000000000, 0.5000000000000000000 ) ;
#54209=CARTESIAN_POINT ( 'NONE',  ( -8.102448949553181734, 128.4950000000000045, 5.886773742842747126 ) ) ;
#54214=CARTESIAN_POINT ( 'NONE',  ( 3.094860106618431583, 133.2049999999999841, 9.525000000000000355 ) ) ;
#54218=ORIENTED_EDGE ( 'NONE', *, *, #28814, .T. ) ;
#54219=CARTESIAN_POINT ( 'NONE',  ( -1.166476076187854022E-15, 145.0549999999999784, 9.525000000000000355 ) ) ;
#54224=DIRECTION ( 'NONE',  ( 0.000000000000000000, 0.000000000000000000, 1.000000000000000000 ) ) ;
#54225=EDGE_LOOP ( 'NONE', ( #56299, #24381, #7130, #5923 ) ) ;
#54226=DIRECTION ( 'NONE',  ( 1.224646799147353207E-16, 1.000000000000000000, -0.000000000000000000 ) ) ;
#54228=ORIENTED_EDGE ( 'NONE', *, *, #18695, .T. ) ;
#54229=LINE ( 'NONE', #21536, #38529 ) ;
#54232=FILL_AREA_STYLE_COLOUR ( '', #65598 ) ;
#54237=FILL_AREA_STYLE ('',( #20865 ) ) ;
#54240=ORIENTED_EDGE ( 'NONE', *, *, #48996, .T. ) ;
#54242=CARTESIAN_POINT ( 'NONE',  ( 6.826472737025119919, 144.0070736234661126, 4.959722759717908325 ) ) ;
#54243=FILL_AREA_STYLE ('',( #32802 ) ) ;
#54249=( NAMED_UNIT ( * ) PLANE_ANGLE_UNIT ( ) SI_UNIT ( $, .RADIAN. ) );
#54252=CARTESIAN_POINT ( 'NONE',  ( -5.598654528085808657, 125.6449999999999818, 7.705886871421373741 ) ) ;
#54253=CIRCLE ( 'NONE', #8235, 1.000000000000000888 ) ;
#54257=VECTOR ( 'NONE', #24201, 1000.000000000000000 ) ;
#54258=CARTESIAN_POINT ( 'NONE',  ( 45.44163888576682098, 10.14721296192227129, 3.260160134650226027 ) ) ;
#54263=CIRCLE ( 'NONE', #64419, 0.4999999999999994449 ) ;
#54264=CARTESIAN_POINT ( 'NONE',  ( -23.71231517720798010, 112.9999999999999858, -7.000000000000000000 ) ) ;
#54266=ORIENTED_EDGE ( 'NONE', *, *, #11100, .F. ) ;
#54267=SURFACE_STYLE_USAGE ( .BOTH. , #65526 ) ;
#54271=EDGE_CURVE ( 'NONE', #35810, #12948, #2324, .T. ) ;
#54273=CARTESIAN_POINT ( 'NONE',  ( -45.50000000000000000, 7.768687147774684831, 6.500000000000000000 ) ) ;
#54277=FILL_AREA_STYLE_COLOUR ( '', #33770 ) ;
#54286=( NAMED_UNIT ( * ) PLANE_ANGLE_UNIT ( ) SI_UNIT ( $, .RADIAN. ) );
#54287=STYLED_ITEM ( 'NONE', ( #35039 ), #47845 ) ;
#54288=AXIS2_PLACEMENT_3D ( 'NONE', #61701, #46652, #19149 ) ;
#54290=CARTESIAN_POINT ( 'NONE',  ( 2.607480562269076430, 156.9070736234661467, -8.025000000000000355 ) ) ;
#54298=CARTESIAN_POINT ( 'NONE',  ( 12.34222745343792127, 114.9999999999999574, 10.18181818181818166 ) ) ;
#54299=DIRECTION ( 'NONE',  ( 1.000000000000000000, 0.000000000000000000, -0.000000000000000000 ) ) ;
#54300=EDGE_CURVE ( 'NONE', #46307, #45388, #18166, .T. ) ;
#54301=( NAMED_UNIT ( * ) PLANE_ANGLE_UNIT ( ) SI_UNIT ( $, .RADIAN. ) );
#54306=ORIENTED_EDGE ( 'NONE', *, *, #9040, .F. ) ;
#54308=CARTESIAN_POINT ( 'NONE',  ( -45.00000000000000000, 9.482577857128609011, -6.485016072424587108 ) ) ;
#54309=VERTEX_POINT ( 'NONE', #29723 ) ;
#54312=MECHANICAL_DESIGN_GEOMETRIC_PRESENTATION_REPRESENTATION('',(#46546),#390);
#54314=DIRECTION ( 'NONE',  ( -0.000000000000000000, -0.000000000000000000, -1.000000000000000000 ) ) ;
#54315=ADVANCED_FACE ( 'NONE', ( #14583 ), #51516, .F. ) ;
#54317=ORIENTED_EDGE ( 'NONE', *, *, #13220, .F. ) ;
#54324=AXIS2_PLACEMENT_3D ( 'NONE', #41894, #63312, #46124 ) ;
#54326=CARTESIAN_POINT ( 'NONE',  ( -5.598654528085806881, 136.7449999999999761, -7.705886871421374629 ) ) ;
#54330=DIRECTION ( 'NONE',  ( 1.000000000000000000, 0.000000000000000000, 0.000000000000000000 ) ) ;
#54331=ORIENTED_EDGE ( 'NONE', *, *, #17803, .T. ) ;
#54333=DIRECTION ( 'NONE',  ( 1.000000000000000000, 0.000000000000000000, 0.000000000000000000 ) ) ;
#54334=CARTESIAN_POINT ( 'NONE',  ( -34.99999999999992895, 112.9999999999999858, -7.000000000000000000 ) ) ;
#54338=CARTESIAN_POINT ( 'NONE',  ( -72.00000000000000000, 13.41640786499872284, 9.500000000000000000 ) ) ;
#54341=STYLED_ITEM ( 'NONE', ( #37570 ), #48335 ) ;
#54344=CARTESIAN_POINT ( 'NONE',  ( 44.82448674805845457, 10.57670410873387823, -3.609649266065385387 ) ) ;
#54345=AXIS2_PLACEMENT_3D ( 'NONE', #12021, #33479, #16640 ) ;
#54347=UNCERTAINTY_MEASURE_WITH_UNIT (LENGTH_MEASURE( 1.000000000000000082E-05 ), #13982, 'distance_accuracy_value', 'NONE');
#54349=SURFACE_SIDE_STYLE ('',( #11085 ) ) ;
#54353=FACE_OUTER_BOUND ( 'NONE', #6980, .T. ) ;
#54354=SURFACE_SIDE_STYLE ('',( #32922 ) ) ;
#54355=FACE_OUTER_BOUND ( 'NONE', #45443, .T. ) ;
#54360=TOROIDAL_SURFACE ( 'NONE', #63362, 29.50000000000000000, 0.5000000000000000000 ) ;
#54361=CARTESIAN_POINT ( 'NONE',  ( -69.99999999999998579, 50.00000000000000000, -6.999999999999988454 ) ) ;
#54367=( GEOMETRIC_REPRESENTATION_CONTEXT ( 3 ) GLOBAL_UNCERTAINTY_ASSIGNED_CONTEXT ( ( #19874 ) ) GLOBAL_UNIT_ASSIGNED_CONTEXT ( ( #37048, #10286, #53203 ) ) REPRESENTATION_CONTEXT ( 'NONE', 'WORKASPACE' ) );
#54368=CARTESIAN_POINT ( 'NONE',  ( 6.826472737025119919, 111.0070736234661553, 4.959722759717908325 ) ) ;
#54370=DIRECTION ( 'NONE',  ( 0.000000000000000000, -1.000000000000000000, 1.301042606982604216E-14 ) ) ;
#54381=CARTESIAN_POINT ( 'NONE',  ( 7.632228543268607446, 134.0429263765338135, 2.479861379858954606 ) ) ;
#54383=ORIENTED_EDGE ( 'NONE', *, *, #58011, .T. ) ;
#54385=DIRECTION ( 'NONE',  ( -0.000000000000000000, -0.000000000000000000, -1.000000000000000000 ) ) ;
#54389=UNCERTAINTY_MEASURE_WITH_UNIT (LENGTH_MEASURE( 1.000000000000000082E-05 ), #3847, 'distance_accuracy_value', 'NONE');
#54392=( NAMED_UNIT ( * ) SI_UNIT ( $, .STERADIAN. ) SOLID_ANGLE_UNIT ( ) );
#54393=ADVANCED_FACE ( 'NONE', ( #29562 ), #45779, .T. ) ;
#54396=VERTEX_POINT ( 'NONE', #24609 ) ;
#54397=EDGE_CURVE ( 'NONE', #37946, #65858, #14415, .T. ) ;
#54401=FACE_OUTER_BOUND ( 'NONE', #1961, .T. ) ;
#54402=CIRCLE ( 'NONE', #16298, 8.000000000000000000 ) ;
#54403=SURFACE_STYLE_FILL_AREA ( #37940 ) ;
#54409=CARTESIAN_POINT ( 'NONE',  ( -7.789749869348518985, 153.4012064374781517, -3.257487185497862203 ) ) ;
#54411=FACE_BOUND ( 'NONE', #10135, .T. ) ;
#54413=CARTESIAN_POINT ( 'NONE',  ( 74.99999999999998579, 119.9999999999997584, 9.500000000000000000 ) ) ;
#54414=EDGE_LOOP ( 'NONE', ( #57509, #54107, #69449, #190 ) ) ;
#54423=DIRECTION ( 'NONE',  ( -1.000000000000000000, 0.000000000000000000, 0.000000000000000000 ) ) ;
#54424=CARTESIAN_POINT ( 'NONE',  ( -8.437984349512095861, 150.6929263765338192, -5.166775262442723748E-16 ) ) ;
#54430=CARTESIAN_POINT ( 'NONE',  ( -3.094860106618432471, 134.7050000000000125, -9.525000000000000355 ) ) ;
#54439=ORIENTED_EDGE ( 'NONE', *, *, #46754, .F. ) ;
#54440=DIRECTION ( 'NONE',  ( 0.000000000000000000, 0.000000000000000000, 1.000000000000000000 ) ) ;
#54444=CARTESIAN_POINT ( 'NONE',  ( 24.21231517720798010, 112.9999999999999858, -7.500000000000000000 ) ) ;
#54446=CARTESIAN_POINT ( 'NONE',  ( -44.99999999999998579, 119.9999999999999716, 10.00000000000000000 ) ) ;
#54447=CARTESIAN_POINT ( 'NONE',  ( 44.50000000000000000, 10.36037961002804408, 3.500000000000000000 ) ) ;
#54449=EDGE_LOOP ( 'NONE', ( #3493, #42089, #32117, #36144 ) ) ;
#54453=PRESENTATION_STYLE_ASSIGNMENT (( #59364 ) ) ;
#54454=( NAMED_UNIT ( * ) SI_UNIT ( $, .STERADIAN. ) SOLID_ANGLE_UNIT ( ) );
#54462=DIRECTION ( 'NONE',  ( -0.000000000000000000, 0.000000000000000000, -1.000000000000000000 ) ) ;
#54464=ORIENTED_EDGE ( 'NONE', *, *, #58361, .F. ) ;
#54465=CYLINDRICAL_SURFACE ( 'NONE', #22031, 0.5000000000000004441 ) ;
#54470=VERTEX_POINT ( 'NONE', #41531 ) ;
#54474=( LENGTH_UNIT ( ) NAMED_UNIT ( * ) SI_UNIT ( .MILLI., .METRE. ) );
#54475=ORIENTED_EDGE ( 'NONE', *, *, #24503, .T. ) ;
#54476=CARTESIAN_POINT ( 'NONE',  ( 4.716976649647099507, 131.6429263765338362, -6.492361379858953008 ) ) ;
#54478=DIRECTION ( 'NONE',  ( 0.000000000000000000, 0.000000000000000000, 1.000000000000000000 ) ) ;
#54482=EDGE_LOOP ( 'NONE', ( #61478, #51342, #6284 ) ) ;
#54484=STYLED_ITEM ( 'NONE', ( #2684 ), #49191 ) ;
#54486=DIRECTION ( 'NONE',  ( 0.000000000000000000, 0.000000000000000000, 1.000000000000000000 ) ) ;
#54488=AXIS2_PLACEMENT_3D ( 'NONE', #43202, #36531, #34925 ) ;
#54490=FACE_OUTER_BOUND ( 'NONE', #40002, .T. ) ;
#54491=UNCERTAINTY_MEASURE_WITH_UNIT (LENGTH_MEASURE( 1.000000000000000082E-05 ), #15115, 'distance_accuracy_value', 'NONE');
#54493=CARTESIAN_POINT ( 'NONE',  ( -2.607480562269032909, 116.4070736234661609, 8.025000000000032330 ) ) ;
#54495=( LENGTH_UNIT ( ) NAMED_UNIT ( * ) SI_UNIT ( .MILLI., .METRE. ) );
#54497=VERTEX_POINT ( 'NONE', #69292 ) ;
#54501=( GEOMETRIC_REPRESENTATION_CONTEXT ( 3 ) GLOBAL_UNCERTAINTY_ASSIGNED_CONTEXT ( ( #19351 ) ) GLOBAL_UNIT_ASSIGNED_CONTEXT ( ( #59201, #20908, #27184 ) ) REPRESENTATION_CONTEXT ( 'NONE', 'WORKASPACE' ) );
#54502=EDGE_LOOP ( 'NONE', ( #9886, #47286, #23351, #22855 ) ) ;
#54503=CARTESIAN_POINT ( 'NONE',  ( -45.50000000000000000, 99.99999999999992895, -10.00000000000000000 ) ) ;
#54506=LINE ( 'NONE', #64381, #43695 ) ;
#54511=ORIENTED_EDGE ( 'NONE', *, *, #17806, .F. ) ;
#54516=CARTESIAN_POINT ( 'NONE',  ( -23.71231517720798010, 112.9999999999999858, -9.500000000000000000 ) ) ;
#54519=CARTESIAN_POINT ( 'NONE',  ( 3.094860106618431583, 156.0949999999999989, 9.525000000000000355 ) ) ;
#54521=FACE_OUTER_BOUND ( 'NONE', #42561, .T. ) ;
#54522=CARTESIAN_POINT ( 'NONE',  ( 0.4882456337924178658, 112.0289864169386789, -8.025000000000002132 ) ) ;
#54523=CARTESIAN_POINT ( 'NONE',  ( 9.827790563157511022E-16, 87.30187232391182306, -8.025000000000000355 ) ) ;
#54527=ADVANCED_FACE ( 'NONE', ( #57694 ), #37358, .F. ) ;
#54532=PRESENTATION_STYLE_ASSIGNMENT (( #37731 ) ) ;
#54533=AXIS2_PLACEMENT_3D ( 'NONE', #69499, #21296, #32919 ) ;
#54540=DIRECTION ( 'NONE',  ( 0.000000000000000000, 0.000000000000000000, 1.000000000000000000 ) ) ;
#54541=ADVANCED_FACE ( 'NONE', ( #62947 ), #42923, .F. ) ;
#54548=ADVANCED_FACE ( 'NONE', ( #255 ), #7341, .T. ) ;
#54549=AXIS2_PLACEMENT_3D ( 'NONE', #28132, #60181, #11991 ) ;
#54551=ORIENTED_EDGE ( 'NONE', *, *, #38007, .T. ) ;
#54552=DIRECTION ( 'NONE',  ( -0.000000000000000000, -1.000000000000000000, -0.000000000000000000 ) ) ;
#54554=MECHANICAL_DESIGN_GEOMETRIC_PRESENTATION_REPRESENTATION('',(#38890),#52386);
#54556=CARTESIAN_POINT ( 'NONE',  ( -5.598654528085806881, 130.7450000000000045, -7.705886871421374629 ) ) ;
#54557=SURFACE_SIDE_STYLE ('',( #38778 ) ) ;
#54560=CARTESIAN_POINT ( 'NONE',  ( 8.102448949553179958, 133.5049999999999955, 5.886773742842750679 ) ) ;
#54563=AXIS2_PLACEMENT_3D ( 'NONE', #69089, #69424, #5047 ) ;
#54565=CARTESIAN_POINT ( 'NONE',  ( -40.82744559481908908, 108.1269596360033347, -3.302666768370059902 ) ) ;
#54566=EDGE_LOOP ( 'NONE', ( #45734, #39156, #56942, #36706 ) ) ;
#54567=CARTESIAN_POINT ( 'NONE',  ( -1.166476076187854022E-15, 154.0550000000000068, 9.525000000000000355 ) ) ;
#54569=UNCERTAINTY_MEASURE_WITH_UNIT (LENGTH_MEASURE( 1.000000000000000082E-05 ), #7356, 'distance_accuracy_value', 'NONE');
#54573=( NAMED_UNIT ( * ) SI_UNIT ( $, .STERADIAN. ) SOLID_ANGLE_UNIT ( ) );
#54577=DIRECTION ( 'NONE',  ( 1.000000000000000000, 0.000000000000000000, 0.000000000000000000 ) ) ;
#54579=ORIENTED_EDGE ( 'NONE', *, *, #26889, .F. ) ;
#54581=UNCERTAINTY_MEASURE_WITH_UNIT (LENGTH_MEASURE( 1.000000000000000082E-05 ), #12438, 'distance_accuracy_value', 'NONE');
#54582=DIRECTION ( 'NONE',  ( -0.000000000000000000, -0.000000000000000000, -1.000000000000000000 ) ) ;
#54584=DIRECTION ( 'NONE',  ( 0.000000000000000000, 0.000000000000000000, -1.000000000000000000 ) ) ;
#54586=ORIENTED_EDGE ( 'NONE', *, *, #44776, .T. ) ;
#54587=CARTESIAN_POINT ( 'NONE',  ( -45.07463294676507815, 8.173953816254709182, -3.593564820753269107 ) ) ;
#54592=DIRECTION ( 'NONE',  ( 0.000000000000000000, 0.000000000000000000, 1.000000000000000000 ) ) ;
#54593=AXIS2_PLACEMENT_3D ( 'NONE', #49385, #64854, #26840 ) ;
#54595=CARTESIAN_POINT ( 'NONE',  ( -15.98999599679679839, 118.4999999999999716, -10.00000000000000000 ) ) ;
#54597=CARTESIAN_POINT ( 'NONE',  ( -75.00000000000000000, 8.745397170020957844, -6.877347455809927013 ) ) ;
#54599=( NAMED_UNIT ( * ) SI_UNIT ( $, .STERADIAN. ) SOLID_ANGLE_UNIT ( ) );
#54600=SURFACE_SIDE_STYLE ('',( #32438 ) ) ;
#54604=CARTESIAN_POINT ( 'NONE',  ( -10.01517768586949231, 131.1949999999999363, -6.132527647946036459E-16 ) ) ;
#54611=CARTESIAN_POINT ( 'NONE',  ( 47.50000000000000000, 14.49137674618942562, -9.500000000000000000 ) ) ;
#54613=EDGE_LOOP ( 'NONE', ( #39515, #4539 ) ) ;
#54620=EDGE_CURVE ( 'NONE', #46203, #30560, #21788, .T. ) ;
#54625=COLOUR_RGB ( '', 0.66274510, 0.83137255, 0.94901961) ;
#54630=ORIENTED_EDGE ( 'NONE', *, *, #6901, .F. ) ;
#54633=FILL_AREA_STYLE_COLOUR ( '', #13884 ) ;
#54634=CIRCLE ( 'NONE', #46880, 8.999999999999994671 ) ;
#54637=DIRECTION ( 'NONE',  ( 1.000000000000000000, 0.000000000000000000, 0.000000000000000000 ) ) ;
#54638=CARTESIAN_POINT ( 'NONE',  ( -9.827790563157511022E-16, 155.5570736234661524, 8.025000000000000355 ) ) ;
#54640=CARTESIAN_POINT ( 'NONE',  ( 7.632228543268607446, 137.0429263765338135, 2.479861379858954606 ) ) ;
#54642=UNCERTAINTY_MEASURE_WITH_UNIT (LENGTH_MEASURE( 1.000000000000000082E-05 ), #57357, 'distance_accuracy_value', 'NONE');
#54644=ADVANCED_FACE ( 'NONE', ( #73 ), #55314, .F. ) ;
#54646=DIRECTION ( 'NONE',  ( 0.000000000000000000, 0.000000000000000000, -1.000000000000000000 ) ) ;
#54647=FILL_AREA_STYLE ('',( #58903 ) ) ;
#54648=( LENGTH_UNIT ( ) NAMED_UNIT ( * ) SI_UNIT ( .MILLI., .METRE. ) );
#54650=ORIENTED_EDGE ( 'NONE', *, *, #42771, .F. ) ;
#54655=CARTESIAN_POINT ( 'NONE',  ( -45.89386150022815514, 9.348154474468870490, -6.165151716360228740 ) ) ;
#54657=FILL_AREA_STYLE ('',( #5759 ) ) ;
#54659=ORIENTED_EDGE ( 'NONE', *, *, #46595, .F. ) ;
#54660=STYLED_ITEM ( 'NONE', ( #53948 ), #508 ) ;
#54661=CARTESIAN_POINT ( 'NONE',  ( 45.00000000000000000, 10.69371294336137979, -5.999999999999999112 ) ) ;
#54662=CARTESIAN_POINT ( 'NONE',  ( -75.00000000000000000, 7.966012280117817923, 7.000000003579910590 ) ) ;
#54664=ORIENTED_EDGE ( 'NONE', *, *, #8673, .F. ) ;
#54666=LINE ( 'NONE', #6468, #52992 ) ;
#54667=( NAMED_UNIT ( * ) SI_UNIT ( $, .STERADIAN. ) SOLID_ANGLE_UNIT ( ) );
#54668=SURFACE_STYLE_USAGE ( .BOTH. , #48066 ) ;
#54672=CARTESIAN_POINT ( 'NONE',  ( -10.01517768586949408, 137.1949999999999363, -6.132527647946036459E-16 ) ) ;
#54674=FILL_AREA_STYLE_COLOUR ( '', #47125 ) ;
#54676=FACE_OUTER_BOUND ( 'NONE', #44312, .T. ) ;
#54680=SURFACE_STYLE_USAGE ( .BOTH. , #28636 ) ;
#54690=CIRCLE ( 'NONE', #708, 23.00000000000000355 ) ;
#54691=DIRECTION ( 'NONE',  ( -0.4468085106382997385, 0.000000000000000000, 0.8946296187927071930 ) ) ;
#54692=( LENGTH_UNIT ( ) NAMED_UNIT ( * ) SI_UNIT ( .MILLI., .METRE. ) );
#54693=EDGE_CURVE ( 'NONE', #38966, #62390, #56425, .T. ) ;
#54698=CARTESIAN_POINT ( 'NONE',  ( 60.00000000000000000, 1.797044900979284448E-15, 10.50000000000000000 ) ) ;
#54699=DIRECTION ( 'NONE',  ( 1.000000000000000000, 3.469446951953611033E-15, 0.000000000000000000 ) ) ;
#54704=DIRECTION ( 'NONE',  ( -1.000000000000000000, 0.000000000000000000, -0.000000000000000000 ) ) ;
#54707=CARTESIAN_POINT ( 'NONE',  ( -4.716976649647097730, 127.3570736234661496, -6.492361379858953896 ) ) ;
#54708=CARTESIAN_POINT ( 'NONE',  ( 75.00000000000000000, 20.36037960999352237, -6.130923279862114939 ) ) ;
#54713=EDGE_CURVE ( 'NONE', #19997, #44738, #13755, .T. ) ;
#54714=VERTEX_POINT ( 'NONE', #28595 ) ;
#54715=CARTESIAN_POINT ( 'NONE',  ( 24.21231517720798010, 113.4999999999999858, -7.000000000000000000 ) ) ;
#54716=TOROIDAL_SURFACE ( 'NONE', #63717, 1.000000000000000000, 0.5000000000000000000 ) ;
#54718=CARTESIAN_POINT ( 'NONE',  ( 6.826472737025121695, 134.4929263765338305, -4.959722759717905660 ) ) ;
#54723=( LENGTH_UNIT ( ) NAMED_UNIT ( * ) SI_UNIT ( .MILLI., .METRE. ) );
#54726=( GEOMETRIC_REPRESENTATION_CONTEXT ( 3 ) GLOBAL_UNCERTAINTY_ASSIGNED_CONTEXT ( ( #4410 ) ) GLOBAL_UNIT_ASSIGNED_CONTEXT ( ( #44545, #43511, #59616 ) ) REPRESENTATION_CONTEXT ( 'NONE', 'WORKASPACE' ) );
#54727=AXIS2_PLACEMENT_3D ( 'NONE', #55158, #6616, #17897 ) ;
#54729=EDGE_LOOP ( 'NONE', ( #62507, #34511, #4285, #14006 ) ) ;
#54731=VERTEX_POINT ( 'NONE', #1114 ) ;
#54733=FILL_AREA_STYLE_COLOUR ( '', #18380 ) ;
#54736=CARTESIAN_POINT ( 'NONE',  ( -45.89905495956738690, 9.405628579031729330, 3.000000000000000000 ) ) ;
#54738=SURFACE_STYLE_USAGE ( .BOTH. , #32261 ) ;
#54750=VERTEX_POINT ( 'NONE', #28933 ) ;
#54751=FACE_OUTER_BOUND ( 'NONE', #39456, .T. ) ;
#54752=CARTESIAN_POINT ( 'NONE',  ( 44.82807636874886725, 9.942692122916287900, 2.999113325960788501 ) ) ;
#54754=( NAMED_UNIT ( * ) PLANE_ANGLE_UNIT ( ) SI_UNIT ( $, .RADIAN. ) );
#54758=AXIS2_PLACEMENT_3D ( 'NONE', #26626, #43235, #195 ) ;
#54760=CARTESIAN_POINT ( 'NONE',  ( -1.166476076187854022E-15, 136.0549999999999784, 9.525000000000000355 ) ) ;
#54761=EDGE_CURVE ( 'NONE', #35924, #5028, #55343, .T. ) ;
#54765=ADVANCED_FACE ( 'NONE', ( #66239 ), #68806, .T. ) ;
#54769=DIRECTION ( 'NONE',  ( 0.000000000000000000, 0.000000000000000000, 1.000000000000000000 ) ) ;
#54772=COLOUR_RGB ( '', 0.09019608, 0.27058824, 0.51372549) ;
#54774=EDGE_CURVE ( 'NONE', #60684, #17419, #19443, .T. ) ;
#54777=DIRECTION ( 'NONE',  ( -0.000000000000000000, -0.000000000000000000, -1.000000000000000000 ) ) ;
#54778=ORIENTED_EDGE ( 'NONE', *, *, #31682, .T. ) ;
#54779=ORIENTED_EDGE ( 'NONE', *, *, #62499, .F. ) ;
#54780=CARTESIAN_POINT ( 'NONE',  ( -48.50000000000000000, 14.49137674618942562, -7.000000000000000000 ) ) ;
#54783=DIRECTION ( 'NONE',  ( 0.000000000000000000, 0.000000000000000000, 1.000000000000000000 ) ) ;
#54784=DIRECTION ( 'NONE',  ( 1.000000000000000000, 0.000000000000000000, -0.000000000000000000 ) ) ;
#54785=CARTESIAN_POINT ( 'NONE',  ( -21.02379604162863913, 154.9999999999999716, -10.50000000000000000 ) ) ;
#54791=( NAMED_UNIT ( * ) PLANE_ANGLE_UNIT ( ) SI_UNIT ( $, .RADIAN. ) );
#54797=CARTESIAN_POINT ( 'NONE',  ( -5.598654528085806881, 157.7450000000000045, -7.705886871421374629 ) ) ;
#54799=( BOUNDED_CURVE ( )  B_SPLINE_CURVE ( 2, ( #42922, #63966, #16172, #15812, #41873, #37295, #10863, #3818, #46828, #47154, #68231 ),
 .UNSPECIFIED., .F., .F. ) 
 B_SPLINE_CURVE_WITH_KNOTS ( ( 3, 2, 2, 2, 2, 3 ),
 ( 0.3823529411764706176, 0.3882352941176471228, 0.3941176470588235725, 0.4000000000000001332, 0.4058823529411765829, 0.4117647058823530326 ),
 .UNSPECIFIED. ) 
 CURVE ( )  GEOMETRIC_REPRESENTATION_ITEM ( )  RATIONAL_B_SPLINE_CURVE ( ( 0.9999999999999995559, 0.9510565162951539753, 1.000000000000000000, 0.9510565162951535312, 1.000000000000000000, 0.9510565162951535312, 1.000000000000000000, 0.9510565162951535312, 1.000000000000000000, 0.9510565162951526430, 1.000000000000000888 ) ) 
 REPRESENTATION_ITEM ( '' )  );
#54801=CARTESIAN_POINT ( 'NONE',  ( -74.14894111157977363, 9.184645374706621013, -6.276135203588958156 ) ) ;
#54803=LINE ( 'NONE', #6987, #31865 ) ;
#54805=CARTESIAN_POINT ( 'NONE',  ( 6.826472737025121695, 131.4929263765337737, -4.959722759717905660 ) ) ;
#54808=COLOUR_RGB ( '', 0.72549020, 0.75294118, 0.79215686) ;
#54810=DIRECTION ( 'NONE',  ( -0.000000000000000000, -0.000000000000000000, -1.000000000000000000 ) ) ;
#54817=( GEOMETRIC_REPRESENTATION_CONTEXT ( 3 ) GLOBAL_UNCERTAINTY_ASSIGNED_CONTEXT ( ( #5954 ) ) GLOBAL_UNIT_ASSIGNED_CONTEXT ( ( #24085, #45909, #23732 ) ) REPRESENTATION_CONTEXT ( 'NONE', 'WORKASPACE' ) );
#54819=CARTESIAN_POINT ( 'NONE',  ( -60.00000000000000000, -2.024042244987997205E-14, 6.999999999999999112 ) ) ;
#54820=( NAMED_UNIT ( * ) SI_UNIT ( $, .STERADIAN. ) SOLID_ANGLE_UNIT ( ) );
#54821=ORIENTED_EDGE ( 'NONE', *, *, #68314, .F. ) ;
#54823=CARTESIAN_POINT ( 'NONE',  ( 45.00000000000000000, 99.99999999999992895, 9.500000000000000000 ) ) ;
#54824=CARTESIAN_POINT ( 'NONE',  ( -45.00000000000000000, 9.680388875877742549, -6.198302543666470932 ) ) ;
#54828=CARTESIAN_POINT ( 'NONE',  ( -45.90207868045609985, 9.410163051192631301, 3.203717355333229655 ) ) ;
#54832=LINE ( 'NONE', #952, #56159 ) ;
#54833=PRESENTATION_STYLE_ASSIGNMENT (( #38731 ) ) ;
#54834=SURFACE_STYLE_USAGE ( .BOTH. , #12979 ) ;
#54843=DIRECTION ( 'NONE',  ( -0.000000000000000000, -0.000000000000000000, -1.000000000000000000 ) ) ;
#54846=CARTESIAN_POINT ( 'NONE',  ( 5.598654528085809545, 154.1449999999999818, -7.705886871421373741 ) ) ;
#54848=CARTESIAN_POINT ( 'NONE',  ( -6.826472737025120807, 112.5070736234661410, -4.959722759717907437 ) ) ;
#54849=ADVANCED_FACE ( 'NONE', ( #24703 ), #34934, .F. ) ;
#54851=LINE ( 'NONE', #54523, #11272 ) ;
#54855=CARTESIAN_POINT ( 'NONE',  ( -20.71231517720797655, 149.4999999999999716, -10.00000000000000000 ) ) ;
#54856=CARTESIAN_POINT ( 'NONE',  ( 14.98999599679679662, 117.9999999999999716, -10.00000000000000000 ) ) ;
#54862=COLOUR_RGB ( '', 0.72549020, 0.75294118, 0.79215686) ;
#54865=ORIENTED_EDGE ( 'NONE', *, *, #49641, .T. ) ;
#54869=CARTESIAN_POINT ( 'NONE',  ( -79.99999999999998579, 50.00000000000000000, -11.50000000000001066 ) ) ;
#54870=COLOUR_RGB ( '', 0.09019608, 0.27058824, 0.51372549) ;
#54871=ADVANCED_FACE ( 'NONE', ( #14892 ), #36293, .T. ) ;
#54872=CARTESIAN_POINT ( 'NONE',  ( 44.99999999999977973, 149.9999999999999716, -9.500000000000000000 ) ) ;
#54873=DIRECTION ( 'NONE',  ( -0.000000000000000000, -0.000000000000000000, -1.000000000000000000 ) ) ;
#54878=ORIENTED_EDGE ( 'NONE', *, *, #6756, .T. ) ;
#54881=ORIENTED_EDGE ( 'NONE', *, *, #10877, .F. ) ;
#54883=CARTESIAN_POINT ( 'NONE',  ( 9.058813317711338797, 132.8449999999999989, -2.943386871421372675 ) ) ;
#54885=CARTESIAN_POINT ( 'NONE',  ( -61.49999999999998579, 50.00000000000000000, -10.00000000000000000 ) ) ;
#54886=CARTESIAN_POINT ( 'NONE',  ( -10.01517768586949408, 135.3049999999999784, -6.132527647946036459E-16 ) ) ;
#54890=CARTESIAN_POINT ( 'NONE',  ( 3.094860106618431583, 160.2050000000000125, 9.525000000000000355 ) ) ;
#54891=CARTESIAN_POINT ( 'NONE',  ( 60.00000000000000000, 1.797044900979284448E-15, -7.000000000000000888 ) ) ;
#54893=VECTOR ( 'NONE', #66006, 1000.000000000000000 ) ;
#54895=STYLED_ITEM ( 'NONE', ( #33664 ), #20075 ) ;
#54896=FILL_AREA_STYLE ('',( #43721 ) ) ;
#54903=( NAMED_UNIT ( * ) PLANE_ANGLE_UNIT ( ) SI_UNIT ( $, .RADIAN. ) );
#54906=CARTESIAN_POINT ( 'NONE',  ( -24.21231517720798010, 113.4999999999999858, 9.500000000000000000 ) ) ;
#54908=CARTESIAN_POINT ( 'NONE',  ( -44.99999999999999289, 9.678668534234134313, 3.511107231047464694 ) ) ;
#54910=VECTOR ( 'NONE', #49030, 1000.000000000000000 ) ;
#54911=CARTESIAN_POINT ( 'NONE',  ( -45.15332280914032737, 8.289991779376686409, -3.464680026297982440 ) ) ;
#54916=MECHANICAL_DESIGN_GEOMETRIC_PRESENTATION_REPRESENTATION('',(#51578),#21230);
#54917=( NAMED_UNIT ( * ) SI_UNIT ( $, .STERADIAN. ) SOLID_ANGLE_UNIT ( ) );
#54920=CARTESIAN_POINT ( 'NONE',  ( -74.99999999999998579, 8.340816515359708916, -6.279506003889757437 ) ) ;
#54921=ORIENTED_EDGE ( 'NONE', *, *, #53071, .F. ) ;
#54923=VECTOR ( 'NONE', #67851, 1000.000000000000000 ) ;
#54928=CARTESIAN_POINT ( 'NONE',  ( -8.102448949553181734, 125.4949999999999903, 5.886773742842747126 ) ) ;
#54931=SURFACE_SIDE_STYLE ('',( #47677 ) ) ;
#54933=EDGE_CURVE ( 'NONE', #57325, #31700, #59148, .T. ) ;
#54934=AXIS2_PLACEMENT_3D ( 'NONE', #1067, #38131, #5363 ) ;
#54941=CIRCLE ( 'NONE', #58335, 0.5000000000000004441 ) ;
#54944=CARTESIAN_POINT ( 'NONE',  ( -45.50000000000000000, -2.024042244987997205E-14, 6.999999999999999112 ) ) ;
#54947=AXIS2_PLACEMENT_3D ( 'NONE', #42409, #64504, #49056 ) ;
#54949=CARTESIAN_POINT ( 'NONE',  ( 24.21231517720798010, 113.4999999999999858, 7.000000000000000000 ) ) ;
#54952=CARTESIAN_POINT ( 'NONE',  ( 6.826472737025121695, 147.6070736234661354, -4.959722759717905660 ) ) ;
#54956=VERTEX_POINT ( 'NONE', #15941 ) ;
#54962=PRESENTATION_STYLE_ASSIGNMENT (( #53936 ) ) ;
#54963=STYLED_ITEM ( 'NONE', ( #13147 ), #14875 ) ;
#54964=CARTESIAN_POINT ( 'NONE',  ( 7.632228543268608334, 153.4570736234661581, -2.479861379858951942 ) ) ;
#54967=PRESENTATION_STYLE_ASSIGNMENT (( #43789 ) ) ;
#54970=CARTESIAN_POINT ( 'NONE',  ( 7.632228543268607446, 132.1570736234661467, 2.479861379858954606 ) ) ;
#54975=VERTEX_POINT ( 'NONE', #27478 ) ;
#54976=( LENGTH_UNIT ( ) NAMED_UNIT ( * ) SI_UNIT ( .MILLI., .METRE. ) );
#54979=AXIS2_PLACEMENT_3D ( 'NONE', #15349, #10726, #25850 ) ;
#54982=FACE_OUTER_BOUND ( 'NONE', #28430, .T. ) ;
#54983=ADVANCED_FACE ( 'NONE', ( #58822 ), #26101, .F. ) ;
#54985=CARTESIAN_POINT ( 'NONE',  ( -45.70728519569756543, 8.623151806617487480, -6.441684343570499571 ) ) ;
#54986=CIRCLE ( 'NONE', #3290, 0.5000000000000004441 ) ;
#54988=CARTESIAN_POINT ( 'NONE',  ( -1.113559396844004956, 154.5000000000000000, -9.459683423334018570 ) ) ;
#54991=VECTOR ( 'NONE', #53568, 1000.000000000000000 ) ;
#54994=ORIENTED_EDGE ( 'NONE', *, *, #13090, .T. ) ;
#54998=CARTESIAN_POINT ( 'NONE',  ( 23.21231517720797655, 118.4999999999999716, 7.000000000000000000 ) ) ;
#55002=CARTESIAN_POINT ( 'NONE',  ( -3.094860106618432471, 130.5949999999999989, -9.525000000000000355 ) ) ;
#55009=DIRECTION ( 'NONE',  ( 0.000000000000000000, 0.000000000000000000, 1.000000000000000000 ) ) ;
#55011=( NAMED_UNIT ( * ) SI_UNIT ( $, .STERADIAN. ) SOLID_ANGLE_UNIT ( ) );
#55012=EDGE_CURVE ( 'NONE', #64235, #26176, #18273, .T. ) ;
#55015=EDGE_CURVE ( 'NONE', #53321, #68848, #7762, .T. ) ;
#55016=DIRECTION ( 'NONE',  ( 0.000000000000000000, 0.000000000000000000, 1.000000000000000000 ) ) ;
#55017=CARTESIAN_POINT ( 'NONE',  ( 48.50000000000000000, 14.49137674618942206, -7.000000000000000000 ) ) ;
#55023=CARTESIAN_POINT ( 'NONE',  ( 44.45130529142733877, 9.817101763808881998, -3.473322258837261867 ) ) ;
#55025=( LENGTH_UNIT ( ) NAMED_UNIT ( * ) SI_UNIT ( .MILLI., .METRE. ) );
#55028=UNCERTAINTY_MEASURE_WITH_UNIT (LENGTH_MEASURE( 1.000000000000000082E-05 ), #32320, 'distance_accuracy_value', 'NONE');
#55030=AXIS2_PLACEMENT_3D ( 'NONE', #12638, #35146, #1340 ) ;
#55032=EDGE_CURVE ( 'NONE', #40785, #43530, #50348, .T. ) ;
#55033=DIRECTION ( 'NONE',  ( 0.000000000000000000, 0.000000000000000000, 1.000000000000000000 ) ) ;
#55036=DIRECTION ( 'NONE',  ( -0.000000000000000000, -0.000000000000000000, 1.000000000000000000 ) ) ;
#55038=( GEOMETRIC_REPRESENTATION_CONTEXT ( 3 ) GLOBAL_UNCERTAINTY_ASSIGNED_CONTEXT ( ( #18641 ) ) GLOBAL_UNIT_ASSIGNED_CONTEXT ( ( #2813, #19009, #35218 ) ) REPRESENTATION_CONTEXT ( 'NONE', 'WORKASPACE' ) );
#55043=PRESENTATION_STYLE_ASSIGNMENT (( #43524 ) ) ;
#55044=AXIS2_PLACEMENT_3D ( 'NONE', #19306, #8074, #9126 ) ;
#55047=EDGE_CURVE ( 'NONE', #31646, #63887, #27224, .T. ) ;
#55049=COLOUR_RGB ( '', 0.40784314, 0.44705882, 0.49803922) ;
#55054=ADVANCED_FACE ( 'NONE', ( #28149 ), #41919, .T. ) ;
#55055=STYLED_ITEM ( 'NONE', ( #43951 ), #34609 ) ;
#55056=CARTESIAN_POINT ( 'NONE',  ( -2.607480562269075097, 119.4070736234661467, 8.025000000000000355 ) ) ;
#55057=COLOUR_RGB ( '', 0.08235294, 0.09019608, 0.10196078) ;
#55058=CARTESIAN_POINT ( 'NONE',  ( 75.00000000000000000, 19.95407619327929183, -6.799666827783447332 ) ) ;
#55059=CIRCLE ( 'NONE', #30294, 0.5000000000000004441 ) ;
#55064=VECTOR ( 'NONE', #46823, 1000.000000000000000 ) ;
#55066=CARTESIAN_POINT ( 'NONE',  ( 34.99999999999999289, 99.99999999999997158, -10.00000000000000000 ) ) ;
#55068=EDGE_LOOP ( 'NONE', ( #7063, #38805 ) ) ;
#55071=CARTESIAN_POINT ( 'NONE',  ( -8.437984349512095861, 123.6929263765338192, -5.166775262442723748E-16 ) ) ;
#55072=( NAMED_UNIT ( * ) PLANE_ANGLE_UNIT ( ) SI_UNIT ( $, .RADIAN. ) );
#55074=DIRECTION ( 'NONE',  ( 1.000000000000000000, -1.596582957076308193E-15, 0.000000000000000000 ) ) ;
#55075=PRESENTATION_STYLE_ASSIGNMENT (( #38271 ) ) ;
#55080=ORIENTED_EDGE ( 'NONE', *, *, #1527, .F. ) ;
#55082=CARTESIAN_POINT ( 'NONE',  ( 60.00000000000000000, 1.797044900979284448E-15, -6.500000000000000000 ) ) ;
#55086=STYLED_ITEM ( 'NONE', ( #13033 ), #45407 ) ;
#55087=ADVANCED_FACE ( 'NONE', ( #23602 ), #17331, .F. ) ;
#55089=VECTOR ( 'NONE', #15535, 1000.000000000000000 ) ;
#55090=LINE ( 'NONE', #1919, #20060 ) ;
#55094=FILL_AREA_STYLE ('',( #13225 ) ) ;
#55097=ORIENTED_EDGE ( 'NONE', *, *, #18202, .T. ) ;
#55098=EDGE_CURVE ( 'NONE', #15891, #10808, #51741, .T. ) ;
#55102=AXIS2_PLACEMENT_3D ( 'NONE', #69434, #42408, #11372 ) ;
#55107=( GEOMETRIC_REPRESENTATION_CONTEXT ( 3 ) GLOBAL_UNCERTAINTY_ASSIGNED_CONTEXT ( ( #52490 ) ) GLOBAL_UNIT_ASSIGNED_CONTEXT ( ( #61780, #35072, #46730 ) ) REPRESENTATION_CONTEXT ( 'NONE', 'WORKASPACE' ) );
#55108=CARTESIAN_POINT ( 'NONE',  ( -2.607480562269116842, 151.2929263765338135, 8.024999999999970157 ) ) ;
#55114=CARTESIAN_POINT ( 'NONE',  ( 9.058813317711338797, 145.9550000000000125, -2.943386871421372675 ) ) ;
#55118=UNCERTAINTY_MEASURE_WITH_UNIT (LENGTH_MEASURE( 1.000000000000000082E-05 ), #28558, 'distance_accuracy_value', 'NONE');
#55119=AXIS2_PLACEMENT_3D ( 'NONE', #54698, #49795, #5813 ) ;
#55124=CARTESIAN_POINT ( 'NONE',  ( 0.000000000000000000, 87.30187232391182306, 8.025000000000000355 ) ) ;
#55125=( NAMED_UNIT ( * ) PLANE_ANGLE_UNIT ( ) SI_UNIT ( $, .RADIAN. ) );
#55126=VERTEX_POINT ( 'NONE', #30597 ) ;
#55127=ORIENTED_EDGE ( 'NONE', *, *, #36524, .F. ) ;
#55128=CARTESIAN_POINT ( 'NONE',  ( -74.99999999999998579, 50.00000000000000000, -12.00000000000000000 ) ) ;
#55133=FACE_OUTER_BOUND ( 'NONE', #36304, .T. ) ;
#55136=ORIENTED_EDGE ( 'NONE', *, *, #46420, .F. ) ;
#55139=EDGE_LOOP ( 'NONE', ( #12460, #49113 ) ) ;
#55144=LINE ( 'NONE', #27367, #41188 ) ;
#55146=AXIS2_PLACEMENT_3D ( 'NONE', #46464, #29175, #19682 ) ;
#55147=PRESENTATION_STYLE_ASSIGNMENT (( #38344 ) ) ;
#55153=CARTESIAN_POINT ( 'NONE',  ( -8.705293062390095926, 110.4999999999999716, -3.890206119981057142 ) ) ;
#55154=CARTESIAN_POINT ( 'NONE',  ( -21.02379604162863913, 110.4999999999999858, -10.50000000000000000 ) ) ;
#55155=CARTESIAN_POINT ( 'NONE',  ( 45.00000000000000000, 10.69371294336137801, 4.000000000000000000 ) ) ;
#55157=CARTESIAN_POINT ( 'NONE',  ( -9.827790563157511022E-16, 139.4429263765338192, 8.025000000000000355 ) ) ;
#55158=CARTESIAN_POINT ( 'NONE',  ( 45.50000000000000000, -1.469576158976824618E-14, -9.500000000000000000 ) ) ;
#55159=STYLED_ITEM ( 'NONE', ( #21497 ), #52566 ) ;
#55161=LINE ( 'NONE', #12600, #50115 ) ;
#55162=ORIENTED_EDGE ( 'NONE', *, *, #5147, .T. ) ;
#55163=AXIS2_PLACEMENT_3D ( 'NONE', #26942, #43900, #10809 ) ;
#55168=DIRECTION ( 'NONE',  ( 0.000000000000000000, 0.000000000000000000, -1.000000000000000000 ) ) ;
#55171=CARTESIAN_POINT ( 'NONE',  ( -5.598654528085808657, 122.6449999999999960, 7.705886871421373741 ) ) ;
#55173=FACE_OUTER_BOUND ( 'NONE', #2094, .T. ) ;
#55177=ORIENTED_EDGE ( 'NONE', *, *, #29248, .F. ) ;
#55178=CARTESIAN_POINT ( 'NONE',  ( -45.91547274699541958, 9.430195759334528915, 3.560059854842081872 ) ) ;
#55182=PLANE ( 'NONE',  #7865 ) ;
#55183=EDGE_CURVE ( 'NONE', #20470, #50261, #35204, .T. ) ;
#55187=B_SPLINE_CURVE_WITH_KNOTS ( 'NONE', 3,
 ( #8410, #60798, #18926, #12973, #2356, #34087, #61487, #2725, #24217, #49018 ),
 .UNSPECIFIED., .F., .F.,
 ( 4, 2, 2, 2, 4 ),
 ( 0.000000000000000000, 0.0004159702800446777042, 0.0008319405600893554084, 0.001247910840134033167, 0.001663881120178710817 ),
 .UNSPECIFIED. ) ;
#55190=SURFACE_STYLE_FILL_AREA ( #33739 ) ;
#55191=ORIENTED_EDGE ( 'NONE', *, *, #8592, .T. ) ;
#55193=MECHANICAL_DESIGN_GEOMETRIC_PRESENTATION_REPRESENTATION('',(#33852),#14811);
#55194=EDGE_CURVE ( 'NONE', #14819, #5042, #47672, .T. ) ;
#55198=CARTESIAN_POINT ( 'NONE',  ( 34.99999999999999289, 99.99999999999998579, -7.000000000000000000 ) ) ;
#55204=CARTESIAN_POINT ( 'NONE',  ( -3.094860106618432471, 122.7049999999999699, -9.525000000000000355 ) ) ;
#55206=AXIS2_PLACEMENT_3D ( 'NONE', #12221, #43282, #44646 ) ;
#55209=COLOUR_RGB ( '', 0.72549020, 0.75294118, 0.79215686) ;
#55212=STYLED_ITEM ( 'NONE', ( #49216 ), #54548 ) ;
#55213=CARTESIAN_POINT ( 'NONE',  ( 41.26950967128010461, 107.7917145016473768, -3.849034857644456409 ) ) ;
#55219=DIRECTION ( 'NONE',  ( -0.000000000000000000, 1.000000000000000000, -0.000000000000000000 ) ) ;
#55220=CONICAL_SURFACE ( 'NONE', #3517, 5.500000000000005329, 0.7853981633974579379 ) ;
#55221=DIRECTION ( 'NONE',  ( -0.000000000000000000, -0.000000000000000000, -1.000000000000000000 ) ) ;
#55225=( LENGTH_UNIT ( ) NAMED_UNIT ( * ) SI_UNIT ( .MILLI., .METRE. ) );
#55229=VECTOR ( 'NONE', #31812, 1000.000000000000000 ) ;
#55231=FILL_AREA_STYLE ('',( #13977 ) ) ;
#55235=ORIENTED_EDGE ( 'NONE', *, *, #14623, .T. ) ;
#55237=CARTESIAN_POINT ( 'NONE',  ( -34.99999999999999289, 99.99999999999998579, 4.000000000000000000 ) ) ;
#55238=ORIENTED_EDGE ( 'NONE', *, *, #18109, .T. ) ;
#55241=CARTESIAN_POINT ( 'NONE',  ( 55.65811388300842566, 13.02565835097472657, -6.500000000000000000 ) ) ;
#55242=CARTESIAN_POINT ( 'NONE',  ( 5.598654528085809545, 133.1449999999999818, -7.705886871421373741 ) ) ;
#55244=ORIENTED_EDGE ( 'NONE', *, *, #21455, .T. ) ;
#55245=MECHANICAL_DESIGN_GEOMETRIC_PRESENTATION_REPRESENTATION('',(#46309),#46411);
#55247=CARTESIAN_POINT ( 'NONE',  ( 10.01517768586949408, 127.8050000000000068, 1.839758294383810543E-15 ) ) ;
#55248=CIRCLE ( 'NONE', #13681, 7.500000000000007105 ) ;
#55252=CARTESIAN_POINT ( 'NONE',  ( 5.598654528085805993, 160.3549999999999898, 7.705886871421374629 ) ) ;
#55254=UNCERTAINTY_MEASURE_WITH_UNIT (LENGTH_MEASURE( 1.000000000000000082E-05 ), #37519, 'distance_accuracy_value', 'NONE');
#55256=CIRCLE ( 'NONE', #19299, 16.00000000000000000 ) ;
#55258=CARTESIAN_POINT ( 'NONE',  ( -14.98999599679678951, 146.9999999999999716, -10.00000000000000000 ) ) ;
#55262=ORIENTED_EDGE ( 'NONE', *, *, #23551, .T. ) ;
#55265=AXIS2_PLACEMENT_3D ( 'NONE', #12778, #63896, #44504 ) ;
#55272=SURFACE_STYLE_USAGE ( .BOTH. , #33149 ) ;
#55273=CARTESIAN_POINT ( 'NONE',  ( 44.99999999999977973, 149.9999999999999716, 10.00000000000000000 ) ) ;
#55275=EDGE_LOOP ( 'NONE', ( #47960, #66017, #34557, #37542 ) ) ;
#55278=CARTESIAN_POINT ( 'NONE',  ( -45.21668476334829734, 8.382617245700997088, -3.141643734658259302 ) ) ;
#55279=CARTESIAN_POINT ( 'NONE',  ( 48.50000000000000000, 14.49137674618942917, 7.000000000000000000 ) ) ;
#55280=STYLED_ITEM ( 'NONE', ( #67312 ), #28742 ) ;
#55282=ORIENTED_EDGE ( 'NONE', *, *, #27467, .F. ) ;
#55283=CARTESIAN_POINT ( 'NONE',  ( 71.62068965517239860, 36.41396814395972115, -7.000000000000000000 ) ) ;
#55284=VECTOR ( 'NONE', #11246, 1000.000000000000000 ) ;
#55288=EDGE_CURVE ( 'NONE', #34398, #30766, #48516, .T. ) ;
#55289=CARTESIAN_POINT ( 'NONE',  ( -74.27256294509165002, 8.702587636786763170, -6.424237564331914285 ) ) ;
#55290=ORIENTED_EDGE ( 'NONE', *, *, #65799, .T. ) ;
#55291=DIRECTION ( 'NONE',  ( -0.000000000000000000, -1.000000000000000000, -0.000000000000000000 ) ) ;
#55295=CARTESIAN_POINT ( 'NONE',  ( -9.058813317711337021, 128.0449999999999875, -2.943386871421374895 ) ) ;
#55297=AXIS2_PLACEMENT_3D ( 'NONE', #65702, #54777, #50570 ) ;
#55307=ORIENTED_EDGE ( 'NONE', *, *, #62830, .T. ) ;
#55309=ORIENTED_EDGE ( 'NONE', *, *, #31596, .F. ) ;
#55311=CARTESIAN_POINT ( 'NONE',  ( -45.90010448357104877, 9.371898184802233800, 6.142471281331792987 ) ) ;
#55314=TOROIDAL_SURFACE ( 'NONE', #14876, 14.49999999999999822, 0.5000000000000000000 ) ;
#55325=DIRECTION ( 'NONE',  ( 0.000000000000000000, 1.000000000000000000, 0.000000000000000000 ) ) ;
#55326=( LENGTH_UNIT ( ) NAMED_UNIT ( * ) SI_UNIT ( .MILLI., .METRE. ) );
#55328=CARTESIAN_POINT ( 'NONE',  ( -4.716976649647098618, 149.2570736234661695, 6.492361379858953008 ) ) ;
#55329=AXIS2_PLACEMENT_3D ( 'NONE', #32797, #54592, #6398 ) ;
#55331=FILL_AREA_STYLE_COLOUR ( '', #63104 ) ;
#55332=STYLED_ITEM ( 'NONE', ( #24439 ), #310 ) ;
#55334=DIRECTION ( 'NONE',  ( 0.000000000000000000, 0.000000000000000000, -1.000000000000000000 ) ) ;
#55335=CARTESIAN_POINT ( 'NONE',  ( 10.01517768586949231, 130.8049999999999784, 1.839758294383810543E-15 ) ) ;
#55336=UNCERTAINTY_MEASURE_WITH_UNIT (LENGTH_MEASURE( 1.000000000000000082E-05 ), #51582, 'distance_accuracy_value', 'NONE');
#55338=DIRECTION ( 'NONE',  ( -0.000000000000000000, -1.000000000000000000, -0.000000000000000000 ) ) ;
#55339=ADVANCED_FACE ( 'NONE', ( #52786 ), #9872, .F. ) ;
#55343=LINE ( 'NONE', #23334, #24938 ) ;
#55345=AXIS2_PLACEMENT_3D ( 'NONE', #1994, #56573, #40090 ) ;
#55346=STYLED_ITEM ( 'NONE', ( #38240 ), #60998 ) ;
#55353=( LENGTH_UNIT ( ) NAMED_UNIT ( * ) SI_UNIT ( .MILLI., .METRE. ) );
#55354=CARTESIAN_POINT ( 'NONE',  ( -45.00000000000000000, 8.552062714373262153, -6.929199553059594230 ) ) ;
#55355=DIRECTION ( 'NONE',  ( -0.000000000000000000, -1.000000000000000000, -0.000000000000000000 ) ) ;
#55360=CARTESIAN_POINT ( 'NONE',  ( -75.00000000000000000, 36.00000000000000711, 9.500000000000000000 ) ) ;
#55364=SURFACE_STYLE_FILL_AREA ( #55718 ) ;
#55373=CARTESIAN_POINT ( 'NONE',  ( -5.598654528085806881, 130.7450000000000045, -7.705886871421374629 ) ) ;
#55375=STYLED_ITEM ( 'NONE', ( #12337 ), #55087 ) ;
#55378=CARTESIAN_POINT ( 'NONE',  ( 48.50000000000000000, 99.99999999999998579, -7.000000000000000000 ) ) ;
#55380=PLANE ( 'NONE',  #43452 ) ;
#55384=CARTESIAN_POINT ( 'NONE',  ( 23.21231517720798010, 117.4999999999999716, -10.00000000000000000 ) ) ;
#55385=( GEOMETRIC_REPRESENTATION_CONTEXT ( 3 ) GLOBAL_UNCERTAINTY_ASSIGNED_CONTEXT ( ( #67793 ) ) GLOBAL_UNIT_ASSIGNED_CONTEXT ( ( #31833, #37528, #27913 ) ) REPRESENTATION_CONTEXT ( 'NONE', 'WORKASPACE' ) );
#55390=ORIENTED_EDGE ( 'NONE', *, *, #44912, .T. ) ;
#55392=CARTESIAN_POINT ( 'NONE',  ( -12.72792206135785698, 115.4999999999999574, 10.50000000000000000 ) ) ;
#55393=( LENGTH_UNIT ( ) NAMED_UNIT ( * ) SI_UNIT ( .MILLI., .METRE. ) );
#55396=CARTESIAN_POINT ( 'NONE',  ( -74.99999999999998579, 146.4999999999999716, 7.000000000000000000 ) ) ;
#55402=EDGE_CURVE ( 'NONE', #22419, #15243, #10556, .T. ) ;
#55403=DIRECTION ( 'NONE',  ( 1.000000000000000000, 0.000000000000000000, 0.000000000000000000 ) ) ;
#55406=CIRCLE ( 'NONE', #7116, 0.5000000000000004441 ) ;
#55410=ORIENTED_EDGE ( 'NONE', *, *, #65130, .T. ) ;
#55412=AXIS2_PLACEMENT_3D ( 'NONE', #26371, #4564, #68612 ) ;
#55413=CARTESIAN_POINT ( 'NONE',  ( -9.827790563157511022E-16, 128.5570736234661524, 8.025000000000000355 ) ) ;
#55419=ORIENTED_EDGE ( 'NONE', *, *, #25804, .T. ) ;
#55420=COLOUR_RGB ( '', 0.31764706, 0.68627451, 0.89019608) ;
#55425=EDGE_LOOP ( 'NONE', ( #49552, #50005, #29592, #14789 ) ) ;
#55428=SURFACE_STYLE_FILL_AREA ( #2949 ) ;
#55429=CARTESIAN_POINT ( 'NONE',  ( 4.716976649647099507, 149.6429263765338078, -6.492361379858953008 ) ) ;
#55433=CONICAL_SURFACE ( 'NONE', #62144, 8.025000000000000355, 0.7853981633974491672 ) ;
#55438=CARTESIAN_POINT ( 'NONE',  ( -7.632228543268608334, 159.8429263765338249, 2.479861379858952830 ) ) ;
#55441=CIRCLE ( 'NONE', #5038, 0.5000000000000004441 ) ;
#55442=SPHERICAL_SURFACE ( 'NONE', #1889, 0.5000000000000000000 ) ;
#55451=DIRECTION ( 'NONE',  ( 1.000000000000000000, 0.000000000000000000, 0.000000000000000000 ) ) ;
#55454=DIRECTION ( 'NONE',  ( -1.000000000000000000, 1.156482317317866302E-16, 0.000000000000000000 ) ) ;
#55455=CARTESIAN_POINT ( 'NONE',  ( -21.02379604162863913, 114.4999999999999574, -10.00000000000000000 ) ) ;
#55456=ORIENTED_EDGE ( 'NONE', *, *, #21200, .T. ) ;
#55458=( NAMED_UNIT ( * ) SI_UNIT ( $, .STERADIAN. ) SOLID_ANGLE_UNIT ( ) );
#55459=PRESENTATION_STYLE_ASSIGNMENT (( #49168 ) ) ;
#55460=LINE ( 'NONE', #58238, #44544 ) ;
#55462=VECTOR ( 'NONE', #48627, 1000.000000000000000 ) ;
#55466=VECTOR ( 'NONE', #29111, 1000.000000000000000 ) ;
#55472=CARTESIAN_POINT ( 'NONE',  ( 23.21231517720797655, 117.4999999999999716, 7.500000000000000000 ) ) ;
#55476=CARTESIAN_POINT ( 'NONE',  ( 15.98999599679679839, 117.4999999999999716, 10.00000000000000000 ) ) ;
#55477=AXIS2_PLACEMENT_3D ( 'NONE', #33350, #48880, #27690 ) ;
#55479=CARTESIAN_POINT ( 'NONE',  ( -9.058813317711338797, 144.4550000000000125, 2.943386871421373563 ) ) ;
#55483=VECTOR ( 'NONE', #5788, 1000.000000000000000 ) ;
#55488=DIRECTION ( 'NONE',  ( 0.000000000000000000, 0.000000000000000000, 1.000000000000000000 ) ) ;
#55490=VERTEX_POINT ( 'NONE', #16886 ) ;
#55493=( GEOMETRIC_REPRESENTATION_CONTEXT ( 3 ) GLOBAL_UNCERTAINTY_ASSIGNED_CONTEXT ( ( #48871 ) ) GLOBAL_UNIT_ASSIGNED_CONTEXT ( ( #21677, #58623, #54026 ) ) REPRESENTATION_CONTEXT ( 'NONE', 'WORKASPACE' ) );
#55497=PRESENTATION_STYLE_ASSIGNMENT (( #60082 ) ) ;
#55499=PRESENTATION_STYLE_ASSIGNMENT (( #60756 ) ) ;
#55502=VERTEX_POINT ( 'NONE', #23503 ) ;
#55503=CARTESIAN_POINT ( 'NONE',  ( -44.50000000000000000, -1.469576158976824302E-14, -4.000000000000000000 ) ) ;
#55504=DIRECTION ( 'NONE',  ( 0.000000000000000000, 1.000000000000000000, -0.000000000000000000 ) ) ;
#55507=FACE_OUTER_BOUND ( 'NONE', #33897, .T. ) ;
#55509=EDGE_LOOP ( 'NONE', ( #27802, #41975 ) ) ;
#55510=AXIS2_PLACEMENT_3D ( 'NONE', #93, #21989, #43492 ) ;
#55511=FACE_OUTER_BOUND ( 'NONE', #68977, .T. ) ;
#55514=ORIENTED_EDGE ( 'NONE', *, *, #11200, .T. ) ;
#55515=MECHANICAL_DESIGN_GEOMETRIC_PRESENTATION_REPRESENTATION('',(#19565),#56628);
#55516=ORIENTED_EDGE ( 'NONE', *, *, #33378, .T. ) ;
#55517=AXIS2_PLACEMENT_3D ( 'NONE', #57513, #57876, #9338 ) ;
#55521=CARTESIAN_POINT ( 'NONE',  ( -7.632228543268608334, 132.8429263765338249, 2.479861379858952830 ) ) ;
#55524=EDGE_CURVE ( 'NONE', #52175, #27683, #34746, .T. ) ;
#55530=DIRECTION ( 'NONE',  ( -0.000000000000000000, -1.000000000000000000, -0.000000000000000000 ) ) ;
#55531=CARTESIAN_POINT ( 'NONE',  ( -7.632228543268607446, 139.6570736234661467, -2.479861379858953718 ) ) ;
#55532=PRESENTATION_STYLE_ASSIGNMENT (( #62183 ) ) ;
#55536=ORIENTED_EDGE ( 'NONE', *, *, #37320, .F. ) ;
#55538=AXIS2_PLACEMENT_3D ( 'NONE', #7002, #24208, #7360 ) ;
#55541=ORIENTED_EDGE ( 'NONE', *, *, #67754, .T. ) ;
#55543=PRESENTATION_STYLE_ASSIGNMENT (( #3411 ) ) ;
#55544=CARTESIAN_POINT ( 'NONE',  ( -71.62068965517238439, 63.58603185604027885, 9.500000000000000000 ) ) ;
#55554=EDGE_CURVE ( 'NONE', #65971, #9835, #13291, .T. ) ;
#55559=CARTESIAN_POINT ( 'NONE',  ( -65.00000000000000000, -1.962809905030629631E-14, 11.50000000000003020 ) ) ;
#55561=FACE_OUTER_BOUND ( 'NONE', #23097, .T. ) ;
#55562=CARTESIAN_POINT ( 'NONE',  ( -34.99999999999992895, 112.9999999999999858, -7.000000000000000000 ) ) ;
#55565=CARTESIAN_POINT ( 'NONE',  ( 8.102448949553183510, 122.1049999999999898, -5.886773742842746238 ) ) ;
#55568=CARTESIAN_POINT ( 'NONE',  ( 15.48999599679679662, 146.4999999999999716, 7.500000000000000000 ) ) ;
#55569=DIRECTION ( 'NONE',  ( 1.000000000000000000, 0.000000000000000000, 0.000000000000000000 ) ) ;
#55570=AXIS2_PLACEMENT_3D ( 'NONE', #6013, #33443, #21863 ) ;
#55572=CARTESIAN_POINT ( 'NONE',  ( 24.21231517720798010, 113.4999999999999858, 7.500000000000000000 ) ) ;
#55573=CARTESIAN_POINT ( 'NONE',  ( 15.98999599679679839, 118.4999999999999716, -7.000000000000000000 ) ) ;
#55580=( LENGTH_UNIT ( ) NAMED_UNIT ( * ) SI_UNIT ( .MILLI., .METRE. ) );
#55582=VERTEX_POINT ( 'NONE', #35109 ) ;
#55583=( LENGTH_UNIT ( ) NAMED_UNIT ( * ) SI_UNIT ( .MILLI., .METRE. ) );
#55586=SURFACE_SIDE_STYLE ('',( #11288 ) ) ;
#55591=ORIENTED_EDGE ( 'NONE', *, *, #39993, .F. ) ;
#55593=ORIENTED_EDGE ( 'NONE', *, *, #46837, .F. ) ;
#55594=CIRCLE ( 'NONE', #19640, 4.999999999999997335 ) ;
#55596=EDGE_LOOP ( 'NONE', ( #63590, #14898, #7045, #7245 ) ) ;
#55598=FILL_AREA_STYLE ('',( #1379 ) ) ;
#55599=ORIENTED_EDGE ( 'NONE', *, *, #40859, .F. ) ;
#55602=DIRECTION ( 'NONE',  ( 0.000000000000000000, 0.000000000000000000, 1.000000000000000000 ) ) ;
#55604=DIRECTION ( 'NONE',  ( -0.000000000000000000, 1.000000000000000000, -0.000000000000000000 ) ) ;
#55605=CARTESIAN_POINT ( 'NONE',  ( 10.01517768586949231, 132.6949999999999363, 1.839758294383810543E-15 ) ) ;
#55609=CARTESIAN_POINT ( 'NONE',  ( 10.01517768586949408, 139.8050000000000068, 1.839758294383810543E-15 ) ) ;
#55612=CARTESIAN_POINT ( 'NONE',  ( 40.99999999999998579, 107.7459666864129275, -3.076101031310279232 ) ) ;
#55613=ORIENTED_EDGE ( 'NONE', *, *, #39590, .T. ) ;
#55614=CARTESIAN_POINT ( 'NONE',  ( -7.632228543268607446, 111.5429263765338135, -2.479861379858953718 ) ) ;
#55616=FILL_AREA_STYLE_COLOUR ( '', #2922 ) ;
#55618=FILL_AREA_STYLE ('',( #7759 ) ) ;
#55623=DIRECTION ( 'NONE',  ( 1.000000000000000000, 0.000000000000000000, 0.000000000000000000 ) ) ;
#55624=ORIENTED_EDGE ( 'NONE', *, *, #44074, .T. ) ;
#55627=CYLINDRICAL_SURFACE ( 'NONE', #272, 0.5000000000000004441 ) ;
#55630=DIRECTION ( 'NONE',  ( 0.000000000000000000, -1.000000000000000000, 0.000000000000000000 ) ) ;
#55631=VECTOR ( 'NONE', #4984, 1000.000000000000000 ) ;
#55632=AXIS2_PLACEMENT_3D ( 'NONE', #18471, #55753, #49449 ) ;
#55633=DIRECTION ( 'NONE',  ( 0.000000000000000000, 0.000000000000000000, 1.000000000000000000 ) ) ;
#55635=SURFACE_SIDE_STYLE ('',( #66171 ) ) ;
#55637=ORIENTED_EDGE ( 'NONE', *, *, #53401, .F. ) ;
#55639=CARTESIAN_POINT ( 'NONE',  ( -45.90208486430518775, 9.410172310978731858, -3.203880287027109919 ) ) ;
#55642=CARTESIAN_POINT ( 'NONE',  ( 0.000000000000000000, 87.30187232391182306, 0.000000000000000000 ) ) ;
#55643=MECHANICAL_DESIGN_GEOMETRIC_PRESENTATION_REPRESENTATION('',(#46710),#30922);
#55647=LINE ( 'NONE', #39157, #15986 ) ;
#55648=CARTESIAN_POINT ( 'NONE',  ( 23.21231517720797655, 117.4999999999999716, 7.000000000000000000 ) ) ;
#55650=COLOUR_RGB ( '', 0.72549020, 0.75294118, 0.79215686) ;
#55651=CARTESIAN_POINT ( 'NONE',  ( -1.166476076187854022E-15, 140.9449999999999932, 9.525000000000000355 ) ) ;
#55653=AXIS2_PLACEMENT_3D ( 'NONE', #56459, #13193, #13543 ) ;
#55655=DIRECTION ( 'NONE',  ( 1.000000000000000000, -0.000000000000000000, -0.000000000000000000 ) ) ;
#55657=DIRECTION ( 'NONE',  ( 0.000000000000000000, 0.000000000000000000, 1.000000000000000000 ) ) ;
#55663=EDGE_CURVE ( 'NONE', #8600, #5084, #2338, .T. ) ;
#55666=ORIENTED_EDGE ( 'NONE', *, *, #33102, .F. ) ;
#55669=ADVANCED_FACE ( 'NONE', ( #62525 ), #27486, .F. ) ;
#55672=CARTESIAN_POINT ( 'NONE',  ( 60.00000000000000000, 1.797044900979284448E-15, -12.00000000000000000 ) ) ;
#55673=EDGE_CURVE ( 'NONE', #28720, #41266, #42868, .T. ) ;
#55674=CARTESIAN_POINT ( 'NONE',  ( -6.826472737025120807, 143.1070736234661638, 4.959722759717906548 ) ) ;
#55675=ORIENTED_EDGE ( 'NONE', *, *, #54774, .F. ) ;
#55678=ORIENTED_EDGE ( 'NONE', *, *, #68550, .F. ) ;
#55679=SURFACE_STYLE_FILL_AREA ( #13102 ) ;
#55684=CARTESIAN_POINT ( 'NONE',  ( 2.607480562269076430, 147.9070736234661467, -8.025000000000000355 ) ) ;
#55685=COLOUR_RGB ( '', 0.72549020, 0.75294118, 0.79215686) ;
#55686=ORIENTED_EDGE ( 'NONE', *, *, #4793, .F. ) ;
#55688=CARTESIAN_POINT ( 'NONE',  ( -8.102448949553179958, 111.0049999999999955, -5.886773742842749790 ) ) ;
#55691=CARTESIAN_POINT ( 'NONE',  ( -6.826472737025120807, 122.1070736234661638, 4.959722759717906548 ) ) ;
#55692=CARTESIAN_POINT ( 'NONE',  ( -8.102448949553181734, 132.6050000000000182, 5.886773742842747126 ) ) ;
#55694=FILL_AREA_STYLE_COLOUR ( '', #6280 ) ;
#55695=TOROIDAL_SURFACE ( 'NONE', #7401, 13.49999999999999822, 0.5000000000000000000 ) ;
#55698=CARTESIAN_POINT ( 'NONE',  ( -23.21231517720797655, 113.4999999999999858, 10.00000000000000000 ) ) ;
#55699=MECHANICAL_DESIGN_GEOMETRIC_PRESENTATION_REPRESENTATION('',(#36677),#46824);
#55702=CYLINDRICAL_SURFACE ( 'NONE', #42978, 0.5000000000000000000 ) ;
#55703=SURFACE_SIDE_STYLE ('',( #50097 ) ) ;
#55705=VERTEX_POINT ( 'NONE', #11493 ) ;
#55706=DIRECTION ( 'NONE',  ( 1.000000000000000000, -0.000000000000000000, -0.000000000000000000 ) ) ;
#55707=CARTESIAN_POINT ( 'NONE',  ( -45.90418876431856887, 9.387410786201595414, -6.121260521433894652 ) ) ;
#55713=EDGE_LOOP ( 'NONE', ( #43913, #28094, #60768, #35578 ) ) ;
#55714=CIRCLE ( 'NONE', #59116, 0.5000000000000004441 ) ;
#55715=CARTESIAN_POINT ( 'NONE',  ( -74.08601561514839773, 9.424559774107397203, 6.049830996511062153 ) ) ;
#55718=FILL_AREA_STYLE ('',( #60976 ) ) ;
#55720=STYLED_ITEM ( 'NONE', ( #40875 ), #1868 ) ;
#55723=CARTESIAN_POINT ( 'NONE',  ( -8.102448949553179958, 146.4949999999999761, 5.886773742842747126 ) ) ;
#55724=MECHANICAL_DESIGN_GEOMETRIC_PRESENTATION_REPRESENTATION('',(#28735),#10782);
#55727=SURFACE_STYLE_FILL_AREA ( #50802 ) ;
#55729=ORIENTED_EDGE ( 'NONE', *, *, #17037, .T. ) ;
#55730=DIRECTION ( 'NONE',  ( 0.000000000000000000, 1.000000000000000000, 0.000000000000000000 ) ) ;
#55732=( NAMED_UNIT ( * ) PLANE_ANGLE_UNIT ( ) SI_UNIT ( $, .RADIAN. ) );
#55735=DIRECTION ( 'NONE',  ( 0.000000000000000000, 0.000000000000000000, -1.000000000000000000 ) ) ;
#55736=CARTESIAN_POINT ( 'NONE',  ( 3.094860106618435136, 112.2949999999999733, -9.525000000000000355 ) ) ;
#55740=EDGE_LOOP ( 'NONE', ( #30385, #10453, #21605, #33008 ) ) ;
#55741=LINE ( 'NONE', #18791, #41492 ) ;
#55746=( NAMED_UNIT ( * ) PLANE_ANGLE_UNIT ( ) SI_UNIT ( $, .RADIAN. ) );
#55748=STYLED_ITEM ( 'NONE', ( #50266 ), #64573 ) ;
#55751=FACE_OUTER_BOUND ( 'NONE', #908, .T. ) ;
#55753=DIRECTION ( 'NONE',  ( -0.000000000000000000, -0.000000000000000000, -1.000000000000000000 ) ) ;
#55754=CARTESIAN_POINT ( 'NONE',  ( -72.50000000000001421, 13.41640786499872284, -10.00000000000000000 ) ) ;
#55759=CARTESIAN_POINT ( 'NONE',  ( 74.49999999999998579, 119.9999999999997584, -10.00000000000000000 ) ) ;
#55761=CARTESIAN_POINT ( 'NONE',  ( -40.78947369313011251, 108.1536491435770131, 3.152202064295502648 ) ) ;
#55769=CARTESIAN_POINT ( 'NONE',  ( -6.826472737025120807, 121.5070736234661410, -4.959722759717907437 ) ) ;
#55771=EDGE_CURVE ( 'NONE', #14638, #44423, #34128, .T. ) ;
#55772=CARTESIAN_POINT ( 'NONE',  ( 75.00000000000000000, 19.44429231213349496, -6.999999999972110309 ) ) ;
#55773=SURFACE_STYLE_USAGE ( .BOTH. , #65969 ) ;
#55778=SURFACE_SIDE_STYLE ('',( #55428 ) ) ;
#55782=CARTESIAN_POINT ( 'NONE',  ( -2.607480562269041791, 123.0929263765338106, -8.025000000000021672 ) ) ;
#55785=ORIENTED_EDGE ( 'NONE', *, *, #28812, .F. ) ;
#55786=DIRECTION ( 'NONE',  ( 1.000000000000000000, 0.000000000000000000, 0.000000000000000000 ) ) ;
#55791=FACE_OUTER_BOUND ( 'NONE', #52553, .T. ) ;
#55792=CARTESIAN_POINT ( 'NONE',  ( -15.98999599679679839, 118.4999999999999716, -7.000000000000000000 ) ) ;
#55796=CARTESIAN_POINT ( 'NONE',  ( 8.102448949553179958, 114.3949999999999676, 5.886773742842750679 ) ) ;
#55804=DIRECTION ( 'NONE',  ( 0.000000000000000000, 0.000000000000000000, 1.000000000000000000 ) ) ;
#55809=CARTESIAN_POINT ( 'NONE',  ( 48.50000000000000000, 14.49137674618942562, 9.500000000000000000 ) ) ;
#55813=ORIENTED_EDGE ( 'NONE', *, *, #57041, .F. ) ;
#55815=CARTESIAN_POINT ( 'NONE',  ( 45.00050070149898573, 10.00016690049882229, 3.905286714425231231 ) ) ;
#55820=EDGE_CURVE ( 'NONE', #16782, #16768, #2598, .T. ) ;
#55823=CARTESIAN_POINT ( 'NONE',  ( 9.058813317711338797, 148.9550000000000125, -2.943386871421372675 ) ) ;
#55824=FILL_AREA_STYLE ('',( #39332 ) ) ;
#55825=UNCERTAINTY_MEASURE_WITH_UNIT (LENGTH_MEASURE( 1.000000000000000082E-05 ), #7206, 'distance_accuracy_value', 'NONE');
#55831=DIRECTION ( 'NONE',  ( -0.000000000000000000, -1.000000000000000000, -0.000000000000000000 ) ) ;
#55832=TOROIDAL_SURFACE ( 'NONE', #62608, 12.50000000000000000, 0.5000000000000000000 ) ;
#55836=CARTESIAN_POINT ( 'NONE',  ( -34.99999999999992184, 109.9999999999999858, 9.500000000000000000 ) ) ;
#55838=ORIENTED_EDGE ( 'NONE', *, *, #23669, .F. ) ;
#55839=DIRECTION ( 'NONE',  ( 0.000000000000000000, 0.000000000000000000, 1.000000000000000000 ) ) ;
#55842=ADVANCED_FACE ( 'NONE', ( #8314 ), #39793, .T. ) ;
#55843=CARTESIAN_POINT ( 'NONE',  ( -45.00000000000000711, 8.747703778475440117, 6.883446876413755966 ) ) ;
#55852=CARTESIAN_POINT ( 'NONE',  ( -3.094860106618434248, 111.9050000000000011, 9.525000000000000355 ) ) ;
#55853=CARTESIAN_POINT ( 'NONE',  ( -34.99999999999992895, 113.4999999999999858, 7.500000000000000000 ) ) ;
#55855=DIRECTION ( 'NONE',  ( 1.000000000000000000, 0.000000000000000000, 0.000000000000000000 ) ) ;
#55858=EDGE_LOOP ( 'NONE', ( #15578, #27471, #58888, #23245 ) ) ;
#55860=CARTESIAN_POINT ( 'NONE',  ( -74.08452722063036333, 9.430195807687214327, -6.039758700367572786 ) ) ;
#55861=DIRECTION ( 'NONE',  ( 0.000000000000000000, 1.000000000000000000, -0.000000000000000000 ) ) ;
#55865=CARTESIAN_POINT ( 'NONE',  ( -4.716976649647097730, 141.2429263765338305, -6.492361379858953896 ) ) ;
#55868=( LENGTH_UNIT ( ) NAMED_UNIT ( * ) SI_UNIT ( .MILLI., .METRE. ) );
#55870=ORIENTED_EDGE ( 'NONE', *, *, #32538, .F. ) ;
#55874=CARTESIAN_POINT ( 'NONE',  ( -7.632228543268608334, 139.9570736234661581, 2.479861379858952830 ) ) ;
#55878=SURFACE_STYLE_USAGE ( .BOTH. , #17905 ) ;
#55901=CARTESIAN_POINT ( 'NONE',  ( -74.96084131305691756, 35.58445536041309509, -9.699738583933323000 ) ) ;
#55902=ADVANCED_FACE ( 'NONE', ( #34666 ), #24127, .F. ) ;
#55906=DIRECTION ( 'NONE',  ( 0.000000000000000000, 0.000000000000000000, 1.000000000000000000 ) ) ;
#55908=EDGE_CURVE ( 'NONE', #3770, #23886, #66726, .T. ) ;
#55911=CARTESIAN_POINT ( 'NONE',  ( 3.094860106618435136, 113.4050000000000011, -9.525000000000000355 ) ) ;
#55917=ORIENTED_EDGE ( 'NONE', *, *, #44458, .T. ) ;
#55921=FACE_OUTER_BOUND ( 'NONE', #39195, .T. ) ;
#55922=EDGE_CURVE ( 'NONE', #32643, #16561, #3819, .T. ) ;
#55923=CARTESIAN_POINT ( 'NONE',  ( -45.50000000000000000, 7.768687147774684831, 6.999999999999999112 ) ) ;
#55929=SURFACE_STYLE_USAGE ( .BOTH. , #66852 ) ;
#55932=MECHANICAL_DESIGN_GEOMETRIC_PRESENTATION_REPRESENTATION('',(#4236),#24481);
#55940=ORIENTED_EDGE ( 'NONE', *, *, #8702, .F. ) ;
#55944=CARTESIAN_POINT ( 'NONE',  ( 5.598654528085809545, 142.1449999999999818, -7.705886871421373741 ) ) ;
#55947=CARTESIAN_POINT ( 'NONE',  ( 0.000000000000000000, 140.5549999999999784, -9.525000000000000355 ) ) ;
#55949=ORIENTED_EDGE ( 'NONE', *, *, #45847, .T. ) ;
#55950=CARTESIAN_POINT ( 'NONE',  ( 9.058813317711337021, 160.6550000000000011, 2.943386871421375783 ) ) ;
#55951=CARTESIAN_POINT ( 'NONE',  ( -60.00000000000000000, -2.024042244987997205E-14, 6.999999999999995559 ) ) ;
#55952=UNCERTAINTY_MEASURE_WITH_UNIT (LENGTH_MEASURE( 1.000000000000000082E-05 ), #56752, 'distance_accuracy_value', 'NONE');
#55953=VECTOR ( 'NONE', #61350, 1000.000000000000000 ) ;
#55954=FILL_AREA_STYLE ('',( #55616 ) ) ;
#55955=VECTOR ( 'NONE', #4742, 1000.000000000000000 ) ;
#55958=ORIENTED_EDGE ( 'NONE', *, *, #60513, .T. ) ;
#55960=DIRECTION ( 'NONE',  ( 0.000000000000000000, 0.000000000000000000, 1.000000000000000000 ) ) ;
#55964=CYLINDRICAL_SURFACE ( 'NONE', #38578, 0.5000000000000004441 ) ;
#55965=UNCERTAINTY_MEASURE_WITH_UNIT (LENGTH_MEASURE( 1.000000000000000082E-05 ), #6629, 'distance_accuracy_value', 'NONE');
#55966=FILL_AREA_STYLE ('',( #29583 ) ) ;
#55968=CARTESIAN_POINT ( 'NONE',  ( 45.00000000000000000, 9.639620389971918613, -7.000000000000000000 ) ) ;
#55969=CYLINDRICAL_SURFACE ( 'NONE', #23143, 0.5000000000000004441 ) ;
#55970=ORIENTED_EDGE ( 'NONE', *, *, #59465, .F. ) ;
#55978=PRESENTATION_STYLE_ASSIGNMENT (( #28884 ) ) ;
#55981=CARTESIAN_POINT ( 'NONE',  ( -75.00000000000000000, 7.768687147774688384, -7.000000000000000000 ) ) ;
#55985=( NAMED_UNIT ( * ) SI_UNIT ( $, .STERADIAN. ) SOLID_ANGLE_UNIT ( ) );
#55987=TOROIDAL_SURFACE ( 'NONE', #34637, 1.000000000000000000, 0.5000000000000000000 ) ;
#55989=CARTESIAN_POINT ( 'NONE',  ( -3.094860106618434248, 137.7950000000000159, 9.525000000000000355 ) ) ;
#55991=CIRCLE ( 'NONE', #12145, 0.5000000000000004441 ) ;
#55996=MECHANICAL_DESIGN_GEOMETRIC_PRESENTATION_REPRESENTATION('',(#63871),#62715);
#55997=ADVANCED_FACE ( 'NONE', ( #31122 ), #15090, .T. ) ;
#55998=DIRECTION ( 'NONE',  ( 0.000000000000000000, 0.000000000000000000, 1.000000000000000000 ) ) ;
#56003=( LENGTH_UNIT ( ) NAMED_UNIT ( * ) SI_UNIT ( .MILLI., .METRE. ) );
#56006=CARTESIAN_POINT ( 'NONE',  ( -15.48999599679679662, 147.4999999999999716, 10.00000000000000000 ) ) ;
#56007=CARTESIAN_POINT ( 'NONE',  ( 0.000000000000000000, 142.0570736234661524, -8.025000000000000355 ) ) ;
#56009=ORIENTED_EDGE ( 'NONE', *, *, #60201, .F. ) ;
#56012=LINE ( 'NONE', #19775, #18892 ) ;
#56016=CARTESIAN_POINT ( 'NONE',  ( -8.102448949553181734, 112.8949999999999818, -5.886773742842749790 ) ) ;
#56017=ORIENTED_EDGE ( 'NONE', *, *, #38583, .F. ) ;
#56018=CARTESIAN_POINT ( 'NONE',  ( 74.99999999999998579, 50.00000000000000000, 7.000000000000000000 ) ) ;
#56019=CARTESIAN_POINT ( 'NONE',  ( -9.058813317711337021, 111.1549999999999869, -2.943386871421374895 ) ) ;
#56021=CARTESIAN_POINT ( 'NONE',  ( -8.437984349512095861, 121.8070736234661524, -5.166775262442723748E-16 ) ) ;
#56022=CARTESIAN_POINT ( 'NONE',  ( -8.102448949553181734, 126.6050000000000040, 5.886773742842747126 ) ) ;
#56023=UNCERTAINTY_MEASURE_WITH_UNIT (LENGTH_MEASURE( 1.000000000000000082E-05 ), #14360, 'distance_accuracy_value', 'NONE');
#56025=CARTESIAN_POINT ( 'NONE',  ( 20.43039690318515156, 114.8190495831791793, 10.32375696423105360 ) ) ;
#56026=CARTESIAN_POINT ( 'NONE',  ( -45.00000000000000000, 9.708372675170618749, 10.00000000000000000 ) ) ;
#56027=FILL_AREA_STYLE ('',( #34244 ) ) ;
#56029=( GEOMETRIC_REPRESENTATION_CONTEXT ( 3 ) GLOBAL_UNCERTAINTY_ASSIGNED_CONTEXT ( ( #6630 ) ) GLOBAL_UNIT_ASSIGNED_CONTEXT ( ( #24819, #25520, #42118 ) ) REPRESENTATION_CONTEXT ( 'NONE', 'WORKASPACE' ) );
#56030=SURFACE_STYLE_USAGE ( .BOTH. , #34936 ) ;
#56035=LINE ( 'NONE', #66612, #45874 ) ;
#56039=CARTESIAN_POINT ( 'NONE',  ( 60.00000000000000000, 1.797044900979284448E-15, 11.50000000000000000 ) ) ;
#56041=SPHERICAL_SURFACE ( 'NONE', #44953, 0.5000000000000000000 ) ;
#56042=ORIENTED_EDGE ( 'NONE', *, *, #39088, .F. ) ;
#56043=CIRCLE ( 'NONE', #58313, 14.49999999999999822 ) ;
#56044=CARTESIAN_POINT ( 'NONE',  ( -75.00000000000000000, 8.589831058620905679, 5.576814063797191245 ) ) ;
#56046=VERTEX_POINT ( 'NONE', #31469 ) ;
#56047=DIRECTION ( 'NONE',  ( 0.000000000000000000, 0.000000000000000000, -1.000000000000000000 ) ) ;
#56049=SPHERICAL_SURFACE ( 'NONE', #6651, 0.5000000000000000000 ) ;
#56052=LINE ( 'NONE', #60981, #13703 ) ;
#56053=CARTESIAN_POINT ( 'NONE',  ( -1.166476076187854022E-15, 137.9449999999999932, 9.525000000000000355 ) ) ;
#56055=COLOUR_RGB ( '', 0.40784314, 0.44705882, 0.49803922) ;
#56057=DIRECTION ( 'NONE',  ( -0.000000000000000000, -1.000000000000000000, 0.000000000000000000 ) ) ;
#56061=DIRECTION ( 'NONE',  ( 1.000000000000000000, 0.000000000000000000, 0.000000000000000000 ) ) ;
#56062=CIRCLE ( 'NONE', #43759, 13.99999999999999822 ) ;
#56067=( LENGTH_UNIT ( ) NAMED_UNIT ( * ) SI_UNIT ( .MILLI., .METRE. ) );
#56071=CIRCLE ( 'NONE', #25737, 0.5000000000000004441 ) ;
#56073=ADVANCED_FACE ( 'NONE', ( #38189 ), #68999, .T. ) ;
#56075=VECTOR ( 'NONE', #58260, 1000.000000000000000 ) ;
#56077=CIRCLE ( 'NONE', #56115, 29.50000000000000000 ) ;
#56081=CARTESIAN_POINT ( 'NONE',  ( 0.000000000000000000, 154.9999999999999716, 0.000000000000000000 ) ) ;
#56085=SURFACE_STYLE_USAGE ( .BOTH. , #57752 ) ;
#56086=CARTESIAN_POINT ( 'NONE',  ( -60.99999999999998579, 50.00000000000000000, 9.500000000000000000 ) ) ;
#56092=CYLINDRICAL_SURFACE ( 'NONE', #1188, 0.5000000000000004441 ) ;
#56096=STYLED_ITEM ( 'NONE', ( #11073 ), #68566 ) ;
#56098=ORIENTED_EDGE ( 'NONE', *, *, #10877, .T. ) ;
#56100=DIRECTION ( 'NONE',  ( 1.000000000000000000, 0.000000000000000000, 0.000000000000000000 ) ) ;
#56101=ORIENTED_EDGE ( 'NONE', *, *, #17803, .F. ) ;
#56103=CARTESIAN_POINT ( 'NONE',  ( 0.000000000000000000, 127.0570736234661666, -8.025000000000000355 ) ) ;
#56109=CARTESIAN_POINT ( 'NONE',  ( -75.00000000000000000, -2.215169945516535778E-14, -6.500000000000000888 ) ) ;
#56115=AXIS2_PLACEMENT_3D ( 'NONE', #26791, #47657, #38118 ) ;
#56121=ORIENTED_EDGE ( 'NONE', *, *, #31523, .T. ) ;
#56122=FILL_AREA_STYLE ('',( #34340 ) ) ;
#56123=ADVANCED_FACE ( 'NONE', ( #65223 ), #38552, .T. ) ;
#56126=SURFACE_STYLE_FILL_AREA ( #12877 ) ;
#56127=( NAMED_UNIT ( * ) PLANE_ANGLE_UNIT ( ) SI_UNIT ( $, .RADIAN. ) );
#56131=ADVANCED_FACE ( 'NONE', ( #19011 ), #19373, .F. ) ;
#56134=DIRECTION ( 'NONE',  ( -0.000000000000000000, -0.000000000000000000, 1.000000000000000000 ) ) ;
#56138=DIRECTION ( 'NONE',  ( 1.000000000000000000, -1.156482317317866302E-16, 0.000000000000000000 ) ) ;
#56139=DIRECTION ( 'NONE',  ( 0.2413793103448194644, -0.9704308468600220117, 0.000000000000000000 ) ) ;
#56147=AXIS2_PLACEMENT_3D ( 'NONE', #19727, #27403, #21811 ) ;
#56157=CARTESIAN_POINT ( 'NONE',  ( -8.102448949553181734, 144.6049999999999613, 5.886773742842747126 ) ) ;
#56159=VECTOR ( 'NONE', #39404, 1000.000000000000000 ) ;
#56162=CARTESIAN_POINT ( 'NONE',  ( -20.04014546381213435, 115.4999999869038163, -10.00000000000000000 ) ) ;
#56166=AXIS2_PLACEMENT_3D ( 'NONE', #9140, #52060, #3815 ) ;
#56167=DIRECTION ( 'NONE',  ( -1.000000000000000000, 0.000000000000000000, -0.000000000000000000 ) ) ;
#56170=EDGE_LOOP ( 'NONE', ( #9602, #23470, #4641, #11753 ) ) ;
#56173=ADVANCED_FACE ( 'NONE', ( #30257 ), #56818, .F. ) ;
#56175=DIRECTION ( 'NONE',  ( 1.000000000000000000, 0.000000000000000000, 0.000000000000000000 ) ) ;
#56176=CIRCLE ( 'NONE', #38272, 1.000000000000000888 ) ;
#56179=ORIENTED_EDGE ( 'NONE', *, *, #64734, .F. ) ;
#56181=FILL_AREA_STYLE ('',( #30132 ) ) ;
#56183=CARTESIAN_POINT ( 'NONE',  ( 5.598654528085805993, 112.3549999999999898, 7.705886871421374629 ) ) ;
#56189=ORIENTED_EDGE ( 'NONE', *, *, #65281, .T. ) ;
#56190=CARTESIAN_POINT ( 'NONE',  ( -3.453468097287629046, 110.4999999999999858, -8.920302546751260664 ) ) ;
#56194=LINE ( 'NONE', #52351, #40905 ) ;
#56195=VERTEX_POINT ( 'NONE', #20557 ) ;
#56196=CARTESIAN_POINT ( 'NONE',  ( -2.607480562269073765, 144.0929263765338249, -8.025000000000000355 ) ) ;
#56198=LINE ( 'NONE', #62521, #50382 ) ;
#56200=( NAMED_UNIT ( * ) SI_UNIT ( $, .STERADIAN. ) SOLID_ANGLE_UNIT ( ) );
#56203=VERTEX_POINT ( 'NONE', #41700 ) ;
#56207=DIRECTION ( 'NONE',  ( 0.000000000000000000, 0.000000000000000000, 1.000000000000000000 ) ) ;
#56208=CARTESIAN_POINT ( 'NONE',  ( 40.99999999999999289, 107.7459666924148110, -3.099782425413943443 ) ) ;
#56211=PRESENTATION_STYLE_ASSIGNMENT (( #23511 ) ) ;
#56213=CARTESIAN_POINT ( 'NONE',  ( 0.000000000000000000, 87.30187232391182306, 0.000000000000000000 ) ) ;
#56218=ORIENTED_EDGE ( 'NONE', *, *, #23676, .T. ) ;
#56221=FILL_AREA_STYLE ('',( #17913 ) ) ;
#56224=FILL_AREA_STYLE ('',( #28435 ) ) ;
#56227=( LENGTH_UNIT ( ) NAMED_UNIT ( * ) SI_UNIT ( .MILLI., .METRE. ) );
#56228=( NAMED_UNIT ( * ) SI_UNIT ( $, .STERADIAN. ) SOLID_ANGLE_UNIT ( ) );
#56229=STYLED_ITEM ( 'NONE', ( #17902 ), #17813 ) ;
#56231=ADVANCED_FACE ( 'NONE', ( #57500 ), #8970, .F. ) ;
#56237=SURFACE_STYLE_FILL_AREA ( #68203 ) ;
#56238=EDGE_CURVE ( 'NONE', #37840, #25507, #62066, .T. ) ;
#56242=DIRECTION ( 'NONE',  ( -0.000000000000000000, -0.000000000000000000, 1.000000000000000000 ) ) ;
#56244=CARTESIAN_POINT ( 'NONE',  ( -3.094860106618432471, 116.7049999999999983, -9.525000000000000355 ) ) ;
#56250=( BOUNDED_CURVE ( )  B_SPLINE_CURVE ( 2, ( #20361, #67880, #62571, #63282, #67514, #15130, #30553, #4155, #35858, #20000, #25625 ),
 .UNSPECIFIED., .F., .F. ) 
 B_SPLINE_CURVE_WITH_KNOTS ( ( 3, 2, 2, 2, 2, 3 ),
 ( 0.7058823529411762943, 0.7117647058823527439, 0.7176470588235291936, 0.7235294117647056433, 0.7294117647058820930, 0.7352941176470586537 ),
 .UNSPECIFIED. ) 
 CURVE ( )  GEOMETRIC_REPRESENTATION_ITEM ( )  RATIONAL_B_SPLINE_CURVE ( ( 1.000000000000001776, 0.9510565162951516438, 1.000000000000000000, 0.9510565162951535312, 1.000000000000000000, 0.9510565162951535312, 1.000000000000000000, 0.9510565162951535312, 1.000000000000000000, 0.9510565162951554186, 0.9999999999999981126 ) ) 
 REPRESENTATION_ITEM ( '' )  );
#56251=CARTESIAN_POINT ( 'NONE',  ( 23.21231517720797655, 117.4999999999999716, 9.500000000000000000 ) ) ;
#56252=( LENGTH_UNIT ( ) NAMED_UNIT ( * ) SI_UNIT ( .MILLI., .METRE. ) );
#56253=( GEOMETRIC_REPRESENTATION_CONTEXT ( 3 ) GLOBAL_UNCERTAINTY_ASSIGNED_CONTEXT ( ( #31150 ) ) GLOBAL_UNIT_ASSIGNED_CONTEXT ( ( #66588, #34562, #2508 ) ) REPRESENTATION_CONTEXT ( 'NONE', 'WORKASPACE' ) );
#56262=ORIENTED_EDGE ( 'NONE', *, *, #66301, .T. ) ;
#56267=ADVANCED_FACE ( 'NONE', ( #13896 ), #68765, .F. ) ;
#56270=CARTESIAN_POINT ( 'NONE',  ( 60.00000000000000000, 110.4999999999999858, -10.00000000000000000 ) ) ;
#56271=CIRCLE ( 'NONE', #66367, 1.000000000000000888 ) ;
#56279=( LENGTH_UNIT ( ) NAMED_UNIT ( * ) SI_UNIT ( .MILLI., .METRE. ) );
#56283=CARTESIAN_POINT ( 'NONE',  ( 8.102448949553183510, 141.9950000000000045, -5.886773742842746238 ) ) ;
#56287=CARTESIAN_POINT ( 'NONE',  ( 5.598654528085805993, 142.3549999999999898, 7.705886871421374629 ) ) ;
#56289=CARTESIAN_POINT ( 'NONE',  ( 41.12389261647935967, 107.5649728523252691, -3.335908204272119981 ) ) ;
#56291=CARTESIAN_POINT ( 'NONE',  ( -9.827790563157511022E-16, 118.4429263765338192, 8.025000000000000355 ) ) ;
#56295=( LENGTH_UNIT ( ) NAMED_UNIT ( * ) SI_UNIT ( .MILLI., .METRE. ) );
#56297=EDGE_LOOP ( 'NONE', ( #37308, #43580, #7462, #23319 ) ) ;
#56299=ORIENTED_EDGE ( 'NONE', *, *, #62001, .F. ) ;
#56300=DIRECTION ( 'NONE',  ( 0.7833176619561811327, 0.6216216216216278179, -0.000000000000000000 ) ) ;
#56305=SURFACE_SIDE_STYLE ('',( #7450 ) ) ;
#56306=ADVANCED_FACE ( 'NONE', ( #53605 ), #478, .T. ) ;
#56307=COLOUR_RGB ( '', 0.08235294, 0.09019608, 0.10196078) ;
#56308=FILL_AREA_STYLE ('',( #23612 ) ) ;
#56310=CARTESIAN_POINT ( 'NONE',  ( 45.00000000000000000, 9.905302582396059208, -6.348323522272433017 ) ) ;
#56312=ORIENTED_EDGE ( 'NONE', *, *, #21352, .T. ) ;
#56315=CYLINDRICAL_SURFACE ( 'NONE', #61614, 8.025000000000000355 ) ;
#56323=ORIENTED_EDGE ( 'NONE', *, *, #58090, .T. ) ;
#56328=CARTESIAN_POINT ( 'NONE',  ( -1.166476076187854022E-15, 143.9449999999999932, 9.525000000000000355 ) ) ;
#56350=CARTESIAN_POINT ( 'NONE',  ( 44.64644201180199445, 9.999999999999980460, -3.314822853082296295 ) ) ;
#56351=AXIS2_PLACEMENT_3D ( 'NONE', #61800, #46032, #13631 ) ;
#56352=CARTESIAN_POINT ( 'NONE',  ( -15.98999599679679839, 146.9999999999999716, 9.500000000000000000 ) ) ;
#56356=ORIENTED_EDGE ( 'NONE', *, *, #42686, .F. ) ;
#56358=PRESENTATION_STYLE_ASSIGNMENT (( #13447 ) ) ;
#56362=DIRECTION ( 'NONE',  ( 0.000000000000000000, 0.000000000000000000, 1.000000000000000000 ) ) ;
#56363=( GEOMETRIC_REPRESENTATION_CONTEXT ( 3 ) GLOBAL_UNCERTAINTY_ASSIGNED_CONTEXT ( ( #39820 ) ) GLOBAL_UNIT_ASSIGNED_CONTEXT ( ( #34408, #1971, #24520 ) ) REPRESENTATION_CONTEXT ( 'NONE', 'WORKASPACE' ) );
#56365=CARTESIAN_POINT ( 'NONE',  ( 5.598654528085809545, 115.1449999999999818, -7.705886871421373741 ) ) ;
#56366=VECTOR ( 'NONE', #35887, 1000.000000000000000 ) ;
#56367=ORIENTED_EDGE ( 'NONE', *, *, #36239, .T. ) ;
#56368=EDGE_CURVE ( 'NONE', #55502, #31194, #12884, .T. ) ;
#56370=CARTESIAN_POINT ( 'NONE',  ( 24.21231517720798010, 112.9999999999999858, 9.500000000000000000 ) ) ;
#56372=CARTESIAN_POINT ( 'NONE',  ( 8.102448949553183510, 134.1049999999999329, -5.886773742842746238 ) ) ;
#56374=( NAMED_UNIT ( * ) PLANE_ANGLE_UNIT ( ) SI_UNIT ( $, .RADIAN. ) );
#56376=ADVANCED_FACE ( 'NONE', ( #59915 ), #11786, .F. ) ;
#56377=AXIS2_PLACEMENT_3D ( 'NONE', #45562, #66982, #28955 ) ;
#56378=DIRECTION ( 'NONE',  ( 3.469446951953610639E-15, -1.000000000000000000, 0.000000000000000000 ) ) ;
#56380=CARTESIAN_POINT ( 'NONE',  ( 24.21231517720798010, 113.4999999999999858, 7.000000000000000000 ) ) ;
#56381=ORIENTED_EDGE ( 'NONE', *, *, #46425, .F. ) ;
#56382=SURFACE_STYLE_USAGE ( .BOTH. , #40234 ) ;
#56383=SPHERICAL_SURFACE ( 'NONE', #17184, 0.5000000000000000000 ) ;
#56385=ORIENTED_EDGE ( 'NONE', *, *, #15492, .F. ) ;
#56388=CARTESIAN_POINT ( 'NONE',  ( -44.99999999999998579, 119.9999999999999716, 9.500000000000000000 ) ) ;
#56393=PRESENTATION_STYLE_ASSIGNMENT (( #45195 ) ) ;
#56396=EDGE_CURVE ( 'NONE', #10181, #15297, #1635, .T. ) ;
#56397=( NAMED_UNIT ( * ) PLANE_ANGLE_UNIT ( ) SI_UNIT ( $, .RADIAN. ) );
#56399=ORIENTED_EDGE ( 'NONE', *, *, #16409, .F. ) ;
#56400=DIRECTION ( 'NONE',  ( 1.000000000000000000, -0.000000000000000000, 0.000000000000000000 ) ) ;
#56401=CARTESIAN_POINT ( 'NONE',  ( 0.000000000000000000, 154.9999999999999716, 0.000000000000000000 ) ) ;
#56403=MECHANICAL_DESIGN_GEOMETRIC_PRESENTATION_REPRESENTATION('',(#17127),#19398);
#56405=CARTESIAN_POINT ( 'NONE',  ( -5.598654528085806881, 145.7449999999999761, -7.705886871421374629 ) ) ;
#56407=TOROIDAL_SURFACE ( 'NONE', #65406, 13.49999999999999822, 0.5000000000000000000 ) ;
#56412=FACE_OUTER_BOUND ( 'NONE', #52955, .T. ) ;
#56413=CARTESIAN_POINT ( 'NONE',  ( 71.99999999999998579, 119.9999999999997868, -7.500000000000000000 ) ) ;
#56414=( NAMED_UNIT ( * ) PLANE_ANGLE_UNIT ( ) SI_UNIT ( $, .RADIAN. ) );
#56417=DIRECTION ( 'NONE',  ( 0.000000000000000000, 1.000000000000000000, -0.000000000000000000 ) ) ;
#56421=COLOUR_RGB ( '', 0.66274510, 0.83137255, 0.94901961) ;
#56424=EDGE_LOOP ( 'NONE', ( #68310, #6997, #53992, #56624 ) ) ;
#56425=CIRCLE ( 'NONE', #18211, 0.5000000000000004441 ) ;
#56427=CARTESIAN_POINT ( 'NONE',  ( -45.00000000000000000, 99.99999999999992895, -9.500000000000000000 ) ) ;
#56431=MECHANICAL_DESIGN_GEOMETRIC_PRESENTATION_REPRESENTATION('',(#47502),#58692);
#56432=SURFACE_STYLE_FILL_AREA ( #36686 ) ;
#56433=AXIS2_PLACEMENT_3D ( 'NONE', #9802, #52706, #9101 ) ;
#56435=DIRECTION ( 'NONE',  ( -0.000000000000000000, -0.000000000000000000, 1.000000000000000000 ) ) ;
#56440=CARTESIAN_POINT ( 'NONE',  ( -34.99999999999999289, 99.99999999999998579, 10.00000000000000000 ) ) ;
#56442=SURFACE_STYLE_USAGE ( .BOTH. , #3999 ) ;
#56446=CARTESIAN_POINT ( 'NONE',  ( -15.98999599679679839, 146.4999999999999716, 7.500000000000000000 ) ) ;
#56450=FACE_OUTER_BOUND ( 'NONE', #21891, .T. ) ;
#56452=VECTOR ( 'NONE', #54704, 1000.000000000000000 ) ;
#56453=CARTESIAN_POINT ( 'NONE',  ( 6.826472737025121695, 129.6070736234661638, -4.959722759717905660 ) ) ;
#56454=CARTESIAN_POINT ( 'NONE',  ( 0.000000000000000000, 87.30187232391182306, 8.025000000000000355 ) ) ;
#56455=CARTESIAN_POINT ( 'NONE',  ( 75.00000000000000000, 19.46449454893560116, -6.525737028834473819 ) ) ;
#56459=CARTESIAN_POINT ( 'NONE',  ( 74.50000000000000000, 3.473944261090200865E-15, -6.999999999999999112 ) ) ;
#56460=ADVANCED_FACE ( 'NONE', ( #12405, #1099, #49725, #24018 ), #7152, .T. ) ;
#56461=DIRECTION ( 'NONE',  ( 1.000000000000000000, 0.000000000000000000, 0.000000000000000000 ) ) ;
#56464=ADVANCED_FACE ( 'NONE', ( #17391 ), #28216, .T. ) ;
#56467=ORIENTED_EDGE ( 'NONE', *, *, #3438, .T. ) ;
#56468=COLOUR_RGB ( '', 0.08235294, 0.09019608, 0.10196078) ;
#56469=CARTESIAN_POINT ( 'NONE',  ( 12.72792206135785875, 1.797044900979284448E-15, -10.00000000000000000 ) ) ;
#56470=CARTESIAN_POINT ( 'NONE',  ( -60.00000000000000000, -2.024042244987997205E-14, 11.50000000000003020 ) ) ;
#56474=ORIENTED_EDGE ( 'NONE', *, *, #19814, .T. ) ;
#56477=MECHANICAL_DESIGN_GEOMETRIC_PRESENTATION_REPRESENTATION('',(#46440),#65476);
#56482=FILL_AREA_STYLE ('',( #60369 ) ) ;
#56483=DIRECTION ( 'NONE',  ( 0.000000000000000000, 0.000000000000000000, 1.000000000000000000 ) ) ;
#56487=CARTESIAN_POINT ( 'NONE',  ( -9.058813317711337021, 113.0449999999999875, -2.943386871421374895 ) ) ;
#56491=ORIENTED_EDGE ( 'NONE', *, *, #42790, .T. ) ;
#56492=CARTESIAN_POINT ( 'NONE',  ( 44.50000000000000000, 99.99999999999992895, 3.500000000000000000 ) ) ;
#56493=( NAMED_UNIT ( * ) SI_UNIT ( $, .STERADIAN. ) SOLID_ANGLE_UNIT ( ) );
#56495=SURFACE_STYLE_USAGE ( .BOTH. , #23441 ) ;
#56497=CARTESIAN_POINT ( 'NONE',  ( -75.00000000000000000, 9.290263934145983171, 6.640705990143894510 ) ) ;
#56500=TOROIDAL_SURFACE ( 'NONE', #29537, 7.500000000000011546, 0.5000000000000000000 ) ;
#56503=DIRECTION ( 'NONE',  ( 0.000000000000000000, 0.000000000000000000, 1.000000000000000000 ) ) ;
#56509=CARTESIAN_POINT ( 'NONE',  ( -10.01517768586949231, 150.3050000000000068, -6.132527647946036459E-16 ) ) ;
#56510=CARTESIAN_POINT ( 'NONE',  ( -48.50000000000000000, 99.99999999999992895, -7.000000000000000000 ) ) ;
#56511=CIRCLE ( 'NONE', #41964, 0.5000000000000004441 ) ;
#56512=UNCERTAINTY_MEASURE_WITH_UNIT (LENGTH_MEASURE( 1.000000000000000082E-05 ), #37966, 'distance_accuracy_value', 'NONE');
#56515=CARTESIAN_POINT ( 'NONE',  ( -20.22843684326250369, 114.9428328902810676, -10.38991920486588327 ) ) ;
#56523=ORIENTED_EDGE ( 'NONE', *, *, #34532, .F. ) ;
#56525=CARTESIAN_POINT ( 'NONE',  ( 71.50000000000000000, 35.92875272052971525, -9.500000000000000000 ) ) ;
#56527=VECTOR ( 'NONE', #34093, 1000.000000000000000 ) ;
#56530=EDGE_CURVE ( 'NONE', #44609, #599, #32028, .T. ) ;
#56533=ORIENTED_EDGE ( 'NONE', *, *, #35286, .F. ) ;
#56536=CARTESIAN_POINT ( 'NONE',  ( -8.102448949553181734, 114.0049999999999812, -5.886773742842749790 ) ) ;
#56539=EDGE_CURVE ( 'NONE', #63248, #19250, #39892, .T. ) ;
#56550=LINE ( 'NONE', #67114, #13905 ) ;
#56551=ORIENTED_EDGE ( 'NONE', *, *, #49043, .T. ) ;
#56552=CARTESIAN_POINT ( 'NONE',  ( 8.437984349512095861, 146.1929263765337907, 1.550032578732817026E-15 ) ) ;
#56557=AXIS2_PLACEMENT_3D ( 'NONE', #20184, #46981, #2927 ) ;
#56567=FACE_BOUND ( 'NONE', #67536, .T. ) ;
#56568=( BOUNDED_CURVE ( )  B_SPLINE_CURVE ( 2, ( #25699, #47930, #299, #64035, #52818, #58768, #26724, #59105, #69331, #36671, #21832 ),
 .UNSPECIFIED., .F., .F. ) 
 B_SPLINE_CURVE_WITH_KNOTS ( ( 3, 2, 2, 2, 2, 3 ),
 ( 0.3235294117647058987, 0.3294117647058823484, 0.3352941176470587981, 0.3411764705882353033, 0.3470588235294117530, 0.3529411764705882582 ),
 .UNSPECIFIED. ) 
 CURVE ( )  GEOMETRIC_REPRESENTATION_ITEM ( )  RATIONAL_B_SPLINE_CURVE ( ( 1.000000000000000000, 0.9510565162951535312, 1.000000000000000000, 0.9510565162951535312, 1.000000000000000000, 0.9510565162951535312, 1.000000000000000000, 0.9510565162951535312, 1.000000000000000000, 0.9510565162951535312, 1.000000000000000000 ) ) 
 REPRESENTATION_ITEM ( '' )  );
#56571=( LENGTH_UNIT ( ) NAMED_UNIT ( * ) SI_UNIT ( .MILLI., .METRE. ) );
#56573=DIRECTION ( 'NONE',  ( -0.7292845505553197105, -0.6842105263157864936, -0.000000000000000000 ) ) ;
#56574=VECTOR ( 'NONE', #60755, 1000.000000000000000 ) ;
#56575=SURFACE_SIDE_STYLE ('',( #40420 ) ) ;
#56581=CARTESIAN_POINT ( 'NONE',  ( 34.99999999999992895, 109.9999999999999858, -9.500000000000000000 ) ) ;
#56583=SURFACE_SIDE_STYLE ('',( #35129 ) ) ;
#56588=DIRECTION ( 'NONE',  ( 0.000000000000000000, 0.000000000000000000, 1.000000000000000000 ) ) ;
#56592=DIRECTION ( 'NONE',  ( 1.000000000000000000, 0.000000000000000000, 0.000000000000000000 ) ) ;
#56594=EDGE_CURVE ( 'NONE', #36214, #53938, #66836, .T. ) ;
#56595=AXIS2_PLACEMENT_3D ( 'NONE', #57547, #13580, #52301 ) ;
#56597=TOROIDAL_SURFACE ( 'NONE', #67797, 16.50000000000000000, 0.5000000000000000000 ) ;
#56600=LINE ( 'NONE', #34447, #35364 ) ;
#56605=CARTESIAN_POINT ( 'NONE',  ( 5.598654528085805993, 115.3549999999999898, 7.705886871421374629 ) ) ;
#56608=AXIS2_PLACEMENT_3D ( 'NONE', #57227, #19936, #15055 ) ;
#56610=UNCERTAINTY_MEASURE_WITH_UNIT (LENGTH_MEASURE( 1.000000000000000082E-05 ), #54495, 'distance_accuracy_value', 'NONE');
#56611=CARTESIAN_POINT ( 'NONE',  ( 41.49999999999997868, 9.999999999999978684, -3.500000000000000000 ) ) ;
#56617=CYLINDRICAL_SURFACE ( 'NONE', #50523, 0.5000000000000004441 ) ;
#56619=EDGE_CURVE ( 'NONE', #3488, #6428, #52173, .T. ) ;
#56624=ORIENTED_EDGE ( 'NONE', *, *, #29954, .F. ) ;
#56628=( GEOMETRIC_REPRESENTATION_CONTEXT ( 3 ) GLOBAL_UNCERTAINTY_ASSIGNED_CONTEXT ( ( #27766 ) ) GLOBAL_UNIT_ASSIGNED_CONTEXT ( ( #24801, #9001, #23776 ) ) REPRESENTATION_CONTEXT ( 'NONE', 'WORKASPACE' ) );
#56630=CIRCLE ( 'NONE', #9446, 8.000000000000007105 ) ;
#56632=SURFACE_STYLE_FILL_AREA ( #61892 ) ;
#56638=CONICAL_SURFACE ( 'NONE', #43236, 8.025000000000000355, 0.7853981633974421728 ) ;
#56639=DIRECTION ( 'NONE',  ( -1.000000000000000000, 0.000000000000000000, 0.000000000000000000 ) ) ;
#56645=EDGE_CURVE ( 'NONE', #53774, #2421, #34283, .T. ) ;
#56647=CARTESIAN_POINT ( 'NONE',  ( 3.094860106618431583, 138.0949999999999989, 9.525000000000000355 ) ) ;
#56649=ORIENTED_EDGE ( 'NONE', *, *, #8824, .F. ) ;
#56650=CARTESIAN_POINT ( 'NONE',  ( 8.102448949553181734, 137.1049999999999898, -5.886773742842746238 ) ) ;
#56654=VERTEX_POINT ( 'NONE', #59841 ) ;
#56655=CARTESIAN_POINT ( 'NONE',  ( -2.607480562269073765, 117.0929263765338249, -8.025000000000000355 ) ) ;
#56662=CARTESIAN_POINT ( 'NONE',  ( 41.11245223800544579, 107.5819305320973172, 3.325569371602613344 ) ) ;
#56663=VERTEX_POINT ( 'NONE', #26760 ) ;
#56674=CARTESIAN_POINT ( 'NONE',  ( 75.00000000000000000, 19.30628705663858113, 7.000000000000000888 ) ) ;
#56677=CARTESIAN_POINT ( 'NONE',  ( -74.50000000000000000, -2.220952357103124925E-14, -9.500000000000000000 ) ) ;
#56680=DIRECTION ( 'NONE',  ( -0.000000000000000000, -0.000000000000000000, -1.000000000000000000 ) ) ;
#56690=AXIS2_PLACEMENT_3D ( 'NONE', #11963, #33419, #13335 ) ;
#56697=CARTESIAN_POINT ( 'NONE',  ( 10.01517768586949231, 135.6949999999999932, 1.839758294383810543E-15 ) ) ;
#56700=UNCERTAINTY_MEASURE_WITH_UNIT (LENGTH_MEASURE( 1.000000000000000082E-05 ), #65621, 'distance_accuracy_value', 'NONE');
#56702=CARTESIAN_POINT ( 'NONE',  ( 47.50000000000000000, 99.99999999999992895, -10.00000000000000000 ) ) ;
#56703=CARTESIAN_POINT ( 'NONE',  ( -41.11245223800543158, 107.5819305320972745, -3.325569371602613788 ) ) ;
#56704=AXIS2_PLACEMENT_3D ( 'NONE', #64715, #22493, #10562 ) ;
#56712=CIRCLE ( 'NONE', #57827, 0.5000000000000004441 ) ;
#56713=SURFACE_SIDE_STYLE ('',( #60924 ) ) ;
#56714=ORIENTED_EDGE ( 'NONE', *, *, #46847, .T. ) ;
#56715=CARTESIAN_POINT ( 'NONE',  ( 0.000000000000000000, 127.0570736234661666, -8.025000000000000355 ) ) ;
#56718=SURFACE_STYLE_FILL_AREA ( #46556 ) ;
#56720=EDGE_CURVE ( 'NONE', #1408, #27268, #5315, .T. ) ;
#56721=FACE_OUTER_BOUND ( 'NONE', #23518, .T. ) ;
#56722=CARTESIAN_POINT ( 'NONE',  ( -45.00000000000000000, 7.967232421023206612, 7.000000003139142279 ) ) ;
#56723=DIRECTION ( 'NONE',  ( 0.000000000000000000, 0.000000000000000000, -1.000000000000000000 ) ) ;
#56725=EDGE_CURVE ( 'NONE', #62320, #63218, #69143, .T. ) ;
#56728=COLOUR_RGB ( '', 0.72549020, 0.75294118, 0.79215686) ;
#56730=SURFACE_STYLE_FILL_AREA ( #35269 ) ;
#56732=( GEOMETRIC_REPRESENTATION_CONTEXT ( 3 ) GLOBAL_UNCERTAINTY_ASSIGNED_CONTEXT ( ( #34112 ) ) GLOBAL_UNIT_ASSIGNED_CONTEXT ( ( #56750, #35289, #40940 ) ) REPRESENTATION_CONTEXT ( 'NONE', 'WORKASPACE' ) );
#56736=CARTESIAN_POINT ( 'NONE',  ( -9.058813317711337021, 116.0449999999999875, -2.943386871421374895 ) ) ;
#56737=( GEOMETRIC_REPRESENTATION_CONTEXT ( 3 ) GLOBAL_UNCERTAINTY_ASSIGNED_CONTEXT ( ( #38409 ) ) GLOBAL_UNIT_ASSIGNED_CONTEXT ( ( #13108, #6788, #44144 ) ) REPRESENTATION_CONTEXT ( 'NONE', 'WORKASPACE' ) );
#56739=DIRECTION ( 'NONE',  ( 1.000000000000000000, 0.000000000000000000, 0.000000000000000000 ) ) ;
#56740=CARTESIAN_POINT ( 'NONE',  ( -10.01517768586949408, 111.3049999999999784, -6.132527647946036459E-16 ) ) ;
#56746=CARTESIAN_POINT ( 'NONE',  ( -5.598654528085806881, 137.8549999999999898, -7.705886871421374629 ) ) ;
#56747=UNCERTAINTY_MEASURE_WITH_UNIT (LENGTH_MEASURE( 1.000000000000000082E-05 ), #30334, 'distance_accuracy_value', 'NONE');
#56748=SURFACE_SIDE_STYLE ('',( #57430 ) ) ;
#56750=( LENGTH_UNIT ( ) NAMED_UNIT ( * ) SI_UNIT ( .MILLI., .METRE. ) );
#56752=( LENGTH_UNIT ( ) NAMED_UNIT ( * ) SI_UNIT ( .MILLI., .METRE. ) );
#56759=DIRECTION ( 'NONE',  ( 0.000000000000000000, 1.000000000000000000, 0.000000000000000000 ) ) ;
#56764=TOROIDAL_SURFACE ( 'NONE', #6232, 22.50000000000000000, 0.5000000000000000000 ) ;
#56768=AXIS2_PLACEMENT_3D ( 'NONE', #37658, #36622, #58040 ) ;
#56770=STYLED_ITEM ( 'NONE', ( #15775 ), #5150 ) ;
#56771=DIRECTION ( 'NONE',  ( 0.000000000000000000, 0.000000000000000000, 1.000000000000000000 ) ) ;
#56772=CARTESIAN_POINT ( 'NONE',  ( -5.598654528085806881, 142.7449999999999761, -7.705886871421374629 ) ) ;
#56776=DIRECTION ( 'NONE',  ( -1.000000000000000000, 0.000000000000000000, 0.000000000000000000 ) ) ;
#56778=AXIS2_PLACEMENT_3D ( 'NONE', #3189, #34913, #2856 ) ;
#56781=CARTESIAN_POINT ( 'NONE',  ( -1.166476076187854022E-15, 110.9449999999999932, 9.525000000000000355 ) ) ;
#56785=FILL_AREA_STYLE_COLOUR ( '', #3241 ) ;
#56786=VERTEX_POINT ( 'NONE', #42337 ) ;
#56787=COLOUR_RGB ( '', 0.09019608, 0.27058824, 0.51372549) ;
#56790=EDGE_CURVE ( 'NONE', #35826, #22128, #63723, .T. ) ;
#56794=ADVANCED_FACE ( 'NONE', ( #39459 ), #7748, .F. ) ;
#56796=CARTESIAN_POINT ( 'NONE',  ( -44.99154893936433552, 9.591540374752316467, -3.000000000000000444 ) ) ;
#56797=CARTESIAN_POINT ( 'NONE',  ( -15.98999599679679839, 118.4999999999999716, -7.000000000000000000 ) ) ;
#56799=ORIENTED_EDGE ( 'NONE', *, *, #24126, .T. ) ;
#56809=EDGE_CURVE ( 'NONE', #64972, #46307, #20838, .T. ) ;
#56810=AXIS2_PLACEMENT_3D ( 'NONE', #6299, #7000, #17585 ) ;
#56813=SURFACE_SIDE_STYLE ('',( #3641 ) ) ;
#56817=AXIS2_PLACEMENT_3D ( 'NONE', #67065, #50197, #56138 ) ;
#56818=CYLINDRICAL_SURFACE ( 'NONE', #39854, 0.5000000000000004441 ) ;
#56819=CARTESIAN_POINT ( 'NONE',  ( 7.632228543268608334, 129.4570736234661581, -2.479861379858951942 ) ) ;
#56821=CARTESIAN_POINT ( 'NONE',  ( 75.00000000000000000, 20.36037961002804053, -6.000000000000000000 ) ) ;
#56823=SURFACE_STYLE_USAGE ( .BOTH. , #35369 ) ;
#56826=TOROIDAL_SURFACE ( 'NONE', #19754, 9.499999999999998224, 0.5000000000000000000 ) ;
#56829=EDGE_CURVE ( 'NONE', #41309, #57325, #28683, .T. ) ;
#56832=DIRECTION ( 'NONE',  ( 1.156482317317873451E-16, 1.000000000000000000, -0.000000000000000000 ) ) ;
#56833=ADVANCED_FACE ( 'NONE', ( #1742 ), #46737, .T. ) ;
#56839=FILL_AREA_STYLE ('',( #66694 ) ) ;
#56840=FILL_AREA_STYLE_COLOUR ( '', #60606 ) ;
#56841=ORIENTED_EDGE ( 'NONE', *, *, #8361, .T. ) ;
#56842=( NAMED_UNIT ( * ) SI_UNIT ( $, .STERADIAN. ) SOLID_ANGLE_UNIT ( ) );
#56846=PRESENTATION_STYLE_ASSIGNMENT (( #51222 ) ) ;
#56849=CARTESIAN_POINT ( 'NONE',  ( -3.094860106618434248, 116.7949999999999733, 9.525000000000000355 ) ) ;
#56852=( LENGTH_UNIT ( ) NAMED_UNIT ( * ) SI_UNIT ( .MILLI., .METRE. ) );
#56854=DIRECTION ( 'NONE',  ( -0.000000000000000000, -1.000000000000000000, -0.000000000000000000 ) ) ;
#56857=DIRECTION ( 'NONE',  ( 0.000000000000000000, 0.000000000000000000, 1.000000000000000000 ) ) ;
#56858=FACE_OUTER_BOUND ( 'NONE', #19023, .T. ) ;
#56870=DIRECTION ( 'NONE',  ( -0.000000000000000000, -0.000000000000000000, -1.000000000000000000 ) ) ;
#56875=CARTESIAN_POINT ( 'NONE',  ( 9.058813317711338797, 157.9549999999999841, -2.943386871421372675 ) ) ;
#56879=DIRECTION ( 'NONE',  ( -0.000000000000000000, -0.000000000000000000, -1.000000000000000000 ) ) ;
#56881=CARTESIAN_POINT ( 'NONE',  ( 40.99999999999998579, 108.0000000000000000, 3.000000000000000000 ) ) ;
#56885=PRESENTATION_STYLE_ASSIGNMENT (( #14674 ) ) ;
#56888=SURFACE_STYLE_FILL_AREA ( #61784 ) ;
#56889=FACE_OUTER_BOUND ( 'NONE', #52031, .T. ) ;
#56890=SURFACE_SIDE_STYLE ('',( #13264 ) ) ;
#56892=ORIENTED_EDGE ( 'NONE', *, *, #28016, .F. ) ;
#56894=VECTOR ( 'NONE', #37161, 1000.000000000000000 ) ;
#56895=SURFACE_STYLE_FILL_AREA ( #61792 ) ;
#56898=CARTESIAN_POINT ( 'NONE',  ( -60.00000000000000000, -2.024042244987997205E-14, 9.500000000000000000 ) ) ;
#56903=PRESENTATION_STYLE_ASSIGNMENT (( #66766 ) ) ;
#56904=DIRECTION ( 'NONE',  ( 0.000000000000000000, 0.000000000000000000, 1.000000000000000000 ) ) ;
#56908=CARTESIAN_POINT ( 'NONE',  ( 6.826472737025121695, 143.4929263765338305, -4.959722759717905660 ) ) ;
#56910=DIRECTION ( 'NONE',  ( -1.000000000000000000, 0.000000000000000000, 0.000000000000000000 ) ) ;
#56916=CARTESIAN_POINT ( 'NONE',  ( 2.607480562269075985, 128.7929263765338135, -8.025000000000000355 ) ) ;
#56918=( NAMED_UNIT ( * ) PLANE_ANGLE_UNIT ( ) SI_UNIT ( $, .RADIAN. ) );
#56923=PRESENTATION_STYLE_ASSIGNMENT (( #2348 ) ) ;
#56926=PRESENTATION_STYLE_ASSIGNMENT (( #8406 ) ) ;
#56927=CARTESIAN_POINT ( 'NONE',  ( -6.826472737025120807, 120.9929263765338021, 4.959722759717906548 ) ) ;
#56930=CARTESIAN_POINT ( 'NONE',  ( -41.49999999999998579, 108.0000000000000000, -3.000000000000000444 ) ) ;
#56931=DIRECTION ( 'NONE',  ( 1.000000000000000000, 0.000000000000000000, 0.000000000000000000 ) ) ;
#56933=CARTESIAN_POINT ( 'NONE',  ( 74.65811388300841145, 19.88603796100278487, 6.000000000000000888 ) ) ;
#56934=ORIENTED_EDGE ( 'NONE', *, *, #38171, .F. ) ;
#56937=DIRECTION ( 'NONE',  ( 0.000000000000000000, 1.000000000000000000, 0.000000000000000000 ) ) ;
#56941=CARTESIAN_POINT ( 'NONE',  ( 40.78947368421051323, 108.1536491499103505, 3.157942443983134506 ) ) ;
#56942=ORIENTED_EDGE ( 'NONE', *, *, #886, .F. ) ;
#56946=SURFACE_STYLE_USAGE ( .BOTH. , #52395 ) ;
#56947=VECTOR ( 'NONE', #24638, 1000.000000000000000 ) ;
#56950=CARTESIAN_POINT ( 'NONE',  ( -9.058813317711337021, 126.1549999999999869, -2.943386871421374895 ) ) ;
#56955=CARTESIAN_POINT ( 'NONE',  ( -75.48275862068965125, 63.99167409976910648, 9.500000000000001776 ) ) ;
#56956=STYLED_ITEM ( 'NONE', ( #65985 ), #50394 ) ;
#56962=EDGE_CURVE ( 'NONE', #19166, #14403, #13726, .T. ) ;
#56967=CARTESIAN_POINT ( 'NONE',  ( -15.98999599679679839, 147.4999999999999716, 9.500000000000000000 ) ) ;
#56972=CARTESIAN_POINT ( 'NONE',  ( 0.000000000000000000, 146.9429263765338192, -8.025000000000000355 ) ) ;
#56974=FILL_AREA_STYLE ('',( #47160 ) ) ;
#56987=CARTESIAN_POINT ( 'NONE',  ( -5.598654528085808657, 140.6449999999999818, 7.705886871421373741 ) ) ;
#56990=DIRECTION ( 'NONE',  ( 1.000000000000000000, 0.000000000000000000, 0.000000000000000000 ) ) ;
#56991=CARTESIAN_POINT ( 'NONE',  ( -8.102448949553179958, 135.6049999999999613, 5.886773742842747126 ) ) ;
#56993=VERTEX_POINT ( 'NONE', #62259 ) ;
#56994=CARTESIAN_POINT ( 'NONE',  ( 7.632228543268607446, 119.0429263765338135, 2.479861379858954606 ) ) ;
#56997=AXIS2_PLACEMENT_3D ( 'NONE', #14707, #35107, #35806 ) ;
#57004=CARTESIAN_POINT ( 'NONE',  ( -12.72792206135785698, 115.4999999999999574, 10.50000000000000000 ) ) ;
#57005=FILL_AREA_STYLE ('',( #4199 ) ) ;
#57009=DIRECTION ( 'NONE',  ( 0.7833176619561811327, 0.6216216216216278179, 4.313366480807235014E-15 ) ) ;
#57010=SURFACE_STYLE_FILL_AREA ( #56308 ) ;
#57011=CARTESIAN_POINT ( 'NONE',  ( -4.716976649647098618, 152.2570736234661695, 6.492361379858953008 ) ) ;
#57012=CARTESIAN_POINT ( 'NONE',  ( 75.00000000000000000, 19.83714805418752292, 6.873786395979866626 ) ) ;
#57022=SURFACE_STYLE_FILL_AREA ( #68281 ) ;
#57026=ORIENTED_EDGE ( 'NONE', *, *, #30962, .T. ) ;
#57027=EDGE_CURVE ( 'NONE', #16746, #50108, #30961, .T. ) ;
#57028=CARTESIAN_POINT ( 'NONE',  ( -75.00000000000000000, 9.657020704707399261, -6.241538579429665390 ) ) ;
#57033=CARTESIAN_POINT ( 'NONE',  ( 9.058813317711338797, 138.8449999999999989, -2.943386871421372675 ) ) ;
#57037=DIRECTION ( 'NONE',  ( 1.156482317317866302E-16, -1.000000000000000000, 1.712231188808094873E-15 ) ) ;
#57038=CARTESIAN_POINT ( 'NONE',  ( -2.607480562268991608, 145.2929263765338419, 8.025000000000060751 ) ) ;
#57041=EDGE_CURVE ( 'NONE', #35366, #31048, #32318, .T. ) ;
#57043=DIRECTION ( 'NONE',  ( -0.000000000000000000, 1.000000000000000000, -0.000000000000000000 ) ) ;
#57045=CIRCLE ( 'NONE', #32330, 13.99999999999999822 ) ;
#57049=FACE_OUTER_BOUND ( 'NONE', #65712, .T. ) ;
#57050=ORIENTED_EDGE ( 'NONE', *, *, #42798, .F. ) ;
#57052=CARTESIAN_POINT ( 'NONE',  ( -44.99999999999999289, 8.411230060885010573, 6.233452521073827413 ) ) ;
#57056=AXIS2_PLACEMENT_3D ( 'NONE', #14992, #68430, #40677 ) ;
#57057=ORIENTED_EDGE ( 'NONE', *, *, #1863, .F. ) ;
#57062=VERTEX_POINT ( 'NONE', #64696 ) ;
#57065=CARTESIAN_POINT ( 'NONE',  ( 8.102448949553181734, 111.3949999999999818, 5.886773742842750679 ) ) ;
#57069=CARTESIAN_POINT ( 'NONE',  ( -5.598654528085806881, 113.8549999999999898, -7.705886871421374629 ) ) ;
#57072=CARTESIAN_POINT ( 'NONE',  ( -3.094860106618434248, 135.9050000000000011, 9.525000000000000355 ) ) ;
#57073=( LENGTH_UNIT ( ) NAMED_UNIT ( * ) SI_UNIT ( .MILLI., .METRE. ) );
#57075=CARTESIAN_POINT ( 'NONE',  ( -40.99999999999998579, 107.7459666924148394, 3.000000000000000000 ) ) ;
#57078=( LENGTH_UNIT ( ) NAMED_UNIT ( * ) SI_UNIT ( .MILLI., .METRE. ) );
#57079=DIRECTION ( 'NONE',  ( 0.000000000000000000, 1.000000000000000000, -0.000000000000000000 ) ) ;
#57082=CARTESIAN_POINT ( 'NONE',  ( 7.968833018235900845, 111.2897112741109567, 3.588351662842293788 ) ) ;
#57085=CARTESIAN_POINT ( 'NONE',  ( -45.00000000000000000, 8.162286782231383597, -6.987283332039737616 ) ) ;
#57087=EDGE_LOOP ( 'NONE', ( #20794, #10664, #35568, #942 ) ) ;
#57090=AXIS2_PLACEMENT_3D ( 'NONE', #27487, #2, #5682 ) ;
#57093=ORIENTED_EDGE ( 'NONE', *, *, #8825, .F. ) ;
#57094=ADVANCED_FACE ( 'NONE', ( #5926 ), #33233, .F. ) ;
#57099=CARTESIAN_POINT ( 'NONE',  ( 5.598654528085809545, 145.1450000000000102, -7.705886871421373741 ) ) ;
#57102=DIRECTION ( 'NONE',  ( -1.000000000000000000, -0.000000000000000000, -0.000000000000000000 ) ) ;
#57104=LINE ( 'NONE', #8926, #65304 ) ;
#57106=CARTESIAN_POINT ( 'NONE',  ( 7.632228543268607446, 120.1570736234661609, 2.479861379858954606 ) ) ;
#57109=( NAMED_UNIT ( * ) PLANE_ANGLE_UNIT ( ) SI_UNIT ( $, .RADIAN. ) );
#57115=PRESENTATION_STYLE_ASSIGNMENT (( #46262 ) ) ;
#57116=DIRECTION ( 'NONE',  ( 0.6216216216216191581, 0.7833176619561879050, 0.000000000000000000 ) ) ;
#57122=TOROIDAL_SURFACE ( 'NONE', #58243, 1.000000000000000000, 0.5000000000000000000 ) ;
#57123=DIRECTION ( 'NONE',  ( 0.000000000000000000, 0.000000000000000000, -1.000000000000000000 ) ) ;
#57127=AXIS2_PLACEMENT_3D ( 'NONE', #19261, #62528, #40768 ) ;
#57128=FILL_AREA_STYLE ('',( #2584 ) ) ;
#57130=COLOUR_RGB ( '', 0.31764706, 0.68627451, 0.89019608) ;
#57131=SURFACE_STYLE_USAGE ( .BOTH. , #24422 ) ;
#57134=CARTESIAN_POINT ( 'NONE',  ( -71.74137931034479720, 63.10081643261027295, -10.00000000000000000 ) ) ;
#57135=PRESENTATION_STYLE_ASSIGNMENT (( #4006 ) ) ;
#57136=ORIENTED_EDGE ( 'NONE', *, *, #22408, .T. ) ;
#57139=CARTESIAN_POINT ( 'NONE',  ( 4.716976649647099507, 129.7570736234661695, -6.492361379858953008 ) ) ;
#57149=CARTESIAN_POINT ( 'NONE',  ( -74.99999999999998579, 50.00000000000000000, 6.500000000000000000 ) ) ;
#57151=ORIENTED_EDGE ( 'NONE', *, *, #60488, .T. ) ;
#57156=ADVANCED_FACE ( 'NONE', ( #55511 ), #54465, .F. ) ;
#57157=( NAMED_UNIT ( * ) SI_UNIT ( $, .STERADIAN. ) SOLID_ANGLE_UNIT ( ) );
#57158=AXIS2_PLACEMENT_3D ( 'NONE', #29334, #23373, #38301 ) ;
#57160=ORIENTED_EDGE ( 'NONE', *, *, #21858, .F. ) ;
#57162=EDGE_CURVE ( 'NONE', #54309, #60087, #47910, .T. ) ;
#57163=DIRECTION ( 'NONE',  ( -0.000000000000000000, -0.000000000000000000, -1.000000000000000000 ) ) ;
#57164=CARTESIAN_POINT ( 'NONE',  ( 12.72792206135785698, 115.4999999999999574, 10.50000000000000000 ) ) ;
#57165=VERTEX_POINT ( 'NONE', #11558 ) ;
#57168=ORIENTED_EDGE ( 'NONE', *, *, #28016, .T. ) ;
#57169=PRESENTATION_STYLE_ASSIGNMENT (( #67385 ) ) ;
#57170=CARTESIAN_POINT ( 'NONE',  ( -9.827790563157511022E-16, 122.5570736234661524, 8.025000000000000355 ) ) ;
#57174=CARTESIAN_POINT ( 'NONE',  ( 65.00000000000000000, 2.409368300552961372E-15, 6.999999999999988454 ) ) ;
#57175=AXIS2_PLACEMENT_3D ( 'NONE', #16728, #65225, #58567 ) ;
#57179=DIRECTION ( 'NONE',  ( 1.000000000000000000, 0.000000000000000000, 0.000000000000000000 ) ) ;
#57181=STYLED_ITEM ( 'NONE', ( #54532 ), #51390 ) ;
#57182=FILL_AREA_STYLE ('',( #51570 ) ) ;
#57187=DIRECTION ( 'NONE',  ( 0.000000000000000000, 0.000000000000000000, 1.000000000000000000 ) ) ;
#57189=CARTESIAN_POINT ( 'NONE',  ( -8.035490232227735063, 111.7463764333768097, 2.031712422923528383 ) ) ;
#57193=EDGE_LOOP ( 'NONE', ( #2242, #23858, #44677, #30358, #49591, #33284, #32856, #32309 ) ) ;
#57197=UNCERTAINTY_MEASURE_WITH_UNIT (LENGTH_MEASURE( 1.000000000000000082E-05 ), #62497, 'distance_accuracy_value', 'NONE');
#57201=CARTESIAN_POINT ( 'NONE',  ( 10.01517768586949231, 160.8049999999999216, 1.839758294383810543E-15 ) ) ;
#57203=CARTESIAN_POINT ( 'NONE',  ( 71.50000000000000000, 14.49137674618942562, -10.00000000000000000 ) ) ;
#57204=DIRECTION ( 'NONE',  ( 0.000000000000000000, 0.000000000000000000, 1.000000000000000000 ) ) ;
#57206=AXIS2_PLACEMENT_3D ( 'NONE', #12164, #18157, #39639 ) ;
#57209=CARTESIAN_POINT ( 'NONE',  ( 0.000000000000000000, 145.0570736234661524, -8.025000000000000355 ) ) ;
#57210=VECTOR ( 'NONE', #50133, 1000.000000000000000 ) ;
#57211=CARTESIAN_POINT ( 'NONE',  ( 45.50000000000000000, 1.797044900979284448E-15, -6.999999999999999112 ) ) ;
#57218=STYLED_ITEM ( 'NONE', ( #3309 ), #10598 ) ;
#57219=ORIENTED_EDGE ( 'NONE', *, *, #31051, .T. ) ;
#57220=( NAMED_UNIT ( * ) PLANE_ANGLE_UNIT ( ) SI_UNIT ( $, .RADIAN. ) );
#57223=AXIS2_PLACEMENT_3D ( 'NONE', #66979, #39224, #12097 ) ;
#57227=CARTESIAN_POINT ( 'NONE',  ( 74.50000000000000000, 3.473944261090200865E-15, 9.500000000000000000 ) ) ;
#57228=ORIENTED_EDGE ( 'NONE', *, *, #29644, .F. ) ;
#57230=SURFACE_STYLE_USAGE ( .BOTH. , #46745 ) ;
#57231=EDGE_LOOP ( 'NONE', ( #39625, #42861, #58355, #10304 ) ) ;
#57232=CARTESIAN_POINT ( 'NONE',  ( 3.094860106618431583, 115.2049999999999983, 9.525000000000000355 ) ) ;
#57234=ORIENTED_EDGE ( 'NONE', *, *, #28096, .T. ) ;
#57237=LINE ( 'NONE', #2321, #18201 ) ;
#57242=FACE_OUTER_BOUND ( 'NONE', #68151, .T. ) ;
#57244=( NAMED_UNIT ( * ) PLANE_ANGLE_UNIT ( ) SI_UNIT ( $, .RADIAN. ) );
#57246=CARTESIAN_POINT ( 'NONE',  ( -8.437984349512095861, 144.6929263765337907, -5.166775262442723748E-16 ) ) ;
#57250=SURFACE_STYLE_FILL_AREA ( #68513 ) ;
#57252=SURFACE_STYLE_USAGE ( .BOTH. , #61470 ) ;
#57254=DIRECTION ( 'NONE',  ( -0.000000000000000000, -1.000000000000000000, 0.000000000000000000 ) ) ;
#57255=FACE_OUTER_BOUND ( 'NONE', #42251, .T. ) ;
#57261=CYLINDRICAL_SURFACE ( 'NONE', #28710, 0.5000000000000004441 ) ;
#57263=CARTESIAN_POINT ( 'NONE',  ( -74.08841717987164088, 9.415467456214850372, 6.077850184675972933 ) ) ;
#57270=EDGE_CURVE ( 'NONE', #27592, #3932, #17537, .T. ) ;
#57272=( LENGTH_UNIT ( ) NAMED_UNIT ( * ) SI_UNIT ( .MILLI., .METRE. ) );
#57274=SURFACE_STYLE_FILL_AREA ( #25945 ) ;
#57276=CARTESIAN_POINT ( 'NONE',  ( 60.00000000000000000, -2.024042244987997205E-14, 10.00000000000000000 ) ) ;
#57279=AXIS2_PLACEMENT_3D ( 'NONE', #54190, #60846, #27778 ) ;
#57281=CIRCLE ( 'NONE', #36012, 10.00000000000000178 ) ;
#57282=ORIENTED_EDGE ( 'NONE', *, *, #3371, .F. ) ;
#57283=SURFACE_STYLE_FILL_AREA ( #15110 ) ;
#57284=SURFACE_STYLE_USAGE ( .BOTH. , #41480 ) ;
#57286=CARTESIAN_POINT ( 'NONE',  ( -41.49999999999998579, 99.99999999999998579, 3.000000000000000000 ) ) ;
#57291=CARTESIAN_POINT ( 'NONE',  ( 9.058813317711337021, 127.6549999999999869, 2.943386871421375783 ) ) ;
#57293=CARTESIAN_POINT ( 'NONE',  ( 71.50000000000000000, 14.49137674618942562, -7.000000000000000000 ) ) ;
#57297=EDGE_CURVE ( 'NONE', #23279, #17642, #32125, .T. ) ;
#57302=ORIENTED_EDGE ( 'NONE', *, *, #19442, .F. ) ;
#57310=ORIENTED_EDGE ( 'NONE', *, *, #58427, .F. ) ;
#57324=FILL_AREA_STYLE ('',( #8108 ) ) ;
#57325=VERTEX_POINT ( 'NONE', #8713 ) ;
#57326=ADVANCED_FACE ( 'NONE', ( #36792 ), #57944, .F. ) ;
#57329=CARTESIAN_POINT ( 'NONE',  ( -3.094860106618434248, 140.7950000000000159, 9.525000000000000355 ) ) ;
#57331=ORIENTED_EDGE ( 'NONE', *, *, #63967, .F. ) ;
#57332=FACE_OUTER_BOUND ( 'NONE', #44620, .T. ) ;
#57333=CARTESIAN_POINT ( 'NONE',  ( 10.01517768586949408, 148.8050000000000068, 1.839758294383810543E-15 ) ) ;
#57336=ORIENTED_EDGE ( 'NONE', *, *, #19865, .F. ) ;
#57337=CARTESIAN_POINT ( 'NONE',  ( 4.716976649647099507, 116.6429263765338078, -6.492361379858953008 ) ) ;
#57338=CARTESIAN_POINT ( 'NONE',  ( 44.99999999999998579, 119.9999999999999716, -9.500000000000000000 ) ) ;
#57339=UNCERTAINTY_MEASURE_WITH_UNIT (LENGTH_MEASURE( 1.000000000000000082E-05 ), #21327, 'distance_accuracy_value', 'NONE');
#57342=CYLINDRICAL_SURFACE ( 'NONE', #25462, 30.00000000000000000 ) ;
#57344=EDGE_CURVE ( 'NONE', #15724, #57165, #66930, .T. ) ;
#57345=PLANE ( 'NONE',  #64662 ) ;
#57349=ORIENTED_EDGE ( 'NONE', *, *, #18872, .F. ) ;
#57352=( NAMED_UNIT ( * ) PLANE_ANGLE_UNIT ( ) SI_UNIT ( $, .RADIAN. ) );
#57353=( LENGTH_UNIT ( ) NAMED_UNIT ( * ) SI_UNIT ( .MILLI., .METRE. ) );
#57357=( LENGTH_UNIT ( ) NAMED_UNIT ( * ) SI_UNIT ( .MILLI., .METRE. ) );
#57358=UNCERTAINTY_MEASURE_WITH_UNIT (LENGTH_MEASURE( 1.000000000000000082E-05 ), #58122, 'distance_accuracy_value', 'NONE');
#57363=CARTESIAN_POINT ( 'NONE',  ( 74.50000000000000000, 19.30628705663858113, 6.500000000000000888 ) ) ;
#57364=CARTESIAN_POINT ( 'NONE',  ( 2.607480562269155921, 145.5929263765338533, 8.024999999999941735 ) ) ;
#57366=STYLED_ITEM ( 'NONE', ( #68825 ), #13601 ) ;
#57369=ADVANCED_FACE ( 'NONE', ( #47347 ), #47720, .T. ) ;
#57370=DIRECTION ( 'NONE',  ( -1.000000000000000000, 0.000000000000000000, 0.000000000000000000 ) ) ;
#57377=EDGE_LOOP ( 'NONE', ( #39491, #9410, #17966, #43231 ) ) ;
#57380=DIRECTION ( 'NONE',  ( -0.000000000000000000, 1.000000000000000000, -0.000000000000000000 ) ) ;
#57382=( BOUNDED_CURVE ( )  B_SPLINE_CURVE ( 2, ( #19052, #52160, #61976, #30653, #3917, #67615, #40561, #19418, #68316, #24339, #14860 ),
 .UNSPECIFIED., .F., .F. ) 
 B_SPLINE_CURVE_WITH_KNOTS ( ( 3, 2, 2, 2, 2, 3 ),
 ( 0.1470588235294118806, 0.1529411764705883026, 0.1588235294117646967, 0.1647058823529411464, 0.1705882352941175684, 0.1764705882352939903 ),
 .UNSPECIFIED. ) 
 CURVE ( )  GEOMETRIC_REPRESENTATION_ITEM ( )  RATIONAL_B_SPLINE_CURVE ( ( 0.9999999999999991118, 0.9510565162951544194, 1.000000000000000000, 0.9510565162951535312, 1.000000000000000000, 0.9510565162951535312, 1.000000000000000000, 0.9510565162951535312, 1.000000000000000000, 0.9510565162951546414, 0.9999999999999988898 ) ) 
 REPRESENTATION_ITEM ( '' )  );
#57383=DIRECTION ( 'NONE',  ( -1.000000000000000000, 0.000000000000000000, 0.000000000000000000 ) ) ;
#57385=CARTESIAN_POINT ( 'NONE',  ( 9.058813317711337021, 144.5449999999999875, 2.943386871421375783 ) ) ;
#57388=DIRECTION ( 'NONE',  ( 0.000000000000000000, 0.000000000000000000, 1.000000000000000000 ) ) ;
#57389=DIRECTION ( 'NONE',  ( 0.000000000000000000, -1.000000000000000000, 0.000000000000000000 ) ) ;
#57391=UNCERTAINTY_MEASURE_WITH_UNIT (LENGTH_MEASURE( 1.000000000000000082E-05 ), #33937, 'distance_accuracy_value', 'NONE');
#57398=FILL_AREA_STYLE_COLOUR ( '', #22497 ) ;
#57401=ORIENTED_EDGE ( 'NONE', *, *, #14299, .F. ) ;
#57404=( BOUNDED_CURVE ( )  B_SPLINE_CURVE ( 2, ( #51299, #45369, #12606, #50602, #55531, #3040, #55874, #39387, #13293, #8035, #61152 ),
 .UNSPECIFIED., .F., .F. ) 
 B_SPLINE_CURVE_WITH_KNOTS ( ( 3, 2, 2, 2, 2, 3 ),
 ( 0.5882352941176473005, 0.5941176470588236391, 0.5999999999999999778, 0.6058823529411763165, 0.6117647058823527662, 0.6176470588235291048 ),
 .UNSPECIFIED. ) 
 CURVE ( )  GEOMETRIC_REPRESENTATION_ITEM ( )  RATIONAL_B_SPLINE_CURVE ( ( 0.9999999999999981126, 0.9510565162951554186, 1.000000000000000000, 0.9510565162951535312, 1.000000000000000000, 0.9510565162951535312, 1.000000000000000000, 0.9510565162951535312, 1.000000000000000000, 0.9510565162951563067, 0.9999999999999972244 ) ) 
 REPRESENTATION_ITEM ( '' )  );
#57405=VECTOR ( 'NONE', #22021, 1000.000000000000000 ) ;
#57406=CARTESIAN_POINT ( 'NONE',  ( -15.48999599679679662, 146.4999999999999716, 9.500000000000000000 ) ) ;
#57408=CARTESIAN_POINT ( 'NONE',  ( 67.50000000000000000, 1.797044900979284448E-15, 12.00000000000000000 ) ) ;
#57413=CARTESIAN_POINT ( 'NONE',  ( -74.50000000000000000, 9.708372675170620525, -6.500000000000000000 ) ) ;
#57414=DIRECTION ( 'NONE',  ( -0.000000000000000000, -1.000000000000000000, -0.000000000000000000 ) ) ;
#57415=ORIENTED_EDGE ( 'NONE', *, *, #22559, .T. ) ;
#57419=CARTESIAN_POINT ( 'NONE',  ( 23.21231517720797655, 117.4999999999999716, -7.500000000000000000 ) ) ;
#57420=CARTESIAN_POINT ( 'NONE',  ( 9.058813317711338797, 111.8449999999999847, -2.943386871421372675 ) ) ;
#57423=CARTESIAN_POINT ( 'NONE',  ( -10.01517768586949408, 123.3049999999999784, -6.132527647946036459E-16 ) ) ;
#57427=ORIENTED_EDGE ( 'NONE', *, *, #64505, .F. ) ;
#57428=CARTESIAN_POINT ( 'NONE',  ( -8.102448949553181734, 138.6049999999999329, 5.886773742842747126 ) ) ;
#57430=SURFACE_STYLE_FILL_AREA ( #8891 ) ;
#57432=DIRECTION ( 'NONE',  ( 0.000000000000000000, 0.000000000000000000, 1.000000000000000000 ) ) ;
#57434=FILL_AREA_STYLE_COLOUR ( '', #2370 ) ;
#57435=EDGE_CURVE ( 'NONE', #31294, #62143, #63814, .T. ) ;
#57440=FACE_OUTER_BOUND ( 'NONE', #37476, .T. ) ;
#57451=ORIENTED_EDGE ( 'NONE', *, *, #42648, .T. ) ;
#57453=EDGE_LOOP ( 'NONE', ( #68066, #30470, #43090, #59230 ) ) ;
#57456=( NAMED_UNIT ( * ) SI_UNIT ( $, .STERADIAN. ) SOLID_ANGLE_UNIT ( ) );
#57457=CARTESIAN_POINT ( 'NONE',  ( 71.49999999999998579, 64.07124727947029896, -7.500000000000000000 ) ) ;
#57464=SURFACE_STYLE_FILL_AREA ( #4304 ) ;
#57466=CARTESIAN_POINT ( 'NONE',  ( -8.102448949553181734, 121.8949999999999818, -5.886773742842749790 ) ) ;
#57468=( NAMED_UNIT ( * ) SI_UNIT ( $, .STERADIAN. ) SOLID_ANGLE_UNIT ( ) );
#57472=ORIENTED_EDGE ( 'NONE', *, *, #5019, .T. ) ;
#57473=DIRECTION ( 'NONE',  ( 1.000000000000000000, 0.000000000000000000, 0.000000000000000000 ) ) ;
#57474=VECTOR ( 'NONE', #7622, 1000.000000000000000 ) ;
#57479=CARTESIAN_POINT ( 'NONE',  ( -44.99678646488361977, 9.646512454965742833, -3.411134130722746072 ) ) ;
#57482=ORIENTED_EDGE ( 'NONE', *, *, #44257, .F. ) ;
#57483=STYLED_ITEM ( 'NONE', ( #10883 ), #35444 ) ;
#57490=FACE_OUTER_BOUND ( 'NONE', #69130, .T. ) ;
#57491=CIRCLE ( 'NONE', #38470, 0.5000000000000004441 ) ;
#57492=DIRECTION ( 'NONE',  ( 1.000000000000000000, 0.000000000000000000, 0.000000000000000000 ) ) ;
#57493=EDGE_CURVE ( 'NONE', #10363, #8139, #66832, .T. ) ;
#57494=VERTEX_POINT ( 'NONE', #44155 ) ;
#57500=FACE_OUTER_BOUND ( 'NONE', #20769, .T. ) ;
#57501=CARTESIAN_POINT ( 'NONE',  ( -4.716976649647098618, 134.2570736234661695, 6.492361379858953008 ) ) ;
#57508=VECTOR ( 'NONE', #42005, 1000.000000000000000 ) ;
#57509=ORIENTED_EDGE ( 'NONE', *, *, #17214, .T. ) ;
#57510=DIRECTION ( 'NONE',  ( 0.000000000000000000, 0.000000000000000000, 1.000000000000000000 ) ) ;
#57511=PRESENTATION_STYLE_ASSIGNMENT (( #47004 ) ) ;
#57513=CARTESIAN_POINT ( 'NONE',  ( 44.99999999999998579, 119.9999999999999716, 7.000000000000000000 ) ) ;
#57520=( LENGTH_UNIT ( ) NAMED_UNIT ( * ) SI_UNIT ( .MILLI., .METRE. ) );
#57526=SURFACE_SIDE_STYLE ('',( #50864 ) ) ;
#57527=FILL_AREA_STYLE ('',( #36466 ) ) ;
#57532=SURFACE_SIDE_STYLE ('',( #24803 ) ) ;
#57534=CARTESIAN_POINT ( 'NONE',  ( -40.82991390394946762, 108.1252238755516828, 3.311222316328668036 ) ) ;
#57536=AXIS2_PLACEMENT_3D ( 'NONE', #33212, #23007, #51130 ) ;
#57537=CARTESIAN_POINT ( 'NONE',  ( -9.058813317711337021, 119.0449999999999875, -2.943386871421374895 ) ) ;
#57540=FILL_AREA_STYLE ('',( #20240 ) ) ;
#57541=FACE_OUTER_BOUND ( 'NONE', #8977, .T. ) ;
#57545=DIRECTION ( 'NONE',  ( 1.000000000000000000, 0.000000000000000000, 0.000000000000000000 ) ) ;
#57547=CARTESIAN_POINT ( 'NONE',  ( 72.49999999999998579, 64.07124727947029896, -9.500000000000000000 ) ) ;
#57548=CARTESIAN_POINT ( 'NONE',  ( -8.468615938765699624, 111.5588028509683198, -0.3477567820242795649 ) ) ;
#57549=CIRCLE ( 'NONE', #66544, 18.50000000000000355 ) ;
#57556=SURFACE_STYLE_USAGE ( .BOTH. , #14652 ) ;
#57557=DIRECTION ( 'NONE',  ( -1.000000000000000000, 0.000000000000000000, 0.000000000000000000 ) ) ;
#57562=CARTESIAN_POINT ( 'NONE',  ( -8.102448949553181734, 153.0050000000000239, -5.886773742842749790 ) ) ;
#57565=DIRECTION ( 'NONE',  ( -0.000000000000000000, -1.000000000000000000, -0.000000000000000000 ) ) ;
#57567=VECTOR ( 'NONE', #49224, 1000.000000000000000 ) ;
#57568=ADVANCED_FACE ( 'NONE', ( #6121 ), #32024, .T. ) ;
#57572=PRESENTATION_STYLE_ASSIGNMENT (( #4416 ) ) ;
#57575=CARTESIAN_POINT ( 'NONE',  ( -34.99999999999992895, 112.9999999999999858, 9.500000000000000000 ) ) ;
#57576=ORIENTED_EDGE ( 'NONE', *, *, #49886, .T. ) ;
#57580=DIRECTION ( 'NONE',  ( 1.000000000000000000, 0.000000000000000000, 0.000000000000000000 ) ) ;
#57581=VECTOR ( 'NONE', #12012, 1000.000000000000000 ) ;
#57582=EDGE_CURVE ( 'NONE', #10638, #43189, #63602, .T. ) ;
#57583=CARTESIAN_POINT ( 'NONE',  ( -20.99026508940074010, 114.7786387612191703, 10.00000000000000000 ) ) ;
#57588=ORIENTED_EDGE ( 'NONE', *, *, #26363, .F. ) ;
#57594=CARTESIAN_POINT ( 'NONE',  ( -3.094860106618434248, 114.9049999999999727, 9.525000000000000355 ) ) ;
#57595=DIRECTION ( 'NONE',  ( 1.000000000000000000, -0.000000000000000000, 0.000000000000000000 ) ) ;
#57596=CARTESIAN_POINT ( 'NONE',  ( 71.50000000000000000, 35.92875272052971525, -7.500000000000000000 ) ) ;
#57597=CONICAL_SURFACE ( 'NONE', #56433, 5.499999999999976907, 0.7853981633974309595 ) ;
#57598=EDGE_CURVE ( 'NONE', #9072, #1577, #63452, .T. ) ;
#57600=VERTEX_POINT ( 'NONE', #18063 ) ;
#57601=VECTOR ( 'NONE', #63684, 1000.000000000000000 ) ;
#57604=DIRECTION ( 'NONE',  ( -1.000000000000000000, 0.000000000000000000, 0.000000000000000000 ) ) ;
#57605=ORIENTED_EDGE ( 'NONE', *, *, #62353, .F. ) ;
#57606=CARTESIAN_POINT ( 'NONE',  ( 6.826472737025119919, 154.8929263765338362, 4.959722759717908325 ) ) ;
#57610=ORIENTED_EDGE ( 'NONE', *, *, #46555, .T. ) ;
#57611=CARTESIAN_POINT ( 'NONE',  ( 19.89974874213240597, 115.4999999999999574, -10.00000000000000000 ) ) ;
#57612=ORIENTED_EDGE ( 'NONE', *, *, #51155, .T. ) ;
#57613=CARTESIAN_POINT ( 'NONE',  ( 20.04013953308945162, 115.4999999999999432, 10.00000000000000000 ) ) ;
#57615=CARTESIAN_POINT ( 'NONE',  ( -60.00000000000000000, -2.024042244987997205E-14, -6.000000000000000000 ) ) ;
#57617=COLOUR_RGB ( '', 0.08235294, 0.09019608, 0.10196078) ;
#57619=CARTESIAN_POINT ( 'NONE',  ( -24.21231517720798010, 113.4999999999999858, -7.500000000000000000 ) ) ;
#57620=EDGE_CURVE ( 'NONE', #320, #6729, #34242, .T. ) ;
#57622=DIRECTION ( 'NONE',  ( -0.000000000000000000, -1.000000000000000000, -0.000000000000000000 ) ) ;
#57623=CIRCLE ( 'NONE', #28405, 0.5000000000000004441 ) ;
#57624=CARTESIAN_POINT ( 'NONE',  ( -74.50000000000000000, 7.768687147774684831, 6.500000000000000000 ) ) ;
#57625=CYLINDRICAL_SURFACE ( 'NONE', #19316, 0.5000000000000004441 ) ;
#57627=ORIENTED_EDGE ( 'NONE', *, *, #59481, .T. ) ;
#57644=CARTESIAN_POINT ( 'NONE',  ( 9.270114131632642085, 154.5000000000000284, -2.232057404141062573 ) ) ;
#57645=DIRECTION ( 'NONE',  ( 0.000000000000000000, 0.000000000000000000, -1.000000000000000000 ) ) ;
#57646=SURFACE_STYLE_FILL_AREA ( #9472 ) ;
#57647=VECTOR ( 'NONE', #34837, 1000.000000000000000 ) ;
#57650=CARTESIAN_POINT ( 'NONE',  ( -1.166476076187854022E-15, 124.0549999999999784, 9.525000000000000355 ) ) ;
#57653=CARTESIAN_POINT ( 'NONE',  ( 20.40217977176331843, 114.8427411095148329, -10.33293932795019465 ) ) ;
#57656=( GEOMETRIC_REPRESENTATION_CONTEXT ( 3 ) GLOBAL_UNCERTAINTY_ASSIGNED_CONTEXT ( ( #25750 ) ) GLOBAL_UNIT_ASSIGNED_CONTEXT ( ( #56227, #7697, #1687 ) ) REPRESENTATION_CONTEXT ( 'NONE', 'WORKASPACE' ) );
#57657=FACE_OUTER_BOUND ( 'NONE', #26269, .T. ) ;
#57658=SPHERICAL_SURFACE ( 'NONE', #46159, 0.5000000000000000000 ) ;
#57666=FACE_OUTER_BOUND ( 'NONE', #22330, .T. ) ;
#57667=ORIENTED_EDGE ( 'NONE', *, *, #21374, .F. ) ;
#57668=AXIS2_PLACEMENT_3D ( 'NONE', #64680, #49541, #11893 ) ;
#57670=SURFACE_STYLE_FILL_AREA ( #15810 ) ;
#57673=COLOUR_RGB ( '', 0.72549020, 0.75294118, 0.79215686) ;
#57675=CARTESIAN_POINT ( 'NONE',  ( -41.84210526315788314, 107.2928455055531600, -4.000000000000000000 ) ) ;
#57676=DIRECTION ( 'NONE',  ( -1.000000000000000000, -0.000000000000000000, -0.000000000000000000 ) ) ;
#57678=ORIENTED_EDGE ( 'NONE', *, *, #53199, .T. ) ;
#57681=LINE ( 'NONE', #8103, #19589 ) ;
#57686=CARTESIAN_POINT ( 'NONE',  ( 48.50000000000000000, 14.49137674618942562, 9.500000000000000000 ) ) ;
#57687=EDGE_LOOP ( 'NONE', ( #14493, #46915, #9726, #45634 ) ) ;
#57688=STYLED_ITEM ( 'NONE', ( #55532 ), #36502 ) ;
#57689=DIRECTION ( 'NONE',  ( 1.000000000000000000, 0.000000000000000000, 0.000000000000000000 ) ) ;
#57690=CARTESIAN_POINT ( 'NONE',  ( 5.598654528085809545, 148.1450000000000102, -7.705886871421373741 ) ) ;
#57693=CARTESIAN_POINT ( 'NONE',  ( 8.102448949553179958, 145.5049999999999670, 5.886773742842750679 ) ) ;
#57694=FACE_OUTER_BOUND ( 'NONE', #15590, .T. ) ;
#57695=FILL_AREA_STYLE_COLOUR ( '', #68910 ) ;
#57696=VECTOR ( 'NONE', #22113, 1000.000000000000000 ) ;
#57698=CARTESIAN_POINT ( 'NONE',  ( 8.437984349512095861, 125.1929263765338192, 1.550032578732817026E-15 ) ) ;
#57699=CARTESIAN_POINT ( 'NONE',  ( 45.00000000000000000, 10.00000000017111468, 6.065867531378962063 ) ) ;
#57700=CIRCLE ( 'NONE', #16199, 16.00000000000000000 ) ;
#57701=VECTOR ( 'NONE', #18875, 1000.000000000000000 ) ;
#57704=VERTEX_POINT ( 'NONE', #23332 ) ;
#57705=CARTESIAN_POINT ( 'NONE',  ( 41.00754902350322340, 107.7352920524769502, 3.098114188008662673 ) ) ;
#57706=ORIENTED_EDGE ( 'NONE', *, *, #7480, .T. ) ;
#57709=SURFACE_STYLE_USAGE ( .BOTH. , #62962 ) ;
#57712=ADVANCED_FACE ( 'NONE', ( #62683 ), #53369, .F. ) ;
#57715=CARTESIAN_POINT ( 'NONE',  ( 0.000000000000000000, 111.9999999999999858, -8.025000000000000355 ) ) ;
#57718=CARTESIAN_POINT ( 'NONE',  ( -34.99999999999992895, 113.4999999999999858, -7.000000000000000000 ) ) ;
#57720=ORIENTED_EDGE ( 'NONE', *, *, #16967, .F. ) ;
#57723=VECTOR ( 'NONE', #3679, 1000.000000000000000 ) ;
#57726=CARTESIAN_POINT ( 'NONE',  ( -48.00000000000000000, 99.99999999999992895, 9.500000000000000000 ) ) ;
#57728=B_SPLINE_CURVE_WITH_KNOTS ( 'NONE', 3,
 ( #19262, #7676, #3760, #51644, #29112, #3400, #62530, #24893, #56208, #50954 ),
 .UNSPECIFIED., .F., .F.,
 ( 4, 2, 2, 2, 4 ),
 ( 0.000000000000000000, 0.0002942714429691380704, 0.0005885428859382761408, 0.0008828143289074142112, 0.001177085771876552282 ),
 .UNSPECIFIED. ) ;
#57734=( GEOMETRIC_REPRESENTATION_CONTEXT ( 3 ) GLOBAL_UNCERTAINTY_ASSIGNED_CONTEXT ( ( #42464 ) ) GLOBAL_UNIT_ASSIGNED_CONTEXT ( ( #39838, #52111, #19369 ) ) REPRESENTATION_CONTEXT ( 'NONE', 'WORKASPACE' ) );
#57737=DIRECTION ( 'NONE',  ( 0.000000000000000000, 0.000000000000000000, 1.000000000000000000 ) ) ;
#57739=CARTESIAN_POINT ( 'NONE',  ( 3.094860106618435136, 148.2949999999999307, -9.525000000000000355 ) ) ;
#57741=EDGE_CURVE ( 'NONE', #27592, #16561, #64145, .T. ) ;
#57743=AXIS2_PLACEMENT_3D ( 'NONE', #27301, #16806, #38280 ) ;
#57745=CARTESIAN_POINT ( 'NONE',  ( -41.25890975875731215, 107.3519676386824671, -3.442113426143909027 ) ) ;
#57752=SURFACE_SIDE_STYLE ('',( #56432 ) ) ;
#57758=ORIENTED_EDGE ( 'NONE', *, *, #1638, .F. ) ;
#57759=CARTESIAN_POINT ( 'NONE',  ( 15.98999599679679839, 146.4999999999999716, -7.000000000000000000 ) ) ;
#57761=ORIENTED_EDGE ( 'NONE', *, *, #60487, .F. ) ;
#57762=EDGE_CURVE ( 'NONE', #57325, #61698, #10681, .T. ) ;
#57765=AXIS2_PLACEMENT_3D ( 'NONE', #8223, #28938, #25086 ) ;
#57766=DIRECTION ( 'NONE',  ( 0.000000000000000000, 0.000000000000000000, -1.000000000000000000 ) ) ;
#57767=CARTESIAN_POINT ( 'NONE',  ( -44.99999999999964473, 8.706976341191598578, 5.725845108613464518 ) ) ;
#57775=FACE_OUTER_BOUND ( 'NONE', #23174, .T. ) ;
#57777=CIRCLE ( 'NONE', #27412, 0.5000000000000004441 ) ;
#57780=CARTESIAN_POINT ( 'NONE',  ( 5.598654528085805993, 117.2449999999999903, 7.705886871421374629 ) ) ;
#57781=EDGE_LOOP ( 'NONE', ( #47615, #24187, #33515, #1059 ) ) ;
#57783=CARTESIAN_POINT ( 'NONE',  ( 5.598654528085809545, 125.2549999999999812, -7.705886871421373741 ) ) ;
#57786=ORIENTED_EDGE ( 'NONE', *, *, #9237, .F. ) ;
#57787=CARTESIAN_POINT ( 'NONE',  ( -9.058813317711337021, 135.1550000000000011, -2.943386871421374895 ) ) ;
#57789=CARTESIAN_POINT ( 'NONE',  ( -15.48999599679679662, 117.9999999999999716, -7.500000000000000000 ) ) ;
#57791=CARTESIAN_POINT ( 'NONE',  ( -55.00000000000000000, -2.024042244987997205E-14, -11.50000000000000355 ) ) ;
#57793=FILL_AREA_STYLE ('',( #30681 ) ) ;
#57794=LINE ( 'NONE', #4278, #57508 ) ;
#57798=( GEOMETRIC_REPRESENTATION_CONTEXT ( 3 ) GLOBAL_UNCERTAINTY_ASSIGNED_CONTEXT ( ( #44718 ) ) GLOBAL_UNIT_ASSIGNED_CONTEXT ( ( #9193, #67223, #50114 ) ) REPRESENTATION_CONTEXT ( 'NONE', 'WORKASPACE' ) );
#57799=CARTESIAN_POINT ( 'NONE',  ( -72.50000000000001421, 14.49137674618942562, -10.00000000000000000 ) ) ;
#57801=FILL_AREA_STYLE ('',( #37778 ) ) ;
#57802=ORIENTED_EDGE ( 'NONE', *, *, #27445, .T. ) ;
#57803=DIRECTION ( 'NONE',  ( 0.000000000000000000, 1.000000000000000000, -0.000000000000000000 ) ) ;
#57809=ORIENTED_EDGE ( 'NONE', *, *, #64732, .F. ) ;
#57813=CARTESIAN_POINT ( 'NONE',  ( 5.598654528085809545, 154.1449999999999818, -7.705886871421373741 ) ) ;
#57816=CIRCLE ( 'NONE', #55538, 0.5000000000000004441 ) ;
#57818=ORIENTED_EDGE ( 'NONE', *, *, #27467, .T. ) ;
#57821=SPHERICAL_SURFACE ( 'NONE', #20123, 0.5000000000000000000 ) ;
#57822=VECTOR ( 'NONE', #23623, 1000.000000000000000 ) ;
#57824=CARTESIAN_POINT ( 'NONE',  ( -9.058813317711338797, 119.3449999999999989, 2.943386871421373563 ) ) ;
#57826=ADVANCED_FACE ( 'NONE', ( #8896 ), #45574, .T. ) ;
#57827=AXIS2_PLACEMENT_3D ( 'NONE', #40480, #35874, #56639 ) ;
#57831=PRESENTATION_STYLE_ASSIGNMENT (( #36413 ) ) ;
#57838=MECHANICAL_DESIGN_GEOMETRIC_PRESENTATION_REPRESENTATION('',(#50016),#34223);
#57839=EDGE_CURVE ( 'NONE', #9072, #20368, #64788, .T. ) ;
#57842=AXIS2_PLACEMENT_3D ( 'NONE', #20570, #42086, #40748 ) ;
#57844=CARTESIAN_POINT ( 'NONE',  ( -20.58910881788679603, 114.8399099445016276, -10.00000000000000355 ) ) ;
#57847=ORIENTED_EDGE ( 'NONE', *, *, #19442, .T. ) ;
#57848=ADVANCED_FACE ( 'NONE', ( #5333, #37421, #32088 ), #4997, .F. ) ;
#57854=CARTESIAN_POINT ( 'NONE',  ( 6.826472737025119919, 151.8929263765337510, 4.959722759717908325 ) ) ;
#57859=DIRECTION ( 'NONE',  ( 0.000000000000000000, 0.000000000000000000, 1.000000000000000000 ) ) ;
#57864=CARTESIAN_POINT ( 'NONE',  ( -34.99999999999992895, 113.4999999999999858, -7.500000000000000000 ) ) ;
#57865=CARTESIAN_POINT ( 'NONE',  ( 7.632228543268607446, 144.1570736234661751, 2.479861379858954606 ) ) ;
#57868=ORIENTED_EDGE ( 'NONE', *, *, #59394, .F. ) ;
#57874=AXIS2_PLACEMENT_3D ( 'NONE', #43157, #46072, #40793 ) ;
#57876=DIRECTION ( 'NONE',  ( -0.000000000000000000, -0.000000000000000000, 1.000000000000000000 ) ) ;
#57877=STYLED_ITEM ( 'NONE', ( #13622 ), #49130 ) ;
#57879=DIRECTION ( 'NONE',  ( 1.000000000000000000, 0.000000000000000000, 0.000000000000000000 ) ) ;
#57884=UNCERTAINTY_MEASURE_WITH_UNIT (LENGTH_MEASURE( 1.000000000000000082E-05 ), #60377, 'distance_accuracy_value', 'NONE');
#57885=ORIENTED_EDGE ( 'NONE', *, *, #45145, .T. ) ;
#57893=PLANE ( 'NONE',  #59362 ) ;
#57895=CARTESIAN_POINT ( 'NONE',  ( -41.26950967128010461, 107.7917145016473910, 3.849034857644454188 ) ) ;
#57897=CARTESIAN_POINT ( 'NONE',  ( -9.058813317711338797, 122.3449999999999847, 2.943386871421373563 ) ) ;
#57900=CARTESIAN_POINT ( 'NONE',  ( 2.607480562269082647, 112.5929263765338106, 8.024999999999993250 ) ) ;
#57901=VECTOR ( 'NONE', #3264, 1000.000000000000000 ) ;
#57902=SURFACE_STYLE_USAGE ( .BOTH. , #20241 ) ;
#57904=SURFACE_SIDE_STYLE ('',( #25518 ) ) ;
#57907=SURFACE_STYLE_USAGE ( .BOTH. , #13939 ) ;
#57910=SURFACE_SIDE_STYLE ('',( #62804 ) ) ;
#57914=ORIENTED_EDGE ( 'NONE', *, *, #13220, .T. ) ;
#57916=EDGE_CURVE ( 'NONE', #25674, #2846, #3927, .T. ) ;
#57918=( GEOMETRIC_REPRESENTATION_CONTEXT ( 3 ) GLOBAL_UNCERTAINTY_ASSIGNED_CONTEXT ( ( #3862 ) ) GLOBAL_UNIT_ASSIGNED_CONTEXT ( ( #13227, #1922, #7284 ) ) REPRESENTATION_CONTEXT ( 'NONE', 'WORKASPACE' ) );
#57921=UNCERTAINTY_MEASURE_WITH_UNIT (LENGTH_MEASURE( 1.000000000000000082E-05 ), #61028, 'distance_accuracy_value', 'NONE');
#57924=AXIS2_PLACEMENT_3D ( 'NONE', #23041, #49432, #11428 ) ;
#57926=CARTESIAN_POINT ( 'NONE',  ( -5.598654528085806881, 152.8549999999999898, -7.705886871421374629 ) ) ;
#57927=EDGE_CURVE ( 'NONE', #48746, #25674, #37751, .T. ) ;
#57928=AXIS2_PLACEMENT_3D ( 'NONE', #53286, #63813, #48046 ) ;
#57929=STYLED_ITEM ( 'NONE', ( #66351 ), #5388 ) ;
#57930=SURFACE_SIDE_STYLE ('',( #63192 ) ) ;
#57933=SURFACE_STYLE_FILL_AREA ( #29432 ) ;
#57937=AXIS2_PLACEMENT_3D ( 'NONE', #57686, #31976, #64333 ) ;
#57940=VECTOR ( 'NONE', #37677, 1000.000000000000000 ) ;
#57942=VERTEX_POINT ( 'NONE', #59855 ) ;
#57944=TOROIDAL_SURFACE ( 'NONE', #27580, 14.49999999999999822, 0.5000000000000000000 ) ;
#57945=CARTESIAN_POINT ( 'NONE',  ( -44.99999999999998579, 119.9999999999999716, 9.500000000000000000 ) ) ;
#57946=AXIS2_PLACEMENT_3D ( 'NONE', #17010, #39874, #61278 ) ;
#57947=CARTESIAN_POINT ( 'NONE',  ( -20.06856914206998610, 114.9886858359306814, 10.44306996520268527 ) ) ;
#57949=( NAMED_UNIT ( * ) PLANE_ANGLE_UNIT ( ) SI_UNIT ( $, .RADIAN. ) );
#57951=ORIENTED_EDGE ( 'NONE', *, *, #5769, .F. ) ;
#57954=ORIENTED_EDGE ( 'NONE', *, *, #4506, .F. ) ;
#57955=CARTESIAN_POINT ( 'NONE',  ( -1.166476076187854022E-15, 121.0549999999999784, 9.525000000000000355 ) ) ;
#57956=DIRECTION ( 'NONE',  ( 0.000000000000000000, 0.000000000000000000, -1.000000000000000000 ) ) ;
#57958=FACE_OUTER_BOUND ( 'NONE', #15045, .T. ) ;
#57960=ORIENTED_EDGE ( 'NONE', *, *, #33913, .F. ) ;
#57961=EDGE_CURVE ( 'NONE', #38966, #25423, #27810, .T. ) ;
#57964=CARTESIAN_POINT ( 'NONE',  ( 7.632228543268608334, 152.3429263765338249, -2.479861379858951942 ) ) ;
#57965=CYLINDRICAL_SURFACE ( 'NONE', #41418, 0.5000000000000004441 ) ;
#57966=MECHANICAL_DESIGN_GEOMETRIC_PRESENTATION_REPRESENTATION('',(#5120),#4001);
#57970=CARTESIAN_POINT ( 'NONE',  ( 20.22778885548742522, 114.9430298377684210, -10.39013442403998866 ) ) ;
#57973=CARTESIAN_POINT ( 'NONE',  ( 48.50000000000000000, 99.99999999999992895, 7.500000000000000000 ) ) ;
#57977=SURFACE_STYLE_FILL_AREA ( #13655 ) ;
#57985=ORIENTED_EDGE ( 'NONE', *, *, #59554, .T. ) ;
#57990=DIRECTION ( 'NONE',  ( 0.000000000000000000, 1.000000000000000000, -0.000000000000000000 ) ) ;
#57995=ADVANCED_FACE ( 'NONE', ( #2800 ), #1689, .F. ) ;
#57997=DIRECTION ( 'NONE',  ( -1.000000000000000000, 0.000000000000000000, 0.000000000000000000 ) ) ;
#58001=( GEOMETRIC_REPRESENTATION_CONTEXT ( 3 ) GLOBAL_UNCERTAINTY_ASSIGNED_CONTEXT ( ( #22883 ) ) GLOBAL_UNIT_ASSIGNED_CONTEXT ( ( #50936, #58548, #67107 ) ) REPRESENTATION_CONTEXT ( 'NONE', 'WORKASPACE' ) );
#58003=( NAMED_UNIT ( * ) SI_UNIT ( $, .STERADIAN. ) SOLID_ANGLE_UNIT ( ) );
#58004=EDGE_CURVE ( 'NONE', #63980, #54030, #65831, .T. ) ;
#58009=DIRECTION ( 'NONE',  ( 0.000000000000000000, 0.000000000000000000, -1.000000000000000000 ) ) ;
#58010=PRESENTATION_STYLE_ASSIGNMENT (( #47124 ) ) ;
#58011=EDGE_CURVE ( 'NONE', #61698, #68819, #17329, .T. ) ;
#58013=CARTESIAN_POINT ( 'NONE',  ( -3.094860106618432471, 128.7049999999999841, -9.525000000000000355 ) ) ;
#58019=UNCERTAINTY_MEASURE_WITH_UNIT (LENGTH_MEASURE( 1.000000000000000082E-05 ), #44649, 'distance_accuracy_value', 'NONE');
#58025=VECTOR ( 'NONE', #46036, 1000.000000000000000 ) ;
#58026=DIRECTION ( 'NONE',  ( 1.000000000000000000, -0.000000000000000000, 0.000000000000000000 ) ) ;
#58027=DIRECTION ( 'NONE',  ( -0.9704308468600219006, -0.2413793103448194921, -0.000000000000000000 ) ) ;
#58028=ORIENTED_EDGE ( 'NONE', *, *, #66467, .F. ) ;
#58029=ORIENTED_EDGE ( 'NONE', *, *, #68149, .T. ) ;
#58030=CARTESIAN_POINT ( 'NONE',  ( -45.57139843939562240, 8.073466093857248893, -6.500000000000084377 ) ) ;
#58034=( NAMED_UNIT ( * ) PLANE_ANGLE_UNIT ( ) SI_UNIT ( $, .RADIAN. ) );
#58035=DIRECTION ( 'NONE',  ( 0.000000000000000000, 0.000000000000000000, -1.000000000000000000 ) ) ;
#58036=LINE ( 'NONE', #47877, #12755 ) ;
#58040=DIRECTION ( 'NONE',  ( -1.000000000000000000, 1.541976423090494529E-14, 0.000000000000000000 ) ) ;
#58042=CARTESIAN_POINT ( 'NONE',  ( 20.99028635741426640, 114.7785533247281933, -10.00000000000000000 ) ) ;
#58044=CARTESIAN_POINT ( 'NONE',  ( 23.71231517720798010, 113.4999999999999858, 7.000000000000000000 ) ) ;
#58046=DIRECTION ( 'NONE',  ( 1.000000000000000000, 0.000000000000000000, 0.000000000000000000 ) ) ;
#58047=CARTESIAN_POINT ( 'NONE',  ( -9.058813317711337021, 146.0449999999999875, -2.943386871421374895 ) ) ;
#58050=ORIENTED_EDGE ( 'NONE', *, *, #46482, .F. ) ;
#58051=CARTESIAN_POINT ( 'NONE',  ( -3.094860106618432471, 149.7049999999999557, -9.525000000000000355 ) ) ;
#58052=SURFACE_STYLE_USAGE ( .BOTH. , #24977 ) ;
#58053=ORIENTED_EDGE ( 'NONE', *, *, #2822, .T. ) ;
#58054=CARTESIAN_POINT ( 'NONE',  ( 4.716976649647096842, 121.7429263765338163, 6.492361379858953896 ) ) ;
#58056=UNCERTAINTY_MEASURE_WITH_UNIT (LENGTH_MEASURE( 1.000000000000000082E-05 ), #8196, 'distance_accuracy_value', 'NONE');
#58058=CARTESIAN_POINT ( 'NONE',  ( 45.65811388300841855, 10.21937129433612235, 6.000000000000000888 ) ) ;
#58062=CARTESIAN_POINT ( 'NONE',  ( -40.78947368421051323, 108.1536491499103505, -3.000000000000000444 ) ) ;
#58065=DIRECTION ( 'NONE',  ( -1.000000000000000000, 0.000000000000000000, 0.000000000000000000 ) ) ;
#58068=CARTESIAN_POINT ( 'NONE',  ( 15.98999599679679839, 117.4999999999999716, -9.500000000000000000 ) ) ;
#58073=CARTESIAN_POINT ( 'NONE',  ( 74.59716837049619187, 19.66257108179090096, 6.399833413891846234 ) ) ;
#58074=DIRECTION ( 'NONE',  ( 0.000000000000000000, -6.938893903907222067E-15, 1.000000000000000000 ) ) ;
#58084=CARTESIAN_POINT ( 'NONE',  ( 34.99999999999999289, 146.4999999999999716, 7.500000000000000000 ) ) ;
#58086=( GEOMETRIC_REPRESENTATION_CONTEXT ( 3 ) GLOBAL_UNCERTAINTY_ASSIGNED_CONTEXT ( ( #67964 ) ) GLOBAL_UNIT_ASSIGNED_CONTEXT ( ( #50689, #29568, #41207 ) ) REPRESENTATION_CONTEXT ( 'NONE', 'WORKASPACE' ) );
#58089=VERTEX_POINT ( 'NONE', #9177 ) ;
#58090=EDGE_CURVE ( 'NONE', #22128, #21243, #58523, .T. ) ;
#58092=SURFACE_STYLE_USAGE ( .BOTH. , #4950 ) ;
#58094=STYLED_ITEM ( 'NONE', ( #20036 ), #40798 ) ;
#58095=CARTESIAN_POINT ( 'NONE',  ( 0.000000000000000000, 148.4449999999999932, -9.525000000000000355 ) ) ;
#58100=CARTESIAN_POINT ( 'NONE',  ( 72.50000000000000000, 1.797044900979284448E-15, -9.500000000000000000 ) ) ;
#58106=EDGE_CURVE ( 'NONE', #53591, #62231, #53465, .T. ) ;
#58107=FILL_AREA_STYLE ('',( #36689 ) ) ;
#58110=ORIENTED_EDGE ( 'NONE', *, *, #63058, .T. ) ;
#58112=B_SPLINE_CURVE_WITH_KNOTS ( 'NONE', 3,
 ( #25586, #51306, #41463, #13660, #35123, #19635, #9097, #67474 ),
 .UNSPECIFIED., .F., .F.,
 ( 4, 2, 2, 4 ),
 ( 0.000000000000000000, 0.0002394028614865243657, 0.0004788057229730487314, 0.0009576114459460974629 ),
 .UNSPECIFIED. ) ;
#58114=( NAMED_UNIT ( * ) PLANE_ANGLE_UNIT ( ) SI_UNIT ( $, .RADIAN. ) );
#58115=CARTESIAN_POINT ( 'NONE',  ( -45.00000000000000000, 8.442834901059519837, 5.542315673751926575 ) ) ;
#58118=VERTEX_POINT ( 'NONE', #46855 ) ;
#58120=MECHANICAL_DESIGN_GEOMETRIC_PRESENTATION_REPRESENTATION('',(#26646),#51379);
#58122=( LENGTH_UNIT ( ) NAMED_UNIT ( * ) SI_UNIT ( .MILLI., .METRE. ) );
#58123=PRESENTATION_STYLE_ASSIGNMENT (( #36705 ) ) ;
#58125=CARTESIAN_POINT ( 'NONE',  ( -1.166476076187854022E-15, 119.9449999999999790, 9.525000000000000355 ) ) ;
#58128=DIRECTION ( 'NONE',  ( 0.000000000000000000, -1.000000000000000000, 0.000000000000000000 ) ) ;
#58129=CARTESIAN_POINT ( 'NONE',  ( -8.102448949553179958, 117.6049999999999898, 5.886773742842747126 ) ) ;
#58131=( NAMED_UNIT ( * ) PLANE_ANGLE_UNIT ( ) SI_UNIT ( $, .RADIAN. ) );
#58132=ORIENTED_EDGE ( 'NONE', *, *, #4, .T. ) ;
#58133=CARTESIAN_POINT ( 'NONE',  ( -5.598654528085808657, 147.7549999999999955, 7.705886871421373741 ) ) ;
#58134=UNCERTAINTY_MEASURE_WITH_UNIT (LENGTH_MEASURE( 1.000000000000000082E-05 ), #5623, 'distance_accuracy_value', 'NONE');
#58136=STYLED_ITEM ( 'NONE', ( #61917 ), #40879 ) ;
#58138=EDGE_CURVE ( 'NONE', #19090, #19777, #30593, .T. ) ;
#58139=VERTEX_POINT ( 'NONE', #68260 ) ;
#58147=DIRECTION ( 'NONE',  ( 0.000000000000000000, 0.000000000000000000, 1.000000000000000000 ) ) ;
#58150=SURFACE_SIDE_STYLE ('',( #15266 ) ) ;
#58157=CARTESIAN_POINT ( 'NONE',  ( -48.81081081081080697, 14.09971791521132900, -9.500000000000000000 ) ) ;
#58159=CARTESIAN_POINT ( 'NONE',  ( 3.094860106618435136, 148.2949999999999591, -9.525000000000000355 ) ) ;
#58161=STYLED_ITEM ( 'NONE', ( #30984 ), #66905 ) ;
#58162=ORIENTED_EDGE ( 'NONE', *, *, #47197, .T. ) ;
#58164=STYLED_ITEM ( 'NONE', ( #62175 ), #58471 ) ;
#58169=CARTESIAN_POINT ( 'NONE',  ( 0.000000000000000000, 115.4449999999999932, -9.525000000000000355 ) ) ;
#58178=PLANE ( 'NONE',  #21995 ) ;
#58179=CARTESIAN_POINT ( 'NONE',  ( -20.55683252178218723, 114.6388620567782084, -10.28289609742943078 ) ) ;
#58184=DIRECTION ( 'NONE',  ( 0.000000000000000000, 0.000000000000000000, 1.000000000000000000 ) ) ;
#58185=CARTESIAN_POINT ( 'NONE',  ( -74.08452722063037754, 9.430195807687216103, 6.000000000000000888 ) ) ;
#58188=ORIENTED_EDGE ( 'NONE', *, *, #32984, .F. ) ;
#58190=CARTESIAN_POINT ( 'NONE',  ( -9.827790563157511022E-16, 137.5570736234661808, 8.025000000000000355 ) ) ;
#58194=CARTESIAN_POINT ( 'NONE',  ( 54.99999999999999289, 2.409368300552961372E-15, -12.00000000000000000 ) ) ;
#58195=CARTESIAN_POINT ( 'NONE',  ( 8.437984349512095861, 141.3070736234661524, 1.550032578732817026E-15 ) ) ;
#58200=UNCERTAINTY_MEASURE_WITH_UNIT (LENGTH_MEASURE( 1.000000000000000082E-05 ), #13019, 'distance_accuracy_value', 'NONE');
#58203=CIRCLE ( 'NONE', #39106, 5.000000000000004441 ) ;
#58204=LINE ( 'NONE', #58901, #27555 ) ;
#58207=ADVANCED_FACE ( 'NONE', ( #63320 ), #57345, .F. ) ;
#58213=SURFACE_STYLE_FILL_AREA ( #21611 ) ;
#58215=ORIENTED_EDGE ( 'NONE', *, *, #67853, .T. ) ;
#58218=MECHANICAL_DESIGN_GEOMETRIC_PRESENTATION_REPRESENTATION('',(#33507),#1946);
#58220=FACE_OUTER_BOUND ( 'NONE', #1654, .T. ) ;
#58225=( NAMED_UNIT ( * ) PLANE_ANGLE_UNIT ( ) SI_UNIT ( $, .RADIAN. ) );
#58227=SURFACE_STYLE_FILL_AREA ( #47745 ) ;
#58230=CARTESIAN_POINT ( 'NONE',  ( 3.094860106618431583, 120.0949999999999847, 9.525000000000000355 ) ) ;
#58232=EDGE_CURVE ( 'NONE', #65858, #61027, #47901, .T. ) ;
#58236=DIRECTION ( 'NONE',  ( 1.000000000000000000, 0.000000000000000000, 0.000000000000000000 ) ) ;
#58238=CARTESIAN_POINT ( 'NONE',  ( -71.18918918918917882, 14.09971791521133255, 7.000000000000000000 ) ) ;
#58239=EDGE_CURVE ( 'NONE', #67189, #47061, #53125, .T. ) ;
#58241=FACE_OUTER_BOUND ( 'NONE', #24496, .T. ) ;
#58243=AXIS2_PLACEMENT_3D ( 'NONE', #36351, #14867, #58454 ) ;
#58248=CARTESIAN_POINT ( 'NONE',  ( 20.74545326270968459, 149.7621816065244218, -9.931116503619028535 ) ) ;
#58250=MECHANICAL_DESIGN_GEOMETRIC_PRESENTATION_REPRESENTATION('',(#20017),#27880);
#58251=CARTESIAN_POINT ( 'NONE',  ( -10.01517768586949231, 153.3050000000000068, -6.132527647946036459E-16 ) ) ;
#58253=( NAMED_UNIT ( * ) PLANE_ANGLE_UNIT ( ) SI_UNIT ( $, .RADIAN. ) );
#58257=STYLED_ITEM ( 'NONE', ( #3033 ), #953 ) ;
#58260=DIRECTION ( 'NONE',  ( 0.000000000000000000, 0.000000000000000000, 1.000000000000000000 ) ) ;
#58264=SURFACE_SIDE_STYLE ('',( #59274 ) ) ;
#58265=EDGE_LOOP ( 'NONE', ( #40173, #53108, #58188, #61459 ) ) ;
#58268=CARTESIAN_POINT ( 'NONE',  ( 7.632228543268608334, 117.4570736234661581, -2.479861379858951942 ) ) ;
#58269=CIRCLE ( 'NONE', #25722, 18.00000000000000355 ) ;
#58275=ORIENTED_EDGE ( 'NONE', *, *, #64901, .F. ) ;
#58277=CARTESIAN_POINT ( 'NONE',  ( -20.74545326270968459, 149.7621816065244218, 9.931116503619028535 ) ) ;
#58278=ORIENTED_EDGE ( 'NONE', *, *, #12870, .T. ) ;
#58279=CARTESIAN_POINT ( 'NONE',  ( 9.058813317711337021, 121.6549999999999869, 2.943386871421375783 ) ) ;
#58289=CARTESIAN_POINT ( 'NONE',  ( 5.806870487293831928, 153.9760667166096084, -6.889211357469143593 ) ) ;
#58291=CARTESIAN_POINT ( 'NONE',  ( -2.607480562269075097, 157.2929263765338135, 8.025000000000000355 ) ) ;
#58294=AXIS2_PLACEMENT_3D ( 'NONE', #5031, #26482, #48008 ) ;
#58296=CARTESIAN_POINT ( 'NONE',  ( -20.94636006565341191, 149.9999999999999716, -9.500000000000000000 ) ) ;
#58298=EDGE_CURVE ( 'NONE', #34398, #36960, #11877, .T. ) ;
#58300=CARTESIAN_POINT ( 'NONE',  ( -14.98999599679679662, 117.9999999999999716, 9.500000000000000000 ) ) ;
#58303=MECHANICAL_DESIGN_GEOMETRIC_PRESENTATION_REPRESENTATION('',(#42578),#67295);
#58305=STYLED_ITEM ( 'NONE', ( #17925 ), #19772 ) ;
#58307=CARTESIAN_POINT ( 'NONE',  ( -74.20353070810536167, 8.974048487541153918, 6.364280603494544941 ) ) ;
#58308=ADVANCED_FACE ( 'NONE', ( #33045 ), #263, .T. ) ;
#58309=DIRECTION ( 'NONE',  ( 0.7071067811865352493, 0.000000000000000000, 0.7071067811865597852 ) ) ;
#58313=AXIS2_PLACEMENT_3D ( 'NONE', #47840, #16137, #37957 ) ;
#58316=DIRECTION ( 'NONE',  ( 0.000000000000000000, 0.000000000000000000, 1.000000000000000000 ) ) ;
#58317=LINE ( 'NONE', #5508, #42476 ) ;
#58328=CARTESIAN_POINT ( 'NONE',  ( 34.99999999999999289, 99.99999999999998579, -9.500000000000000000 ) ) ;
#58330=( LENGTH_UNIT ( ) NAMED_UNIT ( * ) SI_UNIT ( .MILLI., .METRE. ) );
#58333=CARTESIAN_POINT ( 'NONE',  ( -5.598654528085808657, 126.7549999999999812, 7.705886871421373741 ) ) ;
#58335=AXIS2_PLACEMENT_3D ( 'NONE', #38620, #48472, #55074 ) ;
#58348=( GEOMETRIC_REPRESENTATION_CONTEXT ( 3 ) GLOBAL_UNCERTAINTY_ASSIGNED_CONTEXT ( ( #17254 ) ) GLOBAL_UNIT_ASSIGNED_CONTEXT ( ( #58853, #54249, #64478 ) ) REPRESENTATION_CONTEXT ( 'NONE', 'WORKASPACE' ) );
#58352=CARTESIAN_POINT ( 'NONE',  ( -7.632228543268608334, 147.8429263765338249, 2.479861379858952830 ) ) ;
#58355=ORIENTED_EDGE ( 'NONE', *, *, #49800, .F. ) ;
#58360=CARTESIAN_POINT ( 'NONE',  ( 4.716976649647099507, 129.7570736234661695, -6.492361379858953008 ) ) ;
#58361=EDGE_CURVE ( 'NONE', #41081, #3021, #55161, .T. ) ;
#58362=ORIENTED_EDGE ( 'NONE', *, *, #34871, .F. ) ;
#58364=DIRECTION ( 'NONE',  ( -0.000000000000000000, 1.000000000000000000, -0.000000000000000000 ) ) ;
#58365=ORIENTED_EDGE ( 'NONE', *, *, #28585, .F. ) ;
#58367=CIRCLE ( 'NONE', #61704, 26.99999999999999645 ) ;
#58368=CARTESIAN_POINT ( 'NONE',  ( -3.094860106618434248, 149.7949999999999875, 9.525000000000000355 ) ) ;
#58371=ORIENTED_EDGE ( 'NONE', *, *, #31270, .T. ) ;
#58373=CARTESIAN_POINT ( 'NONE',  ( -8.102448949553179958, 153.6049999999999898, 5.886773742842747126 ) ) ;
#58378=CARTESIAN_POINT ( 'NONE',  ( -8.437984349512095861, 123.6929263765338192, -5.166775262442723748E-16 ) ) ;
#58381=PRESENTATION_STYLE_ASSIGNMENT (( #20401 ) ) ;
#58382=SURFACE_SIDE_STYLE ('',( #47544 ) ) ;
#58384=DIRECTION ( 'NONE',  ( -1.156482317317873451E-16, -1.000000000000000000, 0.000000000000000000 ) ) ;
#58389=PLANE ( 'NONE',  #17703 ) ;
#58393=( NAMED_UNIT ( * ) PLANE_ANGLE_UNIT ( ) SI_UNIT ( $, .RADIAN. ) );
#58395=TOROIDAL_SURFACE ( 'NONE', #28026, 26.49999999999999645, 0.5000000000000000000 ) ;
#58397=PRESENTATION_STYLE_ASSIGNMENT (( #63672 ) ) ;
#58400=VERTEX_POINT ( 'NONE', #34415 ) ;
#58401=STYLED_ITEM ( 'NONE', ( #52056 ), #51511 ) ;
#58416=CARTESIAN_POINT ( 'NONE',  ( -71.18918918918917882, 14.09971791521133255, 9.500000000000000000 ) ) ;
#58419=CARTESIAN_POINT ( 'NONE',  ( -74.50000000000000000, -2.208799022165584366E-14, -10.00000000000000000 ) ) ;
#58421=CARTESIAN_POINT ( 'NONE',  ( 5.598654528085809545, 145.1450000000000102, -7.705886871421373741 ) ) ;
#58424=VECTOR ( 'NONE', #6813, 1000.000000000000114 ) ;
#58427=EDGE_CURVE ( 'NONE', #61023, #60866, #9654, .T. ) ;
#58428=CYLINDRICAL_SURFACE ( 'NONE', #51689, 0.5000000000000004441 ) ;
#58434=SURFACE_STYLE_FILL_AREA ( #21848 ) ;
#58435=AXIS2_PLACEMENT_3D ( 'NONE', #49598, #43332, #7016 ) ;
#58439=( GEOMETRIC_REPRESENTATION_CONTEXT ( 3 ) GLOBAL_UNCERTAINTY_ASSIGNED_CONTEXT ( ( #59489 ) ) GLOBAL_UNIT_ASSIGNED_CONTEXT ( ( #5556, #37652, #54104 ) ) REPRESENTATION_CONTEXT ( 'NONE', 'WORKASPACE' ) );
#58440=DIRECTION ( 'NONE',  ( 0.000000000000000000, 0.000000000000000000, 1.000000000000000000 ) ) ;
#58442=EDGE_CURVE ( 'NONE', #28999, #40918, #53994, .T. ) ;
#58445=CARTESIAN_POINT ( 'NONE',  ( -9.827790563157511022E-16, 118.4429263765338192, 8.025000000000000355 ) ) ;
#58453=ORIENTED_EDGE ( 'NONE', *, *, #63772, .T. ) ;
#58454=DIRECTION ( 'NONE',  ( 0.000000000000000000, 0.000000000000000000, 1.000000000000000000 ) ) ;
#58456=ORIENTED_EDGE ( 'NONE', *, *, #69275, .F. ) ;
#58460=CARTESIAN_POINT ( 'NONE',  ( 5.598654528085805993, 123.2449999999999903, 7.705886871421374629 ) ) ;
#58461=DIRECTION ( 'NONE',  ( -1.000000000000000000, 0.000000000000000000, 0.000000000000000000 ) ) ;
#58463=CARTESIAN_POINT ( 'NONE',  ( -8.102448949553179958, 123.0049999999999955, -5.886773742842749790 ) ) ;
#58466=CARTESIAN_POINT ( 'NONE',  ( -60.00000000000000000, -2.024042244987997205E-14, 6.999999999999995559 ) ) ;
#58468=CARTESIAN_POINT ( 'NONE',  ( 9.058813317711338797, 151.9550000000000125, -2.943386871421372675 ) ) ;
#58469=AXIS2_PLACEMENT_3D ( 'NONE', #14298, #63185, #15026 ) ;
#58471=ADVANCED_FACE ( 'NONE', ( #1305 ), #7578, .F. ) ;
#58472=CARTESIAN_POINT ( 'NONE',  ( 20.71462257042833599, 114.4999999999999574, 10.00000000000000000 ) ) ;
#58474=CARTESIAN_POINT ( 'NONE',  ( 44.99999999999998579, 119.9999999999999716, 7.500000000000000000 ) ) ;
#58476=SURFACE_SIDE_STYLE ('',( #26778 ) ) ;
#58479=ORIENTED_EDGE ( 'NONE', *, *, #4944, .F. ) ;
#58481=FILL_AREA_STYLE_COLOUR ( '', #15550 ) ;
#58483=AXIS2_PLACEMENT_3D ( 'NONE', #50721, #3887, #29602 ) ;
#58485=VERTEX_POINT ( 'NONE', #44336 ) ;
#58486=SURFACE_SIDE_STYLE ('',( #48669 ) ) ;
#58488=ORIENTED_EDGE ( 'NONE', *, *, #4174, .T. ) ;
#58489=DIRECTION ( 'NONE',  ( -0.000000000000000000, -0.000000000000000000, -1.000000000000000000 ) ) ;
#58492=MECHANICAL_DESIGN_GEOMETRIC_PRESENTATION_REPRESENTATION('',(#29245),#32659);
#58494=EDGE_CURVE ( 'NONE', #9170, #29261, #61483, .T. ) ;
#58496=CARTESIAN_POINT ( 'NONE',  ( -5.598654528085808657, 149.6450000000000102, 7.705886871421373741 ) ) ;
#58500=EDGE_LOOP ( 'NONE', ( #5565, #13866, #11491, #4891 ) ) ;
#58502=AXIS2_PLACEMENT_3D ( 'NONE', #58883, #16350, #36433 ) ;
#58506=CARTESIAN_POINT ( 'NONE',  ( 5.598654528085809545, 121.1449999999999818, -7.705886871421373741 ) ) ;
#58509=CONICAL_SURFACE ( 'NONE', #22558, 8.025000000000000355, 0.7853981633974491672 ) ;
#58513=COLOUR_RGB ( '', 0.72549020, 0.75294118, 0.79215686) ;
#58518=SURFACE_STYLE_USAGE ( .BOTH. , #25464 ) ;
#58519=EDGE_LOOP ( 'NONE', ( #37583, #58988, #20103, #60795 ) ) ;
#58522=CARTESIAN_POINT ( 'NONE',  ( 71.49999999999998579, 64.07124727947029896, 7.500000000000000000 ) ) ;
#58523=( BOUNDED_CURVE ( )  B_SPLINE_CURVE ( 3, ( #52783, #52101, #14799, #36639 ),
 .UNSPECIFIED., .F., .F. ) 
 B_SPLINE_CURVE_WITH_KNOTS ( ( 4, 4 ),
 ( 1.570796326794896558, 3.141592653589793116 ),
 .UNSPECIFIED. ) 
 CURVE ( )  GEOMETRIC_REPRESENTATION_ITEM ( )  RATIONAL_B_SPLINE_CURVE ( ( 1.000000000000000000, 0.8047378541243649375, 0.8047378541243649375, 1.000000000000000000 ) ) 
 REPRESENTATION_ITEM ( '' )  );
#58531=ORIENTED_EDGE ( 'NONE', *, *, #36259, .T. ) ;
#58533=MECHANICAL_DESIGN_GEOMETRIC_PRESENTATION_REPRESENTATION('',(#2317),#68692);
#58535=DIRECTION ( 'NONE',  ( -0.000000000000000000, 1.000000000000000000, -0.000000000000000000 ) ) ;
#58536=AXIS2_PLACEMENT_3D ( 'NONE', #60497, #8704, #62145 ) ;
#58537=DIRECTION ( 'NONE',  ( 1.000000000000000000, 0.000000000000000000, 0.000000000000000000 ) ) ;
#58538=CARTESIAN_POINT ( 'NONE',  ( 6.826472737025119919, 141.0070736234661695, 4.959722759717908325 ) ) ;
#58539=STYLED_ITEM ( 'NONE', ( #48878 ), #53616 ) ;
#58540=VERTEX_POINT ( 'NONE', #19954 ) ;
#58547=CARTESIAN_POINT ( 'NONE',  ( 6.826472737025119919, 142.8929263765338078, 4.959722759717908325 ) ) ;
#58548=( NAMED_UNIT ( * ) PLANE_ANGLE_UNIT ( ) SI_UNIT ( $, .RADIAN. ) );
#58554=MECHANICAL_DESIGN_GEOMETRIC_PRESENTATION_REPRESENTATION('',(#15902),#54074);
#58555=CARTESIAN_POINT ( 'NONE',  ( -9.827790563157511022E-16, 142.4429263765338192, 8.025000000000000355 ) ) ;
#58556=DIRECTION ( 'NONE',  ( -0.000000000000000000, -0.000000000000000000, 1.000000000000000000 ) ) ;
#58558=EDGE_LOOP ( 'NONE', ( #41436, #39234, #64917, #49936 ) ) ;
#58560=CARTESIAN_POINT ( 'NONE',  ( -21.02379604162863913, 110.4999999999999858, -10.50000000000000000 ) ) ;
#58563=( NAMED_UNIT ( * ) SI_UNIT ( $, .STERADIAN. ) SOLID_ANGLE_UNIT ( ) );
#58567=DIRECTION ( 'NONE',  ( 0.000000000000000000, 0.000000000000000000, 1.000000000000000000 ) ) ;
#58569=DIRECTION ( 'NONE',  ( -0.000000000000000000, 1.000000000000000000, -0.000000000000000000 ) ) ;
#58573=CARTESIAN_POINT ( 'NONE',  ( -1.166476076187854022E-15, 122.9449999999999790, 9.525000000000000355 ) ) ;
#58576=STYLED_ITEM ( 'NONE', ( #66020 ), #12527 ) ;
#58579=DIRECTION ( 'NONE',  ( -1.000000000000000000, 0.000000000000000000, 0.000000000000000000 ) ) ;
#58581=CARTESIAN_POINT ( 'NONE',  ( -6.826472737025120807, 131.1070736234661638, 4.959722759717906548 ) ) ;
#58588=VECTOR ( 'NONE', #59647, 1000.000000000000000 ) ;
#58593=FILL_AREA_STYLE ('',( #15701 ) ) ;
#58594=UNCERTAINTY_MEASURE_WITH_UNIT (LENGTH_MEASURE( 1.000000000000000082E-05 ), #4162, 'distance_accuracy_value', 'NONE');
#58597=CARTESIAN_POINT ( 'NONE',  ( 0.000000000000000000, 87.30187232391182306, 0.000000000000000000 ) ) ;
#58598=STYLED_ITEM ( 'NONE', ( #17345 ), #18369 ) ;
#58600=DIRECTION ( 'NONE',  ( -1.000000000000000000, 0.000000000000000000, 0.000000000000000000 ) ) ;
#58611=FACE_OUTER_BOUND ( 'NONE', #66818, .T. ) ;
#58612=ORIENTED_EDGE ( 'NONE', *, *, #40737, .T. ) ;
#58613=( NAMED_UNIT ( * ) PLANE_ANGLE_UNIT ( ) SI_UNIT ( $, .RADIAN. ) );
#58614=AXIS2_PLACEMENT_3D ( 'NONE', #9141, #31244, #35528 ) ;
#58615=ADVANCED_FACE ( 'NONE', ( #36551 ), #526, .F. ) ;
#58617=CARTESIAN_POINT ( 'NONE',  ( 0.000000000000000000, 118.0570736234661524, -8.025000000000000355 ) ) ;
#58621=CARTESIAN_POINT ( 'NONE',  ( -20.56511377093078252, 115.3174848394179435, 10.00000000000000000 ) ) ;
#58622=AXIS2_PLACEMENT_3D ( 'NONE', #64933, #44236, #6892 ) ;
#58623=( NAMED_UNIT ( * ) PLANE_ANGLE_UNIT ( ) SI_UNIT ( $, .RADIAN. ) );
#58624=ORIENTED_EDGE ( 'NONE', *, *, #16163, .F. ) ;
#58627=CARTESIAN_POINT ( 'NONE',  ( -15.98999599679679839, 117.9999999999999716, -7.500000000000000000 ) ) ;
#58630=EDGE_LOOP ( 'NONE', ( #69385, #11024, #69359, #37384 ) ) ;
#58631=CARTESIAN_POINT ( 'NONE',  ( -3.094860106618432471, 119.7049999999999983, -9.525000000000000355 ) ) ;
#58638=CARTESIAN_POINT ( 'NONE',  ( 3.151604648985912416, 154.2021441917068216, -8.710059496740715446 ) ) ;
#58640=ORIENTED_EDGE ( 'NONE', *, *, #27479, .F. ) ;
#58641=CARTESIAN_POINT ( 'NONE',  ( -2.607480562269073765, 150.0929263765338533, -8.025000000000000355 ) ) ;
#58644=CIRCLE ( 'NONE', #14890, 0.5000000000000004441 ) ;
#58645=CARTESIAN_POINT ( 'NONE',  ( 20.57648122633967347, 114.5694469452588038, -10.27659575647942169 ) ) ;
#58646=ORIENTED_EDGE ( 'NONE', *, *, #45789, .T. ) ;
#58654=VERTEX_POINT ( 'NONE', #37237 ) ;
#58656=CARTESIAN_POINT ( 'NONE',  ( -20.71231517720798010, 149.9999999999999716, -10.00000000000000000 ) ) ;
#58657=CYLINDRICAL_SURFACE ( 'NONE', #54758, 5.000000000000004441 ) ;
#58667=DIRECTION ( 'NONE',  ( -0.000000000000000000, -0.000000000000000000, -1.000000000000000000 ) ) ;
#58672=TOROIDAL_SURFACE ( 'NONE', #2433, 17.50000000000000000, 0.5000000000000000000 ) ;
#58673=CARTESIAN_POINT ( 'NONE',  ( -75.01595440434799400, 35.98078654237776419, -9.636386880385824583 ) ) ;
#58675=CARTESIAN_POINT ( 'NONE',  ( 3.094860106618431583, 136.2049999999999557, 9.525000000000000355 ) ) ;
#58678=EDGE_CURVE ( 'NONE', #38619, #46060, #40194, .T. ) ;
#58683=UNCERTAINTY_MEASURE_WITH_UNIT (LENGTH_MEASURE( 1.000000000000000082E-05 ), #52363, 'distance_accuracy_value', 'NONE');
#58684=EDGE_CURVE ( 'NONE', #16390, #60144, #46648, .T. ) ;
#58686=DIRECTION ( 'NONE',  ( 0.000000000000000000, 0.000000000000000000, 1.000000000000000000 ) ) ;
#58687=ADVANCED_FACE ( 'NONE', ( #172 ), #55442, .T. ) ;
#58688=ORIENTED_EDGE ( 'NONE', *, *, #8726, .F. ) ;
#58689=VECTOR ( 'NONE', #14000, 1000.000000000000000 ) ;
#58690=FACE_OUTER_BOUND ( 'NONE', #62445, .T. ) ;
#58692=( GEOMETRIC_REPRESENTATION_CONTEXT ( 3 ) GLOBAL_UNCERTAINTY_ASSIGNED_CONTEXT ( ( #32085 ) ) GLOBAL_UNIT_ASSIGNED_CONTEXT ( ( #6399, #50717, #60900 ) ) REPRESENTATION_CONTEXT ( 'NONE', 'WORKASPACE' ) );
#58698=CARTESIAN_POINT ( 'NONE',  ( -8.437984349512095861, 136.8070736234661808, -5.166775262442723748E-16 ) ) ;
#58701=SURFACE_SIDE_STYLE ('',( #57670 ) ) ;
#58705=VECTOR ( 'NONE', #26927, 1000.000000000000000 ) ;
#58707=FACE_OUTER_BOUND ( 'NONE', #10649, .T. ) ;
#58709=CARTESIAN_POINT ( 'NONE',  ( 7.632228543268608334, 140.3429263765338249, -2.479861379858951942 ) ) ;
#58712=B_SPLINE_CURVE_WITH_KNOTS ( 'NONE', 3,
 ( #15380, #48087, #68127, #68460, #58248, #10072, #69161, #20967 ),
 .UNSPECIFIED., .F., .F.,
 ( 4, 2, 2, 4 ),
 ( 0.000000000000000000, 0.0004110476197876519158, 0.0006165714296814797440, 0.0008220952395753075180 ),
 .UNSPECIFIED. ) ;
#58713=ORIENTED_EDGE ( 'NONE', *, *, #61075, .T. ) ;
#58715=( NAMED_UNIT ( * ) PLANE_ANGLE_UNIT ( ) SI_UNIT ( $, .RADIAN. ) );
#58717=( NAMED_UNIT ( * ) PLANE_ANGLE_UNIT ( ) SI_UNIT ( $, .RADIAN. ) );
#58720=( NAMED_UNIT ( * ) SI_UNIT ( $, .STERADIAN. ) SOLID_ANGLE_UNIT ( ) );
#58721=CARTESIAN_POINT ( 'NONE',  ( -5.598654528085808657, 149.6450000000000102, 7.705886871421373741 ) ) ;
#58723=ORIENTED_EDGE ( 'NONE', *, *, #66305, .T. ) ;
#58724=AXIS2_PLACEMENT_3D ( 'NONE', #18681, #29571, #66877 ) ;
#58726=CARTESIAN_POINT ( 'NONE',  ( 9.058813317711337021, 145.6549999999999727, 2.943386871421375783 ) ) ;
#58729=ORIENTED_EDGE ( 'NONE', *, *, #50987, .T. ) ;
#58730=CARTESIAN_POINT ( 'NONE',  ( 7.632228543268607446, 122.0429263765338135, 2.479861379858954606 ) ) ;
#58737=EDGE_LOOP ( 'NONE', ( #45074, #56714, #68889, #35102, #61652, #43466 ) ) ;
#58742=CARTESIAN_POINT ( 'NONE',  ( -74.99999999999998579, 50.00000000000000000, -6.500000000000000000 ) ) ;
#58745=AXIS2_PLACEMENT_3D ( 'NONE', #46935, #10302, #20125 ) ;
#58746=DIRECTION ( 'NONE',  ( 1.000000000000000000, 0.000000000000000000, 0.000000000000000000 ) ) ;
#58747=CYLINDRICAL_SURFACE ( 'NONE', #64219, 0.5000000000000004441 ) ;
#58749=EDGE_CURVE ( 'NONE', #40244, #31294, #19033, .T. ) ;
#58750=( GEOMETRIC_REPRESENTATION_CONTEXT ( 3 ) GLOBAL_UNCERTAINTY_ASSIGNED_CONTEXT ( ( #48955 ) ) GLOBAL_UNIT_ASSIGNED_CONTEXT ( ( #51460, #3946, #14183 ) ) REPRESENTATION_CONTEXT ( 'NONE', 'WORKASPACE' ) );
#58752=ORIENTED_EDGE ( 'NONE', *, *, #24456, .T. ) ;
#58754=DIRECTION ( 'NONE',  ( 0.000000000000000000, -1.000000000000000000, 0.000000000000000000 ) ) ;
#58755=TOROIDAL_SURFACE ( 'NONE', #11536, 7.499999999999998224, 0.5000000000000000000 ) ;
#58761=FILL_AREA_STYLE ('',( #32026 ) ) ;
#58766=CARTESIAN_POINT ( 'NONE',  ( -12.72792206135785698, 149.9999999999999716, 10.00000000000000000 ) ) ;
#58768=CARTESIAN_POINT ( 'NONE',  ( 8.437984349512095861, 126.3070736234661524, 1.550032578732816828E-15 ) ) ;
#58771=CARTESIAN_POINT ( 'NONE',  ( -9.058813317711338797, 146.3449999999999989, 2.943386871421373563 ) ) ;
#58780=ORIENTED_EDGE ( 'NONE', *, *, #46357, .T. ) ;
#58785=EDGE_CURVE ( 'NONE', #20552, #48146, #14534, .T. ) ;
#58793=CARTESIAN_POINT ( 'NONE',  ( -45.00000000000000000, 8.681192140609645946, 5.652915417256442865 ) ) ;
#58795=DIRECTION ( 'NONE',  ( 0.000000000000000000, -0.000000000000000000, -1.000000000000000000 ) ) ;
#58798=EDGE_LOOP ( 'NONE', ( #38237, #19677, #40579, #28826 ) ) ;
#58801=VERTEX_POINT ( 'NONE', #50525 ) ;
#58806=CARTESIAN_POINT ( 'NONE',  ( -1.166476076187854022E-15, 122.9449999999999790, 9.525000000000000355 ) ) ;
#58807=CARTESIAN_POINT ( 'NONE',  ( 75.00000000000000000, -2.215169945516535778E-14, 10.00000000000000000 ) ) ;
#58808=STYLED_ITEM ( 'NONE', ( #29048 ), #26656 ) ;
#58810=( GEOMETRIC_REPRESENTATION_CONTEXT ( 3 ) GLOBAL_UNCERTAINTY_ASSIGNED_CONTEXT ( ( #65839 ) ) GLOBAL_UNIT_ASSIGNED_CONTEXT ( ( #55583, #63199, #30827 ) ) REPRESENTATION_CONTEXT ( 'NONE', 'WORKASPACE' ) );
#58811=DIRECTION ( 'NONE',  ( 1.000000000000000000, -0.000000000000000000, -0.000000000000000000 ) ) ;
#58812=CARTESIAN_POINT ( 'NONE',  ( -9.058813317711337021, 117.1549999999999869, -2.943386871421374895 ) ) ;
#58815=CARTESIAN_POINT ( 'NONE',  ( -41.27334858134337026, 107.3315027881082528, -3.464507624620943638 ) ) ;
#58816=ORIENTED_EDGE ( 'NONE', *, *, #25244, .F. ) ;
#58817=CARTESIAN_POINT ( 'NONE',  ( -5.598654528085806881, 143.8549999999999898, -7.705886871421374629 ) ) ;
#58818=UNCERTAINTY_MEASURE_WITH_UNIT (LENGTH_MEASURE( 1.000000000000000082E-05 ), #53224, 'distance_accuracy_value', 'NONE');
#58819=CARTESIAN_POINT ( 'NONE',  ( -65.49999999999998579, 50.00000000000000000, -10.49999999999999822 ) ) ;
#58820=AXIS2_PLACEMENT_3D ( 'NONE', #65551, #33539, #7161 ) ;
#58822=FACE_OUTER_BOUND ( 'NONE', #981, .T. ) ;
#58825=FILL_AREA_STYLE ('',( #14895 ) ) ;
#58828=FILL_AREA_STYLE ('',( #27132 ) ) ;
#58830=( GEOMETRIC_REPRESENTATION_CONTEXT ( 3 ) GLOBAL_UNCERTAINTY_ASSIGNED_CONTEXT ( ( #63522 ) ) GLOBAL_UNIT_ASSIGNED_CONTEXT ( ( #170, #44844, #32252 ) ) REPRESENTATION_CONTEXT ( 'NONE', 'WORKASPACE' ) );
#58831=( LENGTH_UNIT ( ) NAMED_UNIT ( * ) SI_UNIT ( .MILLI., .METRE. ) );
#58832=MECHANICAL_DESIGN_GEOMETRIC_PRESENTATION_REPRESENTATION('',(#28468),#37545);
#58833=SURFACE_SIDE_STYLE ('',( #44439 ) ) ;
#58834=ORIENTED_EDGE ( 'NONE', *, *, #21949, .F. ) ;
#58838=ORIENTED_EDGE ( 'NONE', *, *, #28569, .F. ) ;
#58839=LINE ( 'NONE', #48677, #18294 ) ;
#58840=( NAMED_UNIT ( * ) PLANE_ANGLE_UNIT ( ) SI_UNIT ( $, .RADIAN. ) );
#58844=CARTESIAN_POINT ( 'NONE',  ( -9.827790563157511022E-16, 143.5570736234661524, 8.025000000000000355 ) ) ;
#58845=CARTESIAN_POINT ( 'NONE',  ( 0.000000000000000000, 148.4449999999999932, -9.525000000000000355 ) ) ;
#58853=( LENGTH_UNIT ( ) NAMED_UNIT ( * ) SI_UNIT ( .MILLI., .METRE. ) );
#58857=AXIS2_PLACEMENT_3D ( 'NONE', #38320, #33006, #38673 ) ;
#58859=EDGE_CURVE ( 'NONE', #4364, #60894, #58367, .T. ) ;
#58860=CARTESIAN_POINT ( 'NONE',  ( 5.598654528085805993, 123.2449999999999903, 7.705886871421374629 ) ) ;
#58864=FACE_OUTER_BOUND ( 'NONE', #19751, .T. ) ;
#58866=CIRCLE ( 'NONE', #63375, 0.5000000000000004441 ) ;
#58874=ADVANCED_FACE ( 'NONE', ( #24123 ), #46317, .F. ) ;
#58878=ORIENTED_EDGE ( 'NONE', *, *, #7588, .T. ) ;
#58880=CARTESIAN_POINT ( 'NONE',  ( -71.74137931034479720, 63.10081643261027295, 10.00000000000000000 ) ) ;
#58881=( NAMED_UNIT ( * ) PLANE_ANGLE_UNIT ( ) SI_UNIT ( $, .RADIAN. ) );
#58882=EDGE_CURVE ( 'NONE', #32302, #20280, #51216, .T. ) ;
#58883=CARTESIAN_POINT ( 'NONE',  ( 74.99999999999998579, 50.00000000000000000, -7.500000000000000000 ) ) ;
#58887=CIRCLE ( 'NONE', #44372, 0.5000000000000004441 ) ;
#58888=ORIENTED_EDGE ( 'NONE', *, *, #29136, .F. ) ;
#58890=SURFACE_STYLE_FILL_AREA ( #16692 ) ;
#58891=AXIS2_PLACEMENT_3D ( 'NONE', #19540, #25172, #36091 ) ;
#58893=CARTESIAN_POINT ( 'NONE',  ( -8.437984349512095861, 142.8070736234661808, -5.166775262442723748E-16 ) ) ;
#58894=MECHANICAL_DESIGN_GEOMETRIC_PRESENTATION_REPRESENTATION('',(#6064),#45429);
#58895=TOROIDAL_SURFACE ( 'NONE', #64515, 1.000000000000000000, 0.5000000000000000000 ) ;
#58899=UNCERTAINTY_MEASURE_WITH_UNIT (LENGTH_MEASURE( 1.000000000000000082E-05 ), #3012, 'distance_accuracy_value', 'NONE');
#58901=CARTESIAN_POINT ( 'NONE',  ( -23.21231517720797655, 112.9999999999999858, 10.00000000000000000 ) ) ;
#58903=FILL_AREA_STYLE_COLOUR ( '', #36538 ) ;
#58904=SURFACE_STYLE_FILL_AREA ( #32859 ) ;
#58905=DIRECTION ( 'NONE',  ( -1.000000000000000000, 0.000000000000000000, 0.000000000000000000 ) ) ;
#58906=VERTEX_POINT ( 'NONE', #41035 ) ;
#58907=DIRECTION ( 'NONE',  ( 1.000000000000000000, 0.000000000000000000, 0.000000000000000000 ) ) ;
#58909=ORIENTED_EDGE ( 'NONE', *, *, #24694, .T. ) ;
#58910=LINE ( 'NONE', #26851, #48564 ) ;
#58912=EDGE_CURVE ( 'NONE', #5399, #15891, #35881, .T. ) ;
#58913=MECHANICAL_DESIGN_GEOMETRIC_PRESENTATION_REPRESENTATION('',(#64537),#13962);
#58914=CARTESIAN_POINT ( 'NONE',  ( -48.50000000000000000, 14.49137674618942562, 9.500000000000000000 ) ) ;
#58915=CARTESIAN_POINT ( 'NONE',  ( -71.99999999999998579, 119.9999999999997868, 7.000000000000000000 ) ) ;
#58916=ORIENTED_EDGE ( 'NONE', *, *, #4708, .T. ) ;
#58917=( NAMED_UNIT ( * ) SI_UNIT ( $, .STERADIAN. ) SOLID_ANGLE_UNIT ( ) );
#58919=AXIS2_PLACEMENT_3D ( 'NONE', #55642, #67232, #18708 ) ;
#58920=CARTESIAN_POINT ( 'NONE',  ( 72.00000000000000000, 35.92875272052971525, -10.00000000000000000 ) ) ;
#58922=VERTEX_POINT ( 'NONE', #30413 ) ;
#58925=DIRECTION ( 'NONE',  ( -0.000000000000000000, -0.000000000000000000, 1.000000000000000000 ) ) ;
#58926=COLOUR_RGB ( '', 0.31764706, 0.68627451, 0.89019608) ;
#58929=CARTESIAN_POINT ( 'NONE',  ( 5.598654528085805993, 123.2449999999999903, 7.705886871421374629 ) ) ;
#58932=DIRECTION ( 'NONE',  ( -0.000000000000000000, 1.000000000000000000, -0.000000000000000000 ) ) ;
#58937=ADVANCED_FACE ( 'NONE', ( #31118 ), #64179, .F. ) ;
#58945=ORIENTED_EDGE ( 'NONE', *, *, #11718, .F. ) ;
#58946=( BOUNDED_SURFACE ( )  B_SPLINE_SURFACE ( 3, 2, ( 
 ( #16383, #1130, #55968 ),
 ( #13397, #29585, #43808 ),
 ( #23961, #56310, #21982 ),
 ( #13060, #38546, #34515 ),
 ( #49087, #11755, #774 ),
 ( #24304, #18696, #54661 ) ),
 .UNSPECIFIED., .F., .F., .F. ) 
 B_SPLINE_SURFACE_WITH_KNOTS ( ( 4, 2, 4 ),
 ( 3, 3 ),
 ( 1.570796326794896558, 2.356194490192344837, 3.141592653589793116 ),
 ( 0.000000000000000000, 1.000000000000000000 ),
 .UNSPECIFIED. ) 
 GEOMETRIC_REPRESENTATION_ITEM ( )  RATIONAL_B_SPLINE_SURFACE ( (
 ( 1.000000000000000000, 0.7071067811865523467, 1.000000000000000000),
 ( 1.000000000000000000, 0.6778979487215957001, 1.000000000000000000),
 ( 1.000000000000000000, 0.6465434225954497238, 1.000000000000000000),
 ( 1.000000000000000000, 0.5995650817090790730, 1.000000000000000000),
 ( 1.000000000000000000, 0.5843845446918550790, 1.000000000000000000),
 ( 1.000000000000000000, 0.5847102846637692863, 1.000000000000000000) ) ) 
 REPRESENTATION_ITEM ( '' )  SURFACE ( )  );
#58947=CARTESIAN_POINT ( 'NONE',  ( 44.58498124287053344, 10.41703377194147073, -3.499556662980365829 ) ) ;
#58950=CARTESIAN_POINT ( 'NONE',  ( -15.48999599679679662, 117.9999999999999716, -7.000000000000000000 ) ) ;
#58954=DIRECTION ( 'NONE',  ( -0.000000000000000000, 1.000000000000000000, -0.000000000000000000 ) ) ;
#58957=( GEOMETRIC_REPRESENTATION_CONTEXT ( 3 ) GLOBAL_UNCERTAINTY_ASSIGNED_CONTEXT ( ( #50417 ) ) GLOBAL_UNIT_ASSIGNED_CONTEXT ( ( #52037, #24924, #63268 ) ) REPRESENTATION_CONTEXT ( 'NONE', 'WORKASPACE' ) );
#58964=EDGE_CURVE ( 'NONE', #40506, #2776, #15711, .T. ) ;
#58965=DIRECTION ( 'NONE',  ( 0.000000000000000000, 0.000000000000000000, 1.000000000000000000 ) ) ;
#58966=CARTESIAN_POINT ( 'NONE',  ( -60.00000000000000000, -2.024042244987997205E-14, -6.500000000000000000 ) ) ;
#58967=VECTOR ( 'NONE', #46379, 1000.000000000000114 ) ;
#58969=CARTESIAN_POINT ( 'NONE',  ( 15.48999599679679662, 146.9999999999999716, 7.000000000000000000 ) ) ;
#58970=STYLED_ITEM ( 'NONE', ( #61304 ), #6072 ) ;
#58972=CARTESIAN_POINT ( 'NONE',  ( -7.632228543268607446, 109.6570736234661609, -2.479861379858953718 ) ) ;
#58977=CARTESIAN_POINT ( 'NONE',  ( -20.76401515593078884, 149.8168068008927492, 9.892342186632994583 ) ) ;
#58979=CARTESIAN_POINT ( 'NONE',  ( -5.598654528085808657, 129.7549999999999955, 7.705886871421373741 ) ) ;
#58980=FILL_AREA_STYLE_COLOUR ( '', #53510 ) ;
#58981=SURFACE_STYLE_FILL_AREA ( #31539 ) ;
#58986=( NAMED_UNIT ( * ) SI_UNIT ( $, .STERADIAN. ) SOLID_ANGLE_UNIT ( ) );
#58987=AXIS2_PLACEMENT_3D ( 'NONE', #28368, #39678, #61767 ) ;
#58988=ORIENTED_EDGE ( 'NONE', *, *, #30114, .F. ) ;
#58989=CARTESIAN_POINT ( 'NONE',  ( 0.000000000000000000, 152.9429263765338192, -8.025000000000000355 ) ) ;
#58990=CARTESIAN_POINT ( 'NONE',  ( -74.99999999999998579, 64.49137674618943095, -9.500000000000000000 ) ) ;
#58993=ADVANCED_FACE ( 'NONE', ( #64543 ), #58946, .T. ) ;
#58995=EDGE_LOOP ( 'NONE', ( #43024, #51603, #65462, #3282 ) ) ;
#59000=MECHANICAL_DESIGN_GEOMETRIC_PRESENTATION_REPRESENTATION('',(#68015),#42246);
#59001=EDGE_CURVE ( 'NONE', #66131, #13709, #22313, .T. ) ;
#59002=FACE_OUTER_BOUND ( 'NONE', #44194, .T. ) ;
#59004=CARTESIAN_POINT ( 'NONE',  ( -5.038399427696178101, 153.9194349410952043, 7.410012812680824013 ) ) ;
#59006=ORIENTED_EDGE ( 'NONE', *, *, #6435, .T. ) ;
#59008=DIRECTION ( 'NONE',  ( 0.000000000000000000, 1.000000000000000000, 0.000000000000000000 ) ) ;
#59011=FACE_OUTER_BOUND ( 'NONE', #17900, .T. ) ;
#59013=CARTESIAN_POINT ( 'NONE',  ( -47.50000000000000000, 13.41640786499872284, 9.500000000000000000 ) ) ;
#59019=( GEOMETRIC_REPRESENTATION_CONTEXT ( 3 ) GLOBAL_UNCERTAINTY_ASSIGNED_CONTEXT ( ( #15023 ) ) GLOBAL_UNIT_ASSIGNED_CONTEXT ( ( #594, #43612, #59741 ) ) REPRESENTATION_CONTEXT ( 'NONE', 'WORKASPACE' ) );
#59029=CARTESIAN_POINT ( 'NONE',  ( -74.49999999999998579, 36.50926243676796190, -10.00000000000000000 ) ) ;
#59032=CARTESIAN_POINT ( 'NONE',  ( 9.058813317711338797, 139.9549999999999841, -2.943386871421372675 ) ) ;
#59033=MECHANICAL_DESIGN_GEOMETRIC_PRESENTATION_REPRESENTATION('',(#68044),#23087);
#59037=PRESENTATION_STYLE_ASSIGNMENT (( #32631 ) ) ;
#59039=CIRCLE ( 'NONE', #44477, 0.4999999999999991118 ) ;
#59040=DIRECTION ( 'NONE',  ( 0.7071067811865549002, 8.659560562355021605E-17, -0.7071067811865402453 ) ) ;
#59041=( NAMED_UNIT ( * ) SI_UNIT ( $, .STERADIAN. ) SOLID_ANGLE_UNIT ( ) );
#59042=( LENGTH_UNIT ( ) NAMED_UNIT ( * ) SI_UNIT ( .MILLI., .METRE. ) );
#59045=ORIENTED_EDGE ( 'NONE', *, *, #8369, .T. ) ;
#59046=DIRECTION ( 'NONE',  ( -0.000000000000000000, -0.000000000000000000, 1.000000000000000000 ) ) ;
#59048=CARTESIAN_POINT ( 'NONE',  ( -4.716976649647098618, 148.1429263765338078, 6.492361379858953008 ) ) ;
#59049=CYLINDRICAL_SURFACE ( 'NONE', #59934, 8.025000000000000355 ) ;
#59054=CARTESIAN_POINT ( 'NONE',  ( 74.65811388300841145, 19.88603796100278487, 6.000000000000000888 ) ) ;
#59056=SPHERICAL_SURFACE ( 'NONE', #9996, 0.5000000000000000000 ) ;
#59057=CARTESIAN_POINT ( 'NONE',  ( -60.00000000000000000, -2.024042244987997205E-14, 12.00000000000000000 ) ) ;
#59062=CARTESIAN_POINT ( 'NONE',  ( -9.058813317711338797, 155.3449999999999704, 2.943386871421373563 ) ) ;
#59065=FILL_AREA_STYLE ('',( #11916 ) ) ;
#59067=VERTEX_POINT ( 'NONE', #59938 ) ;
#59068=CARTESIAN_POINT ( 'NONE',  ( 7.632228543268607446, 125.0429263765337993, 2.479861379858954606 ) ) ;
#59072=CIRCLE ( 'NONE', #12976, 4.999999999999997335 ) ;
#59082=DIRECTION ( 'NONE',  ( 0.000000000000000000, 0.000000000000000000, 1.000000000000000000 ) ) ;
#59085=DIRECTION ( 'NONE',  ( 0.000000000000000000, 0.000000000000000000, 1.000000000000000000 ) ) ;
#59090=EDGE_CURVE ( 'NONE', #34430, #44609, #6138, .T. ) ;
#59098=ADVANCED_FACE ( 'NONE', ( #34860 ), #4206, .F. ) ;
#59100=FACE_OUTER_BOUND ( 'NONE', #69427, .T. ) ;
#59105=CARTESIAN_POINT ( 'NONE',  ( 6.826472737025121695, 126.6070736234661496, -4.959722759717905660 ) ) ;
#59107=CARTESIAN_POINT ( 'NONE',  ( -3.094860106618432471, 157.5949999999999989, -9.525000000000000355 ) ) ;
#59109=SURFACE_STYLE_FILL_AREA ( #44377 ) ;
#59112=DIRECTION ( 'NONE',  ( 0.000000000000000000, 0.000000000000000000, 1.000000000000000000 ) ) ;
#59116=AXIS2_PLACEMENT_3D ( 'NONE', #12231, #44658, #39365 ) ;
#59120=SURFACE_STYLE_USAGE ( .BOTH. , #26071 ) ;
#59122=CARTESIAN_POINT ( 'NONE',  ( -45.70684385664927163, 8.620779964796652095, 6.438673729884040853 ) ) ;
#59127=ORIENTED_EDGE ( 'NONE', *, *, #18109, .F. ) ;
#59128=FILL_AREA_STYLE_COLOUR ( '', #27870 ) ;
#59130=ORIENTED_EDGE ( 'NONE', *, *, #55098, .T. ) ;
#59132=DIRECTION ( 'NONE',  ( -0.000000000000000000, 1.000000000000000000, -0.000000000000000000 ) ) ;
#59133=CARTESIAN_POINT ( 'NONE',  ( -8.102448949553181734, 118.8949999999999676, -5.886773742842749790 ) ) ;
#59136=DIRECTION ( 'NONE',  ( 1.000000000000000000, 1.601283208593975100E-14, 0.000000000000000000 ) ) ;
#59137=CARTESIAN_POINT ( 'NONE',  ( 5.598654528085805993, 133.3549999999999898, 7.705886871421374629 ) ) ;
#59141=CARTESIAN_POINT ( 'NONE',  ( -5.598654528085808657, 144.7549999999999955, 7.705886871421373741 ) ) ;
#59143=AXIS2_PLACEMENT_3D ( 'NONE', #36092, #42443, #52625 ) ;
#59144=DIRECTION ( 'NONE',  ( 1.000000000000000000, -0.000000000000000000, 0.000000000000000000 ) ) ;
#59148=LINE ( 'NONE', #26454, #35140 ) ;
#59149=CIRCLE ( 'NONE', #68162, 30.00000000000000000 ) ;
#59153=ORIENTED_EDGE ( 'NONE', *, *, #13098, .F. ) ;
#59156=DIRECTION ( 'NONE',  ( 0.000000000000000000, 0.000000000000000000, 1.000000000000000000 ) ) ;
#59164=EDGE_CURVE ( 'NONE', #35564, #59936, #14116, .T. ) ;
#59165=DIRECTION ( 'NONE',  ( -0.000000000000000000, -1.000000000000000000, -0.000000000000000000 ) ) ;
#59166=SURFACE_STYLE_USAGE ( .BOTH. , #11687 ) ;
#59169=ADVANCED_FACE ( 'NONE', ( #14437 ), #66110, .T. ) ;
#59171=EDGE_LOOP ( 'NONE', ( #1507, #15393, #34221, #31600 ) ) ;
#59173=LINE ( 'NONE', #59877, #54910 ) ;
#59174=CYLINDRICAL_SURFACE ( 'NONE', #39256, 0.5000000000000004441 ) ;
#59176=CARTESIAN_POINT ( 'NONE',  ( -9.058813317711337021, 125.0449999999999875, -2.943386871421374895 ) ) ;
#59178=( NAMED_UNIT ( * ) PLANE_ANGLE_UNIT ( ) SI_UNIT ( $, .RADIAN. ) );
#59179=FILL_AREA_STYLE ('',( #37808 ) ) ;
#59182=EDGE_CURVE ( 'NONE', #30209, #10224, #2151, .T. ) ;
#59184=DIRECTION ( 'NONE',  ( -1.000000000000000000, 0.000000000000000000, 0.000000000000000000 ) ) ;
#59186=DIRECTION ( 'NONE',  ( -0.9704308468600219006, 0.2413793103448194921, 0.000000000000000000 ) ) ;
#59187=DIRECTION ( 'NONE',  ( 0.000000000000000000, 0.000000000000000000, 1.000000000000000000 ) ) ;
#59192=ADVANCED_FACE ( 'NONE', ( #59780 ), #34677, .F. ) ;
#59195=SURFACE_STYLE_FILL_AREA ( #27177 ) ;
#59197=CIRCLE ( 'NONE', #62626, 14.49999999999999822 ) ;
#59199=EDGE_LOOP ( 'NONE', ( #42186, #63687, #44656, #10787, #30124, #50968, #11891, #31483, #69268, #14809 ) ) ;
#59201=( LENGTH_UNIT ( ) NAMED_UNIT ( * ) SI_UNIT ( .MILLI., .METRE. ) );
#59203=FILL_AREA_STYLE_COLOUR ( '', #10620 ) ;
#59204=SURFACE_STYLE_FILL_AREA ( #43106 ) ;
#59205=CARTESIAN_POINT ( 'NONE',  ( 2.607480562269076430, 141.9070736234661183, -8.025000000000000355 ) ) ;
#59209=CARTESIAN_POINT ( 'NONE',  ( 23.21231517720797655, 118.4999999999999716, -7.000000000000000000 ) ) ;
#59211=SURFACE_STYLE_FILL_AREA ( #53613 ) ;
#59221=DIRECTION ( 'NONE',  ( 1.000000000000000000, 0.000000000000000000, -0.000000000000000000 ) ) ;
#59230=ORIENTED_EDGE ( 'NONE', *, *, #41104, .T. ) ;
#59233=ORIENTED_EDGE ( 'NONE', *, *, #31688, .F. ) ;
#59240=CARTESIAN_POINT ( 'NONE',  ( -9.058813317711338797, 128.3449999999999989, 2.943386871421373563 ) ) ;
#59243=LINE ( 'NONE', #37526, #14487 ) ;
#59245=DIRECTION ( 'NONE',  ( -1.000000000000000000, 0.000000000000000000, 0.000000000000000000 ) ) ;
#59247=FILL_AREA_STYLE_COLOUR ( '', #55685 ) ;
#59250=( NAMED_UNIT ( * ) PLANE_ANGLE_UNIT ( ) SI_UNIT ( $, .RADIAN. ) );
#59256=CARTESIAN_POINT ( 'NONE',  ( 44.56131952741539237, 9.853773175805059736, -3.472780323910071409 ) ) ;
#59262=( NAMED_UNIT ( * ) PLANE_ANGLE_UNIT ( ) SI_UNIT ( $, .RADIAN. ) );
#59263=PRESENTATION_STYLE_ASSIGNMENT (( #64212 ) ) ;
#59264=( LENGTH_UNIT ( ) NAMED_UNIT ( * ) SI_UNIT ( .MILLI., .METRE. ) );
#59269=EDGE_CURVE ( 'NONE', #34517, #25180, #14568, .T. ) ;
#59273=CARTESIAN_POINT ( 'NONE',  ( -48.50000000000000000, 50.00000000000000000, 7.000000000000000000 ) ) ;
#59274=SURFACE_STYLE_FILL_AREA ( #42480 ) ;
#59278=CARTESIAN_POINT ( 'NONE',  ( 7.632228543268608334, 111.4570736234661581, -2.479861379858951942 ) ) ;
#59280=CARTESIAN_POINT ( 'NONE',  ( -19.89974874213240597, 114.9999999999999574, 10.00000000000001421 ) ) ;
#59281=CARTESIAN_POINT ( 'NONE',  ( 8.437984349512095861, 138.3070736234661808, 1.550032578732816828E-15 ) ) ;
#59284=EDGE_LOOP ( 'NONE', ( #5251, #30919, #19957 ) ) ;
#59285=ORIENTED_EDGE ( 'NONE', *, *, #66301, .F. ) ;
#59289=EDGE_CURVE ( 'NONE', #6428, #47061, #65142, .T. ) ;
#59290=DIRECTION ( 'NONE',  ( 1.000000000000000000, 0.000000000000000000, 0.000000000000000000 ) ) ;
#59291=VERTEX_POINT ( 'NONE', #22854 ) ;
#59292=ADVANCED_FACE ( 'NONE', ( #13304 ), #34762, .F. ) ;
#59293=CARTESIAN_POINT ( 'NONE',  ( 5.598654528085809545, 125.2549999999999812, -7.705886871421373741 ) ) ;
#59296=CARTESIAN_POINT ( 'NONE',  ( 0.000000000000000000, 149.9429263765338476, -8.025000000000000355 ) ) ;
#59298=ORIENTED_EDGE ( 'NONE', *, *, #58298, .T. ) ;
#59301=SURFACE_STYLE_FILL_AREA ( #31896 ) ;
#59306=DIRECTION ( 'NONE',  ( 0.000000000000000000, 0.000000000000000000, -1.000000000000000000 ) ) ;
#59307=( NAMED_UNIT ( * ) SI_UNIT ( $, .STERADIAN. ) SOLID_ANGLE_UNIT ( ) );
#59312=DIRECTION ( 'NONE',  ( 1.000000000000000000, 0.000000000000000000, 0.000000000000000000 ) ) ;
#59318=CARTESIAN_POINT ( 'NONE',  ( 7.632228543268608334, 116.3429263765338106, -2.479861379858951942 ) ) ;
#59319=CARTESIAN_POINT ( 'NONE',  ( -6.598003871452776892, 153.8282337726623723, 5.909302594220192439 ) ) ;
#59321=COLOUR_RGB ( '', 0.09019608, 0.27058824, 0.51372549) ;
#59326=CARTESIAN_POINT ( 'NONE',  ( 72.00000000000000000, 14.49137674618942562, -7.500000000000000000 ) ) ;
#59327=ORIENTED_EDGE ( 'NONE', *, *, #33736, .T. ) ;
#59328=SURFACE_STYLE_FILL_AREA ( #10827 ) ;
#59333=COLOUR_RGB ( '', 0.66274510, 0.83137255, 0.94901961) ;
#59337=STYLED_ITEM ( 'NONE', ( #37234 ), #971 ) ;
#59338=SURFACE_STYLE_FILL_AREA ( #48507 ) ;
#59341=DIRECTION ( 'NONE',  ( -0.000000000000000000, 0.000000000000000000, 1.000000000000000000 ) ) ;
#59342=CARTESIAN_POINT ( 'NONE',  ( -65.99999999999998579, 50.00000000000000000, 10.50000000000000000 ) ) ;
#59346=CARTESIAN_POINT ( 'NONE',  ( -9.058813317711337021, 138.1550000000000011, -2.943386871421374895 ) ) ;
#59347=CARTESIAN_POINT ( 'NONE',  ( -6.826472737025120807, 126.3929263765338220, -4.959722759717907437 ) ) ;
#59355=DIRECTION ( 'NONE',  ( -1.000000000000000000, 0.000000000000000000, 0.000000000000000000 ) ) ;
#59359=PRESENTATION_STYLE_ASSIGNMENT (( #39351 ) ) ;
#59362=AXIS2_PLACEMENT_3D ( 'NONE', #9714, #24457, #31125 ) ;
#59364=SURFACE_STYLE_USAGE ( .BOTH. , #54103 ) ;
#59373=DIRECTION ( 'NONE',  ( 1.000000000000000000, 0.000000000000000000, 0.000000000000000000 ) ) ;
#59374=EDGE_CURVE ( 'NONE', #48200, #16450, #25872, .T. ) ;
#59376=FACE_OUTER_BOUND ( 'NONE', #11866, .T. ) ;
#59378=ORIENTED_EDGE ( 'NONE', *, *, #52304, .T. ) ;
#59379=AXIS2_PLACEMENT_3D ( 'NONE', #59541, #21936, #53589 ) ;
#59380=SURFACE_STYLE_FILL_AREA ( #27369 ) ;
#59381=CARTESIAN_POINT ( 'NONE',  ( -8.102448949553181734, 154.8949999999999534, -5.886773742842749790 ) ) ;
#59388=CARTESIAN_POINT ( 'NONE',  ( 74.99999999999998579, 50.00000000000000000, -7.500000000000000000 ) ) ;
#59390=CARTESIAN_POINT ( 'NONE',  ( 2.607480562269076430, 134.7929263765338135, -8.025000000000000355 ) ) ;
#59391=DIRECTION ( 'NONE',  ( 0.000000000000000000, 0.000000000000000000, 1.000000000000000000 ) ) ;
#59392=CARTESIAN_POINT ( 'NONE',  ( -75.48275862068965125, 36.00832590023089352, -9.500000000000001776 ) ) ;
#59393=AXIS2_PLACEMENT_3D ( 'NONE', #17172, #60047, #11861 ) ;
#59394=EDGE_CURVE ( 'NONE', #57062, #10613, #10864, .T. ) ;
#59397=ORIENTED_EDGE ( 'NONE', *, *, #35845, .T. ) ;
#59398=CARTESIAN_POINT ( 'NONE',  ( -74.50000000000001421, -2.220952357103124294E-14, 10.00000000000000000 ) ) ;
#59403=( NAMED_UNIT ( * ) PLANE_ANGLE_UNIT ( ) SI_UNIT ( $, .RADIAN. ) );
#59409=CARTESIAN_POINT ( 'NONE',  ( 41.03182778381237483, 107.9802461459568832, 3.207526698639996177 ) ) ;
#59412=LINE ( 'NONE', #27406, #29416 ) ;
#59413=CIRCLE ( 'NONE', #30187, 0.5000000000000004441 ) ;
#59421=DIRECTION ( 'NONE',  ( 0.000000000000000000, 0.000000000000000000, 1.000000000000000000 ) ) ;
#59429=VECTOR ( 'NONE', #69675, 1000.000000000000000 ) ;
#59430=SURFACE_STYLE_USAGE ( .BOTH. , #42305 ) ;
#59432=CARTESIAN_POINT ( 'NONE',  ( 0.000000000000000000, 154.4449999999999932, -9.525000000000000355 ) ) ;
#59435=B_SPLINE_CURVE_WITH_KNOTS ( 'NONE', 3,
 ( #37884, #35495, #52030, #62210, #14036, #10754, #25275, #68199, #56941, #53648 ),
 .UNSPECIFIED., .F., .F.,
 ( 4, 2, 2, 2, 4 ),
 ( 0.000000000000000000, 0.0004658606356703475925, 0.0009317212713406951849, 0.001397581907011042832, 0.001863442542681390370 ),
 .UNSPECIFIED. ) ;
#59437=PRESENTATION_STYLE_ASSIGNMENT (( #4958 ) ) ;
#59438=CARTESIAN_POINT ( 'NONE',  ( -48.50000000000000000, 14.49137674618942562, 7.500000000000000000 ) ) ;
#59439=UNCERTAINTY_MEASURE_WITH_UNIT (LENGTH_MEASURE( 1.000000000000000082E-05 ), #38360, 'distance_accuracy_value', 'NONE');
#59441=LINE ( 'NONE', #64042, #49379 ) ;
#59445=DIRECTION ( 'NONE',  ( 0.000000000000000000, 0.000000000000000000, 1.000000000000000000 ) ) ;
#59447=EDGE_CURVE ( 'NONE', #50360, #35826, #53395, .T. ) ;
#59448=CARTESIAN_POINT ( 'NONE',  ( 15.98999599679679839, 146.9999999999999716, -7.500000000000000000 ) ) ;
#59450=EDGE_LOOP ( 'NONE', ( #3372, #18684, #9098, #50134 ) ) ;
#59452=STYLED_ITEM ( 'NONE', ( #8649 ), #1177 ) ;
#59455=DIRECTION ( 'NONE',  ( -0.000000000000000000, -1.000000000000000000, -0.000000000000000000 ) ) ;
#59457=FACE_OUTER_BOUND ( 'NONE', #40016, .T. ) ;
#59460=( GEOMETRIC_REPRESENTATION_CONTEXT ( 3 ) GLOBAL_UNCERTAINTY_ASSIGNED_CONTEXT ( ( #31990 ) ) GLOBAL_UNIT_ASSIGNED_CONTEXT ( ( #38482, #16316, #5700 ) ) REPRESENTATION_CONTEXT ( 'NONE', 'WORKASPACE' ) );
#59465=EDGE_CURVE ( 'NONE', #40918, #50571, #49114, .T. ) ;
#59468=ORIENTED_EDGE ( 'NONE', *, *, #61221, .T. ) ;
#59469=COLOUR_RGB ( '', 0.09019608, 0.27058824, 0.51372549) ;
#59470=AXIS2_PLACEMENT_3D ( 'NONE', #770, #11751, #65214 ) ;
#59474=CARTESIAN_POINT ( 'NONE',  ( 9.058813317711337021, 132.5449999999999875, 2.943386871421375783 ) ) ;
#59475=CARTESIAN_POINT ( 'NONE',  ( 15.98999599679679839, 118.4999999999999716, 7.000000000000000000 ) ) ;
#59477=COLOUR_RGB ( '', 0.08235294, 0.09019608, 0.10196078) ;
#59479=DIRECTION ( 'NONE',  ( 0.000000000000000000, -1.000000000000000000, 0.000000000000000000 ) ) ;
#59480=CARTESIAN_POINT ( 'NONE',  ( 8.102448949553181734, 128.1049999999999898, -5.886773742842746238 ) ) ;
#59481=EDGE_CURVE ( 'NONE', #39204, #28720, #31492, .T. ) ;
#59485=CARTESIAN_POINT ( 'NONE',  ( -41.61212508608682725, 107.5086115709060834, -4.000000005149773052 ) ) ;
#59487=CARTESIAN_POINT ( 'NONE',  ( -8.102448949553181734, 147.6049999999999329, 5.886773742842747126 ) ) ;
#59489=UNCERTAINTY_MEASURE_WITH_UNIT (LENGTH_MEASURE( 1.000000000000000082E-05 ), #5556, 'distance_accuracy_value', 'NONE');
#59490=VECTOR ( 'NONE', #59040, 1000.000000000000114 ) ;
#59491=( NAMED_UNIT ( * ) SI_UNIT ( $, .STERADIAN. ) SOLID_ANGLE_UNIT ( ) );
#59493=PRESENTATION_STYLE_ASSIGNMENT (( #38093 ) ) ;
#59494=ORIENTED_EDGE ( 'NONE', *, *, #12332, .T. ) ;
#59495=AXIS2_PLACEMENT_3D ( 'NONE', #65860, #60234, #66551 ) ;
#59496=CARTESIAN_POINT ( 'NONE',  ( 40.78947368421051323, 108.1536491499103363, 3.000000000000000000 ) ) ;
#59499=PRESENTATION_STYLE_ASSIGNMENT (( #38103 ) ) ;
#59502=FACE_OUTER_BOUND ( 'NONE', #58737, .T. ) ;
#59504=( NAMED_UNIT ( * ) SI_UNIT ( $, .STERADIAN. ) SOLID_ANGLE_UNIT ( ) );
#59507=CARTESIAN_POINT ( 'NONE',  ( -45.89905495991339990, 9.405628579550478818, -3.102097799525639132 ) ) ;
#59512=TOROIDAL_SURFACE ( 'NONE', #13465, 8.499999999999994671, 0.5000000000000000000 ) ;
#59513=AXIS2_PLACEMENT_3D ( 'NONE', #20779, #47563, #41221 ) ;
#59514=CARTESIAN_POINT ( 'NONE',  ( 2.607480562269160362, 144.9070736234662036, -8.024999999999939959 ) ) ;
#59518=PRESENTATION_STYLE_ASSIGNMENT (( #10325 ) ) ;
#59519=ORIENTED_EDGE ( 'NONE', *, *, #15685, .T. ) ;
#59521=DIRECTION ( 'NONE',  ( -0.000000000000000000, -0.000000000000000000, -1.000000000000000000 ) ) ;
#59524=CARTESIAN_POINT ( 'NONE',  ( -5.598654528085806881, 130.7450000000000045, -7.705886871421374629 ) ) ;
#59526=VECTOR ( 'NONE', #64311, 1000.000000000000000 ) ;
#59527=VECTOR ( 'NONE', #33068, 1000.000000000000000 ) ;
#59529=AXIS2_PLACEMENT_3D ( 'NONE', #55672, #65535, #45158 ) ;
#59535=CIRCLE ( 'NONE', #11244, 0.5000000000000004441 ) ;
#59536=( LENGTH_UNIT ( ) NAMED_UNIT ( * ) SI_UNIT ( .MILLI., .METRE. ) );
#59540=ORIENTED_EDGE ( 'NONE', *, *, #51619, .F. ) ;
#59541=CARTESIAN_POINT ( 'NONE',  ( 15.98999599679679839, 146.4999999999999716, -9.500000000000000000 ) ) ;
#59542=DIRECTION ( 'NONE',  ( 0.000000000000000000, 0.000000000000000000, -1.000000000000000000 ) ) ;
#59545=VECTOR ( 'NONE', #1353, 1000.000000000000000 ) ;
#59546=CARTESIAN_POINT ( 'NONE',  ( -48.00000000000000000, 99.99999999999992895, -7.500000000000000000 ) ) ;
#59547=EDGE_CURVE ( 'NONE', #16561, #40163, #64632, .T. ) ;
#59554=EDGE_CURVE ( 'NONE', #51351, #60581, #16480, .T. ) ;
#59558=EDGE_CURVE ( 'NONE', #12616, #38944, #27308, .T. ) ;
#59559=SURFACE_SIDE_STYLE ('',( #38155 ) ) ;
#59562=CARTESIAN_POINT ( 'NONE',  ( -9.827790563157511022E-16, 152.5570736234661524, 8.025000000000000355 ) ) ;
#59565=CARTESIAN_POINT ( 'NONE',  ( 6.826472737025119919, 136.8929263765338362, 4.959722759717908325 ) ) ;
#59570=ORIENTED_EDGE ( 'NONE', *, *, #37388, .F. ) ;
#59572=( LENGTH_UNIT ( ) NAMED_UNIT ( * ) SI_UNIT ( .MILLI., .METRE. ) );
#59573=( NAMED_UNIT ( * ) SI_UNIT ( $, .STERADIAN. ) SOLID_ANGLE_UNIT ( ) );
#59582=CARTESIAN_POINT ( 'NONE',  ( 9.827790563157511022E-16, 152.9999999999999716, -8.025000000000000355 ) ) ;
#59583=CARTESIAN_POINT ( 'NONE',  ( -45.00000000000000000, 8.062885929673873520, -5.900610682604093604 ) ) ;
#59584=ORIENTED_EDGE ( 'NONE', *, *, #62251, .T. ) ;
#59585=FILL_AREA_STYLE ('',( #32497 ) ) ;
#59587=EDGE_LOOP ( 'NONE', ( #27714, #8101, #49308, #38869 ) ) ;
#59590=ORIENTED_EDGE ( 'NONE', *, *, #30238, .F. ) ;
#59593=DIRECTION ( 'NONE',  ( -7.080503983578803083E-17, 1.000000000000000000, 0.000000000000000000 ) ) ;
#59594=LINE ( 'NONE', #48403, #18472 ) ;
#59597=AXIS2_PLACEMENT_3D ( 'NONE', #54089, #69584, #5898 ) ;
#59598=CARTESIAN_POINT ( 'NONE',  ( 8.102448949553181734, 132.9949999999999477, -5.886773742842746238 ) ) ;
#59600=ADVANCED_FACE ( 'NONE', ( #4151 ), #57658, .F. ) ;
#59602=DIRECTION ( 'NONE',  ( 0.000000000000000000, 1.000000000000000000, 0.000000000000000000 ) ) ;
#59605=CARTESIAN_POINT ( 'NONE',  ( 60.00000000000000000, 1.797044900979284448E-15, 6.999999999999988454 ) ) ;
#59608=CARTESIAN_POINT ( 'NONE',  ( -2.607480562269032909, 131.4070736234661467, 8.025000000000032330 ) ) ;
#59614=ORIENTED_EDGE ( 'NONE', *, *, #56396, .F. ) ;
#59615=( NAMED_UNIT ( * ) PLANE_ANGLE_UNIT ( ) SI_UNIT ( $, .RADIAN. ) );
#59616=( NAMED_UNIT ( * ) SI_UNIT ( $, .STERADIAN. ) SOLID_ANGLE_UNIT ( ) );
#59627=FILL_AREA_STYLE ('',( #1170 ) ) ;
#59628=STYLED_ITEM ( 'NONE', ( #53008 ), #34790 ) ;
#59632=DIRECTION ( 'NONE',  ( 1.000000000000000000, 0.000000000000000000, 0.000000000000000000 ) ) ;
#59633=CIRCLE ( 'NONE', #43969, 0.4999999999999991118 ) ;
#59634=CARTESIAN_POINT ( 'NONE',  ( -44.99999999999998579, 119.9999999999999716, 7.000000000000000000 ) ) ;
#59635=DIRECTION ( 'NONE',  ( 0.000000000000000000, 0.000000000000000000, 1.000000000000000000 ) ) ;
#59641=DIRECTION ( 'NONE',  ( -0.000000000000000000, -0.000000000000000000, -1.000000000000000000 ) ) ;
#59643=LINE ( 'NONE', #27953, #47746 ) ;
#59644=( BOUNDED_CURVE ( )  B_SPLINE_CURVE ( 3, ( #36537, #4441, #26265, #20294 ),
 .UNSPECIFIED., .F., .F. ) 
 B_SPLINE_CURVE_WITH_KNOTS ( ( 4, 4 ),
 ( 4.712388980384691450, 6.283185307179586232 ),
 .UNSPECIFIED. ) 
 CURVE ( )  GEOMETRIC_REPRESENTATION_ITEM ( )  RATIONAL_B_SPLINE_CURVE ( ( 1.000000000000000000, 0.8047378541243654926, 0.8047378541243654926, 1.000000000000000000 ) ) 
 REPRESENTATION_ITEM ( '' )  );
#59645=CARTESIAN_POINT ( 'NONE',  ( -2.607480562269075097, 110.4070736234661467, 8.025000000000000355 ) ) ;
#59646=DIRECTION ( 'NONE',  ( 0.7071067811865352493, 8.659560562354782482E-17, -0.7071067811865597852 ) ) ;
#59647=DIRECTION ( 'NONE',  ( 0.000000000000000000, 1.000000000000000000, -0.000000000000000000 ) ) ;
#59649=CARTESIAN_POINT ( 'NONE',  ( 75.00000000000000000, 19.99999999999998224, -5.999999999999998224 ) ) ;
#59651=EDGE_LOOP ( 'NONE', ( #14845, #61887, #2708, #57349 ) ) ;
#59655=ORIENTED_EDGE ( 'NONE', *, *, #68767, .F. ) ;
#59656=( NAMED_UNIT ( * ) PLANE_ANGLE_UNIT ( ) SI_UNIT ( $, .RADIAN. ) );
#59658=CARTESIAN_POINT ( 'NONE',  ( 6.826472737025119919, 133.8929263765338078, 4.959722759717908325 ) ) ;
#59661=VECTOR ( 'NONE', #66683, 1000.000000000000000 ) ;
#59662=CARTESIAN_POINT ( 'NONE',  ( 74.50000000000000000, -2.220952357103124925E-14, -6.500000000000000000 ) ) ;
#59663=FILL_AREA_STYLE ('',( #61047 ) ) ;
#59667=DIRECTION ( 'NONE',  ( -6.591949208711860648E-14, 0.000000000000000000, 1.000000000000000000 ) ) ;
#59669=ORIENTED_EDGE ( 'NONE', *, *, #60201, .T. ) ;
#59670=AXIS2_PLACEMENT_3D ( 'NONE', #32059, #43011, #5644 ) ;
#59675=( NAMED_UNIT ( * ) SI_UNIT ( $, .STERADIAN. ) SOLID_ANGLE_UNIT ( ) );
#59677=DIRECTION ( 'NONE',  ( 0.000000000000000000, 0.000000000000000000, 1.000000000000000000 ) ) ;
#59681=CARTESIAN_POINT ( 'NONE',  ( -8.234833373661349043, 153.6756281844815248, 2.821501943811211888 ) ) ;
#59682=ORIENTED_EDGE ( 'NONE', *, *, #10660, .T. ) ;
#59685=DIRECTION ( 'NONE',  ( 0.000000000000000000, 0.000000000000000000, 1.000000000000000000 ) ) ;
#59687=CARTESIAN_POINT ( 'NONE',  ( 48.50000000000000000, 14.49137674618942562, -7.000000000000000000 ) ) ;
#59689=PRESENTATION_STYLE_ASSIGNMENT (( #32978 ) ) ;
#59697=EDGE_LOOP ( 'NONE', ( #4008, #757, #47732, #62372 ) ) ;
#59699=CARTESIAN_POINT ( 'NONE',  ( -45.50000000000000000, -2.024042244987997205E-14, 9.500000000000000000 ) ) ;
#59703=( NAMED_UNIT ( * ) SI_UNIT ( $, .STERADIAN. ) SOLID_ANGLE_UNIT ( ) );
#59705=LINE ( 'NONE', #42901, #39357 ) ;
#59708=ADVANCED_FACE ( 'NONE', ( #15465 ), #31540, .T. ) ;
#59710=EDGE_CURVE ( 'NONE', #30297, #52608, #61870, .T. ) ;
#59711=CARTESIAN_POINT ( 'NONE',  ( -3.094860106618434248, 132.9050000000000011, 9.525000000000000355 ) ) ;
#59720=( NAMED_UNIT ( * ) SI_UNIT ( $, .STERADIAN. ) SOLID_ANGLE_UNIT ( ) );
#59721=CIRCLE ( 'NONE', #8065, 0.5000000000000004441 ) ;
#59724=SURFACE_SIDE_STYLE ('',( #63014 ) ) ;
#59727=CARTESIAN_POINT ( 'NONE',  ( -74.99999999999998579, 50.00000000000000000, -6.500000000000000000 ) ) ;
#59728=ORIENTED_EDGE ( 'NONE', *, *, #49967, .F. ) ;
#59729=ORIENTED_EDGE ( 'NONE', *, *, #21047, .T. ) ;
#59730=SURFACE_STYLE_FILL_AREA ( #12217 ) ;
#59731=COLOUR_RGB ( '', 0.72549020, 0.75294118, 0.79215686) ;
#59733=AXIS2_PLACEMENT_3D ( 'NONE', #51185, #34995, #2933 ) ;
#59735=DIRECTION ( 'NONE',  ( 0.000000000000000000, 0.000000000000000000, 1.000000000000000000 ) ) ;
#59738=ORIENTED_EDGE ( 'NONE', *, *, #54761, .F. ) ;
#59741=( NAMED_UNIT ( * ) SI_UNIT ( $, .STERADIAN. ) SOLID_ANGLE_UNIT ( ) );
#59743=VECTOR ( 'NONE', #31207, 1000.000000000000000 ) ;
#59748=CARTESIAN_POINT ( 'NONE',  ( 0.000000000000000000, 157.4449999999999932, -9.525000000000000355 ) ) ;
#59750=ORIENTED_EDGE ( 'NONE', *, *, #33826, .T. ) ;
#59751=( BOUNDED_CURVE ( )  B_SPLINE_CURVE ( 2, ( #49895, #7320, #12566, #32644, #43606, #64996, #16519, #229, #39014, #43945, #27695 ),
 .UNSPECIFIED., .F., .F. ) 
 B_SPLINE_CURVE_WITH_KNOTS ( ( 3, 2, 2, 2, 2, 3 ),
 ( 0.4705882352941177516, 0.4764705882352942012, 0.4823529411764707620, 0.4882352941176472116, 0.4941176470588237724, 0.5000000000000002220 ),
 .UNSPECIFIED. ) 
 CURVE ( )  GEOMETRIC_REPRESENTATION_ITEM ( )  RATIONAL_B_SPLINE_CURVE ( ( 0.9999999999999991118, 0.9510565162951544194, 1.000000000000000000, 0.9510565162951535312, 1.000000000000000000, 0.9510565162951535312, 1.000000000000000000, 0.9510565162951535312, 1.000000000000000000, 0.9510565162951516438, 1.000000000000001776 ) ) 
 REPRESENTATION_ITEM ( '' )  );
#59753=CIRCLE ( 'NONE', #19325, 23.00000000000000355 ) ;
#59755=( NAMED_UNIT ( * ) SI_UNIT ( $, .STERADIAN. ) SOLID_ANGLE_UNIT ( ) );
#59757=ORIENTED_EDGE ( 'NONE', *, *, #69200, .T. ) ;
#59758=CARTESIAN_POINT ( 'NONE',  ( 6.826472737025121695, 134.4929263765338305, -4.959722759717905660 ) ) ;
#59768=( NAMED_UNIT ( * ) SI_UNIT ( $, .STERADIAN. ) SOLID_ANGLE_UNIT ( ) );
#59770=DIRECTION ( 'NONE',  ( 0.000000000000000000, 0.000000000000000000, -1.000000000000000000 ) ) ;
#59771=STYLED_ITEM ( 'NONE', ( #7995 ), #60722 ) ;
#59773=CARTESIAN_POINT ( 'NONE',  ( -44.50000000000000000, 9.499999999999980460, -3.000000000000000444 ) ) ;
#59774=DIRECTION ( 'NONE',  ( 0.000000000000000000, 0.000000000000000000, 1.000000000000000000 ) ) ;
#59778=CARTESIAN_POINT ( 'NONE',  ( -7.632228543268608334, 115.9570736234661581, 2.479861379858952830 ) ) ;
#59779=DIRECTION ( 'NONE',  ( -0.000000000000000000, -1.000000000000000000, -0.000000000000000000 ) ) ;
#59780=FACE_OUTER_BOUND ( 'NONE', #68687, .T. ) ;
#59781=ORIENTED_EDGE ( 'NONE', *, *, #37200, .T. ) ;
#59783=ORIENTED_EDGE ( 'NONE', *, *, #36348, .F. ) ;
#59788=( NAMED_UNIT ( * ) SI_UNIT ( $, .STERADIAN. ) SOLID_ANGLE_UNIT ( ) );
#59791=CYLINDRICAL_SURFACE ( 'NONE', #26749, 0.5000000000000004441 ) ;
#59792=AXIS2_PLACEMENT_3D ( 'NONE', #50591, #2698, #13636 ) ;
#59793=CARTESIAN_POINT ( 'NONE',  ( 60.00000000000000000, 115.4999999999999574, -10.50000000000000000 ) ) ;
#59794=CYLINDRICAL_SURFACE ( 'NONE', #5033, 8.025000000000000355 ) ;
#59795=ORIENTED_EDGE ( 'NONE', *, *, #59269, .T. ) ;
#59796=COLOUR_RGB ( '', 0.09019608, 0.27058824, 0.51372549) ;
#59804=CARTESIAN_POINT ( 'NONE',  ( -10.01517768586949231, 155.1949999999999648, -6.132527647946036459E-16 ) ) ;
#59806=COLOUR_RGB ( '', 0.66274510, 0.83137255, 0.94901961) ;
#59809=CARTESIAN_POINT ( 'NONE',  ( 52.49999999999998579, 2.715530000339800426E-15, -11.50000000000000000 ) ) ;
#59811=ORIENTED_EDGE ( 'NONE', *, *, #22161, .T. ) ;
#59815=SURFACE_SIDE_STYLE ('',( #58434 ) ) ;
#59819=CIRCLE ( 'NONE', #11556, 9.499999999999994671 ) ;
#59820=ORIENTED_EDGE ( 'NONE', *, *, #8594, .T. ) ;
#59822=DIRECTION ( 'NONE',  ( -1.000000000000000000, 0.000000000000000000, 0.000000000000000000 ) ) ;
#59823=FILL_AREA_STYLE ('',( #43692 ) ) ;
#59824=AXIS2_PLACEMENT_3D ( 'NONE', #14423, #63997, #36637 ) ;
#59830=ORIENTED_EDGE ( 'NONE', *, *, #29954, .T. ) ;
#59831=CIRCLE ( 'NONE', #29504, 0.5000000000000004441 ) ;
#59833=ORIENTED_EDGE ( 'NONE', *, *, #39023, .F. ) ;
#59839=VECTOR ( 'NONE', #2150, 1000.000000000000000 ) ;
#59841=CARTESIAN_POINT ( 'NONE',  ( 1.227708416145222385E-15, 109.9999999999999858, 10.02500000000000568 ) ) ;
#59842=CARTESIAN_POINT ( 'NONE',  ( 8.102448949553181734, 126.3949999999999818, 5.886773742842750679 ) ) ;
#59843=DIRECTION ( 'NONE',  ( 0.000000000000000000, -1.000000000000000000, 0.000000000000000000 ) ) ;
#59846=CARTESIAN_POINT ( 'NONE',  ( 5.598654528085809545, 131.2549999999999955, -7.705886871421373741 ) ) ;
#59849=CARTESIAN_POINT ( 'NONE',  ( -41.84210526315788314, 107.2928455055531600, -3.499999999999996891 ) ) ;
#59850=EDGE_LOOP ( 'NONE', ( #59795, #5750, #3598, #69394 ) ) ;
#59851=CARTESIAN_POINT ( 'NONE',  ( -5.598654528085808657, 159.7549999999999670, 7.705886871421373741 ) ) ;
#59852=CARTESIAN_POINT ( 'NONE',  ( -12.48999599679679662, 115.4999999999999574, 10.00000000000000000 ) ) ;
#59853=SURFACE_STYLE_USAGE ( .BOTH. , #5329 ) ;
#59854=DIRECTION ( 'NONE',  ( -1.000000000000000000, 0.000000000000000000, 0.000000000000000000 ) ) ;
#59855=CARTESIAN_POINT ( 'NONE',  ( -21.02379604162863913, 110.4999999999999858, 10.00000000000000000 ) ) ;
#59856=AXIS2_PLACEMENT_3D ( 'NONE', #42200, #10484, #24905 ) ;
#59860=DIRECTION ( 'NONE',  ( -1.000000000000000000, 0.000000000000000000, 0.000000000000000000 ) ) ;
#59863=LINE ( 'NONE', #32785, #30566 ) ;
#59864=MECHANICAL_DESIGN_GEOMETRIC_PRESENTATION_REPRESENTATION('',(#8202),#41985);
#59865=DIRECTION ( 'NONE',  ( -0.000000000000000000, -0.000000000000000000, -1.000000000000000000 ) ) ;
#59867=AXIS2_PLACEMENT_3D ( 'NONE', #58068, #14112, #51389 ) ;
#59870=EDGE_LOOP ( 'NONE', ( #50880, #56262, #1571, #65376, #22138 ) ) ;
#59871=ADVANCED_FACE ( 'NONE', ( #12202 ), #61193, .F. ) ;
#59873=SURFACE_STYLE_FILL_AREA ( #16988 ) ;
#59877=CARTESIAN_POINT ( 'NONE',  ( -71.50000000000000000, 36.32520566882265456, -7.000000000000000000 ) ) ;
#59881=CARTESIAN_POINT ( 'NONE',  ( -3.094860106618432471, 127.5949999999999847, -9.525000000000000355 ) ) ;
#59885=DIRECTION ( 'NONE',  ( -0.000000000000000000, 1.000000000000000000, -0.000000000000000000 ) ) ;
#59887=CARTESIAN_POINT ( 'NONE',  ( -14.98999599679678951, 1.797044900979284448E-15, -9.500000000000000000 ) ) ;
#59894=( GEOMETRIC_REPRESENTATION_CONTEXT ( 3 ) GLOBAL_UNCERTAINTY_ASSIGNED_CONTEXT ( ( #36368 ) ) GLOBAL_UNIT_ASSIGNED_CONTEXT ( ( #45424, #47505, #14389 ) ) REPRESENTATION_CONTEXT ( 'NONE', 'WORKASPACE' ) );
#59897=( NAMED_UNIT ( * ) SI_UNIT ( $, .STERADIAN. ) SOLID_ANGLE_UNIT ( ) );
#59898=EDGE_LOOP ( 'NONE', ( #53467, #47869, #46919, #44542 ) ) ;
#59900=CARTESIAN_POINT ( 'NONE',  ( -45.85105888842022637, 9.184645374706622789, 6.276135203588958156 ) ) ;
#59901=( NAMED_UNIT ( * ) SI_UNIT ( $, .STERADIAN. ) SOLID_ANGLE_UNIT ( ) );
#59904=CARTESIAN_POINT ( 'NONE',  ( -12.72792206135785698, 115.4999999999999574, -10.50000000000000000 ) ) ;
#59905=DIRECTION ( 'NONE',  ( 1.000000000000000000, 0.000000000000000000, 0.000000000000000000 ) ) ;
#59906=DIRECTION ( 'NONE',  ( -0.3162277660168358873, 0.9486832980505145452, 0.000000000000000000 ) ) ;
#59913=MECHANICAL_DESIGN_GEOMETRIC_PRESENTATION_REPRESENTATION('',(#27303),#8264);
#59915=FACE_OUTER_BOUND ( 'NONE', #69558, .T. ) ;
#59916=CARTESIAN_POINT ( 'NONE',  ( -6.826472737025120807, 155.1070736234661069, 4.959722759717906548 ) ) ;
#59919=VERTEX_POINT ( 'NONE', #9997 ) ;
#59923=CARTESIAN_POINT ( 'NONE',  ( 44.50000000000000000, 99.99999999999998579, 4.000000000000000000 ) ) ;
#59927=CARTESIAN_POINT ( 'NONE',  ( 48.00000000000000000, 14.49137674618942562, -10.00000000000000000 ) ) ;
#59928=CARTESIAN_POINT ( 'NONE',  ( -72.50000000000001421, 14.49137674618942562, -9.500000000000000000 ) ) ;
#59933=CARTESIAN_POINT ( 'NONE',  ( -45.00000000000000000, 9.025366258634486272, -6.779481487458365763 ) ) ;
#59934=AXIS2_PLACEMENT_3D ( 'NONE', #10865, #32307, #53762 ) ;
#59936=VERTEX_POINT ( 'NONE', #36766 ) ;
#59937=CIRCLE ( 'NONE', #68956, 0.5000000000000004441 ) ;
#59938=CARTESIAN_POINT ( 'NONE',  ( 19.89974874213239886, 114.9999999999999574, -10.49999999999999645 ) ) ;
#59939=CARTESIAN_POINT ( 'NONE',  ( -75.00000000000000000, 9.656580361551663216, 6.242521039668915250 ) ) ;
#59946=SURFACE_STYLE_FILL_AREA ( #4376 ) ;
#59947=FACE_OUTER_BOUND ( 'NONE', #6124, .T. ) ;
#59950=CARTESIAN_POINT ( 'NONE',  ( 3.094860106618435136, 136.2949999999999875, -9.525000000000000355 ) ) ;
#59952=( BOUNDED_CURVE ( )  B_SPLINE_CURVE ( 2, ( #69115, #63809, #37135, #10378, #54970, #50418, #22646, #39900, #38530, #66951, #27879 ),
 .UNSPECIFIED., .F., .F. ) 
 B_SPLINE_CURVE_WITH_KNOTS ( ( 3, 2, 2, 2, 2, 3 ),
 ( 0.4411764705882353921, 0.4470588235294118973, 0.4529411764705883470, 0.4588235294117647967, 0.4647058823529413019, 0.4705882352941177516 ),
 .UNSPECIFIED. ) 
 CURVE ( )  GEOMETRIC_REPRESENTATION_ITEM ( )  RATIONAL_B_SPLINE_CURVE ( ( 0.9999999999999991118, 0.9510565162951544194, 1.000000000000000000, 0.9510565162951535312, 1.000000000000000000, 0.9510565162951535312, 1.000000000000000000, 0.9510565162951535312, 1.000000000000000000, 0.9510565162951526430, 1.000000000000000888 ) ) 
 REPRESENTATION_ITEM ( '' )  );
#59957=DIRECTION ( 'NONE',  ( -0.000000000000000000, -0.000000000000000000, -1.000000000000000000 ) ) ;
#59960=( NAMED_UNIT ( * ) PLANE_ANGLE_UNIT ( ) SI_UNIT ( $, .RADIAN. ) );
#59962=PLANE ( 'NONE',  #47927 ) ;
#59965=FILL_AREA_STYLE ('',( #23040 ) ) ;
#59973=FACE_OUTER_BOUND ( 'NONE', #53920, .T. ) ;
#59975=UNCERTAINTY_MEASURE_WITH_UNIT (LENGTH_MEASURE( 1.000000000000000082E-05 ), #5040, 'distance_accuracy_value', 'NONE');
#59977=CARTESIAN_POINT ( 'NONE',  ( 0.000000000000000000, 0.000000000000000000, 0.000000000000000000 ) ) ;
#59984=AXIS2_PLACEMENT_3D ( 'NONE', #31822, #48063, #63157 ) ;
#59988=DIRECTION ( 'NONE',  ( -0.000000000000000000, 1.000000000000000000, -0.000000000000000000 ) ) ;
#59992=EDGE_LOOP ( 'NONE', ( #14993, #47993, #55940, #28662 ) ) ;
#59993=DIRECTION ( 'NONE',  ( -0.000000000000000000, 0.000000000000000000, 1.000000000000000000 ) ) ;
#59996=AXIS2_PLACEMENT_3D ( 'NONE', #46573, #58128, #25064 ) ;
#59997=CARTESIAN_POINT ( 'NONE',  ( -4.716976649647097730, 124.3570736234661496, -6.492361379858953896 ) ) ;
#60000=CARTESIAN_POINT ( 'NONE',  ( 20.94636006565341191, 149.9999999999999716, 9.500000000000000000 ) ) ;
#60001=CARTESIAN_POINT ( 'NONE',  ( 7.632228543268607446, 138.1570736234661467, 2.479861379858954606 ) ) ;
#60016=FACE_OUTER_BOUND ( 'NONE', #5781, .T. ) ;
#60018=ORIENTED_EDGE ( 'NONE', *, *, #58106, .T. ) ;
#60020=DIRECTION ( 'NONE',  ( 0.000000000000000000, -1.099520432716498821E-15, 1.000000000000000000 ) ) ;
#60022=ADVANCED_FACE ( 'NONE', ( #38836 ), #29276, .T. ) ;
#60026=EDGE_LOOP ( 'NONE', ( #30646, #1077, #29108, #30001 ) ) ;
#60031=CIRCLE ( 'NONE', #9500, 0.5000000000000004441 ) ;
#60034=( GEOMETRIC_REPRESENTATION_CONTEXT ( 3 ) GLOBAL_UNCERTAINTY_ASSIGNED_CONTEXT ( ( #17939 ) ) GLOBAL_UNIT_ASSIGNED_CONTEXT ( ( #33564, #46512, #29934 ) ) REPRESENTATION_CONTEXT ( 'NONE', 'WORKASPACE' ) );
#60037=CIRCLE ( 'NONE', #29718, 0.5000000000000004441 ) ;
#60038=CARTESIAN_POINT ( 'NONE',  ( -5.015307210679823768, 153.2028691003589245, -6.528277465523972367 ) ) ;
#60043=CARTESIAN_POINT ( 'NONE',  ( -60.00000000000000000, -2.024042244987997205E-14, -10.00000000000000000 ) ) ;
#60044=EDGE_LOOP ( 'NONE', ( #22116, #6360, #26686, #63738 ) ) ;
#60047=DIRECTION ( 'NONE',  ( -0.000000000000000000, -0.000000000000000000, -1.000000000000000000 ) ) ;
#60051=ORIENTED_EDGE ( 'NONE', *, *, #4428, .F. ) ;
#60058=CARTESIAN_POINT ( 'NONE',  ( 71.74137931034479720, 63.10081643261027295, 10.00000000000000000 ) ) ;
#60060=CARTESIAN_POINT ( 'NONE',  ( -8.102448949553181734, 141.0049999999999386, -5.886773742842749790 ) ) ;
#60064=VECTOR ( 'NONE', #3374, 1000.000000000000000 ) ;
#60069=CARTESIAN_POINT ( 'NONE',  ( -74.99999999999998579, 50.00000000000000000, 12.00000000000000000 ) ) ;
#60077=VERTEX_POINT ( 'NONE', #44471 ) ;
#60078=ORIENTED_EDGE ( 'NONE', *, *, #29621, .T. ) ;
#60079=CARTESIAN_POINT ( 'NONE',  ( 75.00000000000000000, 19.30628705663858113, -6.999999999999999112 ) ) ;
#60080=EDGE_CURVE ( 'NONE', #20480, #69284, #29333, .T. ) ;
#60081=( NAMED_UNIT ( * ) SI_UNIT ( $, .STERADIAN. ) SOLID_ANGLE_UNIT ( ) );
#60082=SURFACE_STYLE_USAGE ( .BOTH. , #44310 ) ;
#60084=CARTESIAN_POINT ( 'NONE',  ( 6.826472737025119919, 139.8929263765338362, 4.959722759717908325 ) ) ;
#60087=VERTEX_POINT ( 'NONE', #49704 ) ;
#60088=( NAMED_UNIT ( * ) PLANE_ANGLE_UNIT ( ) SI_UNIT ( $, .RADIAN. ) );
#60094=CARTESIAN_POINT ( 'NONE',  ( 5.598654528085805993, 159.2450000000000045, 7.705886871421374629 ) ) ;
#60095=ORIENTED_EDGE ( 'NONE', *, *, #23142, .F. ) ;
#60098=COLOUR_RGB ( '', 0.08235294, 0.09019608, 0.10196078) ;
#60100=CARTESIAN_POINT ( 'NONE',  ( -23.71231517720798010, 117.9999999999999716, -7.000000000000000000 ) ) ;
#60103=CARTESIAN_POINT ( 'NONE',  ( 7.632228543268607446, 131.0429263765338135, 2.479861379858954606 ) ) ;
#60106=EDGE_CURVE ( 'NONE', #42295, #11259, #52962, .T. ) ;
#60107=CIRCLE ( 'NONE', #54533, 0.5000000000000004441 ) ;
#60108=CARTESIAN_POINT ( 'NONE',  ( 6.826472737025119919, 124.8929263765338220, 4.959722759717908325 ) ) ;
#60111=ORIENTED_EDGE ( 'NONE', *, *, #64247, .F. ) ;
#60113=ORIENTED_EDGE ( 'NONE', *, *, #9323, .T. ) ;
#60115=MECHANICAL_DESIGN_GEOMETRIC_PRESENTATION_REPRESENTATION('',(#57877),#9585);
#60118=CARTESIAN_POINT ( 'NONE',  ( -44.99999999999998579, 119.9999999999999716, -7.000000000000000000 ) ) ;
#60121=FACE_OUTER_BOUND ( 'NONE', #64669, .T. ) ;
#60125=EDGE_CURVE ( 'NONE', #17419, #10952, #38390, .T. ) ;
#60131=CARTESIAN_POINT ( 'NONE',  ( -45.15333726543703818, 8.290013047818442615, 3.464655003380054943 ) ) ;
#60134=CIRCLE ( 'NONE', #26427, 23.00000000000000000 ) ;
#60144=VERTEX_POINT ( 'NONE', #29623 ) ;
#60145=FACE_OUTER_BOUND ( 'NONE', #68081, .T. ) ;
#60146=COLOUR_RGB ( '', 0.72549020, 0.75294118, 0.79215686) ;
#60148=CARTESIAN_POINT ( 'NONE',  ( -48.81081081081080697, 14.09971791521133255, -7.000000000000000000 ) ) ;
#60151=CARTESIAN_POINT ( 'NONE',  ( 9.058813317711337021, 156.5449999999999875, 2.943386871421375783 ) ) ;
#60153=DIRECTION ( 'NONE',  ( -1.000000000000000000, 0.000000000000000000, 0.000000000000000000 ) ) ;
#60154=CARTESIAN_POINT ( 'NONE',  ( -4.716976649647097730, 141.2429263765338305, -6.492361379858953896 ) ) ;
#60158=DIRECTION ( 'NONE',  ( -1.000000000000000000, 0.000000000000000000, 0.000000000000000000 ) ) ;
#60166=VERTEX_POINT ( 'NONE', #66568 ) ;
#60167=ORIENTED_EDGE ( 'NONE', *, *, #5019, .F. ) ;
#60168=COLOUR_RGB ( '', 0.31764706, 0.68627451, 0.89019608) ;
#60173=CARTESIAN_POINT ( 'NONE',  ( -71.99999999999998579, 119.9999999999997868, 7.500000000000000000 ) ) ;
#60177=EDGE_LOOP ( 'NONE', ( #50656, #56367, #54779, #61790 ) ) ;
#60178=AXIS2_PLACEMENT_3D ( 'NONE', #14082, #62257, #13724 ) ;
#60179=EDGE_LOOP ( 'NONE', ( #22930, #55541, #56551, #44921, #17374, #43875, #5589, #48265, #38525, #8795, #69207, #57234, #50240, #3697, #50326, #10652 ) ) ;
#60180=DIRECTION ( 'NONE',  ( 0.000000000000000000, 0.000000000000000000, 1.000000000000000000 ) ) ;
#60181=DIRECTION ( 'NONE',  ( 0.000000000000000000, 1.000000000000000000, -0.000000000000000000 ) ) ;
#60182=VERTEX_POINT ( 'NONE', #40908 ) ;
#60183=( GEOMETRIC_REPRESENTATION_CONTEXT ( 3 ) GLOBAL_UNCERTAINTY_ASSIGNED_CONTEXT ( ( #8773 ) ) GLOBAL_UNIT_ASSIGNED_CONTEXT ( ( #41209, #19354, #51738 ) ) REPRESENTATION_CONTEXT ( 'NONE', 'WORKASPACE' ) );
#60184=COLOUR_RGB ( '', 0.66274510, 0.83137255, 0.94901961) ;
#60186=DIRECTION ( 'NONE',  ( 1.000000000000000000, 0.000000000000000000, 0.000000000000000000 ) ) ;
#60187=CARTESIAN_POINT ( 'NONE',  ( -10.01517768586949231, 131.1949999999999363, -6.132527647946036459E-16 ) ) ;
#60188=MECHANICAL_DESIGN_GEOMETRIC_PRESENTATION_REPRESENTATION('',(#63549),#27621);
#60190=ADVANCED_FACE ( 'NONE', ( #33843 ), #13613, .T. ) ;
#60192=CARTESIAN_POINT ( 'NONE',  ( -1.166476076187854022E-15, 133.0549999999999784, 9.525000000000000355 ) ) ;
#60194=AXIS2_PLACEMENT_3D ( 'NONE', #48700, #22615, #55998 ) ;
#60196=VERTEX_POINT ( 'NONE', #3174 ) ;
#60197=CARTESIAN_POINT ( 'NONE',  ( 3.094860106618431583, 154.2049999999999272, 9.525000000000000355 ) ) ;
#60198=DIRECTION ( 'NONE',  ( 1.000000000000000000, -1.776356839400250465E-15, 0.000000000000000000 ) ) ;
#60200=CARTESIAN_POINT ( 'NONE',  ( -74.99999999999998579, 50.00000000000000000, -10.49999999999999822 ) ) ;
#60201=EDGE_CURVE ( 'NONE', #45776, #32941, #15224, .T. ) ;
#60202=DIRECTION ( 'NONE',  ( 0.000000000000000000, 0.000000000000000000, -1.000000000000000000 ) ) ;
#60203=( NAMED_UNIT ( * ) PLANE_ANGLE_UNIT ( ) SI_UNIT ( $, .RADIAN. ) );
#60205=ORIENTED_EDGE ( 'NONE', *, *, #61057, .T. ) ;
#60206=CARTESIAN_POINT ( 'NONE',  ( -71.50000000000000000, 14.49137674618942562, -9.500000000000000000 ) ) ;
#60212=UNCERTAINTY_MEASURE_WITH_UNIT (LENGTH_MEASURE( 1.000000000000000082E-05 ), #63756, 'distance_accuracy_value', 'NONE');
#60214=SURFACE_STYLE_USAGE ( .BOTH. , #21539 ) ;
#60216=( LENGTH_UNIT ( ) NAMED_UNIT ( * ) SI_UNIT ( .MILLI., .METRE. ) );
#60227=DIRECTION ( 'NONE',  ( -1.000000000000000000, 0.000000000000000000, 0.000000000000000000 ) ) ;
#60228=DIRECTION ( 'NONE',  ( 0.000000000000000000, 0.000000000000000000, 1.000000000000000000 ) ) ;
#60231=ORIENTED_EDGE ( 'NONE', *, *, #3521, .F. ) ;
#60232=FACE_OUTER_BOUND ( 'NONE', #48809, .T. ) ;
#60233=FILL_AREA_STYLE_COLOUR ( '', #57130 ) ;
#60234=DIRECTION ( 'NONE',  ( 0.000000000000000000, 1.000000000000000000, -0.000000000000000000 ) ) ;
#60237=CARTESIAN_POINT ( 'NONE',  ( 3.094860106618435136, 133.2950000000000159, -9.525000000000000355 ) ) ;
#60239=STYLED_ITEM ( 'NONE', ( #20135 ), #1547 ) ;
#60250=DIRECTION ( 'NONE',  ( -0.000000000000000000, -0.000000000000000000, 1.000000000000000000 ) ) ;
#60254=DIRECTION ( 'NONE',  ( -0.000000000000000000, -0.000000000000000000, -1.000000000000000000 ) ) ;
#60258=EDGE_LOOP ( 'NONE', ( #56189, #46110, #60515, #26339 ) ) ;
#60260=AXIS2_PLACEMENT_3D ( 'NONE', #43550, #54385, #37588 ) ;
#60261=EDGE_LOOP ( 'NONE', ( #10801, #24035, #10449, #11433 ) ) ;
#60263=SURFACE_STYLE_USAGE ( .BOTH. , #66586 ) ;
#60266=DIRECTION ( 'NONE',  ( 1.000000000000000000, 0.000000000000000000, 0.000000000000000000 ) ) ;
#60267=FILL_AREA_STYLE_COLOUR ( '', #19667 ) ;
#60268=CARTESIAN_POINT ( 'NONE',  ( 7.632228543268608334, 150.4570736234661581, -2.479861379858951942 ) ) ;
#60269=ORIENTED_EDGE ( 'NONE', *, *, #31007, .F. ) ;
#60270=ADVANCED_FACE ( 'NONE', ( #30645 ), #50698, .T. ) ;
#60275=( GEOMETRIC_REPRESENTATION_CONTEXT ( 3 ) GLOBAL_UNCERTAINTY_ASSIGNED_CONTEXT ( ( #57339 ) ) GLOBAL_UNIT_ASSIGNED_CONTEXT ( ( #21327, #4812, #16101 ) ) REPRESENTATION_CONTEXT ( 'NONE', 'WORKASPACE' ) );
#60284=DIRECTION ( 'NONE',  ( 0.000000000000000000, 0.000000000000000000, -1.000000000000000000 ) ) ;
#60285=( GEOMETRIC_REPRESENTATION_CONTEXT ( 3 ) GLOBAL_UNCERTAINTY_ASSIGNED_CONTEXT ( ( #44585 ) ) GLOBAL_UNIT_ASSIGNED_CONTEXT ( ( #41801, #10456, #42497 ) ) REPRESENTATION_CONTEXT ( 'NONE', 'WORKASPACE' ) );
#60287=CARTESIAN_POINT ( 'NONE',  ( -45.78667142738931517, 8.935426707107499311, -6.369485321263473665 ) ) ;
#60290=DIRECTION ( 'NONE',  ( -0.7071067811865352493, 8.659560562354781249E-17, 0.7071067811865597852 ) ) ;
#60292=ADVANCED_FACE ( 'NONE', ( #41255 ), #51787, .F. ) ;
#60293=CARTESIAN_POINT ( 'NONE',  ( -74.12609030924235753, 9.272074904602392920, 6.224541297626261738 ) ) ;
#60296=CARTESIAN_POINT ( 'NONE',  ( 54.99999999999999289, 2.409368300552961372E-15, -7.000000000000017764 ) ) ;
#60298=DIRECTION ( 'NONE',  ( 1.000000000000000000, 0.000000000000000000, 0.000000000000000000 ) ) ;
#60300=CARTESIAN_POINT ( 'NONE',  ( -8.102448949553179958, 133.8949999999999818, -5.886773742842749790 ) ) ;
#60303=VERTEX_POINT ( 'NONE', #35953 ) ;
#60304=LINE ( 'NONE', #55378, #4343 ) ;
#60306=FILL_AREA_STYLE_COLOUR ( '', #34390 ) ;
#60321=CIRCLE ( 'NONE', #23281, 17.00000000000000000 ) ;
#60323=( NAMED_UNIT ( * ) SI_UNIT ( $, .STERADIAN. ) SOLID_ANGLE_UNIT ( ) );
#60324=SURFACE_STYLE_FILL_AREA ( #33935 ) ;
#60330=FILL_AREA_STYLE_COLOUR ( '', #55049 ) ;
#60331=CARTESIAN_POINT ( 'NONE',  ( -41.47640344042682869, 107.6239624391513559, 3.580003982102259119 ) ) ;
#60332=( NAMED_UNIT ( * ) PLANE_ANGLE_UNIT ( ) SI_UNIT ( $, .RADIAN. ) );
#60333=ORIENTED_EDGE ( 'NONE', *, *, #1631, .F. ) ;
#60336=DIRECTION ( 'NONE',  ( -1.000000000000000000, 0.000000000000000000, 0.000000000000000000 ) ) ;
#60338=CARTESIAN_POINT ( 'NONE',  ( 0.000000000000000000, 87.30187232391182306, 8.025000000000000355 ) ) ;
#60339=CARTESIAN_POINT ( 'NONE',  ( -6.826472737025120807, 124.5070736234661553, -4.959722759717907437 ) ) ;
#60341=LINE ( 'NONE', #33615, #46568 ) ;
#60343=CIRCLE ( 'NONE', #44693, 14.49999999999999822 ) ;
#60348=COLOUR_RGB ( '', 0.66274510, 0.83137255, 0.94901961) ;
#60352=CARTESIAN_POINT ( 'NONE',  ( 8.437984349512095861, 149.1929263765337907, 1.550032578732816828E-15 ) ) ;
#60354=EDGE_LOOP ( 'NONE', ( #63992, #9155, #22465, #35576 ) ) ;
#60359=ORIENTED_EDGE ( 'NONE', *, *, #45789, .F. ) ;
#60361=DIRECTION ( 'NONE',  ( -0.000000000000000000, -0.000000000000000000, -1.000000000000000000 ) ) ;
#60369=FILL_AREA_STYLE_COLOUR ( '', #51508 ) ;
#60370=CARTESIAN_POINT ( 'NONE',  ( -72.00000000000000000, 36.32520566882265456, 7.000000000000000000 ) ) ;
#60377=( LENGTH_UNIT ( ) NAMED_UNIT ( * ) SI_UNIT ( .MILLI., .METRE. ) );
#60387=SURFACE_SIDE_STYLE ('',( #38654 ) ) ;
#60388=CIRCLE ( 'NONE', #69404, 0.5000000000000004441 ) ;
#60392=( GEOMETRIC_REPRESENTATION_CONTEXT ( 3 ) GLOBAL_UNCERTAINTY_ASSIGNED_CONTEXT ( ( #40544 ) ) GLOBAL_UNIT_ASSIGNED_CONTEXT ( ( #55353, #21977, #38179 ) ) REPRESENTATION_CONTEXT ( 'NONE', 'WORKASPACE' ) );
#60395=CARTESIAN_POINT ( 'NONE',  ( -3.094860106618432471, 143.7050000000000125, -9.525000000000000355 ) ) ;
#60396=DIRECTION ( 'NONE',  ( -1.000000000000000000, 0.000000000000000000, 0.000000000000000000 ) ) ;
#60404=( GEOMETRIC_REPRESENTATION_CONTEXT ( 3 ) GLOBAL_UNCERTAINTY_ASSIGNED_CONTEXT ( ( #62952 ) ) GLOBAL_UNIT_ASSIGNED_CONTEXT ( ( #31119, #14621, #9353 ) ) REPRESENTATION_CONTEXT ( 'NONE', 'WORKASPACE' ) );
#60410=ADVANCED_FACE ( 'NONE', ( #32373 ), #16595, .F. ) ;
#60412=( LENGTH_UNIT ( ) NAMED_UNIT ( * ) SI_UNIT ( .MILLI., .METRE. ) );
#60421=EDGE_LOOP ( 'NONE', ( #45160, #23746, #26710, #3304 ) ) ;
#60427=SURFACE_SIDE_STYLE ('',( #64697 ) ) ;
#60433=ADVANCED_FACE ( 'NONE', ( #66122 ), #11415, .T. ) ;
#60434=SURFACE_SIDE_STYLE ('',( #18591 ) ) ;
#60436=CARTESIAN_POINT ( 'NONE',  ( -6.826472737025120807, 138.9929263765338305, 4.959722759717906548 ) ) ;
#60443=ORIENTED_EDGE ( 'NONE', *, *, #2493, .T. ) ;
#60449=DIRECTION ( 'NONE',  ( 1.000000000000000000, 0.000000000000000000, 0.000000000000000000 ) ) ;
#60454=SURFACE_STYLE_FILL_AREA ( #24213 ) ;
#60456=COLOUR_RGB ( '', 0.72549020, 0.75294118, 0.79215686) ;
#60458=CARTESIAN_POINT ( 'NONE',  ( -75.00000000000000000, 33.00000000000000000, -6.500000000000000000 ) ) ;
#60464=LINE ( 'NONE', #61495, #51091 ) ;
#60466=EDGE_CURVE ( 'NONE', #63831, #57600, #37334, .T. ) ;
#60475=CARTESIAN_POINT ( 'NONE',  ( -5.598654528085808657, 158.6449999999999818, 7.705886871421373741 ) ) ;
#60478=CYLINDRICAL_SURFACE ( 'NONE', #1102, 0.5000000000000004441 ) ;
#60485=AXIS2_PLACEMENT_3D ( 'NONE', #22353, #68302, #26066 ) ;
#60487=EDGE_CURVE ( 'NONE', #59067, #5967, #27159, .T. ) ;
#60488=EDGE_CURVE ( 'NONE', #19597, #4894, #50742, .T. ) ;
#60491=COLOUR_RGB ( '', 0.72549020, 0.75294118, 0.79215686) ;
#60497=CARTESIAN_POINT ( 'NONE',  ( -71.50000000000000000, 14.49137674618942562, -7.500000000000000000 ) ) ;
#60500=ORIENTED_EDGE ( 'NONE', *, *, #27909, .T. ) ;
#60503=DIRECTION ( 'NONE',  ( 0.000000000000000000, 0.000000000000000000, 1.000000000000000000 ) ) ;
#60505=ADVANCED_FACE ( 'NONE', ( #57666 ), #66504, .F. ) ;
#60507=CARTESIAN_POINT ( 'NONE',  ( -5.598654528085808657, 131.6449999999999818, 7.705886871421373741 ) ) ;
#60508=( NAMED_UNIT ( * ) SI_UNIT ( $, .STERADIAN. ) SOLID_ANGLE_UNIT ( ) );
#60510=CARTESIAN_POINT ( 'NONE',  ( -9.058813317711337021, 129.1550000000000011, -2.943386871421374895 ) ) ;
#60513=EDGE_CURVE ( 'NONE', #36309, #26603, #65342, .T. ) ;
#60514=CARTESIAN_POINT ( 'NONE',  ( 40.78947368421051323, 108.1536491499103363, -3.000000000000000444 ) ) ;
#60515=ORIENTED_EDGE ( 'NONE', *, *, #9902, .F. ) ;
#60516=CARTESIAN_POINT ( 'NONE',  ( -3.094860106618432471, 158.7049999999999557, -9.525000000000000355 ) ) ;
#60520=CARTESIAN_POINT ( 'NONE',  ( -74.99999999999998579, 50.00000000000000000, 9.500000000000001776 ) ) ;
#60523=CIRCLE ( 'NONE', #20066, 5.499999999999976907 ) ;
#60524=SURFACE_STYLE_USAGE ( .BOTH. , #33473 ) ;
#60525=ORIENTED_EDGE ( 'NONE', *, *, #26, .F. ) ;
#60526=COLOUR_RGB ( '', 0.72549020, 0.75294118, 0.79215686) ;
#60528=FILL_AREA_STYLE ('',( #6385 ) ) ;
#60531=( LENGTH_UNIT ( ) NAMED_UNIT ( * ) SI_UNIT ( .MILLI., .METRE. ) );
#60533=DIRECTION ( 'NONE',  ( 1.000000000000000000, 0.000000000000000000, 0.000000000000000000 ) ) ;
#60534=LINE ( 'NONE', #34514, #52953 ) ;
#60536=VERTEX_POINT ( 'NONE', #62239 ) ;
#60537=AXIS2_PLACEMENT_3D ( 'NONE', #36608, #19673, #14388 ) ;
#60540=CARTESIAN_POINT ( 'NONE',  ( 0.000000000000000000, 115.4999999999999574, 0.000000000000000000 ) ) ;
#60543=VERTEX_POINT ( 'NONE', #25980 ) ;
#60547=EDGE_CURVE ( 'NONE', #56195, #52813, #40666, .T. ) ;
#60550=CARTESIAN_POINT ( 'NONE',  ( 45.00000000000000000, 9.639620389971920389, 6.999999999999999112 ) ) ;
#60552=CARTESIAN_POINT ( 'NONE',  ( -5.598654528085806881, 127.7450000000000045, -7.705886871421374629 ) ) ;
#60555=CARTESIAN_POINT ( 'NONE',  ( -21.02379604162863913, 110.4999999999999858, -10.00000000000000000 ) ) ;
#60557=EDGE_CURVE ( 'NONE', #8139, #2682, #23815, .T. ) ;
#60564=EDGE_CURVE ( 'NONE', #63887, #56195, #67611, .T. ) ;
#60570=COLOUR_RGB ( '', 0.08235294, 0.09019608, 0.10196078) ;
#60572=CARTESIAN_POINT ( 'NONE',  ( -45.89268334517834802, 9.343685333619713873, 6.169793031889358126 ) ) ;
#60575=COLOUR_RGB ( '', 0.40784314, 0.44705882, 0.49803922) ;
#60578=PLANE ( 'NONE',  #59529 ) ;
#60581=VERTEX_POINT ( 'NONE', #16850 ) ;
#60583=ORIENTED_EDGE ( 'NONE', *, *, #16377, .T. ) ;
#60585=( NAMED_UNIT ( * ) SI_UNIT ( $, .STERADIAN. ) SOLID_ANGLE_UNIT ( ) );
#60587=SURFACE_STYLE_FILL_AREA ( #18049 ) ;
#60588=CARTESIAN_POINT ( 'NONE',  ( -4.716976649647097730, 151.3570736234661638, -6.492361379858953896 ) ) ;
#60590=( NAMED_UNIT ( * ) PLANE_ANGLE_UNIT ( ) SI_UNIT ( $, .RADIAN. ) );
#60592=CARTESIAN_POINT ( 'NONE',  ( 0.000000000000000000, 121.0570736234661524, -8.025000000000000355 ) ) ;
#60593=CARTESIAN_POINT ( 'NONE',  ( 8.102448949553181734, 124.5049999999999812, 5.886773742842750679 ) ) ;
#60594=( GEOMETRIC_REPRESENTATION_CONTEXT ( 3 ) GLOBAL_UNCERTAINTY_ASSIGNED_CONTEXT ( ( #55825 ) ) GLOBAL_UNIT_ASSIGNED_CONTEXT ( ( #7206, #33244, #23370 ) ) REPRESENTATION_CONTEXT ( 'NONE', 'WORKASPACE' ) );
#60602=SURFACE_STYLE_USAGE ( .BOTH. , #1825 ) ;
#60603=FILL_AREA_STYLE ('',( #46226 ) ) ;
#60605=EDGE_CURVE ( 'NONE', #53118, #38818, #5482, .T. ) ;
#60606=COLOUR_RGB ( '', 0.31764706, 0.68627451, 0.89019608) ;
#60609=DIRECTION ( 'NONE',  ( -0.000000000000000000, -0.000000000000000000, 1.000000000000000000 ) ) ;
#60611=AXIS2_PLACEMENT_3D ( 'NONE', #61271, #66916, #50729 ) ;
#60622=CIRCLE ( 'NONE', #69625, 0.5000000000000004441 ) ;
#60626=( GEOMETRIC_REPRESENTATION_CONTEXT ( 3 ) GLOBAL_UNCERTAINTY_ASSIGNED_CONTEXT ( ( #20777 ) ) GLOBAL_UNIT_ASSIGNED_CONTEXT ( ( #1128, #5414, #43128 ) ) REPRESENTATION_CONTEXT ( 'NONE', 'WORKASPACE' ) );
#60628=CARTESIAN_POINT ( 'NONE',  ( 34.99999999999999289, 99.99999999999997158, -4.000000000000000000 ) ) ;
#60629=CARTESIAN_POINT ( 'NONE',  ( -9.058813317711338797, 131.3449999999999989, 2.943386871421373563 ) ) ;
#60631=SURFACE_STYLE_USAGE ( .BOTH. , #50450 ) ;
#60632=VERTEX_POINT ( 'NONE', #21758 ) ;
#60635=( NAMED_UNIT ( * ) SI_UNIT ( $, .STERADIAN. ) SOLID_ANGLE_UNIT ( ) );
#60636=SURFACE_SIDE_STYLE ('',( #33915 ) ) ;
#60637=SURFACE_STYLE_FILL_AREA ( #12112 ) ;
#60643=ORIENTED_EDGE ( 'NONE', *, *, #64407, .F. ) ;
#60644=AXIS2_PLACEMENT_3D ( 'NONE', #55573, #66112, #50306 ) ;
#60647=( NAMED_UNIT ( * ) PLANE_ANGLE_UNIT ( ) SI_UNIT ( $, .RADIAN. ) );
#60648=EDGE_CURVE ( 'NONE', #25670, #30747, #4730, .T. ) ;
#60655=PRESENTATION_STYLE_ASSIGNMENT (( #17782 ) ) ;
#60656=CARTESIAN_POINT ( 'NONE',  ( 45.50000000000000000, -1.469576158976824618E-14, -6.500000000000000000 ) ) ;
#60657=DIRECTION ( 'NONE',  ( 0.000000000000000000, 0.000000000000000000, 1.000000000000000000 ) ) ;
#60659=( BOUNDED_CURVE ( )  B_SPLINE_CURVE ( 3, ( #13667, #24547, #19273, #40782 ),
 .UNSPECIFIED., .F., .F. ) 
 B_SPLINE_CURVE_WITH_KNOTS ( ( 4, 4 ),
 ( 4.712388980384692339, 6.283185307179586232 ),
 .UNSPECIFIED. ) 
 CURVE ( )  GEOMETRIC_REPRESENTATION_ITEM ( )  RATIONAL_B_SPLINE_CURVE ( ( 1.000000000000000000, 0.8047378541243654926, 0.8047378541243654926, 1.000000000000000000 ) ) 
 REPRESENTATION_ITEM ( '' )  );
#60661=SURFACE_STYLE_FILL_AREA ( #23062 ) ;
#60665=LINE ( 'NONE', #24092, #59526 ) ;
#60666=( NAMED_UNIT ( * ) PLANE_ANGLE_UNIT ( ) SI_UNIT ( $, .RADIAN. ) );
#60674=VERTEX_POINT ( 'NONE', #33007 ) ;
#60675=PRESENTATION_STYLE_ASSIGNMENT (( #51192 ) ) ;
#60676=CARTESIAN_POINT ( 'NONE',  ( 2.607480562269071989, 125.7070736234661723, 8.025000000000002132 ) ) ;
#60681=VERTEX_POINT ( 'NONE', #54447 ) ;
#60683=DIRECTION ( 'NONE',  ( 1.000000000000000000, -0.000000000000000000, -0.000000000000000000 ) ) ;
#60684=VERTEX_POINT ( 'NONE', #5907 ) ;
#60692=B_SPLINE_CURVE_WITH_KNOTS ( 'NONE', 3,
 ( #28352, #40342, #67069, #36110, #30800, #19559, #45650, #56497, #8675, #9375, #3692, #41053, #24823, #36486 ),
 .UNSPECIFIED., .F., .F.,
 ( 4, 2, 2, 2, 2, 2, 4 ),
 ( 0.000000000000000000, 0.0005917671672764541774, 0.001183534334552908355, 0.001479417918191135335, 0.001775301501829362532, 0.002071185085467589729, 0.002367068669105816710 ),
 .UNSPECIFIED. ) ;
#60694=CARTESIAN_POINT ( 'NONE',  ( -9.827790563157511022E-16, 124.4429263765338192, 8.025000000000000355 ) ) ;
#60696=UNCERTAINTY_MEASURE_WITH_UNIT (LENGTH_MEASURE( 1.000000000000000082E-05 ), #67726, 'distance_accuracy_value', 'NONE');
#60698=CARTESIAN_POINT ( 'NONE',  ( 6.826472737025121695, 161.4929263765338305, -4.959722759717905660 ) ) ;
#60700=COLOUR_RGB ( '', 0.09019608, 0.27058824, 0.51372549) ;
#60706=FILL_AREA_STYLE_COLOUR ( '', #18951 ) ;
#60707=SURFACE_STYLE_FILL_AREA ( #66340 ) ;
#60710=DIRECTION ( 'NONE',  ( -0.000000000000000000, -0.000000000000000000, -1.000000000000000000 ) ) ;
#60713=SURFACE_STYLE_USAGE ( .BOTH. , #50192 ) ;
#60714=LINE ( 'NONE', #62108, #4367 ) ;
#60722=ADVANCED_FACE ( 'NONE', ( #61781 ), #13258, .F. ) ;
#60726=CARTESIAN_POINT ( 'NONE',  ( 60.00000000000000000, 1.797044900979284448E-15, -9.500000000000000000 ) ) ;
#60727=CARTESIAN_POINT ( 'NONE',  ( 44.15219150100326573, 9.717397167001085023, 3.137420992959929489 ) ) ;
#60731=DIRECTION ( 'NONE',  ( 0.000000000000000000, -0.000000000000000000, 1.000000000000000000 ) ) ;
#60732=EDGE_CURVE ( 'NONE', #61248, #66756, #23151, .T. ) ;
#60734=CARTESIAN_POINT ( 'NONE',  ( -8.102448949553181734, 150.6050000000000182, 5.886773742842747126 ) ) ;
#60737=EDGE_CURVE ( 'NONE', #50095, #12034, #32815, .T. ) ;
#60738=UNCERTAINTY_MEASURE_WITH_UNIT (LENGTH_MEASURE( 1.000000000000000082E-05 ), #46100, 'distance_accuracy_value', 'NONE');
#60740=STYLED_ITEM ( 'NONE', ( #20269 ), #16855 ) ;
#60742=EDGE_CURVE ( 'NONE', #61621, #52608, #66556, .T. ) ;
#60743=( LENGTH_UNIT ( ) NAMED_UNIT ( * ) SI_UNIT ( .MILLI., .METRE. ) );
#60745=EDGE_CURVE ( 'NONE', #59067, #197, #2416, .T. ) ;
#60747=ORIENTED_EDGE ( 'NONE', *, *, #69200, .F. ) ;
#60748=ORIENTED_EDGE ( 'NONE', *, *, #6364, .F. ) ;
#60749=FILL_AREA_STYLE_COLOUR ( '', #35272 ) ;
#60751=DIRECTION ( 'NONE',  ( -0.000000000000000000, 1.000000000000000000, -0.000000000000000000 ) ) ;
#60755=DIRECTION ( 'NONE',  ( -0.000000000000000000, -0.000000000000000000, -1.000000000000000000 ) ) ;
#60756=SURFACE_STYLE_USAGE ( .BOTH. , #45680 ) ;
#60768=ORIENTED_EDGE ( 'NONE', *, *, #18581, .F. ) ;
#60771=CARTESIAN_POINT ( 'NONE',  ( 15.98999599679679839, 117.9999999999999716, 10.00000000000000000 ) ) ;
#60773=( NAMED_UNIT ( * ) SI_UNIT ( $, .STERADIAN. ) SOLID_ANGLE_UNIT ( ) );
#60775=CARTESIAN_POINT ( 'NONE',  ( 2.607480562269071989, 133.5929263765337680, 8.025000000000002132 ) ) ;
#60776=CARTESIAN_POINT ( 'NONE',  ( 0.000000000000000000, 87.30187232391182306, 0.000000000000000000 ) ) ;
#60778=COLOUR_RGB ( '', 0.31764706, 0.68627451, 0.89019608) ;
#60779=CARTESIAN_POINT ( 'NONE',  ( -4.716976649647097730, 114.2429263765338163, -6.492361379858953896 ) ) ;
#60784=SURFACE_STYLE_FILL_AREA ( #67463 ) ;
#60787=DIRECTION ( 'NONE',  ( -0.03448275862069643399, 0.9994052928406507164, 0.000000000000000000 ) ) ;
#60789=FILL_AREA_STYLE ('',( #39053 ) ) ;
#60795=ORIENTED_EDGE ( 'NONE', *, *, #46109, .F. ) ;
#60798=CARTESIAN_POINT ( 'NONE',  ( -20.03990113061529144, 115.4999999999999574, 9.999999999999998224 ) ) ;
#60800=( NAMED_UNIT ( * ) PLANE_ANGLE_UNIT ( ) SI_UNIT ( $, .RADIAN. ) );
#60802=FILL_AREA_STYLE_COLOUR ( '', #31453 ) ;
#60803=PRESENTATION_STYLE_ASSIGNMENT (( #54834 ) ) ;
#60808=VERTEX_POINT ( 'NONE', #17864 ) ;
#60810=SURFACE_STYLE_USAGE ( .BOTH. , #26481 ) ;
#60813=CIRCLE ( 'NONE', #27112, 0.5000000000000004441 ) ;
#60816=CARTESIAN_POINT ( 'NONE',  ( 3.432329715542617787, 154.5000000000000284, -8.895958039233530457 ) ) ;
#60818=CARTESIAN_POINT ( 'NONE',  ( 9.827790563157511022E-16, 87.30187232391182306, -8.025000000000000355 ) ) ;
#60819=ADVANCED_FACE ( 'NONE', ( #24494 ), #51966, .T. ) ;
#60820=AXIS2_PLACEMENT_3D ( 'NONE', #61659, #62391, #14208 ) ;
#60823=CARTESIAN_POINT ( 'NONE',  ( -3.094860106618434248, 120.9049999999999869, 9.525000000000000355 ) ) ;
#60825=AXIS2_PLACEMENT_3D ( 'NONE', #38328, #54783, #14320 ) ;
#60826=EDGE_CURVE ( 'NONE', #58400, #20552, #14315, .T. ) ;
#60831=UNCERTAINTY_MEASURE_WITH_UNIT (LENGTH_MEASURE( 1.000000000000000082E-05 ), #47089, 'distance_accuracy_value', 'NONE');
#60833=CARTESIAN_POINT ( 'NONE',  ( 40.78947368421051323, 108.1536491499103363, -3.000000000000000444 ) ) ;
#60834=VERTEX_POINT ( 'NONE', #68840 ) ;
#60843=SURFACE_STYLE_FILL_AREA ( #7405 ) ;
#60845=ORIENTED_EDGE ( 'NONE', *, *, #69490, .F. ) ;
#60846=DIRECTION ( 'NONE',  ( -0.000000000000000000, -0.000000000000000000, -1.000000000000000000 ) ) ;
#60847=( NAMED_UNIT ( * ) SI_UNIT ( $, .STERADIAN. ) SOLID_ANGLE_UNIT ( ) );
#60852=CYLINDRICAL_SURFACE ( 'NONE', #6044, 0.5000000000000004441 ) ;
#60853=SURFACE_STYLE_USAGE ( .BOTH. , #51612 ) ;
#60862=( LENGTH_UNIT ( ) NAMED_UNIT ( * ) SI_UNIT ( .MILLI., .METRE. ) );
#60863=CARTESIAN_POINT ( 'NONE',  ( -3.094860106618432471, 130.5949999999999989, -9.525000000000000355 ) ) ;
#60864=( NAMED_UNIT ( * ) SI_UNIT ( $, .STERADIAN. ) SOLID_ANGLE_UNIT ( ) );
#60866=VERTEX_POINT ( 'NONE', #57575 ) ;
#60868=CARTESIAN_POINT ( 'NONE',  ( 5.598654528085809545, 140.2549999999999955, -7.705886871421373741 ) ) ;
#60869=COLOUR_RGB ( '', 0.31764706, 0.68627451, 0.89019608) ;
#60872=CARTESIAN_POINT ( 'NONE',  ( 8.102448949553181734, 154.5049999999999670, 5.886773742842750679 ) ) ;
#60873=DIRECTION ( 'NONE',  ( 0.000000000000000000, 0.000000000000000000, -1.000000000000000000 ) ) ;
#60874=UNCERTAINTY_MEASURE_WITH_UNIT (LENGTH_MEASURE( 1.000000000000000082E-05 ), #9791, 'distance_accuracy_value', 'NONE');
#60878=SURFACE_SIDE_STYLE ('',( #66520 ) ) ;
#60881=ORIENTED_EDGE ( 'NONE', *, *, #53695, .F. ) ;
#60883=SURFACE_STYLE_USAGE ( .BOTH. , #1759 ) ;
#60885=CIRCLE ( 'NONE', #9245, 0.5000000000000004441 ) ;
#60887=DIRECTION ( 'NONE',  ( 0.000000000000000000, 1.000000000000000000, -0.000000000000000000 ) ) ;
#60888=UNCERTAINTY_MEASURE_WITH_UNIT (LENGTH_MEASURE( 1.000000000000000082E-05 ), #23417, 'distance_accuracy_value', 'NONE');
#60889=VECTOR ( 'NONE', #47272, 1000.000000000000000 ) ;
#60892=FILL_AREA_STYLE ('',( #2086 ) ) ;
#60894=VERTEX_POINT ( 'NONE', #31164 ) ;
#60895=CARTESIAN_POINT ( 'NONE',  ( -44.99310882439082349, 9.606342690214754398, -3.226428160770427489 ) ) ;
#60898=EDGE_LOOP ( 'NONE', ( #35693, #58453, #36491 ) ) ;
#60900=( NAMED_UNIT ( * ) SI_UNIT ( $, .STERADIAN. ) SOLID_ANGLE_UNIT ( ) );
#60901=CARTESIAN_POINT ( 'NONE',  ( -45.91547277936962246, 9.430195807687219656, -6.500000000000000000 ) ) ;
#60903=AXIS2_PLACEMENT_3D ( 'NONE', #40602, #41650, #8916 ) ;
#60906=( LENGTH_UNIT ( ) NAMED_UNIT ( * ) SI_UNIT ( .MILLI., .METRE. ) );
#60911=CARTESIAN_POINT ( 'NONE',  ( 9.058813317711338797, 135.8449999999999989, -2.943386871421372675 ) ) ;
#60917=ADVANCED_FACE ( 'NONE', ( #10778 ), #53352, .T. ) ;
#60921=CIRCLE ( 'NONE', #48630, 10.50000000000000178 ) ;
#60923=MECHANICAL_DESIGN_GEOMETRIC_PRESENTATION_REPRESENTATION('',(#44119),#31712);
#60924=SURFACE_STYLE_FILL_AREA ( #13794 ) ;
#60927=ORIENTED_EDGE ( 'NONE', *, *, #34454, .F. ) ;
#60938=CARTESIAN_POINT ( 'NONE',  ( 34.99999999999999289, 118.4999999999999716, 7.500000000000000000 ) ) ;
#60939=CARTESIAN_POINT ( 'NONE',  ( 8.437984349512095861, 156.3070736234661524, 1.550032578732817026E-15 ) ) ;
#60941=CIRCLE ( 'NONE', #67701, 0.5000000000000004441 ) ;
#60942=ORIENTED_EDGE ( 'NONE', *, *, #28655, .F. ) ;
#60943=CARTESIAN_POINT ( 'NONE',  ( 34.99999999999999289, 99.99999999999998579, 7.500000000000000000 ) ) ;
#60946=CARTESIAN_POINT ( 'NONE',  ( -2.607480562269041791, 121.2070736234661581, -8.025000000000021672 ) ) ;
#60948=CARTESIAN_POINT ( 'NONE',  ( -8.102448949553181734, 129.0049999999999670, -5.886773742842749790 ) ) ;
#60950=CIRCLE ( 'NONE', #7042, 9.499999999999994671 ) ;
#60953=DIRECTION ( 'NONE',  ( 1.000000000000000000, 0.000000000000000000, 0.000000000000000000 ) ) ;
#60956=ORIENTED_EDGE ( 'NONE', *, *, #69561, .F. ) ;
#60957=VECTOR ( 'NONE', #34640, 1000.000000000000000 ) ;
#60958=FILL_AREA_STYLE ('',( #31895 ) ) ;
#60963=AXIS2_PLACEMENT_3D ( 'NONE', #28775, #50259, #1981 ) ;
#60966=ORIENTED_EDGE ( 'NONE', *, *, #55402, .F. ) ;
#60970=MECHANICAL_DESIGN_GEOMETRIC_PRESENTATION_REPRESENTATION('',(#12665),#8175);
#60972=CARTESIAN_POINT ( 'NONE',  ( -74.13368340934296441, 9.243037840626097790, 6.242508038240137225 ) ) ;
#60976=FILL_AREA_STYLE_COLOUR ( '', #35055 ) ;
#60977=AXIS2_PLACEMENT_3D ( 'NONE', #16188, #52769, #4544 ) ;
#60981=CARTESIAN_POINT ( 'NONE',  ( -20.57648123223228254, 154.9999999999999716, 10.27659574468085069 ) ) ;
#60982=CARTESIAN_POINT ( 'NONE',  ( -9.058813317711338797, 146.3449999999999989, 2.943386871421373563 ) ) ;
#60985=ADVANCED_FACE ( 'NONE', ( #58611 ), #20516, .F. ) ;
#60986=ORIENTED_EDGE ( 'NONE', *, *, #61166, .T. ) ;
#60987=( NAMED_UNIT ( * ) PLANE_ANGLE_UNIT ( ) SI_UNIT ( $, .RADIAN. ) );
#60989=SURFACE_STYLE_FILL_AREA ( #18097 ) ;
#60990=SURFACE_STYLE_USAGE ( .BOTH. , #44533 ) ;
#60995=MECHANICAL_DESIGN_GEOMETRIC_PRESENTATION_REPRESENTATION('',(#12692),#55385);
#60996=FILL_AREA_STYLE ('',( #796 ) ) ;
#60998=ADVANCED_FACE ( 'NONE', ( #10440 ), #17175, .F. ) ;
#61004=SURFACE_STYLE_FILL_AREA ( #33251 ) ;
#61013=COLOUR_RGB ( '', 0.09019608, 0.27058824, 0.51372549) ;
#61014=CARTESIAN_POINT ( 'NONE',  ( -24.21231517720798010, 113.4999999999999858, 7.500000000000000000 ) ) ;
#61015=SPHERICAL_SURFACE ( 'NONE', #14773, 0.5000000000000000000 ) ;
#61021=DIRECTION ( 'NONE',  ( 0.000000000000000000, 0.000000000000000000, 1.000000000000000000 ) ) ;
#61022=CARTESIAN_POINT ( 'NONE',  ( -41.13907225104363619, 107.8972693614176137, 3.376186789259631560 ) ) ;
#61023=VERTEX_POINT ( 'NONE', #45246 ) ;
#61025=FILL_AREA_STYLE ('',( #12844 ) ) ;
#61026=CARTESIAN_POINT ( 'NONE',  ( 0.000000000000000000, 110.5741857357814553, -9.450814264218539762 ) ) ;
#61027=VERTEX_POINT ( 'NONE', #61026 ) ;
#61028=( LENGTH_UNIT ( ) NAMED_UNIT ( * ) SI_UNIT ( .MILLI., .METRE. ) );
#61029=MECHANICAL_DESIGN_GEOMETRIC_PRESENTATION_REPRESENTATION('',(#27322),#1530);
#61030=CARTESIAN_POINT ( 'NONE',  ( 7.632228543268608334, 126.4570736234661723, -2.479861379858951942 ) ) ;
#61032=CARTESIAN_POINT ( 'NONE',  ( 21.02379604162863913, 114.9999999999999574, -10.00000000000000000 ) ) ;
#61039=FILL_AREA_STYLE_COLOUR ( '', #52191 ) ;
#61042=ORIENTED_EDGE ( 'NONE', *, *, #53929, .T. ) ;
#61045=EDGE_CURVE ( 'NONE', #9417, #61535, #65271, .T. ) ;
#61047=FILL_AREA_STYLE_COLOUR ( '', #39638 ) ;
#61048=ORIENTED_EDGE ( 'NONE', *, *, #67414, .F. ) ;
#61049=SURFACE_SIDE_STYLE ('',( #29021 ) ) ;
#61050=FACE_OUTER_BOUND ( 'NONE', #28778, .T. ) ;
#61053=ADVANCED_FACE ( 'NONE', ( #1884 ), #35116, .F. ) ;
#61054=VECTOR ( 'NONE', #24249, 1000.000000000000000 ) ;
#61057=EDGE_CURVE ( 'NONE', #15830, #39204, #33608, .T. ) ;
#61061=DIRECTION ( 'NONE',  ( 1.000000000000000000, 0.000000000000000000, -0.000000000000000000 ) ) ;
#61063=AXIS2_PLACEMENT_3D ( 'NONE', #55128, #22450, #65361 ) ;
#61066=CARTESIAN_POINT ( 'NONE',  ( -3.094860106618434248, 110.7949999999999733, 9.525000000000000355 ) ) ;
#61068=CIRCLE ( 'NONE', #66708, 27.49999999999999645 ) ;
#61069=CIRCLE ( 'NONE', #46527, 23.00000000000000000 ) ;
#61071=DIRECTION ( 'NONE',  ( -0.000000000000000000, -1.000000000000000000, -0.000000000000000000 ) ) ;
#61072=VERTEX_POINT ( 'NONE', #1548 ) ;
#61074=CYLINDRICAL_SURFACE ( 'NONE', #56817, 0.5000000000000004441 ) ;
#61075=EDGE_CURVE ( 'NONE', #52813, #8395, #2525, .T. ) ;
#61076=DIRECTION ( 'NONE',  ( -0.000000000000000000, -0.000000000000000000, -1.000000000000000000 ) ) ;
#61079=STYLED_ITEM ( 'NONE', ( #61285 ), #37996 ) ;
#61082=DIRECTION ( 'NONE',  ( 0.000000000000000000, 0.000000000000000000, -1.000000000000000000 ) ) ;
#61099=CARTESIAN_POINT ( 'NONE',  ( 3.094860106618431583, 148.2050000000000125, 9.525000000000000355 ) ) ;
#61108=CARTESIAN_POINT ( 'NONE',  ( 71.50000000000000000, 14.49137674618942562, -9.500000000000000000 ) ) ;
#61119=ORIENTED_EDGE ( 'NONE', *, *, #59447, .T. ) ;
#61121=FILL_AREA_STYLE_COLOUR ( '', #51148 ) ;
#61125=( NAMED_UNIT ( * ) PLANE_ANGLE_UNIT ( ) SI_UNIT ( $, .RADIAN. ) );
#61126=DIRECTION ( 'NONE',  ( 0.000000000000000000, 0.000000000000000000, 1.000000000000000000 ) ) ;
#61128=EDGE_CURVE ( 'NONE', #42152, #45776, #39969, .T. ) ;
#61130=DIRECTION ( 'NONE',  ( 0.000000000000000000, 0.000000000000000000, 1.000000000000000000 ) ) ;
#61137=DIRECTION ( 'NONE',  ( 0.000000000000000000, 0.000000000000000000, 1.000000000000000000 ) ) ;
#61139=EDGE_CURVE ( 'NONE', #61023, #8546, #23917, .T. ) ;
#61141=AXIS2_PLACEMENT_3D ( 'NONE', #36922, #52400, #62561 ) ;
#61143=CARTESIAN_POINT ( 'NONE',  ( 4.716976649647099507, 146.6429263765338078, -6.492361379858953008 ) ) ;
#61152=CARTESIAN_POINT ( 'NONE',  ( -9.827790563157511022E-16, 140.5570736234661524, 8.025000000000000355 ) ) ;
#61153=DIRECTION ( 'NONE',  ( -0.000000000000000000, -0.000000000000000000, -1.000000000000000000 ) ) ;
#61156=DIRECTION ( 'NONE',  ( 0.000000000000000000, 1.000000000000000000, 0.000000000000000000 ) ) ;
#61163=ORIENTED_EDGE ( 'NONE', *, *, #169, .T. ) ;
#61164=DIRECTION ( 'NONE',  ( 0.000000000000000000, 0.000000000000000000, -1.000000000000000000 ) ) ;
#61166=EDGE_CURVE ( 'NONE', #10616, #52417, #12489, .T. ) ;
#61172=CARTESIAN_POINT ( 'NONE',  ( 15.98999599679679839, 146.4999999999999716, -7.500000000000000000 ) ) ;
#61175=DIRECTION ( 'NONE',  ( 0.000000000000000000, 0.000000000000000000, 1.000000000000000000 ) ) ;
#61176=ORIENTED_EDGE ( 'NONE', *, *, #12062, .T. ) ;
#61184=TOROIDAL_SURFACE ( 'NONE', #32011, 14.49999999999999822, 0.5000000000000000000 ) ;
#61187=CARTESIAN_POINT ( 'NONE',  ( -9.058813317711338797, 117.4549999999999841, 2.943386871421373563 ) ) ;
#61193=( BOUNDED_SURFACE ( )  B_SPLINE_SURFACE ( 3, 2, ( 
 ( #23818, #45323, #18560 ),
 ( #56162, #13250, #40042 ),
 ( #61430, #24162, #9668 ),
 ( #21216, #42398, #56515 ),
 ( #42050, #3000, #63454 ),
 ( #63788, #10682, #51258 ),
 ( #15631, #57844, #40362 ),
 ( #20179, #37111, #58179 ),
 ( #15306, #61774, #15989 ),
 ( #52909, #32132, #31416 ) ),
 .UNSPECIFIED., .F., .F., .F. ) 
 B_SPLINE_SURFACE_WITH_KNOTS ( ( 4, 2, 2, 2, 4 ),
 ( 3, 3 ),
 ( 0.0004231141141892710367, 0.0008386083364002310404, 0.001254102558611191152, 0.001669596780822151265, 0.002085091003033111377 ),
 ( 0.000000000000000000, 1.000000000000000000 ),
 .UNSPECIFIED. ) 
 GEOMETRIC_REPRESENTATION_ITEM ( )  RATIONAL_B_SPLINE_SURFACE ( (
 ( 1.000000000000000000, 0.7071067811865573427, 1.000000000000000000),
 ( 1.000000000000000000, 0.7275888720224806816, 1.000000000000000000),
 ( 1.000000000000000000, 0.7463828630404263365, 1.000000000000000000),
 ( 1.000000000000000000, 0.7812714640742435268, 1.000000000000000000),
 ( 1.000000000000000000, 0.7963642535525788935, 1.000000000000000000),
 ( 1.000000000000000000, 0.8224433532025096083, 1.000000000000000000),
 ( 1.000000000000000000, 0.8326146287104877475, 1.000000000000000000),
 ( 1.000000000000000000, 0.8468497872537316118, 1.000000000000000000),
 ( 1.000000000000000000, 0.8504932968929420634, 1.000000000000000000),
 ( 1.000000000000000000, 0.8505317485662416965, 1.000000000000000000) ) ) 
 REPRESENTATION_ITEM ( '' )  SURFACE ( )  );
#61201=DIRECTION ( 'NONE',  ( 0.000000000000000000, 0.000000000000000000, -1.000000000000000000 ) ) ;
#61203=ORIENTED_EDGE ( 'NONE', *, *, #68679, .F. ) ;
#61209=SURFACE_STYLE_FILL_AREA ( #66494 ) ;
#61211=DIRECTION ( 'NONE',  ( 1.000000000000000000, 0.000000000000000000, 0.000000000000000000 ) ) ;
#61216=CIRCLE ( 'NONE', #67972, 0.5000000000000000000 ) ;
#61220=ORIENTED_EDGE ( 'NONE', *, *, #65591, .F. ) ;
#61221=EDGE_CURVE ( 'NONE', #30521, #28945, #19505, .T. ) ;
#61224=DIRECTION ( 'NONE',  ( 1.156482317317873451E-16, -1.000000000000000000, -0.000000000000000000 ) ) ;
#61226=CARTESIAN_POINT ( 'NONE',  ( 3.094860106618435136, 142.2950000000000159, -9.525000000000000355 ) ) ;
#61227=DIRECTION ( 'NONE',  ( 0.000000000000000000, -0.000000000000000000, 1.000000000000000000 ) ) ;
#61228=ORIENTED_EDGE ( 'NONE', *, *, #28096, .F. ) ;
#61230=CARTESIAN_POINT ( 'NONE',  ( -5.598654528085806881, 140.8549999999999898, -7.705886871421374629 ) ) ;
#61233=CARTESIAN_POINT ( 'NONE',  ( -9.058813317711338797, 153.4549999999999841, 2.943386871421373563 ) ) ;
#61236=AXIS2_PLACEMENT_3D ( 'NONE', #43781, #44486, #24015 ) ;
#61239=EDGE_CURVE ( 'NONE', #32321, #21436, #49739, .T. ) ;
#61241=SURFACE_STYLE_FILL_AREA ( #66523 ) ;
#61247=ADVANCED_FACE ( 'NONE', ( #9682 ), #56500, .T. ) ;
#61248=VERTEX_POINT ( 'NONE', #62427 ) ;
#61249=STYLED_ITEM ( 'NONE', ( #38856 ), #56460 ) ;
#61251=CARTESIAN_POINT ( 'NONE',  ( -44.99999999999977973, 149.4999999999999716, 9.500000000000000000 ) ) ;
#61252=( NAMED_UNIT ( * ) PLANE_ANGLE_UNIT ( ) SI_UNIT ( $, .RADIAN. ) );
#61253=SURFACE_SIDE_STYLE ('',( #50706 ) ) ;
#61266=COLOUR_RGB ( '', 0.08235294, 0.09019608, 0.10196078) ;
#61267=CARTESIAN_POINT ( 'NONE',  ( -8.102448949553181734, 142.8949999999999818, -5.886773742842749790 ) ) ;
#61271=CARTESIAN_POINT ( 'NONE',  ( -72.50000000000000000, 35.92875272052971525, -9.500000000000000000 ) ) ;
#61273=DIRECTION ( 'NONE',  ( 1.000000000000000000, 0.000000000000000000, 0.000000000000000000 ) ) ;
#61277=CIRCLE ( 'NONE', #5130, 0.5000000000000004441 ) ;
#61278=DIRECTION ( 'NONE',  ( 1.000000000000000000, 0.000000000000000000, 0.000000000000000000 ) ) ;
#61280=( NAMED_UNIT ( * ) PLANE_ANGLE_UNIT ( ) SI_UNIT ( $, .RADIAN. ) );
#61282=CARTESIAN_POINT ( 'NONE',  ( -4.716976649647098618, 128.2570736234661695, 6.492361379858953008 ) ) ;
#61285=PRESENTATION_STYLE_ASSIGNMENT (( #34549 ) ) ;
#61286=DIRECTION ( 'NONE',  ( 0.000000000000000000, 0.000000000000000000, -1.000000000000000000 ) ) ;
#61288=CARTESIAN_POINT ( 'NONE',  ( -71.18918918918917882, 14.09971791521133255, -7.500000000000000000 ) ) ;
#61289=CARTESIAN_POINT ( 'NONE',  ( -71.74137931034481142, 36.89918356738973415, 10.00000000000000000 ) ) ;
#61290=ORIENTED_EDGE ( 'NONE', *, *, #63392, .F. ) ;
#61292=EDGE_LOOP ( 'NONE', ( #1376, #36648, #57427, #3190 ) ) ;
#61294=ADVANCED_FACE ( 'NONE', ( #14242 ), #16120, .F. ) ;
#61296=FILL_AREA_STYLE ('',( #13451 ) ) ;
#61297=CARTESIAN_POINT ( 'NONE',  ( 4.716976649647099507, 159.7570736234661695, -6.492361379858953008 ) ) ;
#61302=CARTESIAN_POINT ( 'NONE',  ( -8.102448949553179958, 114.6049999999999756, 5.886773742842747126 ) ) ;
#61304=PRESENTATION_STYLE_ASSIGNMENT (( #2140 ) ) ;
#61305=CARTESIAN_POINT ( 'NONE',  ( 3.094860106618435136, 128.4049999999999443, -9.525000000000000355 ) ) ;
#61307=( GEOMETRIC_REPRESENTATION_CONTEXT ( 3 ) GLOBAL_UNCERTAINTY_ASSIGNED_CONTEXT ( ( #26315 ) ) GLOBAL_UNIT_ASSIGNED_CONTEXT ( ( #3529, #35948, #68300 ) ) REPRESENTATION_CONTEXT ( 'NONE', 'WORKASPACE' ) );
#61312=CYLINDRICAL_SURFACE ( 'NONE', #23884, 13.99999999999999822 ) ;
#61313=SURFACE_SIDE_STYLE ('',( #34247 ) ) ;
#61319=DIRECTION ( 'NONE',  ( 0.000000000000000000, -1.000000000000000000, 0.000000000000000000 ) ) ;
#61320=ORIENTED_EDGE ( 'NONE', *, *, #48887, .F. ) ;
#61325=CARTESIAN_POINT ( 'NONE',  ( -75.00000000000000000, 8.189706559487058612, 5.659622407586515358 ) ) ;
#61328=SURFACE_STYLE_USAGE ( .BOTH. , #17752 ) ;
#61329=CARTESIAN_POINT ( 'NONE',  ( -60.00000000000000000, -2.024042244987997205E-14, -10.49999999999999822 ) ) ;
#61333=CARTESIAN_POINT ( 'NONE',  ( -8.102448949553179958, 139.8949999999999818, -5.886773742842749790 ) ) ;
#61338=CARTESIAN_POINT ( 'NONE',  ( 0.000000000000000000, 121.0570736234661524, -8.025000000000000355 ) ) ;
#61342=CARTESIAN_POINT ( 'NONE',  ( -3.094860106618434248, 110.7949999999999733, 9.525000000000000355 ) ) ;
#61346=EDGE_LOOP ( 'NONE', ( #10183, #13072, #69566, #46562 ) ) ;
#61348=DIRECTION ( 'NONE',  ( 1.000000000000000000, 0.000000000000000000, 0.000000000000000000 ) ) ;
#61349=STYLED_ITEM ( 'NONE', ( #33576 ), #8759 ) ;
#61350=DIRECTION ( 'NONE',  ( 1.000000000000000000, -0.000000000000000000, -0.000000000000000000 ) ) ;
#61353=SHAPE_REPRESENTATION_RELATIONSHIP ( 'NONE' , 'NONE' ,  #6947, #14448 ) ;
#61355=STYLED_ITEM ( 'NONE', ( #37598 ), #64822 ) ;
#61357=( NAMED_UNIT ( * ) SI_UNIT ( $, .STERADIAN. ) SOLID_ANGLE_UNIT ( ) );
#61364=DIRECTION ( 'NONE',  ( 1.000000000000000000, 0.000000000000000000, -0.000000000000000000 ) ) ;
#61365=CARTESIAN_POINT ( 'NONE',  ( -71.50000000000000000, 35.92875272052971525, 7.500000000000000000 ) ) ;
#61366=( NAMED_UNIT ( * ) PLANE_ANGLE_UNIT ( ) SI_UNIT ( $, .RADIAN. ) );
#61367=CARTESIAN_POINT ( 'NONE',  ( -41.21596654039937846, 107.8367875949926713, 3.443506282739225988 ) ) ;
#61368=ADVANCED_FACE ( 'NONE', ( #37127 ), #68880, .T. ) ;
#61371=DIRECTION ( 'NONE',  ( 0.000000000000000000, 0.000000000000000000, -1.000000000000000000 ) ) ;
#61372=CARTESIAN_POINT ( 'NONE',  ( 9.827790563157511022E-16, 87.30187232391182306, -8.025000000000000355 ) ) ;
#61373=ORIENTED_EDGE ( 'NONE', *, *, #13034, .T. ) ;
#61374=CARTESIAN_POINT ( 'NONE',  ( -4.716976649647098618, 134.2570736234661695, 6.492361379858953008 ) ) ;
#61375=CARTESIAN_POINT ( 'NONE',  ( 7.632228543268607446, 126.1570736234661467, 2.479861379858954606 ) ) ;
#61385=EDGE_CURVE ( 'NONE', #55490, #15666, #16007, .T. ) ;
#61387=VERTEX_POINT ( 'NONE', #53275 ) ;
#61393=SURFACE_STYLE_USAGE ( .BOTH. , #45275 ) ;
#61394=( NAMED_UNIT ( * ) SI_UNIT ( $, .STERADIAN. ) SOLID_ANGLE_UNIT ( ) );
#61395=ORIENTED_EDGE ( 'NONE', *, *, #32183, .T. ) ;
#61396=( LENGTH_UNIT ( ) NAMED_UNIT ( * ) SI_UNIT ( .MILLI., .METRE. ) );
#61399=( GEOMETRIC_REPRESENTATION_CONTEXT ( 3 ) GLOBAL_UNCERTAINTY_ASSIGNED_CONTEXT ( ( #47593 ) ) GLOBAL_UNIT_ASSIGNED_CONTEXT ( ( #41028, #51541, #57157 ) ) REPRESENTATION_CONTEXT ( 'NONE', 'WORKASPACE' ) );
#61400=( LENGTH_UNIT ( ) NAMED_UNIT ( * ) SI_UNIT ( .MILLI., .METRE. ) );
#61403=CARTESIAN_POINT ( 'NONE',  ( 8.102448949553181734, 114.9949999999999903, -5.886773742842746238 ) ) ;
#61406=DIRECTION ( 'NONE',  ( 1.224646799147353207E-16, 1.000000000000000000, -0.000000000000000000 ) ) ;
#61408=DIRECTION ( 'NONE',  ( -1.000000000000000000, 0.000000000000000000, 0.000000000000000000 ) ) ;
#61409=CARTESIAN_POINT ( 'NONE',  ( 45.02564408152620246, 10.00854802717538306, -3.127379285715777613 ) ) ;
#61425=CARTESIAN_POINT ( 'NONE',  ( 5.598654528085805993, 148.3549999999999898, 7.705886871421374629 ) ) ;
#61426=CARTESIAN_POINT ( 'NONE',  ( -60.00000000000000000, -2.024042244987997205E-14, -12.00000000000000000 ) ) ;
#61429=FACE_OUTER_BOUND ( 'NONE', #40794, .T. ) ;
#61430=CARTESIAN_POINT ( 'NONE',  ( -20.17690446313311625, 115.4776478016129460, -10.00000000000000000 ) ) ;
#61431=EDGE_CURVE ( 'NONE', #62586, #58654, #10367, .T. ) ;
#61432=MECHANICAL_DESIGN_GEOMETRIC_PRESENTATION_REPRESENTATION('',(#26591),#42434);
#61436=AXIS2_PLACEMENT_3D ( 'NONE', #28868, #55960, #8492 ) ;
#61437=PRESENTATION_STYLE_ASSIGNMENT (( #50916 ) ) ;
#61438=SURFACE_SIDE_STYLE ('',( #12563 ) ) ;
#61439=ORIENTED_EDGE ( 'NONE', *, *, #46435, .F. ) ;
#61447=ADVANCED_FACE ( 'NONE', ( #67181 ), #60852, .F. ) ;
#61452=ORIENTED_EDGE ( 'NONE', *, *, #26752, .F. ) ;
#61453=CARTESIAN_POINT ( 'NONE',  ( -9.058813317711337021, 111.1549999999999869, -2.943386871421374895 ) ) ;
#61455=ORIENTED_EDGE ( 'NONE', *, *, #63847, .F. ) ;
#61456=DIRECTION ( 'NONE',  ( 0.000000000000000000, 0.000000000000000000, -1.000000000000000000 ) ) ;
#61457=CARTESIAN_POINT ( 'NONE',  ( -45.50000000000000000, 7.768687147774684831, 6.500000000000000000 ) ) ;
#61459=ORIENTED_EDGE ( 'NONE', *, *, #68232, .F. ) ;
#61461=CARTESIAN_POINT ( 'NONE',  ( 0.000000000000000000, 110.4999999999999858, -9.525000000000000355 ) ) ;
#61465=ORIENTED_EDGE ( 'NONE', *, *, #8602, .F. ) ;
#61466=CARTESIAN_POINT ( 'NONE',  ( -4.716976649647098618, 145.1429263765338078, 6.492361379858953008 ) ) ;
#61470=SURFACE_SIDE_STYLE ('',( #35809 ) ) ;
#61472=( LENGTH_UNIT ( ) NAMED_UNIT ( * ) SI_UNIT ( .MILLI., .METRE. ) );
#61473=CYLINDRICAL_SURFACE ( 'NONE', #47931, 0.5000000000000004441 ) ;
#61475=DIRECTION ( 'NONE',  ( 1.156482317317866302E-16, 1.000000000000000000, 0.000000000000000000 ) ) ;
#61478=ORIENTED_EDGE ( 'NONE', *, *, #33998, .T. ) ;
#61483=CIRCLE ( 'NONE', #13190, 0.5000000000000004441 ) ;
#61485=SURFACE_SIDE_STYLE ('',( #39745 ) ) ;
#61486=MECHANICAL_DESIGN_GEOMETRIC_PRESENTATION_REPRESENTATION('',(#21092),#7580);
#61487=CARTESIAN_POINT ( 'NONE',  ( -20.86757785789463071, 115.0275815560950718, 10.00000000000000000 ) ) ;
#61489=DIRECTION ( 'NONE',  ( 1.000000000000000000, 2.127927463864883264E-14, 0.000000000000000000 ) ) ;
#61495=CARTESIAN_POINT ( 'NONE',  ( 44.99999999999977973, 149.9999999999999716, 9.500000000000000000 ) ) ;
#61498=CARTESIAN_POINT ( 'NONE',  ( 0.000000000000000000, 112.0570736234661666, -8.025000000000000355 ) ) ;
#61501=( GEOMETRIC_REPRESENTATION_CONTEXT ( 3 ) GLOBAL_UNCERTAINTY_ASSIGNED_CONTEXT ( ( #31156 ) ) GLOBAL_UNIT_ASSIGNED_CONTEXT ( ( #61759, #15021, #4401 ) ) REPRESENTATION_CONTEXT ( 'NONE', 'WORKASPACE' ) );
#61502=SURFACE_STYLE_FILL_AREA ( #40114 ) ;
#61505=CARTESIAN_POINT ( 'NONE',  ( -9.058813317711337021, 117.1549999999999869, -2.943386871421374895 ) ) ;
#61510=UNCERTAINTY_MEASURE_WITH_UNIT (LENGTH_MEASURE( 1.000000000000000082E-05 ), #760, 'distance_accuracy_value', 'NONE');
#61513=VERTEX_POINT ( 'NONE', #49065 ) ;
#61520=CARTESIAN_POINT ( 'NONE',  ( 71.62068965517238439, 63.58603185604027885, -7.500000000000000000 ) ) ;
#61523=ORIENTED_EDGE ( 'NONE', *, *, #2107, .T. ) ;
#61525=DIRECTION ( 'NONE',  ( -0.000000000000000000, -0.000000000000000000, 1.000000000000000000 ) ) ;
#61528=LINE ( 'NONE', #24263, #48387 ) ;
#61535=VERTEX_POINT ( 'NONE', #15143 ) ;
#61538=DIRECTION ( 'NONE',  ( 0.000000000000000000, 0.000000000000000000, -1.000000000000000000 ) ) ;
#61539=VERTEX_POINT ( 'NONE', #3459 ) ;
#61540=CIRCLE ( 'NONE', #34595, 0.5000000000000004441 ) ;
#61543=CARTESIAN_POINT ( 'NONE',  ( -8.102448949553181734, 143.4949999999999477, 5.886773742842747126 ) ) ;
#61544=CARTESIAN_POINT ( 'NONE',  ( 7.647808743684392674, 154.4999999999999432, 5.677732506910178500 ) ) ;
#61547=CARTESIAN_POINT ( 'NONE',  ( -3.094860106618432471, 143.7050000000000125, -9.525000000000000355 ) ) ;
#61551=CARTESIAN_POINT ( 'NONE',  ( -2.607480562269075097, 118.2929263765338135, 8.025000000000000355 ) ) ;
#61552=SURFACE_STYLE_USAGE ( .BOTH. , #3479 ) ;
#61553=UNCERTAINTY_MEASURE_WITH_UNIT (LENGTH_MEASURE( 1.000000000000000082E-05 ), #11541, 'distance_accuracy_value', 'NONE');
#61555=( NAMED_UNIT ( * ) PLANE_ANGLE_UNIT ( ) SI_UNIT ( $, .RADIAN. ) );
#61559=ORIENTED_EDGE ( 'NONE', *, *, #12870, .F. ) ;
#61561=DIRECTION ( 'NONE',  ( 0.000000000000000000, 0.000000000000000000, 1.000000000000000000 ) ) ;
#61567=FACE_OUTER_BOUND ( 'NONE', #34734, .T. ) ;
#61568=DIRECTION ( 'NONE',  ( -0.000000000000000000, -0.000000000000000000, 1.000000000000000000 ) ) ;
#61570=( NAMED_UNIT ( * ) PLANE_ANGLE_UNIT ( ) SI_UNIT ( $, .RADIAN. ) );
#61572=ORIENTED_EDGE ( 'NONE', *, *, #32371, .T. ) ;
#61574=DIRECTION ( 'NONE',  ( 1.000000000000000000, 0.000000000000000000, 0.000000000000000000 ) ) ;
#61576=ORIENTED_EDGE ( 'NONE', *, *, #67032, .F. ) ;
#61579=( BOUNDED_SURFACE ( )  B_SPLINE_SURFACE ( 3, 2, ( 
 ( #33491, #34525, #55981 ),
 ( #23973, #65502, #7790 ),
 ( #29239, #33828, #45488 ),
 ( #66906, #54920, #40182 ),
 ( #28178, #49690, #33162 ),
 ( #17688, #39155, #54597 ),
 ( #55289, #50042, #1777 ),
 ( #6403, #27832, #49337 ),
 ( #46528, #46885, #19739 ),
 ( #14131, #19022, #41233 ),
 ( #2826, #20072, #40534 ),
 ( #61946, #51071, #24646 ),
 ( #51412, #35588, #29600 ),
 ( #30981, #62633, #13411 ),
 ( #3156, #4220, #14456 ),
 ( #68285, #3513, #57028 ),
 ( #47215, #41572, #24319 ),
 ( #46164, #25694, #8846 ),
 ( #68634, #45812, #62994 ),
 ( #13773, #67234, #67955 ) ),
 .UNSPECIFIED., .F., .F., .F. ) 
 B_SPLINE_SURFACE_WITH_KNOTS ( ( 4, 2, 2, 2, 2, 2, 2, 2, 2, 4 ),
 ( 3, 3 ),
 ( 0.001620365016234695142, 0.002207270000664797102, 0.002500722492879848408, 0.002794174985094899279, 0.003087627477309950151, 0.003381079969525001457, 0.003527806215632527109, 0.003674532461740052328, 0.003821258707847577547, 0.003967984953955103200 ),
 ( 0.000000000000000000, 1.000000000000000000 ),
 .UNSPECIFIED. ) 
 GEOMETRIC_REPRESENTATION_ITEM ( )  RATIONAL_B_SPLINE_SURFACE ( (
 ( 1.000000000000000000, 0.7071067811865475727, 1.000000000000000000),
 ( 1.000000000000000000, 0.6778671762783700094, 1.000000000000000000),
 ( 1.000000000000000000, 0.6467717707951793349, 1.000000000000000000),
 ( 1.000000000000000000, 0.5961086003387628951, 1.000000000000000000),
 ( 1.000000000000000000, 0.5785481842580926237, 1.000000000000000000),
 ( 1.000000000000000000, 0.5417514570915383798, 1.000000000000000000),
 ( 1.000000000000000000, 0.5224568997730709707, 1.000000000000000000),
 ( 1.000000000000000000, 0.4825437615626911314, 1.000000000000000000),
 ( 1.000000000000000000, 0.4617081702731655191, 1.000000000000000000),
 ( 1.000000000000000000, 0.4191790061639760756, 1.000000000000000000),
 ( 1.000000000000000000, 0.3974966599962702629, 1.000000000000000000),
 ( 1.000000000000000000, 0.3653498311554840283, 1.000000000000000000),
 ( 1.000000000000000000, 0.3548631489840615716, 1.000000000000000000),
 ( 1.000000000000000000, 0.3350876751766880268, 1.000000000000000000),
 ( 1.000000000000000000, 0.3256829922529814181, 1.000000000000000000),
 ( 1.000000000000000000, 0.3094849113515590333, 1.000000000000000000),
 ( 1.000000000000000000, 0.3027429446061458695, 1.000000000000000000),
 ( 1.000000000000000000, 0.2932846354085155149, 1.000000000000000000),
 ( 1.000000000000000000, 0.2906862528187321160, 1.000000000000000000),
 ( 1.000000000000000000, 0.2907356542125049681, 1.000000000000000000) ) ) 
 REPRESENTATION_ITEM ( '' )  SURFACE ( )  );
#61580=CARTESIAN_POINT ( 'NONE',  ( 9.827790563157511022E-16, 87.30187232391182306, -8.025000000000000355 ) ) ;
#61582=DIRECTION ( 'NONE',  ( 0.000000000000000000, 0.000000000000000000, -1.000000000000000000 ) ) ;
#61587=CARTESIAN_POINT ( 'NONE',  ( -3.094860106618434248, 143.7949999999999875, 9.525000000000000355 ) ) ;
#61589=EDGE_CURVE ( 'NONE', #60674, #62454, #58036, .T. ) ;
#61593=UNCERTAINTY_MEASURE_WITH_UNIT (LENGTH_MEASURE( 1.000000000000000082E-05 ), #26895, 'distance_accuracy_value', 'NONE');
#61594=MECHANICAL_DESIGN_GEOMETRIC_PRESENTATION_REPRESENTATION('',(#58257),#44796);
#61595=CARTESIAN_POINT ( 'NONE',  ( -75.00000000000000000, 7.893193270153694208, -6.999999999999999112 ) ) ;
#61601=( NAMED_UNIT ( * ) PLANE_ANGLE_UNIT ( ) SI_UNIT ( $, .RADIAN. ) );
#61604=CARTESIAN_POINT ( 'NONE',  ( -20.71231517720798010, 114.9999999999999574, 10.50000000000000000 ) ) ;
#61606=EDGE_CURVE ( 'NONE', #20924, #23204, #37540, .T. ) ;
#61612=LINE ( 'NONE', #56006, #46012 ) ;
#61613=CARTESIAN_POINT ( 'NONE',  ( 0.000000000000000000, 152.9999999999999716, 0.000000000000000000 ) ) ;
#61614=AXIS2_PLACEMENT_3D ( 'NONE', #31209, #66898, #8152 ) ;
#61615=EDGE_CURVE ( 'NONE', #21177, #24543, #43160, .T. ) ;
#61618=ORIENTED_EDGE ( 'NONE', *, *, #40603, .F. ) ;
#61619=CARTESIAN_POINT ( 'NONE',  ( -44.99999999999998579, 119.9999999999999716, 9.500000000000000000 ) ) ;
#61620=SURFACE_SIDE_STYLE ('',( #18734 ) ) ;
#61621=VERTEX_POINT ( 'NONE', #14400 ) ;
#61625=DIRECTION ( 'NONE',  ( 1.000000000000000000, 0.000000000000000000, 0.000000000000000000 ) ) ;
#61626=CARTESIAN_POINT ( 'NONE',  ( 9.058813317711338797, 114.8449999999999847, -2.943386871421372675 ) ) ;
#61627=STYLED_ITEM ( 'NONE', ( #23024 ), #4680 ) ;
#61630=DIRECTION ( 'NONE',  ( 0.000000000000000000, 0.000000000000000000, 1.000000000000000000 ) ) ;
#61633=CARTESIAN_POINT ( 'NONE',  ( -10.01517768586949231, 141.3050000000000068, -6.132527647946036459E-16 ) ) ;
#61634=UNCERTAINTY_MEASURE_WITH_UNIT (LENGTH_MEASURE( 1.000000000000000082E-05 ), #31344, 'distance_accuracy_value', 'NONE');
#61635=PRESENTATION_STYLE_ASSIGNMENT (( #67287 ) ) ;
#61636=VECTOR ( 'NONE', #42822, 1000.000000000000000 ) ;
#61638=EDGE_LOOP ( 'NONE', ( #14240, #49915, #54659, #47835 ) ) ;
#61648=ORIENTED_EDGE ( 'NONE', *, *, #45557, .F. ) ;
#61652=ORIENTED_EDGE ( 'NONE', *, *, #33297, .T. ) ;
#61653=CARTESIAN_POINT ( 'NONE',  ( -2.607480562269020918, 118.2070736234661439, -8.025000000000037659 ) ) ;
#61655=LINE ( 'NONE', #8583, #3569 ) ;
#61656=CARTESIAN_POINT ( 'NONE',  ( 0.000000000000000000, 145.4449999999999932, -9.525000000000000355 ) ) ;
#61659=CARTESIAN_POINT ( 'NONE',  ( -23.71231517720798010, 112.9999999999999858, 7.000000000000000000 ) ) ;
#61660=CARTESIAN_POINT ( 'NONE',  ( -45.50000000000000000, 7.768687147774684831, -6.500000000000000000 ) ) ;
#61662=STYLED_ITEM ( 'NONE', ( #465 ), #42623 ) ;
#61665=CARTESIAN_POINT ( 'NONE',  ( -8.102448949553181734, 109.8949999999999818, -5.886773742842749790 ) ) ;
#61668=AXIS2_PLACEMENT_3D ( 'NONE', #29338, #28642, #19121 ) ;
#61669=VECTOR ( 'NONE', #8994, 1000.000000000000000 ) ;
#61672=CIRCLE ( 'NONE', #40375, 0.5000000000000004441 ) ;
#61682=AXIS2_PLACEMENT_3D ( 'NONE', #10936, #64754, #59445 ) ;
#61683=EDGE_CURVE ( 'NONE', #54714, #30521, #28459, .T. ) ;
#61684=EDGE_CURVE ( 'NONE', #40912, #42981, #62212, .T. ) ;
#61685=( NAMED_UNIT ( * ) PLANE_ANGLE_UNIT ( ) SI_UNIT ( $, .RADIAN. ) );
#61686=DIRECTION ( 'NONE',  ( 0.000000000000000000, 0.000000000000000000, 1.000000000000000000 ) ) ;
#61688=SURFACE_STYLE_FILL_AREA ( #19489 ) ;
#61693=DIRECTION ( 'NONE',  ( 0.000000000000000000, 0.000000000000000000, 1.000000000000000000 ) ) ;
#61698=VERTEX_POINT ( 'NONE', #5915 ) ;
#61701=CARTESIAN_POINT ( 'NONE',  ( -61.49999999999998579, 50.00000000000000000, 9.500000000000000000 ) ) ;
#61704=AXIS2_PLACEMENT_3D ( 'NONE', #35388, #57163, #45277 ) ;
#61705=CARTESIAN_POINT ( 'NONE',  ( -2.607480562269075097, 137.4070736234661183, 8.025000000000000355 ) ) ;
#61715=DIRECTION ( 'NONE',  ( -0.000000000000000000, 1.000000000000000000, -0.000000000000000000 ) ) ;
#61716=AXIS2_PLACEMENT_3D ( 'NONE', #50653, #67882, #35162 ) ;
#61723=DIRECTION ( 'NONE',  ( -0.7071067811865543451, 8.659560562355015442E-17, 0.7071067811865408004 ) ) ;
#61726=STYLED_ITEM ( 'NONE', ( #37438 ), #41858 ) ;
#61727=EDGE_LOOP ( 'NONE', ( #22867, #15598, #20231, #16802 ) ) ;
#61728=CARTESIAN_POINT ( 'NONE',  ( -48.00000000000000000, 13.41640786499872284, 7.000000000000000000 ) ) ;
#61737=CIRCLE ( 'NONE', #47211, 0.5000000000000004441 ) ;
#61740=MECHANICAL_DESIGN_GEOMETRIC_PRESENTATION_REPRESENTATION('',(#42744),#66282);
#61741=CARTESIAN_POINT ( 'NONE',  ( 5.598654528085805993, 111.2449999999999761, 7.705886871421374629 ) ) ;
#61743=CYLINDRICAL_SURFACE ( 'NONE', #68925, 0.5000000000000004441 ) ;
#61745=ORIENTED_EDGE ( 'NONE', *, *, #2484, .F. ) ;
#61759=( LENGTH_UNIT ( ) NAMED_UNIT ( * ) SI_UNIT ( .MILLI., .METRE. ) );
#61760=VECTOR ( 'NONE', #34886, 1000.000000000000000 ) ;
#61766=CARTESIAN_POINT ( 'NONE',  ( -8.102448949553181734, 150.0049999999999386, -5.886773742842749790 ) ) ;
#61767=DIRECTION ( 'NONE',  ( 0.000000000000000000, 0.000000000000000000, -1.000000000000000000 ) ) ;
#61773=CARTESIAN_POINT ( 'NONE',  ( -74.99999999999998579, 50.00000000000000000, -12.00000000000000000 ) ) ;
#61774=CARTESIAN_POINT ( 'NONE',  ( -20.71462257909523075, 114.5925267038606563, -10.00000000000000000 ) ) ;
#61777=CARTESIAN_POINT ( 'NONE',  ( -4.564701690882220220, 110.6597480665491133, 8.185492600733832447 ) ) ;
#61780=( LENGTH_UNIT ( ) NAMED_UNIT ( * ) SI_UNIT ( .MILLI., .METRE. ) );
#61781=FACE_OUTER_BOUND ( 'NONE', #9268, .T. ) ;
#61782=EDGE_LOOP ( 'NONE', ( #26290, #51532, #17952, #28321 ) ) ;
#61783=ORIENTED_EDGE ( 'NONE', *, *, #35355, .T. ) ;
#61784=FILL_AREA_STYLE ('',( #34388 ) ) ;
#61787=CARTESIAN_POINT ( 'NONE',  ( -45.00000000000000000, 9.708372675170618749, 6.000000000000000888 ) ) ;
#61789=( NAMED_UNIT ( * ) SI_UNIT ( $, .STERADIAN. ) SOLID_ANGLE_UNIT ( ) );
#61790=ORIENTED_EDGE ( 'NONE', *, *, #34328, .F. ) ;
#61791=ORIENTED_EDGE ( 'NONE', *, *, #37221, .T. ) ;
#61792=FILL_AREA_STYLE ('',( #40385 ) ) ;
#61795=CARTESIAN_POINT ( 'NONE',  ( -9.058813317711338797, 111.4549999999999841, 2.943386871421373563 ) ) ;
#61796=CARTESIAN_POINT ( 'NONE',  ( -45.00000000000000000, -1.469576158976824302E-14, 4.000000000000000000 ) ) ;
#61800=CARTESIAN_POINT ( 'NONE',  ( 15.98999599679679839, 118.4999999999999716, -7.500000000000000000 ) ) ;
#61802=VERTEX_POINT ( 'NONE', #66755 ) ;
#61808=DIRECTION ( 'NONE',  ( -0.000000000000000000, -0.000000000000000000, -1.000000000000000000 ) ) ;
#61810=CARTESIAN_POINT ( 'NONE',  ( 6.826472737025119919, 142.8929263765338078, 4.959722759717908325 ) ) ;
#61811=SURFACE_STYLE_FILL_AREA ( #29823 ) ;
#61813=FILL_AREA_STYLE_COLOUR ( '', #22196 ) ;
#61814=ORIENTED_EDGE ( 'NONE', *, *, #5055, .F. ) ;
#61815=AXIS2_PLACEMENT_3D ( 'NONE', #24420, #31088, #13525 ) ;
#61820=CARTESIAN_POINT ( 'NONE',  ( 20.12916642283592950, 110.4999999999999858, 10.05319148936170137 ) ) ;
#61823=SPHERICAL_SURFACE ( 'NONE', #43245, 0.5000000000000000000 ) ;
#61826=VERTEX_POINT ( 'NONE', #39017 ) ;
#61827=DIRECTION ( 'NONE',  ( -0.000000000000000000, 1.000000000000000000, -0.000000000000000000 ) ) ;
#61831=MECHANICAL_DESIGN_GEOMETRIC_PRESENTATION_REPRESENTATION('',(#11286),#13538);
#61837=FACE_OUTER_BOUND ( 'NONE', #2759, .T. ) ;
#61842=VERTEX_POINT ( 'NONE', #1643 ) ;
#61844=ADVANCED_FACE ( 'NONE', ( #49899 ), #7325, .T. ) ;
#61845=FILL_AREA_STYLE ('',( #66813 ) ) ;
#61849=ADVANCED_FACE ( 'NONE', ( #39698 ), #42161, .T. ) ;
#61850=DIRECTION ( 'NONE',  ( 0.000000000000000000, 0.000000000000000000, 1.000000000000000000 ) ) ;
#61851=( GEOMETRIC_REPRESENTATION_CONTEXT ( 3 ) GLOBAL_UNCERTAINTY_ASSIGNED_CONTEXT ( ( #36246 ) ) GLOBAL_UNIT_ASSIGNED_CONTEXT ( ( #15037, #9400, #10772 ) ) REPRESENTATION_CONTEXT ( 'NONE', 'WORKASPACE' ) );
#61852=ORIENTED_EDGE ( 'NONE', *, *, #31270, .F. ) ;
#61856=PRESENTATION_STYLE_ASSIGNMENT (( #3070 ) ) ;
#61859=CARTESIAN_POINT ( 'NONE',  ( 0.000000000000000000, 154.5000000000000000, -9.524999999999998579 ) ) ;
#61860=AXIS2_PLACEMENT_3D ( 'NONE', #63862, #32535, #48090 ) ;
#61865=CARTESIAN_POINT ( 'NONE',  ( 3.094860106618435136, 119.4049999999999727, -9.525000000000000355 ) ) ;
#61867=CARTESIAN_POINT ( 'NONE',  ( -74.08452722063037754, 9.430195807687219656, -6.500000000000000000 ) ) ;
#61870=CIRCLE ( 'NONE', #4582, 0.5000000000000004441 ) ;
#61871=CARTESIAN_POINT ( 'NONE',  ( -84.49999999999997158, 50.00000000000000000, 10.00000000000000000 ) ) ;
#61874=VERTEX_POINT ( 'NONE', #62502 ) ;
#61876=CIRCLE ( 'NONE', #20303, 14.49999999999999822 ) ;
#61878=( BOUNDED_CURVE ( )  B_SPLINE_CURVE ( 2, ( #48821, #11821, #22042, #59658, #54381, #65291, #33293, #54718, #17139, #1207, #28319 ),
 .UNSPECIFIED., .F., .F. ) 
 B_SPLINE_CURVE_WITH_KNOTS ( ( 3, 2, 2, 2, 2, 3 ),
 ( 0.4411764705882353921, 0.4470588235294118973, 0.4529411764705883470, 0.4588235294117647967, 0.4647058823529413019, 0.4705882352941177516 ),
 .UNSPECIFIED. ) 
 CURVE ( )  GEOMETRIC_REPRESENTATION_ITEM ( )  RATIONAL_B_SPLINE_CURVE ( ( 0.9999999999999991118, 0.9510565162951544194, 1.000000000000000000, 0.9510565162951535312, 1.000000000000000000, 0.9510565162951535312, 1.000000000000000000, 0.9510565162951535312, 1.000000000000000000, 0.9510565162951526430, 1.000000000000000888 ) ) 
 REPRESENTATION_ITEM ( '' )  );
#61880=( NAMED_UNIT ( * ) PLANE_ANGLE_UNIT ( ) SI_UNIT ( $, .RADIAN. ) );
#61881=CIRCLE ( 'NONE', #31550, 0.5000000000000004441 ) ;
#61884=( NAMED_UNIT ( * ) PLANE_ANGLE_UNIT ( ) SI_UNIT ( $, .RADIAN. ) );
#61887=ORIENTED_EDGE ( 'NONE', *, *, #61385, .F. ) ;
#61889=DIRECTION ( 'NONE',  ( 0.000000000000000000, -0.000000000000000000, -1.000000000000000000 ) ) ;
#61890=CONICAL_SURFACE ( 'NONE', #45079, 5.000000000000004441, 0.7853981633974587151 ) ;
#61892=FILL_AREA_STYLE ('',( #40474 ) ) ;
#61894=CARTESIAN_POINT ( 'NONE',  ( -74.99999999999998579, 50.00000000000000000, 10.00000000000000000 ) ) ;
#61895=SURFACE_STYLE_FILL_AREA ( #18969 ) ;
#61896=ORIENTED_EDGE ( 'NONE', *, *, #11825, .F. ) ;
#61898=VERTEX_POINT ( 'NONE', #27625 ) ;
#61903=SURFACE_STYLE_USAGE ( .BOTH. , #62593 ) ;
#61904=ORIENTED_EDGE ( 'NONE', *, *, #38417, .T. ) ;
#61908=CARTESIAN_POINT ( 'NONE',  ( 5.598654528085805993, 144.2449999999999761, 7.705886871421374629 ) ) ;
#61911=ORIENTED_EDGE ( 'NONE', *, *, #15685, .F. ) ;
#61913=CARTESIAN_POINT ( 'NONE',  ( -8.102448949553179958, 138.0049999999999670, -5.886773742842749790 ) ) ;
#61916=CARTESIAN_POINT ( 'NONE',  ( 4.716976649647096842, 115.7429263765338163, 6.492361379858953896 ) ) ;
#61917=PRESENTATION_STYLE_ASSIGNMENT (( #13737 ) ) ;
#61922=FACE_OUTER_BOUND ( 'NONE', #53378, .T. ) ;
#61927=ADVANCED_FACE ( 'NONE', ( #26918 ), #15122, .F. ) ;
#61928=( GEOMETRIC_REPRESENTATION_CONTEXT ( 3 ) GLOBAL_UNCERTAINTY_ASSIGNED_CONTEXT ( ( #8823 ) ) GLOBAL_UNIT_ASSIGNED_CONTEXT ( ( #25529, #36834, #36121 ) ) REPRESENTATION_CONTEXT ( 'NONE', 'WORKASPACE' ) );
#61930=SURFACE_STYLE_USAGE ( .BOTH. , #55635 ) ;
#61936=DIRECTION ( 'NONE',  ( -1.000000000000000000, 0.000000000000000000, 0.000000000000000000 ) ) ;
#61940=( LENGTH_UNIT ( ) NAMED_UNIT ( * ) SI_UNIT ( .MILLI., .METRE. ) );
#61942=VECTOR ( 'NONE', #51269, 1000.000000000000000 ) ;
#61944=CARTESIAN_POINT ( 'NONE',  ( 15.48999599679679662, 117.9999999999999716, 7.000000000000000000 ) ) ;
#61945=CARTESIAN_POINT ( 'NONE',  ( -67.49999999999998579, -1.929132118054077781E-14, -12.00000000000000000 ) ) ;
#61946=CARTESIAN_POINT ( 'NONE',  ( -74.13336567797000498, 9.244254510420731208, -6.241797924670647646 ) ) ;
#61949=AXIS2_PLACEMENT_3D ( 'NONE', #24753, #62739, #19841 ) ;
#61951=CARTESIAN_POINT ( 'NONE',  ( -71.62068965517238439, 63.58603185604027885, -9.500000000000000000 ) ) ;
#61952=ADVANCED_FACE ( 'NONE', ( #69190 ), #37575, .T. ) ;
#61953=CARTESIAN_POINT ( 'NONE',  ( -8.102448949553181734, 134.4949999999999477, 5.886773742842747126 ) ) ;
#61958=SURFACE_STYLE_FILL_AREA ( #40546 ) ;
#61959=DIRECTION ( 'NONE',  ( 0.000000000000000000, 0.000000000000000000, 1.000000000000000000 ) ) ;
#61961=FILL_AREA_STYLE_COLOUR ( '', #52354 ) ;
#61965=FACE_OUTER_BOUND ( 'NONE', #18644, .T. ) ;
#61966=FILL_AREA_STYLE_COLOUR ( '', #14806 ) ;
#61968=CARTESIAN_POINT ( 'NONE',  ( -7.632228543268608334, 127.9570736234661439, 2.479861379858952830 ) ) ;
#61969=ORIENTED_EDGE ( 'NONE', *, *, #24969, .T. ) ;
#61971=ADVANCED_FACE ( 'NONE', ( #32230 ), #53681, .F. ) ;
#61973=COLOUR_RGB ( '', 0.66274510, 0.83137255, 0.94901961) ;
#61975=DIRECTION ( 'NONE',  ( -1.000000000000000000, 0.000000000000000000, 0.000000000000000000 ) ) ;
#61976=CARTESIAN_POINT ( 'NONE',  ( 4.716976649647096842, 118.7429263765338163, 6.492361379858953896 ) ) ;
#61978=VECTOR ( 'NONE', #67445, 1000.000000000000000 ) ;
#61980=AXIS2_PLACEMENT_3D ( 'NONE', #64813, #21194, #26130 ) ;
#61981=ORIENTED_EDGE ( 'NONE', *, *, #29852, .F. ) ;
#61986=AXIS2_PLACEMENT_3D ( 'NONE', #28054, #5240, #26683 ) ;
#61988=CARTESIAN_POINT ( 'NONE',  ( -9.058813317711338797, 113.3449999999999847, 2.943386871421373563 ) ) ;
#61990=CARTESIAN_POINT ( 'NONE',  ( 9.058813317711338797, 115.9549999999999841, -2.943386871421372675 ) ) ;
#61994=CARTESIAN_POINT ( 'NONE',  ( 3.094860106618431583, 136.2049999999999557, 9.525000000000000355 ) ) ;
#61995=AXIS2_PLACEMENT_3D ( 'NONE', #21937, #27169, #44473 ) ;
#61996=SURFACE_STYLE_USAGE ( .BOTH. , #56748 ) ;
#61998=CARTESIAN_POINT ( 'NONE',  ( 20.55683252178218723, 114.6388620567782084, 10.28289609742943078 ) ) ;
#62000=COLOUR_RGB ( '', 0.40784314, 0.44705882, 0.49803922) ;
#62001=EDGE_CURVE ( 'NONE', #20924, #46101, #60341, .T. ) ;
#62002=ORIENTED_EDGE ( 'NONE', *, *, #48963, .T. ) ;
#62003=CARTESIAN_POINT ( 'NONE',  ( 0.000000000000000000, 87.30187232391182306, 0.000000000000000000 ) ) ;
#62013=DIRECTION ( 'NONE',  ( -1.000000000000000000, 0.000000000000000000, 0.000000000000000000 ) ) ;
#62020=AXIS2_PLACEMENT_3D ( 'NONE', #59727, #42560, #63962 ) ;
#62022=CARTESIAN_POINT ( 'NONE',  ( -9.058813317711337021, 140.0449999999999875, -2.943386871421374895 ) ) ;
#62026=FILL_AREA_STYLE ('',( #45887 ) ) ;
#62028=CARTESIAN_POINT ( 'NONE',  ( -9.827790563157511022E-16, 119.5570736234661524, 8.025000000000000355 ) ) ;
#62032=SURFACE_SIDE_STYLE ('',( #30029 ) ) ;
#62036=CIRCLE ( 'NONE', #55265, 5.500000000000005329 ) ;
#62037=CARTESIAN_POINT ( 'NONE',  ( -23.71231517720798010, 117.4999999999999716, -7.000000000000000000 ) ) ;
#62038=ORIENTED_EDGE ( 'NONE', *, *, #48431, .T. ) ;
#62045=CARTESIAN_POINT ( 'NONE',  ( -74.99999999999998579, 64.49137674618943095, 6.500000000000000000 ) ) ;
#62046=ORIENTED_EDGE ( 'NONE', *, *, #63772, .F. ) ;
#62049=PRODUCT_CONTEXT ( 'NONE', #38410, 'mechanical' ) ;
#62050=DIRECTION ( 'NONE',  ( 0.000000000000000000, 0.000000000000000000, -1.000000000000000000 ) ) ;
#62054=CARTESIAN_POINT ( 'NONE',  ( 0.000000000000000000, 124.0570736234661524, -8.025000000000000355 ) ) ;
#62055=STYLED_ITEM ( 'NONE', ( #20412 ), #24919 ) ;
#62061=DIRECTION ( 'NONE',  ( -0.000000000000000000, -0.000000000000000000, -1.000000000000000000 ) ) ;
#62066=LINE ( 'NONE', #58194, #46640 ) ;
#62067=CARTESIAN_POINT ( 'NONE',  ( -2.607480562269075097, 131.4070736234661467, 8.025000000000000355 ) ) ;
#62071=VECTOR ( 'NONE', #3948, 1000.000000000000000 ) ;
#62074=CARTESIAN_POINT ( 'NONE',  ( 34.99999999999992895, 112.4999999999999858, -10.00000000000000000 ) ) ;
#62081=EDGE_CURVE ( 'NONE', #20853, #3957, #21873, .T. ) ;
#62082=MECHANICAL_DESIGN_GEOMETRIC_PRESENTATION_REPRESENTATION('',(#51972),#13798);
#62085=UNCERTAINTY_MEASURE_WITH_UNIT (LENGTH_MEASURE( 1.000000000000000082E-05 ), #52179, 'distance_accuracy_value', 'NONE');
#62086=ORIENTED_EDGE ( 'NONE', *, *, #49184, .T. ) ;
#62087=( NAMED_UNIT ( * ) SI_UNIT ( $, .STERADIAN. ) SOLID_ANGLE_UNIT ( ) );
#62088=SURFACE_SIDE_STYLE ('',( #25164 ) ) ;
#62092=ORIENTED_EDGE ( 'NONE', *, *, #50584, .T. ) ;
#62093=AXIS2_PLACEMENT_3D ( 'NONE', #59605, #22682, #33238 ) ;
#62098=( LENGTH_UNIT ( ) NAMED_UNIT ( * ) SI_UNIT ( .MILLI., .METRE. ) );
#62102=CARTESIAN_POINT ( 'NONE',  ( 51.49999999999998579, 2.837994680254535968E-15, -9.999999999999998224 ) ) ;
#62103=CARTESIAN_POINT ( 'NONE',  ( 0.000000000000000000, 115.4449999999999932, -9.525000000000000355 ) ) ;
#62105=COLOUR_RGB ( '', 0.31764706, 0.68627451, 0.89019608) ;
#62108=CARTESIAN_POINT ( 'NONE',  ( -75.00000000000000000, -2.215169945516535778E-14, 6.500000000000000000 ) ) ;
#62109=ORIENTED_EDGE ( 'NONE', *, *, #57493, .F. ) ;
#62113=PRESENTATION_STYLE_ASSIGNMENT (( #4390 ) ) ;
#62114=SURFACE_STYLE_FILL_AREA ( #14284 ) ;
#62116=FACE_OUTER_BOUND ( 'NONE', #40867, .T. ) ;
#62118=AXIS2_PLACEMENT_3D ( 'NONE', #26663, #30920, #41872 ) ;
#62121=ORIENTED_EDGE ( 'NONE', *, *, #23406, .F. ) ;
#62130=CARTESIAN_POINT ( 'NONE',  ( 3.094860106618431583, 157.2050000000000125, 9.525000000000000355 ) ) ;
#62137=CARTESIAN_POINT ( 'NONE',  ( -4.886038412222122318, 110.6451352293558728, 8.015157697669311077 ) ) ;
#62138=DIRECTION ( 'NONE',  ( 0.000000000000000000, 0.000000000000000000, 1.000000000000000000 ) ) ;
#62140=CARTESIAN_POINT ( 'NONE',  ( 23.71231517720798010, 117.4999999999999716, -7.500000000000000000 ) ) ;
#62141=DIRECTION ( 'NONE',  ( 0.000000000000000000, 0.000000000000000000, 1.000000000000000000 ) ) ;
#62143=VERTEX_POINT ( 'NONE', #40304 ) ;
#62144=AXIS2_PLACEMENT_3D ( 'NONE', #32981, #32603, #53407 ) ;
#62145=DIRECTION ( 'NONE',  ( -0.6216216216216311485, 0.7833176619561784682, -5.204170427930414183E-15 ) ) ;
#62147=B_SPLINE_CURVE_WITH_KNOTS ( 'NONE', 3,
 ( #41821, #19958, #41458, #47093, #47458, #9789, #68179, #4827, #57613, #4458 ),
 .UNSPECIFIED., .F., .F.,
 ( 4, 2, 2, 2, 4 ),
 ( 0.000000000000000000, 0.0004222318702814410588, 0.0008444637405628821177, 0.001266695610844323231, 0.001688927481125764235 ),
 .UNSPECIFIED. ) ;
#62148=EDGE_LOOP ( 'NONE', ( #60643, #20021, #1133, #3923 ) ) ;
#62150=SURFACE_STYLE_FILL_AREA ( #29455 ) ;
#62154=PRESENTATION_STYLE_ASSIGNMENT (( #40744 ) ) ;
#62156=ORIENTED_EDGE ( 'NONE', *, *, #27286, .F. ) ;
#62158=COLOUR_RGB ( '', 0.09019608, 0.27058824, 0.51372549) ;
#62167=CARTESIAN_POINT ( 'NONE',  ( -9.534888206947428557, 110.4999999999999716, -0.06015242624886869144 ) ) ;
#62170=CARTESIAN_POINT ( 'NONE',  ( -9.827790563157511022E-16, 125.5570736234661524, 8.025000000000000355 ) ) ;
#62172=CARTESIAN_POINT ( 'NONE',  ( 7.632228543268608334, 149.3429263765338249, -2.479861379858951942 ) ) ;
#62173=DIRECTION ( 'NONE',  ( 0.000000000000000000, 0.000000000000000000, -1.000000000000000000 ) ) ;
#62174=SURFACE_STYLE_USAGE ( .BOTH. , #13288 ) ;
#62175=PRESENTATION_STYLE_ASSIGNMENT (( #13645 ) ) ;
#62180=ORIENTED_EDGE ( 'NONE', *, *, #58859, .F. ) ;
#62181=CARTESIAN_POINT ( 'NONE',  ( 4.716976649647099507, 128.6429263765338362, -6.492361379858953008 ) ) ;
#62183=SURFACE_STYLE_USAGE ( .BOTH. , #51643 ) ;
#62186=COLOUR_RGB ( '', 0.66274510, 0.83137255, 0.94901961) ;
#62188=CARTESIAN_POINT ( 'NONE',  ( 71.49999999999998579, 64.07124727947029896, 7.500000000000000000 ) ) ;
#62193=CARTESIAN_POINT ( 'NONE',  ( -74.99999999999998579, 50.00000000000000000, 6.499999999999999112 ) ) ;
#62194=CARTESIAN_POINT ( 'NONE',  ( -7.632228543268608334, 120.8429263765338249, 2.479861379858952830 ) ) ;
#62196=ORIENTED_EDGE ( 'NONE', *, *, #23194, .F. ) ;
#62197=CARTESIAN_POINT ( 'NONE',  ( -48.50000000000000000, 14.49137674618942562, 7.000000000000000000 ) ) ;
#62198=AXIS2_PLACEMENT_3D ( 'NONE', #52776, #46128, #29914 ) ;
#62206=SURFACE_STYLE_USAGE ( .BOTH. , #29849 ) ;
#62208=AXIS2_PLACEMENT_3D ( 'NONE', #37408, #58811, #1013 ) ;
#62210=CARTESIAN_POINT ( 'NONE',  ( 41.38221592241693259, 107.7000202725880769, 3.906946855746215697 ) ) ;
#62212=( BOUNDED_CURVE ( )  B_SPLINE_CURVE ( 2, ( #64325, #64683, #48194, #60084, #237, #16178, #58709, #27006, #48891, #38331, #22457 ),
 .UNSPECIFIED., .F., .F. ) 
 B_SPLINE_CURVE_WITH_KNOTS ( ( 3, 2, 2, 2, 2, 3 ),
 ( 0.5588235294117649410, 0.5647058823529413907, 0.5705882352941178404, 0.5764705882352942901, 0.5823529411764708508, 0.5882352941176473005 ),
 .UNSPECIFIED. ) 
 CURVE ( )  GEOMETRIC_REPRESENTATION_ITEM ( )  RATIONAL_B_SPLINE_CURVE ( ( 0.9999999999999981126, 0.9510565162951554186, 1.000000000000000000, 0.9510565162951535312, 1.000000000000000000, 0.9510565162951535312, 1.000000000000000000, 0.9510565162951535312, 1.000000000000000000, 0.9510565162951516438, 1.000000000000001776 ) ) 
 REPRESENTATION_ITEM ( '' )  );
#62217=( NAMED_UNIT ( * ) SI_UNIT ( $, .STERADIAN. ) SOLID_ANGLE_UNIT ( ) );
#62221=CARTESIAN_POINT ( 'NONE',  ( -9.058813317711338797, 120.4549999999999983, 2.943386871421373563 ) ) ;
#62224=STYLED_ITEM ( 'NONE', ( #13541 ), #61971 ) ;
#62227=UNCERTAINTY_MEASURE_WITH_UNIT (LENGTH_MEASURE( 1.000000000000000082E-05 ), #49297, 'distance_accuracy_value', 'NONE');
#62228=EDGE_CURVE ( 'NONE', #16390, #5105, #20564, .T. ) ;
#62229=DIRECTION ( 'NONE',  ( 0.000000000000000000, 0.000000000000000000, 1.000000000000000000 ) ) ;
#62231=VERTEX_POINT ( 'NONE', #41355 ) ;
#62235=AXIS2_PLACEMENT_3D ( 'NONE', #37738, #9590, #26420 ) ;
#62239=CARTESIAN_POINT ( 'NONE',  ( 23.71231517720798010, 113.4999999999999858, -9.500000000000000000 ) ) ;
#62243=DIRECTION ( 'NONE',  ( -1.000000000000000000, 0.000000000000000000, 0.000000000000000000 ) ) ;
#62246=DIRECTION ( 'NONE',  ( 0.000000000000000000, 0.000000000000000000, 1.000000000000000000 ) ) ;
#62247=( LENGTH_UNIT ( ) NAMED_UNIT ( * ) SI_UNIT ( .MILLI., .METRE. ) );
#62248=VERTEX_POINT ( 'NONE', #9333 ) ;
#62250=ORIENTED_EDGE ( 'NONE', *, *, #51381, .T. ) ;
#62251=EDGE_CURVE ( 'NONE', #42518, #31691, #14598, .T. ) ;
#62257=DIRECTION ( 'NONE',  ( 0.000000000000000000, 0.000000000000000000, 1.000000000000000000 ) ) ;
#62259=CARTESIAN_POINT ( 'NONE',  ( -74.08452722063037754, 9.430195807687216103, -6.000000000000000000 ) ) ;
#62260=CARTESIAN_POINT ( 'NONE',  ( -5.598654528085808657, 137.6449999999999818, 7.705886871421373741 ) ) ;
#62262=VECTOR ( 'NONE', #7880, 1000.000000000000000 ) ;
#62264=MECHANICAL_DESIGN_GEOMETRIC_PRESENTATION_REPRESENTATION('',(#8404),#63434);
#62266=CARTESIAN_POINT ( 'NONE',  ( 9.058813317711338797, 139.9549999999999841, -2.943386871421372675 ) ) ;
#62268=( NAMED_UNIT ( * ) PLANE_ANGLE_UNIT ( ) SI_UNIT ( $, .RADIAN. ) );
#62270=CARTESIAN_POINT ( 'NONE',  ( -2.607480562269073765, 120.0929263765337964, -8.025000000000000355 ) ) ;
#62272=PRESENTATION_STYLE_ASSIGNMENT (( #39549 ) ) ;
#62273=CARTESIAN_POINT ( 'NONE',  ( -72.00000000000000000, 36.32520566882265456, -7.000000000000000000 ) ) ;
#62275=SPHERICAL_SURFACE ( 'NONE', #11463, 0.5000000000000000000 ) ;
#62277=EDGE_LOOP ( 'NONE', ( #61618, #62851, #67478, #31371 ) ) ;
#62281=CARTESIAN_POINT ( 'NONE',  ( -45.50000000000000000, -2.024042244987997205E-14, 6.500000000000000000 ) ) ;
#62288=( NAMED_UNIT ( * ) SI_UNIT ( $, .STERADIAN. ) SOLID_ANGLE_UNIT ( ) );
#62290=SURFACE_SIDE_STYLE ('',( #40872 ) ) ;
#62293=CARTESIAN_POINT ( 'NONE',  ( 74.65811388299935913, 19.88603796099976151, 6.065461639931116089 ) ) ;
#62294=DIRECTION ( 'NONE',  ( 0.000000000000000000, 1.000000000000000000, 6.938893903907234689E-15 ) ) ;
#62296=DIRECTION ( 'NONE',  ( 0.000000000000000000, 0.000000000000000000, 1.000000000000000000 ) ) ;
#62297=VERTEX_POINT ( 'NONE', #59209 ) ;
#62299=SURFACE_STYLE_USAGE ( .BOTH. , #30970 ) ;
#62301=AXIS2_PLACEMENT_3D ( 'NONE', #7410, #44396, #6350 ) ;
#62304=CARTESIAN_POINT ( 'NONE',  ( 14.98999599679679662, 146.4999999999999716, -10.00000000000000000 ) ) ;
#62311=CARTESIAN_POINT ( 'NONE',  ( 14.98999599679679662, 146.9999999999999716, 10.00000000000000000 ) ) ;
#62313=CARTESIAN_POINT ( 'NONE',  ( -5.598654528085808657, 137.6449999999999818, 7.705886871421373741 ) ) ;
#62316=UNCERTAINTY_MEASURE_WITH_UNIT (LENGTH_MEASURE( 1.000000000000000082E-05 ), #32324, 'distance_accuracy_value', 'NONE');
#62320=VERTEX_POINT ( 'NONE', #5070 ) ;
#62326=COLOUR_RGB ( '', 0.09019608, 0.27058824, 0.51372549) ;
#62327=ORIENTED_EDGE ( 'NONE', *, *, #15131, .T. ) ;
#62334=SURFACE_STYLE_USAGE ( .BOTH. , #51435 ) ;
#62337=ORIENTED_EDGE ( 'NONE', *, *, #39023, .T. ) ;
#62340=VECTOR ( 'NONE', #61371, 1000.000000000000000 ) ;
#62343=CARTESIAN_POINT ( 'NONE',  ( 0.000000000000000000, 114.4999999999999574, 0.000000000000000000 ) ) ;
#62344=ORIENTED_EDGE ( 'NONE', *, *, #42331, .T. ) ;
#62345=AXIS2_PLACEMENT_3D ( 'NONE', #20120, #9261, #25074 ) ;
#62347=DIRECTION ( 'NONE',  ( 0.000000000000000000, 0.000000000000000000, -1.000000000000000000 ) ) ;
#62348=CARTESIAN_POINT ( 'NONE',  ( 4.716976649647096842, 158.8570736234661638, 6.492361379858953896 ) ) ;
#62350=ORIENTED_EDGE ( 'NONE', *, *, #29628, .F. ) ;
#62352=CARTESIAN_POINT ( 'NONE',  ( 10.01517768586949408, 112.8049999999999784, 1.839758294383810543E-15 ) ) ;
#62353=EDGE_CURVE ( 'NONE', #58540, #849, #47713, .T. ) ;
#62356=ORIENTED_EDGE ( 'NONE', *, *, #27918, .F. ) ;
#62357=CARTESIAN_POINT ( 'NONE',  ( 5.598654528085809545, 140.2549999999999955, -7.705886871421373741 ) ) ;
#62360=( NAMED_UNIT ( * ) PLANE_ANGLE_UNIT ( ) SI_UNIT ( $, .RADIAN. ) );
#62362=CARTESIAN_POINT ( 'NONE',  ( 20.17690446313311625, 115.4776478016129460, 10.00000000000000000 ) ) ;
#62363=FILL_AREA_STYLE_COLOUR ( '', #46373 ) ;
#62367=ORIENTED_EDGE ( 'NONE', *, *, #31902, .T. ) ;
#62368=CARTESIAN_POINT ( 'NONE',  ( 5.038399427696168331, 111.0805650589046820, 7.410012812680835559 ) ) ;
#62369=COLOUR_RGB ( '', 0.40784314, 0.44705882, 0.49803922) ;
#62370=CARTESIAN_POINT ( 'NONE',  ( 75.00000000000000000, -2.215169945516535778E-14, 9.500000000000000000 ) ) ;
#62372=ORIENTED_EDGE ( 'NONE', *, *, #39993, .T. ) ;
#62373=FACE_OUTER_BOUND ( 'NONE', #67968, .T. ) ;
#62375=ORIENTED_EDGE ( 'NONE', *, *, #46847, .F. ) ;
#62381=( NAMED_UNIT ( * ) PLANE_ANGLE_UNIT ( ) SI_UNIT ( $, .RADIAN. ) );
#62382=AXIS2_PLACEMENT_3D ( 'NONE', #52759, #4534, #68937 ) ;
#62384=CIRCLE ( 'NONE', #19697, 22.50000000000000000 ) ;
#62386=CARTESIAN_POINT ( 'NONE',  ( -72.50000000000000000, 36.32520566882265456, 9.500000000000000000 ) ) ;
#62387=CARTESIAN_POINT ( 'NONE',  ( 0.000000000000000000, 142.4449999999999932, -9.525000000000000355 ) ) ;
#62389=CARTESIAN_POINT ( 'NONE',  ( 15.98999599679679839, 147.4999999999999716, -9.500000000000000000 ) ) ;
#62390=VERTEX_POINT ( 'NONE', #31445 ) ;
#62391=DIRECTION ( 'NONE',  ( 1.000000000000000000, -0.000000000000000000, 0.000000000000000000 ) ) ;
#62393=LINE ( 'NONE', #56413, #8788 ) ;
#62397=CARTESIAN_POINT ( 'NONE',  ( -5.598654528085808657, 110.6449999999999960, 7.705886871421373741 ) ) ;
#62400=( LENGTH_UNIT ( ) NAMED_UNIT ( * ) SI_UNIT ( .MILLI., .METRE. ) );
#62403=CARTESIAN_POINT ( 'NONE',  ( 74.50000000000000000, -2.135340797662720349E-14, 10.00000000000000000 ) ) ;
#62404=VECTOR ( 'NONE', #2203, 1000.000000000000000 ) ;
#62409=EDGE_CURVE ( 'NONE', #54497, #62454, #59952, .T. ) ;
#62413=B_SPLINE_CURVE_WITH_KNOTS ( 'NONE', 3,
 ( #30160, #34420, #35473, #2713, #50603, #40769, #45370, #13294 ),
 .UNSPECIFIED., .F., .F.,
 ( 4, 2, 2, 4 ),
 ( 0.000000000000000000, 0.0002391162403816553283, 0.0004782324807633106566, 0.0009564649615266002797 ),
 .UNSPECIFIED. ) ;
#62416=DIRECTION ( 'NONE',  ( -0.000000000000000000, -1.000000000000000000, -0.000000000000000000 ) ) ;
#62417=CIRCLE ( 'NONE', #19681, 0.4999999999999991118 ) ;
#62421=VECTOR ( 'NONE', #69343, 1000.000000000000000 ) ;
#62423=EDGE_CURVE ( 'NONE', #51271, #13202, #55441, .T. ) ;
#62424=ORIENTED_EDGE ( 'NONE', *, *, #51404, .F. ) ;
#62426=( LENGTH_UNIT ( ) NAMED_UNIT ( * ) SI_UNIT ( .MILLI., .METRE. ) );
#62427=CARTESIAN_POINT ( 'NONE',  ( -21.02379604162863913, 109.9999999999999858, 9.500000000000000000 ) ) ;
#62428=ORIENTED_EDGE ( 'NONE', *, *, #66953, .F. ) ;
#62430=CARTESIAN_POINT ( 'NONE',  ( -4.716976649647097730, 136.3570736234661638, -6.492361379858953896 ) ) ;
#62437=EDGE_CURVE ( 'NONE', #19491, #15394, #37532, .T. ) ;
#62438=CIRCLE ( 'NONE', #43378, 5.499999999999976907 ) ;
#62439=SURFACE_SIDE_STYLE ('',( #29737 ) ) ;
#62440=CARTESIAN_POINT ( 'NONE',  ( 2.607480562269118174, 150.9070736234661751, -8.024999999999970157 ) ) ;
#62442=AXIS2_PLACEMENT_3D ( 'NONE', #3867, #9191, #35575 ) ;
#62445=EDGE_LOOP ( 'NONE', ( #115, #68869, #37383, #41049 ) ) ;
#62448=CIRCLE ( 'NONE', #63551, 0.5000000000000004441 ) ;
#62449=ORIENTED_EDGE ( 'NONE', *, *, #12064, .F. ) ;
#62450=DIRECTION ( 'NONE',  ( 0.000000000000000000, 0.000000000000000000, 1.000000000000000000 ) ) ;
#62451=CARTESIAN_POINT ( 'NONE',  ( 71.49999999999998579, 64.07124727947029896, -9.500000000000000000 ) ) ;
#62454=VERTEX_POINT ( 'NONE', #29289 ) ;
#62459=CARTESIAN_POINT ( 'NONE',  ( 8.102448949553181734, 117.9949999999999619, -5.886773742842746238 ) ) ;
#62461=( GEOMETRIC_REPRESENTATION_CONTEXT ( 3 ) GLOBAL_UNCERTAINTY_ASSIGNED_CONTEXT ( ( #53135 ) ) GLOBAL_UNIT_ASSIGNED_CONTEXT ( ( #36484, #20605, #51574 ) ) REPRESENTATION_CONTEXT ( 'NONE', 'WORKASPACE' ) );
#62462=CARTESIAN_POINT ( 'NONE',  ( -9.827790563157511022E-16, 133.4429263765338192, 8.025000000000000355 ) ) ;
#62467=CIRCLE ( 'NONE', #13064, 27.49999999999999645 ) ;
#62468=CARTESIAN_POINT ( 'NONE',  ( -60.00000000000000000, -2.024042244987997205E-14, 7.500000000000000000 ) ) ;
#62470=SURFACE_STYLE_USAGE ( .BOTH. , #67760 ) ;
#62476=CARTESIAN_POINT ( 'NONE',  ( -74.99999999999998579, 50.00000000000000000, 6.500000000000000000 ) ) ;
#62480=VECTOR ( 'NONE', #17223, 1000.000000000000000 ) ;
#62482=CARTESIAN_POINT ( 'NONE',  ( 3.094860106618435136, 152.4049999999999443, -9.525000000000000355 ) ) ;
#62483=DIRECTION ( 'NONE',  ( 0.7292845505553197105, -0.6842105263157864936, 0.000000000000000000 ) ) ;
#62485=CARTESIAN_POINT ( 'NONE',  ( -1.113559396844004956, 154.5000000000000000, -9.459683423334018570 ) ) ;
#62487=CARTESIAN_POINT ( 'NONE',  ( -52.50000000000000000, -2.024042244987997205E-14, -11.50000000000000000 ) ) ;
#62491=ADVANCED_FACE ( 'NONE', ( #19440 ), #34928, .T. ) ;
#62492=ADVANCED_FACE ( 'NONE', ( #24361 ), #9258, .F. ) ;
#62495=VERTEX_POINT ( 'NONE', #25412 ) ;
#62497=( LENGTH_UNIT ( ) NAMED_UNIT ( * ) SI_UNIT ( .MILLI., .METRE. ) );
#62499=EDGE_CURVE ( 'NONE', #33108, #69671, #50646, .T. ) ;
#62500=( NAMED_UNIT ( * ) SI_UNIT ( $, .STERADIAN. ) SOLID_ANGLE_UNIT ( ) );
#62501=DIRECTION ( 'NONE',  ( -0.000000000000000000, -0.000000000000000000, 1.000000000000000000 ) ) ;
#62502=CARTESIAN_POINT ( 'NONE',  ( -83.99999999999997158, 50.00000000000000000, -10.49999999999999822 ) ) ;
#62507=ORIENTED_EDGE ( 'NONE', *, *, #29598, .T. ) ;
#62512=( GEOMETRIC_REPRESENTATION_CONTEXT ( 3 ) GLOBAL_UNCERTAINTY_ASSIGNED_CONTEXT ( ( #69339 ) ) GLOBAL_UNIT_ASSIGNED_CONTEXT ( ( #27121, #1024, #59491 ) ) REPRESENTATION_CONTEXT ( 'NONE', 'WORKASPACE' ) );
#62513=CARTESIAN_POINT ( 'NONE',  ( -74.50000000000000000, 9.708372675170615196, -6.000000000000000000 ) ) ;
#62518=VERTEX_POINT ( 'NONE', #6675 ) ;
#62519=CARTESIAN_POINT ( 'NONE',  ( -2.607480562269073765, 147.0929263765337964, -8.025000000000000355 ) ) ;
#62521=CARTESIAN_POINT ( 'NONE',  ( 40.99999999999997868, 9.999999999999978684, 3.500000000000000000 ) ) ;
#62524=ORIENTED_EDGE ( 'NONE', *, *, #29563, .F. ) ;
#62525=FACE_OUTER_BOUND ( 'NONE', #35756, .T. ) ;
#62526=ORIENTED_EDGE ( 'NONE', *, *, #8726, .T. ) ;
#62527=FACE_OUTER_BOUND ( 'NONE', #28143, .T. ) ;
#62528=DIRECTION ( 'NONE',  ( 0.000000000000000000, 0.000000000000000000, 1.000000000000000000 ) ) ;
#62530=CARTESIAN_POINT ( 'NONE',  ( 41.11302593432304775, 107.5810679765800444, -3.326249178529582906 ) ) ;
#62533=DIRECTION ( 'NONE',  ( -0.000000000000000000, -0.000000000000000000, -1.000000000000000000 ) ) ;
#62534=( NAMED_UNIT ( * ) PLANE_ANGLE_UNIT ( ) SI_UNIT ( $, .RADIAN. ) );
#62538=ORIENTED_EDGE ( 'NONE', *, *, #46532, .T. ) ;
#62539=ORIENTED_EDGE ( 'NONE', *, *, #2671, .T. ) ;
#62540=( LENGTH_UNIT ( ) NAMED_UNIT ( * ) SI_UNIT ( .MILLI., .METRE. ) );
#62542=EDGE_LOOP ( 'NONE', ( #53267, #45243, #69327, #34426 ) ) ;
#62545=SURFACE_STYLE_FILL_AREA ( #46791 ) ;
#62549=ORIENTED_EDGE ( 'NONE', *, *, #46004, .F. ) ;
#62551=CARTESIAN_POINT ( 'NONE',  ( 7.632228543268608334, 117.4570736234661581, -2.479861379858951942 ) ) ;
#62553=CARTESIAN_POINT ( 'NONE',  ( 9.061790287476755523, 154.4999999999999432, 2.966495600661384735 ) ) ;
#62554=CARTESIAN_POINT ( 'NONE',  ( 0.000000000000000000, 114.9999999999999574, 0.000000000000000000 ) ) ;
#62558=CARTESIAN_POINT ( 'NONE',  ( 5.598654528085809545, 125.2549999999999812, -7.705886871421373741 ) ) ;
#62561=DIRECTION ( 'NONE',  ( 0.000000000000000000, 0.000000000000000000, -1.000000000000000000 ) ) ;
#62562=EDGE_CURVE ( 'NONE', #61621, #57494, #17941, .T. ) ;
#62564=CARTESIAN_POINT ( 'NONE',  ( 0.000000000000000000, 149.9999999999999716, 0.000000000000000000 ) ) ;
#62566=EDGE_CURVE ( 'NONE', #54956, #44431, #62938, .T. ) ;
#62567=( LENGTH_UNIT ( ) NAMED_UNIT ( * ) SI_UNIT ( .MILLI., .METRE. ) );
#62571=CARTESIAN_POINT ( 'NONE',  ( -4.716976649647097730, 145.3570736234661638, -6.492361379858953896 ) ) ;
#62573=VECTOR ( 'NONE', #52095, 1000.000000000000000 ) ;
#62576=CARTESIAN_POINT ( 'NONE',  ( -9.827790563157511022E-16, 134.5570736234661808, 8.025000000000000355 ) ) ;
#62577=FILL_AREA_STYLE_COLOUR ( '', #52853 ) ;
#62581=CARTESIAN_POINT ( 'NONE',  ( -45.00000000000000000, -2.024042244987997205E-14, -7.000000000000000888 ) ) ;
#62583=DIRECTION ( 'NONE',  ( 0.000000000000000000, 0.000000000000000000, -1.000000000000000000 ) ) ;
#62584=CARTESIAN_POINT ( 'NONE',  ( -74.99999999999998579, 50.00000000000000000, -6.999999999999988454 ) ) ;
#62586=VERTEX_POINT ( 'NONE', #40123 ) ;
#62588=ORIENTED_EDGE ( 'NONE', *, *, #31275, .T. ) ;
#62593=SURFACE_SIDE_STYLE ('',( #41192 ) ) ;
#62594=ORIENTED_EDGE ( 'NONE', *, *, #40538, .T. ) ;
#62596=CARTESIAN_POINT ( 'NONE',  ( -1.166476076187854022E-15, 140.9449999999999932, 9.525000000000000355 ) ) ;
#62598=ORIENTED_EDGE ( 'NONE', *, *, #16704, .F. ) ;
#62600=CARTESIAN_POINT ( 'NONE',  ( -5.598654528085808657, 153.7549999999999670, 7.705886871421373741 ) ) ;
#62601=SURFACE_STYLE_USAGE ( .BOTH. , #40496 ) ;
#62602=PRESENTATION_STYLE_ASSIGNMENT (( #67550 ) ) ;
#62604=CARTESIAN_POINT ( 'NONE',  ( 6.826472737025121695, 119.4929263765338163, -4.959722759717905660 ) ) ;
#62606=AXIS2_PLACEMENT_3D ( 'NONE', #68892, #42524, #63925 ) ;
#62608=AXIS2_PLACEMENT_3D ( 'NONE', #27391, #27728, #49230 ) ;
#62609=ORIENTED_EDGE ( 'NONE', *, *, #48485, .F. ) ;
#62616=SURFACE_STYLE_FILL_AREA ( #8496 ) ;
#62618=ADVANCED_FACE ( 'NONE', ( #11968 ), #1709, .F. ) ;
#62619=CARTESIAN_POINT ( 'NONE',  ( 0.000000000000000000, 151.0570736234661524, -8.025000000000000355 ) ) ;
#62623=CARTESIAN_POINT ( 'NONE',  ( 0.000000000000000000, 87.30187232391182306, 0.000000000000000000 ) ) ;
#62626=AXIS2_PLACEMENT_3D ( 'NONE', #24285, #67553, #9528 ) ;
#62628=ORIENTED_EDGE ( 'NONE', *, *, #5524, .F. ) ;
#62629=FACE_OUTER_BOUND ( 'NONE', #29391, .T. ) ;
#62633=CARTESIAN_POINT ( 'NONE',  ( -75.00000000000000000, 8.442834901059200092, -5.542315673751891936 ) ) ;
#62634=CARTESIAN_POINT ( 'NONE',  ( 71.99999999999998579, 119.9999999999997868, 7.000000000000000000 ) ) ;
#62636=CARTESIAN_POINT ( 'NONE',  ( -20.71231517720798010, 149.9999999999999716, 10.00000000000000000 ) ) ;
#62637=EDGE_CURVE ( 'NONE', #29016, #36102, #33425, .T. ) ;
#62639=CARTESIAN_POINT ( 'NONE',  ( -5.598654528085808657, 146.6450000000000102, 7.705886871421373741 ) ) ;
#62644=ORIENTED_EDGE ( 'NONE', *, *, #35437, .F. ) ;
#62649=FILL_AREA_STYLE_COLOUR ( '', #8992 ) ;
#62652=CARTESIAN_POINT ( 'NONE',  ( 0.000000000000000000, 154.9999999999999716, 0.000000000000000000 ) ) ;
#62654=VECTOR ( 'NONE', #28651, 1000.000000000000000 ) ;
#62655=CARTESIAN_POINT ( 'NONE',  ( 0.000000000000000000, 128.9429263765338192, -8.025000000000000355 ) ) ;
#62656=ORIENTED_EDGE ( 'NONE', *, *, #10976, .F. ) ;
#62659=FACE_OUTER_BOUND ( 'NONE', #25063, .T. ) ;
#62661=LINE ( 'NONE', #3182, #50562 ) ;
#62663=( NAMED_UNIT ( * ) PLANE_ANGLE_UNIT ( ) SI_UNIT ( $, .RADIAN. ) );
#62664=CIRCLE ( 'NONE', #11010, 0.5000000000000004441 ) ;
#62667=ORIENTED_EDGE ( 'NONE', *, *, #41079, .T. ) ;
#62668=DIRECTION ( 'NONE',  ( 0.000000000000000000, 0.000000000000000000, 1.000000000000000000 ) ) ;
#62673=CARTESIAN_POINT ( 'NONE',  ( -3.094860106618432471, 109.5949999999999847, -9.525000000000000355 ) ) ;
#62676=CARTESIAN_POINT ( 'NONE',  ( -5.598654528085806881, 119.8549999999999898, -7.705886871421374629 ) ) ;
#62679=VERTEX_POINT ( 'NONE', #21710 ) ;
#62680=CARTESIAN_POINT ( 'NONE',  ( 9.058813317711338797, 133.9549999999999841, -2.943386871421372675 ) ) ;
#62683=FACE_OUTER_BOUND ( 'NONE', #49755, .T. ) ;
#62684=VERTEX_POINT ( 'NONE', #20322 ) ;
#62685=CYLINDRICAL_SURFACE ( 'NONE', #51970, 0.5000000000000004441 ) ;
#62686=CARTESIAN_POINT ( 'NONE',  ( 34.99999999999999289, 146.4999999999999716, -7.000000000000000000 ) ) ;
#62688=ORIENTED_EDGE ( 'NONE', *, *, #11192, .F. ) ;
#62689=CARTESIAN_POINT ( 'NONE',  ( 8.442136150874052447, 111.5033947631521585, -1.192225150237074205 ) ) ;
#62690=EDGE_CURVE ( 'NONE', #67222, #20172, #12810, .T. ) ;
#62706=CARTESIAN_POINT ( 'NONE',  ( -8.102448949553179958, 151.8950000000000102, -5.886773742842749790 ) ) ;
#62709=EDGE_CURVE ( 'NONE', #56663, #9275, #21021, .T. ) ;
#62712=ORIENTED_EDGE ( 'NONE', *, *, #20176, .T. ) ;
#62713=PLANE ( 'NONE',  #60820 ) ;
#62715=( GEOMETRIC_REPRESENTATION_CONTEXT ( 3 ) GLOBAL_UNCERTAINTY_ASSIGNED_CONTEXT ( ( #52989 ) ) GLOBAL_UNIT_ASSIGNED_CONTEXT ( ( #64024, #21463, #56228 ) ) REPRESENTATION_CONTEXT ( 'NONE', 'WORKASPACE' ) );
#62716=FILL_AREA_STYLE_COLOUR ( '', #11143 ) ;
#62721=CARTESIAN_POINT ( 'NONE',  ( 9.058813317711338797, 111.8449999999999847, -2.943386871421372675 ) ) ;
#62725=( NAMED_UNIT ( * ) PLANE_ANGLE_UNIT ( ) SI_UNIT ( $, .RADIAN. ) );
#62729=AXIS2_PLACEMENT_3D ( 'NONE', #42624, #37005, #31316 ) ;
#62735=CARTESIAN_POINT ( 'NONE',  ( -7.632228543268608334, 124.9570736234661581, 2.479861379858952830 ) ) ;
#62739=DIRECTION ( 'NONE',  ( -0.000000000000000000, -1.000000000000000000, 0.000000000000000000 ) ) ;
#62743=DIRECTION ( 'NONE',  ( -0.000000000000000000, -1.000000000000000000, -0.000000000000000000 ) ) ;
#62746=CARTESIAN_POINT ( 'NONE',  ( 60.99999999999998579, 50.00000000000000000, -9.500000000000000000 ) ) ;
#62751=FILL_AREA_STYLE_COLOUR ( '', #21708 ) ;
#62756=CARTESIAN_POINT ( 'NONE',  ( 7.632228543268607446, 132.1570736234661467, 2.479861379858954606 ) ) ;
#62765=( NAMED_UNIT ( * ) SI_UNIT ( $, .STERADIAN. ) SOLID_ANGLE_UNIT ( ) );
#62768=ORIENTED_EDGE ( 'NONE', *, *, #9237, .T. ) ;
#62771=ORIENTED_EDGE ( 'NONE', *, *, #19725, .T. ) ;
#62774=DIRECTION ( 'NONE',  ( -0.000000000000000000, -0.000000000000000000, -1.000000000000000000 ) ) ;
#62776=UNCERTAINTY_MEASURE_WITH_UNIT (LENGTH_MEASURE( 1.000000000000000082E-05 ), #936, 'distance_accuracy_value', 'NONE');
#62778=CARTESIAN_POINT ( 'NONE',  ( 68.50000000000000000, 1.797044900979284448E-15, -10.49999999999999822 ) ) ;
#62779=DIRECTION ( 'NONE',  ( 0.000000000000000000, 1.000000000000000000, -0.000000000000000000 ) ) ;
#62780=CIRCLE ( 'NONE', #32448, 13.49999999999999822 ) ;
#62784=SURFACE_STYLE_USAGE ( .BOTH. , #19880 ) ;
#62786=MECHANICAL_DESIGN_GEOMETRIC_PRESENTATION_REPRESENTATION('',(#14494),#51555);
#62787=DIRECTION ( 'NONE',  ( -0.000000000000000000, -0.000000000000000000, 1.000000000000000000 ) ) ;
#62791=CARTESIAN_POINT ( 'NONE',  ( 9.058813317711337021, 126.5449999999999875, 2.943386871421375783 ) ) ;
#62792=( GEOMETRIC_REPRESENTATION_CONTEXT ( 3 ) GLOBAL_UNCERTAINTY_ASSIGNED_CONTEXT ( ( #16637 ) ) GLOBAL_UNIT_ASSIGNED_CONTEXT ( ( #42793, #58225, #10047 ) ) REPRESENTATION_CONTEXT ( 'NONE', 'WORKASPACE' ) );
#62797=LINE ( 'NONE', #63842, #1405 ) ;
#62804=SURFACE_STYLE_FILL_AREA ( #40704 ) ;
#62805=CARTESIAN_POINT ( 'NONE',  ( -1.994734356760242244, 110.7119700403975884, -9.105933873098768672 ) ) ;
#62810=DIRECTION ( 'NONE',  ( -0.000000000000000000, 1.000000000000000000, 0.000000000000000000 ) ) ;
#62811=UNCERTAINTY_MEASURE_WITH_UNIT (LENGTH_MEASURE( 1.000000000000000082E-05 ), #51900, 'distance_accuracy_value', 'NONE');
#62814=( GEOMETRIC_REPRESENTATION_CONTEXT ( 3 ) GLOBAL_UNCERTAINTY_ASSIGNED_CONTEXT ( ( #25536 ) ) GLOBAL_UNIT_ASSIGNED_CONTEXT ( ( #21640, #53987, #48420 ) ) REPRESENTATION_CONTEXT ( 'NONE', 'WORKASPACE' ) );
#62818=CARTESIAN_POINT ( 'NONE',  ( -8.102448949553181734, 159.6050000000000182, 5.886773742842747126 ) ) ;
#62819=CARTESIAN_POINT ( 'NONE',  ( -60.00000000000000000, -2.024042244987997205E-14, -12.00000000000000000 ) ) ;
#62820=CARTESIAN_POINT ( 'NONE',  ( -45.00000000000000000, -1.469576158976824302E-14, 10.00000000000000000 ) ) ;
#62826=CARTESIAN_POINT ( 'NONE',  ( -1.447422522083364749, 110.7948483342343593, 9.145303841767344011 ) ) ;
#62829=CARTESIAN_POINT ( 'NONE',  ( -48.00000000000000000, 14.49137674618942562, -7.000000000000000000 ) ) ;
#62830=EDGE_CURVE ( 'NONE', #61802, #61535, #46564, .T. ) ;
#62836=EDGE_CURVE ( 'NONE', #54396, #6517, #38631, .T. ) ;
#62839=AXIS2_PLACEMENT_3D ( 'NONE', #1131, #33560, #65568 ) ;
#62840=CARTESIAN_POINT ( 'NONE',  ( -21.02379601146600763, 114.6388938931947763, 10.00000000000000000 ) ) ;
#62841=CARTESIAN_POINT ( 'NONE',  ( -45.50000000000000000, -1.469576158976824302E-14, 6.999999999999999112 ) ) ;
#62843=PRESENTATION_STYLE_ASSIGNMENT (( #30838 ) ) ;
#62844=ORIENTED_EDGE ( 'NONE', *, *, #64414, .F. ) ;
#62847=CARTESIAN_POINT ( 'NONE',  ( -75.50000000000000000, 35.50862325381056905, -41.30495168499704306 ) ) ;
#62848=ORIENTED_EDGE ( 'NONE', *, *, #51484, .F. ) ;
#62849=CARTESIAN_POINT ( 'NONE',  ( -3.094860106618434248, 123.9049999999999727, 9.525000000000000355 ) ) ;
#62851=ORIENTED_EDGE ( 'NONE', *, *, #51566, .T. ) ;
#62854=EDGE_LOOP ( 'NONE', ( #3450, #58278, #32044, #53218 ) ) ;
#62857=VERTEX_POINT ( 'NONE', #858 ) ;
#62858=CARTESIAN_POINT ( 'NONE',  ( -4.716976649647097730, 156.2429263765338021, -6.492361379858953896 ) ) ;
#62863=CARTESIAN_POINT ( 'NONE',  ( -71.62068965517238439, 63.58603185604027885, 7.000000000000000000 ) ) ;
#62866=( NAMED_UNIT ( * ) PLANE_ANGLE_UNIT ( ) SI_UNIT ( $, .RADIAN. ) );
#62869=CYLINDRICAL_SURFACE ( 'NONE', #9523, 0.5000000000000004441 ) ;
#62870=MECHANICAL_DESIGN_GEOMETRIC_PRESENTATION_REPRESENTATION('',(#16869),#32542);
#62871=DIRECTION ( 'NONE',  ( -0.000000000000000000, 1.000000000000000000, -0.000000000000000000 ) ) ;
#62872=CARTESIAN_POINT ( 'NONE',  ( 71.50000000000000000, 36.32520566882265456, -7.500000000000000000 ) ) ;
#62873=MECHANICAL_DESIGN_GEOMETRIC_PRESENTATION_REPRESENTATION('',(#44957),#7906);
#62874=DIRECTION ( 'NONE',  ( -0.9486832980505138790, -0.3162277660168378857, 0.000000000000000000 ) ) ;
#62877=ORIENTED_EDGE ( 'NONE', *, *, #61139, .T. ) ;
#62879=FACE_OUTER_BOUND ( 'NONE', #25991, .T. ) ;
#62880=( NAMED_UNIT ( * ) SI_UNIT ( $, .STERADIAN. ) SOLID_ANGLE_UNIT ( ) );
#62881=DIRECTION ( 'NONE',  ( -0.000000000000000000, -0.000000000000000000, -1.000000000000000000 ) ) ;
#62882=DIRECTION ( 'NONE',  ( -4.336808689941999001E-16, 1.000000000000000000, 0.000000000000000000 ) ) ;
#62888=( GEOMETRIC_REPRESENTATION_CONTEXT ( 3 ) GLOBAL_UNCERTAINTY_ASSIGNED_CONTEXT ( ( #25830 ) ) GLOBAL_UNIT_ASSIGNED_CONTEXT ( ( #3612, #41675, #41322 ) ) REPRESENTATION_CONTEXT ( 'NONE', 'WORKASPACE' ) );
#62891=EDGE_CURVE ( 'NONE', #51540, #22849, #18453, .T. ) ;
#62895=DIRECTION ( 'NONE',  ( 1.000000000000000000, 0.000000000000000000, 0.000000000000000000 ) ) ;
#62896=FILL_AREA_STYLE_COLOUR ( '', #16772 ) ;
#62900=SURFACE_SIDE_STYLE ('',( #3074 ) ) ;
#62901=CIRCLE ( 'NONE', #16900, 26.49999999999999645 ) ;
#62904=CARTESIAN_POINT ( 'NONE',  ( -9.058813317711338797, 123.4549999999999841, 2.943386871421373563 ) ) ;
#62906=DIRECTION ( 'NONE',  ( -1.000000000000000000, 0.000000000000000000, 0.000000000000000000 ) ) ;
#62911=CARTESIAN_POINT ( 'NONE',  ( 24.21231517720798010, 113.4999999999999858, 7.500000000000000000 ) ) ;
#62917=CARTESIAN_POINT ( 'NONE',  ( 7.632228543268608334, 135.4570736234661581, -2.479861379858951942 ) ) ;
#62921=CARTESIAN_POINT ( 'NONE',  ( -45.89999098806710975, 9.371467124235310919, -6.143012557965069398 ) ) ;
#62923=( BOUNDED_SURFACE ( )  B_SPLINE_SURFACE ( 3, 2, ( 
 ( #22237, #33154, #38806 ),
 ( #59507, #55278, #49681 ),
 ( #65136, #6057, #60895 ),
 ( #33482, #54911, #6739 ),
 ( #27140, #44777, #11329 ),
 ( #27494, #54587, #66175 ),
 ( #48673, #1418, #44442 ),
 ( #43733, #6393, #39149 ) ),
 .UNSPECIFIED., .F., .F., .F. ) 
 B_SPLINE_SURFACE_WITH_KNOTS ( ( 4, 2, 2, 4 ),
 ( 3, 3 ),
 ( 4.336808689942017736E-19, 0.0003058805084468733276, 0.0004588207626703098016, 0.0006117610168937462215 ),
 ( 0.000000000000000000, 1.000000000000000000 ),
 .UNSPECIFIED. ) 
 GEOMETRIC_REPRESENTATION_ITEM ( )  RATIONAL_B_SPLINE_SURFACE ( (
 ( 1.000000000000000000, 0.3766558475679906981, 1.000000000000000000),
 ( 1.000000000000000000, 0.3767717614668182335, 1.000000000000000000),
 ( 1.000000000000000000, 0.3678485930275403604, 1.000000000000000000),
 ( 1.000000000000000000, 0.3444746654570013944, 1.000000000000000000),
 ( 1.000000000000000000, 0.3350482327563981677, 1.000000000000000000),
 ( 1.000000000000000000, 0.3140847209475624568, 1.000000000000000000),
 ( 1.000000000000000000, 0.3025536022197361508, 1.000000000000000000),
 ( 1.000000000000000000, 0.2907356542125085763, 1.000000000000000000) ) ) 
 REPRESENTATION_ITEM ( '' )  SURFACE ( )  );
#62925=UNCERTAINTY_MEASURE_WITH_UNIT (LENGTH_MEASURE( 1.000000000000000082E-05 ), #18196, 'distance_accuracy_value', 'NONE');
#62926=CIRCLE ( 'NONE', #25875, 0.5000000000000004441 ) ;
#62928=( LENGTH_UNIT ( ) NAMED_UNIT ( * ) SI_UNIT ( .MILLI., .METRE. ) );
#62930=ORIENTED_EDGE ( 'NONE', *, *, #25804, .F. ) ;
#62938=B_SPLINE_CURVE_WITH_KNOTS ( 'NONE', 3,
 ( #60833, #66475, #44383, #28110, #13003, #55213, #23906, #45060, #29159, #39431 ),
 .UNSPECIFIED., .F., .F.,
 ( 4, 2, 2, 2, 4 ),
 ( 0.000000000000000000, 0.0004706383985570294502, 0.0009412767971140589005, 0.001411915195671088405, 0.001882553594228117801 ),
 .UNSPECIFIED. ) ;
#62942=CARTESIAN_POINT ( 'NONE',  ( -5.598654528085806881, 151.7450000000000045, -7.705886871421374629 ) ) ;
#62945=CARTESIAN_POINT ( 'NONE',  ( 60.00000000000000000, 1.797044900979284448E-15, -11.50000000000001066 ) ) ;
#62946=CARTESIAN_POINT ( 'NONE',  ( -9.058813317711338797, 147.4550000000000125, 2.943386871421373563 ) ) ;
#62947=FACE_OUTER_BOUND ( 'NONE', #53091, .T. ) ;
#62950=CARTESIAN_POINT ( 'NONE',  ( -4.716976649647097730, 114.2429263765338163, -6.492361379858953896 ) ) ;
#62952=UNCERTAINTY_MEASURE_WITH_UNIT (LENGTH_MEASURE( 1.000000000000000082E-05 ), #31119, 'distance_accuracy_value', 'NONE');
#62959=CARTESIAN_POINT ( 'NONE',  ( 40.99999999999998579, 107.7459666924148252, 3.000000000000000000 ) ) ;
#62962=SURFACE_SIDE_STYLE ('',( #9183 ) ) ;
#62966=UNCERTAINTY_MEASURE_WITH_UNIT (LENGTH_MEASURE( 1.000000000000000082E-05 ), #48576, 'distance_accuracy_value', 'NONE');
#62967=AXIS2_PLACEMENT_3D ( 'NONE', #39338, #64986, #17538 ) ;
#62968=EDGE_CURVE ( 'NONE', #62495, #7517, #67058, .T. ) ;
#62971=DIRECTION ( 'NONE',  ( 0.000000000000000000, -1.000000000000000000, 0.000000000000000000 ) ) ;
#62974=( NAMED_UNIT ( * ) PLANE_ANGLE_UNIT ( ) SI_UNIT ( $, .RADIAN. ) );
#62975=ORIENTED_EDGE ( 'NONE', *, *, #42630, .F. ) ;
#62977=ORIENTED_EDGE ( 'NONE', *, *, #56829, .T. ) ;
#62979=SURFACE_SIDE_STYLE ('',( #40881 ) ) ;
#62984=( NAMED_UNIT ( * ) PLANE_ANGLE_UNIT ( ) SI_UNIT ( $, .RADIAN. ) );
#62985=EDGE_CURVE ( 'NONE', #66402, #10860, #28499, .T. ) ;
#62987=EDGE_CURVE ( 'NONE', #10808, #28945, #44299, .T. ) ;
#62991=AXIS2_PLACEMENT_3D ( 'NONE', #35273, #24350, #34228 ) ;
#62992=ADVANCED_FACE ( 'NONE', ( #21191 ), #44101, .F. ) ;
#62994=CARTESIAN_POINT ( 'NONE',  ( -75.00000000000000000, 9.708372671850062474, -6.049000248777010036 ) ) ;
#62997=CARTESIAN_POINT ( 'NONE',  ( 3.094860106618431583, 153.0949999999999989, 9.525000000000000355 ) ) ;
#63002=CIRCLE ( 'NONE', #25935, 0.4999999999999994449 ) ;
#63004=ORIENTED_EDGE ( 'NONE', *, *, #69275, .T. ) ;
#63010=DIRECTION ( 'NONE',  ( 0.000000000000000000, 0.000000000000000000, 1.000000000000000000 ) ) ;
#63011=LINE ( 'NONE', #14850, #25846 ) ;
#63014=SURFACE_STYLE_FILL_AREA ( #43602 ) ;
#63016=CIRCLE ( 'NONE', #41717, 7.500000000000007105 ) ;
#63024=EDGE_LOOP ( 'NONE', ( #13922, #11678 ) ) ;
#63025=DIRECTION ( 'NONE',  ( 1.000000000000000000, 0.000000000000000000, 0.000000000000000000 ) ) ;
#63028=MECHANICAL_DESIGN_GEOMETRIC_PRESENTATION_REPRESENTATION('',(#10280),#51860);
#63031=CARTESIAN_POINT ( 'NONE',  ( -5.598654528085806881, 121.7449999999999903, -7.705886871421374629 ) ) ;
#63033=ORIENTED_EDGE ( 'NONE', *, *, #58004, .T. ) ;
#63036=CARTESIAN_POINT ( 'NONE',  ( -8.102448949553179958, 120.0049999999999812, -5.886773742842749790 ) ) ;
#63037=( GEOMETRIC_REPRESENTATION_CONTEXT ( 3 ) GLOBAL_UNCERTAINTY_ASSIGNED_CONTEXT ( ( #67218 ) ) GLOBAL_UNIT_ASSIGNED_CONTEXT ( ( #43924, #54754, #558 ) ) REPRESENTATION_CONTEXT ( 'NONE', 'WORKASPACE' ) );
#63041=ORIENTED_EDGE ( 'NONE', *, *, #40603, .T. ) ;
#63042=CARTESIAN_POINT ( 'NONE',  ( -3.094860106618434248, 141.9050000000000011, 9.525000000000000355 ) ) ;
#63043=UNCERTAINTY_MEASURE_WITH_UNIT (LENGTH_MEASURE( 1.000000000000000082E-05 ), #5685, 'distance_accuracy_value', 'NONE');
#63044=CARTESIAN_POINT ( 'NONE',  ( -57.99999999999997868, 50.00000000000000000, 6.500000000000000000 ) ) ;
#63047=CARTESIAN_POINT ( 'NONE',  ( -41.30888752411017606, 107.2690689356287663, 3.464811251346369581 ) ) ;
#63049=FILL_AREA_STYLE ('',( #62363 ) ) ;
#63050=ORIENTED_EDGE ( 'NONE', *, *, #28325, .T. ) ;
#63051=DIRECTION ( 'NONE',  ( -0.000000000000000000, 1.000000000000000000, 0.000000000000000000 ) ) ;
#63052=SURFACE_STYLE_USAGE ( .BOTH. , #58476 ) ;
#63057=CARTESIAN_POINT ( 'NONE',  ( 5.871527698221330027, 111.7477971676043609, -5.859198738425208219 ) ) ;
#63058=EDGE_CURVE ( 'NONE', #61698, #52342, #9531, .T. ) ;
#63060=( LENGTH_UNIT ( ) NAMED_UNIT ( * ) SI_UNIT ( .MILLI., .METRE. ) );
#63066=CARTESIAN_POINT ( 'NONE',  ( 45.65811388300841855, 10.21937129433612235, 3.999999999999999112 ) ) ;
#63068=ORIENTED_EDGE ( 'NONE', *, *, #54713, .T. ) ;
#63070=EDGE_CURVE ( 'NONE', #10224, #26613, #48864, .T. ) ;
#63071=DIRECTION ( 'NONE',  ( 0.000000000000000000, 0.000000000000000000, -1.000000000000000000 ) ) ;
#63075=CARTESIAN_POINT ( 'NONE',  ( -9.058813317711338797, 149.3449999999999989, 2.943386871421373563 ) ) ;
#63077=VECTOR ( 'NONE', #59085, 1000.000000000000000 ) ;
#63078=EDGE_CURVE ( 'NONE', #60536, #4324, #20709, .T. ) ;
#63081=DIRECTION ( 'NONE',  ( -1.000000000000000000, 0.000000000000000000, 0.000000000000000000 ) ) ;
#63085=CARTESIAN_POINT ( 'NONE',  ( 60.00000000000000000, 1.797044900979284448E-15, -12.00000000000000000 ) ) ;
#63086=CARTESIAN_POINT ( 'NONE',  ( 8.102448949553183510, 120.9949999999999761, -5.886773742842746238 ) ) ;
#63088=AXIS2_PLACEMENT_3D ( 'NONE', #23913, #65795, #50313 ) ;
#63091=ORIENTED_EDGE ( 'NONE', *, *, #26062, .T. ) ;
#63092=CARTESIAN_POINT ( 'NONE',  ( 15.98999599679679839, 146.4999999999999716, 10.00000000000000000 ) ) ;
#63099=VECTOR ( 'NONE', #233, 1000.000000000000000 ) ;
#63101=FILL_AREA_STYLE_COLOUR ( '', #59333 ) ;
#63102=( NAMED_UNIT ( * ) SI_UNIT ( $, .STERADIAN. ) SOLID_ANGLE_UNIT ( ) );
#63104=COLOUR_RGB ( '', 0.40784314, 0.44705882, 0.49803922) ;
#63108=CARTESIAN_POINT ( 'NONE',  ( -35.00000000000003553, 10.49999999999998224, 3.000000000000000000 ) ) ;
#63109=ADVANCED_FACE ( 'NONE', ( #48326 ), #53306, .T. ) ;
#63117=ORIENTED_EDGE ( 'NONE', *, *, #50316, .T. ) ;
#63118=CARTESIAN_POINT ( 'NONE',  ( 45.07697505292422591, 10.02565835097472480, -3.091949714863345910 ) ) ;
#63119=SURFACE_STYLE_FILL_AREA ( #31093 ) ;
#63120=ORIENTED_EDGE ( 'NONE', *, *, #21755, .T. ) ;
#63122=CARTESIAN_POINT ( 'NONE',  ( -6.826472737025120807, 134.1070736234661638, 4.959722759717906548 ) ) ;
#63125=ORIENTED_EDGE ( 'NONE', *, *, #8962, .T. ) ;
#63134=CARTESIAN_POINT ( 'NONE',  ( 4.716976649647096842, 142.7429263765338305, 6.492361379858953896 ) ) ;
#63138=ORIENTED_EDGE ( 'NONE', *, *, #54713, .F. ) ;
#63139=SURFACE_SIDE_STYLE ('',( #16025 ) ) ;
#63142=LINE ( 'NONE', #42430, #55229 ) ;
#63145=ADVANCED_FACE ( 'NONE', ( #11688 ), #1560, .T. ) ;
#63151=AXIS2_PLACEMENT_3D ( 'NONE', #30401, #31809, #58907 ) ;
#63154=SPHERICAL_SURFACE ( 'NONE', #57056, 0.5000000000000000000 ) ;
#63155=ORIENTED_EDGE ( 'NONE', *, *, #5453, .F. ) ;
#63156=CIRCLE ( 'NONE', #28269, 18.00000000000000355 ) ;
#63157=DIRECTION ( 'NONE',  ( -1.000000000000000000, 0.000000000000000000, 0.000000000000000000 ) ) ;
#63158=ORIENTED_EDGE ( 'NONE', *, *, #40859, .T. ) ;
#63164=CARTESIAN_POINT ( 'NONE',  ( -5.598654528085806881, 127.7450000000000045, -7.705886871421374629 ) ) ;
#63166=AXIS2_PLACEMENT_3D ( 'NONE', #34573, #49388, #7507 ) ;
#63168=DIRECTION ( 'NONE',  ( -0.000000000000000000, -0.000000000000000000, -1.000000000000000000 ) ) ;
#63170=PRESENTATION_STYLE_ASSIGNMENT (( #35405 ) ) ;
#63173=COLOUR_RGB ( '', 0.31764706, 0.68627451, 0.89019608) ;
#63175=FILL_AREA_STYLE_COLOUR ( '', #51634 ) ;
#63180=CARTESIAN_POINT ( 'NONE',  ( 44.34845674352008871, 9.782818914506675512, -3.509226550553885549 ) ) ;
#63181=( GEOMETRIC_REPRESENTATION_CONTEXT ( 3 ) GLOBAL_UNCERTAINTY_ASSIGNED_CONTEXT ( ( #27878 ) ) GLOBAL_UNIT_ASSIGNED_CONTEXT ( ( #7861, #13139, #2541 ) ) REPRESENTATION_CONTEXT ( 'NONE', 'WORKASPACE' ) );
#63182=CARTESIAN_POINT ( 'NONE',  ( -15.98999599679679839, 118.4999999999999716, 9.500000000000000000 ) ) ;
#63183=CARTESIAN_POINT ( 'NONE',  ( 34.99999999999999289, 113.4999999999999858, 7.500000000000000000 ) ) ;
#63185=DIRECTION ( 'NONE',  ( -0.000000000000000000, -0.000000000000000000, -1.000000000000000000 ) ) ;
#63188=CARTESIAN_POINT ( 'NONE',  ( -3.094860106618434248, 156.9050000000000011, 9.525000000000000355 ) ) ;
#63192=SURFACE_STYLE_FILL_AREA ( #20267 ) ;
#63194=ADVANCED_FACE ( 'NONE', ( #2098 ), #13409, .F. ) ;
#63197=CARTESIAN_POINT ( 'NONE',  ( 0.000000000000000000, 114.9999999999999574, 0.000000000000000000 ) ) ;
#63198=SURFACE_SIDE_STYLE ('',( #8359 ) ) ;
#63199=( NAMED_UNIT ( * ) PLANE_ANGLE_UNIT ( ) SI_UNIT ( $, .RADIAN. ) );
#63202=ORIENTED_EDGE ( 'NONE', *, *, #39843, .T. ) ;
#63205=TOROIDAL_SURFACE ( 'NONE', #18269, 9.500000000000005329, 0.5000000000000000000 ) ;
#63211=ORIENTED_EDGE ( 'NONE', *, *, #23304, .F. ) ;
#63212=EDGE_LOOP ( 'NONE', ( #30578, #34909, #23533, #20906 ) ) ;
#63213=STYLED_ITEM ( 'NONE', ( #9778 ), #7080 ) ;
#63218=VERTEX_POINT ( 'NONE', #61945 ) ;
#63219=EDGE_CURVE ( 'NONE', #19879, #47797, #18005, .T. ) ;
#63220=CARTESIAN_POINT ( 'NONE',  ( 0.000000000000000000, 119.5549999999999926, -9.525000000000000355 ) ) ;
#63226=VECTOR ( 'NONE', #64805, 1000.000000000000000 ) ;
#63228=EDGE_CURVE ( 'NONE', #7688, #31048, #33825, .T. ) ;
#63229=ORIENTED_EDGE ( 'NONE', *, *, #36524, .T. ) ;
#63230=CARTESIAN_POINT ( 'NONE',  ( -6.826472737025120807, 150.9929263765338305, 4.959722759717906548 ) ) ;
#63232=AXIS2_PLACEMENT_3D ( 'NONE', #9880, #25344, #13753 ) ;
#63236=SURFACE_STYLE_USAGE ( .BOTH. , #36555 ) ;
#63237=COLOUR_RGB ( '', 0.08235294, 0.09019608, 0.10196078) ;
#63240=CARTESIAN_POINT ( 'NONE',  ( 12.72792206135785698, 114.9999999999999574, 10.50000000000000000 ) ) ;
#63241=CARTESIAN_POINT ( 'NONE',  ( 7.632228543268608334, 141.4570736234661581, -2.479861379858951942 ) ) ;
#63244=CARTESIAN_POINT ( 'NONE',  ( 24.21231517720798010, 117.4999999999999716, -7.000000000000000000 ) ) ;
#63245=DIRECTION ( 'NONE',  ( -0.000000000000000000, -0.000000000000000000, -1.000000000000000000 ) ) ;
#63248=VERTEX_POINT ( 'NONE', #23287 ) ;
#63249=FACE_OUTER_BOUND ( 'NONE', #7681, .T. ) ;
#63251=CARTESIAN_POINT ( 'NONE',  ( 48.50000000000000000, 14.49137674618942562, -10.00000000000000000 ) ) ;
#63253=FACE_OUTER_BOUND ( 'NONE', #35620, .T. ) ;
#63256=EDGE_CURVE ( 'NONE', #23604, #51230, #2672, .T. ) ;
#63268=( NAMED_UNIT ( * ) SI_UNIT ( $, .STERADIAN. ) SOLID_ANGLE_UNIT ( ) );
#63273=CARTESIAN_POINT ( 'NONE',  ( -10.01517768586949231, 123.3049999999999926, -6.132527647946036459E-16 ) ) ;
#63279=EDGE_LOOP ( 'NONE', ( #37936, #49206, #11377, #10886 ) ) ;
#63282=CARTESIAN_POINT ( 'NONE',  ( -6.826472737025120807, 145.5070736234661410, -4.959722759717907437 ) ) ;
#63286=CARTESIAN_POINT ( 'NONE',  ( -72.00000000000000000, 14.49137674618942562, -10.00000000000000000 ) ) ;
#63287=( NAMED_UNIT ( * ) PLANE_ANGLE_UNIT ( ) SI_UNIT ( $, .RADIAN. ) );
#63290=ORIENTED_EDGE ( 'NONE', *, *, #69580, .T. ) ;
#63292=AXIS2_PLACEMENT_3D ( 'NONE', #20859, #42012, #42699 ) ;
#63297=ORIENTED_EDGE ( 'NONE', *, *, #54693, .F. ) ;
#63303=ORIENTED_EDGE ( 'NONE', *, *, #34655, .F. ) ;
#63305=FILL_AREA_STYLE ('',( #47885 ) ) ;
#63308=CARTESIAN_POINT ( 'NONE',  ( -3.094860106618432471, 148.5949999999999704, -9.525000000000000355 ) ) ;
#63312=DIRECTION ( 'NONE',  ( 0.000000000000000000, 1.000000000000000000, 0.000000000000000000 ) ) ;
#63313=CARTESIAN_POINT ( 'NONE',  ( -8.102448949553179958, 147.0049999999999955, -5.886773742842749790 ) ) ;
#63314=ORIENTED_EDGE ( 'NONE', *, *, #16069, .F. ) ;
#63315=CARTESIAN_POINT ( 'NONE',  ( -2.607480562269075097, 127.2929263765337993, 8.025000000000000355 ) ) ;
#63318=( GEOMETRIC_REPRESENTATION_CONTEXT ( 3 ) GLOBAL_UNCERTAINTY_ASSIGNED_CONTEXT ( ( #14508 ) ) GLOBAL_UNIT_ASSIGNED_CONTEXT ( ( #22104, #10857, #5906 ) ) REPRESENTATION_CONTEXT ( 'NONE', 'WORKASPACE' ) );
#63319=FACE_OUTER_BOUND ( 'NONE', #24796, .T. ) ;
#63320=FACE_OUTER_BOUND ( 'NONE', #19622, .T. ) ;
#63321=ORIENTED_EDGE ( 'NONE', *, *, #31616, .F. ) ;
#63322=CARTESIAN_POINT ( 'NONE',  ( -40.78947368421051323, 108.1536491499103505, -3.157942443983132730 ) ) ;
#63326=DIRECTION ( 'NONE',  ( 0.000000000000000000, 0.000000000000000000, 1.000000000000000000 ) ) ;
#63331=CARTESIAN_POINT ( 'NONE',  ( -65.00000000000000000, -1.962809905030629631E-14, 6.999999999999995559 ) ) ;
#63333=SURFACE_STYLE_FILL_AREA ( #68975 ) ;
#63334=ORIENTED_EDGE ( 'NONE', *, *, #15128, .T. ) ;
#63336=CARTESIAN_POINT ( 'NONE',  ( -66.49999999999998579, 50.00000000000000000, -11.50000000000000000 ) ) ;
#63338=AXIS2_PLACEMENT_3D ( 'NONE', #32970, #12524, #39648 ) ;
#63340=ORIENTED_EDGE ( 'NONE', *, *, #16783, .T. ) ;
#63347=MECHANICAL_DESIGN_GEOMETRIC_PRESENTATION_REPRESENTATION('',(#26123),#12759);
#63351=DIRECTION ( 'NONE',  ( 0.000000000000000000, 1.000000000000000000, -0.000000000000000000 ) ) ;
#63352=CARTESIAN_POINT ( 'NONE',  ( 5.598654528085809545, 148.1450000000000102, -7.705886871421373741 ) ) ;
#63354=CARTESIAN_POINT ( 'NONE',  ( 44.99999999999998579, 119.9999999999999716, -9.500000000000000000 ) ) ;
#63355=AXIS2_PLACEMENT_3D ( 'NONE', #50871, #2628, #56483 ) ;
#63358=STYLED_ITEM ( 'NONE', ( #778 ), #56073 ) ;
#63359=CARTESIAN_POINT ( 'NONE',  ( 0.000000000000000000, 143.9429263765338192, -8.025000000000000355 ) ) ;
#63362=AXIS2_PLACEMENT_3D ( 'NONE', #63354, #14464, #4598 ) ;
#63367=DIRECTION ( 'NONE',  ( 0.000000000000000000, -1.000000000000000000, 0.000000000000000000 ) ) ;
#63370=DIRECTION ( 'NONE',  ( 1.000000000000000000, 0.000000000000000000, 0.000000000000000000 ) ) ;
#63374=CARTESIAN_POINT ( 'NONE',  ( -74.99999999999998579, 50.00000000000000000, 7.500000000000000000 ) ) ;
#63375=AXIS2_PLACEMENT_3D ( 'NONE', #5757, #69128, #20581 ) ;
#63377=CARTESIAN_POINT ( 'NONE',  ( -45.00000000000000000, 8.253551290271557761, 5.607507417892153789 ) ) ;
#63378=CARTESIAN_POINT ( 'NONE',  ( 44.64649554404039122, 9.999999999999978684, 3.314804571885168638 ) ) ;
#63379=FACE_OUTER_BOUND ( 'NONE', #2046, .T. ) ;
#63382=AXIS2_PLACEMENT_3D ( 'NONE', #6400, #382, #1055 ) ;
#63383=EDGE_CURVE ( 'NONE', #46789, #64160, #69018, .T. ) ;
#63384=ORIENTED_EDGE ( 'NONE', *, *, #27860, .F. ) ;
#63389=MECHANICAL_DESIGN_GEOMETRIC_PRESENTATION_REPRESENTATION('',(#4982),#12816);
#63392=EDGE_CURVE ( 'NONE', #65027, #13063, #42299, .T. ) ;
#63394=CARTESIAN_POINT ( 'NONE',  ( -3.094860106618434248, 125.7949999999999733, 9.525000000000000355 ) ) ;
#63395=DIRECTION ( 'NONE',  ( 0.000000000000000000, 0.000000000000000000, 1.000000000000000000 ) ) ;
#63396=ORIENTED_EDGE ( 'NONE', *, *, #6756, .F. ) ;
#63398=CARTESIAN_POINT ( 'NONE',  ( -1.166476076187854022E-15, 121.0549999999999784, 9.525000000000000355 ) ) ;
#63401=FILL_AREA_STYLE ('',( #20484 ) ) ;
#63403=CARTESIAN_POINT ( 'NONE',  ( -8.102448949553181734, 150.6050000000000182, 5.886773742842747126 ) ) ;
#63404=DIRECTION ( 'NONE',  ( 0.000000000000000000, 1.000000000000000000, 0.000000000000000000 ) ) ;
#63411=CARTESIAN_POINT ( 'NONE',  ( 74.65811388300841145, 19.88603796100278487, -6.000000000000000000 ) ) ;
#63412=CARTESIAN_POINT ( 'NONE',  ( 15.48999599679679662, 146.9999999999999716, -9.500000000000000000 ) ) ;
#63415=CARTESIAN_POINT ( 'NONE',  ( 1.085428990800034299, 110.8977621029158769, 9.078527738363955990 ) ) ;
#63421=FILL_AREA_STYLE ('',( #9271 ) ) ;
#63422=ORIENTED_EDGE ( 'NONE', *, *, #1733, .T. ) ;
#63429=SURFACE_STYLE_FILL_AREA ( #42021 ) ;
#63431=CARTESIAN_POINT ( 'NONE',  ( -10.01517768586949408, 149.1949999999999932, -6.132527647946036459E-16 ) ) ;
#63434=( GEOMETRIC_REPRESENTATION_CONTEXT ( 3 ) GLOBAL_UNCERTAINTY_ASSIGNED_CONTEXT ( ( #36292 ) ) GLOBAL_UNIT_ASSIGNED_CONTEXT ( ( #7679, #52008, #51646 ) ) REPRESENTATION_CONTEXT ( 'NONE', 'WORKASPACE' ) );
#63438=CARTESIAN_POINT ( 'NONE',  ( -48.50000000000000000, 14.49137674618942562, 7.500000000000000000 ) ) ;
#63442=CARTESIAN_POINT ( 'NONE',  ( 3.094860106618435136, 115.2949999999999733, -9.525000000000000355 ) ) ;
#63446=ORIENTED_EDGE ( 'NONE', *, *, #6901, .T. ) ;
#63450=CIRCLE ( 'NONE', #12872, 13.99999999999999822 ) ;
#63452=CIRCLE ( 'NONE', #33278, 0.5000000000000004441 ) ;
#63454=CARTESIAN_POINT ( 'NONE',  ( -20.30121256018846765, 114.9093931177592509, -10.36597400192487939 ) ) ;
#63456=PRESENTATION_STYLE_ASSIGNMENT (( #58518 ) ) ;
#63471=( NAMED_UNIT ( * ) PLANE_ANGLE_UNIT ( ) SI_UNIT ( $, .RADIAN. ) );
#63474=DIRECTION ( 'NONE',  ( 1.000000000000000000, 0.000000000000000000, 0.000000000000000000 ) ) ;
#63475=CARTESIAN_POINT ( 'NONE',  ( 6.826472737025119919, 144.0070736234661126, 4.959722759717908325 ) ) ;
#63476=( NAMED_UNIT ( * ) SI_UNIT ( $, .STERADIAN. ) SOLID_ANGLE_UNIT ( ) );
#63479=CARTESIAN_POINT ( 'NONE',  ( -65.99999999999998579, 50.00000000000000000, 12.00000000000000000 ) ) ;
#63480=EDGE_CURVE ( 'NONE', #40163, #60087, #61216, .T. ) ;
#63484=CARTESIAN_POINT ( 'NONE',  ( 75.00000000000000000, 20.36037961002804764, -6.585786437626907741 ) ) ;
#63485=DIRECTION ( 'NONE',  ( -1.000000000000000000, 0.000000000000000000, 0.000000000000000000 ) ) ;
#63486=( NAMED_UNIT ( * ) SI_UNIT ( $, .STERADIAN. ) SOLID_ANGLE_UNIT ( ) );
#63487=ORIENTED_EDGE ( 'NONE', *, *, #59001, .T. ) ;
#63489=CARTESIAN_POINT ( 'NONE',  ( 72.49999999999998579, 64.07124727947029896, 9.500000000000000000 ) ) ;
#63492=CARTESIAN_POINT ( 'NONE',  ( 70.87837837837835764, 13.70805908423324482, -9.500000000000000000 ) ) ;
#63493=CARTESIAN_POINT ( 'NONE',  ( 0.000000000000000000, 109.9999999999999858, 0.000000000000000000 ) ) ;
#63498=SURFACE_STYLE_FILL_AREA ( #14991 ) ;
#63499=ORIENTED_EDGE ( 'NONE', *, *, #23420, .F. ) ;
#63504=CARTESIAN_POINT ( 'NONE',  ( -41.38256758237925936, 107.6997254016901451, 3.907089461173326672 ) ) ;
#63506=CARTESIAN_POINT ( 'NONE',  ( 9.058813317711338797, 120.8449999999999847, -2.943386871421372675 ) ) ;
#63512=CARTESIAN_POINT ( 'NONE',  ( 23.71231517720798010, 112.9999999999999858, 9.500000000000000000 ) ) ;
#63517=( GEOMETRIC_REPRESENTATION_CONTEXT ( 3 ) GLOBAL_UNCERTAINTY_ASSIGNED_CONTEXT ( ( #63043 ) ) GLOBAL_UNIT_ASSIGNED_CONTEXT ( ( #5685, #22587, #1042 ) ) REPRESENTATION_CONTEXT ( 'NONE', 'WORKASPACE' ) );
#63520=LINE ( 'NONE', #20256, #64885 ) ;
#63521=DIRECTION ( 'NONE',  ( 1.000000000000000000, -0.000000000000000000, -0.000000000000000000 ) ) ;
#63522=UNCERTAINTY_MEASURE_WITH_UNIT (LENGTH_MEASURE( 1.000000000000000082E-05 ), #170, 'distance_accuracy_value', 'NONE');
#63524=B_SPLINE_CURVE_WITH_KNOTS ( 'NONE', 3,
 ( #61787, #13618, #51613, #34718, #40738, #24501, #1955, #55843, #19594, #44981, #41091, #45338 ),
 .UNSPECIFIED., .F., .F.,
 ( 4, 2, 2, 2, 2, 4 ),
 ( 0.000000000000000000, 0.0002999083533514614692, 0.0005998167067029229384, 0.001199633413405845877, 0.001799450120108768815, 0.002399266826811691754 ),
 .UNSPECIFIED. ) ;
#63527=VECTOR ( 'NONE', #67471, 1000.000000000000000 ) ;
#63528=EDGE_CURVE ( 'NONE', #22472, #36852, #65054, .T. ) ;
#63529=CARTESIAN_POINT ( 'NONE',  ( 10.01517768586949231, 154.8050000000000352, 1.839758294383810543E-15 ) ) ;
#63530=( NAMED_UNIT ( * ) PLANE_ANGLE_UNIT ( ) SI_UNIT ( $, .RADIAN. ) );
#63531=CARTESIAN_POINT ( 'NONE',  ( -40.99999999999997868, 9.999999999999978684, 3.500000000000000000 ) ) ;
#63532=CIRCLE ( 'NONE', #10765, 13.49999999999999822 ) ;
#63534=UNCERTAINTY_MEASURE_WITH_UNIT (LENGTH_MEASURE( 1.000000000000000082E-05 ), #53578, 'distance_accuracy_value', 'NONE');
#63537=SURFACE_SIDE_STYLE ('',( #57933 ) ) ;
#63543=EDGE_CURVE ( 'NONE', #49361, #65027, #31991, .T. ) ;
#63546=TOROIDAL_SURFACE ( 'NONE', #28733, 13.49999999999999822, 0.5000000000000000000 ) ;
#63549=STYLED_ITEM ( 'NONE', ( #249 ), #57094 ) ;
#63550=CARTESIAN_POINT ( 'NONE',  ( -9.827790563157511022E-16, 116.5570736234661666, 8.025000000000000355 ) ) ;
#63551=AXIS2_PLACEMENT_3D ( 'NONE', #27165, #53262, #32131 ) ;
#63552=FILL_AREA_STYLE_COLOUR ( '', #19153 ) ;
#63557=ORIENTED_EDGE ( 'NONE', *, *, #5546, .T. ) ;
#63561=CARTESIAN_POINT ( 'NONE',  ( 5.598654528085805993, 121.3549999999999898, 7.705886871421374629 ) ) ;
#63564=DIRECTION ( 'NONE',  ( 0.000000000000000000, 0.000000000000000000, -1.000000000000000000 ) ) ;
#63567=VECTOR ( 'NONE', #38204, 1000.000000000000000 ) ;
#63570=UNCERTAINTY_MEASURE_WITH_UNIT (LENGTH_MEASURE( 1.000000000000000082E-05 ), #29101, 'distance_accuracy_value', 'NONE');
#63571=ORIENTED_EDGE ( 'NONE', *, *, #64673, .F. ) ;
#63572=CARTESIAN_POINT ( 'NONE',  ( -7.632228543268608334, 153.8429263765338249, 2.479861379858952830 ) ) ;
#63574=CARTESIAN_POINT ( 'NONE',  ( 34.99999999999999289, 99.99999999999997158, 4.000000000000000000 ) ) ;
#63577=COLOUR_RGB ( '', 0.66274510, 0.83137255, 0.94901961) ;
#63579=CARTESIAN_POINT ( 'NONE',  ( -45.91547277936962246, 9.430195807687219656, 3.611004237778671744 ) ) ;
#63580=SURFACE_STYLE_FILL_AREA ( #42188 ) ;
#63582=( GEOMETRIC_REPRESENTATION_CONTEXT ( 3 ) GLOBAL_UNCERTAINTY_ASSIGNED_CONTEXT ( ( #57884 ) ) GLOBAL_UNIT_ASSIGNED_CONTEXT ( ( #60377, #24467, #55458 ) ) REPRESENTATION_CONTEXT ( 'NONE', 'WORKASPACE' ) );
#63585=EDGE_CURVE ( 'NONE', #9347, #14945, #493, .T. ) ;
#63586=( NAMED_UNIT ( * ) PLANE_ANGLE_UNIT ( ) SI_UNIT ( $, .RADIAN. ) );
#63590=ORIENTED_EDGE ( 'NONE', *, *, #45312, .F. ) ;
#63592=DIRECTION ( 'NONE',  ( 0.000000000000000000, 0.000000000000000000, 1.000000000000000000 ) ) ;
#63593=CARTESIAN_POINT ( 'NONE',  ( 60.00000000000000000, 1.797044900979284448E-15, 6.500000000000000000 ) ) ;
#63594=PRESENTATION_STYLE_ASSIGNMENT (( #52709 ) ) ;
#63602=CIRCLE ( 'NONE', #38791, 0.5000000000000004441 ) ;
#63609=CARTESIAN_POINT ( 'NONE',  ( 9.452512629751957718, 154.4999999999999432, 1.251363035250141920 ) ) ;
#63611=CARTESIAN_POINT ( 'NONE',  ( -74.61046851513155787, 36.28146479779877609, -9.990989611816710081 ) ) ;
#63614=ADVANCED_FACE ( 'NONE', ( #293 ), #59794, .F. ) ;
#63615=CARTESIAN_POINT ( 'NONE',  ( 8.102448949553181734, 130.5049999999999670, 5.886773742842750679 ) ) ;
#63616=CARTESIAN_POINT ( 'NONE',  ( -71.50000000000000000, 35.92875272052971525, -9.500000000000000000 ) ) ;
#63619=UNCERTAINTY_MEASURE_WITH_UNIT (LENGTH_MEASURE( 1.000000000000000082E-05 ), #57073, 'distance_accuracy_value', 'NONE');
#63623=DIRECTION ( 'NONE',  ( 1.000000000000000000, 0.000000000000000000, 0.000000000000000000 ) ) ;
#63627=CIRCLE ( 'NONE', #60260, 1.000000000000000888 ) ;
#63629=STYLED_ITEM ( 'NONE', ( #16966 ), #50074 ) ;
#63639=ORIENTED_EDGE ( 'NONE', *, *, #39088, .T. ) ;
#63645=SURFACE_STYLE_USAGE ( .BOTH. , #47168 ) ;
#63648=EDGE_CURVE ( 'NONE', #47061, #6428, #55594, .T. ) ;
#63649=DIRECTION ( 'NONE',  ( 1.000000000000000000, 0.000000000000000000, 0.000000000000000000 ) ) ;
#63650=CARTESIAN_POINT ( 'NONE',  ( -5.598654528085806881, 145.7449999999999761, -7.705886871421374629 ) ) ;
#63652=EDGE_LOOP ( 'NONE', ( #37253, #40624, #13699 ) ) ;
#63654=CARTESIAN_POINT ( 'NONE',  ( 5.598654528085809545, 149.2549999999999955, -7.705886871421373741 ) ) ;
#63657=CARTESIAN_POINT ( 'NONE',  ( -8.437984349512095861, 126.6929263765338050, -5.166775262442723748E-16 ) ) ;
#63659=UNCERTAINTY_MEASURE_WITH_UNIT (LENGTH_MEASURE( 1.000000000000000082E-05 ), #52851, 'distance_accuracy_value', 'NONE');
#63660=CARTESIAN_POINT ( 'NONE',  ( -74.50000000000000000, 36.50926243676796190, -10.00000000000000000 ) ) ;
#63661=PRESENTATION_STYLE_ASSIGNMENT (( #31992 ) ) ;
#63662=ORIENTED_EDGE ( 'NONE', *, *, #45609, .T. ) ;
#63666=DIRECTION ( 'NONE',  ( -1.000000000000000000, 0.000000000000000000, 0.000000000000000000 ) ) ;
#63672=SURFACE_STYLE_USAGE ( .BOTH. , #38020 ) ;
#63676=ORIENTED_EDGE ( 'NONE', *, *, #36440, .T. ) ;
#63684=DIRECTION ( 'NONE',  ( -0.000000000000000000, -0.000000000000000000, 1.000000000000000000 ) ) ;
#63686=CARTESIAN_POINT ( 'NONE',  ( -75.48275862068965125, 36.00832590023089352, -41.30495168499704306 ) ) ;
#63687=ORIENTED_EDGE ( 'NONE', *, *, #14663, .T. ) ;
#63688=EDGE_CURVE ( 'NONE', #15520, #24259, #60464, .T. ) ;
#63689=PRESENTATION_STYLE_ASSIGNMENT (( #10583 ) ) ;
#63693=TOROIDAL_SURFACE ( 'NONE', #68223, 14.49999999999999822, 0.5000000000000000000 ) ;
#63696=CARTESIAN_POINT ( 'NONE',  ( 8.102448949553181734, 150.3949999999999818, 5.886773742842750679 ) ) ;
#63700=UNCERTAINTY_MEASURE_WITH_UNIT (LENGTH_MEASURE( 1.000000000000000082E-05 ), #58831, 'distance_accuracy_value', 'NONE');
#63707=( LENGTH_UNIT ( ) NAMED_UNIT ( * ) SI_UNIT ( .MILLI., .METRE. ) );
#63708=ORIENTED_EDGE ( 'NONE', *, *, #7716, .T. ) ;
#63709=ORIENTED_EDGE ( 'NONE', *, *, #68633, .F. ) ;
#63711=CARTESIAN_POINT ( 'NONE',  ( -6.826472737025120807, 117.9929263765338021, 4.959722759717906548 ) ) ;
#63712=CARTESIAN_POINT ( 'NONE',  ( -45.00000000000033396, 8.701466902705615070, 5.869459488307998463 ) ) ;
#63713=PLANE ( 'NONE',  #22956 ) ;
#63717=AXIS2_PLACEMENT_3D ( 'NONE', #8817, #63666, #52455 ) ;
#63719=PRESENTATION_STYLE_ASSIGNMENT (( #336 ) ) ;
#63722=EDGE_CURVE ( 'NONE', #7643, #68674, #65769, .T. ) ;
#63723=LINE ( 'NONE', #55241, #38842 ) ;
#63724=CARTESIAN_POINT ( 'NONE',  ( -3.094860106618432471, 121.5949999999999847, -9.525000000000000355 ) ) ;
#63726=FACE_OUTER_BOUND ( 'NONE', #33689, .T. ) ;
#63727=CARTESIAN_POINT ( 'NONE',  ( -9.058813317711338797, 123.4549999999999841, 2.943386871421373563 ) ) ;
#63729=FACE_OUTER_BOUND ( 'NONE', #63279, .T. ) ;
#63731=CARTESIAN_POINT ( 'NONE',  ( 5.598654528085805993, 151.3549999999999898, 7.705886871421374629 ) ) ;
#63737=DIRECTION ( 'NONE',  ( -0.000000000000000000, -0.000000000000000000, 1.000000000000000000 ) ) ;
#63738=ORIENTED_EDGE ( 'NONE', *, *, #53993, .T. ) ;
#63743=ORIENTED_EDGE ( 'NONE', *, *, #49727, .T. ) ;
#63744=CARTESIAN_POINT ( 'NONE',  ( 4.134715136431655225, 111.0353213183942529, 8.000580966448456621 ) ) ;
#63746=FILL_AREA_STYLE_COLOUR ( '', #1467 ) ;
#63753=ORIENTED_EDGE ( 'NONE', *, *, #10742, .T. ) ;
#63755=ADVANCED_FACE ( 'NONE', ( #17604 ), #18627, .T. ) ;
#63756=( LENGTH_UNIT ( ) NAMED_UNIT ( * ) SI_UNIT ( .MILLI., .METRE. ) );
#63758=( BOUNDED_SURFACE ( )  B_SPLINE_SURFACE ( 3, 2, ( 
 ( #21045, #59029, #47852 ),
 ( #15791, #4863, #4141 ),
 ( #31589, #42544, #63611 ),
 ( #5528, #30897, #63943 ),
 ( #42221, #64296, #31231 ),
 ( #37275, #53419, #31941 ),
 ( #25611, #58673, #68909 ),
 ( #36590, #48513, #10503 ),
 ( #10156, #210, #32283 ),
 ( #26641, #48166, #10841 ),
 ( #21739, #15454, #43251 ),
 ( #69574, #21380, #42903 ) ),
 .UNSPECIFIED., .F., .F., .F. ) 
 B_SPLINE_SURFACE_WITH_KNOTS ( ( 4, 2, 2, 2, 2, 4 ),
 ( 3, 3 ),
 ( -6.326733460093544372E-06, 0.0004675000763919686308, 0.0009413268862440307781, 0.001415153696096092817, 0.001652067101022123945, 0.001888980505948155073 ),
 ( 0.000000000000000000, 1.000000000000000000 ),
 .UNSPECIFIED. ) 
 GEOMETRIC_REPRESENTATION_ITEM ( )  RATIONAL_B_SPLINE_SURFACE ( (
 ( 1.000000000000000000, 1.000000000000000000, 1.000000000000000000),
 ( 1.000000000000000000, 0.9999603998840329577, 1.000000000000000000),
 ( 1.000000000000000000, 0.9905097737965633531, 1.000000000000000000),
 ( 1.000000000000000000, 0.9539269352976011973, 1.000000000000000000),
 ( 1.000000000000000000, 0.9259356461951893102, 1.000000000000000000),
 ( 1.000000000000000000, 0.8584222786211590517, 1.000000000000000000),
 ( 1.000000000000000000, 0.8173629853940447276, 1.000000000000000000),
 ( 1.000000000000000000, 0.7644081322687370506, 1.000000000000000000),
 ( 1.000000000000000000, 0.7482903728718443004, 1.000000000000000000),
 ( 1.000000000000000000, 0.7257247660741658057, 1.000000000000000000),
 ( 1.000000000000000000, 0.7190551827508514515, 1.000000000000000000),
 ( 1.000000000000000000, 0.7191949522280786100, 1.000000000000000000) ) ) 
 REPRESENTATION_ITEM ( '' )  SURFACE ( )  );
#63759=DIRECTION ( 'NONE',  ( 0.000000000000000000, 0.000000000000000000, 1.000000000000000000 ) ) ;
#63760=CARTESIAN_POINT ( 'NONE',  ( -5.598654528085806881, 151.7450000000000045, -7.705886871421374629 ) ) ;
#63762=AXIS2_PLACEMENT_3D ( 'NONE', #3701, #62810, #56503 ) ;
#63765=DIRECTION ( 'NONE',  ( 0.000000000000000000, 0.000000000000000000, 1.000000000000000000 ) ) ;
#63767=VECTOR ( 'NONE', #58556, 1000.000000000000000 ) ;
#63769=SURFACE_SIDE_STYLE ('',( #69409 ) ) ;
#63772=EDGE_CURVE ( 'NONE', #31646, #8395, #37675, .T. ) ;
#63773=CARTESIAN_POINT ( 'NONE',  ( -9.058813317711337021, 119.0449999999999875, -2.943386871421374895 ) ) ;
#63780=EDGE_CURVE ( 'NONE', #849, #26112, #51322, .T. ) ;
#63787=CARTESIAN_POINT ( 'NONE',  ( -2.607480562269116842, 149.4070736234661751, 8.024999999999970157 ) ) ;
#63788=CARTESIAN_POINT ( 'NONE',  ( -20.77895614775982125, 115.1380991538496801, -10.00000000000000000 ) ) ;
#63790=ORIENTED_EDGE ( 'NONE', *, *, #33058, .F. ) ;
#63795=CARTESIAN_POINT ( 'NONE',  ( 7.632228543268607446, 147.1570736234661751, 2.479861379858954606 ) ) ;
#63802=CYLINDRICAL_SURFACE ( 'NONE', #49892, 8.025000000000000355 ) ;
#63803=( NAMED_UNIT ( * ) PLANE_ANGLE_UNIT ( ) SI_UNIT ( $, .RADIAN. ) );
#63804=CARTESIAN_POINT ( 'NONE',  ( -2.607480562269073765, 142.2070736234661297, -8.025000000000000355 ) ) ;
#63805=EDGE_LOOP ( 'NONE', ( #60167, #23922, #46658, #35088 ) ) ;
#63806=DIRECTION ( 'NONE',  ( -0.000000000000000000, -0.000000000000000000, -1.000000000000000000 ) ) ;
#63809=CARTESIAN_POINT ( 'NONE',  ( 2.607480562269113733, 131.7070736234662149, 8.024999999999973710 ) ) ;
#63813=DIRECTION ( 'NONE',  ( 0.000000000000000000, 0.000000000000000000, 1.000000000000000000 ) ) ;
#63814=LINE ( 'NONE', #54298, #29910 ) ;
#63816=ORIENTED_EDGE ( 'NONE', *, *, #67769, .F. ) ;
#63817=COLOUR_RGB ( '', 0.08235294, 0.09019608, 0.10196078) ;
#63821=DIRECTION ( 'NONE',  ( -0.7833176619561783571, 0.6216216216216310375, -0.000000000000000000 ) ) ;
#63825=FACE_OUTER_BOUND ( 'NONE', #55858, .T. ) ;
#63826=VECTOR ( 'NONE', #29957, 1000.000000000000000 ) ;
#63827=DIRECTION ( 'NONE',  ( 1.000000000000000000, 0.000000000000000000, 0.000000000000000000 ) ) ;
#63831=VERTEX_POINT ( 'NONE', #25603 ) ;
#63832=FILL_AREA_STYLE ('',( #42441 ) ) ;
#63833=SURFACE_STYLE_USAGE ( .BOTH. , #17074 ) ;
#63835=CARTESIAN_POINT ( 'NONE',  ( -3.094860106618432471, 121.5949999999999847, -9.525000000000000355 ) ) ;
#63836=EDGE_CURVE ( 'NONE', #11552, #4457, #2727, .T. ) ;
#63842=CARTESIAN_POINT ( 'NONE',  ( -15.48999599679679662, 117.9999999999999716, 7.500000000000000000 ) ) ;
#63847=EDGE_CURVE ( 'NONE', #11851, #7249, #46664, .T. ) ;
#63852=( GEOMETRIC_REPRESENTATION_CONTEXT ( 3 ) GLOBAL_UNCERTAINTY_ASSIGNED_CONTEXT ( ( #57358 ) ) GLOBAL_UNIT_ASSIGNED_CONTEXT ( ( #58122, #21503, #43021 ) ) REPRESENTATION_CONTEXT ( 'NONE', 'WORKASPACE' ) );
#63854=EDGE_CURVE ( 'NONE', #38669, #3572, #59435, .T. ) ;
#63855=ORIENTED_EDGE ( 'NONE', *, *, #49187, .T. ) ;
#63856=( BOUNDED_CURVE ( )  B_SPLINE_CURVE ( 2, ( #10609, #25390, #53183, #69013, #26074, #53517, #47954, #63711, #68315, #20094, #58445 ),
 .UNSPECIFIED., .F., .F. ) 
 B_SPLINE_CURVE_WITH_KNOTS ( ( 3, 2, 2, 2, 2, 3 ),
 ( 0.1176470588235295212, 0.1235294117647059986, 0.1294117647058824760, 0.1352941176470589257, 0.1411764705882354032, 0.1470588235294118806 ),
 .UNSPECIFIED. ) 
 CURVE ( )  GEOMETRIC_REPRESENTATION_ITEM ( )  RATIONAL_B_SPLINE_CURVE ( ( 0.9999999999999991118, 0.9510565162951544194, 1.000000000000000000, 0.9510565162951535312, 1.000000000000000000, 0.9510565162951535312, 1.000000000000000000, 0.9510565162951535312, 1.000000000000000000, 0.9510565162951526430, 1.000000000000000888 ) ) 
 REPRESENTATION_ITEM ( '' )  );
#63859=ADVANCED_FACE ( 'NONE', ( #48421 ), #51671, .F. ) ;
#63860=CYLINDRICAL_SURFACE ( 'NONE', #53007, 13.99999999999999822 ) ;
#63862=CARTESIAN_POINT ( 'NONE',  ( 34.99999999999992895, 110.4999999999999858, -9.500000000000000000 ) ) ;
#63863=COLOUR_RGB ( '', 0.72549020, 0.75294118, 0.79215686) ;
#63867=AXIS2_PLACEMENT_3D ( 'NONE', #20604, #30432, #20246 ) ;
#63869=AXIS2_PLACEMENT_3D ( 'NONE', #10122, #26274, #60020 ) ;
#63871=STYLED_ITEM ( 'NONE', ( #37703 ), #68068 ) ;
#63877=CARTESIAN_POINT ( 'NONE',  ( 2.607480562269076430, 117.9070736234661467, -8.025000000000000355 ) ) ;
#63879=AXIS2_PLACEMENT_3D ( 'NONE', #11170, #21039, #52720 ) ;
#63880=CARTESIAN_POINT ( 'NONE',  ( -20.26251832593580104, 115.0246525964671207, 10.00000000000000178 ) ) ;
#63882=ORIENTED_EDGE ( 'NONE', *, *, #63967, .T. ) ;
#63883=TOROIDAL_SURFACE ( 'NONE', #16776, 8.499999999999998224, 0.5000000000000000000 ) ;
#63884=ORIENTED_EDGE ( 'NONE', *, *, #14553, .T. ) ;
#63887=VERTEX_POINT ( 'NONE', #55017 ) ;
#63888=CARTESIAN_POINT ( 'NONE',  ( -10.01517768586949231, 123.3049999999999926, -6.132527647946036459E-16 ) ) ;
#63889=CARTESIAN_POINT ( 'NONE',  ( -15.48999599679679662, 117.9999999999999716, 7.000000000000000000 ) ) ;
#63891=AXIS2_PLACEMENT_3D ( 'NONE', #28046, #49553, #6973 ) ;
#63894=ORIENTED_EDGE ( 'NONE', *, *, #57762, .T. ) ;
#63896=DIRECTION ( 'NONE',  ( 0.000000000000000000, 0.000000000000000000, 1.000000000000000000 ) ) ;
#63899=CARTESIAN_POINT ( 'NONE',  ( 4.716976649647096842, 154.7429263765338021, 6.492361379858953896 ) ) ;
#63900=FILL_AREA_STYLE ('',( #42504 ) ) ;
#63902=MECHANICAL_DESIGN_GEOMETRIC_PRESENTATION_REPRESENTATION('',(#24582),#907);
#63909=CARTESIAN_POINT ( 'NONE',  ( 23.21231517720798010, 113.4999999999999858, -10.00000000000000000 ) ) ;
#63918=CARTESIAN_POINT ( 'NONE',  ( -4.716976649647098618, 121.1429263765338220, 6.492361379858953008 ) ) ;
#63925=DIRECTION ( 'NONE',  ( 0.000000000000000000, 0.000000000000000000, 1.000000000000000000 ) ) ;
#63926=SURFACE_SIDE_STYLE ('',( #49509 ) ) ;
#63936=MECHANICAL_DESIGN_GEOMETRIC_PRESENTATION_REPRESENTATION('',(#52774),#5521);
#63938=ADVANCED_FACE ( 'NONE', ( #50129 ), #56764, .T. ) ;
#63943=CARTESIAN_POINT ( 'NONE',  ( -74.71853681387480606, 36.06263896201981112, -9.953338452735643216 ) ) ;
#63944=MECHANICAL_DESIGN_GEOMETRIC_PRESENTATION_REPRESENTATION('',(#50501),#59460);
#63946=CARTESIAN_POINT ( 'NONE',  ( 0.000000000000000000, 128.5549999999999784, -9.525000000000000355 ) ) ;
#63947=CARTESIAN_POINT ( 'NONE',  ( 20.20529291564252716, 114.9650358309326492, -10.39743153126989128 ) ) ;
#63949=( GEOMETRIC_REPRESENTATION_CONTEXT ( 3 ) GLOBAL_UNCERTAINTY_ASSIGNED_CONTEXT ( ( #60888 ) ) GLOBAL_UNIT_ASSIGNED_CONTEXT ( ( #23417, #39636, #62087 ) ) REPRESENTATION_CONTEXT ( 'NONE', 'WORKASPACE' ) );
#63953=VECTOR ( 'NONE', #38888, 1000.000000000000000 ) ;
#63954=FILL_AREA_STYLE_COLOUR ( '', #64072 ) ;
#63956=EDGE_LOOP ( 'NONE', ( #54865, #13014, #27725, #62538 ) ) ;
#63962=DIRECTION ( 'NONE',  ( 1.000000000000000000, 0.000000000000000000, 0.000000000000000000 ) ) ;
#63965=CARTESIAN_POINT ( 'NONE',  ( -45.86897471612435595, 9.253287829606158255, -6.241231906388602368 ) ) ;
#63966=CARTESIAN_POINT ( 'NONE',  ( 2.607480562269093305, 130.5929263765337964, 8.024999999999986144 ) ) ;
#63967=EDGE_CURVE ( 'NONE', #29123, #29357, #18785, .T. ) ;
#63970=SURFACE_SIDE_STYLE ('',( #25639 ) ) ;
#63971=CARTESIAN_POINT ( 'NONE',  ( 60.00000000000000000, 1.797044900979284448E-15, 11.50000000000000000 ) ) ;
#63972=ORIENTED_EDGE ( 'NONE', *, *, #67492, .T. ) ;
#63974=EDGE_LOOP ( 'NONE', ( #35441, #36387, #26543 ) ) ;
#63976=CARTESIAN_POINT ( 'NONE',  ( 20.86757785789463071, 115.0275815560950718, -10.00000000000000000 ) ) ;
#63978=DIRECTION ( 'NONE',  ( -1.156482317317866302E-16, -1.000000000000000000, -2.430666987508116652E-16 ) ) ;
#63980=VERTEX_POINT ( 'NONE', #28970 ) ;
#63983=( NAMED_UNIT ( * ) PLANE_ANGLE_UNIT ( ) SI_UNIT ( $, .RADIAN. ) );
#63984=CARTESIAN_POINT ( 'NONE',  ( -3.094860106618432471, 154.5949999999999704, -9.525000000000000355 ) ) ;
#63988=CARTESIAN_POINT ( 'NONE',  ( 9.058813317711338797, 145.9550000000000125, -2.943386871421372675 ) ) ;
#63989=FILL_AREA_STYLE_COLOUR ( '', #49672 ) ;
#63992=ORIENTED_EDGE ( 'NONE', *, *, #64809, .T. ) ;
#63993=CARTESIAN_POINT ( 'NONE',  ( 0.000000000000000000, 122.9429263765338192, -8.025000000000000355 ) ) ;
#63995=CARTESIAN_POINT ( 'NONE',  ( -75.25488889474493703, 36.12129367854308981, -9.832813668515733241 ) ) ;
#63996=ADVANCED_FACE ( 'NONE', ( #51858 ), #69416, .T. ) ;
#63997=DIRECTION ( 'NONE',  ( 1.000000000000000000, 0.000000000000000000, 0.000000000000000000 ) ) ;
#63998=DIRECTION ( 'NONE',  ( -0.000000000000000000, -0.000000000000000000, 1.000000000000000000 ) ) ;
#64001=MECHANICAL_DESIGN_GEOMETRIC_PRESENTATION_REPRESENTATION('',(#11230),#44965);
#64002=CARTESIAN_POINT ( 'NONE',  ( -41.84210526315788314, 107.2928455055531600, -4.000000000000000000 ) ) ;
#64003=ORIENTED_EDGE ( 'NONE', *, *, #32174, .T. ) ;
#64005=COLOUR_RGB ( '', 0.72549020, 0.75294118, 0.79215686) ;
#64012=AXIS2_PLACEMENT_3D ( 'NONE', #46604, #8230, #40960 ) ;
#64013=SURFACE_STYLE_FILL_AREA ( #26380 ) ;
#64014=SURFACE_STYLE_FILL_AREA ( #23109 ) ;
#64016=ORIENTED_EDGE ( 'NONE', *, *, #28088, .T. ) ;
#64017=EDGE_CURVE ( 'NONE', #66508, #67023, #17465, .T. ) ;
#64024=( LENGTH_UNIT ( ) NAMED_UNIT ( * ) SI_UNIT ( .MILLI., .METRE. ) );
#64025=ADVANCED_FACE ( 'NONE', ( #38222 ), #64211, .F. ) ;
#64027=( LENGTH_UNIT ( ) NAMED_UNIT ( * ) SI_UNIT ( .MILLI., .METRE. ) );
#64029=EDGE_LOOP ( 'NONE', ( #23481, #31974, #44219, #14702 ) ) ;
#64034=COLOUR_RGB ( '', 0.09019608, 0.27058824, 0.51372549) ;
#64035=CARTESIAN_POINT ( 'NONE',  ( 6.826472737025119919, 126.0070736234661695, 4.959722759717908325 ) ) ;
#64037=CARTESIAN_POINT ( 'NONE',  ( -3.094860106618434248, 152.7949999999999591, 9.525000000000000355 ) ) ;
#64039=( NAMED_UNIT ( * ) SI_UNIT ( $, .STERADIAN. ) SOLID_ANGLE_UNIT ( ) );
#64040=SURFACE_SIDE_STYLE ('',( #48953 ) ) ;
#64042=CARTESIAN_POINT ( 'NONE',  ( 15.48999599679679662, 147.4999999999999716, -10.00000000000000000 ) ) ;
#64050=STYLED_ITEM ( 'NONE', ( #636 ), #11205 ) ;
#64057=CARTESIAN_POINT ( 'NONE',  ( -45.00000000000000000, 9.118333594695746669, 6.737587966311194165 ) ) ;
#64065=CARTESIAN_POINT ( 'NONE',  ( 45.00000000000000000, -1.469576158976824618E-14, 9.500000000000000000 ) ) ;
#64067=VECTOR ( 'NONE', #33080, 1000.000000000000000 ) ;
#64070=CARTESIAN_POINT ( 'NONE',  ( -8.102448949553181734, 116.4949999999999761, 5.886773742842747126 ) ) ;
#64071=( LENGTH_UNIT ( ) NAMED_UNIT ( * ) SI_UNIT ( .MILLI., .METRE. ) );
#64072=COLOUR_RGB ( '', 0.08235294, 0.09019608, 0.10196078) ;
#64076=CARTESIAN_POINT ( 'NONE',  ( -5.598654528085808657, 123.7549999999999955, 7.705886871421373741 ) ) ;
#64079=DIRECTION ( 'NONE',  ( -1.156482317317873451E-16, -1.000000000000000000, 0.000000000000000000 ) ) ;
#64081=CARTESIAN_POINT ( 'NONE',  ( 9.058813317711337021, 151.6549999999999727, 2.943386871421375783 ) ) ;
#64083=ADVANCED_FACE ( 'NONE', ( #5806 ), #11442, .F. ) ;
#64084=DIRECTION ( 'NONE',  ( 0.000000000000000000, 0.000000000000000000, -1.000000000000000000 ) ) ;
#64085=EDGE_CURVE ( 'NONE', #1577, #69035, #60107, .T. ) ;
#64090=DIRECTION ( 'NONE',  ( -0.000000000000000000, -0.000000000000000000, -1.000000000000000000 ) ) ;
#64091=FACE_OUTER_BOUND ( 'NONE', #50366, .T. ) ;
#64098=CARTESIAN_POINT ( 'NONE',  ( 15.98999599679679839, 118.4999999999999716, 7.500000000000000000 ) ) ;
#64099=FILL_AREA_STYLE_COLOUR ( '', #45594 ) ;
#64101=EDGE_LOOP ( 'NONE', ( #40751, #10950, #24522, #24596 ) ) ;
#64102=EDGE_CURVE ( 'NONE', #42981, #11929, #46544, .T. ) ;
#64105=ORIENTED_EDGE ( 'NONE', *, *, #53677, .T. ) ;
#64106=CIRCLE ( 'NONE', #61815, 0.5000000000000004441 ) ;
#64107=DIRECTION ( 'NONE',  ( -0.000000000000000000, -0.000000000000000000, -1.000000000000000000 ) ) ;
#64109=MECHANICAL_DESIGN_GEOMETRIC_PRESENTATION_REPRESENTATION('',(#59628),#30387);
#64110=( LENGTH_UNIT ( ) NAMED_UNIT ( * ) SI_UNIT ( .MILLI., .METRE. ) );
#64113=MECHANICAL_DESIGN_GEOMETRIC_PRESENTATION_REPRESENTATION('',(#7975),#55107);
#64115=EDGE_LOOP ( 'NONE', ( #52802, #55514, #38549, #12353 ) ) ;
#64121=EDGE_CURVE ( 'NONE', #67711, #15394, #67602, .T. ) ;
#64122=CARTESIAN_POINT ( 'NONE',  ( 0.000000000000000000, 121.4449999999999790, -9.525000000000000355 ) ) ;
#64125=ADVANCED_FACE ( 'NONE', ( #17780 ), #13008, .F. ) ;
#64134=CARTESIAN_POINT ( 'NONE',  ( -6.826472737025120807, 149.1070736234661354, 4.959722759717906548 ) ) ;
#64136=FACE_OUTER_BOUND ( 'NONE', #17581, .T. ) ;
#64139=CARTESIAN_POINT ( 'NONE',  ( -45.91547277936962956, 9.430195807687216103, 6.000000000000000888 ) ) ;
#64140=CARTESIAN_POINT ( 'NONE',  ( 4.716976649647099507, 152.6429263765338078, -6.492361379858953008 ) ) ;
#64141=( BOUNDED_SURFACE ( )  B_SPLINE_SURFACE ( 3, 2, ( 
 ( #49799, #44895, #7230 ),
 ( #28659, #66303, #66666 ),
 ( #23742, #60331, #50156 ),
 ( #2931, #61367, #12135 ),
 ( #7909, #61022, #29720 ),
 ( #12840, #13526, #34305 ),
 ( #55761, #24421, #29353 ),
 ( #23068, #7567, #33603 ) ),
 .UNSPECIFIED., .F., .F., .F. ) 
 B_SPLINE_SURFACE_WITH_KNOTS ( ( 4, 2, 2, 4 ),
 ( 3, 3 ),
 ( 0.0006464147718099833234, 0.001546301970866990460, 0.001996245570395494082, 0.002446189169923997705 ),
 ( 0.000000000000000000, 1.000000000000000000 ),
 .UNSPECIFIED. ) 
 GEOMETRIC_REPRESENTATION_ITEM ( )  RATIONAL_B_SPLINE_SURFACE ( (
 ( 1.000000000000000000, 0.7071067811865475727, 1.000000000000000000),
 ( 1.000000000000000000, 0.7604340084995849791, 1.000000000000000000),
 ( 1.000000000000000000, 0.8048286378025968357, 1.000000000000000000),
 ( 1.000000000000000000, 0.8534265415373917252, 1.000000000000000000),
 ( 1.000000000000000000, 0.8663147087826937875, 1.000000000000000000),
 ( 1.000000000000000000, 0.8838688826995332315, 1.000000000000000000),
 ( 1.000000000000000000, 0.8885266032449491425, 1.000000000000000000),
 ( 1.000000000000000000, 0.8885233166386380388, 1.000000000000000000) ) ) 
 REPRESENTATION_ITEM ( '' )  SURFACE ( )  );
#64145=B_SPLINE_CURVE_WITH_KNOTS ( 'NONE', 3,
 ( #46221, #26099, #35640, #63047, #13827, #14889, #25754, #47633, #67641, #57075 ),
 .UNSPECIFIED., .F., .F.,
 ( 4, 2, 2, 2, 4 ),
 ( 0.000000000000000000, 0.0002942714429691386125, 0.0005885428859382772250, 0.0008828143289074158375, 0.001177085771876554450 ),
 .UNSPECIFIED. ) ;
#64149=MECHANICAL_DESIGN_GEOMETRIC_PRESENTATION_REPRESENTATION('',(#13582),#3446);
#64150=FILL_AREA_STYLE_COLOUR ( '', #58926 ) ;
#64153=CARTESIAN_POINT ( 'NONE',  ( 6.826472737025121695, 138.6070736234661638, -4.959722759717905660 ) ) ;
#64154=ORIENTED_EDGE ( 'NONE', *, *, #61589, .F. ) ;
#64158=AXIS2_PLACEMENT_3D ( 'NONE', #14859, #37389, #57766 ) ;
#64160=VERTEX_POINT ( 'NONE', #1528 ) ;
#64161=( LENGTH_UNIT ( ) NAMED_UNIT ( * ) SI_UNIT ( .MILLI., .METRE. ) );
#64163=( NAMED_UNIT ( * ) PLANE_ANGLE_UNIT ( ) SI_UNIT ( $, .RADIAN. ) );
#64165=SURFACE_STYLE_FILL_AREA ( #51989 ) ;
#64167=FILL_AREA_STYLE ('',( #30768 ) ) ;
#64171=TOROIDAL_SURFACE ( 'NONE', #23752, 18.50000000000000355, 0.5000000000000000000 ) ;
#64179=PLANE ( 'NONE',  #11164 ) ;
#64181=VERTEX_POINT ( 'NONE', #1872 ) ;
#64182=PRESENTATION_STYLE_ASSIGNMENT (( #62784 ) ) ;
#64183=ORIENTED_EDGE ( 'NONE', *, *, #46144, .F. ) ;
#64185=( NAMED_UNIT ( * ) PLANE_ANGLE_UNIT ( ) SI_UNIT ( $, .RADIAN. ) );
#64188=CARTESIAN_POINT ( 'NONE',  ( -10.01517768586949408, 125.1950000000000074, -6.132527647946036459E-16 ) ) ;
#64192=ORIENTED_EDGE ( 'NONE', *, *, #16638, .T. ) ;
#64195=VECTOR ( 'NONE', #40257, 1000.000000000000000 ) ;
#64196=DIRECTION ( 'NONE',  ( 0.000000000000000000, -1.000000000000000000, 0.000000000000000000 ) ) ;
#64201=STYLED_ITEM ( 'NONE', ( #22809 ), #22077 ) ;
#64204=STYLED_ITEM ( 'NONE', ( #44328 ), #35438 ) ;
#64205=EDGE_LOOP ( 'NONE', ( #66125, #53140 ) ) ;
#64206=CARTESIAN_POINT ( 'NONE',  ( 45.61109309484434249, 10.20369769828143092, -3.650011426053815011 ) ) ;
#64207=DIRECTION ( 'NONE',  ( -0.000000000000000000, -0.000000000000000000, -1.000000000000000000 ) ) ;
#64208=UNCERTAINTY_MEASURE_WITH_UNIT (LENGTH_MEASURE( 1.000000000000000082E-05 ), #68007, 'distance_accuracy_value', 'NONE');
#64210=STYLED_ITEM ( 'NONE', ( #56926 ), #28413 ) ;
#64211=CYLINDRICAL_SURFACE ( 'NONE', #41066, 8.025000000000000355 ) ;
#64212=SURFACE_STYLE_USAGE ( .BOTH. , #4780 ) ;
#64213=FACE_OUTER_BOUND ( 'NONE', #3295, .T. ) ;
#64215=CARTESIAN_POINT ( 'NONE',  ( 74.50000000000000000, -2.220952357103124925E-14, -6.999999999999999112 ) ) ;
#64219=AXIS2_PLACEMENT_3D ( 'NONE', #31655, #16557, #42961 ) ;
#64222=MECHANICAL_DESIGN_GEOMETRIC_PRESENTATION_REPRESENTATION('',(#19270),#14849);
#64228=CARTESIAN_POINT ( 'NONE',  ( -4.716976649647097730, 112.3570736234661496, -6.492361379858953896 ) ) ;
#64229=CIRCLE ( 'NONE', #24918, 0.5000000000000004441 ) ;
#64231=CARTESIAN_POINT ( 'NONE',  ( -19.89974874213240241, 114.9999999999999574, 10.49999999999999822 ) ) ;
#64232=CYLINDRICAL_SURFACE ( 'NONE', #66522, 0.5000000000000004441 ) ;
#64233=AXIS2_PLACEMENT_3D ( 'NONE', #21692, #6204, #7254 ) ;
#64234=ADVANCED_FACE ( 'NONE', ( #27935 ), #55695, .T. ) ;
#64235=VERTEX_POINT ( 'NONE', #39607 ) ;
#64241=ORIENTED_EDGE ( 'NONE', *, *, #5007, .T. ) ;
#64242=CARTESIAN_POINT ( 'NONE',  ( 9.058813317711338797, 118.9549999999999983, -2.943386871421372675 ) ) ;
#64243=FACE_OUTER_BOUND ( 'NONE', #30839, .T. ) ;
#64244=CYLINDRICAL_SURFACE ( 'NONE', #50211, 0.5000000000000004441 ) ;
#64245=STYLED_ITEM ( 'NONE', ( #41983 ), #22481 ) ;
#64247=EDGE_CURVE ( 'NONE', #37997, #67791, #49013, .T. ) ;
#64249=ORIENTED_EDGE ( 'NONE', *, *, #10517, .F. ) ;
#64251=CARTESIAN_POINT ( 'NONE',  ( 71.62068965517238439, 63.58603185604027885, 9.500000000000000000 ) ) ;
#64255=CARTESIAN_POINT ( 'NONE',  ( -2.607480562269075097, 151.2929263765338135, 8.025000000000000355 ) ) ;
#64257=AXIS2_PLACEMENT_3D ( 'NONE', #62386, #31746, #63759 ) ;
#64260=CARTESIAN_POINT ( 'NONE',  ( 20.42980746818723503, 114.8194254430358399, -10.32394991351191571 ) ) ;
#64263=DIRECTION ( 'NONE',  ( 0.3162277660168358873, -0.9486832980505145452, 0.000000000000000000 ) ) ;
#64264=FILL_AREA_STYLE ('',( #54733 ) ) ;
#64265=SURFACE_STYLE_FILL_AREA ( #14713 ) ;
#64272=CARTESIAN_POINT ( 'NONE',  ( -2.607480562269116842, 121.2929263765337993, 8.024999999999970157 ) ) ;
#64273=LINE ( 'NONE', #49503, #31305 ) ;
#64290=AXIS2_PLACEMENT_3D ( 'NONE', #613, #28059, #21798 ) ;
#64296=CARTESIAN_POINT ( 'NONE',  ( -74.89071377870236290, 36.10880737351290293, -9.849303885975091433 ) ) ;
#64298=CARTESIAN_POINT ( 'NONE',  ( 8.102448949553183510, 137.1049999999999898, -5.886773742842746238 ) ) ;
#64302=AXIS2_PLACEMENT_3D ( 'NONE', #3573, #19081, #29296 ) ;
#64304=UNCERTAINTY_MEASURE_WITH_UNIT (LENGTH_MEASURE( 1.000000000000000082E-05 ), #68400, 'distance_accuracy_value', 'NONE');
#64305=SURFACE_SIDE_STYLE ('',( #21391 ) ) ;
#64306=VERTEX_POINT ( 'NONE', #26411 ) ;
#64308=CARTESIAN_POINT ( 'NONE',  ( -55.00000000000000000, -1.962809905030629631E-14, 6.999999999999995559 ) ) ;
#64310=FILL_AREA_STYLE_COLOUR ( '', #31678 ) ;
#64311=DIRECTION ( 'NONE',  ( -0.000000000000000000, -0.000000000000000000, -1.000000000000000000 ) ) ;
#64313=CARTESIAN_POINT ( 'NONE',  ( -71.50000000000000000, 14.49137674618942562, 7.500000000000000000 ) ) ;
#64316=EDGE_LOOP ( 'NONE', ( #12966, #18699, #57168, #6359 ) ) ;
#64317=DIRECTION ( 'NONE',  ( -0.7071067811865543451, 0.000000000000000000, -0.7071067811865408004 ) ) ;
#64320=MECHANICAL_DESIGN_GEOMETRIC_PRESENTATION_REPRESENTATION('',(#9316),#32913);
#64323=( GEOMETRIC_REPRESENTATION_CONTEXT ( 3 ) GLOBAL_UNCERTAINTY_ASSIGNED_CONTEXT ( ( #18059 ) ) GLOBAL_UNIT_ASSIGNED_CONTEXT ( ( #40868, #46504, #14810 ) ) REPRESENTATION_CONTEXT ( 'NONE', 'WORKASPACE' ) );
#64325=CARTESIAN_POINT ( 'NONE',  ( -9.827790563157511022E-16, 139.4429263765338192, 8.025000000000000355 ) ) ;
#64330=CARTESIAN_POINT ( 'NONE',  ( 20.56536453975222756, 115.3173173917729173, -10.00000000000000000 ) ) ;
#64333=DIRECTION ( 'NONE',  ( 1.000000000000000000, 0.000000000000000000, 0.000000000000000000 ) ) ;
#64337=( GEOMETRIC_REPRESENTATION_CONTEXT ( 3 ) GLOBAL_UNCERTAINTY_ASSIGNED_CONTEXT ( ( #1619 ) ) GLOBAL_UNIT_ASSIGNED_CONTEXT ( ( #22366, #140, #37568 ) ) REPRESENTATION_CONTEXT ( 'NONE', 'WORKASPACE' ) );
#64339=CARTESIAN_POINT ( 'NONE',  ( 5.598654528085805993, 147.2449999999999761, 7.705886871421374629 ) ) ;
#64345=SURFACE_STYLE_FILL_AREA ( #68597 ) ;
#64349=CARTESIAN_POINT ( 'NONE',  ( 2.607480562269071989, 130.5929263765337964, 8.025000000000002132 ) ) ;
#64352=CARTESIAN_POINT ( 'NONE',  ( 6.826472737025121695, 125.4929263765338021, -4.959722759717905660 ) ) ;
#64354=AXIS2_PLACEMENT_3D ( 'NONE', #14514, #35990, #68344 ) ;
#64355=ORIENTED_EDGE ( 'NONE', *, *, #29563, .T. ) ;
#64357=ORIENTED_EDGE ( 'NONE', *, *, #58232, .T. ) ;
#64359=FILL_AREA_STYLE_COLOUR ( '', #44700 ) ;
#64362=CIRCLE ( 'NONE', #44221, 0.5000000000000004441 ) ;
#64363=CARTESIAN_POINT ( 'NONE',  ( -19.89974874213240597, 115.4999999999999574, -10.50000000000000000 ) ) ;
#64365=UNCERTAINTY_MEASURE_WITH_UNIT (LENGTH_MEASURE( 1.000000000000000082E-05 ), #6172, 'distance_accuracy_value', 'NONE');
#64367=DIRECTION ( 'NONE',  ( 1.000000000000000000, 0.000000000000000000, 0.000000000000000000 ) ) ;
#64368=CARTESIAN_POINT ( 'NONE',  ( 41.00000002860134884, 108.0041655605199367, 3.103651540213804516 ) ) ;
#64369=CARTESIAN_POINT ( 'NONE',  ( 23.71231517720798010, 118.4999999999999716, -7.500000000000000000 ) ) ;
#64370=ORIENTED_EDGE ( 'NONE', *, *, #25502, .T. ) ;
#64380=AXIS2_PLACEMENT_3D ( 'NONE', #51931, #24816, #15363 ) ;
#64381=CARTESIAN_POINT ( 'NONE',  ( 41.49999999999998579, 108.0000000000000000, -3.500000000000000000 ) ) ;
#64391=CARTESIAN_POINT ( 'NONE',  ( -5.598654528085808657, 155.6449999999999818, 7.705886871421373741 ) ) ;
#64394=VECTOR ( 'NONE', #64317, 1000.000000000000114 ) ;
#64395=VECTOR ( 'NONE', #32149, 1000.000000000000000 ) ;
#64397=DIRECTION ( 'NONE',  ( 1.000000000000000000, 0.000000000000000000, 0.000000000000000000 ) ) ;
#64398=UNCERTAINTY_MEASURE_WITH_UNIT (LENGTH_MEASURE( 1.000000000000000082E-05 ), #15169, 'distance_accuracy_value', 'NONE');
#64399=CARTESIAN_POINT ( 'NONE',  ( 23.21231517720797655, 117.4999999999999716, -9.500000000000000000 ) ) ;
#64407=EDGE_CURVE ( 'NONE', #28358, #39909, #25709, .T. ) ;
#64413=FACE_OUTER_BOUND ( 'NONE', #19774, .T. ) ;
#64414=EDGE_CURVE ( 'NONE', #2776, #49636, #30166, .T. ) ;
#64415=VECTOR ( 'NONE', #15553, 1000.000000000000000 ) ;
#64418=( NAMED_UNIT ( * ) PLANE_ANGLE_UNIT ( ) SI_UNIT ( $, .RADIAN. ) );
#64419=AXIS2_PLACEMENT_3D ( 'NONE', #52521, #47264, #9255 ) ;
#64425=SURFACE_STYLE_FILL_AREA ( #53193 ) ;
#64426=ORIENTED_EDGE ( 'NONE', *, *, #22968, .T. ) ;
#64428=LINE ( 'NONE', #10954, #16976 ) ;
#64429=DIRECTION ( 'NONE',  ( 6.938893903907222067E-15, 0.000000000000000000, -1.000000000000000000 ) ) ;
#64430=CARTESIAN_POINT ( 'NONE',  ( -5.598654528085806881, 124.7449999999999903, -7.705886871421374629 ) ) ;
#64436=CARTESIAN_POINT ( 'NONE',  ( -10.01517768586949408, 132.3049999999999784, -6.132527647946036459E-16 ) ) ;
#64439=ADVANCED_FACE ( 'NONE', ( #19265 ), #57261, .F. ) ;
#64442=CARTESIAN_POINT ( 'NONE',  ( -5.598654528085806881, 149.8549999999999898, -7.705886871421374629 ) ) ;
#64446=DIRECTION ( 'NONE',  ( 1.000000000000000000, 0.000000000000000000, -0.000000000000000000 ) ) ;
#64449=CIRCLE ( 'NONE', #7150, 0.5000000000000004441 ) ;
#64452=SURFACE_SIDE_STYLE ('',( #32092 ) ) ;
#64454=VERTEX_POINT ( 'NONE', #3403 ) ;
#64455=UNCERTAINTY_MEASURE_WITH_UNIT (LENGTH_MEASURE( 1.000000000000000082E-05 ), #35889, 'distance_accuracy_value', 'NONE');
#64457=PRESENTATION_STYLE_ASSIGNMENT (( #17341 ) ) ;
#64458=( NAMED_UNIT ( * ) PLANE_ANGLE_UNIT ( ) SI_UNIT ( $, .RADIAN. ) );
#64463=AXIS2_PLACEMENT_3D ( 'NONE', #63374, #53516, #26747 ) ;
#64467=AXIS2_PLACEMENT_3D ( 'NONE', #60370, #17156, #27987 ) ;
#64468=FACE_OUTER_BOUND ( 'NONE', #61346, .T. ) ;
#64471=AXIS2_PLACEMENT_3D ( 'NONE', #50184, #12516, #6218 ) ;
#64475=VERTEX_POINT ( 'NONE', #9095 ) ;
#64476=CARTESIAN_POINT ( 'NONE',  ( -71.50000000000000000, 14.49137674618942562, -7.500000000000000000 ) ) ;
#64477=SURFACE_STYLE_USAGE ( .BOTH. , #44455 ) ;
#64478=( NAMED_UNIT ( * ) SI_UNIT ( $, .STERADIAN. ) SOLID_ANGLE_UNIT ( ) );
#64479=VECTOR ( 'NONE', #51698, 1000.000000000000000 ) ;
#64481=CARTESIAN_POINT ( 'NONE',  ( 9.058813317711338797, 129.8449999999999989, -2.943386871421372675 ) ) ;
#64487=FACE_OUTER_BOUND ( 'NONE', #18937, .T. ) ;
#64489=ADVANCED_FACE ( 'NONE', ( #3046 ), #18920, .F. ) ;
#64492=ADVANCED_FACE ( 'NONE', ( #34758 ), #40416, .F. ) ;
#64495=VECTOR ( 'NONE', #53674, 1000.000000000000000 ) ;
#64497=CARTESIAN_POINT ( 'NONE',  ( 74.99999999999998579, 50.00000000000000000, 7.500000000000000000 ) ) ;
#64498=ORIENTED_EDGE ( 'NONE', *, *, #14145, .T. ) ;
#64503=( NAMED_UNIT ( * ) PLANE_ANGLE_UNIT ( ) SI_UNIT ( $, .RADIAN. ) );
#64504=DIRECTION ( 'NONE',  ( -0.000000000000000000, -0.000000000000000000, -1.000000000000000000 ) ) ;
#64505=EDGE_CURVE ( 'NONE', #31668, #65582, #29825, .T. ) ;
#64507=AXIS2_PLACEMENT_3D ( 'NONE', #11636, #54540, #33101 ) ;
#64508=ORIENTED_EDGE ( 'NONE', *, *, #35286, .T. ) ;
#64513=CARTESIAN_POINT ( 'NONE',  ( 7.632228543268607446, 141.1570736234661751, 2.479861379858954606 ) ) ;
#64515=AXIS2_PLACEMENT_3D ( 'NONE', #50172, #18825, #44914 ) ;
#64520=UNCERTAINTY_MEASURE_WITH_UNIT (LENGTH_MEASURE( 1.000000000000000082E-05 ), #33249, 'distance_accuracy_value', 'NONE');
#64526=EDGE_CURVE ( 'NONE', #2848, #60303, #17512, .T. ) ;
#64529=( LENGTH_UNIT ( ) NAMED_UNIT ( * ) SI_UNIT ( .MILLI., .METRE. ) );
#64535=( NAMED_UNIT ( * ) PLANE_ANGLE_UNIT ( ) SI_UNIT ( $, .RADIAN. ) );
#64537=STYLED_ITEM ( 'NONE', ( #18249 ), #7774 ) ;
#64542=( GEOMETRIC_REPRESENTATION_CONTEXT ( 3 ) GLOBAL_UNCERTAINTY_ASSIGNED_CONTEXT ( ( #9484 ) ) GLOBAL_UNIT_ASSIGNED_CONTEXT ( ( #29945, #50369, #40181 ) ) REPRESENTATION_CONTEXT ( 'NONE', 'WORKASPACE' ) );
#64543=FACE_OUTER_BOUND ( 'NONE', #8373, .T. ) ;
#64549=( NAMED_UNIT ( * ) PLANE_ANGLE_UNIT ( ) SI_UNIT ( $, .RADIAN. ) );
#64550=DIRECTION ( 'NONE',  ( 1.000000000000000000, 0.000000000000000000, 0.000000000000000000 ) ) ;
#64553=CARTESIAN_POINT ( 'NONE',  ( -10.01517768586949408, 128.1949999999999932, -6.132527647946036459E-16 ) ) ;
#64555=( NAMED_UNIT ( * ) PLANE_ANGLE_UNIT ( ) SI_UNIT ( $, .RADIAN. ) );
#64556=ORIENTED_EDGE ( 'NONE', *, *, #15309, .F. ) ;
#64557=CIRCLE ( 'NONE', #8432, 0.5000000000000000000 ) ;
#64564=EDGE_CURVE ( 'NONE', #59291, #52539, #65401, .T. ) ;
#64569=VERTEX_POINT ( 'NONE', #28785 ) ;
#64571=CARTESIAN_POINT ( 'NONE',  ( 44.88867800444037925, 10.61949827965496063, -3.673511479703639449 ) ) ;
#64572=FACE_OUTER_BOUND ( 'NONE', #47884, .T. ) ;
#64573=ADVANCED_FACE ( 'NONE', ( #623 ), #65030, .F. ) ;
#64577=( BOUNDED_CURVE ( )  B_SPLINE_CURVE ( 2, ( #68745, #68054, #8609, #24411, #46634, #41334, #62735, #14569, #9667, #36038, #41685 ),
 .UNSPECIFIED., .F., .F. ) 
 B_SPLINE_CURVE_WITH_KNOTS ( ( 3, 2, 2, 2, 2, 3 ),
 ( 0.2941176470588235392, 0.2999999999999999889, 0.3058823529411764941, 0.3117647058823529438, 0.3176470588235293935, 0.3235294117647058987 ),
 .UNSPECIFIED. ) 
 CURVE ( )  GEOMETRIC_REPRESENTATION_ITEM ( )  RATIONAL_B_SPLINE_CURVE ( ( 1.000000000000000000, 0.9510565162951535312, 1.000000000000000000, 0.9510565162951535312, 1.000000000000000000, 0.9510565162951535312, 1.000000000000000000, 0.9510565162951535312, 1.000000000000000000, 0.9510565162951535312, 1.000000000000000000 ) ) 
 REPRESENTATION_ITEM ( '' )  );
#64578=CYLINDRICAL_SURFACE ( 'NONE', #61860, 0.5000000000000004441 ) ;
#64581=EDGE_CURVE ( 'NONE', #3932, #9272, #37824, .T. ) ;
#64583=DIRECTION ( 'NONE',  ( -0.000000000000000000, -0.000000000000000000, -1.000000000000000000 ) ) ;
#64587=CIRCLE ( 'NONE', #16315, 13.50000000000000533 ) ;
#64588=CARTESIAN_POINT ( 'NONE',  ( -71.49999999999998579, 64.07124727947029896, 7.500000000000000000 ) ) ;
#64594=CARTESIAN_POINT ( 'NONE',  ( -7.632228543268607446, 138.5429263765338135, -2.479861379858953718 ) ) ;
#64595=FILL_AREA_STYLE_COLOUR ( '', #57617 ) ;
#64597=ORIENTED_EDGE ( 'NONE', *, *, #10422, .T. ) ;
#64598=CIRCLE ( 'NONE', #44413, 13.00000000000000533 ) ;
#64600=CARTESIAN_POINT ( 'NONE',  ( 7.632228543268607446, 117.1570736234661609, 2.479861379858954606 ) ) ;
#64601=CARTESIAN_POINT ( 'NONE',  ( 74.62643842725373133, 19.76989462323605906, -6.307273367294813582 ) ) ;
#64609=CARTESIAN_POINT ( 'NONE',  ( 0.000000000000000000, 131.5549999999999784, -9.525000000000000355 ) ) ;
#64612=DIRECTION ( 'NONE',  ( 1.000000000000000000, 0.000000000000000000, 0.000000000000000000 ) ) ;
#64613=EDGE_CURVE ( 'NONE', #60581, #55705, #17555, .T. ) ;
#64615=ORIENTED_EDGE ( 'NONE', *, *, #46555, .F. ) ;
#64617=DIRECTION ( 'NONE',  ( 0.000000000000000000, 0.000000000000000000, 1.000000000000000000 ) ) ;
#64621=DIRECTION ( 'NONE',  ( -1.000000000000000000, -0.000000000000000000, -0.000000000000000000 ) ) ;
#64629=( LENGTH_UNIT ( ) NAMED_UNIT ( * ) SI_UNIT ( .MILLI., .METRE. ) );
#64632=LINE ( 'NONE', #36893, #9116 ) ;
#64640=DIRECTION ( 'NONE',  ( 0.6216216216216191581, -0.7833176619561879050, 0.000000000000000000 ) ) ;
#64645=EDGE_CURVE ( 'NONE', #55705, #51980, #17903, .T. ) ;
#64648=AXIS2_PLACEMENT_3D ( 'NONE', #47109, #58316, #69230 ) ;
#64650=ORIENTED_EDGE ( 'NONE', *, *, #31106, .T. ) ;
#64652=CARTESIAN_POINT ( 'NONE',  ( 45.00000000000000000, -1.469576158976824618E-14, 10.00000000000000000 ) ) ;
#64655=SURFACE_STYLE_FILL_AREA ( #43250 ) ;
#64656=CARTESIAN_POINT ( 'NONE',  ( 0.000000000000000000, 149.9999999999999716, 0.000000000000000000 ) ) ;
#64660=CARTESIAN_POINT ( 'NONE',  ( 5.598654528085809545, 137.2549999999999955, -7.705886871421373741 ) ) ;
#64662=AXIS2_PLACEMENT_3D ( 'NONE', #30951, #35202, #8486 ) ;
#64665=DIRECTION ( 'NONE',  ( 0.000000000000000000, 0.000000000000000000, -1.000000000000000000 ) ) ;
#64669=EDGE_LOOP ( 'NONE', ( #2810, #58456, #11583, #22910 ) ) ;
#64673=EDGE_CURVE ( 'NONE', #58485, #30209, #51233, .T. ) ;
#64677=CARTESIAN_POINT ( 'NONE',  ( -4.716976649647097730, 136.3570736234661638, -6.492361379858953896 ) ) ;
#64680=CARTESIAN_POINT ( 'NONE',  ( -15.98999599679679839, 118.4999999999999716, 7.500000000000000000 ) ) ;
#64681=DIRECTION ( 'NONE',  ( 0.000000000000000000, 0.000000000000000000, -1.000000000000000000 ) ) ;
#64682=CARTESIAN_POINT ( 'NONE',  ( -71.50000000000000000, 14.49137674618942562, 9.500000000000000000 ) ) ;
#64683=CARTESIAN_POINT ( 'NONE',  ( 2.607480562269155921, 139.5929263765337964, 8.024999999999941735 ) ) ;
#64687=COLOUR_RGB ( '', 0.08235294, 0.09019608, 0.10196078) ;
#64693=MECHANICAL_DESIGN_GEOMETRIC_PRESENTATION_REPRESENTATION('',(#10810),#65854);
#64696=CARTESIAN_POINT ( 'NONE',  ( 0.000000000000000000, 119.9429263765338050, -8.025000000000000355 ) ) ;
#64697=SURFACE_STYLE_FILL_AREA ( #11559 ) ;
#64704=ORIENTED_EDGE ( 'NONE', *, *, #41004, .F. ) ;
#64705=CARTESIAN_POINT ( 'NONE',  ( -7.632228543268608334, 123.8429263765338249, 2.479861379858952830 ) ) ;
#64706=( NAMED_UNIT ( * ) SI_UNIT ( $, .STERADIAN. ) SOLID_ANGLE_UNIT ( ) );
#64710=EDGE_LOOP ( 'NONE', ( #49316, #65797, #51930, #30229 ) ) ;
#64712=ORIENTED_EDGE ( 'NONE', *, *, #33378, .F. ) ;
#64715=CARTESIAN_POINT ( 'NONE',  ( -60.00000000000000000, -2.024042244987997205E-14, 7.000000000000000000 ) ) ;
#64716=CARTESIAN_POINT ( 'NONE',  ( -24.21231517720798010, 112.4999999999999858, 10.00000000000000000 ) ) ;
#64719=PRESENTATION_STYLE_ASSIGNMENT (( #16898 ) ) ;
#64722=CARTESIAN_POINT ( 'NONE',  ( 44.99999999999977973, 147.4999999999999716, 10.00000000000000000 ) ) ;
#64724=VERTEX_POINT ( 'NONE', #35474 ) ;
#64727=DIRECTION ( 'NONE',  ( 0.000000000000000000, -1.000000000000000000, 0.000000000000000000 ) ) ;
#64728=( NAMED_UNIT ( * ) PLANE_ANGLE_UNIT ( ) SI_UNIT ( $, .RADIAN. ) );
#64731=ORIENTED_EDGE ( 'NONE', *, *, #39826, .T. ) ;
#64732=EDGE_CURVE ( 'NONE', #3817, #6686, #62467, .T. ) ;
#64733=( GEOMETRIC_REPRESENTATION_CONTEXT ( 3 ) GLOBAL_UNCERTAINTY_ASSIGNED_CONTEXT ( ( #7451 ) ) GLOBAL_UNIT_ASSIGNED_CONTEXT ( ( #28264, #19388, #65935 ) ) REPRESENTATION_CONTEXT ( 'NONE', 'WORKASPACE' ) );
#64734=EDGE_CURVE ( 'NONE', #57704, #23416, #57728, .T. ) ;
#64735=DIRECTION ( 'NONE',  ( -0.000000000000000000, -0.000000000000000000, -1.000000000000000000 ) ) ;
#64736=FACE_OUTER_BOUND ( 'NONE', #40732, .T. ) ;
#64742=CARTESIAN_POINT ( 'NONE',  ( 9.058813317711337021, 112.6549999999999869, 2.943386871421375783 ) ) ;
#64745=ADVANCED_FACE ( 'NONE', ( #18606 ), #61473, .T. ) ;
#64749=DIRECTION ( 'NONE',  ( -1.000000000000000000, 0.000000000000000000, 0.000000000000000000 ) ) ;
#64750=ORIENTED_EDGE ( 'NONE', *, *, #8533, .F. ) ;
#64754=DIRECTION ( 'NONE',  ( 0.000000000000000000, 1.000000000000000000, 0.000000000000000000 ) ) ;
#64760=CARTESIAN_POINT ( 'NONE',  ( 60.00000000000000000, 1.797044900979284448E-15, -12.00000000000000000 ) ) ;
#64763=CARTESIAN_POINT ( 'NONE',  ( -45.00000000000000000, 8.588294701370031703, 5.575869277511095845 ) ) ;
#64771=CARTESIAN_POINT ( 'NONE',  ( 14.98999599679679662, 117.9999999999999716, 9.500000000000000000 ) ) ;
#64775=CARTESIAN_POINT ( 'NONE',  ( -9.058813317711337021, 134.0449999999999875, -2.943386871421374895 ) ) ;
#64776=CARTESIAN_POINT ( 'NONE',  ( 74.99999999999998579, 50.00000000000000000, -7.000000000000000000 ) ) ;
#64779=LINE ( 'NONE', #17319, #6022 ) ;
#64780=CARTESIAN_POINT ( 'NONE',  ( -9.058813317711338797, 126.4549999999999841, 2.943386871421373563 ) ) ;
#64785=ORIENTED_EDGE ( 'NONE', *, *, #66902, .F. ) ;
#64786=CARTESIAN_POINT ( 'NONE',  ( -3.094860106618432471, 146.7049999999999841, -9.525000000000000355 ) ) ;
#64787=COLOUR_RGB ( '', 0.66274510, 0.83137255, 0.94901961) ;
#64788=LINE ( 'NONE', #21172, #46686 ) ;
#64793=SURFACE_SIDE_STYLE ('',( #33809 ) ) ;
#64796=SURFACE_SIDE_STYLE ('',( #367 ) ) ;
#64798=FILL_AREA_STYLE ('',( #64099 ) ) ;
#64799=CARTESIAN_POINT ( 'NONE',  ( -74.50000000000000000, -1.856352308976905642E-14, 6.500000000000000000 ) ) ;
#64800=ORIENTED_EDGE ( 'NONE', *, *, #53382, .T. ) ;
#64801=FILL_AREA_STYLE ('',( #43414 ) ) ;
#64803=ORIENTED_EDGE ( 'NONE', *, *, #6006, .F. ) ;
#64804=ADVANCED_FACE ( 'NONE', ( #35115 ), #9731, .F. ) ;
#64805=DIRECTION ( 'NONE',  ( -1.000000000000000000, 0.000000000000000000, -0.000000000000000000 ) ) ;
#64806=DIRECTION ( 'NONE',  ( 1.000000000000000000, 0.000000000000000000, 0.000000000000000000 ) ) ;
#64807=( NAMED_UNIT ( * ) SI_UNIT ( $, .STERADIAN. ) SOLID_ANGLE_UNIT ( ) );
#64809=EDGE_CURVE ( 'NONE', #38944, #11547, #67003, .T. ) ;
#64813=CARTESIAN_POINT ( 'NONE',  ( 0.000000000000000000, 114.4999999999999574, 0.000000000000000000 ) ) ;
#64814=FILL_AREA_STYLE ('',( #60233 ) ) ;
#64817=CARTESIAN_POINT ( 'NONE',  ( -9.058813317711337021, 131.0449999999999875, -2.943386871421374895 ) ) ;
#64821=DIRECTION ( 'NONE',  ( 0.000000000000000000, -1.000000000000000000, 0.000000000000000000 ) ) ;
#64822=ADVANCED_FACE ( 'NONE', ( #25931 ), #31906, .T. ) ;
#64826=MECHANICAL_DESIGN_GEOMETRIC_PRESENTATION_REPRESENTATION('',(#37971),#22203);
#64827=CARTESIAN_POINT ( 'NONE',  ( -4.716976649647098618, 149.2570736234661695, 6.492361379858953008 ) ) ;
#64829=ORIENTED_EDGE ( 'NONE', *, *, #42787, .T. ) ;
#64836=DIRECTION ( 'NONE',  ( 0.000000000000000000, 0.000000000000000000, 1.000000000000000000 ) ) ;
#64837=CARTESIAN_POINT ( 'NONE',  ( 67.50000000000000000, 1.797044900979284448E-15, 11.50000000000000000 ) ) ;
#64839=ORIENTED_EDGE ( 'NONE', *, *, #21496, .F. ) ;
#64841=EDGE_LOOP ( 'NONE', ( #3675, #39877, #25149, #27034 ) ) ;
#64843=SURFACE_STYLE_USAGE ( .BOTH. , #59559 ) ;
#64846=CARTESIAN_POINT ( 'NONE',  ( -4.716976649647098618, 140.2570736234661410, 6.492361379858953008 ) ) ;
#64852=CARTESIAN_POINT ( 'NONE',  ( 54.99999999999999289, 2.409368300552961372E-15, -12.00000000000000000 ) ) ;
#64854=DIRECTION ( 'NONE',  ( 0.000000000000000000, 1.000000000000000000, 0.000000000000000000 ) ) ;
#64855=SURFACE_STYLE_USAGE ( .BOTH. , #43473 ) ;
#64857=ORIENTED_EDGE ( 'NONE', *, *, #65799, .F. ) ;
#64862=SURFACE_SIDE_STYLE ('',( #7175 ) ) ;
#64874=DIRECTION ( 'NONE',  ( 0.000000000000000000, 0.000000000000000000, 1.000000000000000000 ) ) ;
#64875=SURFACE_STYLE_USAGE ( .BOTH. , #457 ) ;
#64878=CARTESIAN_POINT ( 'NONE',  ( -8.102448949553179958, 134.4949999999999477, 5.886773742842747126 ) ) ;
#64882=CARTESIAN_POINT ( 'NONE',  ( 0.000000000000000000, 114.4999999999999574, 23.00000000000000000 ) ) ;
#64883=ORIENTED_EDGE ( 'NONE', *, *, #32756, .F. ) ;
#64884=DIRECTION ( 'NONE',  ( -0.000000000000000000, -0.000000000000000000, -1.000000000000000000 ) ) ;
#64885=VECTOR ( 'NONE', #48086, 1000.000000000000000 ) ;
#64888=DIRECTION ( 'NONE',  ( 0.000000000000000000, 1.000000000000000000, 0.000000000000000000 ) ) ;
#64889=CIRCLE ( 'NONE', #41331, 14.49999999999999822 ) ;
#64891=DIRECTION ( 'NONE',  ( 1.000000000000000000, 0.000000000000000000, 0.000000000000000000 ) ) ;
#64897=CARTESIAN_POINT ( 'NONE',  ( 44.75458990717763896, 9.918196635725919919, -3.527112199763385192 ) ) ;
#64898=( NAMED_UNIT ( * ) SI_UNIT ( $, .STERADIAN. ) SOLID_ANGLE_UNIT ( ) );
#64901=EDGE_CURVE ( 'NONE', #67841, #10695, #2959, .T. ) ;
#64905=SURFACE_STYLE_USAGE ( .BOTH. , #43520 ) ;
#64906=FACE_OUTER_BOUND ( 'NONE', #42324, .T. ) ;
#64909=COLOUR_RGB ( '', 0.72549020, 0.75294118, 0.79215686) ;
#64911=COLOUR_RGB ( '', 0.66274510, 0.83137255, 0.94901961) ;
#64914=ORIENTED_EDGE ( 'NONE', *, *, #4513, .T. ) ;
#64916=SURFACE_STYLE_USAGE ( .BOTH. , #43531 ) ;
#64917=ORIENTED_EDGE ( 'NONE', *, *, #63480, .F. ) ;
#64920=CARTESIAN_POINT ( 'NONE',  ( -6.826472737025120807, 113.1070736234661638, 4.959722759717906548 ) ) ;
#64922=FACE_BOUND ( 'NONE', #36567, .T. ) ;
#64927=STYLED_ITEM ( 'NONE', ( #15350 ), #41399 ) ;
#64933=CARTESIAN_POINT ( 'NONE',  ( 0.000000000000000000, 149.9999999999999716, 0.000000000000000000 ) ) ;
#64936=CARTESIAN_POINT ( 'NONE',  ( 8.035289517290014061, 153.2535762506718413, 2.032298507828633749 ) ) ;
#64938=SURFACE_STYLE_USAGE ( .BOTH. , #44584 ) ;
#64939=SURFACE_STYLE_FILL_AREA ( #5160 ) ;
#64950=DIRECTION ( 'NONE',  ( -1.000000000000000000, 1.224646799147349509E-16, 0.000000000000000000 ) ) ;
#64955=AXIS2_PLACEMENT_3D ( 'NONE', #36188, #8730, #51642 ) ;
#64957=CARTESIAN_POINT ( 'NONE',  ( -6.240333192270997920, 153.8516573869858632, 6.318785644388177580 ) ) ;
#64958=ORIENTED_EDGE ( 'NONE', *, *, #26144, .T. ) ;
#64966=SURFACE_SIDE_STYLE ('',( #43573 ) ) ;
#64970=VECTOR ( 'NONE', #36039, 1000.000000000000000 ) ;
#64972=VERTEX_POINT ( 'NONE', #28697 ) ;
#64973=DIRECTION ( 'NONE',  ( -0.000000000000000000, 1.000000000000000000, -0.000000000000000000 ) ) ;
#64974=DIRECTION ( 'NONE',  ( 0.000000000000000000, -0.000000000000000000, 1.000000000000000000 ) ) ;
#64975=CARTESIAN_POINT ( 'NONE',  ( 51.99999999999998579, 1.797044900979284448E-15, 12.00000000000000000 ) ) ;
#64977=( NAMED_UNIT ( * ) PLANE_ANGLE_UNIT ( ) SI_UNIT ( $, .RADIAN. ) );
#64980=CARTESIAN_POINT ( 'NONE',  ( -1.166476076187854022E-15, 133.0549999999999784, 9.525000000000000355 ) ) ;
#64985=UNCERTAINTY_MEASURE_WITH_UNIT (LENGTH_MEASURE( 1.000000000000000082E-05 ), #6481, 'distance_accuracy_value', 'NONE');
#64986=DIRECTION ( 'NONE',  ( 0.000000000000000000, 0.000000000000000000, 1.000000000000000000 ) ) ;
#64987=ORIENTED_EDGE ( 'NONE', *, *, #33357, .F. ) ;
#64989=CARTESIAN_POINT ( 'NONE',  ( -7.632228543268608334, 132.8429263765338249, 2.479861379858952830 ) ) ;
#64990=DIRECTION ( 'NONE',  ( 0.000000000000000000, 0.000000000000000000, -1.000000000000000000 ) ) ;
#64992=FILL_AREA_STYLE_COLOUR ( '', #68957 ) ;
#64996=CARTESIAN_POINT ( 'NONE',  ( -8.437984349512095861, 135.6929263765338192, -5.166775262442723748E-16 ) ) ;
#64997=CIRCLE ( 'NONE', #32457, 0.5000000000000004441 ) ;
#64998=DIRECTION ( 'NONE',  ( 0.000000000000000000, -0.000000000000000000, -1.000000000000000000 ) ) ;
#64999=AXIS2_PLACEMENT_3D ( 'NONE', #47048, #4407, #20974 ) ;
#65001=STYLED_ITEM ( 'NONE', ( #16320 ), #66717 ) ;
#65005=DIRECTION ( 'NONE',  ( 0.000000000000000000, 0.000000000000000000, 1.000000000000000000 ) ) ;
#65006=CARTESIAN_POINT ( 'NONE',  ( -71.49999999999998579, 64.07124727947029896, 10.00000000000000000 ) ) ;
#65008=CARTESIAN_POINT ( 'NONE',  ( 54.50000000000002132, 1.797044900979284448E-15, -12.00000000000000000 ) ) ;
#65010=ORIENTED_EDGE ( 'NONE', *, *, #19167, .F. ) ;
#65013=DIRECTION ( 'NONE',  ( 0.000000000000000000, 0.000000000000000000, 1.000000000000000000 ) ) ;
#65014=CARTESIAN_POINT ( 'NONE',  ( 5.598654528085805993, 156.2450000000000045, 7.705886871421374629 ) ) ;
#65020=SURFACE_STYLE_FILL_AREA ( #39035 ) ;
#65022=ORIENTED_EDGE ( 'NONE', *, *, #20724, .T. ) ;
#65023=CARTESIAN_POINT ( 'NONE',  ( 0.000000000000000000, 131.9429263765338192, -8.025000000000000355 ) ) ;
#65026=ORIENTED_EDGE ( 'NONE', *, *, #25095, .F. ) ;
#65027=VERTEX_POINT ( 'NONE', #34344 ) ;
#65030=CYLINDRICAL_SURFACE ( 'NONE', #8561, 26.99999999999999645 ) ;
#65032=SURFACE_STYLE_USAGE ( .BOTH. , #43642 ) ;
#65038=PRESENTATION_STYLE_ASSIGNMENT (( #16560 ) ) ;
#65039=CARTESIAN_POINT ( 'NONE',  ( 41.27334858134414475, 107.3315027881082528, 3.464507624621605331 ) ) ;
#65045=LINE ( 'NONE', #1326, #33442 ) ;
#65047=ORIENTED_EDGE ( 'NONE', *, *, #63070, .F. ) ;
#65048=( NAMED_UNIT ( * ) PLANE_ANGLE_UNIT ( ) SI_UNIT ( $, .RADIAN. ) );
#65049=CARTESIAN_POINT ( 'NONE',  ( 45.00000000000000000, 10.69371294336137801, 10.00000000000000000 ) ) ;
#65050=STYLED_ITEM ( 'NONE', ( #57115 ), #20646 ) ;
#65052=DIRECTION ( 'NONE',  ( 0.000000000000000000, 0.000000000000000000, -1.000000000000000000 ) ) ;
#65053=CIRCLE ( 'NONE', #34716, 22.50000000000000000 ) ;
#65054=LINE ( 'NONE', #48238, #8412 ) ;
#65057=DIRECTION ( 'NONE',  ( 1.000000000000000000, 0.000000000000000000, 0.000000000000000000 ) ) ;
#65060=CARTESIAN_POINT ( 'NONE',  ( 48.81081081081080697, 14.09971791521133255, 7.000000000000000000 ) ) ;
#65064=CARTESIAN_POINT ( 'NONE',  ( 5.598654528085809545, 157.1449999999999818, -7.705886871421373741 ) ) ;
#65069=UNCERTAINTY_MEASURE_WITH_UNIT (LENGTH_MEASURE( 1.000000000000000082E-05 ), #67715, 'distance_accuracy_value', 'NONE');
#65071=ORIENTED_EDGE ( 'NONE', *, *, #28088, .F. ) ;
#65075=AXIS2_PLACEMENT_3D ( 'NONE', #65940, #17769, #40977 ) ;
#65076=SURFACE_STYLE_USAGE ( .BOTH. , #22188 ) ;
#65077=SURFACE_SIDE_STYLE ('',( #11281 ) ) ;
#65080=DIRECTION ( 'NONE',  ( -0.000000000000000000, -0.000000000000000000, -1.000000000000000000 ) ) ;
#65082=UNCERTAINTY_MEASURE_WITH_UNIT (LENGTH_MEASURE( 1.000000000000000082E-05 ), #3328, 'distance_accuracy_value', 'NONE');
#65090=ORIENTED_EDGE ( 'NONE', *, *, #36813, .T. ) ;
#65091=CARTESIAN_POINT ( 'NONE',  ( 71.50000000000000000, 99.99999999999998579, -7.000000000000000000 ) ) ;
#65093=VERTEX_POINT ( 'NONE', #50532 ) ;
#65095=AXIS2_PLACEMENT_3D ( 'NONE', #49985, #1723, #44041 ) ;
#65099=CARTESIAN_POINT ( 'NONE',  ( -9.058813317711338797, 134.3449999999999989, 2.943386871421373563 ) ) ;
#65100=STYLED_ITEM ( 'NONE', ( #37442 ), #4948 ) ;
#65101=ADVANCED_FACE ( 'NONE', ( #66702 ), #18518, .F. ) ;
#65102=ORIENTED_EDGE ( 'NONE', *, *, #7549, .F. ) ;
#65105=CARTESIAN_POINT ( 'NONE',  ( -8.102448949553179958, 132.6049999999999898, 5.886773742842747126 ) ) ;
#65108=CARTESIAN_POINT ( 'NONE',  ( -40.95866658621363854, 108.0312444614857128, -3.562488397568094989 ) ) ;
#65110=CARTESIAN_POINT ( 'NONE',  ( 0.000000000000000000, 155.5550000000000068, -9.525000000000000355 ) ) ;
#65113=CIRCLE ( 'NONE', #48299, 17.50000000000000000 ) ;
#65115=ADVANCED_FACE ( 'NONE', ( #25173 ), #31127, .T. ) ;
#65118=SURFACE_STYLE_FILL_AREA ( #54896 ) ;
#65122=DIRECTION ( 'NONE',  ( -0.000000000000000000, -0.000000000000000000, -1.000000000000000000 ) ) ;
#65126=( LENGTH_UNIT ( ) NAMED_UNIT ( * ) SI_UNIT ( .MILLI., .METRE. ) );
#65129=SURFACE_STYLE_FILL_AREA ( #370 ) ;
#65130=EDGE_CURVE ( 'NONE', #32643, #61826, #23322, .T. ) ;
#65131=CARTESIAN_POINT ( 'NONE',  ( -65.00000000000000000, -1.962809905030629631E-14, -7.000000000000024869 ) ) ;
#65132=SURFACE_STYLE_FILL_AREA ( #22234 ) ;
#65133=CARTESIAN_POINT ( 'NONE',  ( -34.99999999999999289, 99.99999999999998579, -10.00000000000000000 ) ) ;
#65136=CARTESIAN_POINT ( 'NONE',  ( -45.90208536020663388, 9.410173053538171573, -3.203892945547820226 ) ) ;
#65142=CIRCLE ( 'NONE', #12359, 4.999999999999997335 ) ;
#65143=DIRECTION ( 'NONE',  ( -0.000000000000000000, -0.000000000000000000, -1.000000000000000000 ) ) ;
#65146=AXIS2_PLACEMENT_3D ( 'NONE', #65511, #29608, #34202 ) ;
#65150=FACE_OUTER_BOUND ( 'NONE', #13307, .T. ) ;
#65152=CARTESIAN_POINT ( 'NONE',  ( 0.000000000000000000, 133.4449999999999932, -9.525000000000000355 ) ) ;
#65157=CIRCLE ( 'NONE', #24671, 0.5000000000000004441 ) ;
#65164=CARTESIAN_POINT ( 'NONE',  ( 0.000000000000000000, 148.0570736234661524, -8.025000000000000355 ) ) ;
#65169=DIRECTION ( 'NONE',  ( 1.000000000000000000, 0.000000000000000000, 0.000000000000000000 ) ) ;
#65170=EDGE_LOOP ( 'NONE', ( #56934, #35785, #28259, #15238 ) ) ;
#65178=DIRECTION ( 'NONE',  ( 0.000000000000000000, -1.000000000000000000, 0.000000000000000000 ) ) ;
#65184=EDGE_LOOP ( 'NONE', ( #57057, #68431, #28164 ) ) ;
#65186=EDGE_CURVE ( 'NONE', #69284, #57165, #26204, .T. ) ;
#65188=( BOUNDED_CURVE ( )  B_SPLINE_CURVE ( 2, ( #30503, #31556, #15083, #69215, #53037, #47817, #52360, #21016, #62181, #56916, #8729 ),
 .UNSPECIFIED., .F., .F. ) 
 B_SPLINE_CURVE_WITH_KNOTS ( ( 3, 2, 2, 2, 2, 3 ),
 ( 0.3235294117647058987, 0.3294117647058823484, 0.3352941176470587981, 0.3411764705882353033, 0.3470588235294117530, 0.3529411764705882582 ),
 .UNSPECIFIED. ) 
 CURVE ( )  GEOMETRIC_REPRESENTATION_ITEM ( )  RATIONAL_B_SPLINE_CURVE ( ( 1.000000000000000000, 0.9510565162951535312, 1.000000000000000000, 0.9510565162951535312, 1.000000000000000000, 0.9510565162951535312, 1.000000000000000000, 0.9510565162951535312, 1.000000000000000000, 0.9510565162951535312, 1.000000000000000000 ) ) 
 REPRESENTATION_ITEM ( '' )  );
#65190=CARTESIAN_POINT ( 'NONE',  ( -2.607480562269073765, 148.2070736234661581, -8.025000000000000355 ) ) ;
#65191=EDGE_CURVE ( 'NONE', #3129, #2414, #21259, .T. ) ;
#65194=( LENGTH_UNIT ( ) NAMED_UNIT ( * ) SI_UNIT ( .MILLI., .METRE. ) );
#65199=FILL_AREA_STYLE_COLOUR ( '', #33261 ) ;
#65200=CYLINDRICAL_SURFACE ( 'NONE', #26222, 0.5000000000000004441 ) ;
#65201=AXIS2_PLACEMENT_3D ( 'NONE', #38511, #60254, #12748 ) ;
#65204=VERTEX_POINT ( 'NONE', #10401 ) ;
#65208=ORIENTED_EDGE ( 'NONE', *, *, #33292, .T. ) ;
#65211=CARTESIAN_POINT ( 'NONE',  ( -45.00000000000000000, 9.115532208874116193, -6.738970650128846884 ) ) ;
#65213=ORIENTED_EDGE ( 'NONE', *, *, #3610, .F. ) ;
#65214=DIRECTION ( 'NONE',  ( 0.000000000000000000, 0.000000000000000000, 1.000000000000000000 ) ) ;
#65216=( GEOMETRIC_REPRESENTATION_CONTEXT ( 3 ) GLOBAL_UNCERTAINTY_ASSIGNED_CONTEXT ( ( #14467 ) ) GLOBAL_UNIT_ASSIGNED_CONTEXT ( ( #11371, #66209, #22272 ) ) REPRESENTATION_CONTEXT ( 'NONE', 'WORKASPACE' ) );
#65219=DIRECTION ( 'NONE',  ( 0.000000000000000000, 0.000000000000000000, 1.000000000000000000 ) ) ;
#65222=CARTESIAN_POINT ( 'NONE',  ( 0.000000000000000000, 149.9999999999999716, 0.000000000000000000 ) ) ;
#65223=FACE_OUTER_BOUND ( 'NONE', #7856, .T. ) ;
#65224=( GEOMETRIC_REPRESENTATION_CONTEXT ( 3 ) GLOBAL_UNCERTAINTY_ASSIGNED_CONTEXT ( ( #32057 ) ) GLOBAL_UNIT_ASSIGNED_CONTEXT ( ( #49599, #65419, #45389 ) ) REPRESENTATION_CONTEXT ( 'NONE', 'WORKASPACE' ) );
#65225=DIRECTION ( 'NONE',  ( -0.000000000000000000, 1.000000000000000000, 0.000000000000000000 ) ) ;
#65226=DIRECTION ( 'NONE',  ( 1.000000000000000000, 0.000000000000000000, 0.000000000000000000 ) ) ;
#65229=CARTESIAN_POINT ( 'NONE',  ( -1.166476076187854022E-15, 134.9449999999999932, 9.525000000000000355 ) ) ;
#65233=MECHANICAL_DESIGN_GEOMETRIC_PRESENTATION_REPRESENTATION('',(#11315),#33803);
#65234=SURFACE_SIDE_STYLE ('',( #6152 ) ) ;
#65236=DIRECTION ( 'NONE',  ( 0.000000000000000000, 0.000000000000000000, -1.000000000000000000 ) ) ;
#65243=( GEOMETRIC_REPRESENTATION_CONTEXT ( 3 ) GLOBAL_UNCERTAINTY_ASSIGNED_CONTEXT ( ( #43352 ) ) GLOBAL_UNIT_ASSIGNED_CONTEXT ( ( #53743, #5899, #27342 ) ) REPRESENTATION_CONTEXT ( 'NONE', 'WORKASPACE' ) );
#65246=ADVANCED_FACE ( 'NONE', ( #59947 ), #32185, .F. ) ;
#65247=CARTESIAN_POINT ( 'NONE',  ( 44.97648960591794776, 10.67803934730668658, -3.825005713026913057 ) ) ;
#65248=FILL_AREA_STYLE ('',( #43840 ) ) ;
#65255=DIRECTION ( 'NONE',  ( -1.000000000000000000, 0.000000000000000000, 0.000000000000000000 ) ) ;
#65257=( NAMED_UNIT ( * ) PLANE_ANGLE_UNIT ( ) SI_UNIT ( $, .RADIAN. ) );
#65261=DIRECTION ( 'NONE',  ( -0.000000000000000000, 1.000000000000000000, -0.000000000000000000 ) ) ;
#65262=CARTESIAN_POINT ( 'NONE',  ( 60.00000000000000000, 1.797044900979284448E-15, -12.00000000000000000 ) ) ;
#65264=CARTESIAN_POINT ( 'NONE',  ( 60.00000000000000000, 1.797044900979284448E-15, -10.49999999999999822 ) ) ;
#65267=( NAMED_UNIT ( * ) SI_UNIT ( $, .STERADIAN. ) SOLID_ANGLE_UNIT ( ) );
#65271=LINE ( 'NONE', #66308, #56452 ) ;
#65273=CARTESIAN_POINT ( 'NONE',  ( -20.71231517720798010, 149.9999999999999716, 10.00000000000000000 ) ) ;
#65274=CIRCLE ( 'NONE', #36076, 0.5000000000000004441 ) ;
#65275=CARTESIAN_POINT ( 'NONE',  ( 2.607480562269076430, 126.9070736234661467, -8.025000000000000355 ) ) ;
#65279=COLOUR_RGB ( '', 0.31764706, 0.68627451, 0.89019608) ;
#65281=EDGE_CURVE ( 'NONE', #13722, #52924, #52506, .T. ) ;
#65283=ORIENTED_EDGE ( 'NONE', *, *, #68232, .T. ) ;
#65288=LINE ( 'NONE', #17805, #4117 ) ;
#65290=AXIS2_PLACEMENT_3D ( 'NONE', #62652, #14852, #69348 ) ;
#65291=CARTESIAN_POINT ( 'NONE',  ( 8.437984349512095861, 134.1929263765338192, 1.550032578732816828E-15 ) ) ;
#65293=ORIENTED_EDGE ( 'NONE', *, *, #16562, .T. ) ;
#65295=CARTESIAN_POINT ( 'NONE',  ( -20.20444455447386645, 114.9652390998742533, -10.39771284005833252 ) ) ;
#65297=CARTESIAN_POINT ( 'NONE',  ( -23.71231517720798010, 117.9999999999999716, 7.500000000000000000 ) ) ;
#65298=STYLED_ITEM ( 'NONE', ( #39670 ), #12629 ) ;
#65304=VECTOR ( 'NONE', #30348, 1000.000000000000000 ) ;
#65305=ORIENTED_EDGE ( 'NONE', *, *, #58138, .F. ) ;
#65306=( GEOMETRIC_REPRESENTATION_CONTEXT ( 3 ) GLOBAL_UNCERTAINTY_ASSIGNED_CONTEXT ( ( #47712 ) ) GLOBAL_UNIT_ASSIGNED_CONTEXT ( ( #1639, #22111, #60081 ) ) REPRESENTATION_CONTEXT ( 'NONE', 'WORKASPACE' ) );
#65308=ORIENTED_EDGE ( 'NONE', *, *, #29870, .T. ) ;
#65317=CARTESIAN_POINT ( 'NONE',  ( -4.559337023122181698, 153.1785496352698601, -6.825287955804306250 ) ) ;
#65318=ORIENTED_EDGE ( 'NONE', *, *, #56539, .F. ) ;
#65322=PRESENTATION_STYLE_ASSIGNMENT (( #23118 ) ) ;
#65323=FILL_AREA_STYLE_COLOUR ( '', #37725 ) ;
#65324=ORIENTED_EDGE ( 'NONE', *, *, #45101, .T. ) ;
#65332=ORIENTED_EDGE ( 'NONE', *, *, #23406, .T. ) ;
#65340=CARTESIAN_POINT ( 'NONE',  ( 0.000000000000000000, 140.5549999999999784, -9.525000000000000355 ) ) ;
#65342=CIRCLE ( 'NONE', #29373, 0.5000000000000004441 ) ;
#65343=CARTESIAN_POINT ( 'NONE',  ( 5.512442546757785777, 154.3838412429289804, 7.633710229762624699 ) ) ;
#65344=DIRECTION ( 'NONE',  ( 1.000000000000000000, 0.000000000000000000, 0.000000000000000000 ) ) ;
#65346=MECHANICAL_DESIGN_GEOMETRIC_PRESENTATION_REPRESENTATION('',(#12505),#46265);
#65350=DIRECTION ( 'NONE',  ( -0.000000000000000000, -0.000000000000000000, -1.000000000000000000 ) ) ;
#65353=STYLED_ITEM ( 'NONE', ( #1060 ), #11966 ) ;
#65354=ADVANCED_FACE ( 'NONE', ( #67946 ), #5264, .F. ) ;
#65355=CYLINDRICAL_SURFACE ( 'NONE', #14718, 0.5000000000000004441 ) ;
#65356=EDGE_CURVE ( 'NONE', #18512, #56203, #17661, .T. ) ;
#65357=CARTESIAN_POINT ( 'NONE',  ( 45.00000000000000000, 9.639620389971918613, -6.999999999999999112 ) ) ;
#65360=ORIENTED_EDGE ( 'NONE', *, *, #6287, .F. ) ;
#65361=DIRECTION ( 'NONE',  ( 1.000000000000000000, 0.000000000000000000, 0.000000000000000000 ) ) ;
#65362=TOROIDAL_SURFACE ( 'NONE', #44082, 1.000000000000000000, 0.5000000000000000000 ) ;
#65365=EDGE_CURVE ( 'NONE', #9536, #56195, #13148, .T. ) ;
#65366=CARTESIAN_POINT ( 'NONE',  ( 71.50000000000000000, 14.49137674618942562, -9.500000000000000000 ) ) ;
#65370=EDGE_CURVE ( 'NONE', #11547, #69397, #3148, .T. ) ;
#65373=ORIENTED_EDGE ( 'NONE', *, *, #30032, .T. ) ;
#65374=CYLINDRICAL_SURFACE ( 'NONE', #50052, 0.5000000000000000000 ) ;
#65375=AXIS2_PLACEMENT_3D ( 'NONE', #50797, #24726, #12442 ) ;
#65376=ORIENTED_EDGE ( 'NONE', *, *, #34252, .T. ) ;
#65380=CARTESIAN_POINT ( 'NONE',  ( 3.094860106618431583, 156.0949999999999989, 9.525000000000000355 ) ) ;
#65382=EDGE_LOOP ( 'NONE', ( #51359, #61290, #35356, #68614 ) ) ;
#65383=ORIENTED_EDGE ( 'NONE', *, *, #59182, .F. ) ;
#65387=SURFACE_SIDE_STYLE ('',( #22830 ) ) ;
#65388=CARTESIAN_POINT ( 'NONE',  ( -67.99999999999998579, -2.024042244987997205E-14, -10.49999999999999822 ) ) ;
#65390=CARTESIAN_POINT ( 'NONE',  ( 6.826472737025121695, 137.4929263765338305, -4.959722759717905660 ) ) ;
#65394=ADVANCED_FACE ( 'NONE', ( #41562 ), #19014, .F. ) ;
#65397=EDGE_LOOP ( 'NONE', ( #52359, #22483, #34073, #65208 ) ) ;
#65400=DIRECTION ( 'NONE',  ( -0.000000000000000000, 1.000000000000000000, 0.000000000000000000 ) ) ;
#65401=LINE ( 'NONE', #7357, #6327 ) ;
#65404=FACE_OUTER_BOUND ( 'NONE', #37143, .T. ) ;
#65405=ORIENTED_EDGE ( 'NONE', *, *, #61128, .T. ) ;
#65406=AXIS2_PLACEMENT_3D ( 'NONE', #60520, #17328, #10973 ) ;
#65412=CIRCLE ( 'NONE', #46364, 0.5000000000000004441 ) ;
#65413=ORIENTED_EDGE ( 'NONE', *, *, #267, .T. ) ;
#65414=CARTESIAN_POINT ( 'NONE',  ( -45.91046261216711599, 9.422709103004114795, 3.407326739365095225 ) ) ;
#65419=( NAMED_UNIT ( * ) PLANE_ANGLE_UNIT ( ) SI_UNIT ( $, .RADIAN. ) );
#65421=( GEOMETRIC_REPRESENTATION_CONTEXT ( 3 ) GLOBAL_UNCERTAINTY_ASSIGNED_CONTEXT ( ( #20922 ) ) GLOBAL_UNIT_ASSIGNED_CONTEXT ( ( #37755, #4633, #43028 ) ) REPRESENTATION_CONTEXT ( 'NONE', 'WORKASPACE' ) );
#65423=DIRECTION ( 'NONE',  ( -1.000000000000000000, 0.000000000000000000, 0.000000000000000000 ) ) ;
#65429=DIRECTION ( 'NONE',  ( 0.000000000000000000, -1.000000000000000000, 0.000000000000000000 ) ) ;
#65431=CARTESIAN_POINT ( 'NONE',  ( 10.01517768586949231, 153.6949999999999932, 1.839758294383810543E-15 ) ) ;
#65434=EDGE_CURVE ( 'NONE', #5399, #21155, #53584, .T. ) ;
#65435=PRESENTATION_STYLE_ASSIGNMENT (( #44380 ) ) ;
#65437=CARTESIAN_POINT ( 'NONE',  ( 9.827790563157511022E-16, 87.30187232391182306, -8.025000000000000355 ) ) ;
#65438=EDGE_LOOP ( 'NONE', ( #30661, #52464, #11409, #48561 ) ) ;
#65447=PRESENTATION_STYLE_ASSIGNMENT (( #16259 ) ) ;
#65459=VERTEX_POINT ( 'NONE', #15866 ) ;
#65460=ORIENTED_EDGE ( 'NONE', *, *, #46976, .T. ) ;
#65462=ORIENTED_EDGE ( 'NONE', *, *, #34317, .T. ) ;
#65465=CARTESIAN_POINT ( 'NONE',  ( 5.598654528085805993, 126.2449999999999903, 7.705886871421374629 ) ) ;
#65468=FACE_OUTER_BOUND ( 'NONE', #19855, .T. ) ;
#65469=CARTESIAN_POINT ( 'NONE',  ( -8.102448949553179958, 135.0050000000000239, -5.886773742842749790 ) ) ;
#65471=CARTESIAN_POINT ( 'NONE',  ( 40.95793942982998459, 108.0317815798972418, -3.561444987364487780 ) ) ;
#65473=CARTESIAN_POINT ( 'NONE',  ( -9.058813317711338797, 156.4549999999999841, 2.943386871421373563 ) ) ;
#65474=DIRECTION ( 'NONE',  ( 1.000000000000000000, 0.000000000000000000, 0.000000000000000000 ) ) ;
#65476=( GEOMETRIC_REPRESENTATION_CONTEXT ( 3 ) GLOBAL_UNCERTAINTY_ASSIGNED_CONTEXT ( ( #31296 ) ) GLOBAL_UNIT_ASSIGNED_CONTEXT ( ( #54723, #55072, #11483 ) ) REPRESENTATION_CONTEXT ( 'NONE', 'WORKASPACE' ) );
#65484=VERTEX_POINT ( 'NONE', #15192 ) ;
#65486=( GEOMETRIC_REPRESENTATION_CONTEXT ( 3 ) GLOBAL_UNCERTAINTY_ASSIGNED_CONTEXT ( ( #66596 ) ) GLOBAL_UNIT_ASSIGNED_CONTEXT ( ( #28087, #12266, #29506 ) ) REPRESENTATION_CONTEXT ( 'NONE', 'WORKASPACE' ) );
#65487=( LENGTH_UNIT ( ) NAMED_UNIT ( * ) SI_UNIT ( .MILLI., .METRE. ) );
#65488=FACE_OUTER_BOUND ( 'NONE', #31352, .T. ) ;
#65491=SURFACE_STYLE_FILL_AREA ( #64801 ) ;
#65498=CARTESIAN_POINT ( 'NONE',  ( 0.000000000000000000, 145.0570736234661524, -8.025000000000000355 ) ) ;
#65499=DIRECTION ( 'NONE',  ( 0.000000000000000000, 1.000000000000000000, 0.000000000000000000 ) ) ;
#65502=CARTESIAN_POINT ( 'NONE',  ( -75.00000000000000000, 7.952411872162292283, -6.456960098911577184 ) ) ;
#65506=CARTESIAN_POINT ( 'NONE',  ( -3.094860106618434248, 128.7949999999999875, 9.525000000000000355 ) ) ;
#65510=AXIS2_PLACEMENT_3D ( 'NONE', #53791, #48923, #622 ) ;
#65511=CARTESIAN_POINT ( 'NONE',  ( 34.99999999999992895, 112.4999999999999858, 9.500000000000000000 ) ) ;
#65516=TOROIDAL_SURFACE ( 'NONE', #4859, 1.000000000000000000, 0.5000000000000000000 ) ;
#65519=COLOUR_RGB ( '', 0.72549020, 0.75294118, 0.79215686) ;
#65522=CARTESIAN_POINT ( 'NONE',  ( 0.000000000000000000, 149.9999999999999716, 0.000000000000000000 ) ) ;
#65526=SURFACE_SIDE_STYLE ('',( #32827 ) ) ;
#65531=STYLED_ITEM ( 'NONE', ( #35490 ), #26459 ) ;
#65532=EDGE_CURVE ( 'NONE', #22472, #18963, #68258, .T. ) ;
#65535=DIRECTION ( 'NONE',  ( 0.000000000000000000, 0.000000000000000000, 1.000000000000000000 ) ) ;
#65537=EDGE_LOOP ( 'NONE', ( #36627, #13761, #39496, #12435 ) ) ;
#65543=AXIS2_PLACEMENT_3D ( 'NONE', #26949, #11848, #185 ) ;
#65546=CARTESIAN_POINT ( 'NONE',  ( 0.000000000000000000, 148.0570736234661524, -8.025000000000000355 ) ) ;
#65547=CIRCLE ( 'NONE', #34114, 0.5000000000000004441 ) ;
#65551=CARTESIAN_POINT ( 'NONE',  ( -44.99999999999977973, 146.4999999999999716, 7.500000000000000000 ) ) ;
#65556=TOROIDAL_SURFACE ( 'NONE', #17296, 16.44999999999999574, 0.5000000000000000000 ) ;
#65560=COLOUR_RGB ( '', 0.08235294, 0.09019608, 0.10196078) ;
#65561=DIRECTION ( 'NONE',  ( -1.156482317317873451E-16, -1.000000000000000000, 0.000000000000000000 ) ) ;
#65562=CARTESIAN_POINT ( 'NONE',  ( -45.87390969075753588, 9.272074904602295220, -6.224541297626196013 ) ) ;
#65564=DIRECTION ( 'NONE',  ( 1.000000000000000000, 0.000000000000000000, 0.000000000000000000 ) ) ;
#65567=MECHANICAL_DESIGN_GEOMETRIC_PRESENTATION_REPRESENTATION('',(#16200),#4911);
#65568=DIRECTION ( 'NONE',  ( 0.000000000000000000, 0.000000000000000000, 1.000000000000000000 ) ) ;
#65577=CIRCLE ( 'NONE', #40911, 13.00000000000000533 ) ;
#65578=CARTESIAN_POINT ( 'NONE',  ( -5.598654528085806881, 133.7450000000000045, -7.705886871421374629 ) ) ;
#65582=VERTEX_POINT ( 'NONE', #23201 ) ;
#65586=STYLED_ITEM ( 'NONE', ( #46953 ), #62992 ) ;
#65591=EDGE_CURVE ( 'NONE', #42583, #45809, #65045, .T. ) ;
#65592=VECTOR ( 'NONE', #33011, 1000.000000000000000 ) ;
#65598=COLOUR_RGB ( '', 0.31764706, 0.68627451, 0.89019608) ;
#65599=SURFACE_STYLE_FILL_AREA ( #65248 ) ;
#65604=AXIS2_PLACEMENT_3D ( 'NONE', #33517, #45152, #32832 ) ;
#65608=COLOUR_RGB ( '', 0.66274510, 0.83137255, 0.94901961) ;
#65610=DIRECTION ( 'NONE',  ( -0.000000000000000000, -1.000000000000000000, 0.000000000000000000 ) ) ;
#65613=( BOUNDED_CURVE ( )  B_SPLINE_CURVE ( 2, ( #60592, #60946, #12765, #51122, #34237, #56021, #2868, #55691, #12410, #67283, #33870 ),
 .UNSPECIFIED., .F., .F. ) 
 B_SPLINE_CURVE_WITH_KNOTS ( ( 3, 2, 2, 2, 2, 3 ),
 ( 0.2352941176470587370, 0.2411764705882352144, 0.2470588235294116919, 0.2529411764705881693, 0.2588235294117646745, 0.2647058823529411242 ),
 .UNSPECIFIED. ) 
 CURVE ( )  GEOMETRIC_REPRESENTATION_ITEM ( )  RATIONAL_B_SPLINE_CURVE ( ( 1.000000000000000666, 0.9510565162951529761, 1.000000000000000000, 0.9510565162951535312, 1.000000000000000000, 0.9510565162951535312, 1.000000000000000000, 0.9510565162951535312, 1.000000000000000000, 0.9510565162951539753, 0.9999999999999995559 ) ) 
 REPRESENTATION_ITEM ( '' )  );
#65619=DIRECTION ( 'NONE',  ( -1.000000000000000000, 0.000000000000000000, 0.000000000000000000 ) ) ;
#65621=( LENGTH_UNIT ( ) NAMED_UNIT ( * ) SI_UNIT ( .MILLI., .METRE. ) );
#65624=CARTESIAN_POINT ( 'NONE',  ( -47.50000000000000000, 99.99999999999992895, 9.500000000000000000 ) ) ;
#65626=STYLED_ITEM ( 'NONE', ( #52518 ), #2568 ) ;
#65627=CARTESIAN_POINT ( 'NONE',  ( 2.607480562269076430, 123.9070736234661467, -8.025000000000000355 ) ) ;
#65630=CARTESIAN_POINT ( 'NONE',  ( 75.00000000000000000, 19.70845863561317657, -6.466567654931034248 ) ) ;
#65640=CARTESIAN_POINT ( 'NONE',  ( 7.632228543268607446, 149.0429263765338135, 2.479861379858954606 ) ) ;
#65642=ORIENTED_EDGE ( 'NONE', *, *, #3623, .F. ) ;
#65643=ADVANCED_FACE ( 'NONE', ( #7691 ), #48934, .F. ) ;
#65645=DIRECTION ( 'NONE',  ( -1.000000000000000000, -0.000000000000000000, -0.000000000000000000 ) ) ;
#65647=ORIENTED_EDGE ( 'NONE', *, *, #57916, .F. ) ;
#65649=FILL_AREA_STYLE_COLOUR ( '', #54870 ) ;
#65656=SURFACE_STYLE_USAGE ( .BOTH. , #16117 ) ;
#65659=DIRECTION ( 'NONE',  ( 1.000000000000000000, 0.000000000000000000, 0.000000000000000000 ) ) ;
#65661=CARTESIAN_POINT ( 'NONE',  ( -0.9728900412908211282, 153.0000000000000000, -7.965808808122195828 ) ) ;
#65662=ORIENTED_EDGE ( 'NONE', *, *, #68224, .T. ) ;
#65665=TOROIDAL_SURFACE ( 'NONE', #48846, 12.50000000000000000, 0.5000000000000000000 ) ;
#65676=SURFACE_STYLE_USAGE ( .BOTH. , #33330 ) ;
#65677=AXIS2_PLACEMENT_3D ( 'NONE', #64363, #10901, #55168 ) ;
#65678=CARTESIAN_POINT ( 'NONE',  ( 44.32257855570070149, 10.24209864716889307, 3.524404701559999520 ) ) ;
#65682=AXIS2_PLACEMENT_3D ( 'NONE', #16909, #6650, #49252 ) ;
#65684=CARTESIAN_POINT ( 'NONE',  ( 3.094860106618431583, 151.2049999999999841, 9.525000000000000355 ) ) ;
#65688=STYLED_ITEM ( 'NONE', ( #46218 ), #62491 ) ;
#65689=CARTESIAN_POINT ( 'NONE',  ( 5.812336001418906051, 154.3979462032312995, 7.425621158966782431 ) ) ;
#65690=UNCERTAINTY_MEASURE_WITH_UNIT (LENGTH_MEASURE( 1.000000000000000082E-05 ), #7244, 'distance_accuracy_value', 'NONE');
#65696=CARTESIAN_POINT ( 'NONE',  ( -23.21231517720798010, 1.797044900979284448E-15, -9.500000000000000000 ) ) ;
#65697=CIRCLE ( 'NONE', #7263, 5.000000000000004441 ) ;
#65701=CARTESIAN_POINT ( 'NONE',  ( 24.21231517720798010, 113.4999999999999858, -9.500000000000000000 ) ) ;
#65702=CARTESIAN_POINT ( 'NONE',  ( 71.49999999999998579, 64.07124727947029896, -7.000000000000000000 ) ) ;
#65705=MECHANICAL_DESIGN_GEOMETRIC_PRESENTATION_REPRESENTATION('',(#8441),#35399);
#65709=SURFACE_STYLE_USAGE ( .BOTH. , #23477 ) ;
#65712=EDGE_LOOP ( 'NONE', ( #58646, #57954, #48919, #32563 ) ) ;
#65715=PRESENTATION_STYLE_ASSIGNMENT (( #16863 ) ) ;
#65717=FILL_AREA_STYLE ('',( #44318 ) ) ;
#65719=ORIENTED_EDGE ( 'NONE', *, *, #29118, .T. ) ;
#65721=CARTESIAN_POINT ( 'NONE',  ( -8.102448949553181734, 157.8950000000000102, -5.886773742842749790 ) ) ;
#65723=ORIENTED_EDGE ( 'NONE', *, *, #8813, .T. ) ;
#65724=EDGE_CURVE ( 'NONE', #23416, #35108, #9103, .T. ) ;
#65726=CARTESIAN_POINT ( 'NONE',  ( -74.20344633242609689, 8.974374905500289046, -6.364158535394771832 ) ) ;
#65727=CARTESIAN_POINT ( 'NONE',  ( -40.49999999999998579, 107.7459666924148394, -3.000000000000000444 ) ) ;
#65729=CARTESIAN_POINT ( 'NONE',  ( -8.437984349512095861, 138.6929263765338192, -5.166775262442723748E-16 ) ) ;
#65732=( GEOMETRIC_REPRESENTATION_CONTEXT ( 3 ) GLOBAL_UNCERTAINTY_ASSIGNED_CONTEXT ( ( #10162 ) ) GLOBAL_UNIT_ASSIGNED_CONTEXT ( ( #41249, #14472, #17453 ) ) REPRESENTATION_CONTEXT ( 'NONE', 'WORKASPACE' ) );
#65741=DIRECTION ( 'NONE',  ( 1.156482317317873451E-16, -1.000000000000000000, -0.000000000000000000 ) ) ;
#65742=DIRECTION ( 'NONE',  ( 0.9994052928406508274, 0.03448275862069643399, -0.000000000000000000 ) ) ;
#65755=EDGE_LOOP ( 'NONE', ( #54778, #11836, #16442, #50354 ) ) ;
#65756=CARTESIAN_POINT ( 'NONE',  ( -45.89905495969589566, 9.405628579224391217, 3.101891717392576187 ) ) ;
#65760=CIRCLE ( 'NONE', #66878, 23.00000000000000000 ) ;
#65765=DIRECTION ( 'NONE',  ( 0.000000000000000000, 0.000000000000000000, -1.000000000000000000 ) ) ;
#65767=( GEOMETRIC_REPRESENTATION_CONTEXT ( 3 ) GLOBAL_UNCERTAINTY_ASSIGNED_CONTEXT ( ( #39087 ) ) GLOBAL_UNIT_ASSIGNED_CONTEXT ( ( #68008, #9616, #9948 ) ) REPRESENTATION_CONTEXT ( 'NONE', 'WORKASPACE' ) );
#65769=LINE ( 'NONE', #2737, #18549 ) ;
#65770=VERTEX_POINT ( 'NONE', #25264 ) ;
#65772=EDGE_CURVE ( 'NONE', #68774, #34213, #18927, .T. ) ;
#65773=MECHANICAL_DESIGN_GEOMETRIC_PRESENTATION_REPRESENTATION('',(#8499),#36606);
#65776=CARTESIAN_POINT ( 'NONE',  ( 71.50000000000000000, 35.92875272052971525, -7.500000000000000000 ) ) ;
#65777=ADVANCED_FACE ( 'NONE', ( #37255 ), #58657, .F. ) ;
#65779=CARTESIAN_POINT ( 'NONE',  ( 3.094860106618435136, 154.2949999999999875, -9.525000000000000355 ) ) ;
#65781=PRESENTATION_STYLE_ASSIGNMENT (( #54176 ) ) ;
#65782=CARTESIAN_POINT ( 'NONE',  ( -6.826472737025120807, 141.3929263765338078, -4.959722759717907437 ) ) ;
#65788=FILL_AREA_STYLE_COLOUR ( '', #62326 ) ;
#65789=ORIENTED_EDGE ( 'NONE', *, *, #4593, .T. ) ;
#65795=DIRECTION ( 'NONE',  ( -1.000000000000000000, 0.000000000000000000, 0.000000000000000000 ) ) ;
#65797=ORIENTED_EDGE ( 'NONE', *, *, #15467, .T. ) ;
#65798=MECHANICAL_DESIGN_GEOMETRIC_PRESENTATION_REPRESENTATION('',(#57929),#63582);
#65799=EDGE_CURVE ( 'NONE', #32643, #30766, #58317, .T. ) ;
#65801=SPHERICAL_SURFACE ( 'NONE', #11683, 0.5000000000000000000 ) ;
#65817=CARTESIAN_POINT ( 'NONE',  ( 0.000000000000000000, 130.4449999999999648, -9.525000000000000355 ) ) ;
#65821=CARTESIAN_POINT ( 'NONE',  ( 9.058813317711337021, 127.6549999999999869, 2.943386871421375783 ) ) ;
#65824=CARTESIAN_POINT ( 'NONE',  ( 41.21596654039887397, 107.8367875949926429, -3.443506282739404512 ) ) ;
#65825=ORIENTED_EDGE ( 'NONE', *, *, #4023, .T. ) ;
#65826=CARTESIAN_POINT ( 'NONE',  ( 5.598654528085809545, 158.2549999999999670, -7.705886871421373741 ) ) ;
#65828=UNCERTAINTY_MEASURE_WITH_UNIT (LENGTH_MEASURE( 1.000000000000000082E-05 ), #41809, 'distance_accuracy_value', 'NONE');
#65829=FACE_OUTER_BOUND ( 'NONE', #12336, .T. ) ;
#65831=LINE ( 'NONE', #13049, #41078 ) ;
#65834=ORIENTED_EDGE ( 'NONE', *, *, #28886, .T. ) ;
#65836=( NAMED_UNIT ( * ) PLANE_ANGLE_UNIT ( ) SI_UNIT ( $, .RADIAN. ) );
#65839=UNCERTAINTY_MEASURE_WITH_UNIT (LENGTH_MEASURE( 1.000000000000000082E-05 ), #55583, 'distance_accuracy_value', 'NONE');
#65842=( NAMED_UNIT ( * ) SI_UNIT ( $, .STERADIAN. ) SOLID_ANGLE_UNIT ( ) );
#65843=CARTESIAN_POINT ( 'NONE',  ( 44.99999999999977973, 146.9999999999999716, 7.000000000000000000 ) ) ;
#65845=EDGE_LOOP ( 'NONE', ( #32054, #26971, #12776 ) ) ;
#65852=ORIENTED_EDGE ( 'NONE', *, *, #13167, .F. ) ;
#65854=( GEOMETRIC_REPRESENTATION_CONTEXT ( 3 ) GLOBAL_UNCERTAINTY_ASSIGNED_CONTEXT ( ( #20805 ) ) GLOBAL_UNIT_ASSIGNED_CONTEXT ( ( #34571, #62360, #51126 ) ) REPRESENTATION_CONTEXT ( 'NONE', 'WORKASPACE' ) );
#65858=VERTEX_POINT ( 'NONE', #53402 ) ;
#65859=CARTESIAN_POINT ( 'NONE',  ( 0.000000000000000000, 142.0570736234661524, -8.025000000000000355 ) ) ;
#65860=CARTESIAN_POINT ( 'NONE',  ( 21.02379604162863913, 109.9999999999999858, 10.50000000000000000 ) ) ;
#65863=CARTESIAN_POINT ( 'NONE',  ( 9.058813317711337021, 132.5449999999999875, 2.943386871421375783 ) ) ;
#65873=DIRECTION ( 'NONE',  ( -0.000000000000000000, -0.000000000000000000, -1.000000000000000000 ) ) ;
#65875=DIRECTION ( 'NONE',  ( -0.000000000000000000, -0.000000000000000000, -1.000000000000000000 ) ) ;
#65876=EDGE_LOOP ( 'NONE', ( #16091, #54020, #605, #18352 ) ) ;
#65878=EDGE_CURVE ( 'NONE', #16768, #50360, #60343, .T. ) ;
#65880=CARTESIAN_POINT ( 'NONE',  ( -45.86904680146955116, 9.253562910438322575, 6.241030289661793518 ) ) ;
#65881=DIRECTION ( 'NONE',  ( -0.000000000000000000, -0.000000000000000000, -1.000000000000000000 ) ) ;
#65884=( NAMED_UNIT ( * ) SI_UNIT ( $, .STERADIAN. ) SOLID_ANGLE_UNIT ( ) );
#65890=DIRECTION ( 'NONE',  ( 1.000000000000000000, 0.000000000000000000, 0.000000000000000000 ) ) ;
#65891=SURFACE_SIDE_STYLE ('',( #66587 ) ) ;
#65894=( NAMED_UNIT ( * ) SI_UNIT ( $, .STERADIAN. ) SOLID_ANGLE_UNIT ( ) );
#65895=CARTESIAN_POINT ( 'NONE',  ( -2.607480562269075097, 149.4070736234661751, 8.025000000000000355 ) ) ;
#65896=ORIENTED_EDGE ( 'NONE', *, *, #3633, .T. ) ;
#65898=CARTESIAN_POINT ( 'NONE',  ( 9.058813317711337021, 127.6549999999999869, 2.943386871421375783 ) ) ;
#65900=CIRCLE ( 'NONE', #69279, 5.499999999999976907 ) ;
#65901=FILL_AREA_STYLE_COLOUR ( '', #28204 ) ;
#65905=SURFACE_STYLE_FILL_AREA ( #56027 ) ;
#65906=VERTEX_POINT ( 'NONE', #20691 ) ;
#65907=FACE_OUTER_BOUND ( 'NONE', #6438, .T. ) ;
#65913=CARTESIAN_POINT ( 'NONE',  ( -45.00000000000000000, 8.421502636539827336, -6.236752812775022470 ) ) ;
#65915=DIRECTION ( 'NONE',  ( -0.000000000000000000, 1.000000000000000000, 0.000000000000000000 ) ) ;
#65922=ORIENTED_EDGE ( 'NONE', *, *, #43895, .F. ) ;
#65924=SURFACE_SIDE_STYLE ('',( #49413 ) ) ;
#65928=CARTESIAN_POINT ( 'NONE',  ( -23.71231517720798010, 117.4999999999999716, 10.00000000000000000 ) ) ;
#65929=CARTESIAN_POINT ( 'NONE',  ( -3.094860106618432471, 136.5949999999999989, -9.525000000000000355 ) ) ;
#65931=EDGE_CURVE ( 'NONE', #47977, #26603, #23302, .T. ) ;
#65932=DIRECTION ( 'NONE',  ( 1.000000000000000000, 0.000000000000000000, 0.000000000000000000 ) ) ;
#65934=( NAMED_UNIT ( * ) PLANE_ANGLE_UNIT ( ) SI_UNIT ( $, .RADIAN. ) );
#65935=( NAMED_UNIT ( * ) SI_UNIT ( $, .STERADIAN. ) SOLID_ANGLE_UNIT ( ) );
#65939=VECTOR ( 'NONE', #61723, 1000.000000000000114 ) ;
#65940=CARTESIAN_POINT ( 'NONE',  ( 45.50000000000000000, 9.639620389971918613, -6.999999999999999112 ) ) ;
#65946=DIRECTION ( 'NONE',  ( 0.000000000000000000, 0.000000000000000000, 1.000000000000000000 ) ) ;
#65957=CYLINDRICAL_SURFACE ( 'NONE', #41375, 8.025000000000000355 ) ;
#65965=DIRECTION ( 'NONE',  ( 1.000000000000000000, 0.000000000000000000, 0.000000000000000000 ) ) ;
#65966=CARTESIAN_POINT ( 'NONE',  ( -7.632228543268608334, 124.9570736234661581, 2.479861379858952830 ) ) ;
#65967=DIRECTION ( 'NONE',  ( 0.000000000000000000, 1.000000000000000000, -0.000000000000000000 ) ) ;
#65968=PRESENTATION_STYLE_ASSIGNMENT (( #22370 ) ) ;
#65969=SURFACE_SIDE_STYLE ('',( #33959 ) ) ;
#65971=VERTEX_POINT ( 'NONE', #1593 ) ;
#65975=ORIENTED_EDGE ( 'NONE', *, *, #41671, .F. ) ;
#65981=ORIENTED_EDGE ( 'NONE', *, *, #14692, .F. ) ;
#65984=ADVANCED_FACE ( 'NONE', ( #66010 ), #33653, .F. ) ;
#65985=PRESENTATION_STYLE_ASSIGNMENT (( #64938 ) ) ;
#65987=CARTESIAN_POINT ( 'NONE',  ( -9.827790563157511022E-16, 160.4429263765338192, 8.025000000000000355 ) ) ;
#65989=AXIS2_PLACEMENT_3D ( 'NONE', #66285, #44877, #53996 ) ;
#65991=VECTOR ( 'NONE', #10550, 1000.000000000000000 ) ;
#65992=ADVANCED_FACE ( 'NONE', ( #12533 ), #22409, .T. ) ;
#65998=FACE_OUTER_BOUND ( 'NONE', #10876, .T. ) ;
#66001=SURFACE_SIDE_STYLE ('',( #64014 ) ) ;
#66006=DIRECTION ( 'NONE',  ( -0.000000000000000000, 1.000000000000000000, -0.000000000000000000 ) ) ;
#66008=CARTESIAN_POINT ( 'NONE',  ( 8.437984349512095861, 122.1929263765337907, 1.550032578732816828E-15 ) ) ;
#66009=SURFACE_STYLE_FILL_AREA ( #2978 ) ;
#66010=FACE_OUTER_BOUND ( 'NONE', #41560, .T. ) ;
#66017=ORIENTED_EDGE ( 'NONE', *, *, #186, .F. ) ;
#66019=AXIS2_PLACEMENT_3D ( 'NONE', #18183, #64974, #881 ) ;
#66020=PRESENTATION_STYLE_ASSIGNMENT (( #49868 ) ) ;
#66026=CARTESIAN_POINT ( 'NONE',  ( 8.102448949553181734, 151.5049999999999955, 5.886773742842750679 ) ) ;
#66029=CARTESIAN_POINT ( 'NONE',  ( 2.128399401614408669E-13, 154.1464374838464266, 9.171437483846471395 ) ) ;
#66032=DIRECTION ( 'NONE',  ( 1.000000000000000000, 0.000000000000000000, 0.000000000000000000 ) ) ;
#66034=AXIS2_PLACEMENT_3D ( 'NONE', #25851, #24452, #20227 ) ;
#66035=DIRECTION ( 'NONE',  ( -0.8946296187927070820, 0.000000000000000000, 0.4468085106382997385 ) ) ;
#66044=EDGE_LOOP ( 'NONE', ( #37302, #58780, #60078, #65789 ) ) ;
#66048=EDGE_CURVE ( 'NONE', #49280, #45911, #39160, .T. ) ;
#66062=CARTESIAN_POINT ( 'NONE',  ( 4.716976649647096842, 139.7429263765338305, 6.492361379858953896 ) ) ;
#66063=DIRECTION ( 'NONE',  ( 0.000000000000000000, 0.000000000000000000, 1.000000000000000000 ) ) ;
#66065=VECTOR ( 'NONE', #69050, 1000.000000000000000 ) ;
#66068=DIRECTION ( 'NONE',  ( 0.000000000000000000, 0.000000000000000000, 1.000000000000000000 ) ) ;
#66072=VERTEX_POINT ( 'NONE', #46701 ) ;
#66075=DIRECTION ( 'NONE',  ( 0.000000000000000000, -1.000000000000000000, 0.000000000000000000 ) ) ;
#66076=CIRCLE ( 'NONE', #14408, 1.000000000000000888 ) ;
#66079=EDGE_LOOP ( 'NONE', ( #59285, #31006, #39802, #39147, #13100, #66418 ) ) ;
#66083=DIRECTION ( 'NONE',  ( 0.000000000000000000, 0.000000000000000000, -1.000000000000000000 ) ) ;
#66088=CARTESIAN_POINT ( 'NONE',  ( -45.21668476461162811, 8.382617247524210669, 3.000000000000000444 ) ) ;
#66090=ORIENTED_EDGE ( 'NONE', *, *, #5314, .T. ) ;
#66091=CARTESIAN_POINT ( 'NONE',  ( -12.72792206135785698, 149.9999999999999716, -10.00000000000000000 ) ) ;
#66103=CARTESIAN_POINT ( 'NONE',  ( 8.102448949553183510, 119.1049999999999756, -5.886773742842746238 ) ) ;
#66107=DIRECTION ( 'NONE',  ( 0.000000000000000000, 0.000000000000000000, -1.000000000000000000 ) ) ;
#66110=( BOUNDED_SURFACE ( )  B_SPLINE_SURFACE ( 3, 2, ( 
 ( #57363, #8501, #56674 ),
 ( #29932, #67938, #20419 ),
 ( #41556, #41923, #30610 ),
 ( #9190, #15187, #57012 ),
 ( #58073, #3497, #36653 ),
 ( #52113, #26025, #68974 ),
 ( #25350, #51394, #3141 ),
 ( #24632, #67573, #40874 ),
 ( #62293, #8827, #25000 ),
 ( #30253, #51755, #46509 ) ),
 .UNSPECIFIED., .F., .F., .T. ) 
 B_SPLINE_SURFACE_WITH_KNOTS ( ( 4, 2, 2, 2, 4 ),
 ( 3, 3 ),
 ( 4.712388980384689674, 5.105088062083414258, 5.497787143782137953, 5.890486225480861648, 6.283185307179586232 ),
 ( 0.000000000000000000, 1.000000000000000000 ),
 .UNSPECIFIED. ) 
 GEOMETRIC_REPRESENTATION_ITEM ( )  RATIONAL_B_SPLINE_SURFACE ( (
 ( 1.000000000000000000, 0.7071067811865482389, 1.000000000000000000),
 ( 1.000000000000000000, 0.7217502572880009071, 1.000000000000000000),
 ( 1.000000000000000000, 0.7359001690391617778, 1.000000000000000000),
 ( 1.000000000000000000, 0.7614408922481175068, 1.000000000000000000),
 ( 1.000000000000000000, 0.7728233248393500121, 1.000000000000000000),
 ( 1.000000000000000000, 0.7915339219236553481, 1.000000000000000000),
 ( 1.000000000000000000, 0.7988629633398777186, 1.000000000000000000),
 ( 1.000000000000000000, 0.8087168080150187732, 1.000000000000000000),
 ( 1.000000000000000000, 0.8112499556556335145, 1.000000000000000000),
 ( 1.000000000000000000, 0.8112421851755602376, 1.000000000000000000) ) ) 
 REPRESENTATION_ITEM ( '' )  SURFACE ( )  );
#66112=DIRECTION ( 'NONE',  ( -0.000000000000000000, 0.000000000000000000, 1.000000000000000000 ) ) ;
#66114=ORIENTED_EDGE ( 'NONE', *, *, #33297, .F. ) ;
#66119=STYLED_ITEM ( 'NONE', ( #32213 ), #51092 ) ;
#66120=EDGE_CURVE ( 'NONE', #9275, #64306, #40045, .T. ) ;
#66122=FACE_OUTER_BOUND ( 'NONE', #16023, .T. ) ;
#66123=EDGE_LOOP ( 'NONE', ( #31110, #44317, #28219, #23153 ) ) ;
#66124=CIRCLE ( 'NONE', #30162, 0.4999999999999994449 ) ;
#66125=ORIENTED_EDGE ( 'NONE', *, *, #20001, .T. ) ;
#66131=VERTEX_POINT ( 'NONE', #8330 ) ;
#66134=EDGE_CURVE ( 'NONE', #29454, #28945, #820, .T. ) ;
#66137=CARTESIAN_POINT ( 'NONE',  ( 0.000000000000000000, 152.9999999999999716, 0.000000000000000000 ) ) ;
#66142=CARTESIAN_POINT ( 'NONE',  ( 10.01517768586949231, 129.6949999999999648, 1.839758294383810543E-15 ) ) ;
#66143=ORIENTED_EDGE ( 'NONE', *, *, #56790, .T. ) ;
#66145=CARTESIAN_POINT ( 'NONE',  ( -3.094860106618434248, 141.9050000000000011, 9.525000000000000355 ) ) ;
#66146=EDGE_CURVE ( 'NONE', #19166, #52175, #58203, .T. ) ;
#66148=VECTOR ( 'NONE', #66821, 1000.000000000000000 ) ;
#66149=( NAMED_UNIT ( * ) PLANE_ANGLE_UNIT ( ) SI_UNIT ( $, .RADIAN. ) );
#66151=CARTESIAN_POINT ( 'NONE',  ( 10.01517768586949231, 157.8050000000000068, 1.839758294383810543E-15 ) ) ;
#66155=VECTOR ( 'NONE', #59602, 1000.000000000000000 ) ;
#66158=ORIENTED_EDGE ( 'NONE', *, *, #38697, .F. ) ;
#66159=EDGE_CURVE ( 'NONE', #44595, #68002, #42450, .T. ) ;
#66163=CARTESIAN_POINT ( 'NONE',  ( 20.05202421861157447, 114.9999999999999432, 10.44839000960907960 ) ) ;
#66164=CARTESIAN_POINT ( 'NONE',  ( 15.98999599679679839, 118.4999999999999716, 9.500000000000000000 ) ) ;
#66167=DIRECTION ( 'NONE',  ( 0.000000000000000000, -1.000000000000000000, 0.000000000000000000 ) ) ;
#66168=FILL_AREA_STYLE ('',( #39143 ) ) ;
#66170=PRESENTATION_STYLE_ASSIGNMENT (( #55272 ) ) ;
#66171=SURFACE_STYLE_FILL_AREA ( #2452 ) ;
#66172=ORIENTED_EDGE ( 'NONE', *, *, #25967, .F. ) ;
#66175=CARTESIAN_POINT ( 'NONE',  ( -44.99928706149596280, 9.682046777738220200, -3.525278482175732808 ) ) ;
#66178=ORIENTED_EDGE ( 'NONE', *, *, #23418, .T. ) ;
#66181=DIRECTION ( 'NONE',  ( -0.000000000000000000, -0.000000000000000000, 1.000000000000000000 ) ) ;
#66185=EDGE_LOOP ( 'NONE', ( #61648, #63816, #58162, #68219 ) ) ;
#66186=PLANE ( 'NONE',  #49502 ) ;
#66189=CARTESIAN_POINT ( 'NONE',  ( -9.058813317711337021, 140.0449999999999875, -2.943386871421374895 ) ) ;
#66192=EDGE_CURVE ( 'NONE', #7834, #14638, #20245, .T. ) ;
#66199=CIRCLE ( 'NONE', #51599, 0.5000000000000004441 ) ;
#66209=( NAMED_UNIT ( * ) PLANE_ANGLE_UNIT ( ) SI_UNIT ( $, .RADIAN. ) );
#66213=EDGE_CURVE ( 'NONE', #373, #61874, #12137, .T. ) ;
#66218=EDGE_CURVE ( 'NONE', #9977, #58400, #37529, .T. ) ;
#66219=ORIENTED_EDGE ( 'NONE', *, *, #32386, .T. ) ;
#66222=DIRECTION ( 'NONE',  ( 1.000000000000000000, 0.000000000000000000, -0.000000000000000000 ) ) ;
#66225=CARTESIAN_POINT ( 'NONE',  ( -7.632228543268608334, 148.9570736234661581, 2.479861379858952830 ) ) ;
#66231=CARTESIAN_POINT ( 'NONE',  ( -60.00000000000000000, -2.024042244987997205E-14, 9.500000000000000000 ) ) ;
#66232=CARTESIAN_POINT ( 'NONE',  ( 3.094860106618435136, 131.4049999999999727, -9.525000000000000355 ) ) ;
#66234=DIRECTION ( 'NONE',  ( 0.000000000000000000, 1.000000000000000000, -0.000000000000000000 ) ) ;
#66239=FACE_OUTER_BOUND ( 'NONE', #3085, .T. ) ;
#66241=CARTESIAN_POINT ( 'NONE',  ( 44.50000000000000000, -1.469576158976824618E-14, -4.000000000000000000 ) ) ;
#66242=( GEOMETRIC_REPRESENTATION_CONTEXT ( 3 ) GLOBAL_UNCERTAINTY_ASSIGNED_CONTEXT ( ( #38958 ) ) GLOBAL_UNIT_ASSIGNED_CONTEXT ( ( #32581, #49487, #54392 ) ) REPRESENTATION_CONTEXT ( 'NONE', 'WORKASPACE' ) );
#66243=VECTOR ( 'NONE', #46150, 1000.000000000000000 ) ;
#66245=ORIENTED_EDGE ( 'NONE', *, *, #10360, .F. ) ;
#66247=CARTESIAN_POINT ( 'NONE',  ( -44.99999999999999289, 8.547452476119513420, -5.556748833515239738 ) ) ;
#66253=CARTESIAN_POINT ( 'NONE',  ( -74.09161580380370538, 9.403326511829389389, 6.097699930223767772 ) ) ;
#66255=VERTEX_POINT ( 'NONE', #21274 ) ;
#66257=CARTESIAN_POINT ( 'NONE',  ( 0.000000000000000000, 118.0570736234661524, -8.025000000000000355 ) ) ;
#66259=DIRECTION ( 'NONE',  ( 1.000000000000000000, 0.000000000000000000, 0.000000000000000000 ) ) ;
#66262=EDGE_CURVE ( 'NONE', #49593, #11358, #30111, .T. ) ;
#66265=CARTESIAN_POINT ( 'NONE',  ( 5.598654528085809545, 139.1449999999999818, -7.705886871421373741 ) ) ;
#66268=ORIENTED_EDGE ( 'NONE', *, *, #20569, .T. ) ;
#66271=CARTESIAN_POINT ( 'NONE',  ( -20.57648123223228254, 110.4999999999999858, -10.27659574468085069 ) ) ;
#66273=DIRECTION ( 'NONE',  ( 1.000000000000000000, 0.000000000000000000, -0.000000000000000000 ) ) ;
#66276=CARTESIAN_POINT ( 'NONE',  ( -45.00000000000000000, -1.469576158976824302E-14, 10.00000000000000000 ) ) ;
#66281=ORIENTED_EDGE ( 'NONE', *, *, #38007, .F. ) ;
#66282=( GEOMETRIC_REPRESENTATION_CONTEXT ( 3 ) GLOBAL_UNCERTAINTY_ASSIGNED_CONTEXT ( ( #42566 ) ) GLOBAL_UNIT_ASSIGNED_CONTEXT ( ( #44030, #6674, #7034 ) ) REPRESENTATION_CONTEXT ( 'NONE', 'WORKASPACE' ) );
#66285=CARTESIAN_POINT ( 'NONE',  ( -15.98999599679679839, 146.4999999999999716, -7.000000000000000000 ) ) ;
#66291=( NAMED_UNIT ( * ) PLANE_ANGLE_UNIT ( ) SI_UNIT ( $, .RADIAN. ) );
#66293=CARTESIAN_POINT ( 'NONE',  ( 45.00000000000000000, 9.999999999999980460, 4.000000000000000000 ) ) ;
#66294=DIRECTION ( 'NONE',  ( 0.000000000000000000, 1.000000000000000000, 0.000000000000000000 ) ) ;
#66295=VECTOR ( 'NONE', #47826, 1000.000000000000000 ) ;
#66299=CARTESIAN_POINT ( 'NONE',  ( -75.48275862068965125, 63.99167409976910648, 6.499999999999999112 ) ) ;
#66301=EDGE_CURVE ( 'NONE', #64454, #60681, #68558, .T. ) ;
#66302=PRESENTATION_STYLE_ASSIGNMENT (( #23391 ) ) ;
#66303=CARTESIAN_POINT ( 'NONE',  ( -41.68104242135606796, 107.4439537334013437, 3.570039632082458336 ) ) ;
#66305=EDGE_CURVE ( 'NONE', #6097, #19233, #14643, .T. ) ;
#66308=CARTESIAN_POINT ( 'NONE',  ( 23.71231517720798010, 112.4999999999999858, 10.00000000000000000 ) ) ;
#66311=CARTESIAN_POINT ( 'NONE',  ( -4.716976649647098618, 122.2570736234661553, 6.492361379858953008 ) ) ;
#66312=LINE ( 'NONE', #61032, #58588 ) ;
#66315=COLOUR_RGB ( '', 0.66274510, 0.83137255, 0.94901961) ;
#66316=CARTESIAN_POINT ( 'NONE',  ( 34.99999999999999289, 99.99999999999998579, 7.000000000000000000 ) ) ;
#66319=EDGE_CURVE ( 'NONE', #4746, #38702, #4389, .T. ) ;
#66322=FACE_OUTER_BOUND ( 'NONE', #38909, .T. ) ;
#66329=CARTESIAN_POINT ( 'NONE',  ( -20.57648123223228254, 114.4999999999999574, -10.27659574468085069 ) ) ;
#66330=CARTESIAN_POINT ( 'NONE',  ( 45.00000000000000000, 10.18984267075364336, 6.892226874380345869 ) ) ;
#66333=PLANE ( 'NONE',  #29114 ) ;
#66337=ORIENTED_EDGE ( 'NONE', *, *, #36594, .F. ) ;
#66339=CARTESIAN_POINT ( 'NONE',  ( -60.00000000000000000, -2.024042244987997205E-14, 6.500000000000000000 ) ) ;
#66340=FILL_AREA_STYLE ('',( #66701 ) ) ;
#66346=LINE ( 'NONE', #44942, #29594 ) ;
#66351=PRESENTATION_STYLE_ASSIGNMENT (( #29771 ) ) ;
#66356=CARTESIAN_POINT ( 'NONE',  ( 48.81081081081080697, 14.09971791521133255, -7.000000000000000000 ) ) ;
#66367=AXIS2_PLACEMENT_3D ( 'NONE', #5643, #32742, #43371 ) ;
#66370=CARTESIAN_POINT ( 'NONE',  ( 3.094860106618435136, 143.4049999999999443, -9.525000000000000355 ) ) ;
#66371=LINE ( 'NONE', #33673, #29767 ) ;
#66374=CARTESIAN_POINT ( 'NONE',  ( 2.879676288001297824, 154.2659213600069847, 8.840802594141084825 ) ) ;
#66378=CARTESIAN_POINT ( 'NONE',  ( -48.81081081081080697, 14.09971791521132900, -7.500000000000000000 ) ) ;
#66391=ADVANCED_FACE ( 'NONE', ( #54676 ), #55987, .T. ) ;
#66392=CIRCLE ( 'NONE', #14758, 8.000000000000000000 ) ;
#66393=CARTESIAN_POINT ( 'NONE',  ( -24.21231517720798010, 113.4999999999999858, -7.500000000000000000 ) ) ;
#66394=( LENGTH_UNIT ( ) NAMED_UNIT ( * ) SI_UNIT ( .MILLI., .METRE. ) );
#66395=( BOUNDED_CURVE ( )  B_SPLINE_CURVE ( 3, ( #37643, #42917, #32638, #65357 ),
 .UNSPECIFIED., .F., .F. ) 
 B_SPLINE_CURVE_WITH_KNOTS ( ( 4, 4 ),
 ( 3.141592653589793116, 4.712388980384689674 ),
 .UNSPECIFIED. ) 
 CURVE ( )  GEOMETRIC_REPRESENTATION_ITEM ( )  RATIONAL_B_SPLINE_CURVE ( ( 1.000000000000000000, 0.8047378541243649375, 0.8047378541243649375, 1.000000000000000000 ) ) 
 REPRESENTATION_ITEM ( '' )  );
#66397=ORIENTED_EDGE ( 'NONE', *, *, #37640, .F. ) ;
#66400=FACE_OUTER_BOUND ( 'NONE', #50975, .T. ) ;
#66402=VERTEX_POINT ( 'NONE', #38561 ) ;
#66403=CARTESIAN_POINT ( 'NONE',  ( 9.058813317711338797, 112.9549999999999841, -2.943386871421372675 ) ) ;
#66405=ORIENTED_EDGE ( 'NONE', *, *, #23575, .F. ) ;
#66406=AXIS2_PLACEMENT_3D ( 'NONE', #40473, #25306, #2404 ) ;
#66415=SURFACE_STYLE_USAGE ( .BOTH. , #29470 ) ;
#66417=CARTESIAN_POINT ( 'NONE',  ( 44.79289321881345387, 10.55564175590369658, 3.499999999999996447 ) ) ;
#66418=ORIENTED_EDGE ( 'NONE', *, *, #6743, .F. ) ;
#66419=CARTESIAN_POINT ( 'NONE',  ( 6.826472737025119919, 139.8929263765338362, 4.959722759717908325 ) ) ;
#66426=SURFACE_STYLE_USAGE ( .BOTH. , #50601 ) ;
#66428=DIRECTION ( 'NONE',  ( -0.000000000000000000, -1.000000000000000000, -0.000000000000000000 ) ) ;
#66431=SURFACE_STYLE_FILL_AREA ( #60789 ) ;
#66433=CARTESIAN_POINT ( 'NONE',  ( 45.50000000000000000, 1.797044900979284448E-15, 9.500000000000000000 ) ) ;
#66434=ORIENTED_EDGE ( 'NONE', *, *, #40448, .T. ) ;
#66435=CIRCLE ( 'NONE', #13600, 5.000000000000004441 ) ;
#66436=DIRECTION ( 'NONE',  ( -1.000000000000000000, 0.000000000000000000, 0.000000000000000000 ) ) ;
#66445=ORIENTED_EDGE ( 'NONE', *, *, #16175, .F. ) ;
#66452=CARTESIAN_POINT ( 'NONE',  ( -74.74007105697891973, 36.01955776115826069, -9.942355741406379011 ) ) ;
#66454=VECTOR ( 'NONE', #13507, 1000.000000000000000 ) ;
#66455=DIRECTION ( 'NONE',  ( 1.000000000000000000, 0.000000000000000000, 0.000000000000000000 ) ) ;
#66456=DIRECTION ( 'NONE',  ( -0.000000000000000000, -0.000000000000000000, -1.000000000000000000 ) ) ;
#66461=AXIS2_PLACEMENT_3D ( 'NONE', #28959, #27315, #29322 ) ;
#66463=CARTESIAN_POINT ( 'NONE',  ( 9.058813317711337021, 118.6549999999999869, 2.943386871421375783 ) ) ;
#66467=EDGE_CURVE ( 'NONE', #23204, #30840, #43829, .T. ) ;
#66469=SURFACE_SIDE_STYLE ('',( #12288 ) ) ;
#66471=UNCERTAINTY_MEASURE_WITH_UNIT (LENGTH_MEASURE( 1.000000000000000082E-05 ), #53700, 'distance_accuracy_value', 'NONE');
#66475=CARTESIAN_POINT ( 'NONE',  ( 40.78947368421052033, 108.1536491499103221, -3.158024016299528558 ) ) ;
#66486=( LENGTH_UNIT ( ) NAMED_UNIT ( * ) SI_UNIT ( .MILLI., .METRE. ) );
#66488=ORIENTED_EDGE ( 'NONE', *, *, #25346, .F. ) ;
#66494=FILL_AREA_STYLE ('',( #24262 ) ) ;
#66497=FILL_AREA_STYLE_COLOUR ( '', #31795 ) ;
#66500=ORIENTED_EDGE ( 'NONE', *, *, #10517, .T. ) ;
#66504=TOROIDAL_SURFACE ( 'NONE', #5823, 1.000000000000000000, 0.5000000000000000000 ) ;
#66507=CARTESIAN_POINT ( 'NONE',  ( -3.094860106618432471, 139.5949999999999420, -9.525000000000000355 ) ) ;
#66508=VERTEX_POINT ( 'NONE', #66271 ) ;
#66509=VECTOR ( 'NONE', #59854, 1000.000000000000000 ) ;
#66511=CARTESIAN_POINT ( 'NONE',  ( -10.01517768586949408, 144.3049999999999784, -6.132527647946036459E-16 ) ) ;
#66512=MECHANICAL_DESIGN_GEOMETRIC_PRESENTATION_REPRESENTATION('',(#28256),#45155);
#66514=CARTESIAN_POINT ( 'NONE',  ( 40.78947369313011251, 108.1536491435769989, -3.152202064295424488 ) ) ;
#66516=CARTESIAN_POINT ( 'NONE',  ( -8.102448949553181734, 159.0049999999999670, -5.886773742842749790 ) ) ;
#66517=DIRECTION ( 'NONE',  ( 1.000000000000000000, 0.000000000000000000, 0.000000000000000000 ) ) ;
#66518=UNCERTAINTY_MEASURE_WITH_UNIT (LENGTH_MEASURE( 1.000000000000000082E-05 ), #38352, 'distance_accuracy_value', 'NONE');
#66520=SURFACE_STYLE_FILL_AREA ( #8128 ) ;
#66522=AXIS2_PLACEMENT_3D ( 'NONE', #62841, #14682, #15054 ) ;
#66523=FILL_AREA_STYLE ('',( #38792 ) ) ;
#66524=ORIENTED_EDGE ( 'NONE', *, *, #42525, .F. ) ;
#66529=ORIENTED_EDGE ( 'NONE', *, *, #62637, .F. ) ;
#66532=COLOUR_RGB ( '', 0.66274510, 0.83137255, 0.94901961) ;
#66533=DIRECTION ( 'NONE',  ( 1.000000000000000000, 0.000000000000000000, 0.000000000000000000 ) ) ;
#66534=DIRECTION ( 'NONE',  ( 0.000000000000000000, 0.000000000000000000, 1.000000000000000000 ) ) ;
#66536=DIRECTION ( 'NONE',  ( 0.000000000000000000, -1.000000000000000000, 0.000000000000000000 ) ) ;
#66537=ORIENTED_EDGE ( 'NONE', *, *, #49967, .T. ) ;
#66540=AXIS2_PLACEMENT_3D ( 'NONE', #21908, #43420, #60227 ) ;
#66544=AXIS2_PLACEMENT_3D ( 'NONE', #41834, #9451, #25940 ) ;
#66549=ORIENTED_EDGE ( 'NONE', *, *, #60466, .F. ) ;
#66551=DIRECTION ( 'NONE',  ( 0.000000000000000000, 0.000000000000000000, 1.000000000000000000 ) ) ;
#66553=EDGE_CURVE ( 'NONE', #57942, #60077, #19108, .T. ) ;
#66554=CARTESIAN_POINT ( 'NONE',  ( -3.094860106618432471, 142.5950000000000273, -9.525000000000000355 ) ) ;
#66556=CIRCLE ( 'NONE', #14913, 0.5000000000000004441 ) ;
#66560=CIRCLE ( 'NONE', #64290, 8.500000000000007105 ) ;
#66561=EDGE_CURVE ( 'NONE', #10808, #20549, #62393, .T. ) ;
#66564=VECTOR ( 'NONE', #3302, 1000.000000000000000 ) ;
#66566=AXIS2_PLACEMENT_3D ( 'NONE', #64776, #10623, #58461 ) ;
#66568=CARTESIAN_POINT ( 'NONE',  ( -23.21231517720797655, 117.9999999999999716, -9.500000000000000000 ) ) ;
#66571=ORIENTED_EDGE ( 'NONE', *, *, #27780, .F. ) ;
#66575=EDGE_CURVE ( 'NONE', #52539, #27715, #43770, .T. ) ;
#66576=( NAMED_UNIT ( * ) PLANE_ANGLE_UNIT ( ) SI_UNIT ( $, .RADIAN. ) );
#66578=SURFACE_STYLE_FILL_AREA ( #29267 ) ;
#66583=AXIS2_PLACEMENT_3D ( 'NONE', #22162, #42979, #4945 ) ;
#66586=SURFACE_SIDE_STYLE ('',( #55679 ) ) ;
#66587=SURFACE_STYLE_FILL_AREA ( #38854 ) ;
#66588=( LENGTH_UNIT ( ) NAMED_UNIT ( * ) SI_UNIT ( .MILLI., .METRE. ) );
#66589=CARTESIAN_POINT ( 'NONE',  ( 0.000000000000000000, 154.0570736234661524, -8.025000000000000355 ) ) ;
#66590=CIRCLE ( 'NONE', #2511, 14.49999999999999822 ) ;
#66592=DIRECTION ( 'NONE',  ( 0.000000000000000000, 0.000000000000000000, 1.000000000000000000 ) ) ;
#66594=( NAMED_UNIT ( * ) SI_UNIT ( $, .STERADIAN. ) SOLID_ANGLE_UNIT ( ) );
#66595=CARTESIAN_POINT ( 'NONE',  ( 3.094860106618431583, 127.2049999999999841, 9.525000000000000355 ) ) ;
#66596=UNCERTAINTY_MEASURE_WITH_UNIT (LENGTH_MEASURE( 1.000000000000000082E-05 ), #28087, 'distance_accuracy_value', 'NONE');
#66598=SPHERICAL_SURFACE ( 'NONE', #4007, 0.5000000000000000000 ) ;
#66604=MECHANICAL_DESIGN_GEOMETRIC_PRESENTATION_REPRESENTATION('',(#7048),#64337);
#66605=CYLINDRICAL_SURFACE ( 'NONE', #64302, 7.999999999999992895 ) ;
#66610=ADVANCED_FACE ( 'NONE', ( #29325 ), #34965, .T. ) ;
#66612=CARTESIAN_POINT ( 'NONE',  ( -15.48999599679679662, 146.4999999999999716, -7.000000000000000000 ) ) ;
#66613=CARTESIAN_POINT ( 'NONE',  ( 45.00000000000000000, 99.99999999999992895, 10.00000000000000000 ) ) ;
#66614=PRESENTATION_STYLE_ASSIGNMENT (( #38273 ) ) ;
#66618=ORIENTED_EDGE ( 'NONE', *, *, #46144, .T. ) ;
#66619=CARTESIAN_POINT ( 'NONE',  ( -75.00000000000000000, 9.609158271987205069, 6.330303435919315547 ) ) ;
#66622=CARTESIAN_POINT ( 'NONE',  ( -7.632228543268608334, 118.9570736234661581, 2.479861379858952830 ) ) ;
#66623=SURFACE_SIDE_STYLE ('',( #15677 ) ) ;
#66627=FACE_OUTER_BOUND ( 'NONE', #12143, .T. ) ;
#66628=CARTESIAN_POINT ( 'NONE',  ( 3.094860106618431583, 144.0949999999999420, 9.525000000000000355 ) ) ;
#66631=ADVANCED_FACE ( 'NONE', ( #3245 ), #22293, .F. ) ;
#66632=CARTESIAN_POINT ( 'NONE',  ( -74.99999999999998579, 50.00000000000000000, 10.00000000000000000 ) ) ;
#66637=COLOUR_RGB ( '', 0.08235294, 0.09019608, 0.10196078) ;
#66642=( GEOMETRIC_REPRESENTATION_CONTEXT ( 3 ) GLOBAL_UNCERTAINTY_ASSIGNED_CONTEXT ( ( #65082 ) ) GLOBAL_UNIT_ASSIGNED_CONTEXT ( ( #3328, #3685, #42116 ) ) REPRESENTATION_CONTEXT ( 'NONE', 'WORKASPACE' ) );
#66645=LINE ( 'NONE', #29698, #57210 ) ;
#66646=VERTEX_POINT ( 'NONE', #37091 ) ;
#66655=DIRECTION ( 'NONE',  ( 1.000000000000000000, 0.000000000000000000, 0.000000000000000000 ) ) ;
#66658=PRESENTATION_STYLE_ASSIGNMENT (( #29710 ) ) ;
#66663=CARTESIAN_POINT ( 'NONE',  ( -60.00000000000000000, -2.024042244987997205E-14, -6.500000000000000000 ) ) ;
#66665=CARTESIAN_POINT ( 'NONE',  ( 44.99999999999998579, 119.9999999999999716, -7.000000000000000000 ) ) ;
#66666=CARTESIAN_POINT ( 'NONE',  ( -41.39002736484395228, 107.1345546009600014, 3.500000000000000000 ) ) ;
#66670=CARTESIAN_POINT ( 'NONE',  ( -12.34222745343792127, 115.4999999999999574, 10.18181818181818166 ) ) ;
#66671=( NAMED_UNIT ( * ) SI_UNIT ( $, .STERADIAN. ) SOLID_ANGLE_UNIT ( ) );
#66672=ORIENTED_EDGE ( 'NONE', *, *, #65532, .F. ) ;
#66673=CARTESIAN_POINT ( 'NONE',  ( 0.000000000000000000, 109.9999999999999858, 22.50000000000000000 ) ) ;
#66674=ADVANCED_FACE ( 'NONE', ( #10328 ), #53244, .F. ) ;
#66675=CARTESIAN_POINT ( 'NONE',  ( -4.716976649647098618, 125.2570736234661695, 6.492361379858953008 ) ) ;
#66676=STYLED_ITEM ( 'NONE', ( #9085 ), #55669 ) ;
#66677=CONICAL_SURFACE ( 'NONE', #30702, 5.000000000000004441, 0.7853981633974587151 ) ;
#66681=CYLINDRICAL_SURFACE ( 'NONE', #55653, 0.5000000000000004441 ) ;
#66682=MECHANICAL_DESIGN_GEOMETRIC_PRESENTATION_REPRESENTATION('',(#7185),#63318);
#66683=DIRECTION ( 'NONE',  ( -1.000000000000000000, 0.000000000000000000, 0.000000000000000000 ) ) ;
#66685=PRESENTATION_STYLE_ASSIGNMENT (( #7251 ) ) ;
#66689=TOROIDAL_SURFACE ( 'NONE', #36414, 1.000000000000000000, 0.5000000000000000000 ) ;
#66693=CARTESIAN_POINT ( 'NONE',  ( -41.49999999999997868, 10.49999999999998046, -3.000000000000000000 ) ) ;
#66694=FILL_AREA_STYLE_COLOUR ( '', #68470 ) ;
#66699=DIRECTION ( 'NONE',  ( -0.000000000000000000, -1.000000000000000000, -0.000000000000000000 ) ) ;
#66701=FILL_AREA_STYLE_COLOUR ( '', #21782 ) ;
#66702=FACE_OUTER_BOUND ( 'NONE', #68951, .T. ) ;
#66705=CARTESIAN_POINT ( 'NONE',  ( 9.058813317711337021, 114.5449999999999733, 2.943386871421375783 ) ) ;
#66708=AXIS2_PLACEMENT_3D ( 'NONE', #53137, #53477, #37339 ) ;
#66709=EDGE_CURVE ( 'NONE', #3378, #631, #10007, .T. ) ;
#66712=ORIENTED_EDGE ( 'NONE', *, *, #47898, .T. ) ;
#66714=CARTESIAN_POINT ( 'NONE',  ( 71.62068965517238439, 63.58603185604027885, -9.500000000000000000 ) ) ;
#66716=ORIENTED_EDGE ( 'NONE', *, *, #36330, .T. ) ;
#66717=ADVANCED_FACE ( 'NONE', ( #65150 ), #39159, .T. ) ;
#66720=( NAMED_UNIT ( * ) SI_UNIT ( $, .STERADIAN. ) SOLID_ANGLE_UNIT ( ) );
#66723=MECHANICAL_DESIGN_GEOMETRIC_PRESENTATION_REPRESENTATION('',(#19562),#26282);
#66726=CIRCLE ( 'NONE', #46592, 0.5000000000000004441 ) ;
#66727=CARTESIAN_POINT ( 'NONE',  ( 24.21231517720798010, 113.4999999999999858, 7.500000000000000000 ) ) ;
#66731=DIRECTION ( 'NONE',  ( -0.000000000000000000, -0.000000000000000000, -1.000000000000000000 ) ) ;
#66733=EDGE_CURVE ( 'NONE', #16450, #35776, #59173, .T. ) ;
#66736=CARTESIAN_POINT ( 'NONE',  ( -5.598654528085808657, 144.7549999999999955, 7.705886871421373741 ) ) ;
#66737=PRESENTATION_STYLE_ASSIGNMENT (( #45316 ) ) ;
#66741=( NAMED_UNIT ( * ) PLANE_ANGLE_UNIT ( ) SI_UNIT ( $, .RADIAN. ) );
#66743=LINE ( 'NONE', #56881, #41497 ) ;
#66745=DIRECTION ( 'NONE',  ( -0.000000000000000000, -0.000000000000000000, -1.000000000000000000 ) ) ;
#66746=CARTESIAN_POINT ( 'NONE',  ( -74.50000000000000000, -2.208799022165584366E-14, -7.000000000000000888 ) ) ;
#66751=ADVANCED_FACE ( 'NONE', ( #11000 ), #49340, .F. ) ;
#66755=CARTESIAN_POINT ( 'NONE',  ( 23.21231517720797655, 113.4999999999999858, 10.00000000000000000 ) ) ;
#66756=VERTEX_POINT ( 'NONE', #35234 ) ;
#66758=DIRECTION ( 'NONE',  ( -0.000000000000000000, -0.000000000000000000, -1.000000000000000000 ) ) ;
#66759=( NAMED_UNIT ( * ) SI_UNIT ( $, .STERADIAN. ) SOLID_ANGLE_UNIT ( ) );
#66761=ORIENTED_EDGE ( 'NONE', *, *, #278, .T. ) ;
#66766=SURFACE_STYLE_USAGE ( .BOTH. , #30139 ) ;
#66769=ORIENTED_EDGE ( 'NONE', *, *, #8696, .T. ) ;
#66770=AXIS2_PLACEMENT_3D ( 'NONE', #62623, #8503, #62296 ) ;
#66776=CIRCLE ( 'NONE', #26331, 0.5000000000000004441 ) ;
#66778=CARTESIAN_POINT ( 'NONE',  ( 0.000000000000000000, 140.9429263765338192, -8.025000000000000355 ) ) ;
#66782=PRESENTATION_STYLE_ASSIGNMENT (( #62174 ) ) ;
#66789=( NAMED_UNIT ( * ) SI_UNIT ( $, .STERADIAN. ) SOLID_ANGLE_UNIT ( ) );
#66795=ORIENTED_EDGE ( 'NONE', *, *, #33742, .T. ) ;
#66796=( NAMED_UNIT ( * ) SI_UNIT ( $, .STERADIAN. ) SOLID_ANGLE_UNIT ( ) );
#66801=CARTESIAN_POINT ( 'NONE',  ( -60.00000000000000000, -2.024042244987997205E-14, -7.000000000000024869 ) ) ;
#66802=EDGE_LOOP ( 'NONE', ( #67350, #26201, #11643, #22 ) ) ;
#66804=DIRECTION ( 'NONE',  ( -0.000000000000000000, -0.000000000000000000, 1.000000000000000000 ) ) ;
#66805=B_SPLINE_CURVE_WITH_KNOTS ( 'NONE', 3,
 ( #51420, #20449, #51777, #40898, #15214, #56703, #3526, #57745, #41952, #46178, #68648, #29958 ),
 .UNSPECIFIED., .F., .F.,
 ( 4, 2, 2, 2, 2, 4 ),
 ( 0.000000000000000000, 0.0001470450322352830183, 0.0002940900644705660366, 0.0005881801289411579857, 0.0008822701934117498264, 0.001176360257882341775 ),
 .UNSPECIFIED. ) ;
#66813=FILL_AREA_STYLE_COLOUR ( '', #45337 ) ;
#66818=EDGE_LOOP ( 'NONE', ( #40200, #51763, #44076, #66947 ) ) ;
#66821=DIRECTION ( 'NONE',  ( 0.000000000000000000, 1.000000000000000000, -0.000000000000000000 ) ) ;
#66829=CARTESIAN_POINT ( 'NONE',  ( -5.598654528085806881, 113.8549999999999898, -7.705886871421374629 ) ) ;
#66832=CIRCLE ( 'NONE', #29756, 0.5000000000000004441 ) ;
#66836=CIRCLE ( 'NONE', #36543, 0.5000000000000004441 ) ;
#66837=CARTESIAN_POINT ( 'NONE',  ( -67.99999999999998579, -2.024042244987997205E-14, -11.50000000000000000 ) ) ;
#66841=CIRCLE ( 'NONE', #1637, 5.000000000000004441 ) ;
#66844=CARTESIAN_POINT ( 'NONE',  ( 0.000000000000000000, 87.30187232391182306, 0.000000000000000000 ) ) ;
#66845=LINE ( 'NONE', #45754, #26908 ) ;
#66848=DIRECTION ( 'NONE',  ( -1.000000000000000000, 0.000000000000000000, 0.000000000000000000 ) ) ;
#66852=SURFACE_SIDE_STYLE ('',( #61209 ) ) ;
#66853=DIRECTION ( 'NONE',  ( -1.000000000000000000, 0.000000000000000000, 0.000000000000000000 ) ) ;
#66858=ORIENTED_EDGE ( 'NONE', *, *, #39693, .T. ) ;
#66864=MECHANICAL_DESIGN_GEOMETRIC_PRESENTATION_REPRESENTATION('',(#5079),#59019);
#66866=CARTESIAN_POINT ( 'NONE',  ( 10.01517768586949231, 141.6949999999999363, 1.839758294383810543E-15 ) ) ;
#66870=CARTESIAN_POINT ( 'NONE',  ( 9.058813317711337021, 139.6550000000000011, 2.943386871421375783 ) ) ;
#66873=EDGE_LOOP ( 'NONE', ( #54331, #6219, #39009, #11659 ) ) ;
#66874=CARTESIAN_POINT ( 'NONE',  ( -7.632228543268608334, 117.8429263765338249, 2.479861379858952830 ) ) ;
#66875=DIRECTION ( 'NONE',  ( 0.000000000000000000, 0.000000000000000000, 1.000000000000000000 ) ) ;
#66877=DIRECTION ( 'NONE',  ( 1.000000000000000000, 0.000000000000000000, 0.000000000000000000 ) ) ;
#66878=AXIS2_PLACEMENT_3D ( 'NONE', #4256, #25733, #21504 ) ;
#66893=( NAMED_UNIT ( * ) PLANE_ANGLE_UNIT ( ) SI_UNIT ( $, .RADIAN. ) );
#66894=ORIENTED_EDGE ( 'NONE', *, *, #57344, .F. ) ;
#66895=EDGE_CURVE ( 'NONE', #9170, #60684, #16752, .T. ) ;
#66896=EDGE_LOOP ( 'NONE', ( #23010, #67582, #15772, #16926 ) ) ;
#66898=DIRECTION ( 'NONE',  ( -0.000000000000000000, 1.000000000000000000, -0.000000000000000000 ) ) ;
#66900=VERTEX_POINT ( 'NONE', #60550 ) ;
#66902=EDGE_CURVE ( 'NONE', #48671, #7813, #29042, .T. ) ;
#66905=ADVANCED_FACE ( 'NONE', ( #23976 ), #34197, .F. ) ;
#66906=CARTESIAN_POINT ( 'NONE',  ( -74.35506026930195844, 8.371839367610338201, -6.471715848474757671 ) ) ;
#66909=SURFACE_STYLE_USAGE ( .BOTH. , #18374 ) ;
#66911=CARTESIAN_POINT ( 'NONE',  ( -9.058813317711337021, 143.0449999999999875, -2.943386871421374895 ) ) ;
#66914=CIRCLE ( 'NONE', #34312, 0.4999999999999994449 ) ;
#66915=AXIS2_PLACEMENT_3D ( 'NONE', #22242, #23522, #56931 ) ;
#66916=DIRECTION ( 'NONE',  ( 0.000000000000000000, -1.000000000000000000, -0.000000000000000000 ) ) ;
#66917=CARTESIAN_POINT ( 'NONE',  ( 54.49999999999999289, 2.470600640510329340E-15, -6.500000000000000000 ) ) ;
#66928=CARTESIAN_POINT ( 'NONE',  ( -7.632228543268607446, 127.6570736234661467, -2.479861379858953718 ) ) ;
#66930=CIRCLE ( 'NONE', #44432, 0.5000000000000004441 ) ;
#66933=CIRCLE ( 'NONE', #13489, 0.5000000000000004441 ) ;
#66934=FILL_AREA_STYLE_COLOUR ( '', #30394 ) ;
#66935=CARTESIAN_POINT ( 'NONE',  ( -45.50000000000000000, 7.768687147774683943, 6.500000000000000888 ) ) ;
#66937=CARTESIAN_POINT ( 'NONE',  ( 23.71231517720798010, 113.4999999999999858, -7.500000000000000000 ) ) ;
#66945=SURFACE_SIDE_STYLE ('',( #60587 ) ) ;
#66946=CARTESIAN_POINT ( 'NONE',  ( 10.01517768586949231, 114.6949999999999932, 1.839758294383810543E-15 ) ) ;
#66947=ORIENTED_EDGE ( 'NONE', *, *, #66048, .F. ) ;
#66950=CARTESIAN_POINT ( 'NONE',  ( 0.000000000000000000, 134.5549999999999784, -9.525000000000000355 ) ) ;
#66951=CARTESIAN_POINT ( 'NONE',  ( 2.607480562269034241, 132.9070736234661467, -8.025000000000032330 ) ) ;
#66952=CARTESIAN_POINT ( 'NONE',  ( 20.99077900071323199, 114.7777241159145518, 10.00000000000000000 ) ) ;
#66953=EDGE_CURVE ( 'NONE', #34565, #28179, #4590, .T. ) ;
#66959=FACE_OUTER_BOUND ( 'NONE', #7791, .T. ) ;
#66960=FILL_AREA_STYLE ('',( #13124 ) ) ;
#66966=CARTESIAN_POINT ( 'NONE',  ( 0.000000000000000000, 120.0249999999999773, 0.000000000000000000 ) ) ;
#66974=CARTESIAN_POINT ( 'NONE',  ( -74.99999999999998579, 8.119648659858185624, 6.397056658262309625 ) ) ;
#66976=EDGE_LOOP ( 'NONE', ( #67200, #7845, #59519, #10045 ) ) ;
#66979=CARTESIAN_POINT ( 'NONE',  ( 40.49999999999998579, 107.7459666924148252, 10.00000000000000000 ) ) ;
#66982=DIRECTION ( 'NONE',  ( 0.000000000000000000, -1.000000000000000000, 0.000000000000000000 ) ) ;
#66983=CARTESIAN_POINT ( 'NONE',  ( -3.094860106618434248, 140.7950000000000159, 9.525000000000000355 ) ) ;
#66984=( GEOMETRIC_REPRESENTATION_CONTEXT ( 3 ) GLOBAL_UNCERTAINTY_ASSIGNED_CONTEXT ( ( #61510 ) ) GLOBAL_UNIT_ASSIGNED_CONTEXT ( ( #760, #64163, #33209 ) ) REPRESENTATION_CONTEXT ( 'NONE', 'WORKASPACE' ) );
#66987=PLANE ( 'NONE',  #20426 ) ;
#66992=( NAMED_UNIT ( * ) SI_UNIT ( $, .STERADIAN. ) SOLID_ANGLE_UNIT ( ) );
#66995=FACE_OUTER_BOUND ( 'NONE', #49301, .T. ) ;
#66996=ORIENTED_EDGE ( 'NONE', *, *, #69657, .T. ) ;
#66999=CYLINDRICAL_SURFACE ( 'NONE', #40672, 23.00000000000000000 ) ;
#67003=CIRCLE ( 'NONE', #25414, 0.5000000000000004441 ) ;
#67007=LINE ( 'NONE', #55754, #3110 ) ;
#67009=ORIENTED_EDGE ( 'NONE', *, *, #57162, .F. ) ;
#67016=CARTESIAN_POINT ( 'NONE',  ( 6.826472737025121695, 123.6070736234661496, -4.959722759717905660 ) ) ;
#67018=AXIS2_PLACEMENT_3D ( 'NONE', #41438, #42849, #31538 ) ;
#67019=FILL_AREA_STYLE_COLOUR ( '', #39537 ) ;
#67022=CARTESIAN_POINT ( 'NONE',  ( 60.00000000000000000, 1.797044900979284448E-15, -11.50000000000000000 ) ) ;
#67023=VERTEX_POINT ( 'NONE', #42304 ) ;
#67025=CARTESIAN_POINT ( 'NONE',  ( -2.607480562269073765, 133.2070736234661013, -8.025000000000000355 ) ) ;
#67032=EDGE_CURVE ( 'NONE', #5967, #12255, #10243, .T. ) ;
#67034=CARTESIAN_POINT ( 'NONE',  ( 7.632228543268608334, 150.4570736234661581, -2.479861379858951942 ) ) ;
#67035=FACE_OUTER_BOUND ( 'NONE', #1283, .T. ) ;
#67040=FACE_OUTER_BOUND ( 'NONE', #51640, .T. ) ;
#67043=UNCERTAINTY_MEASURE_WITH_UNIT (LENGTH_MEASURE( 1.000000000000000082E-05 ), #13061, 'distance_accuracy_value', 'NONE');
#67045=EDGE_CURVE ( 'NONE', #8875, #13986, #4231, .T. ) ;
#67047=PRESENTATION_STYLE_ASSIGNMENT (( #9352 ) ) ;
#67049=CIRCLE ( 'NONE', #53586, 0.5000000000000004441 ) ;
#67051=ORIENTED_EDGE ( 'NONE', *, *, #53677, .F. ) ;
#67052=MECHANICAL_DESIGN_GEOMETRIC_PRESENTATION_REPRESENTATION('',(#56956),#61399);
#67055=FILL_AREA_STYLE ('',( #40007 ) ) ;
#67058=LINE ( 'NONE', #57174, #57723 ) ;
#67061=EDGE_CURVE ( 'NONE', #12165, #48372, #14134, .T. ) ;
#67063=ORIENTED_EDGE ( 'NONE', *, *, #37950, .T. ) ;
#67065=CARTESIAN_POINT ( 'NONE',  ( -74.50000000000000000, -2.220952357103124925E-14, -9.500000000000000000 ) ) ;
#67067=MECHANICAL_DESIGN_GEOMETRIC_PRESENTATION_REPRESENTATION('',(#58094),#39022);
#67069=CARTESIAN_POINT ( 'NONE',  ( -75.00000000000000000, 8.164352767049518178, 6.987111781054302639 ) ) ;
#67070=CARTESIAN_POINT ( 'NONE',  ( -6.854883122194315170, 111.1401193526694726, -5.667071715363107387 ) ) ;
#67073=ORIENTED_EDGE ( 'NONE', *, *, #9902, .T. ) ;
#67078=CARTESIAN_POINT ( 'NONE',  ( 5.598654528085805993, 145.3549999999999898, 7.705886871421374629 ) ) ;
#67079=CARTESIAN_POINT ( 'NONE',  ( 60.49999999999998579, 50.00000000000000000, 6.999999999999999112 ) ) ;
#67089=DIRECTION ( 'NONE',  ( -0.000000000000000000, -0.000000000000000000, -1.000000000000000000 ) ) ;
#67090=CARTESIAN_POINT ( 'NONE',  ( 0.000000000000000000, 114.9999999999999574, 0.000000000000000000 ) ) ;
#67095=( NAMED_UNIT ( * ) PLANE_ANGLE_UNIT ( ) SI_UNIT ( $, .RADIAN. ) );
#67097=ADVANCED_FACE ( 'NONE', ( #25364 ), #45622, .T. ) ;
#67098=EDGE_LOOP ( 'NONE', ( #62086, #60111, #61452, #58640 ) ) ;
#67100=DIRECTION ( 'NONE',  ( 1.000000000000000000, 0.000000000000000000, 0.000000000000000000 ) ) ;
#67101=COLOUR_RGB ( '', 0.40784314, 0.44705882, 0.49803922) ;
#67102=ADVANCED_FACE ( 'NONE', ( #43923 ), #5353, .F. ) ;
#67107=( NAMED_UNIT ( * ) SI_UNIT ( $, .STERADIAN. ) SOLID_ANGLE_UNIT ( ) );
#67110=VERTEX_POINT ( 'NONE', #7295 ) ;
#67114=CARTESIAN_POINT ( 'NONE',  ( 12.72792206135785698, 114.9999999999999574, 10.50000000000000000 ) ) ;
#67116=CARTESIAN_POINT ( 'NONE',  ( -6.826472737025120807, 144.9929263765337737, 4.959722759717906548 ) ) ;
#67117=CYLINDRICAL_SURFACE ( 'NONE', #43652, 0.5000000000000004441 ) ;
#67124=( GEOMETRIC_REPRESENTATION_CONTEXT ( 3 ) GLOBAL_UNCERTAINTY_ASSIGNED_CONTEXT ( ( #36873 ) ) GLOBAL_UNIT_ASSIGNED_CONTEXT ( ( #68256, #50092, #20764 ) ) REPRESENTATION_CONTEXT ( 'NONE', 'WORKASPACE' ) );
#67129=PRESENTATION_STYLE_ASSIGNMENT (( #19630 ) ) ;
#67131=DIRECTION ( 'NONE',  ( -0.3162277660168378857, 0.9486832980505138790, 0.000000000000000000 ) ) ;
#67132=CARTESIAN_POINT ( 'NONE',  ( -6.826472737025120807, 120.3929263765338220, -4.959722759717907437 ) ) ;
#67140=ORIENTED_EDGE ( 'NONE', *, *, #11634, .T. ) ;
#67142=DIRECTION ( 'NONE',  ( 0.000000000000000000, -1.000000000000000000, 0.000000000000000000 ) ) ;
#67143=ADVANCED_FACE ( 'NONE', ( #27670 ), #50212, .T. ) ;
#67148=CARTESIAN_POINT ( 'NONE',  ( 71.50000000000000000, 14.49137674618942562, -7.500000000000000000 ) ) ;
#67151=CYLINDRICAL_SURFACE ( 'NONE', #31297, 8.999999999999994671 ) ;
#67154=CARTESIAN_POINT ( 'NONE',  ( -74.49999999999998579, 119.9999999999997726, 9.500000000000000000 ) ) ;
#67160=CARTESIAN_POINT ( 'NONE',  ( -8.102448949553181734, 117.0049999999999670, -5.886773742842749790 ) ) ;
#67165=( NAMED_UNIT ( * ) PLANE_ANGLE_UNIT ( ) SI_UNIT ( $, .RADIAN. ) );
#67166=( NAMED_UNIT ( * ) PLANE_ANGLE_UNIT ( ) SI_UNIT ( $, .RADIAN. ) );
#67172=DIRECTION ( 'NONE',  ( 0.000000000000000000, 0.000000000000000000, -1.000000000000000000 ) ) ;
#67177=( NAMED_UNIT ( * ) SI_UNIT ( $, .STERADIAN. ) SOLID_ANGLE_UNIT ( ) );
#67179=AXIS2_PLACEMENT_3D ( 'NONE', #63493, #15344, #12425 ) ;
#67181=FACE_OUTER_BOUND ( 'NONE', #64841, .T. ) ;
#67189=VERTEX_POINT ( 'NONE', #41060 ) ;
#67191=DIRECTION ( 'NONE',  ( 1.000000000000000000, -0.000000000000000000, -0.000000000000000000 ) ) ;
#67193=CARTESIAN_POINT ( 'NONE',  ( 3.094860106618435136, 136.2949999999999875, -9.525000000000000355 ) ) ;
#67197=CARTESIAN_POINT ( 'NONE',  ( -8.102448949553179958, 138.6049999999999613, 5.886773742842747126 ) ) ;
#67198=( NAMED_UNIT ( * ) PLANE_ANGLE_UNIT ( ) SI_UNIT ( $, .RADIAN. ) );
#67199=DIRECTION ( 'NONE',  ( 1.000000000000000000, 0.000000000000000000, 0.000000000000000000 ) ) ;
#67200=ORIENTED_EDGE ( 'NONE', *, *, #35241, .F. ) ;
#67201=CARTESIAN_POINT ( 'NONE',  ( -6.826472737025120807, 114.3929263765337936, -4.959722759717907437 ) ) ;
#67202=DIRECTION ( 'NONE',  ( -1.000000000000000000, 0.000000000000000000, 0.000000000000000000 ) ) ;
#67203=UNCERTAINTY_MEASURE_WITH_UNIT (LENGTH_MEASURE( 1.000000000000000082E-05 ), #25480, 'distance_accuracy_value', 'NONE');
#67206=EDGE_CURVE ( 'NONE', #13013, #11295, #7621, .T. ) ;
#67207=PRESENTATION_STYLE_ASSIGNMENT (( #29204 ) ) ;
#67208=PRESENTATION_STYLE_ASSIGNMENT (( #8811 ) ) ;
#67210=DIRECTION ( 'NONE',  ( 0.000000000000000000, 0.000000000000000000, 1.000000000000000000 ) ) ;
#67217=FACE_OUTER_BOUND ( 'NONE', #68795, .T. ) ;
#67218=UNCERTAINTY_MEASURE_WITH_UNIT (LENGTH_MEASURE( 1.000000000000000082E-05 ), #43924, 'distance_accuracy_value', 'NONE');
#67221=CARTESIAN_POINT ( 'NONE',  ( 48.50000000000000000, 13.41640786499872284, -7.500000000000000000 ) ) ;
#67222=VERTEX_POINT ( 'NONE', #45307 ) ;
#67223=( NAMED_UNIT ( * ) PLANE_ANGLE_UNIT ( ) SI_UNIT ( $, .RADIAN. ) );
#67229=DIRECTION ( 'NONE',  ( 0.000000000000000000, -0.000000000000000000, 1.000000000000000000 ) ) ;
#67232=DIRECTION ( 'NONE',  ( -0.000000000000000000, 1.000000000000000000, -0.000000000000000000 ) ) ;
#67234=CARTESIAN_POINT ( 'NONE',  ( -75.00000000000000000, 8.062885781073912739, -5.999999999999991118 ) ) ;
#67237=AXIS2_PLACEMENT_3D ( 'NONE', #43408, #44087, #26783 ) ;
#67241=CARTESIAN_POINT ( 'NONE',  ( 3.094860106618435136, 139.2949999999999591, -9.525000000000000355 ) ) ;
#67244=MECHANICAL_DESIGN_GEOMETRIC_PRESENTATION_REPRESENTATION('',(#5406),#54817);
#67246=VECTOR ( 'NONE', #60361, 1000.000000000000000 ) ;
#67252=FILL_AREA_STYLE ('',( #62649 ) ) ;
#67255=ORIENTED_EDGE ( 'NONE', *, *, #22431, .F. ) ;
#67258=EDGE_CURVE ( 'NONE', #48671, #64454, #2277, .T. ) ;
#67260=DIRECTION ( 'NONE',  ( 0.9704308468600219006, 0.2413793103448194366, 0.000000000000000000 ) ) ;
#67262=DIRECTION ( 'NONE',  ( -1.000000000000000000, 0.000000000000000000, 0.000000000000000000 ) ) ;
#67267=ORIENTED_EDGE ( 'NONE', *, *, #36363, .F. ) ;
#67268=DIRECTION ( 'NONE',  ( -0.000000000000000000, 1.000000000000000000, -0.000000000000000000 ) ) ;
#67269=( NAMED_UNIT ( * ) PLANE_ANGLE_UNIT ( ) SI_UNIT ( $, .RADIAN. ) );
#67271=EDGE_CURVE ( 'NONE', #36102, #6580, #60388, .T. ) ;
#67273=CARTESIAN_POINT ( 'NONE',  ( 19.89974874213240597, 115.4999999999999574, 10.00000000000000000 ) ) ;
#67274=ADVANCED_FACE ( 'NONE', ( #29784 ), #35056, .T. ) ;
#67276=CARTESIAN_POINT ( 'NONE',  ( -10.01517768586949231, 113.1949999999999790, -6.132527647946036459E-16 ) ) ;
#67277=STYLED_ITEM ( 'NONE', ( #37159 ), #4526 ) ;
#67278=ORIENTED_EDGE ( 'NONE', *, *, #13976, .F. ) ;
#67280=DIRECTION ( 'NONE',  ( 0.000000000000000000, 0.000000000000000000, 1.000000000000000000 ) ) ;
#67283=CARTESIAN_POINT ( 'NONE',  ( -2.607480562269095969, 122.4070736234661609, 8.024999999999986144 ) ) ;
#67284=ORIENTED_EDGE ( 'NONE', *, *, #51697, .F. ) ;
#67285=CARTESIAN_POINT ( 'NONE',  ( 10.01517768586949231, 142.8049999999999500, 1.839758294383810543E-15 ) ) ;
#67287=SURFACE_STYLE_USAGE ( .BOTH. , #51820 ) ;
#67290=FILL_AREA_STYLE_COLOUR ( '', #63577 ) ;
#67295=( GEOMETRIC_REPRESENTATION_CONTEXT ( 3 ) GLOBAL_UNCERTAINTY_ASSIGNED_CONTEXT ( ( #37688 ) ) GLOBAL_UNIT_ASSIGNED_CONTEXT ( ( #12808, #65934, #17765 ) ) REPRESENTATION_CONTEXT ( 'NONE', 'WORKASPACE' ) );
#67296=( NAMED_UNIT ( * ) PLANE_ANGLE_UNIT ( ) SI_UNIT ( $, .RADIAN. ) );
#67300=MECHANICAL_DESIGN_GEOMETRIC_PRESENTATION_REPRESENTATION('',(#21232),#24590);
#67303=VERTEX_POINT ( 'NONE', #4064 ) ;
#67305=CARTESIAN_POINT ( 'NONE',  ( -23.71231517720798010, 118.4999999999999716, -7.500000000000000000 ) ) ;
#67312=PRESENTATION_STYLE_ASSIGNMENT (( #34597 ) ) ;
#67313=CARTESIAN_POINT ( 'NONE',  ( 8.102448949553181734, 141.9950000000000045, -5.886773742842746238 ) ) ;
#67315=AXIS2_PLACEMENT_3D ( 'NONE', #2563, #40266, #28639 ) ;
#67316=CARTESIAN_POINT ( 'NONE',  ( 21.02379604162863913, 114.4999999999999574, 10.00000000000000000 ) ) ;
#67318=DIRECTION ( 'NONE',  ( -0.000000000000000000, -0.000000000000000000, -1.000000000000000000 ) ) ;
#67320=CIRCLE ( 'NONE', #25728, 0.5000000000000004441 ) ;
#67322=DIRECTION ( 'NONE',  ( 0.000000000000000000, 1.000000000000000000, -0.000000000000000000 ) ) ;
#67333=DIRECTION ( 'NONE',  ( 0.000000000000000000, 0.000000000000000000, 1.000000000000000000 ) ) ;
#67345=EDGE_CURVE ( 'NONE', #37946, #39825, #69492, .T. ) ;
#67350=ORIENTED_EDGE ( 'NONE', *, *, #23980, .T. ) ;
#67352=CARTESIAN_POINT ( 'NONE',  ( -74.99999999999998579, 50.00000000000000000, 9.500000000000000000 ) ) ;
#67353=EDGE_CURVE ( 'NONE', #29444, #6055, #118, .T. ) ;
#67354=( NAMED_UNIT ( * ) SI_UNIT ( $, .STERADIAN. ) SOLID_ANGLE_UNIT ( ) );
#67358=CARTESIAN_POINT ( 'NONE',  ( 2.607480562269076430, 132.9070736234661183, -8.025000000000000355 ) ) ;
#67363=COLOUR_RGB ( '', 0.08235294, 0.09019608, 0.10196078) ;
#67364=EDGE_LOOP ( 'NONE', ( #64241, #16488, #48023, #28941 ) ) ;
#67366=CARTESIAN_POINT ( 'NONE',  ( 15.98999599679679839, 146.4999999999999716, -7.500000000000000000 ) ) ;
#67368=( LENGTH_UNIT ( ) NAMED_UNIT ( * ) SI_UNIT ( .MILLI., .METRE. ) );
#67376=VECTOR ( 'NONE', #5092, 1000.000000000000000 ) ;
#67378=FILL_AREA_STYLE_COLOUR ( '', #17920 ) ;
#67380=FILL_AREA_STYLE ('',( #56840 ) ) ;
#67382=ORIENTED_EDGE ( 'NONE', *, *, #9666, .T. ) ;
#67383=SURFACE_SIDE_STYLE ('',( #45958 ) ) ;
#67385=SURFACE_STYLE_USAGE ( .BOTH. , #57532 ) ;
#67386=SURFACE_SIDE_STYLE ('',( #60707 ) ) ;
#67388=STYLED_ITEM ( 'NONE', ( #69660 ), #15314 ) ;
#67391=CARTESIAN_POINT ( 'NONE',  ( -1.166476076187854022E-15, 113.9449999999999932, 9.525000000000000355 ) ) ;
#67393=EDGE_CURVE ( 'NONE', #25423, #46060, #8705, .T. ) ;
#67394=( LENGTH_UNIT ( ) NAMED_UNIT ( * ) SI_UNIT ( .MILLI., .METRE. ) );
#67398=CARTESIAN_POINT ( 'NONE',  ( 7.632228543268607446, 122.0429263765338135, 2.479861379858954606 ) ) ;
#67399=DIRECTION ( 'NONE',  ( -1.000000000000000000, 0.000000000000000000, 0.000000000000000000 ) ) ;
#67407=CARTESIAN_POINT ( 'NONE',  ( 71.74137931034481142, 36.89918356738973415, 10.00000000000000000 ) ) ;
#67408=COLOUR_RGB ( '', 0.66274510, 0.83137255, 0.94901961) ;
#67410=DIRECTION ( 'NONE',  ( -1.000000000000000000, 4.336808689941999001E-16, -0.000000000000000000 ) ) ;
#67414=EDGE_CURVE ( 'NONE', #35956, #49132, #63520, .T. ) ;
#67415=CARTESIAN_POINT ( 'NONE',  ( 0.000000000000000000, 155.5550000000000068, -9.525000000000000355 ) ) ;
#67421=MECHANICAL_DESIGN_GEOMETRIC_PRESENTATION_REPRESENTATION('',(#40497),#41600);
#67423=FILL_AREA_STYLE ('',( #41779 ) ) ;
#67424=DIRECTION ( 'NONE',  ( -0.000000000000000000, -1.000000000000000000, -0.000000000000000000 ) ) ;
#67425=ADVANCED_FACE ( 'NONE', ( #64572 ), #10421, .F. ) ;
#67428=MECHANICAL_DESIGN_GEOMETRIC_PRESENTATION_REPRESENTATION('',(#19115),#32572);
#67430=LINE ( 'NONE', #45335, #49841 ) ;
#67433=ADVANCED_FACE ( 'NONE', ( #16748 ), #49782, .F. ) ;
#67442=ORIENTED_EDGE ( 'NONE', *, *, #32272, .T. ) ;
#67443=( GEOMETRIC_REPRESENTATION_CONTEXT ( 3 ) GLOBAL_UNCERTAINTY_ASSIGNED_CONTEXT ( ( #51688 ) ) GLOBAL_UNIT_ASSIGNED_CONTEXT ( ( #62567, #51341, #25970 ) ) REPRESENTATION_CONTEXT ( 'NONE', 'WORKASPACE' ) );
#67445=DIRECTION ( 'NONE',  ( 1.000000000000000000, 0.000000000000000000, 0.000000000000000000 ) ) ;
#67447=ORIENTED_EDGE ( 'NONE', *, *, #2671, .F. ) ;
#67448=CARTESIAN_POINT ( 'NONE',  ( 48.00000000000000000, 14.49137674618942562, 7.500000000000000000 ) ) ;
#67454=CARTESIAN_POINT ( 'NONE',  ( 4.716976649647096842, 148.7429263765338021, 6.492361379858953896 ) ) ;
#67463=FILL_AREA_STYLE ('',( #45019 ) ) ;
#67464=CARTESIAN_POINT ( 'NONE',  ( -45.89905495956740111, 9.405628579031729330, 3.102072197697236966 ) ) ;
#67465=DIRECTION ( 'NONE',  ( 0.4468085106382997385, 0.000000000000000000, -0.8946296187927071930 ) ) ;
#67466=CARTESIAN_POINT ( 'NONE',  ( -60.00000000000000000, -2.024042244987997205E-14, 7.500000000000000000 ) ) ;
#67468=DIRECTION ( 'NONE',  ( 1.000000000000000000, 0.000000000000000000, -0.000000000000000000 ) ) ;
#67470=CARTESIAN_POINT ( 'NONE',  ( 2.607480562268946311, 140.7070736234661581, 8.025000000000092726 ) ) ;
#67471=DIRECTION ( 'NONE',  ( -0.000000000000000000, -0.000000000000000000, -1.000000000000000000 ) ) ;
#67472=ADVANCED_FACE ( 'NONE', ( #27929 ), #22008, .T. ) ;
#67474=CARTESIAN_POINT ( 'NONE',  ( -74.50000000000001421, 36.50926243676796190, 10.00000000000000000 ) ) ;
#67477=STYLED_ITEM ( 'NONE', ( #33521 ), #52450 ) ;
#67478=ORIENTED_EDGE ( 'NONE', *, *, #32902, .F. ) ;
#67479=SURFACE_SIDE_STYLE ('',( #30171 ) ) ;
#67482=ORIENTED_EDGE ( 'NONE', *, *, #61431, .F. ) ;
#67485=DIRECTION ( 'NONE',  ( -1.000000000000000000, -0.000000000000000000, -0.000000000000000000 ) ) ;
#67488=CIRCLE ( 'NONE', #37205, 8.499999999999992895 ) ;
#67489=ORIENTED_EDGE ( 'NONE', *, *, #11675, .F. ) ;
#67490=EDGE_LOOP ( 'NONE', ( #22664, #26343, #69126, #21285 ) ) ;
#67491=CARTESIAN_POINT ( 'NONE',  ( -74.69168400679268416, 36.11678010213625356, -9.964505089229481527 ) ) ;
#67492=EDGE_CURVE ( 'NONE', #20552, #18963, #67685, .T. ) ;
#67493=( LENGTH_UNIT ( ) NAMED_UNIT ( * ) SI_UNIT ( .MILLI., .METRE. ) );
#67495=CARTESIAN_POINT ( 'NONE',  ( 8.150468726202566572, 154.4999999999999147, 4.948482742093330167 ) ) ;
#67496=MECHANICAL_DESIGN_GEOMETRIC_PRESENTATION_REPRESENTATION('',(#5671),#37210);
#67501=CARTESIAN_POINT ( 'NONE',  ( -5.598654528085808657, 117.7549999999999812, 7.705886871421373741 ) ) ;
#67509=ORIENTED_EDGE ( 'NONE', *, *, #33894, .T. ) ;
#67514=CARTESIAN_POINT ( 'NONE',  ( -7.632228543268607446, 145.6570736234661751, -2.479861379858953718 ) ) ;
#67515=EDGE_CURVE ( 'NONE', #57165, #64235, #39948, .T. ) ;
#67520=CARTESIAN_POINT ( 'NONE',  ( 71.62068965517238439, 63.58603185604027885, 7.000000000000000000 ) ) ;
#67521=DIRECTION ( 'NONE',  ( -1.000000000000000000, 0.000000000000000000, 0.000000000000000000 ) ) ;
#67522=EDGE_LOOP ( 'NONE', ( #25919, #56356, #48625, #37827, #16317 ) ) ;
#67523=ORIENTED_EDGE ( 'NONE', *, *, #1851, .T. ) ;
#67524=AXIS2_PLACEMENT_3D ( 'NONE', #11465, #831, #22726 ) ;
#67527=PRESENTATION_STYLE_ASSIGNMENT (( #55929 ) ) ;
#67528=AXIS2_PLACEMENT_3D ( 'NONE', #69352, #43010, #46905 ) ;
#67530=PRESENTATION_STYLE_ASSIGNMENT (( #18659 ) ) ;
#67533=VERTEX_POINT ( 'NONE', #30036 ) ;
#67536=EDGE_LOOP ( 'NONE', ( #31082, #28692 ) ) ;
#67538=DIRECTION ( 'NONE',  ( 0.000000000000000000, 0.000000000000000000, 1.000000000000000000 ) ) ;
#67540=ADVANCED_FACE ( 'NONE', ( #9297 ), #25455, .T. ) ;
#67542=CARTESIAN_POINT ( 'NONE',  ( -10.01517768586949231, 143.1949999999999932, -6.132527647946036459E-16 ) ) ;
#67546=VERTEX_POINT ( 'NONE', #36032 ) ;
#67548=CARTESIAN_POINT ( 'NONE',  ( 10.01517768586949408, 142.8049999999999500, 1.839758294383810543E-15 ) ) ;
#67550=SURFACE_STYLE_USAGE ( .BOTH. , #51372 ) ;
#67552=CARTESIAN_POINT ( 'NONE',  ( 4.716976649647099507, 119.6429263765338078, -6.492361379858953008 ) ) ;
#67553=DIRECTION ( 'NONE',  ( -0.000000000000000000, -0.000000000000000000, -1.000000000000000000 ) ) ;
#67556=CARTESIAN_POINT ( 'NONE',  ( -71.50000000000000000, 35.92875272052971525, 7.500000000000000000 ) ) ;
#67558=ORIENTED_EDGE ( 'NONE', *, *, #26464, .T. ) ;
#67567=DIRECTION ( 'NONE',  ( 0.000000000000000000, 1.000000000000000000, 0.000000000000000000 ) ) ;
#67572=CARTESIAN_POINT ( 'NONE',  ( -7.632228543268607446, 151.6570736234661751, -2.479861379858953718 ) ) ;
#67573=CARTESIAN_POINT ( 'NONE',  ( 75.00000000000000000, 19.97932849626379692, 6.162720495828319045 ) ) ;
#67574=( NAMED_UNIT ( * ) SI_UNIT ( $, .STERADIAN. ) SOLID_ANGLE_UNIT ( ) );
#67575=VERTEX_POINT ( 'NONE', #37102 ) ;
#67576=DIRECTION ( 'NONE',  ( 1.000000000000000000, -1.156482317317866302E-16, 0.000000000000000000 ) ) ;
#67580=SURFACE_STYLE_FILL_AREA ( #9197 ) ;
#67582=ORIENTED_EDGE ( 'NONE', *, *, #2041, .F. ) ;
#67583=FILL_AREA_STYLE_COLOUR ( '', #34040 ) ;
#67590=ORIENTED_EDGE ( 'NONE', *, *, #13920, .F. ) ;
#67592=AXIS2_PLACEMENT_3D ( 'NONE', #13169, #51873, #34628 ) ;
#67593=DIRECTION ( 'NONE',  ( -1.000000000000000000, 0.000000000000000000, 0.000000000000000000 ) ) ;
#67596=CARTESIAN_POINT ( 'NONE',  ( -9.058813317711338797, 143.3449999999999989, 2.943386871421373563 ) ) ;
#67602=LINE ( 'NONE', #55396, #16366 ) ;
#67606=SURFACE_STYLE_USAGE ( .BOTH. , #46185 ) ;
#67610=ORIENTED_EDGE ( 'NONE', *, *, #20909, .F. ) ;
#67611=CIRCLE ( 'NONE', #17077, 0.5000000000000004441 ) ;
#67612=DIRECTION ( 'NONE',  ( 1.000000000000000000, 0.000000000000000000, 0.000000000000000000 ) ) ;
#67613=VECTOR ( 'NONE', #7163, 1000.000000000000000 ) ;
#67615=CARTESIAN_POINT ( 'NONE',  ( 8.437984349512095861, 119.1929263765337907, 1.550032578732816828E-15 ) ) ;
#67620=ORIENTED_EDGE ( 'NONE', *, *, #59558, .F. ) ;
#67627=AXIS2_PLACEMENT_3D ( 'NONE', #29652, #66592, #18744 ) ;
#67630=CARTESIAN_POINT ( 'NONE',  ( 0.000000000000000000, 160.0570736234661524, -8.025000000000000355 ) ) ;
#67633=CARTESIAN_POINT ( 'NONE',  ( -1.166476076187854022E-15, 112.0549999999999926, 9.525000000000000355 ) ) ;
#67636=CARTESIAN_POINT ( 'NONE',  ( 5.598654528085805993, 139.3549999999999898, 7.705886871421374629 ) ) ;
#67638=( NAMED_UNIT ( * ) PLANE_ANGLE_UNIT ( ) SI_UNIT ( $, .RADIAN. ) );
#67639=CIRCLE ( 'NONE', #56377, 0.5000000000000004441 ) ;
#67640=( NAMED_UNIT ( * ) PLANE_ANGLE_UNIT ( ) SI_UNIT ( $, .RADIAN. ) );
#67641=CARTESIAN_POINT ( 'NONE',  ( -40.99999999999998579, 107.7459666924148252, 3.099782425413943443 ) ) ;
#67642=( GEOMETRIC_REPRESENTATION_CONTEXT ( 3 ) GLOBAL_UNCERTAINTY_ASSIGNED_CONTEXT ( ( #41260 ) ) GLOBAL_UNIT_ASSIGNED_CONTEXT ( ( #2355, #18617, #51655 ) ) REPRESENTATION_CONTEXT ( 'NONE', 'WORKASPACE' ) );
#67643=SURFACE_STYLE_FILL_AREA ( #63049 ) ;
#67645=DIRECTION ( 'NONE',  ( 0.000000000000000000, 0.000000000000000000, 1.000000000000000000 ) ) ;
#67646=PRESENTATION_STYLE_ASSIGNMENT (( #45540 ) ) ;
#67648=EDGE_LOOP ( 'NONE', ( #33009, #42489 ) ) ;
#67656=COLOUR_RGB ( '', 0.72549020, 0.75294118, 0.79215686) ;
#67657=DIRECTION ( 'NONE',  ( 1.000000000000000000, 0.000000000000000000, 0.000000000000000000 ) ) ;
#67660=LINE ( 'NONE', #24382, #8094 ) ;
#67661=ADVANCED_FACE ( 'NONE', ( #58864 ), #53255, .T. ) ;
#67662=CARTESIAN_POINT ( 'NONE',  ( -74.99999999999998579, 50.00000000000000000, 7.000000000000000000 ) ) ;
#67665=CARTESIAN_POINT ( 'NONE',  ( 3.094860106618431583, 141.0949999999999989, 9.525000000000000355 ) ) ;
#67675=CARTESIAN_POINT ( 'NONE',  ( 21.02379604162863913, 110.4999999999999858, 10.50000000000000000 ) ) ;
#67676=CARTESIAN_POINT ( 'NONE',  ( 0.000000000000000000, 110.4999999999999858, 0.000000000000000000 ) ) ;
#67685=LINE ( 'NONE', #2197, #1904 ) ;
#67687=DIRECTION ( 'NONE',  ( -0.000000000000000000, -1.000000000000000000, -0.000000000000000000 ) ) ;
#67688=MECHANICAL_DESIGN_GEOMETRIC_PRESENTATION_REPRESENTATION('',(#37412),#46374);
#67693=LINE ( 'NONE', #30043, #57901 ) ;
#67695=CARTESIAN_POINT ( 'NONE',  ( 74.50000000000000000, 19.30628705663858469, 6.999999999999999112 ) ) ;
#67701=AXIS2_PLACEMENT_3D ( 'NONE', #24314, #34189, #44781 ) ;
#67705=COLOUR_RGB ( '', 0.72549020, 0.75294118, 0.79215686) ;
#67709=FILL_AREA_STYLE ('',( #51188 ) ) ;
#67710=SURFACE_SIDE_STYLE ('',( #63119 ) ) ;
#67711=VERTEX_POINT ( 'NONE', #33174 ) ;
#67715=( LENGTH_UNIT ( ) NAMED_UNIT ( * ) SI_UNIT ( .MILLI., .METRE. ) );
#67716=CARTESIAN_POINT ( 'NONE',  ( -6.826472737025120807, 131.1070736234661638, 4.959722759717906548 ) ) ;
#67718=TOROIDAL_SURFACE ( 'NONE', #58724, 7.499999999999998224, 0.5000000000000000000 ) ;
#67724=CLOSED_SHELL ( 'NONE', ( #35026, #9582, #16339, #42236, #28172, #50445, #28816, #41486, #40130, #28357, #30819, #29193, #60270, #63194, #55339, #52202, #20002, #68392, #58615, #51459, #3627, #56794, #29389, #32716, #35773, #44065, #41333, #10900, #39144, #56131, #63614, #30940, #48652, #38257, #33605, #32276, #68723, #41232, #64025, #60292, #42141, #21789, #10891, #54120, #46264, #42623, #56833, #35309, #1334, #57995, #47003, #49121, #61247, #16648, #1783, #35828, #8906, #20646, #60433, #57326, #65354, #47693, #60819, #47057, #17813, #28829, #23900, #24173, #65777, #65246, #4948, #32251, #65992, #35779, #43534, #52940, #23274, #32163, #25118, #16951, #51001, #38234, #43363, #30359, #26600, #68785, #57848, #39347, #36751, #52566, #51621, #66751, #29449, #13999, #66674, #38962, #1868, #12527, #4768, #28085, #5388, #56460, #1741, #37215, #63755, #8013, #50279, #30399, #646, #50506, #65643, #19120, #44686, #11205, #29799, #49191, #67921, #36818, #19531, #64822, #22340, #33954, #60917, #67274, #10382, #24919, #24302, #12629, #48180, #56267, #69040, #17883, #13010, #22638, #12491, #50999, #15619, #252, #69257, #58937, #32089, #6906, #8759, #58207, #1109, #8233, #38742, #45698, #3698, #5127, #28234, #43439, #17160, #7878, #12804, #50394, #21691, #63859, #40143, #34613, #11664, #2568, #28103, #1177, #7618, #36673, #26973, #40225, #4196, #21278, #11533, #28849, #48335, #324, #11987, #2427, #4509, #48029, #60410, #61971, #14160, #508, #63109, #51228, #52385, #953, #47220, #46858, #60190, #43560, #25627, #41280, #14700, #33134, #31064, #26656, #39122, #59292, #22661, #35927, #30480, #67540, #26884, #51511, #19930, #10177, #36502, #28413, #6454, #14985, #10590, #68566, #16001, #28742, #655, #32306, #22097, #9712, #4435, #18831, #35444, #27838, #28807, #51092, #2312, #11509, #19473, #17923, #7774, #55842, #12139, #5150, #49780, #15038, #50993, #20075, #19408, #8448, #14875, #56123, #47145, #11966, #63145, #5396, #40879, #65115, #48177, #13601, #36174, #54871, #24846, #6072, #47845, #46191, #16422, #59708, #37996, #50731, #41858, #6977, #31349, #23814, #20089, #24837, #14060, #34863, #52528, #26459, #61849, #8360, #25190, #52450, #4408, #7858, #57156, #61447, #43323, #21929, #60998, #53924, #62992, #5718, #57712, #65101, #14964, #8571, #65984, #27772, #46256, #40490, #16855, #42856, #41578, #34548, #52916, #5800, #15603, #34790, #45092, #19668, #67102, #11468, #55087, #26115, #59600, #36609, #12707, #38514, #48567, #38236, #27846, #54644, #51078, #58874, #17314, #17033, #41361, #14812, #52525, #48750, #55669, #39202, #6816, #9569, #29206, #22077, #59871, #63938, #30860, #35510, #16578, #68959, #9738, #64489, #2910, #49130, #45997, #34733, #54849, #32465, #21057, #20656, #67433, #26314, #66610, #50223, #38664, #66717, #46513, #8662, #32592, #54548, #69676, #15314, #64573, #18369, #22165, #54393, #24315, #67472, #49897, #22481, #41802, #21122, #20490, #11453, #35839, #29531, #29705, #3795, #64439, #24930, #1450, #6571, #45407, #16264, #37076, #48104, #56231, #61368, #33173, #34693, #66905, #60722, #64234, #23634, #8375, #1791, #54541, #310, #43940, #61927, #47136, #48654, #53301, #46, #62492, #40798, #43032, #54315, #44762, #53599, #38897, #58308, #22837, #53616, #1993, #4754, #14526, #57826, #30729, #16335, #971, #35600, #51466, #66391, #38903, #61844, #46308, #66631, #54983, #44058, #17719, #67425, #55902, #23821, #56306, #48203, #41399, #47812, #62618, #10848, #67661, #14177, #1457, #42555, #54765, #5619, #60505, #51390, #41836, #56073, #34512, #61952, #69414, #56173, #17576, #19772, #50074, #58687, #7806, #53305, #31515, #37546, #4526, #33046, #25881, #59098, #55054, #1547, #25017, #47148, #68068, #50902, #3945, #49822, #61294, #57568, #21212, #7080, #57094, #55997, #54527, #35438, #38249, #39675, #58471, #27767, #27490, #39268, #49883, #33509, #7097, #17186, #62491, #18880, #65394, #3751, #10598, #6209, #64083, #56464, #64125, #36824, #49078, #45950, #34609, #32962, #59192, #4680, #35833, #6402, #35959, #35666, #64492, #26271, #10958, #38152, #26043, #61053, #60985, #19050, #64804, #6352, #56376, #10970, #53752, #19535, #18384, #43738, #57369, #68169, #7416, #37006, #18826, #36661, #2752, #36069, #43194, #21526, #29103, #9719, #22257, #41659, #7795, #47025, #15456, #50284, #60022, #67143, #30235, #54093, #67097, #59169, #2733, #48072, #20423, #22385, #64745, #4295, #49572, #58993, #2084, #51808, #25549, #63996, #52907, #10426 ) ) ;
#67725=FILL_AREA_STYLE_COLOUR ( '', #61973 ) ;
#67726=( LENGTH_UNIT ( ) NAMED_UNIT ( * ) SI_UNIT ( .MILLI., .METRE. ) );
#67729=ORIENTED_EDGE ( 'NONE', *, *, #59001, .F. ) ;
#67730=( GEOMETRIC_REPRESENTATION_CONTEXT ( 3 ) GLOBAL_UNCERTAINTY_ASSIGNED_CONTEXT ( ( #13000 ) ) GLOBAL_UNIT_ASSIGNED_CONTEXT ( ( #34505, #6723, #54573 ) ) REPRESENTATION_CONTEXT ( 'NONE', 'WORKASPACE' ) );
#67731=CARTESIAN_POINT ( 'NONE',  ( -71.99999999999998579, 119.9999999999997868, 7.000000000000000000 ) ) ;
#67732=UNCERTAINTY_MEASURE_WITH_UNIT (LENGTH_MEASURE( 1.000000000000000082E-05 ), #9636, 'distance_accuracy_value', 'NONE');
#67736=DIRECTION ( 'NONE',  ( 0.000000000000000000, 1.000000000000000000, 0.000000000000000000 ) ) ;
#67737=SURFACE_SIDE_STYLE ('',( #9709 ) ) ;
#67747=CARTESIAN_POINT ( 'NONE',  ( -5.598654528085806881, 115.7449999999999903, -7.705886871421374629 ) ) ;
#67752=ORIENTED_EDGE ( 'NONE', *, *, #23832, .T. ) ;
#67754=EDGE_CURVE ( 'NONE', #42377, #8109, #16330, .T. ) ;
#67760=SURFACE_SIDE_STYLE ('',( #29415 ) ) ;
#67762=EDGE_CURVE ( 'NONE', #18324, #56663, #7773, .T. ) ;
#67763=( GEOMETRIC_REPRESENTATION_CONTEXT ( 3 ) GLOBAL_UNCERTAINTY_ASSIGNED_CONTEXT ( ( #5118 ) ) GLOBAL_UNIT_ASSIGNED_CONTEXT ( ( #52629, #24812, #46331 ) ) REPRESENTATION_CONTEXT ( 'NONE', 'WORKASPACE' ) );
#67765=VERTEX_POINT ( 'NONE', #49037 ) ;
#67767=CIRCLE ( 'NONE', #68883, 0.5000000000000004441 ) ;
#67769=EDGE_CURVE ( 'NONE', #2776, #10312, #726, .T. ) ;
#67770=DIRECTION ( 'NONE',  ( 1.000000000000000000, 0.000000000000000000, -0.000000000000000000 ) ) ;
#67771=UNCERTAINTY_MEASURE_WITH_UNIT (LENGTH_MEASURE( 1.000000000000000082E-05 ), #63060, 'distance_accuracy_value', 'NONE');
#67773=CARTESIAN_POINT ( 'NONE',  ( -45.00000000000000000, 9.999999999999980460, 3.000000000000000000 ) ) ;
#67775=CARTESIAN_POINT ( 'NONE',  ( -8.102448949553181734, 159.0049999999999670, -5.886773742842749790 ) ) ;
#67776=DIRECTION ( 'NONE',  ( -0.000000000000000000, -0.000000000000000000, 1.000000000000000000 ) ) ;
#67785=VECTOR ( 'NONE', #47627, 1000.000000000000000 ) ;
#67786=AXIS2_PLACEMENT_3D ( 'NONE', #38756, #54185, #69678 ) ;
#67789=SURFACE_STYLE_FILL_AREA ( #9408 ) ;
#67790=ORIENTED_EDGE ( 'NONE', *, *, #5314, .F. ) ;
#67791=VERTEX_POINT ( 'NONE', #56702 ) ;
#67792=SURFACE_SIDE_STYLE ('',( #56888 ) ) ;
#67793=UNCERTAINTY_MEASURE_WITH_UNIT (LENGTH_MEASURE( 1.000000000000000082E-05 ), #31833, 'distance_accuracy_value', 'NONE');
#67795=EDGE_CURVE ( 'NONE', #50095, #62857, #35242, .T. ) ;
#67797=AXIS2_PLACEMENT_3D ( 'NONE', #68480, #2400, #20277 ) ;
#67800=ORIENTED_EDGE ( 'NONE', *, *, #23132, .F. ) ;
#67801=ORIENTED_EDGE ( 'NONE', *, *, #67045, .T. ) ;
#67802=SURFACE_SIDE_STYLE ('',( #56895 ) ) ;
#67803=ORIENTED_EDGE ( 'NONE', *, *, #69634, .T. ) ;
#67804=CARTESIAN_POINT ( 'NONE',  ( 48.00000000000000000, 99.99999999999992895, -7.500000000000000000 ) ) ;
#67809=CARTESIAN_POINT ( 'NONE',  ( 40.49999999999998579, 107.7459666924148252, -3.000000000000000444 ) ) ;
#67812=AXIS2_PLACEMENT_3D ( 'NONE', #26108, #58147, #14903 ) ;
#67813=CARTESIAN_POINT ( 'NONE',  ( -9.527307077157137982, 110.5000000000000568, 0.3845708726071553896 ) ) ;
#67817=CARTESIAN_POINT ( 'NONE',  ( 7.632228543268608334, 143.3429263765338249, -2.479861379858951942 ) ) ;
#67820=EDGE_CURVE ( 'NONE', #43189, #15660, #39508, .T. ) ;
#67825=VERTEX_POINT ( 'NONE', #8170 ) ;
#67829=DIRECTION ( 'NONE',  ( -0.000000000000000000, -0.000000000000000000, -1.000000000000000000 ) ) ;
#67830=DIRECTION ( 'NONE',  ( -0.000000000000000000, -0.000000000000000000, -1.000000000000000000 ) ) ;
#67835=SURFACE_SIDE_STYLE ('',( #46410 ) ) ;
#67836=VECTOR ( 'NONE', #19620, 1000.000000000000000 ) ;
#67841=VERTEX_POINT ( 'NONE', #66917 ) ;
#67843=CARTESIAN_POINT ( 'NONE',  ( 15.48999599679679662, 118.4999999999999716, 9.500000000000000000 ) ) ;
#67845=CIRCLE ( 'NONE', #55477, 26.99999999999999645 ) ;
#67846=FILL_AREA_STYLE_COLOUR ( '', #6226 ) ;
#67851=DIRECTION ( 'NONE',  ( -0.000000000000000000, -1.000000000000000000, -0.000000000000000000 ) ) ;
#67853=EDGE_CURVE ( 'NONE', #60166, #24214, #35728, .T. ) ;
#67854=CIRCLE ( 'NONE', #68966, 5.000000000000004441 ) ;
#67856=SURFACE_STYLE_USAGE ( .BOTH. , #24915 ) ;
#67857=ORIENTED_EDGE ( 'NONE', *, *, #43660, .F. ) ;
#67868=CARTESIAN_POINT ( 'NONE',  ( -10.01517768586949231, 129.3050000000000068, -6.132527647946036459E-16 ) ) ;
#67871=( GEOMETRIC_REPRESENTATION_CONTEXT ( 3 ) GLOBAL_UNCERTAINTY_ASSIGNED_CONTEXT ( ( #65690 ) ) GLOBAL_UNIT_ASSIGNED_CONTEXT ( ( #7244, #29008, #23402 ) ) REPRESENTATION_CONTEXT ( 'NONE', 'WORKASPACE' ) );
#67872=DIRECTION ( 'NONE',  ( -0.000000000000000000, -0.000000000000000000, -1.000000000000000000 ) ) ;
#67875=DIRECTION ( 'NONE',  ( 1.000000000000000000, 0.000000000000000000, 0.000000000000000000 ) ) ;
#67876=DIRECTION ( 'NONE',  ( 0.000000000000000000, 1.000000000000000000, 0.000000000000000000 ) ) ;
#67880=CARTESIAN_POINT ( 'NONE',  ( -2.607480562268989832, 145.2070736234661581, -8.025000000000060751 ) ) ;
#67881=MECHANICAL_DESIGN_GEOMETRIC_PRESENTATION_REPRESENTATION('',(#19557),#25186);
#67882=DIRECTION ( 'NONE',  ( -0.000000000000000000, -0.000000000000000000, -1.000000000000000000 ) ) ;
#67883=CARTESIAN_POINT ( 'NONE',  ( 4.716976649647096842, 134.8570736234661638, 6.492361379858953896 ) ) ;
#67890=COLOUR_RGB ( '', 0.31764706, 0.68627451, 0.89019608) ;
#67893=FACE_OUTER_BOUND ( 'NONE', #27381, .T. ) ;
#67905=CARTESIAN_POINT ( 'NONE',  ( 9.058813317711337021, 138.5449999999999875, 2.943386871421375783 ) ) ;
#67911=CARTESIAN_POINT ( 'NONE',  ( -9.058813317711338797, 150.4550000000000125, 2.943386871421373563 ) ) ;
#67913=FILL_AREA_STYLE_COLOUR ( '', #19517 ) ;
#67916=CARTESIAN_POINT ( 'NONE',  ( -4.716976649647098618, 112.1429263765338220, 6.492361379858953008 ) ) ;
#67917=CARTESIAN_POINT ( 'NONE',  ( -52.00000000000000000, -1.926070501056209087E-14, 12.00000000000000000 ) ) ;
#67919=LINE ( 'NONE', #19709, #9379 ) ;
#67920=( NAMED_UNIT ( * ) PLANE_ANGLE_UNIT ( ) SI_UNIT ( $, .RADIAN. ) );
#67921=ADVANCED_FACE ( 'NONE', ( #19034, #13080 ), #21822, .T. ) ;
#67924=EDGE_LOOP ( 'NONE', ( #67482, #52693, #28476, #4160 ) ) ;
#67926=ORIENTED_EDGE ( 'NONE', *, *, #48160, .F. ) ;
#67930=PRESENTATION_STYLE_ASSIGNMENT (( #46861 ) ) ;
#67935=EDGE_CURVE ( 'NONE', #16524, #57704, #54506, .T. ) ;
#67936=DIRECTION ( 'NONE',  ( 0.000000000000000000, 0.000000000000000000, 1.000000000000000000 ) ) ;
#67937=CARTESIAN_POINT ( 'NONE',  ( -6.826472737025120807, 151.5070736234661979, -4.959722759717907437 ) ) ;
#67938=CARTESIAN_POINT ( 'NONE',  ( 75.00000000000000000, 19.38064346792905823, 6.520279032830130994 ) ) ;
#67940=ORIENTED_EDGE ( 'NONE', *, *, #25557, .T. ) ;
#67941=PRESENTATION_STYLE_ASSIGNMENT (( #40877 ) ) ;
#67946=FACE_OUTER_BOUND ( 'NONE', #65170, .T. ) ;
#67949=ORIENTED_EDGE ( 'NONE', *, *, #41571, .T. ) ;
#67950=FACE_OUTER_BOUND ( 'NONE', #40598, .T. ) ;
#67954=ORIENTED_EDGE ( 'NONE', *, *, #37200, .F. ) ;
#67955=CARTESIAN_POINT ( 'NONE',  ( -75.00000000000000000, 9.708372675170618749, -6.000000000000000000 ) ) ;
#67957=DIRECTION ( 'NONE',  ( 1.000000000000000000, 0.000000000000000000, 0.000000000000000000 ) ) ;
#67958=DIRECTION ( 'NONE',  ( -0.000000000000000000, -0.000000000000000000, -1.000000000000000000 ) ) ;
#67959=CARTESIAN_POINT ( 'NONE',  ( -8.102448949553181734, 151.8950000000000102, -5.886773742842749790 ) ) ;
#67962=LINE ( 'NONE', #35943, #31441 ) ;
#67963=EDGE_CURVE ( 'NONE', #20480, #28179, #42543, .T. ) ;
#67964=UNCERTAINTY_MEASURE_WITH_UNIT (LENGTH_MEASURE( 1.000000000000000082E-05 ), #50689, 'distance_accuracy_value', 'NONE');
#67965=MECHANICAL_DESIGN_GEOMETRIC_PRESENTATION_REPRESENTATION('',(#23011),#58957);
#67966=CARTESIAN_POINT ( 'NONE',  ( -7.632228543268607446, 144.5429263765338135, -2.479861379858953718 ) ) ;
#67967=AXIS2_PLACEMENT_3D ( 'NONE', #43904, #1227, #39305 ) ;
#67968=EDGE_LOOP ( 'NONE', ( #24358, #37517, #27789, #68193 ) ) ;
#67972=AXIS2_PLACEMENT_3D ( 'NONE', #30620, #25359, #68282 ) ;
#67973=CARTESIAN_POINT ( 'NONE',  ( 41.49999999999998579, 99.99999999999998579, 3.000000000000000000 ) ) ;
#67975=MECHANICAL_DESIGN_GEOMETRIC_PRESENTATION_REPRESENTATION('',(#54484),#52266);
#67976=( NAMED_UNIT ( * ) SI_UNIT ( $, .STERADIAN. ) SOLID_ANGLE_UNIT ( ) );
#67978=CARTESIAN_POINT ( 'NONE',  ( -7.632228543268607446, 129.5429263765338135, -2.479861379858953718 ) ) ;
#67979=ORIENTED_EDGE ( 'NONE', *, *, #67492, .F. ) ;
#67980=MECHANICAL_DESIGN_GEOMETRIC_PRESENTATION_REPRESENTATION('',(#23028),#25273);
#67981=CARTESIAN_POINT ( 'NONE',  ( -6.422934014168760974, 111.9999999999999858, 4.811085495980506721 ) ) ;
#67987=COLOUR_RGB ( '', 0.09019608, 0.27058824, 0.51372549) ;
#67993=CARTESIAN_POINT ( 'NONE',  ( -7.632228543268607446, 157.6570736234661467, -2.479861379858953718 ) ) ;
#67994=COLOUR_RGB ( '', 0.08235294, 0.09019608, 0.10196078) ;
#67999=CARTESIAN_POINT ( 'NONE',  ( 3.094860106618431583, 115.2049999999999841, 9.525000000000000355 ) ) ;
#68001=AXIS2_PLACEMENT_3D ( 'NONE', #50901, #60396, #2995 ) ;
#68002=VERTEX_POINT ( 'NONE', #22510 ) ;
#68003=CARTESIAN_POINT ( 'NONE',  ( -8.102448949553181734, 135.6049999999999613, 5.886773742842747126 ) ) ;
#68004=UNCERTAINTY_MEASURE_WITH_UNIT (LENGTH_MEASURE( 1.000000000000000082E-05 ), #20803, 'distance_accuracy_value', 'NONE');
#68007=( LENGTH_UNIT ( ) NAMED_UNIT ( * ) SI_UNIT ( .MILLI., .METRE. ) );
#68008=( LENGTH_UNIT ( ) NAMED_UNIT ( * ) SI_UNIT ( .MILLI., .METRE. ) );
#68013=VERTEX_POINT ( 'NONE', #22160 ) ;
#68015=STYLED_ITEM ( 'NONE', ( #63594 ), #8360 ) ;
#68017=EDGE_LOOP ( 'NONE', ( #27571, #4573, #39027, #6815 ) ) ;
#68018=( NAMED_UNIT ( * ) SI_UNIT ( $, .STERADIAN. ) SOLID_ANGLE_UNIT ( ) );
#68021=DIRECTION ( 'NONE',  ( -0.000000000000000000, -0.000000000000000000, -1.000000000000000000 ) ) ;
#68022=MECHANICAL_DESIGN_GEOMETRIC_PRESENTATION_REPRESENTATION('',(#51143),#20814);
#68023=CARTESIAN_POINT ( 'NONE',  ( 65.49999999999997158, 1.797044900979284448E-15, 12.00000000000000000 ) ) ;
#68027=FACE_OUTER_BOUND ( 'NONE', #46138, .T. ) ;
#68032=CARTESIAN_POINT ( 'NONE',  ( 5.598654528085805993, 147.2449999999999761, 7.705886871421374629 ) ) ;
#68035=ORIENTED_EDGE ( 'NONE', *, *, #5783, .T. ) ;
#68036=CARTESIAN_POINT ( 'NONE',  ( -74.49999999999998579, 64.49137674618943095, -9.500000000000000000 ) ) ;
#68039=COLOUR_RGB ( '', 0.31764706, 0.68627451, 0.89019608) ;
#68041=EDGE_CURVE ( 'NONE', #7407, #65484, #5609, .T. ) ;
#68042=CARTESIAN_POINT ( 'NONE',  ( 9.058813317711337021, 111.5449999999999875, 2.943386871421375783 ) ) ;
#68044=STYLED_ITEM ( 'NONE', ( #1754 ), #57995 ) ;
#68049=FILL_AREA_STYLE ('',( #51863 ) ) ;
#68054=CARTESIAN_POINT ( 'NONE',  ( -2.607480562269073321, 124.2070736234661581, -8.025000000000000355 ) ) ;
#68057=EDGE_LOOP ( 'NONE', ( #68189, #2309, #6110, #57809 ) ) ;
#68066=ORIENTED_EDGE ( 'NONE', *, *, #1699, .F. ) ;
#68068=ADVANCED_FACE ( 'NONE', ( #38389 ), #59791, .T. ) ;
#68069=PRESENTATION_STYLE_ASSIGNMENT (( #14587 ) ) ;
#68071=ORIENTED_EDGE ( 'NONE', *, *, #22570, .T. ) ;
#68073=STYLED_ITEM ( 'NONE', ( #65715 ), #5718 ) ;
#68075=CARTESIAN_POINT ( 'NONE',  ( 4.716976649647099507, 132.7570736234661695, -6.492361379858953008 ) ) ;
#68077=VERTEX_POINT ( 'NONE', #34440 ) ;
#68081=EDGE_LOOP ( 'NONE', ( #16865, #3877, #17164, #22662, #33308, #15346, #40374, #6021 ) ) ;
#68082=DIRECTION ( 'NONE',  ( -0.000000000000000000, -1.000000000000000000, 0.000000000000000000 ) ) ;
#68083=CIRCLE ( 'NONE', #2843, 7.500000000000007105 ) ;
#68085=CARTESIAN_POINT ( 'NONE',  ( -60.00000000000000000, -2.024042244987997205E-14, -11.50000000000000355 ) ) ;
#68098=CARTESIAN_POINT ( 'NONE',  ( 65.50000000000000000, 1.797044900979284448E-15, -6.500000000000000000 ) ) ;
#68100=SURFACE_SIDE_STYLE ('',( #52616 ) ) ;
#68103=ORIENTED_EDGE ( 'NONE', *, *, #68161, .T. ) ;
#68106=CARTESIAN_POINT ( 'NONE',  ( -34.99999999999992895, 110.4999999999999858, -10.00000000000000000 ) ) ;
#68109=CARTESIAN_POINT ( 'NONE',  ( -5.598654528085808657, 113.6449999999999818, 7.705886871421373741 ) ) ;
#68115=CARTESIAN_POINT ( 'NONE',  ( -52.00000000000000000, -1.926070501056209087E-14, 10.50000000000000000 ) ) ;
#68118=DIRECTION ( 'NONE',  ( 0.000000000000000000, 0.000000000000000000, 1.000000000000000000 ) ) ;
#68126=SURFACE_STYLE_FILL_AREA ( #46712 ) ;
#68127=CARTESIAN_POINT ( 'NONE',  ( 20.83146879675249963, 149.9524772093542708, -9.749920261344563244 ) ) ;
#68129=CARTESIAN_POINT ( 'NONE',  ( -74.99999999999998579, 50.00000000000000000, -10.00000000000000000 ) ) ;
#68133=CARTESIAN_POINT ( 'NONE',  ( -5.598654528085808657, 156.7549999999999670, 7.705886871421373741 ) ) ;
#68134=MECHANICAL_DESIGN_GEOMETRIC_PRESENTATION_REPRESENTATION('',(#20930),#42321);
#68138=DIRECTION ( 'NONE',  ( 0.000000000000000000, 0.000000000000000000, 1.000000000000000000 ) ) ;
#68147=CARTESIAN_POINT ( 'NONE',  ( -20.71462257042821520, 114.4999999999999574, 10.00000000000000355 ) ) ;
#68149=EDGE_CURVE ( 'NONE', #7058, #43960, #49287, .T. ) ;
#68150=( NAMED_UNIT ( * ) SI_UNIT ( $, .STERADIAN. ) SOLID_ANGLE_UNIT ( ) );
#68151=EDGE_LOOP ( 'NONE', ( #22440, #1489, #34001, #41346 ) ) ;
#68154=CYLINDRICAL_SURFACE ( 'NONE', #6188, 0.5000000000000004441 ) ;
#68157=CARTESIAN_POINT ( 'NONE',  ( 10.01517768586949231, 121.8049999999999784, 1.839758294383810543E-15 ) ) ;
#68158=DIRECTION ( 'NONE',  ( -0.000000000000000000, -0.000000000000000000, -1.000000000000000000 ) ) ;
#68161=EDGE_CURVE ( 'NONE', #6517, #11358, #3782, .T. ) ;
#68162=AXIS2_PLACEMENT_3D ( 'NONE', #21887, #21524, #53542 ) ;
#68166=EDGE_LOOP ( 'NONE', ( #15351, #22123, #67447, #32694 ) ) ;
#68167=CARTESIAN_POINT ( 'NONE',  ( -9.436264504443260037, 110.5000000000000284, -1.368519874741629172 ) ) ;
#68169=ADVANCED_FACE ( 'NONE', ( #52383 ), #51318, .T. ) ;
#68170=LINE ( 'NONE', #8022, #58689 ) ;
#68172=CARTESIAN_POINT ( 'NONE',  ( 7.632228543268608334, 155.3429263765338249, -2.479861379858951942 ) ) ;
#68178=ORIENTED_EDGE ( 'NONE', *, *, #53556, .F. ) ;
#68179=CARTESIAN_POINT ( 'NONE',  ( 20.44220712062818635, 115.3857587453612865, 10.00000000000000000 ) ) ;
#68181=SURFACE_SIDE_STYLE ('',( #63580 ) ) ;
#68186=CARTESIAN_POINT ( 'NONE',  ( -74.13102528387565826, 9.253287829606156478, 6.241231906388601480 ) ) ;
#68187=DIRECTION ( 'NONE',  ( -0.000000000000000000, -0.000000000000000000, 1.000000000000000000 ) ) ;
#68188=ORIENTED_EDGE ( 'NONE', *, *, #15292, .T. ) ;
#68189=ORIENTED_EDGE ( 'NONE', *, *, #35606, .T. ) ;
#68190=CARTESIAN_POINT ( 'NONE',  ( -15.98999599679679839, 146.9999999999999716, -7.500000000000000000 ) ) ;
#68191=DIRECTION ( 'NONE',  ( -1.000000000000000000, 0.000000000000000000, 0.000000000000000000 ) ) ;
#68192=CARTESIAN_POINT ( 'NONE',  ( -75.50000000000000000, 64.49137674618943095, 6.499999999999999112 ) ) ;
#68193=ORIENTED_EDGE ( 'NONE', *, *, #39228, .F. ) ;
#68194=SURFACE_SIDE_STYLE ('',( #57274 ) ) ;
#68199=CARTESIAN_POINT ( 'NONE',  ( 40.83001745922079806, 108.1251451958518146, 3.311254650320280213 ) ) ;
#68201=EDGE_CURVE ( 'NONE', #20613, #55582, #25711, .T. ) ;
#68203=FILL_AREA_STYLE ('',( #9117 ) ) ;
#68206=FILL_AREA_STYLE_COLOUR ( '', #33160 ) ;
#68207=PRESENTATION_STYLE_ASSIGNMENT (( #14745 ) ) ;
#68208=CARTESIAN_POINT ( 'NONE',  ( -20.71231517720798010, 110.4999999999999858, 10.00000000000000000 ) ) ;
#68211=CARTESIAN_POINT ( 'NONE',  ( -9.058813317711337021, 123.1549999999999869, -2.943386871421374895 ) ) ;
#68215=CIRCLE ( 'NONE', #21001, 0.5000000000000000000 ) ;
#68219=ORIENTED_EDGE ( 'NONE', *, *, #45629, .F. ) ;
#68223=AXIS2_PLACEMENT_3D ( 'NONE', #36070, #25489, #26770 ) ;
#68224=EDGE_CURVE ( 'NONE', #38783, #57325, #25600, .T. ) ;
#68225=CARTESIAN_POINT ( 'NONE',  ( -75.50000000000000000, 64.49137674618943095, -10.00000000000000000 ) ) ;
#68229=ORIENTED_EDGE ( 'NONE', *, *, #10261, .F. ) ;
#68231=CARTESIAN_POINT ( 'NONE',  ( 0.000000000000000000, 131.9429263765338192, -8.025000000000000355 ) ) ;
#68232=EDGE_CURVE ( 'NONE', #16380, #66646, #40352, .T. ) ;
#68235=PRESENTATION_STYLE_ASSIGNMENT (( #30567 ) ) ;
#68240=DIRECTION ( 'NONE',  ( 0.000000000000000000, 0.000000000000000000, 1.000000000000000000 ) ) ;
#68243=DIRECTION ( 'NONE',  ( 0.000000000000000000, 1.000000000000000000, 0.000000000000000000 ) ) ;
#68245=ORIENTED_EDGE ( 'NONE', *, *, #52996, .T. ) ;
#68248=CARTESIAN_POINT ( 'NONE',  ( 8.102448949553183510, 150.9950000000000045, -5.886773742842746238 ) ) ;
#68250=CARTESIAN_POINT ( 'NONE',  ( -3.094860106618434248, 150.9049999999999727, 9.525000000000000355 ) ) ;
#68254=ORIENTED_EDGE ( 'NONE', *, *, #34541, .T. ) ;
#68255=CARTESIAN_POINT ( 'NONE',  ( -6.826472737025120807, 114.9929263765338163, 4.959722759717906548 ) ) ;
#68256=( LENGTH_UNIT ( ) NAMED_UNIT ( * ) SI_UNIT ( .MILLI., .METRE. ) );
#68257=CARTESIAN_POINT ( 'NONE',  ( 45.00000000000000000, 9.999999999999992895, 6.000000000000001776 ) ) ;
#68258=CIRCLE ( 'NONE', #45827, 0.5000000000000004441 ) ;
#68260=CARTESIAN_POINT ( 'NONE',  ( 20.94636006565341191, 149.9999999999999716, -9.500000000000000000 ) ) ;
#68261=( GEOMETRIC_REPRESENTATION_CONTEXT ( 3 ) GLOBAL_UNCERTAINTY_ASSIGNED_CONTEXT ( ( #22939 ) ) GLOBAL_UNIT_ASSIGNED_CONTEXT ( ( #36645, #52790, #68266 ) ) REPRESENTATION_CONTEXT ( 'NONE', 'WORKASPACE' ) );
#68266=( NAMED_UNIT ( * ) SI_UNIT ( $, .STERADIAN. ) SOLID_ANGLE_UNIT ( ) );
#68270=FACE_OUTER_BOUND ( 'NONE', #26079, .T. ) ;
#68271=CARTESIAN_POINT ( 'NONE',  ( -74.99999999999998579, 50.00000000000000000, -10.00000000000000000 ) ) ;
#68274=CARTESIAN_POINT ( 'NONE',  ( 8.437984349512095861, 146.1929263765338192, 1.550032578732816828E-15 ) ) ;
#68275=EDGE_LOOP ( 'NONE', ( #66500, #33361, #35796, #25773 ) ) ;
#68281=FILL_AREA_STYLE ('',( #67583 ) ) ;
#68282=DIRECTION ( 'NONE',  ( 0.000000000000000000, -3.469446951953614189E-15, -1.000000000000000000 ) ) ;
#68283=ORIENTED_EDGE ( 'NONE', *, *, #28325, .F. ) ;
#68285=CARTESIAN_POINT ( 'NONE',  ( -74.09571531523221211, 9.387774908331740775, -6.120769290545540642 ) ) ;
#68290=CARTESIAN_POINT ( 'NONE',  ( -9.058813317711338797, 149.3449999999999989, 2.943386871421373563 ) ) ;
#68296=CARTESIAN_POINT ( 'NONE',  ( -7.632228543268608334, 144.8429263765338249, 2.479861379858952830 ) ) ;
#68300=( NAMED_UNIT ( * ) SI_UNIT ( $, .STERADIAN. ) SOLID_ANGLE_UNIT ( ) );
#68302=DIRECTION ( 'NONE',  ( 0.000000000000000000, -1.000000000000000000, 0.000000000000000000 ) ) ;
#68307=DIRECTION ( 'NONE',  ( 1.000000000000000000, 0.000000000000000000, 0.000000000000000000 ) ) ;
#68308=SURFACE_STYLE_USAGE ( .BOTH. , #69347 ) ;
#68309=FILL_AREA_STYLE ('',( #30284 ) ) ;
#68310=ORIENTED_EDGE ( 'NONE', *, *, #26889, .T. ) ;
#68311=( GEOMETRIC_REPRESENTATION_CONTEXT ( 3 ) GLOBAL_UNCERTAINTY_ASSIGNED_CONTEXT ( ( #33392 ) ) GLOBAL_UNIT_ASSIGNED_CONTEXT ( ( #42824, #31858, #20975 ) ) REPRESENTATION_CONTEXT ( 'NONE', 'WORKASPACE' ) );
#68312=( NAMED_UNIT ( * ) PLANE_ANGLE_UNIT ( ) SI_UNIT ( $, .RADIAN. ) );
#68314=EDGE_CURVE ( 'NONE', #7436, #15321, #56043, .T. ) ;
#68315=CARTESIAN_POINT ( 'NONE',  ( -4.716976649647098618, 118.1429263765338078, 6.492361379858953008 ) ) ;
#68316=CARTESIAN_POINT ( 'NONE',  ( 4.716976649647099507, 119.6429263765338078, -6.492361379858953008 ) ) ;
#68320=MECHANICAL_DESIGN_GEOMETRIC_PRESENTATION_REPRESENTATION('',(#21112),#42492);
#68321=ORIENTED_EDGE ( 'NONE', *, *, #56539, .T. ) ;
#68324=CARTESIAN_POINT ( 'NONE',  ( -21.02379604162863558, 114.6409683457797115, -9.999999999999998224 ) ) ;
#68326=EDGE_LOOP ( 'NONE', ( #63676, #22632, #36256, #20760 ) ) ;
#68328=CARTESIAN_POINT ( 'NONE',  ( -10.01517768586949231, 125.1950000000000074, -6.132527647946036459E-16 ) ) ;
#68331=CARTESIAN_POINT ( 'NONE',  ( -5.598654528085806881, 116.8549999999999898, -7.705886871421374629 ) ) ;
#68336=CARTESIAN_POINT ( 'NONE',  ( 10.01517768586949231, 133.8049999999999784, 1.839758294383810543E-15 ) ) ;
#68337=DIRECTION ( 'NONE',  ( -1.000000000000000000, 0.000000000000000000, 0.000000000000000000 ) ) ;
#68340=DIRECTION ( 'NONE',  ( 1.000000000000000000, 0.000000000000000000, 0.000000000000000000 ) ) ;
#68343=DIRECTION ( 'NONE',  ( -1.000000000000000000, 0.000000000000000000, 0.000000000000000000 ) ) ;
#68344=DIRECTION ( 'NONE',  ( 1.000000000000000000, 0.000000000000000000, 0.000000000000000000 ) ) ;
#68346=VERTEX_POINT ( 'NONE', #37614 ) ;
#68350=CYLINDRICAL_SURFACE ( 'NONE', #34300, 0.5000000000000004441 ) ;
#68362=FACE_OUTER_BOUND ( 'NONE', #26960, .T. ) ;
#68368=DIRECTION ( 'NONE',  ( 3.469446951953611033E-15, 0.000000000000000000, 1.000000000000000000 ) ) ;
#68370=CARTESIAN_POINT ( 'NONE',  ( -45.00000000000000000, 99.99999999999992895, 10.00000000000000000 ) ) ;
#68371=CARTESIAN_POINT ( 'NONE',  ( 9.058813317711338797, 117.8449999999999847, -2.943386871421372675 ) ) ;
#68376=ORIENTED_EDGE ( 'NONE', *, *, #22968, .F. ) ;
#68377=CARTESIAN_POINT ( 'NONE',  ( 23.21231517720798010, 117.4999999999999716, -9.500000000000000000 ) ) ;
#68386=MECHANICAL_DESIGN_GEOMETRIC_PRESENTATION_REPRESENTATION('',(#36997),#4320);
#68387=DIRECTION ( 'NONE',  ( -0.7833176619561783571, 0.6216216216216310375, 0.000000000000000000 ) ) ;
#68392=ADVANCED_FACE ( 'NONE', ( #42892 ), #22076, .F. ) ;
#68393=FACE_OUTER_BOUND ( 'NONE', #8557, .T. ) ;
#68395=EDGE_CURVE ( 'NONE', #57600, #56195, #39661, .T. ) ;
#68396=( LENGTH_UNIT ( ) NAMED_UNIT ( * ) SI_UNIT ( .MILLI., .METRE. ) );
#68400=( LENGTH_UNIT ( ) NAMED_UNIT ( * ) SI_UNIT ( .MILLI., .METRE. ) );
#68405=CARTESIAN_POINT ( 'NONE',  ( -6.826472737025120807, 137.1070736234661354, 4.959722759717906548 ) ) ;
#68407=AXIS2_PLACEMENT_3D ( 'NONE', #41665, #63081, #31061 ) ;
#68408=ORIENTED_EDGE ( 'NONE', *, *, #41565, .F. ) ;
#68412=EDGE_LOOP ( 'NONE', ( #3185, #24366, #60881, #36805 ) ) ;
#68413=SURFACE_STYLE_USAGE ( .BOTH. , #4019 ) ;
#68414=CARTESIAN_POINT ( 'NONE',  ( 34.99999999999999289, 99.99999999999998579, -3.500000000000000000 ) ) ;
#68422=CARTESIAN_POINT ( 'NONE',  ( -74.99999999999998579, 50.00000000000000000, -12.00000000000000000 ) ) ;
#68424=( GEOMETRIC_REPRESENTATION_CONTEXT ( 3 ) GLOBAL_UNCERTAINTY_ASSIGNED_CONTEXT ( ( #26360 ) ) GLOBAL_UNIT_ASSIGNED_CONTEXT ( ( #9467, #35499, #24921 ) ) REPRESENTATION_CONTEXT ( 'NONE', 'WORKASPACE' ) );
#68430=DIRECTION ( 'NONE',  ( 0.000000000000000000, 1.000000000000000000, 0.000000000000000000 ) ) ;
#68431=ORIENTED_EDGE ( 'NONE', *, *, #41671, .T. ) ;
#68432=( NAMED_UNIT ( * ) SI_UNIT ( $, .STERADIAN. ) SOLID_ANGLE_UNIT ( ) );
#68433=EDGE_LOOP ( 'NONE', ( #2346, #54821, #59655, #17344 ) ) ;
#68435=( NAMED_UNIT ( * ) SI_UNIT ( $, .STERADIAN. ) SOLID_ANGLE_UNIT ( ) );
#68440=CARTESIAN_POINT ( 'NONE',  ( -10.01517768586949408, 119.1949999999999790, -6.132527647946036459E-16 ) ) ;
#68443=FACE_OUTER_BOUND ( 'NONE', #17802, .T. ) ;
#68447=SURFACE_STYLE_USAGE ( .BOTH. , #57904 ) ;
#68449=CARTESIAN_POINT ( 'NONE',  ( -71.62068965517238439, 63.58603185604027885, 7.500000000000000000 ) ) ;
#68451=CARTESIAN_POINT ( 'NONE',  ( -3.148793198257116455, 110.7976376722492802, -8.711325744658216408 ) ) ;
#68454=MECHANICAL_DESIGN_GEOMETRIC_PRESENTATION_REPRESENTATION('',(#54963),#19019);
#68459=EDGE_CURVE ( 'NONE', #47153, #34665, #23454, .T. ) ;
#68460=CARTESIAN_POINT ( 'NONE',  ( 20.76401515593078884, 149.8168068008927492, -9.892342186632994583 ) ) ;
#68461=UNCERTAINTY_MEASURE_WITH_UNIT (LENGTH_MEASURE( 1.000000000000000082E-05 ), #55868, 'distance_accuracy_value', 'NONE');
#68463=DIRECTION ( 'NONE',  ( 0.9704308468600219006, 0.2413793103448194366, -0.000000000000000000 ) ) ;
#68466=CARTESIAN_POINT ( 'NONE',  ( -3.094860106618434248, 159.9050000000000011, 9.525000000000000355 ) ) ;
#68467=CARTESIAN_POINT ( 'NONE',  ( -44.50000000000000000, 99.99999999999992895, -3.500000000000000000 ) ) ;
#68469=FILL_AREA_STYLE_COLOUR ( '', #828 ) ;
#68470=COLOUR_RGB ( '', 0.08235294, 0.09019608, 0.10196078) ;
#68471=VECTOR ( 'NONE', #2961, 1000.000000000000000 ) ;
#68476=DIRECTION ( 'NONE',  ( -0.000000000000000000, -1.000000000000000000, 0.000000000000000000 ) ) ;
#68477=AXIS2_PLACEMENT_3D ( 'NONE', #26128, #6065, #27150 ) ;
#68479=CARTESIAN_POINT ( 'NONE',  ( -24.21231517720798365, 50.00000000000000000, 7.500000000000000000 ) ) ;
#68480=CARTESIAN_POINT ( 'NONE',  ( 0.000000000000000000, 115.4999999999999574, 0.000000000000000000 ) ) ;
#68481=CIRCLE ( 'NONE', #61716, 9.999999999999998224 ) ;
#68487=AXIS2_PLACEMENT_3D ( 'NONE', #9318, #41343, #9677 ) ;
#68491=AXIS2_PLACEMENT_3D ( 'NONE', #5015, #58489, #21184 ) ;
#68492=CARTESIAN_POINT ( 'NONE',  ( -20.03861782943699765, 115.4999999895429994, 10.00000000000000000 ) ) ;
#68497=ORIENTED_EDGE ( 'NONE', *, *, #56720, .T. ) ;
#68500=CYLINDRICAL_SURFACE ( 'NONE', #38394, 0.5000000000000004441 ) ;
#68502=CARTESIAN_POINT ( 'NONE',  ( 10.01517768586949231, 115.8049999999999784, 1.839758294383810543E-15 ) ) ;
#68503=SURFACE_SIDE_STYLE ('',( #58981 ) ) ;
#68504=DIRECTION ( 'NONE',  ( -0.000000000000000000, -0.000000000000000000, -1.000000000000000000 ) ) ;
#68506=ORIENTED_EDGE ( 'NONE', *, *, #48826, .T. ) ;
#68508=CARTESIAN_POINT ( 'NONE',  ( -9.384346074379580571, 110.5000000000000000, 1.688215766215464653 ) ) ;
#68510=PLANE ( 'NONE',  #24998 ) ;
#68511=EDGE_LOOP ( 'NONE', ( #6161, #27361, #37671 ) ) ;
#68512=CARTESIAN_POINT ( 'NONE',  ( 4.716976649647096842, 151.7429263765338021, 6.492361379858953896 ) ) ;
#68513=FILL_AREA_STYLE ('',( #61813 ) ) ;
#68517=CYLINDRICAL_SURFACE ( 'NONE', #27087, 4.999999999999997335 ) ;
#68522=CARTESIAN_POINT ( 'NONE',  ( 7.632228543268607446, 141.1570736234661751, 2.479861379858954606 ) ) ;
#68525=CARTESIAN_POINT ( 'NONE',  ( -69.99999999999998579, 50.00000000000000000, 11.50000000000003730 ) ) ;
#68532=DIRECTION ( 'NONE',  ( 0.000000000000000000, 0.000000000000000000, 1.000000000000000000 ) ) ;
#68535=FILL_AREA_STYLE ('',( #31572 ) ) ;
#68539=EDGE_CURVE ( 'NONE', #11684, #24423, #51588, .T. ) ;
#68549=AXIS2_PLACEMENT_3D ( 'NONE', #38593, #59988, #11800 ) ;
#68550=EDGE_CURVE ( 'NONE', #19233, #69035, #50205, .T. ) ;
#68553=CARTESIAN_POINT ( 'NONE',  ( 9.058813317711338797, 130.9549999999999841, -2.943386871421372675 ) ) ;
#68555=EDGE_CURVE ( 'NONE', #37991, #61027, #23800, .T. ) ;
#68556=CARTESIAN_POINT ( 'NONE',  ( -75.00000000000001421, 9.708372675170622301, -6.100541755698617230 ) ) ;
#68558=B_SPLINE_CURVE_WITH_KNOTS ( 'NONE', 3,
 ( #19894, #9729, #31136, #36819 ),
 .UNSPECIFIED., .F., .F.,
 ( 4, 4 ),
 ( 0.000000000000000000, 0.0004221139024916740600 ),
 .UNSPECIFIED. ) ;
#68559=MECHANICAL_DESIGN_GEOMETRIC_PRESENTATION_REPRESENTATION('',(#46139),#47256);
#68561=CARTESIAN_POINT ( 'NONE',  ( 68.00000000000000000, 2.776762340297169183E-15, -11.50000000000000000 ) ) ;
#68562=UNCERTAINTY_MEASURE_WITH_UNIT (LENGTH_MEASURE( 1.000000000000000082E-05 ), #51975, 'distance_accuracy_value', 'NONE');
#68566=ADVANCED_FACE ( 'NONE', ( #62116 ), #6682, .T. ) ;
#68571=SURFACE_STYLE_USAGE ( .BOTH. , #4159 ) ;
#68573=ORIENTED_EDGE ( 'NONE', *, *, #23832, .F. ) ;
#68574=( NAMED_UNIT ( * ) PLANE_ANGLE_UNIT ( ) SI_UNIT ( $, .RADIAN. ) );
#68580=CARTESIAN_POINT ( 'NONE',  ( -57.99999999999997868, 50.00000000000000000, -6.500000000000000000 ) ) ;
#68581=DIRECTION ( 'NONE',  ( -0.000000000000000000, 1.000000000000000000, -0.000000000000000000 ) ) ;
#68586=ORIENTED_EDGE ( 'NONE', *, *, #12783, .T. ) ;
#68587=SURFACE_SIDE_STYLE ('',( #15487 ) ) ;
#68590=VECTOR ( 'NONE', #21362, 1000.000000000000000 ) ;
#68593=CARTESIAN_POINT ( 'NONE',  ( -5.598654528085808657, 146.6450000000000102, 7.705886871421373741 ) ) ;
#68596=CARTESIAN_POINT ( 'NONE',  ( -8.102448949553179958, 150.0049999999999386, -5.886773742842749790 ) ) ;
#68597=FILL_AREA_STYLE ('',( #69615 ) ) ;
#68598=VECTOR ( 'NONE', #51596, 1000.000000000000000 ) ;
#68601=CARTESIAN_POINT ( 'NONE',  ( 8.437984349512095861, 128.1929263765338192, 1.550032578732817026E-15 ) ) ;
#68602=CARTESIAN_POINT ( 'NONE',  ( 45.65811388300841855, 10.21937129433612057, -3.598410089384286081 ) ) ;
#68603=UNCERTAINTY_MEASURE_WITH_UNIT (LENGTH_MEASURE( 1.000000000000000082E-05 ), #56852, 'distance_accuracy_value', 'NONE');
#68606=CARTESIAN_POINT ( 'NONE',  ( 0.000000000000000000, 127.0570736234661666, -8.025000000000000355 ) ) ;
#68608=CIRCLE ( 'NONE', #47308, 9.999999999999998224 ) ;
#68612=DIRECTION ( 'NONE',  ( 1.000000000000000000, 0.000000000000000000, 0.000000000000000000 ) ) ;
#68614=ORIENTED_EDGE ( 'NONE', *, *, #2107, .F. ) ;
#68615=DIRECTION ( 'NONE',  ( -0.000000000000000000, -0.000000000000000000, -1.000000000000000000 ) ) ;
#68621=CARTESIAN_POINT ( 'NONE',  ( -71.50000000000000000, 14.49137674618942562, -7.500000000000000000 ) ) ;
#68627=ORIENTED_EDGE ( 'NONE', *, *, #30321, .F. ) ;
#68632=EDGE_LOOP ( 'NONE', ( #1734, #46154, #44973, #16288 ) ) ;
#68633=EDGE_CURVE ( 'NONE', #53241, #14677, #20608, .T. ) ;
#68634=CARTESIAN_POINT ( 'NONE',  ( -74.08452722211991670, 9.430195805462506797, -6.024500123752368985 ) ) ;
#68635=DIRECTION ( 'NONE',  ( -1.000000000000000000, 0.000000000000000000, 0.000000000000000000 ) ) ;
#68639=CARTESIAN_POINT ( 'NONE',  ( 0.000000000000000000, 145.4449999999999932, -9.525000000000000355 ) ) ;
#68641=CIRCLE ( 'NONE', #14762, 0.5000000000000004441 ) ;
#68643=SURFACE_SIDE_STYLE ('',( #37015 ) ) ;
#68645=STYLED_ITEM ( 'NONE', ( #28840 ), #34733 ) ;
#68648=CARTESIAN_POINT ( 'NONE',  ( -41.45361433042954502, 107.0152407614178713, -3.500000000000000888 ) ) ;
#68649=ORIENTED_EDGE ( 'NONE', *, *, #32300, .F. ) ;
#68657=CARTESIAN_POINT ( 'NONE',  ( 71.49999999999998579, 64.07124727947029896, 7.500000000000000000 ) ) ;
#68658=MECHANICAL_DESIGN_GEOMETRIC_PRESENTATION_REPRESENTATION('',(#32677),#16999);
#68660=EDGE_LOOP ( 'NONE', ( #9194, #47521 ) ) ;
#68661=MECHANICAL_DESIGN_GEOMETRIC_PRESENTATION_REPRESENTATION('',(#11348),#13549);
#68662=DIRECTION ( 'NONE',  ( -0.000000000000000000, 1.000000000000000000, -0.000000000000000000 ) ) ;
#68663=UNCERTAINTY_MEASURE_WITH_UNIT (LENGTH_MEASURE( 1.000000000000000082E-05 ), #12972, 'distance_accuracy_value', 'NONE');
#68666=CARTESIAN_POINT ( 'NONE',  ( -45.00000000000000000, 8.189963308881127446, 5.659193869480894534 ) ) ;
#68670=ORIENTED_EDGE ( 'NONE', *, *, #14038, .F. ) ;
#68674=VERTEX_POINT ( 'NONE', #4394 ) ;
#68675=CARTESIAN_POINT ( 'NONE',  ( 15.98999599679679839, 146.9999999999999716, -10.00000000000000000 ) ) ;
#68677=CARTESIAN_POINT ( 'NONE',  ( -9.058813317711338797, 122.3449999999999847, 2.943386871421373563 ) ) ;
#68679=EDGE_CURVE ( 'NONE', #22515, #30516, #31168, .T. ) ;
#68682=CARTESIAN_POINT ( 'NONE',  ( 0.000000000000000000, 116.5549999999999926, -9.525000000000000355 ) ) ;
#68687=EDGE_LOOP ( 'NONE', ( #61395, #22589, #54650, #51476 ) ) ;
#68688=CARTESIAN_POINT ( 'NONE',  ( -1.166476076187854022E-15, 148.0549999999999784, 9.525000000000000355 ) ) ;
#68691=CARTESIAN_POINT ( 'NONE',  ( -14.98999599679679662, 118.4999999999999716, -9.500000000000000000 ) ) ;
#68692=( GEOMETRIC_REPRESENTATION_CONTEXT ( 3 ) GLOBAL_UNCERTAINTY_ASSIGNED_CONTEXT ( ( #16014 ) ) GLOBAL_UNIT_ASSIGNED_CONTEXT ( ( #7411, #995, #38425 ) ) REPRESENTATION_CONTEXT ( 'NONE', 'WORKASPACE' ) );
#68696=CARTESIAN_POINT ( 'NONE',  ( 74.50000000000000000, 19.30628705663858113, -6.500000000000000000 ) ) ;
#68697=DIRECTION ( 'NONE',  ( 1.000000000000000000, -0.000000000000000000, -0.000000000000000000 ) ) ;
#68700=ORIENTED_EDGE ( 'NONE', *, *, #51619, .T. ) ;
#68701=CARTESIAN_POINT ( 'NONE',  ( 8.586026971066655022, 111.4549650702766570, -0.1239747060112400823 ) ) ;
#68704=ORIENTED_EDGE ( 'NONE', *, *, #278, .F. ) ;
#68705=( NAMED_UNIT ( * ) SI_UNIT ( $, .STERADIAN. ) SOLID_ANGLE_UNIT ( ) );
#68706=CARTESIAN_POINT ( 'NONE',  ( -15.98999599679679839, 146.4999999999999716, 10.00000000000000000 ) ) ;
#68711=( LENGTH_UNIT ( ) NAMED_UNIT ( * ) SI_UNIT ( .MILLI., .METRE. ) );
#68713=ORIENTED_EDGE ( 'NONE', *, *, #37933, .T. ) ;
#68719=AXIS2_PLACEMENT_3D ( 'NONE', #66663, #39960, #61364 ) ;
#68720=CARTESIAN_POINT ( 'NONE',  ( -5.598654528085808657, 152.6449999999999818, 7.705886871421373741 ) ) ;
#68723=ADVANCED_FACE ( 'NONE', ( #58241 ), #36826, .F. ) ;
#68725=ORIENTED_EDGE ( 'NONE', *, *, #44458, .F. ) ;
#68728=( GEOMETRIC_REPRESENTATION_CONTEXT ( 3 ) GLOBAL_UNCERTAINTY_ASSIGNED_CONTEXT ( ( #39899 ) ) GLOBAL_UNIT_ASSIGNED_CONTEXT ( ( #279, #53478, #10567 ) ) REPRESENTATION_CONTEXT ( 'NONE', 'WORKASPACE' ) );
#68729=PRESENTATION_STYLE_ASSIGNMENT (( #47301 ) ) ;
#68732=CARTESIAN_POINT ( 'NONE',  ( -8.102448949553181734, 118.8949999999999676, -5.886773742842749790 ) ) ;
#68735=AXIS2_PLACEMENT_3D ( 'NONE', #35862, #58027, #14765 ) ;
#68740=AXIS2_PLACEMENT_3D ( 'NONE', #3615, #14935, #64397 ) ;
#68745=CARTESIAN_POINT ( 'NONE',  ( 0.000000000000000000, 124.0570736234661524, -8.025000000000000355 ) ) ;
#68755=CARTESIAN_POINT ( 'NONE',  ( 7.632228543268607446, 152.0429263765338135, 2.479861379858954606 ) ) ;
#68756=CARTESIAN_POINT ( 'NONE',  ( 4.716976649647096842, 146.8570736234661638, 6.492361379858953896 ) ) ;
#68760=VECTOR ( 'NONE', #48586, 1000.000000000000000 ) ;
#68762=( NAMED_UNIT ( * ) PLANE_ANGLE_UNIT ( ) SI_UNIT ( $, .RADIAN. ) );
#68765=CYLINDRICAL_SURFACE ( 'NONE', #10645, 5.000000000000004441 ) ;
#68766=CARTESIAN_POINT ( 'NONE',  ( -7.632228543268607446, 145.6570736234661751, -2.479861379858953718 ) ) ;
#68767=EDGE_CURVE ( 'NONE', #37491, #7436, #37075, .T. ) ;
#68769=DIRECTION ( 'NONE',  ( -0.000000000000000000, -0.000000000000000000, -1.000000000000000000 ) ) ;
#68771=UNCERTAINTY_MEASURE_WITH_UNIT (LENGTH_MEASURE( 1.000000000000000082E-05 ), #14219, 'distance_accuracy_value', 'NONE');
#68774=VERTEX_POINT ( 'NONE', #6844 ) ;
#68775=DIRECTION ( 'NONE',  ( 0.000000000000000000, 1.000000000000000000, -0.000000000000000000 ) ) ;
#68776=CARTESIAN_POINT ( 'NONE',  ( -9.827790563157511022E-16, 134.5570736234661808, 8.025000000000000355 ) ) ;
#68779=ORIENTED_EDGE ( 'NONE', *, *, #25967, .T. ) ;
#68780=CARTESIAN_POINT ( 'NONE',  ( 60.00000000000000000, -2.024042244987997205E-14, -9.500000000000000000 ) ) ;
#68783=CARTESIAN_POINT ( 'NONE',  ( 23.21231517720797655, 118.4999999999999716, -7.500000000000000000 ) ) ;
#68785=ADVANCED_FACE ( 'NONE', ( #2187 ), #12455, .F. ) ;
#68788=LINE ( 'NONE', #58915, #9465 ) ;
#68795=EDGE_LOOP ( 'NONE', ( #11914, #49669, #17497, #20754 ) ) ;
#68802=SURFACE_SIDE_STYLE ('',( #58227 ) ) ;
#68804=CARTESIAN_POINT ( 'NONE',  ( -9.058813317711337021, 122.0449999999999875, -2.943386871421374895 ) ) ;
#68806=TOROIDAL_SURFACE ( 'NONE', #21582, 1.000000000000000000, 0.5000000000000000000 ) ;
#68809=FACE_OUTER_BOUND ( 'NONE', #38674, .T. ) ;
#68811=EDGE_CURVE ( 'NONE', #17063, #19777, #15705, .T. ) ;
#68814=DIRECTION ( 'NONE',  ( 1.000000000000000000, 0.000000000000000000, 0.000000000000000000 ) ) ;
#68815=COLOUR_RGB ( '', 0.40784314, 0.44705882, 0.49803922) ;
#68819=VERTEX_POINT ( 'NONE', #6157 ) ;
#68822=CARTESIAN_POINT ( 'NONE',  ( 0.000000000000000000, 111.9999999999999858, -8.025000000000000355 ) ) ;
#68823=LINE ( 'NONE', #46713, #23726 ) ;
#68825=PRESENTATION_STYLE_ASSIGNMENT (( #21294 ) ) ;
#68826=AXIS2_PLACEMENT_3D ( 'NONE', #16713, #38178, #765 ) ;
#68827=CARTESIAN_POINT ( 'NONE',  ( -9.058813317711338797, 156.4549999999999841, 2.943386871421373563 ) ) ;
#68828=FACE_OUTER_BOUND ( 'NONE', #25044, .T. ) ;
#68830=EDGE_CURVE ( 'NONE', #9977, #51271, #17898, .T. ) ;
#68832=AXIS2_PLACEMENT_3D ( 'NONE', #32674, #49925, #33710 ) ;
#68836=CYLINDRICAL_SURFACE ( 'NONE', #30442, 0.5000000000000004441 ) ;
#68838=FILL_AREA_STYLE_COLOUR ( '', #47678 ) ;
#68840=CARTESIAN_POINT ( 'NONE',  ( 74.65811388300841145, 19.88603796100278487, -6.000000000000000000 ) ) ;
#68843=SURFACE_SIDE_STYLE ('',( #47062 ) ) ;
#68844=VECTOR ( 'NONE', #49318, 1000.000000000000000 ) ;
#68845=CARTESIAN_POINT ( 'NONE',  ( -6.826472737025120807, 116.1070736234661496, 4.959722759717906548 ) ) ;
#68848=VERTEX_POINT ( 'NONE', #55384 ) ;
#68854=CARTESIAN_POINT ( 'NONE',  ( -20.94636006565341191, 149.9999999999999716, 9.500000000000000000 ) ) ;
#68856=CARTESIAN_POINT ( 'NONE',  ( -8.102448949553181734, 117.0049999999999670, -5.886773742842749790 ) ) ;
#68862=ORIENTED_EDGE ( 'NONE', *, *, #65365, .T. ) ;
#68863=B_SPLINE_CURVE_WITH_KNOTS ( 'NONE', 3,
 ( #63660, #26689, #36969, #11225, #63995, #4555, #32329, #53781, #42591, #59392 ),
 .UNSPECIFIED., .F., .F.,
 ( 4, 2, 2, 2, 4 ),
 ( -6.387773809479085465E-06, 0.0006440562338507882902, 0.0009692782376809175489, 0.001131889239595995677, 0.001294500241511073804 ),
 .UNSPECIFIED. ) ;
#68864=AXIS2_PLACEMENT_3D ( 'NONE', #53808, #67142, #65765 ) ;
#68865=CARTESIAN_POINT ( 'NONE',  ( -9.064020486552543332, 110.4999999999999858, 2.960432884595932901 ) ) ;
#68866=( NAMED_UNIT ( * ) PLANE_ANGLE_UNIT ( ) SI_UNIT ( $, .RADIAN. ) );
#68867=EDGE_CURVE ( 'NONE', #20480, #19090, #44190, .T. ) ;
#68869=ORIENTED_EDGE ( 'NONE', *, *, #40707, .T. ) ;
#68870=CARTESIAN_POINT ( 'NONE',  ( -8.437984349512095861, 150.6929263765338192, -5.166775262442723748E-16 ) ) ;
#68873=EDGE_CURVE ( 'NONE', #22128, #49325, #8913, .T. ) ;
#68874=CARTESIAN_POINT ( 'NONE',  ( -20.71231517720797299, 149.6390813561872619, -10.00000000000000000 ) ) ;
#68875=CARTESIAN_POINT ( 'NONE',  ( 20.77797364267480518, 115.1388508835393907, -10.00000000000000000 ) ) ;
#68877=FACE_OUTER_BOUND ( 'NONE', #7579, .T. ) ;
#68879=( GEOMETRIC_REPRESENTATION_CONTEXT ( 3 ) GLOBAL_UNCERTAINTY_ASSIGNED_CONTEXT ( ( #20618 ) ) GLOBAL_UNIT_ASSIGNED_CONTEXT ( ( #47102, #63586, #31913 ) ) REPRESENTATION_CONTEXT ( 'NONE', 'WORKASPACE' ) );
#68880=TOROIDAL_SURFACE ( 'NONE', #26167, 1.000000000000000000, 0.5000000000000000000 ) ;
#68881=CARTESIAN_POINT ( 'NONE',  ( -15.48999599679679662, 118.4999999999999716, 9.500000000000000000 ) ) ;
#68882=DIRECTION ( 'NONE',  ( 1.000000000000000000, 0.000000000000000000, 0.000000000000000000 ) ) ;
#68883=AXIS2_PLACEMENT_3D ( 'NONE', #45013, #4104, #52690 ) ;
#68884=CARTESIAN_POINT ( 'NONE',  ( -74.08452722063037754, 9.430195807687216103, 6.000000000000000888 ) ) ;
#68889=ORIENTED_EDGE ( 'NONE', *, *, #65931, .T. ) ;
#68892=CARTESIAN_POINT ( 'NONE',  ( 0.000000000000000000, 114.9999999999999574, 0.000000000000000000 ) ) ;
#68893=CARTESIAN_POINT ( 'NONE',  ( 2.607480562269098634, 113.7070736234661723, 8.024999999999984368 ) ) ;
#68894=ORIENTED_EDGE ( 'NONE', *, *, #39135, .F. ) ;
#68895=PRESENTATION_STYLE_ASSIGNMENT (( #19972 ) ) ;
#68902=VERTEX_POINT ( 'NONE', #46254 ) ;
#68903=VECTOR ( 'NONE', #58384, 1000.000000000000000 ) ;
#68904=CARTESIAN_POINT ( 'NONE',  ( 60.00000000000000000, -2.024042244987997205E-14, -9.500000000000000000 ) ) ;
#68906=CIRCLE ( 'NONE', #37509, 0.5000000000000004441 ) ;
#68908=( NAMED_UNIT ( * ) PLANE_ANGLE_UNIT ( ) SI_UNIT ( $, .RADIAN. ) );
#68909=CARTESIAN_POINT ( 'NONE',  ( -74.91404241719055790, 35.67552983406591949, -9.789663199941575300 ) ) ;
#68910=COLOUR_RGB ( '', 0.66274510, 0.83137255, 0.94901961) ;
#68913=CARTESIAN_POINT ( 'NONE',  ( -9.058813317711337021, 129.1550000000000011, -2.943386871421374895 ) ) ;
#68914=DIRECTION ( 'NONE',  ( 0.000000000000000000, 0.000000000000000000, 1.000000000000000000 ) ) ;
#68918=TOROIDAL_SURFACE ( 'NONE', #37524, 29.50000000000000000, 0.5000000000000000000 ) ;
#68920=LINE ( 'NONE', #64308, #59490 ) ;
#68922=CARTESIAN_POINT ( 'NONE',  ( 23.71231517720798010, 112.9999999999999858, -7.000000000000000000 ) ) ;
#68925=AXIS2_PLACEMENT_3D ( 'NONE', #34350, #17830, #55454 ) ;
#68928=CARTESIAN_POINT ( 'NONE',  ( -45.91158282012835201, 9.415467456214855702, -6.077850184675973821 ) ) ;
#68932=DIRECTION ( 'NONE',  ( 1.000000000000000000, 0.000000000000000000, 0.000000000000000000 ) ) ;
#68933=DIRECTION ( 'NONE',  ( -0.000000000000000000, -0.000000000000000000, -1.000000000000000000 ) ) ;
#68937=DIRECTION ( 'NONE',  ( -1.000000000000000000, 0.000000000000000000, 1.734723475976805517E-15 ) ) ;
#68941=( GEOMETRIC_REPRESENTATION_CONTEXT ( 3 ) GLOBAL_UNCERTAINTY_ASSIGNED_CONTEXT ( ( #60874 ) ) GLOBAL_UNIT_ASSIGNED_CONTEXT ( ( #9791, #62866, #14344 ) ) REPRESENTATION_CONTEXT ( 'NONE', 'WORKASPACE' ) );
#68943=CARTESIAN_POINT ( 'NONE',  ( 0.000000000000000000, 151.4449999999999932, -9.525000000000000355 ) ) ;
#68947=CARTESIAN_POINT ( 'NONE',  ( 3.094860106618431583, 148.2049999999999841, 9.525000000000000355 ) ) ;
#68948=( NAMED_UNIT ( * ) PLANE_ANGLE_UNIT ( ) SI_UNIT ( $, .RADIAN. ) );
#68951=EDGE_LOOP ( 'NONE', ( #39811, #16860, #14259, #10482 ) ) ;
#68952=CARTESIAN_POINT ( 'NONE',  ( 2.607480562269076430, 122.7929263765338135, -8.025000000000000355 ) ) ;
#68955=FILL_AREA_STYLE ('',( #19710 ) ) ;
#68956=AXIS2_PLACEMENT_3D ( 'NONE', #65727, #2329, #23495 ) ;
#68957=COLOUR_RGB ( '', 0.31764706, 0.68627451, 0.89019608) ;
#68958=CYLINDRICAL_SURFACE ( 'NONE', #59824, 0.5000000000000004441 ) ;
#68959=ADVANCED_FACE ( 'NONE', ( #7881 ), #35869, .T. ) ;
#68961=ORIENTED_EDGE ( 'NONE', *, *, #5524, .T. ) ;
#68966=AXIS2_PLACEMENT_3D ( 'NONE', #62945, #14091, #56990 ) ;
#68968=EDGE_CURVE ( 'NONE', #8600, #62679, #44896, .T. ) ;
#68973=DIRECTION ( 'NONE',  ( 0.000000000000000000, 0.000000000000000000, 1.000000000000000000 ) ) ;
#68974=CARTESIAN_POINT ( 'NONE',  ( 75.00000000000000000, 20.14920990499772913, 6.614546734589652033 ) ) ;
#68975=FILL_AREA_STYLE ('',( #3498 ) ) ;
#68976=ORIENTED_EDGE ( 'NONE', *, *, #30641, .F. ) ;
#68977=EDGE_LOOP ( 'NONE', ( #57282, #51107, #8148, #30611 ) ) ;
#68980=AXIS2_PLACEMENT_3D ( 'NONE', #50307, #23227, #13339 ) ;
#68988=CIRCLE ( 'NONE', #33014, 8.000000000000007105 ) ;
#68989=DIRECTION ( 'NONE',  ( 1.000000000000000000, 0.000000000000000000, 0.000000000000000000 ) ) ;
#68990=CYLINDRICAL_SURFACE ( 'NONE', #34923, 0.5000000000000004441 ) ;
#68992=DIRECTION ( 'NONE',  ( 0.000000000000000000, 0.000000000000000000, 1.000000000000000000 ) ) ;
#68993=FILL_AREA_STYLE ('',( #38038 ) ) ;
#68995=CARTESIAN_POINT ( 'NONE',  ( 5.598654528085805993, 150.2449999999999761, 7.705886871421374629 ) ) ;
#68998=COLOUR_RGB ( '', 0.72549020, 0.75294118, 0.79215686) ;
#68999=TOROIDAL_SURFACE ( 'NONE', #47707, 13.49999999999999822, 0.5000000000000000000 ) ;
#69003=AXIS2_PLACEMENT_3D ( 'NONE', #37028, #14476, #3533 ) ;
#69006=FILL_AREA_STYLE_COLOUR ( '', #28427 ) ;
#69007=SURFACE_STYLE_FILL_AREA ( #68309 ) ;
#69011=PRESENTATION_STYLE_ASSIGNMENT (( #59120 ) ) ;
#69013=CARTESIAN_POINT ( 'NONE',  ( -6.826472737025120807, 117.3929263765338078, -4.959722759717907437 ) ) ;
#69014=DIRECTION ( 'NONE',  ( -0.2413793103448194644, -0.9704308468600220117, 0.000000000000000000 ) ) ;
#69018=CIRCLE ( 'NONE', #49946, 0.5000000000000004441 ) ;
#69021=CARTESIAN_POINT ( 'NONE',  ( 2.816687638038912352E-15, 154.4999999999999432, 23.00000000000000000 ) ) ;
#69027=CARTESIAN_POINT ( 'NONE',  ( -9.058813317711338797, 119.3449999999999989, 2.943386871421373563 ) ) ;
#69028=CARTESIAN_POINT ( 'NONE',  ( 0.000000000000000000, 111.9999999999999858, -8.025000000000000355 ) ) ;
#69029=EDGE_CURVE ( 'NONE', #5601, #9272, #13151, .T. ) ;
#69031=EDGE_CURVE ( 'NONE', #34861, #55490, #6659, .T. ) ;
#69032=CARTESIAN_POINT ( 'NONE',  ( 9.058813317711337021, 121.6549999999999869, 2.943386871421375783 ) ) ;
#69035=VERTEX_POINT ( 'NONE', #38397 ) ;
#69036=CARTESIAN_POINT ( 'NONE',  ( -5.598654528085808657, 150.7549999999999955, 7.705886871421373741 ) ) ;
#69040=ADVANCED_FACE ( 'NONE', ( #38740 ), #43343, .F. ) ;
#69041=DIRECTION ( 'NONE',  ( -0.000000000000000000, -1.000000000000000000, -0.000000000000000000 ) ) ;
#69043=ORIENTED_EDGE ( 'NONE', *, *, #43353, .T. ) ;
#69044=COLOUR_RGB ( '', 0.40784314, 0.44705882, 0.49803922) ;
#69045=CARTESIAN_POINT ( 'NONE',  ( -74.99999999999998579, 119.9999999999997726, 9.500000000000000000 ) ) ;
#69048=CARTESIAN_POINT ( 'NONE',  ( 5.015307210679814887, 111.7971308996410045, -6.528277465523999901 ) ) ;
#69049=STYLED_ITEM ( 'NONE', ( #67941 ), #56173 ) ;
#69050=DIRECTION ( 'NONE',  ( -0.000000000000000000, 1.000000000000000000, -0.000000000000000000 ) ) ;
#69052=CIRCLE ( 'NONE', #38753, 0.5000000000000004441 ) ;
#69053=DIRECTION ( 'NONE',  ( 1.000000000000000000, -1.156482317317866302E-16, 0.000000000000000000 ) ) ;
#69061=EDGE_LOOP ( 'NONE', ( #33618, #25821, #62046, #16765 ) ) ;
#69063=FACE_OUTER_BOUND ( 'NONE', #21555, .T. ) ;
#69066=CARTESIAN_POINT ( 'NONE',  ( -9.058813317711337021, 149.0449999999999875, -2.943386871421374895 ) ) ;
#69069=COLOUR_RGB ( '', 0.09019608, 0.27058824, 0.51372549) ;
#69072=DIRECTION ( 'NONE',  ( -1.000000000000000000, 0.000000000000000000, 0.000000000000000000 ) ) ;
#69077=CARTESIAN_POINT ( 'NONE',  ( -5.598654528085806881, 115.7449999999999903, -7.705886871421374629 ) ) ;
#69082=EDGE_CURVE ( 'NONE', #62231, #17220, #52897, .T. ) ;
#69089=CARTESIAN_POINT ( 'NONE',  ( -60.00000000000000000, -2.024042244987997205E-14, -11.50000000000000000 ) ) ;
#69092=( LENGTH_UNIT ( ) NAMED_UNIT ( * ) SI_UNIT ( .MILLI., .METRE. ) );
#69096=CARTESIAN_POINT ( 'NONE',  ( 60.00000000000000000, 1.797044900979284448E-15, 6.500000000000000000 ) ) ;
#69098=CIRCLE ( 'NONE', #41048, 1.000000000000000888 ) ;
#69099=CARTESIAN_POINT ( 'NONE',  ( 2.607480562269118174, 152.7929263765338135, -8.024999999999970157 ) ) ;
#69101=( BOUNDED_SURFACE ( )  B_SPLINE_SURFACE ( 3, 2, ( 
 ( #36118, #63180, #26225 ),
 ( #47764, #55023, #27928 ),
 ( #49439, #59256, #117 ),
 ( #58947, #64897, #16747 ),
 ( #27241, #69491, #38911 ),
 ( #54344, #21646, #5798 ),
 ( #64571, #6850, #32912 ),
 ( #65247, #48428, #64206 ),
 ( #32530, #49115, #43163 ),
 ( #800, #48085, #43510 ) ),
 .UNSPECIFIED., .F., .F., .F. ) 
 B_SPLINE_SURFACE_WITH_KNOTS ( ( 4, 2, 2, 2, 4 ),
 ( 3, 3 ),
 ( 4.181938019525841099, 4.707249841439277382, 5.232561663352713666, 5.757873485266149949, 6.283185307179586232 ),
 ( 0.000000000000000000, 1.000000000000000000 ),
 .UNSPECIFIED. ) 
 GEOMETRIC_REPRESENTATION_ITEM ( )  RATIONAL_B_SPLINE_SURFACE ( (
 ( 1.000000000000000000, 0.7615729461579494597, 1.000000000000000000),
 ( 1.000000000000000000, 0.7459210345859041968, 1.000000000000000000),
 ( 1.000000000000000000, 0.7272421848981694970, 1.000000000000000000),
 ( 1.000000000000000000, 0.6881200523220029064, 1.000000000000000000),
 ( 1.000000000000000000, 0.6676671612971883940, 1.000000000000000000),
 ( 1.000000000000000000, 0.6306589281295537086, 1.000000000000000000),
 ( 1.000000000000000000, 0.6141839381258914488, 1.000000000000000000),
 ( 1.000000000000000000, 0.5911458751171522197, 1.000000000000000000),
 ( 1.000000000000000000, 0.5846320934540327752, 1.000000000000000000),
 ( 1.000000000000000000, 0.5847102846637711737, 1.000000000000000000) ) ) 
 REPRESENTATION_ITEM ( '' )  SURFACE ( )  );
#69109=CARTESIAN_POINT ( 'NONE',  ( 8.437984349512095861, 147.3070736234662093, 1.550032578732817026E-15 ) ) ;
#69111=CIRCLE ( 'NONE', #38816, 0.5000000000000004441 ) ;
#69115=CARTESIAN_POINT ( 'NONE',  ( -9.827790563157511022E-16, 131.5570736234661524, 8.025000000000000355 ) ) ;
#69120=CARTESIAN_POINT ( 'NONE',  ( -84.49999999999997158, 50.00000000000000000, -9.999999999999998224 ) ) ;
#69126=ORIENTED_EDGE ( 'NONE', *, *, #25177, .T. ) ;
#69128=DIRECTION ( 'NONE',  ( 1.000000000000000000, 0.000000000000000000, 0.000000000000000000 ) ) ;
#69130=EDGE_LOOP ( 'NONE', ( #64154, #56017, #27091, #41444 ) ) ;
#69132=DIRECTION ( 'NONE',  ( 0.000000000000000000, 0.000000000000000000, -1.000000000000000000 ) ) ;
#69135=CARTESIAN_POINT ( 'NONE',  ( -74.08452723581622479, 9.430195785006297626, 6.025268399887226067 ) ) ;
#69138=ORIENTED_EDGE ( 'NONE', *, *, #33979, .T. ) ;
#69139=CYLINDRICAL_SURFACE ( 'NONE', #57223, 0.5000000000000004441 ) ;
#69140=( LENGTH_UNIT ( ) NAMED_UNIT ( * ) SI_UNIT ( .MILLI., .METRE. ) );
#69142=CARTESIAN_POINT ( 'NONE',  ( -3.094860106618432471, 118.5949999999999847, -9.525000000000000355 ) ) ;
#69143=CIRCLE ( 'NONE', #50067, 7.500000000000000000 ) ;
#69145=MECHANICAL_DESIGN_GEOMETRIC_PRESENTATION_REPRESENTATION('',(#41089),#17489);
#69151=PRESENTATION_STYLE_ASSIGNMENT (( #22000 ) ) ;
#69154=CARTESIAN_POINT ( 'NONE',  ( -71.50000000000000000, 35.92875272052971525, 9.500000000000000000 ) ) ;
#69159=CARTESIAN_POINT ( 'NONE',  ( 70.87837837837835764, 13.70805908423323949, 9.500000000000000000 ) ) ;
#69160=AXIS2_PLACEMENT_3D ( 'NONE', #63251, #35486, #14729 ) ;
#69161=CARTESIAN_POINT ( 'NONE',  ( 20.71231517720798365, 149.5697028012963301, -10.00000000000000000 ) ) ;
#69166=DIRECTION ( 'NONE',  ( -0.000000000000000000, 1.000000000000000000, -0.000000000000000000 ) ) ;
#69167=( NAMED_UNIT ( * ) SI_UNIT ( $, .STERADIAN. ) SOLID_ANGLE_UNIT ( ) );
#69168=FACE_OUTER_BOUND ( 'NONE', #48329, .T. ) ;
#69171=FILL_AREA_STYLE ('',( #15386 ) ) ;
#69172=UNCERTAINTY_MEASURE_WITH_UNIT (LENGTH_MEASURE( 1.000000000000000082E-05 ), #20524, 'distance_accuracy_value', 'NONE');
#69176=EDGE_CURVE ( 'NONE', #6055, #47666, #5557, .T. ) ;
#69179=CARTESIAN_POINT ( 'NONE',  ( -7.632228543268608334, 138.8429263765337964, 2.479861379858952830 ) ) ;
#69181=CARTESIAN_POINT ( 'NONE',  ( -12.72792206135785165, 1.797044900979284448E-15, 10.00000000000000000 ) ) ;
#69186=CARTESIAN_POINT ( 'NONE',  ( -2.607480562269073765, 112.2070736234661581, -8.025000000000000355 ) ) ;
#69188=CARTESIAN_POINT ( 'NONE',  ( -20.42980746818723503, 114.8194254430358399, 10.32394991351191571 ) ) ;
#69190=FACE_OUTER_BOUND ( 'NONE', #9433, .T. ) ;
#69191=EDGE_CURVE ( 'NONE', #23204, #46742, #11203, .T. ) ;
#69197=CARTESIAN_POINT ( 'NONE',  ( 3.094860106618435136, 119.4049999999999727, -9.525000000000000355 ) ) ;
#69199=FACE_OUTER_BOUND ( 'NONE', #16518, .T. ) ;
#69200=EDGE_CURVE ( 'NONE', #67546, #19997, #2142, .T. ) ;
#69201=CARTESIAN_POINT ( 'NONE',  ( -51.50000000000000000, -2.024042244987997205E-14, -9.999999999999998224 ) ) ;
#69203=ORIENTED_EDGE ( 'NONE', *, *, #6261, .F. ) ;
#69206=EDGE_CURVE ( 'NONE', #69671, #23279, #23215, .T. ) ;
#69207=ORIENTED_EDGE ( 'NONE', *, *, #4944, .T. ) ;
#69208=CARTESIAN_POINT ( 'NONE',  ( -6.826472737025120807, 156.3929263765337794, -4.959722759717907437 ) ) ;
#69210=AXIS2_PLACEMENT_3D ( 'NONE', #21019, #42512, #10127 ) ;
#69212=CARTESIAN_POINT ( 'NONE',  ( -15.98999599679679839, 117.4999999999999716, 9.500000000000000000 ) ) ;
#69213=CARTESIAN_POINT ( 'NONE',  ( 20.71462257042821520, 114.4999999999999574, -10.00000000000000355 ) ) ;
#69215=CARTESIAN_POINT ( 'NONE',  ( 6.826472737025119919, 127.8929263765338220, 4.959722759717908325 ) ) ;
#69218=( NAMED_UNIT ( * ) SI_UNIT ( $, .STERADIAN. ) SOLID_ANGLE_UNIT ( ) );
#69219=( NAMED_UNIT ( * ) SI_UNIT ( $, .STERADIAN. ) SOLID_ANGLE_UNIT ( ) );
#69223=( BOUNDED_CURVE ( )  B_SPLINE_CURVE ( 2, ( #2948, #45262, #19519, #29738, #1894, #41020, #67034, #45615, #23762, #62440, #14254 ),
 .UNSPECIFIED., .F., .F. ) 
 B_SPLINE_CURVE_WITH_KNOTS ( ( 3, 2, 2, 2, 2, 3 ),
 ( 0.7941176470588233727, 0.7999999999999999334, 0.8058823529411763831, 0.8117647058823528328, 0.8176470588235292825, 0.8235294117647057321 ),
 .UNSPECIFIED. ) 
 CURVE ( )  GEOMETRIC_REPRESENTATION_ITEM ( )  RATIONAL_B_SPLINE_CURVE ( ( 1.000000000000000888, 0.9510565162951526430, 1.000000000000000000, 0.9510565162951535312, 1.000000000000000000, 0.9510565162951535312, 1.000000000000000000, 0.9510565162951535312, 1.000000000000000000, 0.9510565162951544194, 0.9999999999999991118 ) ) 
 REPRESENTATION_ITEM ( '' )  );
#69230=DIRECTION ( 'NONE',  ( 1.000000000000000000, 0.000000000000000000, 0.000000000000000000 ) ) ;
#69232=CARTESIAN_POINT ( 'NONE',  ( 2.607480562269034241, 114.9070736234661467, -8.025000000000032330 ) ) ;
#69234=ORIENTED_EDGE ( 'NONE', *, *, #46357, .F. ) ;
#69247=CARTESIAN_POINT ( 'NONE',  ( 72.00000000000000000, 14.49137674618942562, 7.500000000000000000 ) ) ;
#69248=DIRECTION ( 'NONE',  ( 1.000000000000000000, -0.000000000000000000, -0.000000000000000000 ) ) ;
#69250=CARTESIAN_POINT ( 'NONE',  ( 0.000000000000000000, 131.5549999999999784, -9.525000000000000355 ) ) ;
#69253=UNCERTAINTY_MEASURE_WITH_UNIT (LENGTH_MEASURE( 1.000000000000000082E-05 ), #40089, 'distance_accuracy_value', 'NONE');
#69254=CARTESIAN_POINT ( 'NONE',  ( -41.49999999999998579, 99.99999999999998579, -3.500000000000000000 ) ) ;
#69255=PRESENTATION_STYLE_ASSIGNMENT (( #48873 ) ) ;
#69257=ADVANCED_FACE ( 'NONE', ( #55561 ), #8763, .T. ) ;
#69258=CARTESIAN_POINT ( 'NONE',  ( 72.00000000000000000, 14.49137674618942562, -7.000000000000000000 ) ) ;
#69259=EDGE_CURVE ( 'NONE', #62684, #14708, #46802, .T. ) ;
#69260=( GEOMETRIC_REPRESENTATION_CONTEXT ( 3 ) GLOBAL_UNCERTAINTY_ASSIGNED_CONTEXT ( ( #22094 ) ) GLOBAL_UNIT_ASSIGNED_CONTEXT ( ( #13215, #13563, #30087 ) ) REPRESENTATION_CONTEXT ( 'NONE', 'WORKASPACE' ) );
#69267=CARTESIAN_POINT ( 'NONE',  ( -7.632228543268607446, 136.6570736234661467, -2.479861379858953718 ) ) ;
#69268=ORIENTED_EDGE ( 'NONE', *, *, #25502, .F. ) ;
#69270=FACE_OUTER_BOUND ( 'NONE', #32749, .T. ) ;
#69272=SURFACE_STYLE_USAGE ( .BOTH. , #53097 ) ;
#69275=EDGE_CURVE ( 'NONE', #41197, #52602, #20243, .T. ) ;
#69279=AXIS2_PLACEMENT_3D ( 'NONE', #33619, #838, #33289 ) ;
#69280=( LENGTH_UNIT ( ) NAMED_UNIT ( * ) SI_UNIT ( .MILLI., .METRE. ) );
#69283=SURFACE_STYLE_USAGE ( .BOTH. , #68587 ) ;
#69284=VERTEX_POINT ( 'NONE', #41154 ) ;
#69286=B_SPLINE_CURVE_WITH_KNOTS ( 'NONE', 3,
 ( #51796, #24340, #24675, #41264, #63378, #8871, #41603, #13801 ),
 .UNSPECIFIED., .F., .F.,
 ( 4, 2, 2, 4 ),
 ( 0.000000000000000000, 0.0001769990489079868224, 0.0003539980978159736448, 0.0007079961956319273404 ),
 .UNSPECIFIED. ) ;
#69287=CARTESIAN_POINT ( 'NONE',  ( 10.01517768586949231, 150.6949999999999648, 1.839758294383810543E-15 ) ) ;
#69291=CARTESIAN_POINT ( 'NONE',  ( 9.058813317711338797, 151.9550000000000125, -2.943386871421372675 ) ) ;
#69292=CARTESIAN_POINT ( 'NONE',  ( -9.827790563157511022E-16, 131.5570736234661524, 8.025000000000000355 ) ) ;
#69295=CARTESIAN_POINT ( 'NONE',  ( 4.716976649647099507, 128.6429263765338362, -6.492361379858953008 ) ) ;
#69296=CARTESIAN_POINT ( 'NONE',  ( 45.65811388300841855, 10.21937129433612235, -4.000000000000000000 ) ) ;
#69305=FACE_OUTER_BOUND ( 'NONE', #34443, .T. ) ;
#69307=CARTESIAN_POINT ( 'NONE',  ( -24.21231517720798010, 117.4999999999999716, -7.000000000000000000 ) ) ;
#69311=CARTESIAN_POINT ( 'NONE',  ( 0.000000000000000000, 154.9999999999999716, 0.000000000000000000 ) ) ;
#69312=CARTESIAN_POINT ( 'NONE',  ( 40.95866658621363854, 108.0312444614856986, 3.562488397567471932 ) ) ;
#69313=( LENGTH_UNIT ( ) NAMED_UNIT ( * ) SI_UNIT ( .MILLI., .METRE. ) );
#69314=EDGE_LOOP ( 'NONE', ( #32737, #11904, #65283, #66996, #2307, #61791, #33300, #3506, #13305, #32107, #18758, #35308, #45764, #39098, #23080, #30075, #6988, #42760, #17832 ) ) ;
#69317=STYLED_ITEM ( 'NONE', ( #12440 ), #65354 ) ;
#69320=EDGE_LOOP ( 'NONE', ( #41908, #13834 ) ) ;
#69323=AXIS2_PLACEMENT_3D ( 'NONE', #2442, #56300, #13053 ) ;
#69324=DIRECTION ( 'NONE',  ( 7.080503983578803083E-17, 1.000000000000000000, -0.000000000000000000 ) ) ;
#69327=ORIENTED_EDGE ( 'NONE', *, *, #64085, .F. ) ;
#69328=( NAMED_UNIT ( * ) PLANE_ANGLE_UNIT ( ) SI_UNIT ( $, .RADIAN. ) );
#69329=CARTESIAN_POINT ( 'NONE',  ( -45.00000000000000000, 10.49999999999998224, -4.000000000000000000 ) ) ;
#69330=LINE ( 'NONE', #26399, #62262 ) ;
#69331=CARTESIAN_POINT ( 'NONE',  ( 4.716976649647099507, 126.7570736234661695, -6.492361379858953008 ) ) ;
#69334=CARTESIAN_POINT ( 'NONE',  ( -8.102448949553181734, 152.4949999999999477, 5.886773742842747126 ) ) ;
#69339=UNCERTAINTY_MEASURE_WITH_UNIT (LENGTH_MEASURE( 1.000000000000000082E-05 ), #27121, 'distance_accuracy_value', 'NONE');
#69340=SURFACE_SIDE_STYLE ('',( #43356 ) ) ;
#69341=VERTEX_POINT ( 'NONE', #21378 ) ;
#69343=DIRECTION ( 'NONE',  ( -0.000000000000000000, 1.000000000000000000, -0.000000000000000000 ) ) ;
#69345=DIRECTION ( 'NONE',  ( 0.000000000000000000, 0.000000000000000000, 1.000000000000000000 ) ) ;
#69347=SURFACE_SIDE_STYLE ('',( #25040 ) ) ;
#69348=DIRECTION ( 'NONE',  ( 0.000000000000000000, 0.000000000000000000, -1.000000000000000000 ) ) ;
#69350=ORIENTED_EDGE ( 'NONE', *, *, #26651, .T. ) ;
#69352=CARTESIAN_POINT ( 'NONE',  ( -75.00000000000000000, -2.215169945516535778E-14, 10.00000000000000000 ) ) ;
#69356=CARTESIAN_POINT ( 'NONE',  ( 44.99999999999977973, 149.9999999999999716, 10.00000000000000000 ) ) ;
#69357=AXIS2_PLACEMENT_3D ( 'NONE', #36203, #62881, #19274 ) ;
#69358=EDGE_CURVE ( 'NONE', #44514, #23604, #59705, .T. ) ;
#69359=ORIENTED_EDGE ( 'NONE', *, *, #63228, .T. ) ;
#69362=VERTEX_POINT ( 'NONE', #59342 ) ;
#69367=CARTESIAN_POINT ( 'NONE',  ( -55.00000000000000000, -2.024042244987997205E-14, -12.00000000000000000 ) ) ;
#69368=CARTESIAN_POINT ( 'NONE',  ( 8.102448949553181734, 123.3949999999999676, 5.886773742842750679 ) ) ;
#69371=DIRECTION ( 'NONE',  ( -0.000000000000000000, -0.000000000000000000, -1.000000000000000000 ) ) ;
#69372=CARTESIAN_POINT ( 'NONE',  ( 0.000000000000000000, 125.5550000000000068, -9.525000000000000355 ) ) ;
#69375=CARTESIAN_POINT ( 'NONE',  ( -75.00000000000000000, -2.215169945516535778E-14, -6.500000000000000888 ) ) ;
#69377=CARTESIAN_POINT ( 'NONE',  ( 8.102448949553183510, 152.1049999999999613, -5.886773742842746238 ) ) ;
#69384=DIRECTION ( 'NONE',  ( 1.000000000000000000, 0.000000000000000000, 0.000000000000000000 ) ) ;
#69385=ORIENTED_EDGE ( 'NONE', *, *, #31051, .F. ) ;
#69391=EDGE_LOOP ( 'NONE', ( #24210, #25993, #51388, #4300 ) ) ;
#69393=SURFACE_STYLE_USAGE ( .BOTH. , #58150 ) ;
#69394=ORIENTED_EDGE ( 'NONE', *, *, #41920, .T. ) ;
#69397=VERTEX_POINT ( 'NONE', #5527 ) ;
#69402=DIRECTION ( 'NONE',  ( 0.000000000000000000, 0.000000000000000000, 1.000000000000000000 ) ) ;
#69404=AXIS2_PLACEMENT_3D ( 'NONE', #50894, #36120, #19203 ) ;
#69407=AXIS2_PLACEMENT_3D ( 'NONE', #56388, #30329, #51832 ) ;
#69409=SURFACE_STYLE_FILL_AREA ( #11001 ) ;
#69412=CARTESIAN_POINT ( 'NONE',  ( -9.058813317711338797, 122.3449999999999847, 2.943386871421373563 ) ) ;
#69414=ADVANCED_FACE ( 'NONE', ( #15790 ), #31587, .F. ) ;
#69416=( BOUNDED_SURFACE ( )  B_SPLINE_SURFACE ( 1, 2, ( 
 ( #45572, #40617, #40979, #61665, #29694, #8933, #30353, #3604, #62397, #61342, #56781, #8596, #35327, #3250, #68042, #25108, #62721, #24738, #8252, #55736, #2908, #50460, #46624, #14214, #18457, #29330, #24400, #34607, #45894, #2188, #30030, #23718, #19828, #45216, #39940, #41318, #13152, #7882, #50809, #63442, #58169, #9291, #69077, #15289, #20879, #21563, #48336, #4683, #30711, #31760, #26136, #25791, #9985, #42037, #41668, #3979, #68371, #36024, #36753, #47306, #47673, #10330, #42383, #68732, #63773, #25450, #57824, #20528, #9652, #31404, #32121, #26485, #52898, #15621, #37096, #53249, #52218, #63086, #58506, #46964, #64122, #5035, #14925, #57466, #4308, #48010, #69412, #37456, #21201, #42724, #43075, #15974, #58860, #36410, #53574, #10667, #20162, #31067, #5361, #14550, #26802, #52563, #28, #6753, #59176, #28183, #39161, #54928, #54252, #27507, #38489, #50048, #49694, #44110, #22607, #27841, #12370, #6073, #1063, #1428, #32813, #59881, #60552, #33833, #55295, #22957, #21922, #17358, #38824, #65506, #12036, #28546, #7117, #23294, #44459, #49034, #64481, #723, #11003, #1784, #33496, #48687, #59524, #33169, #64817, #54604, #32441, #22255, #16325, #37801, #53902, #5708, #16997, #49343, #65863, #393, #43433, #43751, #27157, #60237, #65152, #16664, #38129, #11699, #17693, #11344, #6409, #61953, #34200, #39503, #14135, #3518, #2832, #44791, #30272, #56697, #60911, #8517, #19394, #35237, #34530, #7796, #18713, #51770, #29952, #24325, #45817, #8164, #62313, #55989, #51079, #51417, #13077, #40186, #40891, #35595, #57033, #3161, #2105, #67241, #19027, #40539, #13779, #8852, #66189, #18012, #24652, #29243, #12728, #50725, #55651, #7467, #46169, #28892, #39863, #13417, #45136, #34881, #50377, #2470, #23628, #66554, #18377, #61267, #66911, #29605, #67596, #23981, #45495, #61587, #56328, #52820, #25700, #37365, #57385, #4224, #14461, #41240, #58421, #47221, #68639, #19744, #9906, #20444, #31322, #32037, #58771, #15207, #62639, #42308, #36674, #36315, #41946, #52486, #52136, #35940, #9210, #46534, #63352, #57739, #58095, #20801, #4595, #9570, #26054, #30628, #68290, #30988, #20076, #47588, #42632, #37013, #68995, #63696, #15540, #10247, #3891, #25367, #31684, #46889, #4954, #53160, #41576, #67959, #14838, #26402, #47933, #69334, #21128, #64037, #15881, #62997, #10588, #53498, #25024, #65431, #44374, #6329, #54846, #65779, #59432, #42987, #11263, #21835, #17280, #59804, #38744, #16918, #64391, #17615, #10926, #54519, #33754, #33082, #60151, #39081, #48248, #11615, #65064, #22874, #69663, #59107, #5281, #32361, #26726, #32718, #648, #27760, #60475, #11960, #28105, #43347, #27422, #22523, #6665, #21477, #49264, #44021, #973, #49610, #5621 ),
 ( #48950, #38401, #33417, #1344, #12283, #16239, #37717, #22176, #53822, #43671, #27073, #48608, #301, #54173, #64742, #16585, #38040, #5983, #23543, #55911, #12996, #49965, #66829, #18637, #2377, #7386, #45053, #45743, #34792, #8435, #23896, #3078, #56605, #2018, #1702, #7027, #44713, #34451, #40117, #17932, #23219, #56244, #28817, #67160, #61505, #29521, #61187, #13333, #67501, #28454, #18946, #29152, #8069, #50985, #66463, #40449, #7713, #66103, #29868, #61865, #39422, #2750, #40806, #50638, #24242, #35150, #62221, #19301, #45409, #60823, #13691, #51333, #18287, #24569, #46082, #12643, #34107, #55565, #50299, #14047, #39772, #55204, #31233, #41852, #68211, #63273, #62904, #35847, #46443, #30541, #57650, #53073, #47490, #14748, #15118, #36223, #4496, #51682, #62558, #19987, #3428, #15458, #41488, #14376, #56950, #25284, #25614, #36595, #58333, #52398, #4144, #42546, #46806, #52728, #57291, #4867, #25961, #24931, #30189, #26310, #63946, #58013, #35507, #21050, #68913, #67868, #20711, #10158, #42224, #9477, #30900, #47127, #8768, #63615, #9823, #36921, #68553, #47855, #20350, #31591, #69250, #3798, #19661, #41157, #9123, #52043, #49186, #42905, #38307, #59711, #64980, #32995, #49527, #6573, #44288, #6250, #212, #15793, #21743, #31945, #33338, #54430, #69577, #10843, #54085, #16150, #5893, #53422, #43254, #37277, #54760, #58675, #5201, #37970, #565, #27675, #21382, #64298, #64660, #28018, #43592, #16504, #1256, #48170, #59346, #26645, #37628, #888, #11176, #32624, #10507, #22090, #27336, #16836, #22429, #48866, #59032, #43930, #11524, #32287, #65340, #17190, #38662, #60060, #11875, #22787, #53738, #5532, #26982, #48515, #7984, #39677, #18191, #50218, #2662, #6941, #28367, #45314, #34018, #66370, #23457, #60395, #7628, #29062, #12909, #17853, #55479, #56157, #66736, #18863, #34374, #13595, #67078, #12552, #12198, #17532, #55114, #44963, #50560, #49874, #33672, #18551, #39331, #29428, #2283, #40036, #1940, #23812, #8347, #39002, #50899, #61099, #61425, #13246, #7301, #24157, #55823, #1613, #40357, #45662, #23139, #34701, #51252, #61766, #35062, #56509, #28730, #60734, #29792, #24483, #2993, #65684, #44629, #66026, #25882, #15382, #30451, #13957, #51952, #62482, #36503, #30817, #57926, #57562, #35425, #58251, #51591, #25533, #4779, #4069, #9746, #10075, #19210, #52316, #36127, #63529, #40720, #30113, #45990, #3346, #67415, #3709, #41415, #47047, #36837, #52647, #68827, #14301, #68133, #63188, #47399, #62130, #20262, #15029, #41767, #20621, #56875, #8686, #31499, #19912, #24840, #46355, #25203, #67775, #19575, #31153, #46720, #62818, #41068, #68466, #14658, #4406, #52986, #35765, #9394, #57201, #42134, #9033, #37552, #126, #53660 ) ),
 .UNSPECIFIED., .F., .F., .F. ) 
 B_SPLINE_SURFACE_WITH_KNOTS ( ( 2, 2 ),
 ( 3, 2, 2, 2, 2, 2, 2, 2, 2, 2, 2, 2, 2, 2, 2, 2, 2, 2, 2, 2, 2, 2, 2, 2, 2, 2, 2, 2, 2, 2, 2, 2, 2, 2, 2, 2, 2, 2, 2, 2, 2, 2, 2, 2, 2, 2, 2, 2, 2, 2, 2, 2, 2, 2, 2, 2, 2, 2, 2, 2, 2, 2, 2, 2, 2, 2, 2, 2, 2, 2, 2, 2, 2, 2, 2, 2, 2, 2, 2, 2, 2, 2, 2, 2, 2, 2, 2, 2, 2, 2, 2, 2, 2, 2, 2, 2, 2, 2, 2, 2, 2, 2, 2, 2, 2, 2, 2, 2, 2, 2, 2, 2, 2, 2, 2, 2, 2, 2, 2, 2, 2, 2, 2, 2, 2, 2, 2, 2, 2, 2, 2, 2, 2, 2, 2, 2, 2, 2, 2, 2, 2, 2, 2, 2, 2, 2, 2, 2, 2, 2, 2, 2, 2, 2, 2, 2, 2, 2, 2, 2, 2, 2, 2, 2, 2, 2, 2, 2, 2, 2, 3 ),
 ( 0.000000000000000000, 1.000000000000000000 ),
 ( 0.000000000000000000, 0.005882352941176470507, 0.01176470588235294101, 0.01764705882352941152, 0.02352941176470588203, 0.02941176470588235253, 0.03529411764705882304, 0.04117647058823529355, 0.04705882352941176405, 0.05294117647058823456, 0.05882352941176470507, 0.06470588235294118251, 0.07058823529411764608, 0.07647058823529412352, 0.08235294117647058709, 0.08823529411764706454, 0.09411764705882352811, 0.1000000000000000056, 0.1058823529411764691, 0.1117647058823529466, 0.1176470588235294101, 0.1235294117647058876, 0.1294117647058823650, 0.1352941176470588147, 0.1411764705882352922, 0.1470588235294117696, 0.1529411764705882470, 0.1588235294117646967, 0.1647058823529411742, 0.1705882352941176516, 0.1764705882352941291, 0.1823529411764705788, 0.1882352941176470562, 0.1941176470588235337, 0.2000000000000000111, 0.2058823529411764608, 0.2117647058823529382, 0.2176470588235294157, 0.2235294117647058931, 0.2294117647058823428, 0.2352941176470588203, 0.2411764705882352977, 0.2470588235294117752, 0.2529411764705882248, 0.2588235294117647300, 0.2647058823529411797, 0.2705882352941176294, 0.2764705882352941346, 0.2823529411764705843, 0.2882352941176470340, 0.2941176470588235392, 0.2999999999999999889, 0.3058823529411764941, 0.3117647058823529438, 0.3176470588235293935, 0.3235294117647058987, 0.3294117647058823484, 0.3352941176470587981, 0.3411764705882353033, 0.3470588235294117530, 0.3529411764705882582, 0.3588235294117647078, 0.3647058823529411575, 0.3705882352941176627, 0.3764705882352941124, 0.3823529411764705621, 0.3882352941176470673, 0.3941176470588235170, 0.4000000000000000222, 0.4058823529411764719, 0.4117647058823529216, 0.4176470588235294268, 0.4235294117647058765, 0.4294117647058823262, 0.4352941176470588314, 0.4411764705882352811, 0.4470588235294117863, 0.4529411764705882359, 0.4588235294117646856, 0.4647058823529411908, 0.4705882352941176405, 0.4764705882352940902, 0.4823529411764705954, 0.4882352941176470451, 0.4941176470588235503, 0.5000000000000000000, 0.5058823529411764497, 0.5117647058823528994, 0.5176470588235294601, 0.5235294117647059098, 0.5294117647058823595, 0.5352941176470588092, 0.5411764705882352589, 0.5470588235294118196, 0.5529411764705882693, 0.5588235294117647189, 0.5647058823529411686, 0.5705882352941176183, 0.5764705882352940680, 0.5823529411764706287, 0.5882352941176470784, 0.5941176470588235281, 0.5999999999999999778, 0.6058823529411764275, 0.6117647058823529882, 0.6176470588235294379, 0.6235294117647058876, 0.6294117647058823373, 0.6352941176470587870, 0.6411764705882353477, 0.6470588235294117974, 0.6529411764705882470, 0.6588235294117646967, 0.6647058823529411464, 0.6705882352941175961, 0.6764705882352941568, 0.6823529411764706065, 0.6882352941176470562, 0.6941176470588235059, 0.6999999999999999556, 0.7058823529411765163, 0.7117647058823529660, 0.7176470588235294157, 0.7235294117647058654, 0.7294117647058823151, 0.7352941176470588758, 0.7411764705882353255, 0.7470588235294117752, 0.7529411764705882248, 0.7588235294117646745, 0.7647058823529411242, 0.7705882352941176849, 0.7764705882352941346, 0.7823529411764705843, 0.7882352941176470340, 0.7941176470588234837, 0.8000000000000000444, 0.8058823529411764941, 0.8117647058823529438, 0.8176470588235293935, 0.8235294117647058432, 0.8294117647058824039, 0.8352941176470588536, 0.8411764705882353033, 0.8470588235294117530, 0.8529411764705882026, 0.8588235294117646523, 0.8647058823529412130, 0.8705882352941176627, 0.8764705882352941124, 0.8823529411764705621, 0.8882352941176470118, 0.8941176470588235725, 0.9000000000000000222, 0.9058823529411764719, 0.9117647058823529216, 0.9176470588235293713, 0.9235294117647059320, 0.9294117647058823817, 0.9352941176470588314, 0.9411764705882352811, 0.9470588235294117307, 0.9529411764705881804, 0.9588235294117647411, 0.9647058823529411908, 0.9705882352941176405, 0.9764705882352940902, 0.9823529411764705399, 0.9882352941176471006, 0.9941176470588235503, 1.000000000000000000 ),
 .UNSPECIFIED. ) 
 GEOMETRIC_REPRESENTATION_ITEM ( )  RATIONAL_B_SPLINE_SURFACE ( (
 ( 1.000000000000000000, 0.9510565162951535312, 1.000000000000000000, 0.9510565162951535312, 1.000000000000000000, 0.9510565162951535312, 1.000000000000000000, 0.9510565162951535312, 1.000000000000000000, 0.9510565162951535312, 1.000000000000000000, 0.9510565162951535312, 1.000000000000000000, 0.9510565162951535312, 1.000000000000000000, 0.9510565162951535312, 1.000000000000000000, 0.9510565162951535312, 1.000000000000000000, 0.9510565162951535312, 1.000000000000000000, 0.9510565162951535312, 1.000000000000000000, 0.9510565162951535312, 1.000000000000000000, 0.9510565162951535312, 1.000000000000000000, 0.9510565162951535312, 1.000000000000000000, 0.9510565162951535312, 1.000000000000000000, 0.9510565162951535312, 1.000000000000000000, 0.9510565162951535312, 1.000000000000000000, 0.9510565162951535312, 1.000000000000000000, 0.9510565162951535312, 1.000000000000000000, 0.9510565162951535312, 1.000000000000000000, 0.9510565162951535312, 1.000000000000000000, 0.9510565162951535312, 1.000000000000000000, 0.9510565162951535312, 1.000000000000000000, 0.9510565162951535312, 1.000000000000000000, 0.9510565162951535312, 1.000000000000000000, 0.9510565162951535312, 1.000000000000000000, 0.9510565162951535312, 1.000000000000000000, 0.9510565162951535312, 1.000000000000000000, 0.9510565162951535312, 1.000000000000000000, 0.9510565162951535312, 1.000000000000000000, 0.9510565162951535312, 1.000000000000000000, 0.9510565162951535312, 1.000000000000000000, 0.9510565162951535312, 1.000000000000000000, 0.9510565162951535312, 1.000000000000000000, 0.9510565162951535312, 1.000000000000000000, 0.9510565162951535312, 1.000000000000000000, 0.9510565162951535312, 1.000000000000000000, 0.9510565162951535312, 1.000000000000000000, 0.9510565162951535312, 1.000000000000000000, 0.9510565162951535312, 1.000000000000000000, 0.9510565162951535312, 1.000000000000000000, 0.9510565162951535312, 1.000000000000000000, 0.9510565162951535312, 1.000000000000000000, 0.9510565162951535312, 1.000000000000000000, 0.9510565162951535312, 1.000000000000000000, 0.9510565162951535312, 1.000000000000000000, 0.9510565162951535312, 1.000000000000000000, 0.9510565162951535312, 1.000000000000000000, 0.9510565162951535312, 1.000000000000000000, 0.9510565162951535312, 1.000000000000000000, 0.9510565162951535312, 1.000000000000000000, 0.9510565162951535312, 1.000000000000000000, 0.9510565162951535312, 1.000000000000000000, 0.9510565162951535312, 1.000000000000000000, 0.9510565162951535312, 1.000000000000000000, 0.9510565162951535312, 1.000000000000000000, 0.9510565162951535312, 1.000000000000000000, 0.9510565162951535312, 1.000000000000000000, 0.9510565162951535312, 1.000000000000000000, 0.9510565162951535312, 1.000000000000000000, 0.9510565162951535312, 1.000000000000000000, 0.9510565162951535312, 1.000000000000000000, 0.9510565162951535312, 1.000000000000000000, 0.9510565162951535312, 1.000000000000000000, 0.9510565162951535312, 1.000000000000000000, 0.9510565162951535312, 1.000000000000000000, 0.9510565162951535312, 1.000000000000000000, 0.9510565162951535312, 1.000000000000000000, 0.9510565162951535312, 1.000000000000000000, 0.9510565162951535312, 1.000000000000000000, 0.9510565162951535312, 1.000000000000000000, 0.9510565162951535312, 1.000000000000000000, 0.9510565162951535312, 1.000000000000000000, 0.9510565162951535312, 1.000000000000000000, 0.9510565162951535312, 1.000000000000000000, 0.9510565162951535312, 1.000000000000000000, 0.9510565162951535312, 1.000000000000000000, 0.9510565162951535312, 1.000000000000000000, 0.9510565162951535312, 1.000000000000000000, 0.9510565162951535312, 1.000000000000000000, 0.9510565162951535312, 1.000000000000000000, 0.9510565162951535312, 1.000000000000000000, 0.9510565162951535312, 1.000000000000000000, 0.9510565162951535312, 1.000000000000000000, 0.9510565162951535312, 1.000000000000000000, 0.9510565162951535312, 1.000000000000000000, 0.9510565162951535312, 1.000000000000000000, 0.9510565162951535312, 1.000000000000000000, 0.9510565162951535312, 1.000000000000000000, 0.9510565162951535312, 1.000000000000000000, 0.9510565162951535312, 1.000000000000000000, 0.9510565162951535312, 1.000000000000000000, 0.9510565162951535312, 1.000000000000000000, 0.9510565162951535312, 1.000000000000000000, 0.9510565162951535312, 1.000000000000000000, 0.9510565162951535312, 1.000000000000000000, 0.9510565162951535312, 1.000000000000000000, 0.9510565162951535312, 1.000000000000000000, 0.9510565162951535312, 1.000000000000000000, 0.9510565162951535312, 1.000000000000000000, 0.9510565162951535312, 1.000000000000000000, 0.9510565162951535312, 1.000000000000000000, 0.9510565162951535312, 1.000000000000000000, 0.9510565162951535312, 1.000000000000000000, 0.9510565162951535312, 1.000000000000000000, 0.9510565162951535312, 1.000000000000000000, 0.9510565162951535312, 1.000000000000000000, 0.9510565162951535312, 1.000000000000000000, 0.9510565162951535312, 1.000000000000000000, 0.9510565162951535312, 1.000000000000000000, 0.9510565162951535312, 1.000000000000000000, 0.9510565162951535312, 1.000000000000000000, 0.9510565162951535312, 1.000000000000000000, 0.9510565162951535312, 1.000000000000000000, 0.9510565162951535312, 1.000000000000000000, 0.9510565162951535312, 1.000000000000000000, 0.9510565162951535312, 1.000000000000000000, 0.9510565162951535312, 1.000000000000000000, 0.9510565162951535312, 1.000000000000000000, 0.9510565162951535312, 1.000000000000000000, 0.9510565162951535312, 1.000000000000000000, 0.9510565162951535312, 1.000000000000000000, 0.9510565162951535312, 1.000000000000000000, 0.9510565162951535312, 1.000000000000000000, 0.9510565162951535312, 1.000000000000000000, 0.9510565162951535312, 1.000000000000000000, 0.9510565162951535312, 1.000000000000000000, 0.9510565162951535312, 1.000000000000000000, 0.9510565162951535312, 1.000000000000000000, 0.9510565162951535312, 1.000000000000000000, 0.9510565162951535312, 1.000000000000000000, 0.9510565162951535312, 1.000000000000000000, 0.9510565162951535312, 1.000000000000000000, 0.9510565162951535312, 1.000000000000000000, 0.9510565162951535312, 1.000000000000000000, 0.9510565162951535312, 1.000000000000000000, 0.9510565162951535312, 1.000000000000000000, 0.9510565162951535312, 1.000000000000000000, 0.9510565162951535312, 1.000000000000000000, 0.9510565162951535312, 1.000000000000000000, 0.9510565162951535312, 1.000000000000000000, 0.9510565162951535312, 1.000000000000000000, 0.9510565162951535312, 1.000000000000000000, 0.9510565162951535312, 1.000000000000000000, 0.9510565162951535312, 1.000000000000000000, 0.9510565162951535312, 1.000000000000000000, 0.9510565162951535312, 1.000000000000000000, 0.9510565162951535312, 1.000000000000000000, 0.9510565162951535312, 1.000000000000000000, 0.9510565162951535312, 1.000000000000000000, 0.9510565162951535312, 1.000000000000000000, 0.9510565162951535312, 1.000000000000000000, 0.9510565162951535312, 1.000000000000000000, 0.9510565162951535312, 1.000000000000000000, 0.9510565162951535312, 1.000000000000000000, 0.9510565162951535312, 1.000000000000000000, 0.9510565162951535312, 1.000000000000000000, 0.9510565162951535312, 1.000000000000000000, 0.9510565162951535312, 1.000000000000000000, 0.9510565162951535312, 1.000000000000000000, 0.9510565162951535312, 1.000000000000000000, 0.9510565162951535312, 1.000000000000000000, 0.9510565162951535312, 1.000000000000000000, 0.9510565162951535312, 1.000000000000000000, 0.9510565162951535312, 1.000000000000000000, 0.9510565162951535312, 1.000000000000000000, 0.9510565162951535312, 1.000000000000000000, 0.9510565162951535312, 1.000000000000000000, 0.9510565162951535312, 1.000000000000000000, 0.9510565162951535312, 1.000000000000000000),
 ( 1.000000000000000000, 0.9510565162951535312, 1.000000000000000000, 0.9510565162951535312, 1.000000000000000000, 0.9510565162951535312, 1.000000000000000000, 0.9510565162951535312, 1.000000000000000000, 0.9510565162951535312, 1.000000000000000000, 0.9510565162951535312, 1.000000000000000000, 0.9510565162951535312, 1.000000000000000000, 0.9510565162951535312, 1.000000000000000000, 0.9510565162951535312, 1.000000000000000000, 0.9510565162951535312, 1.000000000000000000, 0.9510565162951535312, 1.000000000000000000, 0.9510565162951535312, 1.000000000000000000, 0.9510565162951535312, 1.000000000000000000, 0.9510565162951535312, 1.000000000000000000, 0.9510565162951535312, 1.000000000000000000, 0.9510565162951535312, 1.000000000000000000, 0.9510565162951535312, 1.000000000000000000, 0.9510565162951535312, 1.000000000000000000, 0.9510565162951535312, 1.000000000000000000, 0.9510565162951535312, 1.000000000000000000, 0.9510565162951535312, 1.000000000000000000, 0.9510565162951535312, 1.000000000000000000, 0.9510565162951535312, 1.000000000000000000, 0.9510565162951535312, 1.000000000000000000, 0.9510565162951535312, 1.000000000000000000, 0.9510565162951535312, 1.000000000000000000, 0.9510565162951535312, 1.000000000000000000, 0.9510565162951535312, 1.000000000000000000, 0.9510565162951535312, 1.000000000000000000, 0.9510565162951535312, 1.000000000000000000, 0.9510565162951535312, 1.000000000000000000, 0.9510565162951535312, 1.000000000000000000, 0.9510565162951535312, 1.000000000000000000, 0.9510565162951535312, 1.000000000000000000, 0.9510565162951535312, 1.000000000000000000, 0.9510565162951535312, 1.000000000000000000, 0.9510565162951535312, 1.000000000000000000, 0.9510565162951535312, 1.000000000000000000, 0.9510565162951535312, 1.000000000000000000, 0.9510565162951535312, 1.000000000000000000, 0.9510565162951535312, 1.000000000000000000, 0.9510565162951535312, 1.000000000000000000, 0.9510565162951535312, 1.000000000000000000, 0.9510565162951535312, 1.000000000000000000, 0.9510565162951535312, 1.000000000000000000, 0.9510565162951535312, 1.000000000000000000, 0.9510565162951535312, 1.000000000000000000, 0.9510565162951535312, 1.000000000000000000, 0.9510565162951535312, 1.000000000000000000, 0.9510565162951535312, 1.000000000000000000, 0.9510565162951535312, 1.000000000000000000, 0.9510565162951535312, 1.000000000000000000, 0.9510565162951535312, 1.000000000000000000, 0.9510565162951535312, 1.000000000000000000, 0.9510565162951535312, 1.000000000000000000, 0.9510565162951535312, 1.000000000000000000, 0.9510565162951535312, 1.000000000000000000, 0.9510565162951535312, 1.000000000000000000, 0.9510565162951535312, 1.000000000000000000, 0.9510565162951535312, 1.000000000000000000, 0.9510565162951535312, 1.000000000000000000, 0.9510565162951535312, 1.000000000000000000, 0.9510565162951535312, 1.000000000000000000, 0.9510565162951535312, 1.000000000000000000, 0.9510565162951535312, 1.000000000000000000, 0.9510565162951535312, 1.000000000000000000, 0.9510565162951535312, 1.000000000000000000, 0.9510565162951535312, 1.000000000000000000, 0.9510565162951535312, 1.000000000000000000, 0.9510565162951535312, 1.000000000000000000, 0.9510565162951535312, 1.000000000000000000, 0.9510565162951535312, 1.000000000000000000, 0.9510565162951535312, 1.000000000000000000, 0.9510565162951535312, 1.000000000000000000, 0.9510565162951535312, 1.000000000000000000, 0.9510565162951535312, 1.000000000000000000, 0.9510565162951535312, 1.000000000000000000, 0.9510565162951535312, 1.000000000000000000, 0.9510565162951535312, 1.000000000000000000, 0.9510565162951535312, 1.000000000000000000, 0.9510565162951535312, 1.000000000000000000, 0.9510565162951535312, 1.000000000000000000, 0.9510565162951535312, 1.000000000000000000, 0.9510565162951535312, 1.000000000000000000, 0.9510565162951535312, 1.000000000000000000, 0.9510565162951535312, 1.000000000000000000, 0.9510565162951535312, 1.000000000000000000, 0.9510565162951535312, 1.000000000000000000, 0.9510565162951535312, 1.000000000000000000, 0.9510565162951535312, 1.000000000000000000, 0.9510565162951535312, 1.000000000000000000, 0.9510565162951535312, 1.000000000000000000, 0.9510565162951535312, 1.000000000000000000, 0.9510565162951535312, 1.000000000000000000, 0.9510565162951535312, 1.000000000000000000, 0.9510565162951535312, 1.000000000000000000, 0.9510565162951535312, 1.000000000000000000, 0.9510565162951535312, 1.000000000000000000, 0.9510565162951535312, 1.000000000000000000, 0.9510565162951535312, 1.000000000000000000, 0.9510565162951535312, 1.000000000000000000, 0.9510565162951535312, 1.000000000000000000, 0.9510565162951535312, 1.000000000000000000, 0.9510565162951535312, 1.000000000000000000, 0.9510565162951535312, 1.000000000000000000, 0.9510565162951535312, 1.000000000000000000, 0.9510565162951535312, 1.000000000000000000, 0.9510565162951535312, 1.000000000000000000, 0.9510565162951535312, 1.000000000000000000, 0.9510565162951535312, 1.000000000000000000, 0.9510565162951535312, 1.000000000000000000, 0.9510565162951535312, 1.000000000000000000, 0.9510565162951535312, 1.000000000000000000, 0.9510565162951535312, 1.000000000000000000, 0.9510565162951535312, 1.000000000000000000, 0.9510565162951535312, 1.000000000000000000, 0.9510565162951535312, 1.000000000000000000, 0.9510565162951535312, 1.000000000000000000, 0.9510565162951535312, 1.000000000000000000, 0.9510565162951535312, 1.000000000000000000, 0.9510565162951535312, 1.000000000000000000, 0.9510565162951535312, 1.000000000000000000, 0.9510565162951535312, 1.000000000000000000, 0.9510565162951535312, 1.000000000000000000, 0.9510565162951535312, 1.000000000000000000, 0.9510565162951535312, 1.000000000000000000, 0.9510565162951535312, 1.000000000000000000, 0.9510565162951535312, 1.000000000000000000, 0.9510565162951535312, 1.000000000000000000, 0.9510565162951535312, 1.000000000000000000, 0.9510565162951535312, 1.000000000000000000, 0.9510565162951535312, 1.000000000000000000, 0.9510565162951535312, 1.000000000000000000, 0.9510565162951535312, 1.000000000000000000, 0.9510565162951535312, 1.000000000000000000, 0.9510565162951535312, 1.000000000000000000, 0.9510565162951535312, 1.000000000000000000, 0.9510565162951535312, 1.000000000000000000, 0.9510565162951535312, 1.000000000000000000, 0.9510565162951535312, 1.000000000000000000, 0.9510565162951535312, 1.000000000000000000, 0.9510565162951535312, 1.000000000000000000, 0.9510565162951535312, 1.000000000000000000, 0.9510565162951535312, 1.000000000000000000, 0.9510565162951535312, 1.000000000000000000, 0.9510565162951535312, 1.000000000000000000, 0.9510565162951535312, 1.000000000000000000, 0.9510565162951535312, 1.000000000000000000, 0.9510565162951535312, 1.000000000000000000, 0.9510565162951535312, 1.000000000000000000, 0.9510565162951535312, 1.000000000000000000, 0.9510565162951535312, 1.000000000000000000, 0.9510565162951535312, 1.000000000000000000, 0.9510565162951535312, 1.000000000000000000, 0.9510565162951535312, 1.000000000000000000, 0.9510565162951535312, 1.000000000000000000, 0.9510565162951535312, 1.000000000000000000, 0.9510565162951535312, 1.000000000000000000, 0.9510565162951535312, 1.000000000000000000, 0.9510565162951535312, 1.000000000000000000, 0.9510565162951535312, 1.000000000000000000, 0.9510565162951535312, 1.000000000000000000, 0.9510565162951535312, 1.000000000000000000, 0.9510565162951535312, 1.000000000000000000, 0.9510565162951535312, 1.000000000000000000, 0.9510565162951535312, 1.000000000000000000, 0.9510565162951535312, 1.000000000000000000, 0.9510565162951535312, 1.000000000000000000, 0.9510565162951535312, 1.000000000000000000, 0.9510565162951535312, 1.000000000000000000) ) ) 
 REPRESENTATION_ITEM ( '' )  SURFACE ( )  );
#69418=( GEOMETRIC_REPRESENTATION_CONTEXT ( 3 ) GLOBAL_UNCERTAINTY_ASSIGNED_CONTEXT ( ( #54389 ) ) GLOBAL_UNIT_ASSIGNED_CONTEXT ( ( #3847, #46853, #24982 ) ) REPRESENTATION_CONTEXT ( 'NONE', 'WORKASPACE' ) );
#69424=DIRECTION ( 'NONE',  ( 0.000000000000000000, 0.000000000000000000, 1.000000000000000000 ) ) ;
#69427=EDGE_LOOP ( 'NONE', ( #33192, #29308, #40934, #63499 ) ) ;
#69434=CARTESIAN_POINT ( 'NONE',  ( 23.71231517720798010, 112.9999999999999858, 7.000000000000000000 ) ) ;
#69437=CARTESIAN_POINT ( 'NONE',  ( 71.50000000000000000, 35.92875272052971525, -10.00000000000000000 ) ) ;
#69438=FACE_OUTER_BOUND ( 'NONE', #20042, .T. ) ;
#69442=CARTESIAN_POINT ( 'NONE',  ( 2.607480562269076430, 138.9070736234661467, -8.025000000000000355 ) ) ;
#69449=ORIENTED_EDGE ( 'NONE', *, *, #37100, .F. ) ;
#69452=CARTESIAN_POINT ( 'NONE',  ( 71.50000000000000000, 14.49137674618942739, -7.500000000000000000 ) ) ;
#69455=DIRECTION ( 'NONE',  ( -0.000000000000000000, -0.000000000000000000, -1.000000000000000000 ) ) ;
#69457=DIRECTION ( 'NONE',  ( 1.000000000000000000, 0.000000000000000000, 0.000000000000000000 ) ) ;
#69459=ORIENTED_EDGE ( 'NONE', *, *, #21851, .T. ) ;
#69460=CARTESIAN_POINT ( 'NONE',  ( 0.000000000000000000, 116.9429263765338192, -8.025000000000000355 ) ) ;
#69464=( NAMED_UNIT ( * ) PLANE_ANGLE_UNIT ( ) SI_UNIT ( $, .RADIAN. ) );
#69467=CARTESIAN_POINT ( 'NONE',  ( 40.78947368421051323, 108.1536491499103363, 10.00000000000000000 ) ) ;
#69468=ORIENTED_EDGE ( 'NONE', *, *, #31429, .T. ) ;
#69471=DIRECTION ( 'NONE',  ( 0.000000000000000000, 1.000000000000000000, -0.000000000000000000 ) ) ;
#69473=CARTESIAN_POINT ( 'NONE',  ( -3.094860106618432471, 124.5949999999999704, -9.525000000000000355 ) ) ;
#69475=AXIS2_PLACEMENT_3D ( 'NONE', #22517, #17926, #66455 ) ;
#69476=CARTESIAN_POINT ( 'NONE',  ( -60.00000000000000000, -2.024042244987997205E-14, 10.50000000000000000 ) ) ;
#69480=( GEOMETRIC_REPRESENTATION_CONTEXT ( 3 ) GLOBAL_UNCERTAINTY_ASSIGNED_CONTEXT ( ( #52445 ) ) GLOBAL_UNIT_ASSIGNED_CONTEXT ( ( #68711, #27495, #48674 ) ) REPRESENTATION_CONTEXT ( 'NONE', 'WORKASPACE' ) );
#69481=CARTESIAN_POINT ( 'NONE',  ( -7.632228543268608334, 130.9570736234661581, 2.479861379858952830 ) ) ;
#69486=MECHANICAL_DESIGN_GEOMETRIC_PRESENTATION_REPRESENTATION('',(#14391),#28986);
#69489=CIRCLE ( 'NONE', #24518, 0.5000000000000004441 ) ;
#69490=EDGE_CURVE ( 'NONE', #41057, #64160, #56176, .T. ) ;
#69491=CARTESIAN_POINT ( 'NONE',  ( 44.83562443654410146, 9.945208145514939702, -3.584089800672845882 ) ) ;
#69492=LINE ( 'NONE', #68822, #52573 ) ;
#69493=SURFACE_SIDE_STYLE ('',( #10423 ) ) ;
#69497=CIRCLE ( 'NONE', #42569, 1.000000000000000888 ) ;
#69498=VECTOR ( 'NONE', #36105, 1000.000000000000000 ) ;
#69499=CARTESIAN_POINT ( 'NONE',  ( -41.49999999999997868, 10.49999999999998224, -3.000000000000000444 ) ) ;
#69501=FACE_OUTER_BOUND ( 'NONE', #60258, .T. ) ;
#69506=CARTESIAN_POINT ( 'NONE',  ( 20.71231517720797655, 149.4999999999999716, 10.00000000000000000 ) ) ;
#69511=CARTESIAN_POINT ( 'NONE',  ( -4.716976649647098618, 113.2570736234661553, 6.492361379858953008 ) ) ;
#69512=CIRCLE ( 'NONE', #57158, 0.5000000000000004441 ) ;
#69522=CARTESIAN_POINT ( 'NONE',  ( 8.102448949553183510, 122.1049999999999898, -5.886773742842746238 ) ) ;
#69523=SURFACE_STYLE_USAGE ( .BOTH. , #15407 ) ;
#69525=AXIS2_PLACEMENT_3D ( 'NONE', #10835, #555, #23133 ) ;
#69526=CIRCLE ( 'NONE', #39243, 0.5000000000000004441 ) ;
#69527=CARTESIAN_POINT ( 'NONE',  ( -74.99999999999998579, 50.00000000000000000, -11.50000000000001066 ) ) ;
#69529=ORIENTED_EDGE ( 'NONE', *, *, #6364, .T. ) ;
#69530=( GEOMETRIC_REPRESENTATION_CONTEXT ( 3 ) GLOBAL_UNCERTAINTY_ASSIGNED_CONTEXT ( ( #41723 ) ) GLOBAL_UNIT_ASSIGNED_CONTEXT ( ( #18517, #7951, #50870 ) ) REPRESENTATION_CONTEXT ( 'NONE', 'WORKASPACE' ) );
#69532=CARTESIAN_POINT ( 'NONE',  ( 45.50000000000000000, 10.69371294336137979, -4.000000000000000000 ) ) ;
#69533=FILL_AREA_STYLE_COLOUR ( '', #223 ) ;
#69534=ORIENTED_EDGE ( 'NONE', *, *, #58678, .T. ) ;
#69535=CARTESIAN_POINT ( 'NONE',  ( 7.632228543268607446, 152.0429263765338135, 2.479861379858954606 ) ) ;
#69540=CARTESIAN_POINT ( 'NONE',  ( 20.44134218812435932, 115.3860596766049440, -10.00000000000000000 ) ) ;
#69543=CARTESIAN_POINT ( 'NONE',  ( -45.50000000000000000, 1.797044900979284448E-15, -10.00000000000000000 ) ) ;
#69549=DIRECTION ( 'NONE',  ( 0.000000000000000000, 0.000000000000000000, 1.000000000000000000 ) ) ;
#69550=CARTESIAN_POINT ( 'NONE',  ( -8.586026971066690550, 153.5450349297233572, -0.1239747060112212501 ) ) ;
#69552=( GEOMETRIC_REPRESENTATION_CONTEXT ( 3 ) GLOBAL_UNCERTAINTY_ASSIGNED_CONTEXT ( ( #19916 ) ) GLOBAL_UNIT_ASSIGNED_CONTEXT ( ( #35677, #9290, #51857 ) ) REPRESENTATION_CONTEXT ( 'NONE', 'WORKASPACE' ) );
#69556=DIRECTION ( 'NONE',  ( 1.000000000000000000, -0.000000000000000000, 0.000000000000000000 ) ) ;
#69558=EDGE_LOOP ( 'NONE', ( #6060, #66281, #31886, #58275 ) ) ;
#69559=CARTESIAN_POINT ( 'NONE',  ( -57.99999999999997868, 50.00000000000000000, -6.500000000000000000 ) ) ;
#69561=EDGE_CURVE ( 'NONE', #31194, #36960, #47267, .T. ) ;
#69566=ORIENTED_EDGE ( 'NONE', *, *, #579, .T. ) ;
#69567=SURFACE_STYLE_USAGE ( .BOTH. , #36583 ) ;
#69570=FILL_AREA_STYLE_COLOUR ( '', #19186 ) ;
#69572=CARTESIAN_POINT ( 'NONE',  ( -41.49999999999998579, 106.9282032302754999, 3.500000000000000000 ) ) ;
#69574=CARTESIAN_POINT ( 'NONE',  ( -75.48275862068965125, 36.00832590023089352, -9.500000000000000000 ) ) ;
#69577=CARTESIAN_POINT ( 'NONE',  ( -5.598654528085806881, 134.8549999999999898, -7.705886871421374629 ) ) ;
#69580=EDGE_CURVE ( 'NONE', #38790, #2677, #14639, .T. ) ;
#69584=DIRECTION ( 'NONE',  ( 0.000000000000000000, 1.000000000000000000, -0.000000000000000000 ) ) ;
#69586=SURFACE_SIDE_STYLE ('',( #33000 ) ) ;
#69588=STYLED_ITEM ( 'NONE', ( #21903 ), #41836 ) ;
#69591=CIRCLE ( 'NONE', #12331, 8.499999999999992895 ) ;
#69593=CYLINDRICAL_SURFACE ( 'NONE', #43184, 8.999999999999994671 ) ;
#69596=DIRECTION ( 'NONE',  ( 0.000000000000000000, 0.000000000000000000, 1.000000000000000000 ) ) ;
#69605=SURFACE_SIDE_STYLE ('',( #5919 ) ) ;
#69611=CARTESIAN_POINT ( 'NONE',  ( -3.094860106618432471, 145.5949999999999136, -9.525000000000000355 ) ) ;
#69612=DIRECTION ( 'NONE',  ( -0.000000000000000000, 0.000000000000000000, 1.000000000000000000 ) ) ;
#69615=FILL_AREA_STYLE_COLOUR ( '', #41807 ) ;
#69619=CARTESIAN_POINT ( 'NONE',  ( -4.716976649647098618, 124.1429263765338220, 6.492361379858953008 ) ) ;
#69625=AXIS2_PLACEMENT_3D ( 'NONE', #8086, #34467, #24948 ) ;
#69631=SURFACE_STYLE_FILL_AREA ( #10216 ) ;
#69634=EDGE_CURVE ( 'NONE', #35727, #15634, #34862, .T. ) ;
#69636=DIRECTION ( 'NONE',  ( 1.000000000000000000, 0.000000000000000000, -0.000000000000000000 ) ) ;
#69637=SURFACE_SIDE_STYLE ('',( #32691 ) ) ;
#69644=EDGE_CURVE ( 'NONE', #54309, #6097, #25880, .T. ) ;
#69647=DIRECTION ( 'NONE',  ( 0.000000000000000000, 0.000000000000000000, 1.000000000000000000 ) ) ;
#69653=CARTESIAN_POINT ( 'NONE',  ( -74.99999999999998579, 50.00000000000000000, -12.00000000000000000 ) ) ;
#69657=EDGE_CURVE ( 'NONE', #66646, #27816, #21394, .T. ) ;
#69660=PRESENTATION_STYLE_ASSIGNMENT (( #59430 ) ) ;
#69663=CARTESIAN_POINT ( 'NONE',  ( 0.000000000000000000, 157.4449999999999932, -9.525000000000000355 ) ) ;
#69665=CARTESIAN_POINT ( 'NONE',  ( -7.632228543268607446, 112.6570736234661609, -2.479861379858953718 ) ) ;
#69667=AXIS2_PLACEMENT_3D ( 'NONE', #13661, #15093, #36196 ) ;
#69668=DIRECTION ( 'NONE',  ( 0.000000000000000000, 0.000000000000000000, 1.000000000000000000 ) ) ;
#69669=DIRECTION ( 'NONE',  ( 0.000000000000000000, 0.000000000000000000, -1.000000000000000000 ) ) ;
#69671=VERTEX_POINT ( 'NONE', #5443 ) ;
#69675=DIRECTION ( 'NONE',  ( -1.000000000000000000, 0.000000000000000000, -0.000000000000000000 ) ) ;
#69676=ADVANCED_FACE ( 'NONE', ( #6167 ), #16750, .T. ) ;
#69678=DIRECTION ( 'NONE',  ( 0.000000000000000000, 0.000000000000000000, 1.000000000000000000 ) ) ;
#69681=VERTEX_POINT ( 'NONE', #122 ) ;
#69682=EDGE_LOOP ( 'NONE', ( #16282, #23325, #13619, #17685 ) ) ;
#69687=CARTESIAN_POINT ( 'NONE',  ( -45.00000000000000711, 8.062885798612171584, 5.903555993538923019 ) ) ;
ENDSEC;
END-ISO-10303-21;
